ISO-10303-21;
HEADER;
FILE_DESCRIPTION (('STEP AP214'),
    '1' );
FILE_NAME ('Back Cover.step',
    '2026-10-24T11:32:06',
    ( '' ),
    ( '' ),
    'SwSTEP 2.0',
    'SolidWorks 2025',
    '' );
FILE_SCHEMA (( 'AUTOMOTIVE_DESIGN' ));
ENDSEC;

DATA;
#1=ORIENTED_EDGE ( 'NONE', *, *, #41545, .F. ) ;
#2=DIRECTION ( 'NONE',  ( -0.000000000000000000, 1.000000000000000000, -0.000000000000000000 ) ) ;
#8=ORIENTED_EDGE ( 'NONE', *, *, #4272, .T. ) ;
#9=ORIENTED_EDGE ( 'NONE', *, *, #40098, .F. ) ;
#11=EDGE_CURVE ( 'NONE', #30195, #20299, #27750, .T. ) ;
#12=EDGE_LOOP ( 'NONE', ( #15734, #18361, #15608, #13795, #3369 ) ) ;
#13=LINE ( 'NONE', #35645, #41620 ) ;
#14=AXIS2_PLACEMENT_3D ( 'NONE', #39527, #281, #16034 ) ;
#16=VECTOR ( 'NONE', #2889, 39.37007874015748143 ) ;
#17=DIRECTION ( 'NONE',  ( -1.000000000000000000, 0.000000000000000000, -0.000000000000000000 ) ) ;
#19=ORIENTED_EDGE ( 'NONE', *, *, #43886, .F. ) ;
#20=ORIENTED_EDGE ( 'NONE', *, *, #36805, .T. ) ;
#21=CARTESIAN_POINT ( 'NONE',  ( -1.985260859929297572, 0.000000000000000000, 0.9448818897637749625 ) ) ;
#22=PLANE ( 'NONE',  #45699 ) ;
#23=AXIS2_PLACEMENT_3D ( 'NONE', #45636, #18051, #42046 ) ;
#24=VERTEX_POINT ( 'NONE', #23123 ) ;
#25=CARTESIAN_POINT ( 'NONE',  ( 0.2727639067037610499, 0.000000000000000000, 1.417322834645662777 ) ) ;
#26=DIRECTION ( 'NONE',  ( 1.000000000000000000, -0.000000000000000000, 0.000000000000000000 ) ) ;
#27=EDGE_CURVE ( 'NONE', #10700, #41467, #27241, .T. ) ;
#29=DIRECTION ( 'NONE',  ( 1.000000000000000000, 0.000000000000000000, 0.000000000000000000 ) ) ;
#30=CARTESIAN_POINT ( 'NONE',  ( -1.091055626815042645, 3.346456692913386100, 1.889763779527550147 ) ) ;
#31=ORIENTED_EDGE ( 'NONE', *, *, #29718, .F. ) ;
#34=EDGE_CURVE ( 'NONE', #42119, #2129, #11002, .T. ) ;
#38=CARTESIAN_POINT ( 'NONE',  ( -0.3486774197067339376, 0.000000000000000000, 2.204724409448808764 ) ) ;
#39=FACE_OUTER_BOUND ( 'NONE', #43225, .T. ) ;
#43=FACE_OUTER_BOUND ( 'NONE', #749, .T. ) ;
#44=ORIENTED_EDGE ( 'NONE', *, *, #47362, .F. ) ;
#46=ORIENTED_EDGE ( 'NONE', *, *, #11822, .F. ) ;
#49=PLANE ( 'NONE',  #39583 ) ;
#50=DIRECTION ( 'NONE',  ( 1.734723475976806848E-16, -0.000000000000000000, 1.000000000000000000 ) ) ;
#51=VECTOR ( 'NONE', #38671, 39.37007874015748143 ) ;
#52=ORIENTED_EDGE ( 'NONE', *, *, #36287, .T. ) ;
#54=VERTEX_POINT ( 'NONE', #23369 ) ;
#55=ORIENTED_EDGE ( 'NONE', *, *, #40975, .F. ) ;
#57=PLANE ( 'NONE',  #9017 ) ;
#58=VERTEX_POINT ( 'NONE', #22875 ) ;
#59=EDGE_LOOP ( 'NONE', ( #42044, #32903, #33887, #36079 ) ) ;
#60=CARTESIAN_POINT ( 'NONE',  ( 1.091055626815043311, 3.346456692913386100, 1.801691980386208591 ) ) ;
#65=VERTEX_POINT ( 'NONE', #11508 ) ;
#67=LINE ( 'NONE', #23560, #12596 ) ;
#68=DIRECTION ( 'NONE',  ( 1.734723475976806848E-16, -0.000000000000000000, 1.000000000000000000 ) ) ;
#69=ORIENTED_EDGE ( 'NONE', *, *, #18487, .T. ) ;
#72=EDGE_CURVE ( 'NONE', #49919, #13698, #39123, .T. ) ;
#73=ORIENTED_EDGE ( 'NONE', *, *, #20191, .T. ) ;
#74=EDGE_CURVE ( 'NONE', #40300, #35551, #37050, .T. ) ;
#75=LINE ( 'NONE', #35456, #37348 ) ;
#77=ORIENTED_EDGE ( 'NONE', *, *, #24929, .F. ) ;
#78=LINE ( 'NONE', #47286, #4826 ) ;
#79=EDGE_CURVE ( 'NONE', #50716, #12064, #21041, .T. ) ;
#81=CARTESIAN_POINT ( 'NONE',  ( -0.8942052331142547050, 3.346456692913386100, 0.3149606299212580063 ) ) ;
#84=ORIENTED_EDGE ( 'NONE', *, *, #20132, .T. ) ;
#85=ORIENTED_EDGE ( 'NONE', *, *, #1655, .T. ) ;
#86=ORIENTED_EDGE ( 'NONE', *, *, #35024, .F. ) ;
#87=CARTESIAN_POINT ( 'NONE',  ( -2.454875160333845674, 0.000000000000000000, -0.3543307086614173040 ) ) ;
#89=VECTOR ( 'NONE', #24437, 39.37007874015748143 ) ;
#91=ADVANCED_FACE ( 'NONE', ( #40920 ), #12786, .F. ) ;
#96=EDGE_CURVE ( 'NONE', #18423, #30154, #5544, .T. ) ;
#97=VECTOR ( 'NONE', #41859, 39.37007874015748143 ) ;
#98=CARTESIAN_POINT ( 'NONE',  ( 0.8182917201112819283, 0.000000000000000000, -0.6692913385826764205 ) ) ;
#99=EDGE_LOOP ( 'NONE', ( #34506, #24501, #26752, #36610 ) ) ;
#101=LINE ( 'NONE', #15846, #7552 ) ;
#102=CARTESIAN_POINT ( 'NONE',  ( -0.8182917201112819283, 3.267716535433071279, -1.417322834645664331 ) ) ;
#104=EDGE_CURVE ( 'NONE', #46852, #34665, #24146, .T. ) ;
#105=ORIENTED_EDGE ( 'NONE', *, *, #7025, .F. ) ;
#106=PLANE ( 'NONE',  #20146 ) ;
#107=CARTESIAN_POINT ( 'NONE',  ( 1.636583440222563857, 3.267716535433071279, -2.839019714148966584E-16 ) ) ;
#110=LINE ( 'NONE', #16120, #44470 ) ;
#114=FACE_OUTER_BOUND ( 'NONE', #41587, .T. ) ;
#117=DIRECTION ( 'NONE',  ( -1.000000000000000000, 0.000000000000000000, 1.734723475976806848E-16 ) ) ;
#118=ORIENTED_EDGE ( 'NONE', *, *, #20637, .F. ) ;
#119=ORIENTED_EDGE ( 'NONE', *, *, #43992, .F. ) ;
#120=FACE_OUTER_BOUND ( 'NONE', #11448, .T. ) ;
#121=DIRECTION ( 'NONE',  ( -1.000000000000000000, -0.000000000000000000, -0.000000000000000000 ) ) ;
#122=VERTEX_POINT ( 'NONE', #36283 ) ;
#123=DIRECTION ( 'NONE',  ( 1.000000000000000000, 0.000000000000000000, -3.469446951953613696E-16 ) ) ;
#124=LINE ( 'NONE', #20773, #45818 ) ;
#126=VECTOR ( 'NONE', #40753, 39.37007874015748143 ) ;
#128=AXIS2_PLACEMENT_3D ( 'NONE', #50687, #394, #43496 ) ;
#129=VERTEX_POINT ( 'NONE', #32937 ) ;
#130=ORIENTED_EDGE ( 'NONE', *, *, #3262, .F. ) ;
#132=CARTESIAN_POINT ( 'NONE',  ( 0.2727639067037604392, 3.267716535433071279, -4.731699523581607276E-17 ) ) ;
#133=DIRECTION ( 'NONE',  ( -0.000000000000000000, 1.000000000000000000, -0.000000000000000000 ) ) ;
#134=CIRCLE ( 'NONE', #18276, 2.106299212598425008 ) ;
#135=ORIENTED_EDGE ( 'NONE', *, *, #12667, .T. ) ;
#136=DIRECTION ( 'NONE',  ( -1.000000000000000000, 0.000000000000000000, 0.000000000000000000 ) ) ;
#139=DIRECTION ( 'NONE',  ( 1.000000000000000000, -0.000000000000000000, 0.000000000000000000 ) ) ;
#140=EDGE_CURVE ( 'NONE', #9076, #17493, #4524, .T. ) ;
#142=EDGE_CURVE ( 'NONE', #28374, #48689, #28779, .T. ) ;
#144=ORIENTED_EDGE ( 'NONE', *, *, #45478, .T. ) ;
#147=ORIENTED_EDGE ( 'NONE', *, *, #31440, .T. ) ;
#148=CARTESIAN_POINT ( 'NONE',  ( -1.439733046521776583, 0.000000000000000000, -0.6299212598425177889 ) ) ;
#152=CARTESIAN_POINT ( 'NONE',  ( -0.3486774197067339376, 0.000000000000000000, 0.3149606299212577287 ) ) ;
#153=CARTESIAN_POINT ( 'NONE',  ( 1.363819533518803251, 3.346456692913386100, -0.4724409448818889246 ) ) ;
#154=ORIENTED_EDGE ( 'NONE', *, *, #33358, .F. ) ;
#155=FACE_OUTER_BOUND ( 'NONE', #42021, .T. ) ;
#156=CARTESIAN_POINT ( 'NONE',  ( 1.560669927219590747, 0.000000000000000000, 0.1574803149606283648 ) ) ;
#158=ORIENTED_EDGE ( 'NONE', *, *, #45905, .F. ) ;
#159=VECTOR ( 'NONE', #591, 39.37007874015748143 ) ;
#160=DIRECTION ( 'NONE',  ( 1.000000000000000000, 0.000000000000000000, -3.469446951953613696E-16 ) ) ;
#163=PLANE ( 'NONE',  #50112 ) ;
#164=EDGE_CURVE ( 'NONE', #49397, #27417, #48360, .T. ) ;
#165=CARTESIAN_POINT ( 'NONE',  ( -0.8942052331142547050, 0.000000000000000000, 1.574803149606291974 ) ) ;
#168=VECTOR ( 'NONE', #49245, 39.37007874015748143 ) ;
#169=VECTOR ( 'NONE', #37058, 39.37007874015748143 ) ;
#171=ORIENTED_EDGE ( 'NONE', *, *, #24690, .T. ) ;
#172=CARTESIAN_POINT ( 'NONE',  ( -1.636583440222564301, 0.000000000000000000, -1.259842519685034468 ) ) ;
#173=ADVANCED_FACE ( 'NONE', ( #43745 ), #44519, .F. ) ;
#175=VECTOR ( 'NONE', #24706, 39.37007874015748143 ) ;
#176=DIRECTION ( 'NONE',  ( -3.469446951953613696E-16, 0.000000000000000000, -1.000000000000000000 ) ) ;
#177=CARTESIAN_POINT ( 'NONE',  ( 1.363819533518803029, 0.000000000000000000, -1.102362204724405714 ) ) ;
#178=ORIENTED_EDGE ( 'NONE', *, *, #35535, .T. ) ;
#179=EDGE_CURVE ( 'NONE', #37571, #48901, #4780, .T. ) ;
#180=VERTEX_POINT ( 'NONE', #28260 ) ;
#181=ORIENTED_EDGE ( 'NONE', *, *, #30395, .F. ) ;
#182=DIRECTION ( 'NONE',  ( -1.000000000000000000, 0.000000000000000000, 0.000000000000000000 ) ) ;
#183=VERTEX_POINT ( 'NONE', #20529 ) ;
#186=FACE_OUTER_BOUND ( 'NONE', #12865, .T. ) ;
#187=VERTEX_POINT ( 'NONE', #32677 ) ;
#192=CARTESIAN_POINT ( 'NONE',  ( 1.560669927219590303, 3.186757942779276043, -1.929133858267710666 ) ) ;
#193=ORIENTED_EDGE ( 'NONE', *, *, #27839, .T. ) ;
#194=ORIENTED_EDGE ( 'NONE', *, *, #36175, .F. ) ;
#195=LINE ( 'NONE', #42802, #49556 ) ;
#197=EDGE_CURVE ( 'NONE', #41904, #49094, #20264, .T. ) ;
#199=CARTESIAN_POINT ( 'NONE',  ( 0.7423782071083092626, 3.346456692913386100, 1.259842519685033357 ) ) ;
#201=ORIENTED_EDGE ( 'NONE', *, *, #10126, .T. ) ;
#202=ORIENTED_EDGE ( 'NONE', *, *, #12575, .F. ) ;
#203=ADVANCED_FACE ( 'NONE', ( #47849 ), #44006, .F. ) ;
#207=AXIS2_PLACEMENT_3D ( 'NONE', #10792, #6422, #49732 ) ;
#208=CARTESIAN_POINT ( 'NONE',  ( 0.4696143004045476577, 3.346456692913386100, -2.053280005709960054 ) ) ;
#210=DIRECTION ( 'NONE',  ( 1.734723475976806848E-16, -0.000000000000000000, 1.000000000000000000 ) ) ;
#212=VECTOR ( 'NONE', #8799, 39.37007874015748143 ) ;
#213=LINE ( 'NONE', #20347, #9362 ) ;
#216=VERTEX_POINT ( 'NONE', #10437 ) ;
#217=CARTESIAN_POINT ( 'NONE',  ( -2.182111253630085734, 3.267716535433070391, -1.099868863272876141 ) ) ;
#218=DIRECTION ( 'NONE',  ( -1.000000000000000000, 0.000000000000000000, -0.000000000000000000 ) ) ;
#220=CARTESIAN_POINT ( 'NONE',  ( -0.8942052331142547050, 3.346456692913386100, 0.3149606299212580063 ) ) ;
#223=ORIENTED_EDGE ( 'NONE', *, *, #26199, .T. ) ;
#232=CARTESIAN_POINT ( 'NONE',  ( -0.5455278134075214336, 3.346456692913386100, 2.095509194042718182 ) ) ;
#233=ORIENTED_EDGE ( 'NONE', *, *, #15254, .F. ) ;
#234=ADVANCED_FACE ( 'NONE', ( #37814 ), #18182, .F. ) ;
#236=VECTOR ( 'NONE', #4525, 39.37007874015748143 ) ;
#237=CARTESIAN_POINT ( 'NONE',  ( 1.091055626815042645, 3.346456692913386100, 1.062992125984246083 ) ) ;
#241=VECTOR ( 'NONE', #21691, 39.37007874015748143 ) ;
#242=VECTOR ( 'NONE', #7716, 39.37007874015748143 ) ;
#243=DIRECTION ( 'NONE',  ( 1.000000000000000000, 0.000000000000000000, 0.000000000000000000 ) ) ;
#245=EDGE_LOOP ( 'NONE', ( #3861, #29192, #10688, #26365 ) ) ;
#246=AXIS2_PLACEMENT_3D ( 'NONE', #45801, #41451, #45296 ) ;
#247=LINE ( 'NONE', #16001, #16461 ) ;
#248=ORIENTED_EDGE ( 'NONE', *, *, #20841, .F. ) ;
#249=ORIENTED_EDGE ( 'NONE', *, *, #14890, .F. ) ;
#251=CARTESIAN_POINT ( 'NONE',  ( -0.3486774197067339376, 3.267716535433071279, -8.878505979408855953E-16 ) ) ;
#252=PLANE ( 'NONE',  #20266 ) ;
#253=ADVANCED_FACE ( 'NONE', ( #6050 ), #49625, .F. ) ;
#255=EDGE_CURVE ( 'NONE', #10831, #25675, #41179, .T. ) ;
#256=DIRECTION ( 'NONE',  ( -0.000000000000000000, 1.000000000000000000, -0.000000000000000000 ) ) ;
#259=EDGE_CURVE ( 'NONE', #12398, #42413, #45266, .T. ) ;
#261=CARTESIAN_POINT ( 'NONE',  ( -1.909347346926324462, 3.267716535433071279, 3.312189666507127188E-16 ) ) ;
#262=EDGE_CURVE ( 'NONE', #25798, #30055, #28914, .T. ) ;
#263=EDGE_CURVE ( 'NONE', #7287, #17531, #25669, .T. ) ;
#264=ORIENTED_EDGE ( 'NONE', *, *, #41294, .T. ) ;
#265=ORIENTED_EDGE ( 'NONE', *, *, #24485, .F. ) ;
#267=ORIENTED_EDGE ( 'NONE', *, *, #44788, .T. ) ;
#268=CARTESIAN_POINT ( 'NONE',  ( 0.000000000000000000, 3.346456692913386100, 0.000000000000000000 ) ) ;
#271=CARTESIAN_POINT ( 'NONE',  ( -1.909347346926324906, 3.346456692913386100, 1.417322834645662333 ) ) ;
#272=VERTEX_POINT ( 'NONE', #25412 ) ;
#273=ORIENTED_EDGE ( 'NONE', *, *, #29883, .F. ) ;
#276=CARTESIAN_POINT ( 'NONE',  ( 0.2727639067037604947, 0.000000000000000000, -1.102362204724405714 ) ) ;
#278=ORIENTED_EDGE ( 'NONE', *, *, #17127, .T. ) ;
#279=CARTESIAN_POINT ( 'NONE',  ( -0.8942052331142547050, 3.267716535433071279, 0.6299212598425164567 ) ) ;
#281=DIRECTION ( 'NONE',  ( 1.000000000000000000, 0.000000000000000000, -3.469446951953613696E-16 ) ) ;
#282=AXIS2_PLACEMENT_3D ( 'NONE', #22647, #6901, #3030 ) ;
#283=CARTESIAN_POINT ( 'NONE',  ( 1.636583440222563635, 3.346456692913386100, -1.259842519685035800 ) ) ;
#284=CARTESIAN_POINT ( 'NONE',  ( -1.363819533518803473, 3.346456692913386100, -1.102362204724405270 ) ) ;
#285=VECTOR ( 'NONE', #30019, 39.37007874015748143 ) ;
#287=LINE ( 'NONE', #43396, #2001 ) ;
#290=ORIENTED_EDGE ( 'NONE', *, *, #42530, .T. ) ;
#291=ORIENTED_EDGE ( 'NONE', *, *, #20423, .T. ) ;
#292=DIRECTION ( 'NONE',  ( 0.000000000000000000, 0.000000000000000000, -1.000000000000000000 ) ) ;
#293=DIRECTION ( 'NONE',  ( 1.000000000000000000, -0.000000000000000000, 0.000000000000000000 ) ) ;
#294=CARTESIAN_POINT ( 'NONE',  ( 1.560669927219591191, 3.267716535433071279, -5.414661521997678257E-16 ) ) ;
#295=EDGE_CURVE ( 'NONE', #22386, #50303, #6570, .T. ) ;
#296=ORIENTED_EDGE ( 'NONE', *, *, #48148, .F. ) ;
#298=EDGE_CURVE ( 'NONE', #1486, #10637, #29549, .T. ) ;
#300=DIRECTION ( 'NONE',  ( -1.000000000000000000, 0.000000000000000000, -0.000000000000000000 ) ) ;
#302=DIRECTION ( 'NONE',  ( 1.000000000000000000, -0.000000000000000000, 0.000000000000000000 ) ) ;
#305=DIRECTION ( 'NONE',  ( 0.000000000000000000, 0.000000000000000000, -1.000000000000000000 ) ) ;
#306=DIRECTION ( 'NONE',  ( 1.734723475976806848E-16, 0.000000000000000000, 1.000000000000000000 ) ) ;
#308=ORIENTED_EDGE ( 'NONE', *, *, #49146, .F. ) ;
#309=AXIS2_PLACEMENT_3D ( 'NONE', #1939, #49889, #41689 ) ;
#310=ORIENTED_EDGE ( 'NONE', *, *, #37633, .T. ) ;
#313=FACE_OUTER_BOUND ( 'NONE', #47009, .T. ) ;
#314=AXIS2_PLACEMENT_3D ( 'NONE', #49649, #33963, #9444 ) ;
#315=ORIENTED_EDGE ( 'NONE', *, *, #38294, .T. ) ;
#317=AXIS2_PLACEMENT_3D ( 'NONE', #5899, #45371, #26286 ) ;
#318=PLANE ( 'NONE',  #29771 ) ;
#319=CARTESIAN_POINT ( 'NONE',  ( -0.8182917201112819283, 3.346456692913386100, -1.102362204724405492 ) ) ;
#322=AXIS2_PLACEMENT_3D ( 'NONE', #49852, #14794, #14539 ) ;
#323=AXIS2_PLACEMENT_3D ( 'NONE', #40043, #1313, #12678 ) ;
#325=EDGE_CURVE ( 'NONE', #49197, #2752, #37560, .T. ) ;
#326=FACE_OUTER_BOUND ( 'NONE', #46204, .T. ) ;
#327=LINE ( 'NONE', #24338, #15105 ) ;
#328=CARTESIAN_POINT ( 'NONE',  ( 0.5455278134075211005, 3.267716535433071279, -9.463399047163218249E-17 ) ) ;
#329=VERTEX_POINT ( 'NONE', #17676 ) ;
#330=DIRECTION ( 'NONE',  ( -1.000000000000000000, 0.000000000000000000, 1.734723475976806848E-16 ) ) ;
#331=CARTESIAN_POINT ( 'NONE',  ( -1.636583440222563635, 0.000000000000000000, -4.780733988912460139E-16 ) ) ;
#332=VECTOR ( 'NONE', #35923, 39.37007874015748143 ) ;
#334=EDGE_CURVE ( 'NONE', #5779, #3769, #41676, .T. ) ;
#336=EDGE_LOOP ( 'NONE', ( #16852, #9231, #42778, #18516 ) ) ;
#337=VERTEX_POINT ( 'NONE', #19683 ) ;
#338=DIRECTION ( 'NONE',  ( -1.000000000000000000, 0.000000000000000000, 0.000000000000000000 ) ) ;
#341=LINE ( 'NONE', #32361, #28589 ) ;
#342=DIRECTION ( 'NONE',  ( -3.469446951953613696E-16, 0.000000000000000000, -1.000000000000000000 ) ) ;
#345=ORIENTED_EDGE ( 'NONE', *, *, #38896, .F. ) ;
#346=LINE ( 'NONE', #44226, #45050 ) ;
#349=DIRECTION ( 'NONE',  ( 1.000000000000000000, 0.000000000000000000, 0.000000000000000000 ) ) ;
#351=VERTEX_POINT ( 'NONE', #7572 ) ;
#352=VECTOR ( 'NONE', #28731, 39.37007874015748143 ) ;
#357=VECTOR ( 'NONE', #24500, 39.37007874015748143 ) ;
#359=DIRECTION ( 'NONE',  ( 0.000000000000000000, 0.000000000000000000, -1.000000000000000000 ) ) ;
#362=DIRECTION ( 'NONE',  ( 1.000000000000000000, 0.000000000000000000, 0.000000000000000000 ) ) ;
#364=CARTESIAN_POINT ( 'NONE',  ( 1.015142113812069091, 0.000000000000000000, -2.047244094488181343 ) ) ;
#365=LINE ( 'NONE', #8117, #25832 ) ;
#366=DIRECTION ( 'NONE',  ( -1.000000000000000000, 0.000000000000000000, 1.734723475976806848E-16 ) ) ;
#369=EDGE_CURVE ( 'NONE', #14478, #12822, #50374, .T. ) ;
#370=VERTEX_POINT ( 'NONE', #15572 ) ;
#371=CARTESIAN_POINT ( 'NONE',  ( 1.091055626815042423, 3.346456692913386100, -1.456692913385822630 ) ) ;
#373=VERTEX_POINT ( 'NONE', #11444 ) ;
#374=DIRECTION ( 'NONE',  ( -3.469446951953613696E-16, 0.000000000000000000, -1.000000000000000000 ) ) ;
#376=PLANE ( 'NONE',  #43282 ) ;
#377=DIRECTION ( 'NONE',  ( -1.000000000000000000, 0.000000000000000000, -0.000000000000000000 ) ) ;
#379=ORIENTED_EDGE ( 'NONE', *, *, #9138, .F. ) ;
#381=LINE ( 'NONE', #27740, #4269 ) ;
#382=CARTESIAN_POINT ( 'NONE',  ( -2.009899395340762673, 3.267716535433071279, 0.6299212598425164567 ) ) ;
#383=VERTEX_POINT ( 'NONE', #23307 ) ;
#385=CARTESIAN_POINT ( 'NONE',  ( 0.4696143004045478797, 0.000000000000000000, 0.2755905511810994302 ) ) ;
#387=DIRECTION ( 'NONE',  ( 0.000000000000000000, 0.000000000000000000, 1.000000000000000000 ) ) ;
#388=VERTEX_POINT ( 'NONE', #31573 ) ;
#391=ORIENTED_EDGE ( 'NONE', *, *, #26902, .T. ) ;
#392=CARTESIAN_POINT ( 'NONE',  ( 0.000000000000000000, 3.267716535433071279, -0.4724409448818889246 ) ) ;
#393=CARTESIAN_POINT ( 'NONE',  ( 0.8182917201112824834, 0.000000000000000000, 1.732283464566921172 ) ) ;
#394=DIRECTION ( 'NONE',  ( 1.000000000000000000, 0.000000000000000000, -3.469446951953613696E-16 ) ) ;
#395=FACE_BOUND ( 'NONE', #50997, .T. ) ;
#396=CIRCLE ( 'NONE', #47377, 2.165354330708661568 ) ;
#400=VECTOR ( 'NONE', #34966, 39.37007874015748143 ) ;
#401=EDGE_LOOP ( 'NONE', ( #7876, #18097, #6204, #3333 ) ) ;
#402=ORIENTED_EDGE ( 'NONE', *, *, #35422, .F. ) ;
#403=PLANE ( 'NONE',  #14331 ) ;
#404=VECTOR ( 'NONE', #48657, 39.37007874015748143 ) ;
#405=ORIENTED_EDGE ( 'NONE', *, *, #35866, .F. ) ;
#406=ORIENTED_EDGE ( 'NONE', *, *, #2601, .T. ) ;
#408=ORIENTED_EDGE ( 'NONE', *, *, #14418, .T. ) ;
#409=VECTOR ( 'NONE', #23768, 39.37007874015748143 ) ;
#410=DIRECTION ( 'NONE',  ( 1.734723475976806848E-16, 0.000000000000000000, 1.000000000000000000 ) ) ;
#412=FACE_OUTER_BOUND ( 'NONE', #31135, .T. ) ;
#414=DIRECTION ( 'NONE',  ( 1.000000000000000000, 0.000000000000000000, 0.000000000000000000 ) ) ;
#417=EDGE_LOOP ( 'NONE', ( #37334, #24980, #11182, #19337 ) ) ;
#418=PLANE ( 'NONE',  #6868 ) ;
#421=VERTEX_POINT ( 'NONE', #7821 ) ;
#422=LINE ( 'NONE', #4054, #41329 ) ;
#424=ORIENTED_EDGE ( 'NONE', *, *, #34956, .T. ) ;
#425=CARTESIAN_POINT ( 'NONE',  ( -1.439733046521776139, 3.346456692913386100, 1.259842519685033357 ) ) ;
#429=AXIS2_PLACEMENT_3D ( 'NONE', #42019, #14139, #38655 ) ;
#430=EDGE_CURVE ( 'NONE', #5602, #43368, #11459, .T. ) ;
#434=EDGE_LOOP ( 'NONE', ( #15887, #17893, #8935, #4099 ) ) ;
#435=DIRECTION ( 'NONE',  ( -1.000000000000000000, -0.000000000000000000, -0.000000000000000000 ) ) ;
#439=LINE ( 'NONE', #16192, #44064 ) ;
#441=EDGE_CURVE ( 'NONE', #1296, #33691, #46526, .T. ) ;
#442=ORIENTED_EDGE ( 'NONE', *, *, #24074, .F. ) ;
#443=EDGE_CURVE ( 'NONE', #43528, #17266, #27682, .T. ) ;
#445=ORIENTED_EDGE ( 'NONE', *, *, #47952, .T. ) ;
#446=ORIENTED_EDGE ( 'NONE', *, *, #13837, .F. ) ;
#447=CARTESIAN_POINT ( 'NONE',  ( 1.091055626815042423, 3.267716535433071279, -1.889763779527552368 ) ) ;
#448=VERTEX_POINT ( 'NONE', #34443 ) ;
#451=LINE ( 'NONE', #47138, #47795 ) ;
#452=EDGE_CURVE ( 'NONE', #19346, #17026, #50131, .T. ) ;
#453=ORIENTED_EDGE ( 'NONE', *, *, #12794, .F. ) ;
#454=LINE ( 'NONE', #12073, #27390 ) ;
#456=VERTEX_POINT ( 'NONE', #30563 ) ;
#457=EDGE_CURVE ( 'NONE', #27808, #46201, #7070, .T. ) ;
#460=LINE ( 'NONE', #199, #37825 ) ;
#462=EDGE_CURVE ( 'NONE', #25931, #40389, #3190, .T. ) ;
#464=ORIENTED_EDGE ( 'NONE', *, *, #28101, .F. ) ;
#466=AXIS2_PLACEMENT_3D ( 'NONE', #49592, #32189, #4812 ) ;
#467=LINE ( 'NONE', #17436, #12190 ) ;
#468=VECTOR ( 'NONE', #49916, 39.37007874015748143 ) ;
#469=ORIENTED_EDGE ( 'NONE', *, *, #20201, .F. ) ;
#470=CARTESIAN_POINT ( 'NONE',  ( -0.3486774197067340486, 3.346456692913386100, 0.1181102362204703021 ) ) ;
#471=ADVANCED_FACE ( 'NONE', ( #7325 ), #23067, .F. ) ;
#472=VERTEX_POINT ( 'NONE', #15316 ) ;
#475=VECTOR ( 'NONE', #44694, 39.37007874015748143 ) ;
#476=CARTESIAN_POINT ( 'NONE',  ( 0.4696143004045478797, 3.267716535433071279, -1.629301903132387260E-16 ) ) ;
#477=ORIENTED_EDGE ( 'NONE', *, *, #24701, .F. ) ;
#478=ORIENTED_EDGE ( 'NONE', *, *, #43095, .F. ) ;
#481=DIRECTION ( 'NONE',  ( -0.000000000000000000, 1.000000000000000000, -0.000000000000000000 ) ) ;
#483=EDGE_CURVE ( 'NONE', #34071, #17239, #28961, .T. ) ;
#484=CARTESIAN_POINT ( 'NONE',  ( 0.5455278134075214336, 3.267716535433071279, -9.463399047163224412E-17 ) ) ;
#488=ORIENTED_EDGE ( 'NONE', *, *, #2043, .T. ) ;
#489=CARTESIAN_POINT ( 'NONE',  ( 0.7423782071083085965, 3.267716535433071279, -2.575641807848709701E-16 ) ) ;
#490=ORIENTED_EDGE ( 'NONE', *, *, #3167, .F. ) ;
#491=DIRECTION ( 'NONE',  ( -1.000000000000000000, 0.000000000000000000, 1.734723475976806848E-16 ) ) ;
#495=CARTESIAN_POINT ( 'NONE',  ( 1.091055626815042423, 0.000000000000000000, -1.771653543307081691 ) ) ;
#496=CARTESIAN_POINT ( 'NONE',  ( -2.182111253630085290, 3.346456692913386100, -0.5118110236220464460 ) ) ;
#498=ORIENTED_EDGE ( 'NONE', *, *, #40681, .F. ) ;
#499=VECTOR ( 'NONE', #35723, 39.37007874015748143 ) ;
#502=AXIS2_PLACEMENT_3D ( 'NONE', #14889, #10510, #7397 ) ;
#504=VECTOR ( 'NONE', #27260, 39.37007874015748143 ) ;
#506=PLANE ( 'NONE',  #7292 ) ;
#508=VERTEX_POINT ( 'NONE', #40596 ) ;
#509=FACE_OUTER_BOUND ( 'NONE', #36357, .T. ) ;
#510=DIRECTION ( 'NONE',  ( 1.734723475976806848E-16, -0.000000000000000000, 1.000000000000000000 ) ) ;
#511=VECTOR ( 'NONE', #44704, 39.37007874015748143 ) ;
#514=VERTEX_POINT ( 'NONE', #17105 ) ;
#515=EDGE_LOOP ( 'NONE', ( #4866, #26370, #10701, #21871 ) ) ;
#518=FACE_BOUND ( 'NONE', #10209, .T. ) ;
#519=CARTESIAN_POINT ( 'NONE',  ( -1.091055626815042645, 0.000000000000000000, -1.141732283464563569 ) ) ;
#520=CARTESIAN_POINT ( 'NONE',  ( -0.2727639067037608278, 3.346456692913386100, -0.3543307086614175816 ) ) ;
#521=EDGE_CURVE ( 'NONE', #50302, #42898, #4716, .T. ) ;
#522=ORIENTED_EDGE ( 'NONE', *, *, #13187, .F. ) ;
#524=LINE ( 'NONE', #261, #38940 ) ;
#525=ORIENTED_EDGE ( 'NONE', *, *, #1312, .T. ) ;
#527=EDGE_CURVE ( 'NONE', #43386, #26232, #48549, .T. ) ;
#528=VERTEX_POINT ( 'NONE', #4968 ) ;
#530=CARTESIAN_POINT ( 'NONE',  ( 1.636583440222563857, 3.267716535433071279, 1.062992125984245639 ) ) ;
#531=EDGE_CURVE ( 'NONE', #42180, #16004, #35958, .T. ) ;
#532=EDGE_CURVE ( 'NONE', #19885, #12012, #8584, .T. ) ;
#533=CIRCLE ( 'NONE', #35177, 2.165354330708661568 ) ;
#534=CARTESIAN_POINT ( 'NONE',  ( 1.363819533518803251, 3.267716535433071279, -0.9842519685039348154 ) ) ;
#535=CARTESIAN_POINT ( 'NONE',  ( -0.3486774197067339376, 0.000000000000000000, -1.574803149606293529 ) ) ;
#536=VERTEX_POINT ( 'NONE', #16595 ) ;
#538=CARTESIAN_POINT ( 'NONE',  ( 2.105931235793975009, 3.346456692913386100, -0.03937007874015936021 ) ) ;
#539=VECTOR ( 'NONE', #22638, 39.37007874015748143 ) ;
#540=DIRECTION ( 'NONE',  ( -1.000000000000000000, 0.000000000000000000, 0.000000000000000000 ) ) ;
#542=DIRECTION ( 'NONE',  ( 1.734723475976806848E-16, -0.000000000000000000, 1.000000000000000000 ) ) ;
#544=CARTESIAN_POINT ( 'NONE',  ( 0.2727639067037604392, 3.346456692913386100, 0.5905511811023579360 ) ) ;
#545=DIRECTION ( 'NONE',  ( -1.000000000000000000, 0.000000000000000000, 0.000000000000000000 ) ) ;
#548=EDGE_CURVE ( 'NONE', #767, #17945, #12977, .T. ) ;
#549=DIRECTION ( 'NONE',  ( -1.000000000000000000, 0.000000000000000000, 1.734723475976806848E-16 ) ) ;
#552=VERTEX_POINT ( 'NONE', #12717 ) ;
#555=ORIENTED_EDGE ( 'NONE', *, *, #24551, .F. ) ;
#556=EDGE_CURVE ( 'NONE', #30179, #17684, #28446, .T. ) ;
#557=ORIENTED_EDGE ( 'NONE', *, *, #2112, .T. ) ;
#559=LINE ( 'NONE', #39798, #12175 ) ;
#561=ORIENTED_EDGE ( 'NONE', *, *, #22890, .T. ) ;
#562=ADVANCED_FACE ( 'NONE', ( #47529 ), #16853, .F. ) ;
#564=EDGE_CURVE ( 'NONE', #23735, #472, #44698, .T. ) ;
#566=CARTESIAN_POINT ( 'NONE',  ( -1.985260859929297794, 3.267716535433071279, -0.1968503937007880511 ) ) ;
#567=ORIENTED_EDGE ( 'NONE', *, *, #25329, .F. ) ;
#569=EDGE_LOOP ( 'NONE', ( #16128, #15928, #15236, #39581 ) ) ;
#572=DIRECTION ( 'NONE',  ( -3.469446951953613696E-16, 0.000000000000000000, -1.000000000000000000 ) ) ;
#575=VERTEX_POINT ( 'NONE', #19929 ) ;
#576=ORIENTED_EDGE ( 'NONE', *, *, #30302, .T. ) ;
#578=DIRECTION ( 'NONE',  ( 0.000000000000000000, 0.000000000000000000, -1.000000000000000000 ) ) ;
#579=ORIENTED_EDGE ( 'NONE', *, *, #21790, .T. ) ;
#582=FACE_OUTER_BOUND ( 'NONE', #22566, .T. ) ;
#587=CARTESIAN_POINT ( 'NONE',  ( 1.091055626815042645, 3.267716535433071279, 0.9448818897637746295 ) ) ;
#588=VECTOR ( 'NONE', #9109, 39.37007874015748143 ) ;
#589=PLANE ( 'NONE',  #36074 ) ;
#590=ORIENTED_EDGE ( 'NONE', *, *, #45368, .T. ) ;
#591=DIRECTION ( 'NONE',  ( -0.000000000000000000, 1.000000000000000000, -0.000000000000000000 ) ) ;
#592=DIRECTION ( 'NONE',  ( -1.000000000000000000, -0.000000000000000000, -0.000000000000000000 ) ) ;
#593=ORIENTED_EDGE ( 'NONE', *, *, #32954, .T. ) ;
#597=DIRECTION ( 'NONE',  ( 0.000000000000000000, 0.000000000000000000, 1.000000000000000000 ) ) ;
#598=CARTESIAN_POINT ( 'NONE',  ( -1.909347346926324462, 3.346456692913386100, 0.7874015748031456541 ) ) ;
#599=DIRECTION ( 'NONE',  ( -1.000000000000000000, 0.000000000000000000, 1.734723475976806848E-16 ) ) ;
#600=ADVANCED_FACE ( 'NONE', ( #326 ), #16077, .F. ) ;
#601=DIRECTION ( 'NONE',  ( -1.000000000000000000, 0.000000000000000000, -0.000000000000000000 ) ) ;
#605=EDGE_CURVE ( 'NONE', #10001, #15411, #43680, .T. ) ;
#606=VERTEX_POINT ( 'NONE', #5983 ) ;
#607=CARTESIAN_POINT ( 'NONE',  ( -0.07591351300297333182, 0.000000000000000000, -0.1574803149606301411 ) ) ;
#608=DIRECTION ( 'NONE',  ( -0.000000000000000000, 1.000000000000000000, -0.000000000000000000 ) ) ;
#609=VECTOR ( 'NONE', #21997, 39.37007874015748143 ) ;
#610=AXIS2_PLACEMENT_3D ( 'NONE', #25837, #13461, #17336 ) ;
#611=DIRECTION ( 'NONE',  ( -0.000000000000000000, 1.000000000000000000, -0.000000000000000000 ) ) ;
#612=DIRECTION ( 'NONE',  ( 0.000000000000000000, 0.000000000000000000, -1.000000000000000000 ) ) ;
#614=AXIS2_PLACEMENT_3D ( 'NONE', #23088, #14843, #31348 ) ;
#617=EDGE_CURVE ( 'NONE', #42860, #2302, #45709, .T. ) ;
#620=CARTESIAN_POINT ( 'NONE',  ( 0.2727639067037604947, 0.000000000000000000, 0.4724409448818868706 ) ) ;
#621=EDGE_CURVE ( 'NONE', #43980, #50349, #21739, .T. ) ;
#622=PLANE ( 'NONE',  #40169 ) ;
#623=CARTESIAN_POINT ( 'NONE',  ( 0.000000000000000000, 3.267716535433071279, 0.4330708661417290162 ) ) ;
#624=ORIENTED_EDGE ( 'NONE', *, *, #34860, .F. ) ;
#625=CARTESIAN_POINT ( 'NONE',  ( -3.927031490892378253E-16, 0.000000000000000000, -2.204724409448811429 ) ) ;
#627=EDGE_CURVE ( 'NONE', #37376, #24669, #34123, .T. ) ;
#628=DIRECTION ( 'NONE',  ( 0.000000000000000000, -1.000000000000000000, 0.000000000000000000 ) ) ;
#629=EDGE_CURVE ( 'NONE', #27835, #12857, #13991, .T. ) ;
#630=ORIENTED_EDGE ( 'NONE', *, *, #20994, .T. ) ;
#631=FACE_OUTER_BOUND ( 'NONE', #6545, .T. ) ;
#634=CIRCLE ( 'NONE', #36092, 2.106299212598425008 ) ;
#636=DIRECTION ( 'NONE',  ( -1.000000000000000000, 0.000000000000000000, -0.000000000000000000 ) ) ;
#637=LINE ( 'NONE', #27992, #779 ) ;
#639=ORIENTED_EDGE ( 'NONE', *, *, #2477, .F. ) ;
#641=DIRECTION ( 'NONE',  ( -0.000000000000000000, 0.000000000000000000, 1.000000000000000000 ) ) ;
#642=DIRECTION ( 'NONE',  ( 0.000000000000000000, 0.000000000000000000, -1.000000000000000000 ) ) ;
#644=LINE ( 'NONE', #36784, #6080 ) ;
#647=LINE ( 'NONE', #5284, #38047 ) ;
#653=VECTOR ( 'NONE', #28879, 39.37007874015748143 ) ;
#656=FACE_BOUND ( 'NONE', #18999, .T. ) ;
#657=ORIENTED_EDGE ( 'NONE', *, *, #15041, .F. ) ;
#659=ORIENTED_EDGE ( 'NONE', *, *, #49999, .F. ) ;
#660=VERTEX_POINT ( 'NONE', #17606 ) ;
#662=ORIENTED_EDGE ( 'NONE', *, *, #5685, .T. ) ;
#664=PLANE ( 'NONE',  #11276 ) ;
#666=ORIENTED_EDGE ( 'NONE', *, *, #47141, .F. ) ;
#668=EDGE_CURVE ( 'NONE', #49945, #20320, #44427, .T. ) ;
#673=CARTESIAN_POINT ( 'NONE',  ( -1.363819533518803029, 3.267716535433071279, 0.2755905511810996522 ) ) ;
#674=LINE ( 'NONE', #20018, #15684 ) ;
#675=LINE ( 'NONE', #152, #6376 ) ;
#677=EDGE_LOOP ( 'NONE', ( #44248, #22228, #9359, #47883 ) ) ;
#679=LINE ( 'NONE', #22028, #24389 ) ;
#680=CARTESIAN_POINT ( 'NONE',  ( -0.3486774197067334380, 3.346456692913386100, 0.6299212598425164567 ) ) ;
#681=VERTEX_POINT ( 'NONE', #37751 ) ;
#682=DIRECTION ( 'NONE',  ( -1.000000000000000000, -0.000000000000000000, -0.000000000000000000 ) ) ;
#683=ADVANCED_FACE ( 'NONE', ( #25859 ), #33375, .F. ) ;
#684=EDGE_CURVE ( 'NONE', #20090, #19616, #6245, .T. ) ;
#685=CARTESIAN_POINT ( 'NONE',  ( -3.927031490892378253E-16, 3.346456692913386100, -1.889763779527552146 ) ) ;
#686=ORIENTED_EDGE ( 'NONE', *, *, #5220, .F. ) ;
#687=DIRECTION ( 'NONE',  ( -0.000000000000000000, 1.000000000000000000, -0.000000000000000000 ) ) ;
#688=VECTOR ( 'NONE', #36333, 39.37007874015748143 ) ;
#690=DIRECTION ( 'NONE',  ( -3.469446951953613696E-16, 0.000000000000000000, -1.000000000000000000 ) ) ;
#691=EDGE_CURVE ( 'NONE', #38575, #28934, #17862, .T. ) ;
#694=CARTESIAN_POINT ( 'NONE',  ( -0.2727639067037608278, 3.346456692913386100, -0.03937007874015908959 ) ) ;
#696=CARTESIAN_POINT ( 'NONE',  ( -0.8182917201112819283, 0.000000000000000000, -2.047244094488181343 ) ) ;
#697=CARTESIAN_POINT ( 'NONE',  ( 0.000000000000000000, 3.267716535433071279, -1.259842519685035134 ) ) ;
#700=CARTESIAN_POINT ( 'NONE',  ( 1.015142113812069757, 3.267716535433071279, -3.521981712565034361E-16 ) ) ;
#701=LINE ( 'NONE', #16453, #21905 ) ;
#702=VECTOR ( 'NONE', #26815, 39.37007874015748143 ) ;
#704=ORIENTED_EDGE ( 'NONE', *, *, #29300, .T. ) ;
#705=CARTESIAN_POINT ( 'NONE',  ( -0.8182917201112819283, 0.000000000000000000, -0.03937007874015895081 ) ) ;
#706=VERTEX_POINT ( 'NONE', #45202 ) ;
#707=VECTOR ( 'NONE', #10273, 39.37007874015748143 ) ;
#708=CARTESIAN_POINT ( 'NONE',  ( -0.6214413264104945434, 3.267716535433071279, 0.1574803149606285035 ) ) ;
#709=ADVANCED_FACE ( 'NONE', ( #44955 ), #29989, .F. ) ;
#712=AXIS2_PLACEMENT_3D ( 'NONE', #34837, #11341, #39468 ) ;
#713=VERTEX_POINT ( 'NONE', #41112 ) ;
#714=DIRECTION ( 'NONE',  ( 1.000000000000000000, 0.000000000000000000, -3.469446951953613696E-16 ) ) ;
#717=CARTESIAN_POINT ( 'NONE',  ( 0.1968503937007878291, 3.267716535433071279, 2.097080421798980687 ) ) ;
#718=ORIENTED_EDGE ( 'NONE', *, *, #12741, .F. ) ;
#721=VERTEX_POINT ( 'NONE', #45453 ) ;
#722=EDGE_LOOP ( 'NONE', ( #32212, #14805, #21294, #41586 ) ) ;
#723=DIRECTION ( 'NONE',  ( 1.000000000000000000, 0.000000000000000000, 0.000000000000000000 ) ) ;
#724=EDGE_CURVE ( 'NONE', #34623, #508, #49561, .T. ) ;
#725=CARTESIAN_POINT ( 'NONE',  ( -0.6214413264104939882, 0.000000000000000000, 1.417322834645662777 ) ) ;
#726=EDGE_LOOP ( 'NONE', ( #49248, #34876, #20386, #6495 ) ) ;
#727=DIRECTION ( 'NONE',  ( -0.000000000000000000, 0.000000000000000000, 1.000000000000000000 ) ) ;
#728=VERTEX_POINT ( 'NONE', #22249 ) ;
#729=CARTESIAN_POINT ( 'NONE',  ( 1.091055626815043311, 0.000000000000000000, 1.574803149606291974 ) ) ;
#732=AXIS2_PLACEMENT_3D ( 'NONE', #19178, #34942, #50622 ) ;
#733=VECTOR ( 'NONE', #35619, 39.37007874015748143 ) ;
#734=EDGE_CURVE ( 'NONE', #39696, #36547, #5477, .T. ) ;
#735=EDGE_CURVE ( 'NONE', #421, #8195, #12268, .T. ) ;
#738=ORIENTED_EDGE ( 'NONE', *, *, #7376, .T. ) ;
#739=VERTEX_POINT ( 'NONE', #34624 ) ;
#740=LINE ( 'NONE', #12610, #44243 ) ;
#742=DIRECTION ( 'NONE',  ( 0.000000000000000000, 0.000000000000000000, -1.000000000000000000 ) ) ;
#743=CARTESIAN_POINT ( 'NONE',  ( 1.636583440222563857, 3.346456692913386100, -0.8267716535433055070 ) ) ;
#744=VECTOR ( 'NONE', #32906, 39.37007874015748143 ) ;
#745=LINE ( 'NONE', #4613, #42478 ) ;
#747=CARTESIAN_POINT ( 'NONE',  ( 2.378961647330872786, 3.346456692913386100, 0.6299212598425161236 ) ) ;
#749=EDGE_LOOP ( 'NONE', ( #24155, #3982, #6135, #40516 ) ) ;
#751=ORIENTED_EDGE ( 'NONE', *, *, #2533, .F. ) ;
#752=CARTESIAN_POINT ( 'NONE',  ( 1.833433833923351353, 3.346456692913386100, 0.6299212598425164567 ) ) ;
#753=ADVANCED_FACE ( 'NONE', ( #39247 ), #7507, .F. ) ;
#755=FACE_OUTER_BOUND ( 'NONE', #21219, .T. ) ;
#757=CARTESIAN_POINT ( 'NONE',  ( -1.363819533518803473, 3.346456692913386100, -0.7874015748031470974 ) ) ;
#760=EDGE_LOOP ( 'NONE', ( #34527, #20006, #15993, #48619 ) ) ;
#761=EDGE_CURVE ( 'NONE', #2304, #42940, #15253, .T. ) ;
#763=FACE_BOUND ( 'NONE', #51044, .T. ) ;
#765=CARTESIAN_POINT ( 'NONE',  ( -1.091055626815042645, 3.267716535433071279, -0.1968503937007881899 ) ) ;
#766=EDGE_CURVE ( 'NONE', #14307, #38168, #3376, .T. ) ;
#767=VERTEX_POINT ( 'NONE', #19117 ) ;
#768=VECTOR ( 'NONE', #44218, 39.37007874015748143 ) ;
#770=PLANE ( 'NONE',  #4978 ) ;
#771=VECTOR ( 'NONE', #44811, 39.37007874015748143 ) ;
#773=EDGE_LOOP ( 'NONE', ( #73, #46389, #9582, #33616 ) ) ;
#775=ADVANCED_FACE ( 'NONE', ( #42612 ), #18880, .F. ) ;
#776=CARTESIAN_POINT ( 'NONE',  ( 0.000000000000000000, 3.267716535433071279, -0.03937007874015908959 ) ) ;
#777=CARTESIAN_POINT ( 'NONE',  ( 0.000000000000000000, 3.267716535433071279, -1.732283464566922726 ) ) ;
#778=FACE_BOUND ( 'NONE', #45683, .T. ) ;
#779=VECTOR ( 'NONE', #11048, 39.37007874015748143 ) ;
#781=FACE_OUTER_BOUND ( 'NONE', #19671, .T. ) ;
#784=VERTEX_POINT ( 'NONE', #3126 ) ;
#787=LINE ( 'NONE', #32039, #20183 ) ;
#790=VECTOR ( 'NONE', #14937, 39.37007874015748143 ) ;
#791=CARTESIAN_POINT ( 'NONE',  ( -0.6214413264104945434, 0.000000000000000000, -1.732283464566922726 ) ) ;
#794=EDGE_LOOP ( 'NONE', ( #25554, #27544, #44506, #46711 ) ) ;
#795=VERTEX_POINT ( 'NONE', #46708 ) ;
#797=DIRECTION ( 'NONE',  ( 1.000000000000000000, 0.000000000000000000, -3.469446951953613696E-16 ) ) ;
#799=DIRECTION ( 'NONE',  ( 1.734723475976806848E-16, -0.000000000000000000, 1.000000000000000000 ) ) ;
#802=VECTOR ( 'NONE', #23259, 39.37007874015748143 ) ;
#803=LINE ( 'NONE', #27900, #7797 ) ;
#804=DIRECTION ( 'NONE',  ( 0.000000000000000000, -1.000000000000000000, 0.000000000000000000 ) ) ;
#809=ORIENTED_EDGE ( 'NONE', *, *, #33052, .T. ) ;
#811=DIRECTION ( 'NONE',  ( 1.734723475976806848E-16, 0.000000000000000000, 1.000000000000000000 ) ) ;
#812=DIRECTION ( 'NONE',  ( 1.000000000000000000, 0.000000000000000000, -3.469446951953613696E-16 ) ) ;
#813=DIRECTION ( 'NONE',  ( -0.000000000000000000, 1.000000000000000000, -0.000000000000000000 ) ) ;
#814=VERTEX_POINT ( 'NONE', #50555 ) ;
#815=EDGE_CURVE ( 'NONE', #903, #26348, #50808, .T. ) ;
#818=ORIENTED_EDGE ( 'NONE', *, *, #10811, .T. ) ;
#819=CARTESIAN_POINT ( 'NONE',  ( 0.000000000000000000, 3.267716535433071279, 0.000000000000000000 ) ) ;
#820=EDGE_CURVE ( 'NONE', #12778, #27951, #43105, .T. ) ;
#821=EDGE_LOOP ( 'NONE', ( #9721, #36977, #33550, #6151 ) ) ;
#822=DIRECTION ( 'NONE',  ( 0.000000000000000000, -1.000000000000000000, 0.000000000000000000 ) ) ;
#824=DIRECTION ( 'NONE',  ( -3.469446951953613696E-16, 0.000000000000000000, -1.000000000000000000 ) ) ;
#825=ADVANCED_FACE ( 'NONE', ( #2877 ), #3886, .F. ) ;
#827=ORIENTED_EDGE ( 'NONE', *, *, #8146, .T. ) ;
#828=EDGE_LOOP ( 'NONE', ( #17732, #25689, #7939, #44891 ) ) ;
#830=CARTESIAN_POINT ( 'NONE',  ( 1.363819533518803251, 3.267716535433071279, 0.5905511811023579360 ) ) ;
#831=ORIENTED_EDGE ( 'NONE', *, *, #31034, .T. ) ;
#835=LINE ( 'NONE', #8068, #7117 ) ;
#836=DIRECTION ( 'NONE',  ( 1.734723475976806848E-16, -0.000000000000000000, 1.000000000000000000 ) ) ;
#837=EDGE_CURVE ( 'NONE', #35448, #18861, #19618, .T. ) ;
#842=CARTESIAN_POINT ( 'NONE',  ( 0.5455278134075212115, 3.346456692913386100, -0.9448818897637765168 ) ) ;
#843=CARTESIAN_POINT ( 'NONE',  ( -1.363819533518803695, 3.267716535433071279, 2.365849761790806473E-16 ) ) ;
#844=CARTESIAN_POINT ( 'NONE',  ( -1.363819533518803473, 3.346456692913386100, -1.417322834645664109 ) ) ;
#846=CARTESIAN_POINT ( 'NONE',  ( 1.560669927219590303, 3.267716535433071279, -1.732283464566923170 ) ) ;
#848=ORIENTED_EDGE ( 'NONE', *, *, #23875, .F. ) ;
#849=DIRECTION ( 'NONE',  ( 0.000000000000000000, 0.000000000000000000, -1.000000000000000000 ) ) ;
#850=VERTEX_POINT ( 'NONE', #26860 ) ;
#851=EDGE_LOOP ( 'NONE', ( #27475, #12376, #37476, #23396 ) ) ;
#852=AXIS2_PLACEMENT_3D ( 'NONE', #4132, #16256, #19102 ) ;
#858=CARTESIAN_POINT ( 'NONE',  ( 0.2727639067037610499, 0.000000000000000000, 1.732283464566921172 ) ) ;
#861=ADVANCED_FACE ( 'NONE', ( #38506 ), #7260, .F. ) ;
#863=ORIENTED_EDGE ( 'NONE', *, *, #49296, .T. ) ;
#864=DIRECTION ( 'NONE',  ( 1.734723475976806848E-16, -0.000000000000000000, 1.000000000000000000 ) ) ;
#870=CARTESIAN_POINT ( 'NONE',  ( 0.000000000000000000, 3.346456692913386100, 0.000000000000000000 ) ) ;
#871=DIRECTION ( 'NONE',  ( -1.000000000000000000, 0.000000000000000000, -0.000000000000000000 ) ) ;
#874=DIRECTION ( 'NONE',  ( 1.000000000000000000, -0.000000000000000000, 0.000000000000000000 ) ) ;
#875=VECTOR ( 'NONE', #46875, 39.37007874015748143 ) ;
#878=ORIENTED_EDGE ( 'NONE', *, *, #34136, .F. ) ;
#879=DIRECTION ( 'NONE',  ( 1.734723475976806848E-16, 0.000000000000000000, 1.000000000000000000 ) ) ;
#880=LINE ( 'NONE', #27725, #20893 ) ;
#881=PLANE ( 'NONE',  #3640 ) ;
#882=EDGE_LOOP ( 'NONE', ( #36469, #24723, #16988, #18000 ) ) ;
#883=DIRECTION ( 'NONE',  ( 1.000000000000000000, -0.000000000000000000, 0.000000000000000000 ) ) ;
#884=CIRCLE ( 'NONE', #48679, 2.106299212598425008 ) ;
#885=CARTESIAN_POINT ( 'NONE',  ( 1.928732080931637505, 3.346456692913386100, -0.9842519685039348154 ) ) ;
#886=ORIENTED_EDGE ( 'NONE', *, *, #33174, .T. ) ;
#889=LINE ( 'NONE', #16126, #46909 ) ;
#891=ADVANCED_FACE ( 'NONE', ( #4141 ), #28129, .F. ) ;
#892=ADVANCED_FACE ( 'NONE', ( #27875 ), #4653, .F. ) ;
#896=LINE ( 'NONE', #4512, #8403 ) ;
#897=CARTESIAN_POINT ( 'NONE',  ( 0.5455278134075211005, 3.346456692913386100, -1.456692913385822630 ) ) ;
#899=DIRECTION ( 'NONE',  ( -3.469446951953613696E-16, 0.000000000000000000, -1.000000000000000000 ) ) ;
#900=LINE ( 'NONE', #45766, #18611 ) ;
#901=CARTESIAN_POINT ( 'NONE',  ( 0.2727639067037604392, 0.000000000000000000, -0.03937007874015908959 ) ) ;
#902=CARTESIAN_POINT ( 'NONE',  ( -0.3486774197067339376, 3.346456692913386100, -1.259842519685035134 ) ) ;
#903=VERTEX_POINT ( 'NONE', #12391 ) ;
#904=VERTEX_POINT ( 'NONE', #1287 ) ;
#905=DIRECTION ( 'NONE',  ( -1.000000000000000000, -0.000000000000000000, -0.000000000000000000 ) ) ;
#906=CARTESIAN_POINT ( 'NONE',  ( 3.927031490892378253E-16, 3.267716535433071279, 1.692913385826762873 ) ) ;
#907=FACE_OUTER_BOUND ( 'NONE', #32075, .T. ) ;
#908=CARTESIAN_POINT ( 'NONE',  ( 1.833433833923351353, 0.000000000000000000, 0.3149606299212576177 ) ) ;
#909=FACE_BOUND ( 'NONE', #8066, .T. ) ;
#910=ORIENTED_EDGE ( 'NONE', *, *, #17652, .F. ) ;
#912=VERTEX_POINT ( 'NONE', #43619 ) ;
#913=ORIENTED_EDGE ( 'NONE', *, *, #40482, .F. ) ;
#914=EDGE_CURVE ( 'NONE', #7908, #34106, #43872, .T. ) ;
#915=CARTESIAN_POINT ( 'NONE',  ( -0.8942052331142552601, 0.000000000000000000, -1.574803149606293529 ) ) ;
#917=EDGE_CURVE ( 'NONE', #7644, #10410, #8521, .T. ) ;
#919=VERTEX_POINT ( 'NONE', #20648 ) ;
#924=VERTEX_POINT ( 'NONE', #17048 ) ;
#925=ADVANCED_FACE ( 'NONE', ( #27618 ), #19867, .F. ) ;
#926=VECTOR ( 'NONE', #47714, 39.37007874015748143 ) ;
#928=CARTESIAN_POINT ( 'NONE',  ( 0.5455278134075208785, 0.000000000000000000, -1.771653543307081025 ) ) ;
#929=PLANE ( 'NONE',  #10245 ) ;
#930=LINE ( 'NONE', #35533, #39603 ) ;
#931=DIRECTION ( 'NONE',  ( -1.000000000000000000, -0.000000000000000000, -0.000000000000000000 ) ) ;
#932=DIRECTION ( 'NONE',  ( -1.000000000000000000, -0.000000000000000000, -0.000000000000000000 ) ) ;
#934=LINE ( 'NONE', #1444, #9330 ) ;
#935=PLANE ( 'NONE',  #45777 ) ;
#936=DIRECTION ( 'NONE',  ( -3.469446951953613696E-16, 0.000000000000000000, -1.000000000000000000 ) ) ;
#941=PLANE ( 'NONE',  #42748 ) ;
#947=EDGE_LOOP ( 'NONE', ( #29123, #50516, #44377, #14679 ) ) ;
#948=FACE_BOUND ( 'NONE', #13602, .T. ) ;
#949=LINE ( 'NONE', #1458, #1178 ) ;
#952=DIRECTION ( 'NONE',  ( 1.734723475976806848E-16, -0.000000000000000000, 1.000000000000000000 ) ) ;
#953=CARTESIAN_POINT ( 'NONE',  ( -0.3486774197067339376, 0.000000000000000000, -0.3149606299212593941 ) ) ;
#956=ORIENTED_EDGE ( 'NONE', *, *, #17590, .F. ) ;
#957=ORIENTED_EDGE ( 'NONE', *, *, #40205, .T. ) ;
#958=EDGE_CURVE ( 'NONE', #11836, #35629, #47977, .T. ) ;
#959=DIRECTION ( 'NONE',  ( -0.000000000000000000, 1.000000000000000000, -0.000000000000000000 ) ) ;
#960=ORIENTED_EDGE ( 'NONE', *, *, #36010, .T. ) ;
#961=VECTOR ( 'NONE', #49944, 39.37007874015748143 ) ;
#962=DIRECTION ( 'NONE',  ( -3.469446951953613696E-16, 0.000000000000000000, -1.000000000000000000 ) ) ;
#964=EDGE_CURVE ( 'NONE', #3496, #3427, #24528, .T. ) ;
#965=CARTESIAN_POINT ( 'NONE',  ( -4.268512490100411402E-16, 3.267716535433071279, -2.401574803149598480 ) ) ;
#967=ORIENTED_EDGE ( 'NONE', *, *, #27641, .F. ) ;
#968=CARTESIAN_POINT ( 'NONE',  ( -0.5455278134075213226, 3.267716535433071279, 9.463399047163224412E-17 ) ) ;
#969=CARTESIAN_POINT ( 'NONE',  ( -0.5455278134075214336, 3.346456692913386100, -1.259842519685035134 ) ) ;
#971=DIRECTION ( 'NONE',  ( -0.000000000000000000, 1.000000000000000000, -0.000000000000000000 ) ) ;
#973=DIRECTION ( 'NONE',  ( -3.469446951953613696E-16, 0.000000000000000000, -1.000000000000000000 ) ) ;
#974=ADVANCED_FACE ( 'NONE', ( #31768 ), #32542, .F. ) ;
#977=DIRECTION ( 'NONE',  ( -1.000000000000000000, -0.000000000000000000, -0.000000000000000000 ) ) ;
#979=ORIENTED_EDGE ( 'NONE', *, *, #15372, .T. ) ;
#980=DIRECTION ( 'NONE',  ( 1.734723475976806848E-16, -0.000000000000000000, 1.000000000000000000 ) ) ;
#981=ORIENTED_EDGE ( 'NONE', *, *, #8600, .F. ) ;
#983=AXIS2_PLACEMENT_3D ( 'NONE', #50342, #14533, #2406 ) ;
#986=LINE ( 'NONE', #4865, #10723 ) ;
#987=ORIENTED_EDGE ( 'NONE', *, *, #38720, .T. ) ;
#988=AXIS2_PLACEMENT_3D ( 'NONE', #38689, #38436, #3565 ) ;
#991=DIRECTION ( 'NONE',  ( -3.469446951953613696E-16, 0.000000000000000000, -1.000000000000000000 ) ) ;
#992=CARTESIAN_POINT ( 'NONE',  ( 1.287906020515829919, 3.267716535433071279, -1.771653543307081691 ) ) ;
#993=VECTOR ( 'NONE', #22067, 39.37007874015748143 ) ;
#994=FACE_OUTER_BOUND ( 'NONE', #10388, .T. ) ;
#995=CARTESIAN_POINT ( 'NONE',  ( 1.363819533518803695, 3.346456692913386100, 1.535433070866133898 ) ) ;
#996=AXIS2_PLACEMENT_3D ( 'NONE', #15783, #27913, #39285 ) ;
#997=DIRECTION ( 'NONE',  ( 0.000000000000000000, -1.000000000000000000, 0.000000000000000000 ) ) ;
#998=ORIENTED_EDGE ( 'NONE', *, *, #45478, .F. ) ;
#999=DIRECTION ( 'NONE',  ( 1.734723475976806848E-16, -0.000000000000000000, 1.000000000000000000 ) ) ;
#1000=DIRECTION ( 'NONE',  ( -1.000000000000000000, 0.000000000000000000, -0.000000000000000000 ) ) ;
#1001=EDGE_LOOP ( 'NONE', ( #26786, #37902, #50195, #9710 ) ) ;
#1002=CARTESIAN_POINT ( 'NONE',  ( 0.000000000000000000, 3.267716535433071279, -1.417322834645664331 ) ) ;
#1003=ORIENTED_EDGE ( 'NONE', *, *, #17058, .T. ) ;
#1005=DIRECTION ( 'NONE',  ( 0.000000000000000000, -1.000000000000000000, 0.000000000000000000 ) ) ;
#1006=DIRECTION ( 'NONE',  ( 1.734723475976806848E-16, 0.000000000000000000, 1.000000000000000000 ) ) ;
#1007=CARTESIAN_POINT ( 'NONE',  ( -0.8942052331142552601, 3.346456692913386100, -1.889763779527552146 ) ) ;
#1008=VERTEX_POINT ( 'NONE', #20909 ) ;
#1009=DIRECTION ( 'NONE',  ( -1.000000000000000000, 0.000000000000000000, 0.000000000000000000 ) ) ;
#1010=EDGE_CURVE ( 'NONE', #9489, #2168, #36665, .T. ) ;
#1011=FACE_BOUND ( 'NONE', #46470, .T. ) ;
#1012=EDGE_CURVE ( 'NONE', #36186, #15116, #40790, .T. ) ;
#1013=ORIENTED_EDGE ( 'NONE', *, *, #2786, .T. ) ;
#1017=DIRECTION ( 'NONE',  ( 0.000000000000000000, 0.000000000000000000, -1.000000000000000000 ) ) ;
#1018=CARTESIAN_POINT ( 'NONE',  ( -1.363819533518803473, 3.346456692913386100, -0.1574803149606300023 ) ) ;
#1019=VECTOR ( 'NONE', #7452, 39.37007874015748143 ) ;
#1020=ADVANCED_FACE ( 'NONE', ( #17300 ), #37945, .F. ) ;
#1021=VECTOR ( 'NONE', #24147, 39.37007874015748143 ) ;
#1022=CARTESIAN_POINT ( 'NONE',  ( 1.909347346926324684, 3.346456692913386100, 0.1574803149606280872 ) ) ;
#1024=ORIENTED_EDGE ( 'NONE', *, *, #14890, .T. ) ;
#1026=VECTOR ( 'NONE', #49061, 39.37007874015748143 ) ;
#1028=FACE_BOUND ( 'NONE', #16644, .T. ) ;
#1029=VECTOR ( 'NONE', #35152, 39.37007874015748143 ) ;
#1030=VECTOR ( 'NONE', #10332, 39.37007874015748143 ) ;
#1032=EDGE_CURVE ( 'NONE', #6504, #4531, #26055, .T. ) ;
#1033=LINE ( 'NONE', #16790, #43158 ) ;
#1038=VERTEX_POINT ( 'NONE', #41052 ) ;
#1039=VERTEX_POINT ( 'NONE', #49502 ) ;
#1041=LINE ( 'NONE', #48247, #49671 ) ;
#1042=CARTESIAN_POINT ( 'NONE',  ( 0.2727639067037605503, 3.267716535433071279, -4.731699523581609125E-17 ) ) ;
#1043=DIRECTION ( 'NONE',  ( 1.734723475976806848E-16, -0.000000000000000000, 1.000000000000000000 ) ) ;
#1045=ORIENTED_EDGE ( 'NONE', *, *, #50865, .F. ) ;
#1047=DIRECTION ( 'NONE',  ( -3.469446951953613696E-16, 0.000000000000000000, -1.000000000000000000 ) ) ;
#1048=DIRECTION ( 'NONE',  ( -1.000000000000000000, -0.000000000000000000, -0.000000000000000000 ) ) ;
#1050=CARTESIAN_POINT ( 'NONE',  ( 0.000000000000000000, 3.267716535433071279, -0.1968503937007874405 ) ) ;
#1051=LINE ( 'NONE', #9314, #18238 ) ;
#1053=DIRECTION ( 'NONE',  ( 1.000000000000000000, 0.000000000000000000, 0.000000000000000000 ) ) ;
#1054=CARTESIAN_POINT ( 'NONE',  ( 0.4696143004045479352, 3.267716535433071279, -1.102362204724405714 ) ) ;
#1056=VERTEX_POINT ( 'NONE', #1547 ) ;
#1057=DIRECTION ( 'NONE',  ( 1.734723475976806848E-16, -0.000000000000000000, 1.000000000000000000 ) ) ;
#1059=VERTEX_POINT ( 'NONE', #17549 ) ;
#1060=VECTOR ( 'NONE', #15527, 39.37007874015748143 ) ;
#1062=DIRECTION ( 'NONE',  ( -1.000000000000000000, 0.000000000000000000, -0.000000000000000000 ) ) ;
#1063=CARTESIAN_POINT ( 'NONE',  ( -0.5455278134075214336, 0.000000000000000000, -0.3149606299212593941 ) ) ;
#1065=EDGE_LOOP ( 'NONE', ( #15452, #25045, #35705, #16560 ) ) ;
#1067=ORIENTED_EDGE ( 'NONE', *, *, #39592, .T. ) ;
#1068=CARTESIAN_POINT ( 'NONE',  ( -1.712496953225537633, 0.000000000000000000, -0.6692913385826758654 ) ) ;
#1070=ORIENTED_EDGE ( 'NONE', *, *, #20041, .F. ) ;
#1071=EDGE_CURVE ( 'NONE', #19845, #37743, #1798, .T. ) ;
#1073=CARTESIAN_POINT ( 'NONE',  ( 0.000000000000000000, 2.362204724409439294, -2.952755905511811552 ) ) ;
#1074=CARTESIAN_POINT ( 'NONE',  ( 1.363819533518803251, 0.000000000000000000, 1.102362204724403938 ) ) ;
#1075=EDGE_CURVE ( 'NONE', #27292, #42794, #48995, .T. ) ;
#1078=EDGE_LOOP ( 'NONE', ( #26374, #17593, #10106, #4070 ) ) ;
#1082=EDGE_LOOP ( 'NONE', ( #41251, #1474, #22226, #42100 ) ) ;
#1083=CARTESIAN_POINT ( 'NONE',  ( 1.015142113812069313, 3.346456692913386100, 0.2755905511810994302 ) ) ;
#1084=LINE ( 'NONE', #48035, #43388 ) ;
#1086=ORIENTED_EDGE ( 'NONE', *, *, #15124, .F. ) ;
#1087=DIRECTION ( 'NONE',  ( -0.000000000000000000, 1.000000000000000000, -0.000000000000000000 ) ) ;
#1089=DIRECTION ( 'NONE',  ( 1.000000000000000000, 0.000000000000000000, -3.469446951953613696E-16 ) ) ;
#1090=ORIENTED_EDGE ( 'NONE', *, *, #7820, .F. ) ;
#1092=VECTOR ( 'NONE', #12393, 39.37007874015748143 ) ;
#1094=PLANE ( 'NONE',  #30734 ) ;
#1095=ORIENTED_EDGE ( 'NONE', *, *, #45812, .F. ) ;
#1096=AXIS2_PLACEMENT_3D ( 'NONE', #3994, #7862, #26965 ) ;
#1097=ORIENTED_EDGE ( 'NONE', *, *, #35685, .T. ) ;
#1098=DIRECTION ( 'NONE',  ( -0.000000000000000000, 0.000000000000000000, 1.000000000000000000 ) ) ;
#1101=FACE_OUTER_BOUND ( 'NONE', #13167, .T. ) ;
#1102=EDGE_CURVE ( 'NONE', #14290, #26003, #10310, .T. ) ;
#1103=CARTESIAN_POINT ( 'NONE',  ( 1.560669927219590525, 3.267716535433071279, -5.414661521997676285E-16 ) ) ;
#1106=EDGE_LOOP ( 'NONE', ( #28845, #3707, #6094, #23795 ) ) ;
#1109=ORIENTED_EDGE ( 'NONE', *, *, #8111, .F. ) ;
#1110=DIRECTION ( 'NONE',  ( -1.000000000000000000, 0.000000000000000000, 0.000000000000000000 ) ) ;
#1111=EDGE_CURVE ( 'NONE', #14945, #25938, #2309, .T. ) ;
#1112=PLANE ( 'NONE',  #11089 ) ;
#1113=CARTESIAN_POINT ( 'NONE',  ( 0.000000000000000000, 3.267716535433071279, -0.4724409448818886470 ) ) ;
#1114=CARTESIAN_POINT ( 'NONE',  ( 2.378961647330872786, 3.267716535433071279, -8.253681236146643855E-16 ) ) ;
#1115=DIRECTION ( 'NONE',  ( -0.000000000000000000, 1.000000000000000000, -0.000000000000000000 ) ) ;
#1116=ORIENTED_EDGE ( 'NONE', *, *, #33103, .T. ) ;
#1117=CARTESIAN_POINT ( 'NONE',  ( -0.8182917201112819283, 0.000000000000000000, -1.417322834645664331 ) ) ;
#1119=LINE ( 'NONE', #13262, #12517 ) ;
#1122=CARTESIAN_POINT ( 'NONE',  ( -0.8182917201112814842, 3.267716535433071279, 0.4724409448818872592 ) ) ;
#1124=DIRECTION ( 'NONE',  ( -0.000000000000000000, 1.000000000000000000, -0.000000000000000000 ) ) ;
#1125=VERTEX_POINT ( 'NONE', #6440 ) ;
#1126=LINE ( 'NONE', #20233, #44035 ) ;
#1127=LINE ( 'NONE', #36765, #14295 ) ;
#1130=ORIENTED_EDGE ( 'NONE', *, *, #8974, .F. ) ;
#1131=AXIS2_PLACEMENT_3D ( 'NONE', #16246, #43081, #39223 ) ;
#1132=FACE_BOUND ( 'NONE', #14256, .T. ) ;
#1133=LINE ( 'NONE', #16897, #41890 ) ;
#1134=ORIENTED_EDGE ( 'NONE', *, *, #45624, .T. ) ;
#1136=VECTOR ( 'NONE', #31899, 39.37007874015748143 ) ;
#1138=VECTOR ( 'NONE', #5184, 39.37007874015748143 ) ;
#1139=CARTESIAN_POINT ( 'NONE',  ( -1.091055626815042645, 3.346456692913386100, -1.889763779527552146 ) ) ;
#1140=LINE ( 'NONE', #32916, #16448 ) ;
#1141=DIRECTION ( 'NONE',  ( -1.000000000000000000, -0.000000000000000000, -0.000000000000000000 ) ) ;
#1142=ADVANCED_FACE ( 'NONE', ( #22192 ), #45142, .F. ) ;
#1144=EDGE_CURVE ( 'NONE', #49145, #50578, #9807, .T. ) ;
#1145=DIRECTION ( 'NONE',  ( 0.000000000000000000, -1.000000000000000000, 0.000000000000000000 ) ) ;
#1146=ORIENTED_EDGE ( 'NONE', *, *, #12692, .F. ) ;
#1147=VERTEX_POINT ( 'NONE', #44639 ) ;
#1148=DIRECTION ( 'NONE',  ( 0.000000000000000000, 0.000000000000000000, -1.000000000000000000 ) ) ;
#1149=VECTOR ( 'NONE', #2088, 39.37007874015748143 ) ;
#1150=ADVANCED_FACE ( 'NONE', ( #9549 ), #14943, .F. ) ;
#1151=DIRECTION ( 'NONE',  ( -1.000000000000000000, 0.000000000000000000, -0.000000000000000000 ) ) ;
#1152=VERTEX_POINT ( 'NONE', #14692 ) ;
#1153=PLANE ( 'NONE',  #23389 ) ;
#1154=DIRECTION ( 'NONE',  ( -0.000000000000000000, 1.000000000000000000, -0.000000000000000000 ) ) ;
#1156=DIRECTION ( 'NONE',  ( -0.000000000000000000, 1.000000000000000000, -0.000000000000000000 ) ) ;
#1157=ORIENTED_EDGE ( 'NONE', *, *, #179, .T. ) ;
#1158=ORIENTED_EDGE ( 'NONE', *, *, #15486, .T. ) ;
#1160=LINE ( 'NONE', #28009, #50491 ) ;
#1162=VERTEX_POINT ( 'NONE', #23435 ) ;
#1163=DIRECTION ( 'NONE',  ( -0.000000000000000000, 1.000000000000000000, -0.000000000000000000 ) ) ;
#1164=FACE_BOUND ( 'NONE', #5789, .T. ) ;
#1165=ORIENTED_EDGE ( 'NONE', *, *, #34224, .F. ) ;
#1167=ORIENTED_EDGE ( 'NONE', *, *, #11323, .F. ) ;
#1168=ORIENTED_EDGE ( 'NONE', *, *, #40374, .T. ) ;
#1171=EDGE_CURVE ( 'NONE', #33562, #2530, #34816, .T. ) ;
#1172=VERTEX_POINT ( 'NONE', #39190 ) ;
#1173=CARTESIAN_POINT ( 'NONE',  ( 0.7423782071083091516, 3.267716535433071279, 1.377952755905504256 ) ) ;
#1177=CIRCLE ( 'NONE', #314, 2.106299212598425008 ) ;
#1178=VECTOR ( 'NONE', #40202, 39.37007874015748143 ) ;
#1179=DIRECTION ( 'NONE',  ( -0.000000000000000000, 1.000000000000000000, -0.000000000000000000 ) ) ;
#1180=DIRECTION ( 'NONE',  ( -0.000000000000000000, 1.000000000000000000, -0.000000000000000000 ) ) ;
#1182=CARTESIAN_POINT ( 'NONE',  ( 0.2727639067037604947, 0.000000000000000000, -0.7874015748031473194 ) ) ;
#1183=VECTOR ( 'NONE', #10683, 39.37007874015748143 ) ;
#1184=AXIS2_PLACEMENT_3D ( 'NONE', #33536, #45363, #22407 ) ;
#1185=EDGE_CURVE ( 'NONE', #16476, #20835, #6693, .T. ) ;
#1186=EDGE_CURVE ( 'NONE', #30118, #10548, #3573, .T. ) ;
#1188=DIRECTION ( 'NONE',  ( -1.000000000000000000, 0.000000000000000000, -0.000000000000000000 ) ) ;
#1190=VECTOR ( 'NONE', #48209, 39.37007874015748143 ) ;
#1192=CARTESIAN_POINT ( 'NONE',  ( -0.07591351300297277671, 3.346456692913386100, 1.732283464566921172 ) ) ;
#1193=LINE ( 'NONE', #47628, #45436 ) ;
#1194=ORIENTED_EDGE ( 'NONE', *, *, #13124, .F. ) ;
#1195=DIRECTION ( 'NONE',  ( -0.000000000000000000, 1.000000000000000000, -0.000000000000000000 ) ) ;
#1196=DIRECTION ( 'NONE',  ( -0.000000000000000000, 1.000000000000000000, -0.000000000000000000 ) ) ;
#1198=CARTESIAN_POINT ( 'NONE',  ( 0.5455278134075212115, 3.267716535433071279, -1.259842519685035134 ) ) ;
#1201=DIRECTION ( 'NONE',  ( -3.469446951953613696E-16, 0.000000000000000000, -1.000000000000000000 ) ) ;
#1202=ORIENTED_EDGE ( 'NONE', *, *, #46352, .T. ) ;
#1203=CARTESIAN_POINT ( 'NONE',  ( 0.4696143004045479352, 0.000000000000000000, 0.7874015748031454320 ) ) ;
#1204=ADVANCED_FACE ( 'NONE', ( #15451 ), #15195, .F. ) ;
#1205=VERTEX_POINT ( 'NONE', #3318 ) ;
#1206=FACE_BOUND ( 'NONE', #41476, .T. ) ;
#1207=DIRECTION ( 'NONE',  ( -1.000000000000000000, 0.000000000000000000, 1.734723475976806848E-16 ) ) ;
#1208=CARTESIAN_POINT ( 'NONE',  ( 1.015142113812069313, 3.346456692913386100, -0.1574803149606301411 ) ) ;
#1209=CARTESIAN_POINT ( 'NONE',  ( -2.156388021673881994, 3.346456692913386100, -0.1968503937007880511 ) ) ;
#1210=EDGE_CURVE ( 'NONE', #2485, #3425, #46405, .T. ) ;
#1211=EDGE_CURVE ( 'NONE', #15158, #32340, #43047, .T. ) ;
#1213=VERTEX_POINT ( 'NONE', #7700 ) ;
#1215=LINE ( 'NONE', #28832, #18052 ) ;
#1216=EDGE_CURVE ( 'NONE', #6110, #3179, #26310, .T. ) ;
#1217=ORIENTED_EDGE ( 'NONE', *, *, #17495, .F. ) ;
#1219=DIRECTION ( 'NONE',  ( 1.734723475976806848E-16, 0.000000000000000000, 1.000000000000000000 ) ) ;
#1220=ORIENTED_EDGE ( 'NONE', *, *, #17572, .T. ) ;
#1222=VECTOR ( 'NONE', #30351, 39.37007874015748143 ) ;
#1224=ORIENTED_EDGE ( 'NONE', *, *, #41520, .F. ) ;
#1227=VECTOR ( 'NONE', #48658, 39.37007874015748143 ) ;
#1231=ORIENTED_EDGE ( 'NONE', *, *, #42981, .T. ) ;
#1232=ORIENTED_EDGE ( 'NONE', *, *, #23643, .T. ) ;
#1233=ORIENTED_EDGE ( 'NONE', *, *, #5607, .T. ) ;
#1235=ORIENTED_EDGE ( 'NONE', *, *, #21671, .F. ) ;
#1236=LINE ( 'NONE', #1490, #21314 ) ;
#1237=ORIENTED_EDGE ( 'NONE', *, *, #11037, .F. ) ;
#1239=EDGE_CURVE ( 'NONE', #36543, #39867, #49754, .T. ) ;
#1240=CARTESIAN_POINT ( 'NONE',  ( -1.166969139818015977, 3.267716535433071279, 4.048737525165546155E-16 ) ) ;
#1243=EDGE_CURVE ( 'NONE', #25538, #48074, #27054, .T. ) ;
#1244=LINE ( 'NONE', #13128, #49990 ) ;
#1246=VECTOR ( 'NONE', #36949, 39.37007874015748143 ) ;
#1247=CARTESIAN_POINT ( 'NONE',  ( 1.363819533518803029, 3.346456692913386100, -1.929133858267710666 ) ) ;
#1250=CYLINDRICAL_SURFACE ( 'NONE', #40010, 2.874015748031496731 ) ;
#1251=AXIS2_PLACEMENT_3D ( 'NONE', #33743, #49426, #37868 ) ;
#1253=LINE ( 'NONE', #39731, #35886 ) ;
#1254=ORIENTED_EDGE ( 'NONE', *, *, #45638, .T. ) ;
#1255=CARTESIAN_POINT ( 'NONE',  ( 1.363819533518803695, 3.267716535433071279, 1.681890501046755748 ) ) ;
#1257=AXIS2_PLACEMENT_3D ( 'NONE', #44252, #39878, #32398 ) ;
#1258=ORIENTED_EDGE ( 'NONE', *, *, #49705, .T. ) ;
#1260=EDGE_CURVE ( 'NONE', #22883, #35609, #10812, .T. ) ;
#1261=EDGE_LOOP ( 'NONE', ( #37406, #30893, #37324, #37824 ) ) ;
#1266=LINE ( 'NONE', #36129, #46507 ) ;
#1267=CARTESIAN_POINT ( 'NONE',  ( 2.106197740627111514, 3.267716535433070391, -1.239052911296964155 ) ) ;
#1269=CARTESIAN_POINT ( 'NONE',  ( 0.000000000000000000, 3.267716535433071279, 0.1574803149606283648 ) ) ;
#1270=DIRECTION ( 'NONE',  ( 1.000000000000000000, 0.000000000000000000, -3.469446951953613696E-16 ) ) ;
#1273=DIRECTION ( 'NONE',  ( -3.469446951953613696E-16, 0.000000000000000000, -1.000000000000000000 ) ) ;
#1274=EDGE_CURVE ( 'NONE', #25478, #18496, #10536, .T. ) ;
#1275=EDGE_LOOP ( 'NONE', ( #31845, #29624, #7999, #48821 ) ) ;
#1276=CARTESIAN_POINT ( 'NONE',  ( 1.560669927219590747, 3.267716535433071279, -0.4724409448818889246 ) ) ;
#1277=FACE_OUTER_BOUND ( 'NONE', #3325, .T. ) ;
#1281=ORIENTED_EDGE ( 'NONE', *, *, #24917, .F. ) ;
#1286=ORIENTED_EDGE ( 'NONE', *, *, #48201, .T. ) ;
#1287=CARTESIAN_POINT ( 'NONE',  ( -0.07591351300297340121, 3.346456692913386100, 0.2755905511810995412 ) ) ;
#1288=LINE ( 'NONE', #41552, #16770 ) ;
#1289=VECTOR ( 'NONE', #34121, 39.37007874015748143 ) ;
#1290=VERTEX_POINT ( 'NONE', #30186 ) ;
#1292=VECTOR ( 'NONE', #43156, 39.37007874015748143 ) ;
#1293=PLANE ( 'NONE',  #34468 ) ;
#1294=ORIENTED_EDGE ( 'NONE', *, *, #28016, .F. ) ;
#1296=VERTEX_POINT ( 'NONE', #45903 ) ;
#1299=LINE ( 'NONE', #28918, #4446 ) ;
#1300=DIRECTION ( 'NONE',  ( -3.469446951953613696E-16, 0.000000000000000000, -1.000000000000000000 ) ) ;
#1301=EDGE_LOOP ( 'NONE', ( #13180, #28397, #49854, #1740 ) ) ;
#1302=VERTEX_POINT ( 'NONE', #10566 ) ;
#1303=EDGE_CURVE ( 'NONE', #39809, #31903, #12592, .T. ) ;
#1306=EDGE_CURVE ( 'NONE', #33691, #7296, #460, .T. ) ;
#1307=CARTESIAN_POINT ( 'NONE',  ( -1.909347346926324906, 3.346456692913386100, -1.102362204724405492 ) ) ;
#1308=DIRECTION ( 'NONE',  ( -3.469446951953613696E-16, 0.000000000000000000, -1.000000000000000000 ) ) ;
#1309=EDGE_CURVE ( 'NONE', #40155, #19068, #35328, .T. ) ;
#1310=DIRECTION ( 'NONE',  ( 1.734723475976806848E-16, 0.000000000000000000, 1.000000000000000000 ) ) ;
#1311=LINE ( 'NONE', #12418, #13606 ) ;
#1312=EDGE_CURVE ( 'NONE', #41751, #18135, #36094, .T. ) ;
#1313=DIRECTION ( 'NONE',  ( 0.000000000000000000, 1.000000000000000000, 0.000000000000000000 ) ) ;
#1314=ORIENTED_EDGE ( 'NONE', *, *, #43415, .F. ) ;
#1315=DIRECTION ( 'NONE',  ( 0.000000000000000000, 0.000000000000000000, -1.000000000000000000 ) ) ;
#1316=LINE ( 'NONE', #17580, #7907 ) ;
#1317=VECTOR ( 'NONE', #50449, 39.37007874015748143 ) ;
#1319=VERTEX_POINT ( 'NONE', #4853 ) ;
#1321=EDGE_LOOP ( 'NONE', ( #14358, #29914, #16565, #8986 ) ) ;
#1322=LINE ( 'NONE', #44929, #7595 ) ;
#1323=CARTESIAN_POINT ( 'NONE',  ( -1.363819533518803473, 3.232777166330603524, 2.047244094488179567 ) ) ;
#1325=AXIS2_PLACEMENT_3D ( 'NONE', #17612, #33631, #45208 ) ;
#1326=EDGE_LOOP ( 'NONE', ( #37731, #21247, #33641, #22836 ) ) ;
#1327=AXIS2_PLACEMENT_3D ( 'NONE', #15441, #20052, #31187 ) ;
#1330=CARTESIAN_POINT ( 'NONE',  ( 2.182111253630085290, 3.267716535433071279, 0.6299212598425161236 ) ) ;
#1332=ORIENTED_EDGE ( 'NONE', *, *, #7973, .T. ) ;
#1334=DIRECTION ( 'NONE',  ( -0.000000000000000000, 1.000000000000000000, -0.000000000000000000 ) ) ;
#1335=ORIENTED_EDGE ( 'NONE', *, *, #8664, .F. ) ;
#1336=VERTEX_POINT ( 'NONE', #47919 ) ;
#1338=CARTESIAN_POINT ( 'NONE',  ( -0.5455278134075214336, 3.346456692913386100, -0.8267716535433049518 ) ) ;
#1340=VERTEX_POINT ( 'NONE', #43815 ) ;
#1341=DIRECTION ( 'NONE',  ( 1.734723475976806848E-16, -0.000000000000000000, 1.000000000000000000 ) ) ;
#1345=EDGE_LOOP ( 'NONE', ( #14466, #13105, #2271, #43670 ) ) ;
#1347=CARTESIAN_POINT ( 'NONE',  ( -1.091055626815042645, 3.346456692913386100, -0.8267716535433052849 ) ) ;
#1348=DIRECTION ( 'NONE',  ( 1.734723475976806848E-16, -0.000000000000000000, 1.000000000000000000 ) ) ;
#1350=VERTEX_POINT ( 'NONE', #4091 ) ;
#1351=DIRECTION ( 'NONE',  ( -1.000000000000000000, 0.000000000000000000, -0.000000000000000000 ) ) ;
#1352=DIRECTION ( 'NONE',  ( -1.000000000000000000, 0.000000000000000000, -0.000000000000000000 ) ) ;
#1355=CYLINDRICAL_SURFACE ( 'NONE', #10134, 2.165354330708661568 ) ;
#1356=ORIENTED_EDGE ( 'NONE', *, *, #31505, .T. ) ;
#1357=EDGE_LOOP ( 'NONE', ( #4836, #40485, #13324, #36088 ) ) ;
#1358=PLANE ( 'NONE',  #28689 ) ;
#1359=CIRCLE ( 'NONE', #13716, 2.106299212598425008 ) ;
#1360=DIRECTION ( 'NONE',  ( -0.000000000000000000, 1.000000000000000000, -0.000000000000000000 ) ) ;
#1361=VECTOR ( 'NONE', #15893, 39.37007874015748143 ) ;
#1362=CARTESIAN_POINT ( 'NONE',  ( 0.000000000000000000, 3.346456692913386100, 0.000000000000000000 ) ) ;
#1363=LINE ( 'NONE', #24092, #9840 ) ;
#1364=ORIENTED_EDGE ( 'NONE', *, *, #483, .T. ) ;
#1365=VERTEX_POINT ( 'NONE', #12855 ) ;
#1366=VECTOR ( 'NONE', #23366, 39.37007874015748143 ) ;
#1367=EDGE_CURVE ( 'NONE', #42304, #46532, #29108, .T. ) ;
#1369=ORIENTED_EDGE ( 'NONE', *, *, #49691, .T. ) ;
#1370=DIRECTION ( 'NONE',  ( -1.000000000000000000, 0.000000000000000000, 1.734723475976806848E-16 ) ) ;
#1371=CARTESIAN_POINT ( 'NONE',  ( -0.8182917201112819283, 3.346456692913386100, 1.850393700787391849 ) ) ;
#1372=EDGE_CURVE ( 'NONE', #32862, #32147, #47663, .T. ) ;
#1373=EDGE_CURVE ( 'NONE', #37743, #48914, #20594, .T. ) ;
#1374=EDGE_CURVE ( 'NONE', #23037, #1172, #36966, .T. ) ;
#1375=PLANE ( 'NONE',  #9364 ) ;
#1380=LINE ( 'NONE', #24881, #34779 ) ;
#1382=FACE_OUTER_BOUND ( 'NONE', #42254, .T. ) ;
#1383=CARTESIAN_POINT ( 'NONE',  ( -0.2727639067037607168, 3.267716535433071279, 4.731699523581612206E-17 ) ) ;
#1384=ADVANCED_FACE ( 'NONE', ( #47408 ), #19561, .F. ) ;
#1386=ORIENTED_EDGE ( 'NONE', *, *, #5098, .F. ) ;
#1387=VECTOR ( 'NONE', #5887, 39.37007874015748143 ) ;
#1389=CARTESIAN_POINT ( 'NONE',  ( 1.015142113812069313, 0.000000000000000000, -1.299212598425193210 ) ) ;
#1390=VECTOR ( 'NONE', #8484, 39.37007874015748143 ) ;
#1394=LINE ( 'NONE', #16384, #47596 ) ;
#1395=VERTEX_POINT ( 'NONE', #20068 ) ;
#1396=PLANE ( 'NONE',  #35293 ) ;
#1397=PLANE ( 'NONE',  #49846 ) ;
#1398=PLANE ( 'NONE',  #31292 ) ;
#1399=CARTESIAN_POINT ( 'NONE',  ( -1.363819533518803473, 3.346456692913386100, -1.732283464566922726 ) ) ;
#1400=CIRCLE ( 'NONE', #26130, 2.165354330708661568 ) ;
#1401=ADVANCED_FACE ( 'NONE', ( #41191 ), #15697, .F. ) ;
#1403=VECTOR ( 'NONE', #33369, 39.37007874015748143 ) ;
#1404=EDGE_LOOP ( 'NONE', ( #33045, #20964, #12498, #39924 ) ) ;
#1405=VERTEX_POINT ( 'NONE', #23697 ) ;
#1407=PLANE ( 'NONE',  #5666 ) ;
#1408=ORIENTED_EDGE ( 'NONE', *, *, #4605, .T. ) ;
#1409=FACE_OUTER_BOUND ( 'NONE', #9486, .T. ) ;
#1411=DIRECTION ( 'NONE',  ( -3.469446951953613696E-16, 0.000000000000000000, -1.000000000000000000 ) ) ;
#1412=EDGE_CURVE ( 'NONE', #16466, #39052, #35835, .T. ) ;
#1413=LINE ( 'NONE', #40154, #1767 ) ;
#1414=ORIENTED_EDGE ( 'NONE', *, *, #46798, .F. ) ;
#1416=CARTESIAN_POINT ( 'NONE',  ( 1.363819533518803029, 0.000000000000000000, -1.929133858267710666 ) ) ;
#1418=LINE ( 'NONE', #33441, #21438 ) ;
#1419=ORIENTED_EDGE ( 'NONE', *, *, #7625, .T. ) ;
#1421=FACE_BOUND ( 'NONE', #15515, .T. ) ;
#1422=EDGE_LOOP ( 'NONE', ( #48854, #9068, #24586, #5617 ) ) ;
#1423=EDGE_CURVE ( 'NONE', #14385, #23466, #4592, .T. ) ;
#1424=CARTESIAN_POINT ( 'NONE',  ( -0.2727639067037602727, 3.267716535433071279, 1.535433070866133898 ) ) ;
#1425=VERTEX_POINT ( 'NONE', #46288 ) ;
#1427=DIRECTION ( 'NONE',  ( 1.734723475976806848E-16, 0.000000000000000000, 1.000000000000000000 ) ) ;
#1430=VECTOR ( 'NONE', #29772, 39.37007874015748143 ) ;
#1431=ORIENTED_EDGE ( 'NONE', *, *, #17621, .T. ) ;
#1433=ORIENTED_EDGE ( 'NONE', *, *, #4896, .T. ) ;
#1437=LINE ( 'NONE', #21826, #23418 ) ;
#1438=EDGE_CURVE ( 'NONE', #4136, #10342, #34202, .T. ) ;
#1439=CARTESIAN_POINT ( 'NONE',  ( -0.2727639067037602172, 3.346456692913386100, 0.7874015748031456541 ) ) ;
#1440=EDGE_CURVE ( 'NONE', #20848, #17201, #14828, .T. ) ;
#1441=CARTESIAN_POINT ( 'NONE',  ( -2.142325647309101022, 3.346456692913386100, -0.3149606299212589500 ) ) ;
#1442=DIRECTION ( 'NONE',  ( -1.000000000000000000, 0.000000000000000000, 0.000000000000000000 ) ) ;
#1443=VERTEX_POINT ( 'NONE', #26690 ) ;
#1444=CARTESIAN_POINT ( 'NONE',  ( 0.000000000000000000, 3.267716535433071279, 1.377952755905504256 ) ) ;
#1446=CARTESIAN_POINT ( 'NONE',  ( -1.363819533518803029, 3.267716535433071279, -0.03937007874015868020 ) ) ;
#1447=EDGE_LOOP ( 'NONE', ( #36747, #1419, #41092, #39920 ) ) ;
#1449=DIRECTION ( 'NONE',  ( -0.000000000000000000, 1.000000000000000000, -0.000000000000000000 ) ) ;
#1450=ORIENTED_EDGE ( 'NONE', *, *, #40215, .T. ) ;
#1452=DIRECTION ( 'NONE',  ( 1.734723475976806848E-16, -0.000000000000000000, 1.000000000000000000 ) ) ;
#1454=ORIENTED_EDGE ( 'NONE', *, *, #28750, .F. ) ;
#1455=CARTESIAN_POINT ( 'NONE',  ( -1.985260859929298016, 3.346456692913386100, -0.6299212598425177889 ) ) ;
#1456=ORIENTED_EDGE ( 'NONE', *, *, #18152, .T. ) ;
#1457=FACE_BOUND ( 'NONE', #25360, .T. ) ;
#1458=CARTESIAN_POINT ( 'NONE',  ( -1.166969139818015977, 0.000000000000000000, -1.732283464566922726 ) ) ;
#1459=LINE ( 'NONE', #49673, #20174 ) ;
#1462=AXIS2_PLACEMENT_3D ( 'NONE', #47954, #8246, #20103 ) ;
#1463=EDGE_CURVE ( 'NONE', #9823, #30686, #41688, .T. ) ;
#1465=ORIENTED_EDGE ( 'NONE', *, *, #35217, .T. ) ;
#1469=LINE ( 'NONE', #41231, #13722 ) ;
#1470=ORIENTED_EDGE ( 'NONE', *, *, #10486, .F. ) ;
#1472=LINE ( 'NONE', #48168, #1735 ) ;
#1473=EDGE_CURVE ( 'NONE', #12064, #14934, #38077, .T. ) ;
#1474=ORIENTED_EDGE ( 'NONE', *, *, #15341, .T. ) ;
#1476=ADVANCED_FACE ( 'NONE', ( #34453 ), #45784, .F. ) ;
#1478=DIRECTION ( 'NONE',  ( 1.000000000000000000, 0.000000000000000000, 0.000000000000000000 ) ) ;
#1479=ORIENTED_EDGE ( 'NONE', *, *, #12340, .F. ) ;
#1480=ADVANCED_FACE ( 'NONE', ( #37572 ), #33706, .F. ) ;
#1481=DIRECTION ( 'NONE',  ( 1.000000000000000000, 0.000000000000000000, 0.000000000000000000 ) ) ;
#1482=ORIENTED_EDGE ( 'NONE', *, *, #49175, .T. ) ;
#1483=ORIENTED_EDGE ( 'NONE', *, *, #43029, .F. ) ;
#1485=EDGE_LOOP ( 'NONE', ( #11618, #41738, #39037, #40316 ) ) ;
#1486=VERTEX_POINT ( 'NONE', #26190 ) ;
#1487=DIRECTION ( 'NONE',  ( -0.000000000000000000, 1.000000000000000000, -0.000000000000000000 ) ) ;
#1488=LINE ( 'NONE', #43185, #46966 ) ;
#1490=CARTESIAN_POINT ( 'NONE',  ( -1.091055626815042645, 3.346456692913386100, -1.889763779527552146 ) ) ;
#1491=VERTEX_POINT ( 'NONE', #49138 ) ;
#1498=ORIENTED_EDGE ( 'NONE', *, *, #4933, .F. ) ;
#1499=CARTESIAN_POINT ( 'NONE',  ( -1.636583440222563635, 3.267716535433071279, 0.3149606299212578953 ) ) ;
#1502=EDGE_LOOP ( 'NONE', ( #31771, #38803, #42664, #49372 ) ) ;
#1503=LINE ( 'NONE', #17260, #1060 ) ;
#1504=CARTESIAN_POINT ( 'NONE',  ( 0.8182917201112819283, 0.000000000000000000, 0.7874015748031454320 ) ) ;
#1505=CIRCLE ( 'NONE', #22115, 2.106299212598425008 ) ;
#1506=CARTESIAN_POINT ( 'NONE',  ( 0.7423782071083092626, 3.267716535433071279, 2.204724409448808764 ) ) ;
#1507=DIRECTION ( 'NONE',  ( 0.000000000000000000, -1.000000000000000000, 0.000000000000000000 ) ) ;
#1509=VECTOR ( 'NONE', #3169, 39.37007874015748143 ) ;
#1511=ORIENTED_EDGE ( 'NONE', *, *, #45175, .T. ) ;
#1512=DIRECTION ( 'NONE',  ( -1.000000000000000000, 0.000000000000000000, -0.000000000000000000 ) ) ;
#1513=LINE ( 'NONE', #25260, #357 ) ;
#1514=EDGE_CURVE ( 'NONE', #39073, #15435, #17686, .T. ) ;
#1515=AXIS2_PLACEMENT_3D ( 'NONE', #11770, #3779, #19010 ) ;
#1518=VECTOR ( 'NONE', #37521, 39.37007874015748143 ) ;
#1519=ORIENTED_EDGE ( 'NONE', *, *, #19813, .F. ) ;
#1522=DIRECTION ( 'NONE',  ( 1.734723475976806848E-16, -0.000000000000000000, 1.000000000000000000 ) ) ;
#1524=LINE ( 'NONE', #1007, #42561 ) ;
#1525=ORIENTED_EDGE ( 'NONE', *, *, #27749, .T. ) ;
#1526=PLANE ( 'NONE',  #10949 ) ;
#1527=LINE ( 'NONE', #1778, #6484 ) ;
#1530=ORIENTED_EDGE ( 'NONE', *, *, #41636, .F. ) ;
#1531=LINE ( 'NONE', #5402, #7913 ) ;
#1534=VECTOR ( 'NONE', #39883, 39.37007874015748143 ) ;
#1536=ADVANCED_FACE ( 'NONE', ( #25680 ), #6062, .F. ) ;
#1537=ADVANCED_FACE ( 'NONE', ( #42687 ), #22828, .F. ) ;
#1544=FACE_BOUND ( 'NONE', #39627, .T. ) ;
#1545=ORIENTED_EDGE ( 'NONE', *, *, #36924, .T. ) ;
#1547=CARTESIAN_POINT ( 'NONE',  ( 1.091055626815042645, 3.346456692913386100, 1.259842519685033357 ) ) ;
#1548=LINE ( 'NONE', #17803, #48888 ) ;
#1551=CARTESIAN_POINT ( 'NONE',  ( -2.182111253630085290, 3.267716535433071279, 0.9448818897637749625 ) ) ;
#1552=CARTESIAN_POINT ( 'NONE',  ( -0.07591351300297340121, 0.000000000000000000, -0.6692913385826758654 ) ) ;
#1555=EDGE_CURVE ( 'NONE', #37961, #7571, #46783, .T. ) ;
#1556=VECTOR ( 'NONE', #7667, 39.37007874015748143 ) ;
#1558=CARTESIAN_POINT ( 'NONE',  ( 4.268512490100411402E-16, 0.000000000000000000, 1.259842519685033357 ) ) ;
#1564=ORIENTED_EDGE ( 'NONE', *, *, #13652, .T. ) ;
#1568=EDGE_CURVE ( 'NONE', #14018, #21172, #31081, .T. ) ;
#1569=LINE ( 'NONE', #21447, #24143 ) ;
#1571=CARTESIAN_POINT ( 'NONE',  ( 1.363819533518803251, 0.000000000000000000, -0.3543307086614178592 ) ) ;
#1573=VECTOR ( 'NONE', #27421, 39.37007874015748143 ) ;
#1574=LINE ( 'NONE', #41080, #47272 ) ;
#1575=ORIENTED_EDGE ( 'NONE', *, *, #47162, .T. ) ;
#1576=CARTESIAN_POINT ( 'NONE',  ( -1.091055626815042201, 0.000000000000000000, 1.377952755905504256 ) ) ;
#1578=VERTEX_POINT ( 'NONE', #35709 ) ;
#1579=ORIENTED_EDGE ( 'NONE', *, *, #15201, .F. ) ;
#1580=VECTOR ( 'NONE', #29287, 39.37007874015748143 ) ;
#1581=AXIS2_PLACEMENT_3D ( 'NONE', #2961, #22331, #45285 ) ;
#1582=FACE_OUTER_BOUND ( 'NONE', #36479, .T. ) ;
#1583=PLANE ( 'NONE',  #13002 ) ;
#1584=VERTEX_POINT ( 'NONE', #50386 ) ;
#1585=AXIS2_PLACEMENT_3D ( 'NONE', #26722, #41973, #14607 ) ;
#1586=ORIENTED_EDGE ( 'NONE', *, *, #43598, .F. ) ;
#1587=DIRECTION ( 'NONE',  ( -0.000000000000000000, 1.000000000000000000, -0.000000000000000000 ) ) ;
#1588=VECTOR ( 'NONE', #4753, 39.37007874015748143 ) ;
#1589=EDGE_LOOP ( 'NONE', ( #50913, #7896, #28381, #9176, #15019 ) ) ;
#1590=CARTESIAN_POINT ( 'NONE',  ( -1.909347346926324906, 0.000000000000000000, 1.220472440944875059 ) ) ;
#1591=CARTESIAN_POINT ( 'NONE',  ( -0.3486774197067334935, 3.346456692913386100, 1.062992125984246083 ) ) ;
#1595=ORIENTED_EDGE ( 'NONE', *, *, #15115, .T. ) ;
#1596=LINE ( 'NONE', #40340, #9833 ) ;
#1598=ORIENTED_EDGE ( 'NONE', *, *, #35690, .T. ) ;
#1599=VERTEX_POINT ( 'NONE', #39075 ) ;
#1600=LINE ( 'NONE', #18365, #23163 ) ;
#1601=CARTESIAN_POINT ( 'NONE',  ( 0.8182917201112819283, 3.267716535433071279, -0.3543307086614175816 ) ) ;
#1602=CARTESIAN_POINT ( 'NONE',  ( -1.166969139818015755, 3.346456692913386100, 1.220472440944875281 ) ) ;
#1603=EDGE_CURVE ( 'NONE', #50064, #21920, #50634, .T. ) ;
#1604=VERTEX_POINT ( 'NONE', #15328 ) ;
#1605=DIRECTION ( 'NONE',  ( -3.469446951953613696E-16, 0.000000000000000000, -1.000000000000000000 ) ) ;
#1606=DIRECTION ( 'NONE',  ( 1.000000000000000000, 0.000000000000000000, 0.000000000000000000 ) ) ;
#1609=ORIENTED_EDGE ( 'NONE', *, *, #38867, .T. ) ;
#1610=CARTESIAN_POINT ( 'NONE',  ( 3.927031490892378253E-16, 3.267716535433071279, 1.062992125984246083 ) ) ;
#1611=DIRECTION ( 'NONE',  ( 0.000000000000000000, -1.000000000000000000, 0.000000000000000000 ) ) ;
#1612=DIRECTION ( 'NONE',  ( 1.000000000000000000, 0.000000000000000000, 0.000000000000000000 ) ) ;
#1613=ORIENTED_EDGE ( 'NONE', *, *, #5854, .F. ) ;
#1614=EDGE_LOOP ( 'NONE', ( #22471, #18066, #13906, #37039 ) ) ;
#1616=CARTESIAN_POINT ( 'NONE',  ( -0.07591351300297340121, 0.000000000000000000, -0.9842519685039344823 ) ) ;
#1617=EDGE_CURVE ( 'NONE', #31137, #15706, #11703, .T. ) ;
#1622=VERTEX_POINT ( 'NONE', #3453 ) ;
#1623=EDGE_CURVE ( 'NONE', #6479, #17812, #34954, .T. ) ;
#1626=VERTEX_POINT ( 'NONE', #16088 ) ;
#1627=DIRECTION ( 'NONE',  ( 1.734723475976806848E-16, -0.000000000000000000, 1.000000000000000000 ) ) ;
#1628=CARTESIAN_POINT ( 'NONE',  ( -0.6214413264104945434, 3.267716535433071279, -0.4724409448818886470 ) ) ;
#1629=DIRECTION ( 'NONE',  ( -1.000000000000000000, 0.000000000000000000, 1.734723475976806848E-16 ) ) ;
#1630=DIRECTION ( 'NONE',  ( -3.469446951953613696E-16, 0.000000000000000000, -1.000000000000000000 ) ) ;
#1631=LINE ( 'NONE', #45228, #6467 ) ;
#1632=ORIENTED_EDGE ( 'NONE', *, *, #21926, .T. ) ;
#1634=CARTESIAN_POINT ( 'NONE',  ( 1.091055626815043311, 3.346456692913386100, 1.692913385826762873 ) ) ;
#1635=ORIENTED_EDGE ( 'NONE', *, *, #24237, .F. ) ;
#1636=DIRECTION ( 'NONE',  ( -0.000000000000000000, 0.000000000000000000, 1.000000000000000000 ) ) ;
#1638=FACE_OUTER_BOUND ( 'NONE', #3691, .T. ) ;
#1641=LINE ( 'NONE', #34358, #40692 ) ;
#1642=LINE ( 'NONE', #41399, #24250 ) ;
#1644=VERTEX_POINT ( 'NONE', #27442 ) ;
#1647=EDGE_LOOP ( 'NONE', ( #27290, #42930, #46936, #29764 ) ) ;
#1648=CARTESIAN_POINT ( 'NONE',  ( 0.8182917201112818173, 3.267716535433071279, -1.419509857074483292E-16 ) ) ;
#1649=AXIS2_PLACEMENT_3D ( 'NONE', #34585, #15464, #50270 ) ;
#1652=DIRECTION ( 'NONE',  ( -1.000000000000000000, 0.000000000000000000, -0.000000000000000000 ) ) ;
#1654=LINE ( 'NONE', #9919, #37011 ) ;
#1655=EDGE_CURVE ( 'NONE', #26751, #21978, #78, .T. ) ;
#1657=ORIENTED_EDGE ( 'NONE', *, *, #42499, .F. ) ;
#1659=LINE ( 'NONE', #17410, #31240 ) ;
#1661=EDGE_LOOP ( 'NONE', ( #33119, #48791, #28504, #6328 ) ) ;
#1663=LINE ( 'NONE', #25160, #17034 ) ;
#1664=AXIS2_PLACEMENT_3D ( 'NONE', #17091, #44942, #28694 ) ;
#1666=EDGE_CURVE ( 'NONE', #11390, #7825, #23318, .T. ) ;
#1670=EDGE_CURVE ( 'NONE', #44829, #1816, #12215, .T. ) ;
#1672=LINE ( 'NONE', #45024, #35703 ) ;
#1673=DIRECTION ( 'NONE',  ( -0.000000000000000000, 1.000000000000000000, -0.000000000000000000 ) ) ;
#1674=ADVANCED_FACE ( 'NONE', ( #11206 ), #38579, .F. ) ;
#1675=VERTEX_POINT ( 'NONE', #7336 ) ;
#1676=LINE ( 'NONE', #22319, #43793 ) ;
#1677=FACE_BOUND ( 'NONE', #2315, .T. ) ;
#1680=EDGE_LOOP ( 'NONE', ( #9632, #27406, #21404, #44753 ) ) ;
#1681=VERTEX_POINT ( 'NONE', #8341 ) ;
#1682=DIRECTION ( 'NONE',  ( 1.000000000000000000, 0.000000000000000000, -3.469446951953613696E-16 ) ) ;
#1683=EDGE_CURVE ( 'NONE', #28119, #24628, #44465, .T. ) ;
#1687=ORIENTED_EDGE ( 'NONE', *, *, #19498, .T. ) ;
#1689=PLANE ( 'NONE',  #49156 ) ;
#1690=DIRECTION ( 'NONE',  ( 1.734723475976806848E-16, -0.000000000000000000, 1.000000000000000000 ) ) ;
#1691=VECTOR ( 'NONE', #12297, 39.37007874015748143 ) ;
#1693=EDGE_CURVE ( 'NONE', #39686, #6600, #20983, .T. ) ;
#1694=CARTESIAN_POINT ( 'NONE',  ( -1.909347346926324906, 3.346456692913386100, -0.4724409448818884805 ) ) ;
#1697=CARTESIAN_POINT ( 'NONE',  ( -1.091055626815042645, 0.000000000000000000, -0.1968503937007881899 ) ) ;
#1698=EDGE_LOOP ( 'NONE', ( #13563, #37310, #36206, #29821 ) ) ;
#1702=CARTESIAN_POINT ( 'NONE',  ( -1.166969139818015977, 0.000000000000000000, 2.047244094488179567 ) ) ;
#1704=DIRECTION ( 'NONE',  ( -0.000000000000000000, 1.000000000000000000, -0.000000000000000000 ) ) ;
#1708=DIRECTION ( 'NONE',  ( -1.000000000000000000, -0.000000000000000000, -0.000000000000000000 ) ) ;
#1711=LINE ( 'NONE', #41721, #35410 ) ;
#1712=ORIENTED_EDGE ( 'NONE', *, *, #9689, .F. ) ;
#1713=FACE_BOUND ( 'NONE', #5681, .T. ) ;
#1714=PLANE ( 'NONE',  #46503 ) ;
#1715=DIRECTION ( 'NONE',  ( -3.469446951953613696E-16, 0.000000000000000000, -1.000000000000000000 ) ) ;
#1716=CARTESIAN_POINT ( 'NONE',  ( -2.142325647309101022, 3.267716535433071279, 0.3149606299212578953 ) ) ;
#1717=ORIENTED_EDGE ( 'NONE', *, *, #34571, .T. ) ;
#1718=EDGE_LOOP ( 'NONE', ( #24085, #45191, #49058, #2610 ) ) ;
#1719=CARTESIAN_POINT ( 'NONE',  ( 0.8182917201112824834, 3.346456692913386100, 1.940849049717691122 ) ) ;
#1721=CARTESIAN_POINT ( 'NONE',  ( -0.8942052331142552601, 0.000000000000000000, -0.5118110236220467790 ) ) ;
#1722=EDGE_LOOP ( 'NONE', ( #36845, #4176, #19214, #50603 ) ) ;
#1724=AXIS2_PLACEMENT_3D ( 'NONE', #17826, #2082, #41078 ) ;
#1725=DIRECTION ( 'NONE',  ( -1.000000000000000000, 0.000000000000000000, 1.734723475976806848E-16 ) ) ;
#1726=VECTOR ( 'NONE', #37882, 39.37007874015748143 ) ;
#1727=EDGE_CURVE ( 'NONE', #31288, #35644, #1505, .T. ) ;
#1732=ORIENTED_EDGE ( 'NONE', *, *, #8597, .F. ) ;
#1733=CARTESIAN_POINT ( 'NONE',  ( 0.1968503937007870241, 0.000000000000000000, -1.889763779527552146 ) ) ;
#1735=VECTOR ( 'NONE', #32990, 39.37007874015748143 ) ;
#1737=ORIENTED_EDGE ( 'NONE', *, *, #27170, .T. ) ;
#1740=ORIENTED_EDGE ( 'NONE', *, *, #17841, .F. ) ;
#1741=DIRECTION ( 'NONE',  ( 1.000000000000000000, 0.000000000000000000, -3.469446951953613696E-16 ) ) ;
#1742=ORIENTED_EDGE ( 'NONE', *, *, #31920, .T. ) ;
#1744=ADVANCED_FACE ( 'NONE', ( #4979 ), #1358, .F. ) ;
#1746=VERTEX_POINT ( 'NONE', #4727 ) ;
#1747=DIRECTION ( 'NONE',  ( -3.469446951953613696E-16, 0.000000000000000000, -1.000000000000000000 ) ) ;
#1749=VERTEX_POINT ( 'NONE', #28970 ) ;
#1750=FACE_OUTER_BOUND ( 'NONE', #45333, .T. ) ;
#1752=AXIS2_PLACEMENT_3D ( 'NONE', #8218, #27822, #27568 ) ;
#1753=CARTESIAN_POINT ( 'NONE',  ( -1.195183497228115035E-16, 0.000000000000000000, -0.3149606299212591165 ) ) ;
#1754=ADVANCED_FACE ( 'NONE', ( #24603 ), #12464, .F. ) ;
#1756=VECTOR ( 'NONE', #17200, 39.37007874015748143 ) ;
#1758=CARTESIAN_POINT ( 'NONE',  ( 0.000000000000000000, 3.267716535433071279, 1.259842519685033357 ) ) ;
#1759=VERTEX_POINT ( 'NONE', #20719 ) ;
#1760=DIRECTION ( 'NONE',  ( -1.000000000000000000, -0.000000000000000000, -0.000000000000000000 ) ) ;
#1763=AXIS2_PLACEMENT_3D ( 'NONE', #9871, #37757, #5743 ) ;
#1764=ORIENTED_EDGE ( 'NONE', *, *, #34871, .F. ) ;
#1765=CARTESIAN_POINT ( 'NONE',  ( -0.07591351300297316529, 3.267716535433071279, 2.633779063002562669E-17 ) ) ;
#1767=VECTOR ( 'NONE', #4520, 39.37007874015748143 ) ;
#1768=VERTEX_POINT ( 'NONE', #32878 ) ;
#1770=EDGE_CURVE ( 'NONE', #2803, #35147, #32616, .T. ) ;
#1772=VECTOR ( 'NONE', #28811, 39.37007874015748143 ) ;
#1773=CARTESIAN_POINT ( 'NONE',  ( -1.091055626815042645, 0.000000000000000000, -0.6299212598425177889 ) ) ;
#1776=EDGE_LOOP ( 'NONE', ( #15327, #17178, #12022, #18609 ) ) ;
#1778=CARTESIAN_POINT ( 'NONE',  ( 1.560669927219591413, 3.346456692913386100, 1.732283464566921172 ) ) ;
#1783=EDGE_CURVE ( 'NONE', #40457, #35065, #13244, .T. ) ;
#1785=DIRECTION ( 'NONE',  ( 1.734723475976806848E-16, -0.000000000000000000, 1.000000000000000000 ) ) ;
#1786=LINE ( 'NONE', #22181, #28170 ) ;
#1787=ADVANCED_FACE ( 'NONE', ( #27955 ), #39833, .F. ) ;
#1788=LINE ( 'NONE', #21928, #21403 ) ;
#1789=EDGE_CURVE ( 'NONE', #26586, #34031, #38975, .T. ) ;
#1790=ORIENTED_EDGE ( 'NONE', *, *, #32995, .F. ) ;
#1791=ORIENTED_EDGE ( 'NONE', *, *, #3018, .T. ) ;
#1792=CARTESIAN_POINT ( 'NONE',  ( 4.097771990496412577E-16, 3.346456692913386100, 2.106299212598425008 ) ) ;
#1794=FACE_BOUND ( 'NONE', #50025, .T. ) ;
#1795=ORIENTED_EDGE ( 'NONE', *, *, #21839, .F. ) ;
#1796=AXIS2_PLACEMENT_3D ( 'NONE', #21511, #1892, #40382 ) ;
#1798=LINE ( 'NONE', #21425, #50069 ) ;
#1799=PLANE ( 'NONE',  #32439 ) ;
#1800=ORIENTED_EDGE ( 'NONE', *, *, #34831, .T. ) ;
#1801=VERTEX_POINT ( 'NONE', #16251 ) ;
#1802=CARTESIAN_POINT ( 'NONE',  ( -1.166969139818015977, 3.267716535433071279, 1.732283464566920950 ) ) ;
#1803=VECTOR ( 'NONE', #44755, 39.37007874015748143 ) ;
#1806=ORIENTED_EDGE ( 'NONE', *, *, #35108, .T. ) ;
#1808=ORIENTED_EDGE ( 'NONE', *, *, #48554, .F. ) ;
#1809=DIRECTION ( 'NONE',  ( 1.734723475976806848E-16, 0.000000000000000000, 1.000000000000000000 ) ) ;
#1810=VECTOR ( 'NONE', #40053, 39.37007874015748143 ) ;
#1812=FACE_OUTER_BOUND ( 'NONE', #1326, .T. ) ;
#1815=ORIENTED_EDGE ( 'NONE', *, *, #33358, .T. ) ;
#1816=VERTEX_POINT ( 'NONE', #43344 ) ;
#1818=PLANE ( 'NONE',  #7661 ) ;
#1819=LINE ( 'NONE', #40304, #19353 ) ;
#1820=EDGE_CURVE ( 'NONE', #13717, #20069, #3359, .T. ) ;
#1821=CARTESIAN_POINT ( 'NONE',  ( 1.015142113812069091, 3.253856391387305536, -2.229897935479296045 ) ) ;
#1825=CARTESIAN_POINT ( 'NONE',  ( -2.061297163897529483, 3.267716535433071279, 0.4330708661417290162 ) ) ;
#1826=ADVANCED_FACE ( 'NONE', ( #7990 ), #27856, .F. ) ;
#1827=ORIENTED_EDGE ( 'NONE', *, *, #3133, .T. ) ;
#1828=CARTESIAN_POINT ( 'NONE',  ( -0.6214413264104939882, 3.267716535433071279, 1.535433070866133898 ) ) ;
#1829=LINE ( 'NONE', #40563, #10390 ) ;
#1831=VERTEX_POINT ( 'NONE', #46693 ) ;
#1834=AXIS2_PLACEMENT_3D ( 'NONE', #15753, #31513, #47209 ) ;
#1836=ORIENTED_EDGE ( 'NONE', *, *, #33749, .F. ) ;
#1837=VECTOR ( 'NONE', #23812, 39.37007874015748143 ) ;
#1838=ORIENTED_EDGE ( 'NONE', *, *, #44996, .T. ) ;
#1840=VECTOR ( 'NONE', #44776, 39.37007874015748143 ) ;
#1841=EDGE_CURVE ( 'NONE', #33606, #24319, #3868, .T. ) ;
#1842=EDGE_LOOP ( 'NONE', ( #30346, #11606, #34513, #5960 ) ) ;
#1843=AXIS2_PLACEMENT_3D ( 'NONE', #16566, #20425, #811 ) ;
#1844=CARTESIAN_POINT ( 'NONE',  ( -1.195183497228115035E-16, 3.346456692913386100, -0.6299212598425177889 ) ) ;
#1846=CARTESIAN_POINT ( 'NONE',  ( 2.106197740627111958, 3.346456692913386100, 0.9055118110236164419 ) ) ;
#1847=EDGE_CURVE ( 'NONE', #17810, #1039, #27094, .T. ) ;
#1848=ORIENTED_EDGE ( 'NONE', *, *, #23704, .F. ) ;
#1850=CARTESIAN_POINT ( 'NONE',  ( -1.091055626815042645, 0.000000000000000000, -7.512581982576723358E-16 ) ) ;
#1853=EDGE_LOOP ( 'NONE', ( #21363, #32081, #38553, #8334 ) ) ;
#1855=CARTESIAN_POINT ( 'NONE',  ( -0.8182917201112814842, 3.346456692913386100, 0.2755905511810998187 ) ) ;
#1857=ORIENTED_EDGE ( 'NONE', *, *, #46260, .T. ) ;
#1859=LINE ( 'NONE', #45203, #33289 ) ;
#1860=DIRECTION ( 'NONE',  ( -3.469446951953613696E-16, 0.000000000000000000, -1.000000000000000000 ) ) ;
#1861=ORIENTED_EDGE ( 'NONE', *, *, #31742, .T. ) ;
#1863=LINE ( 'NONE', #30253, #34328 ) ;
#1864=LINE ( 'NONE', #10380, #46254 ) ;
#1871=EDGE_LOOP ( 'NONE', ( #19907, #19633, #9084, #50749 ) ) ;
#1872=VERTEX_POINT ( 'NONE', #31489 ) ;
#1873=VECTOR ( 'NONE', #38631, 39.37007874015748143 ) ;
#1876=ORIENTED_EDGE ( 'NONE', *, *, #27813, .F. ) ;
#1877=FACE_OUTER_BOUND ( 'NONE', #19574, .T. ) ;
#1879=VECTOR ( 'NONE', #23022, 39.37007874015748143 ) ;
#1881=EDGE_CURVE ( 'NONE', #44810, #17605, #4374, .T. ) ;
#1883=EDGE_CURVE ( 'NONE', #18808, #35441, #39487, .T. ) ;
#1885=FACE_OUTER_BOUND ( 'NONE', #35656, .T. ) ;
#1887=VECTOR ( 'NONE', #39407, 39.37007874015748143 ) ;
#1888=ORIENTED_EDGE ( 'NONE', *, *, #17950, .T. ) ;
#1889=ADVANCED_FACE ( 'NONE', ( #43854 ), #23476, .F. ) ;
#1891=LINE ( 'NONE', #48139, #6225 ) ;
#1892=DIRECTION ( 'NONE',  ( -0.000000000000000000, -1.000000000000000000, -0.000000000000000000 ) ) ;
#1893=EDGE_CURVE ( 'NONE', #49676, #22883, #39228, .T. ) ;
#1894=ORIENTED_EDGE ( 'NONE', *, *, #43085, .F. ) ;
#1895=DIRECTION ( 'NONE',  ( -1.000000000000000000, -0.000000000000000000, -0.000000000000000000 ) ) ;
#1896=PLANE ( 'NONE',  #49188 ) ;
#1899=CARTESIAN_POINT ( 'NONE',  ( -0.3486774197067339376, 3.267716535433071279, 2.137096964226333107 ) ) ;
#1901=ORIENTED_EDGE ( 'NONE', *, *, #11412, .F. ) ;
#1902=CARTESIAN_POINT ( 'NONE',  ( 0.7423782071083084855, 3.267716535433071279, -2.575641807848709208E-16 ) ) ;
#1903=LINE ( 'NONE', #33920, #25761 ) ;
#1904=EDGE_CURVE ( 'NONE', #39081, #5779, #4125, .T. ) ;
#1905=VERTEX_POINT ( 'NONE', #237 ) ;
#1906=CARTESIAN_POINT ( 'NONE',  ( 1.363819533518803695, 3.346456692913386100, 1.605145679676862835 ) ) ;
#1907=DIRECTION ( 'NONE',  ( -0.000000000000000000, 1.000000000000000000, -0.000000000000000000 ) ) ;
#1910=CARTESIAN_POINT ( 'NONE',  ( 0.5455278134075211005, 0.000000000000000000, -0.5118110236220467790 ) ) ;
#1913=ORIENTED_EDGE ( 'NONE', *, *, #39250, .F. ) ;
#1916=LINE ( 'NONE', #48352, #8127 ) ;
#1919=PLANE ( 'NONE',  #14377 ) ;
#1920=LINE ( 'NONE', #25923, #20294 ) ;
#1922=EDGE_CURVE ( 'NONE', #50744, #13274, #1527, .T. ) ;
#1923=CIRCLE ( 'NONE', #33258, 2.165354330708661568 ) ;
#1925=ORIENTED_EDGE ( 'NONE', *, *, #24754, .T. ) ;
#1926=ORIENTED_EDGE ( 'NONE', *, *, #43337, .T. ) ;
#1927=CARTESIAN_POINT ( 'NONE',  ( -0.2727639067037602172, 3.346456692913386100, 1.102362204724404160 ) ) ;
#1928=CARTESIAN_POINT ( 'NONE',  ( -0.8182917201112819283, 0.000000000000000000, 1.850393700787391849 ) ) ;
#1929=FACE_OUTER_BOUND ( 'NONE', #20700, .T. ) ;
#1930=EDGE_LOOP ( 'NONE', ( #23938, #32963, #17065, #45642 ) ) ;
#1931=CARTESIAN_POINT ( 'NONE',  ( 1.287906020515830141, 3.346456692913386100, 1.259842519685033357 ) ) ;
#1932=FACE_BOUND ( 'NONE', #27495, .T. ) ;
#1933=VECTOR ( 'NONE', #48071, 39.37007874015748143 ) ;
#1934=ORIENTED_EDGE ( 'NONE', *, *, #7135, .F. ) ;
#1935=CARTESIAN_POINT ( 'NONE',  ( -0.07591351300297333182, 3.346456692913386100, -1.732283464566922726 ) ) ;
#1936=ORIENTED_EDGE ( 'NONE', *, *, #4912, .F. ) ;
#1939=CARTESIAN_POINT ( 'NONE',  ( 0.000000000000000000, 3.346456692913386100, 0.000000000000000000 ) ) ;
#1943=DIRECTION ( 'NONE',  ( 1.000000000000000000, 0.000000000000000000, 0.000000000000000000 ) ) ;
#1944=ORIENTED_EDGE ( 'NONE', *, *, #20132, .F. ) ;
#1945=CARTESIAN_POINT ( 'NONE',  ( 1.091055626815042645, 3.346456692913386100, -8.878505979408855953E-16 ) ) ;
#1947=CARTESIAN_POINT ( 'NONE',  ( -0.2727639067037607723, 0.000000000000000000, 0.1574803149606283648 ) ) ;
#1949=ADVANCED_FACE ( 'NONE', ( #36649 ), #48980, .F. ) ;
#1950=FACE_OUTER_BOUND ( 'NONE', #43350, .T. ) ;
#1952=ORIENTED_EDGE ( 'NONE', *, *, #9468, .T. ) ;
#1954=FACE_OUTER_BOUND ( 'NONE', #16449, .T. ) ;
#1955=VECTOR ( 'NONE', #41461, 39.37007874015748143 ) ;
#1956=PLANE ( 'NONE',  #42142 ) ;
#1958=VECTOR ( 'NONE', #12006, 39.37007874015748143 ) ;
#1959=VECTOR ( 'NONE', #13764, 39.37007874015748854 ) ;
#1960=VERTEX_POINT ( 'NONE', #21154 ) ;
#1961=DIRECTION ( 'NONE',  ( 1.000000000000000000, -0.000000000000000000, 0.000000000000000000 ) ) ;
#1963=ORIENTED_EDGE ( 'NONE', *, *, #46858, .F. ) ;
#1967=CARTESIAN_POINT ( 'NONE',  ( -1.716666360678977599, 3.346456692913386100, 1.220472440944875281 ) ) ;
#1969=ORIENTED_EDGE ( 'NONE', *, *, #17010, .T. ) ;
#1970=CARTESIAN_POINT ( 'NONE',  ( -0.2727639067037602172, 0.000000000000000000, 2.047244094488179567 ) ) ;
#1972=FACE_BOUND ( 'NONE', #28570, .T. ) ;
#1973=LINE ( 'NONE', #21851, #42402 ) ;
#1974=LINE ( 'NONE', #21346, #14410 ) ;
#1975=EDGE_CURVE ( 'NONE', #29456, #40420, #33290, .T. ) ;
#1976=DIRECTION ( 'NONE',  ( -0.000000000000000000, 1.000000000000000000, -0.000000000000000000 ) ) ;
#1978=ORIENTED_EDGE ( 'NONE', *, *, #45941, .T. ) ;
#1979=DIRECTION ( 'NONE',  ( 1.734723475976806848E-16, -0.000000000000000000, 1.000000000000000000 ) ) ;
#1981=ADVANCED_FACE ( 'NONE', ( #48469, #16771, #40265, #33041, #47959, #32529, #44877, #48723, #40520, #9529, #13402, #5659, #36390, #4889, #1011, #44620, #20889, #5141, #25018, #24258, #25277, #12896, #40003, #9273, #4634, #41034, #20633, #20377, #36133, #763, #16514, #12633, #44116, #12831, #9464, #29073, #1206, #44558, #13597, #44310, #32979, #44813, #25211, #40969, #28823, #25460, #8951, #29333, #5077, #1457, #32723, #5332, #5589, #49171, #1972, #48654, #17214, #13090, #48400, #9207, #21341, #24709, #48154, #9722, #37351, #24955, #37094, #45066, #17461, #16708, #20826, #40707, #41222, #36326, #1713, #32462, #13339, #33227, #28564, #48910, #5842, #40460, #21592, #17720, #33485, #36583, #13849, #29596, #45315, #21085, #9972, #16965, #40200, #36841, #4829, #20574, #948, #26470, #34737, #38611, #41723, #30101, #49922, #41975, #3233, #29846, #45817, #42217, #34487, #6858, #41468, #46322, #22860, #18226, #14609, #50173, #2989, #2231, #6360, #10483, #10984, #34237, #33985, #18981, #45562, #6095, #18483, #21850, #2731, #25972, #18737, #26724, #14865, #22106, #30356, #46076, #30608, #37864, #10735, #2489, #50419, #26226, #22608, #42472 ), #38361, .F. ) ;
#1982=LINE ( 'NONE', #6368, #2995 ) ;
#1983=ORIENTED_EDGE ( 'NONE', *, *, #34002, .F. ) ;
#1985=EDGE_LOOP ( 'NONE', ( #10367, #36295, #11306, #46455 ) ) ;
#1987=VECTOR ( 'NONE', #19193, 39.37007874015748143 ) ;
#1989=VECTOR ( 'NONE', #20549, 39.37007874015748143 ) ;
#1990=ORIENTED_EDGE ( 'NONE', *, *, #18984, .T. ) ;
#1991=LINE ( 'NONE', #14373, #45448 ) ;
#1992=VECTOR ( 'NONE', #27537, 39.37007874015748143 ) ;
#1993=ORIENTED_EDGE ( 'NONE', *, *, #2686, .F. ) ;
#1994=VERTEX_POINT ( 'NONE', #15109 ) ;
#1997=AXIS2_PLACEMENT_3D ( 'NONE', #5441, #804, #16558 ) ;
#1998=ORIENTED_EDGE ( 'NONE', *, *, #46406, .T. ) ;
#1999=ORIENTED_EDGE ( 'NONE', *, *, #46946, .T. ) ;
#2000=DIRECTION ( 'NONE',  ( 1.000000000000000000, 0.000000000000000000, 0.000000000000000000 ) ) ;
#2001=VECTOR ( 'NONE', #23786, 39.37007874015748143 ) ;
#2002=EDGE_LOOP ( 'NONE', ( #43852, #43434, #22980, #21233 ) ) ;
#2003=DIRECTION ( 'NONE',  ( 1.000000000000000000, -0.000000000000000000, 0.000000000000000000 ) ) ;
#2005=DIRECTION ( 'NONE',  ( -0.000000000000000000, 0.000000000000000000, 1.000000000000000000 ) ) ;
#2007=FACE_OUTER_BOUND ( 'NONE', #28920, .T. ) ;
#2010=EDGE_CURVE ( 'NONE', #48838, #20798, #19752, .T. ) ;
#2011=DIRECTION ( 'NONE',  ( 0.000000000000000000, -1.000000000000000000, 0.000000000000000000 ) ) ;
#2012=DIRECTION ( 'NONE',  ( 0.000000000000000000, 1.000000000000000000, 0.000000000000000000 ) ) ;
#2013=LINE ( 'NONE', #47941, #38398 ) ;
#2015=EDGE_CURVE ( 'NONE', #19298, #47601, #17971, .T. ) ;
#2016=CARTESIAN_POINT ( 'NONE',  ( -0.8942052331142552601, 0.000000000000000000, -1.771653543307081025 ) ) ;
#2017=EDGE_CURVE ( 'NONE', #41776, #22927, #14099, .T. ) ;
#2018=CARTESIAN_POINT ( 'NONE',  ( -2.182111253630085290, 0.000000000000000000, 0.4330708661417290162 ) ) ;
#2019=EDGE_LOOP ( 'NONE', ( #1254, #36247, #6486, #7808 ) ) ;
#2020=DIRECTION ( 'NONE',  ( -1.000000000000000000, 0.000000000000000000, 0.000000000000000000 ) ) ;
#2023=CARTESIAN_POINT ( 'NONE',  ( -0.8942052331142552601, 0.000000000000000000, -0.6299212598425177889 ) ) ;
#2024=ORIENTED_EDGE ( 'NONE', *, *, #22534, .T. ) ;
#2025=DIRECTION ( 'NONE',  ( -3.469446951953613696E-16, 0.000000000000000000, -1.000000000000000000 ) ) ;
#2026=VECTOR ( 'NONE', #27967, 39.37007874015748143 ) ;
#2027=VECTOR ( 'NONE', #20312, 39.37007874015748143 ) ;
#2031=PLANE ( 'NONE',  #23384 ) ;
#2032=CIRCLE ( 'NONE', #23460, 2.443628662382284489 ) ;
#2033=DIRECTION ( 'NONE',  ( -0.000000000000000000, 1.000000000000000000, -0.000000000000000000 ) ) ;
#2034=CARTESIAN_POINT ( 'NONE',  ( 0.8182917201112817063, 0.000000000000000000, -1.417322834645664331 ) ) ;
#2036=LINE ( 'NONE', #14923, #24443 ) ;
#2037=ORIENTED_EDGE ( 'NONE', *, *, #20509, .T. ) ;
#2038=LINE ( 'NONE', #6923, #3533 ) ;
#2039=AXIS2_PLACEMENT_3D ( 'NONE', #7726, #15726, #39220 ) ;
#2041=PLANE ( 'NONE',  #15531 ) ;
#2043=EDGE_CURVE ( 'NONE', #45470, #12597, #31618, .T. ) ;
#2044=DIRECTION ( 'NONE',  ( -3.469446951953613696E-16, 0.000000000000000000, -1.000000000000000000 ) ) ;
#2045=CARTESIAN_POINT ( 'NONE',  ( 0.5455278134075211005, 0.000000000000000000, 0.4330708661417287386 ) ) ;
#2048=ADVANCED_FACE ( 'NONE', ( #11995 ), #8123, .F. ) ;
#2049=LINE ( 'NONE', #6685, #4305 ) ;
#2053=CARTESIAN_POINT ( 'NONE',  ( -0.6214413264104945434, 3.267716535433071279, -0.9842519685039342603 ) ) ;
#2054=FACE_BOUND ( 'NONE', #15095, .T. ) ;
#2055=ORIENTED_EDGE ( 'NONE', *, *, #37185, .F. ) ;
#2056=EDGE_CURVE ( 'NONE', #6833, #47979, #42964, .T. ) ;
#2057=DIRECTION ( 'NONE',  ( 1.734723475976806848E-16, -0.000000000000000000, 1.000000000000000000 ) ) ;
#2060=EDGE_LOOP ( 'NONE', ( #50689, #8405, #10719, #45390 ) ) ;
#2062=CIRCLE ( 'NONE', #40827, 2.106299212598425008 ) ;
#2067=ORIENTED_EDGE ( 'NONE', *, *, #16930, .F. ) ;
#2069=VERTEX_POINT ( 'NONE', #31116 ) ;
#2072=CARTESIAN_POINT ( 'NONE',  ( 0.000000000000000000, 3.267716535433071279, -0.6299212598425181220 ) ) ;
#2073=CARTESIAN_POINT ( 'NONE',  ( -0.8942052331142552601, 3.267716535433071279, -1.907064071829739582 ) ) ;
#2074=DIRECTION ( 'NONE',  ( -3.469446951953613696E-16, 0.000000000000000000, -1.000000000000000000 ) ) ;
#2076=ORIENTED_EDGE ( 'NONE', *, *, #96, .T. ) ;
#2077=CIRCLE ( 'NONE', #32561, 2.106299212598425008 ) ;
#2081=CARTESIAN_POINT ( 'NONE',  ( -2.454875160333845674, 3.346456692913386100, -0.03937007874015881204 ) ) ;
#2082=DIRECTION ( 'NONE',  ( 0.000000000000000000, 1.000000000000000000, 0.000000000000000000 ) ) ;
#2083=ADVANCED_FACE ( 'NONE', ( #35241 ), #47062, .F. ) ;
#2084=CARTESIAN_POINT ( 'NONE',  ( -0.5455278134075214336, 3.267716535433071279, -0.6299212598425175669 ) ) ;
#2085=ADVANCED_FACE ( 'NONE', ( #27989 ), #43726, .F. ) ;
#2086=CARTESIAN_POINT ( 'NONE',  ( -1.985260859929297572, 3.267716535433071279, 6.887757239314511260E-16 ) ) ;
#2087=VERTEX_POINT ( 'NONE', #39872 ) ;
#2088=DIRECTION ( 'NONE',  ( -0.000000000000000000, 1.000000000000000000, -0.000000000000000000 ) ) ;
#2089=DIRECTION ( 'NONE',  ( -1.000000000000000000, -0.000000000000000000, -0.000000000000000000 ) ) ;
#2090=ORIENTED_EDGE ( 'NONE', *, *, #40283, .F. ) ;
#2091=VERTEX_POINT ( 'NONE', #39110 ) ;
#2092=CARTESIAN_POINT ( 'NONE',  ( 0.9832762519060537221, 3.254021347498972094, -2.244094488188969283 ) ) ;
#2093=ORIENTED_EDGE ( 'NONE', *, *, #50503, .F. ) ;
#2094=AXIS2_PLACEMENT_3D ( 'NONE', #24493, #48198, #44596 ) ;
#2096=ORIENTED_EDGE ( 'NONE', *, *, #48432, .T. ) ;
#2097=DIRECTION ( 'NONE',  ( -0.000000000000000000, 1.000000000000000000, -0.000000000000000000 ) ) ;
#2098=VECTOR ( 'NONE', #21981, 39.37007874015748143 ) ;
#2101=DIRECTION ( 'NONE',  ( 1.734723475976806848E-16, -0.000000000000000000, 1.000000000000000000 ) ) ;
#2103=VERTEX_POINT ( 'NONE', #50667 ) ;
#2104=VERTEX_POINT ( 'NONE', #16386 ) ;
#2107=ORIENTED_EDGE ( 'NONE', *, *, #38743, .T. ) ;
#2108=VERTEX_POINT ( 'NONE', #32139 ) ;
#2109=LINE ( 'NONE', #37233, #30621 ) ;
#2110=CARTESIAN_POINT ( 'NONE',  ( 0.1968503937007869686, 3.346456692913386100, -2.401574803149598480 ) ) ;
#2112=EDGE_CURVE ( 'NONE', #49063, #44346, #7867, .T. ) ;
#2114=EDGE_CURVE ( 'NONE', #1008, #4354, #7367, .T. ) ;
#2116=DIRECTION ( 'NONE',  ( 0.000000000000000000, 0.000000000000000000, 1.000000000000000000 ) ) ;
#2117=DIRECTION ( 'NONE',  ( -0.000000000000000000, 1.000000000000000000, -0.000000000000000000 ) ) ;
#2121=CARTESIAN_POINT ( 'NONE',  ( -0.2727639067037608278, 0.000000000000000000, -1.299212598425193210 ) ) ;
#2122=DIRECTION ( 'NONE',  ( -3.469446951953613696E-16, 0.000000000000000000, -1.000000000000000000 ) ) ;
#2123=VERTEX_POINT ( 'NONE', #15615 ) ;
#2124=ORIENTED_EDGE ( 'NONE', *, *, #24368, .T. ) ;
#2126=DIRECTION ( 'NONE',  ( 0.000000000000000000, 0.000000000000000000, -1.000000000000000000 ) ) ;
#2127=ADVANCED_FACE ( 'NONE', ( #27476 ), #43221, .F. ) ;
#2129=VERTEX_POINT ( 'NONE', #13279 ) ;
#2132=VECTOR ( 'NONE', #33580, 39.37007874015748143 ) ;
#2133=DIRECTION ( 'NONE',  ( 1.734723475976806848E-16, -0.000000000000000000, 1.000000000000000000 ) ) ;
#2134=ORIENTED_EDGE ( 'NONE', *, *, #15843, .T. ) ;
#2135=DIRECTION ( 'NONE',  ( 1.734723475976806848E-16, 0.000000000000000000, 1.000000000000000000 ) ) ;
#2136=CARTESIAN_POINT ( 'NONE',  ( -3.927031490892378253E-16, 3.267716535433071279, -1.889763779527552146 ) ) ;
#2137=CIRCLE ( 'NONE', #43349, 2.106299212598425008 ) ;
#2138=ADVANCED_FACE ( 'NONE', ( #24642 ), #1396, .F. ) ;
#2140=EDGE_CURVE ( 'NONE', #8542, #8317, #4782, .T. ) ;
#2141=EDGE_CURVE ( 'NONE', #1994, #23693, #20758, .T. ) ;
#2144=CARTESIAN_POINT ( 'NONE',  ( -0.3486774197067334380, 3.346456692913386100, 1.574803149606291974 ) ) ;
#2145=VECTOR ( 'NONE', #4186, 39.37007874015748143 ) ;
#2146=EDGE_LOOP ( 'NONE', ( #1482, #16863, #46508, #15990 ) ) ;
#2147=EDGE_CURVE ( 'NONE', #23949, #38782, #5267, .T. ) ;
#2148=DIRECTION ( 'NONE',  ( 1.000000000000000000, 0.000000000000000000, 0.000000000000000000 ) ) ;
#2149=LINE ( 'NONE', #49345, #43308 ) ;
#2150=CARTESIAN_POINT ( 'NONE',  ( 0.8182917201112819283, 0.000000000000000000, -0.7874015748031473194 ) ) ;
#2152=CARTESIAN_POINT ( 'NONE',  ( 1.363819533518803029, 3.267716535433071279, -2.365849761790804994E-16 ) ) ;
#2154=DIRECTION ( 'NONE',  ( -1.000000000000000000, 0.000000000000000000, -0.000000000000000000 ) ) ;
#2155=ORIENTED_EDGE ( 'NONE', *, *, #10077, .F. ) ;
#2156=PLANE ( 'NONE',  #41575 ) ;
#2157=ORIENTED_EDGE ( 'NONE', *, *, #20849, .F. ) ;
#2160=VERTEX_POINT ( 'NONE', #48595 ) ;
#2163=FACE_OUTER_BOUND ( 'NONE', #23547, .T. ) ;
#2165=PLANE ( 'NONE',  #45793 ) ;
#2166=VECTOR ( 'NONE', #4421, 39.37007874015748143 ) ;
#2168=VERTEX_POINT ( 'NONE', #25397 ) ;
#2170=LINE ( 'NONE', #21031, #50351 ) ;
#2171=VECTOR ( 'NONE', #2851, 39.37007874015748143 ) ;
#2172=DIRECTION ( 'NONE',  ( 1.734723475976806848E-16, -0.000000000000000000, 1.000000000000000000 ) ) ;
#2175=DIRECTION ( 'NONE',  ( -0.000000000000000000, 0.000000000000000000, 1.000000000000000000 ) ) ;
#2177=LINE ( 'NONE', #38064, #35200 ) ;
#2180=VERTEX_POINT ( 'NONE', #24894 ) ;
#2181=ADVANCED_FACE ( 'NONE', ( #44747 ), #9399, .F. ) ;
#2184=VECTOR ( 'NONE', #49480, 39.37007874015748143 ) ;
#2185=LINE ( 'NONE', #28781, #28022 ) ;
#2187=ORIENTED_EDGE ( 'NONE', *, *, #30207, .T. ) ;
#2188=CARTESIAN_POINT ( 'NONE',  ( -1.166969139818016199, 3.346456692913386100, -1.823990790610291013 ) ) ;
#2189=EDGE_CURVE ( 'NONE', #45998, #35616, #44249, .T. ) ;
#2190=CARTESIAN_POINT ( 'NONE',  ( 1.560669927219590525, 3.267716535433071279, -0.3543307086614178592 ) ) ;
#2191=AXIS2_PLACEMENT_3D ( 'NONE', #7129, #50430, #12266 ) ;
#2192=ORIENTED_EDGE ( 'NONE', *, *, #3229, .F. ) ;
#2195=EDGE_LOOP ( 'NONE', ( #50078, #19189, #11181, #21896 ) ) ;
#2196=DIRECTION ( 'NONE',  ( -0.000000000000000000, 1.000000000000000000, -0.000000000000000000 ) ) ;
#2197=PLANE ( 'NONE',  #19286 ) ;
#2198=EDGE_CURVE ( 'NONE', #31414, #50326, #5527, .T. ) ;
#2199=ORIENTED_EDGE ( 'NONE', *, *, #48460, .F. ) ;
#2200=LINE ( 'NONE', #28794, #28556 ) ;
#2202=EDGE_LOOP ( 'NONE', ( #41177, #39326, #6550, #5166 ) ) ;
#2204=CARTESIAN_POINT ( 'NONE',  ( 0.7423782071083087075, 0.000000000000000000, -0.9448818897637765168 ) ) ;
#2205=DIRECTION ( 'NONE',  ( 1.734723475976806848E-16, -0.000000000000000000, 1.000000000000000000 ) ) ;
#2206=EDGE_CURVE ( 'NONE', #18373, #5670, #28756, .T. ) ;
#2207=VECTOR ( 'NONE', #37854, 39.37007874015748143 ) ;
#2208=LINE ( 'NONE', #9188, #46178 ) ;
#2209=ADVANCED_FACE ( 'NONE', ( #9145 ), #40400, .F. ) ;
#2210=CARTESIAN_POINT ( 'NONE',  ( 1.363819533518803251, 3.346456692913386100, 1.220472440944875281 ) ) ;
#2211=DIRECTION ( 'NONE',  ( 1.000000000000000000, 0.000000000000000000, 0.000000000000000000 ) ) ;
#2212=VECTOR ( 'NONE', #9248, 39.37007874015748143 ) ;
#2213=ORIENTED_EDGE ( 'NONE', *, *, #3477, .F. ) ;
#2214=LINE ( 'NONE', #21579, #43914 ) ;
#2216=EDGE_CURVE ( 'NONE', #7713, #35081, #29268, .T. ) ;
#2217=EDGE_CURVE ( 'NONE', #47517, #11723, #17658, .T. ) ;
#2218=DIRECTION ( 'NONE',  ( -1.000000000000000000, 0.000000000000000000, 1.734723475976806848E-16 ) ) ;
#2219=VERTEX_POINT ( 'NONE', #28240 ) ;
#2220=FACE_OUTER_BOUND ( 'NONE', #828, .T. ) ;
#2221=PLANE ( 'NONE',  #45081 ) ;
#2223=CARTESIAN_POINT ( 'NONE',  ( 0.000000000000000000, 3.267716535433071279, -2.244094488188968395 ) ) ;
#2225=PLANE ( 'NONE',  #33295 ) ;
#2227=AXIS2_PLACEMENT_3D ( 'NONE', #7320, #34937, #31831 ) ;
#2229=PLANE ( 'NONE',  #38701 ) ;
#2230=ORIENTED_EDGE ( 'NONE', *, *, #16362, .F. ) ;
#2231=FACE_BOUND ( 'NONE', #3970, .T. ) ;
#2233=LINE ( 'NONE', #36843, #43244 ) ;
#2234=DIRECTION ( 'NONE',  ( -1.000000000000000000, 0.000000000000000000, 0.000000000000000000 ) ) ;
#2235=ORIENTED_EDGE ( 'NONE', *, *, #298, .F. ) ;
#2236=ORIENTED_EDGE ( 'NONE', *, *, #36947, .T. ) ;
#2237=DIRECTION ( 'NONE',  ( -0.000000000000000000, 1.000000000000000000, -0.000000000000000000 ) ) ;
#2238=CARTESIAN_POINT ( 'NONE',  ( 1.015142113812069313, 3.346456692913386100, 0.7874015748031454320 ) ) ;
#2239=ORIENTED_EDGE ( 'NONE', *, *, #17711, .T. ) ;
#2240=DIRECTION ( 'NONE',  ( -0.000000000000000000, 1.000000000000000000, -0.000000000000000000 ) ) ;
#2241=VERTEX_POINT ( 'NONE', #48343 ) ;
#2242=CARTESIAN_POINT ( 'NONE',  ( 2.106197740627112402, 3.346456692913386100, 0.1574803149606280872 ) ) ;
#2243=VECTOR ( 'NONE', #13775, 39.37007874015748143 ) ;
#2247=ORIENTED_EDGE ( 'NONE', *, *, #8547, .F. ) ;
#2248=ADVANCED_FACE ( 'NONE', ( #36265 ), #16645, .F. ) ;
#2250=ORIENTED_EDGE ( 'NONE', *, *, #34945, .T. ) ;
#2251=ORIENTED_EDGE ( 'NONE', *, *, #16576, .T. ) ;
#2252=EDGE_CURVE ( 'NONE', #2180, #26524, #49360, .T. ) ;
#2253=ORIENTED_EDGE ( 'NONE', *, *, #41769, .T. ) ;
#2254=EDGE_LOOP ( 'NONE', ( #38376, #36963, #7977, #38935 ) ) ;
#2255=CARTESIAN_POINT ( 'NONE',  ( 1.636583440222563857, 0.000000000000000000, 1.062992125984245639 ) ) ;
#2258=DIRECTION ( 'NONE',  ( -1.000000000000000000, 0.000000000000000000, 1.734723475976806848E-16 ) ) ;
#2259=CARTESIAN_POINT ( 'NONE',  ( 0.7423782071083091516, 3.346456692913386100, 1.377952755905504256 ) ) ;
#2261=PLANE ( 'NONE',  #12368 ) ;
#2262=CARTESIAN_POINT ( 'NONE',  ( 1.636583440222563857, 0.000000000000000000, -0.3149606299212596716 ) ) ;
#2263=DIRECTION ( 'NONE',  ( 1.734723475976806848E-16, -0.000000000000000000, 1.000000000000000000 ) ) ;
#2266=LINE ( 'NONE', #49713, #24996 ) ;
#2268=EDGE_CURVE ( 'NONE', #45405, #32424, #49608, .T. ) ;
#2269=DIRECTION ( 'NONE',  ( 1.734723475976806848E-16, -0.000000000000000000, 1.000000000000000000 ) ) ;
#2270=DIRECTION ( 'NONE',  ( 0.000000000000000000, -1.000000000000000000, 0.000000000000000000 ) ) ;
#2271=ORIENTED_EDGE ( 'NONE', *, *, #2436, .T. ) ;
#2273=LINE ( 'NONE', #18023, #37672 ) ;
#2275=CARTESIAN_POINT ( 'NONE',  ( 0.5455278134075211005, 3.267716535433071279, 0.4330708661417287386 ) ) ;
#2276=VECTOR ( 'NONE', #13484, 39.37007874015748143 ) ;
#2277=VECTOR ( 'NONE', #43910, 39.37007874015748143 ) ;
#2278=DIRECTION ( 'NONE',  ( 0.000000000000000000, 0.000000000000000000, 1.000000000000000000 ) ) ;
#2282=ORIENTED_EDGE ( 'NONE', *, *, #11605, .F. ) ;
#2283=DIRECTION ( 'NONE',  ( -3.469446951953613696E-16, 0.000000000000000000, -1.000000000000000000 ) ) ;
#2284=FACE_OUTER_BOUND ( 'NONE', #35475, .T. ) ;
#2285=CARTESIAN_POINT ( 'NONE',  ( -2.182111253630085290, 3.346456692913386100, 0.1181102362204704270 ) ) ;
#2286=CARTESIAN_POINT ( 'NONE',  ( -1.363819533518803473, 0.000000000000000000, -0.4724409448818886470 ) ) ;
#2287=CARTESIAN_POINT ( 'NONE',  ( 0.1968503937007873017, 0.000000000000000000, -1.574803149606293529 ) ) ;
#2288=ORIENTED_EDGE ( 'NONE', *, *, #9406, .F. ) ;
#2289=CARTESIAN_POINT ( 'NONE',  ( 1.015142113812069313, 3.267716535433071279, -3.521981712565032882E-16 ) ) ;
#2291=ORIENTED_EDGE ( 'NONE', *, *, #25331, .T. ) ;
#2292=EDGE_LOOP ( 'NONE', ( #24210, #36504, #29232, #35366 ) ) ;
#2295=CARTESIAN_POINT ( 'NONE',  ( 0.000000000000000000, 3.267716535433071279, 2.047244094488179567 ) ) ;
#2296=VECTOR ( 'NONE', #8934, 39.37007874015748143 ) ;
#2297=LINE ( 'NONE', #6681, #12873 ) ;
#2298=VERTEX_POINT ( 'NONE', #10158 ) ;
#2300=DIRECTION ( 'NONE',  ( 0.000000000000000000, -1.000000000000000000, 0.000000000000000000 ) ) ;
#2302=VERTEX_POINT ( 'NONE', #21786 ) ;
#2304=VERTEX_POINT ( 'NONE', #37797 ) ;
#2306=FACE_BOUND ( 'NONE', #42970, .T. ) ;
#2309=LINE ( 'NONE', #36922, #13859 ) ;
#2310=CARTESIAN_POINT ( 'NONE',  ( 1.560669927219590525, 3.267716535433071279, -5.414661521997676285E-16 ) ) ;
#2311=AXIS2_PLACEMENT_3D ( 'NONE', #14353, #37606, #38112 ) ;
#2314=ORIENTED_EDGE ( 'NONE', *, *, #12927, .T. ) ;
#2315=EDGE_LOOP ( 'NONE', ( #20777, #23819, #16602, #48748 ) ) ;
#2317=FACE_OUTER_BOUND ( 'NONE', #32941, .T. ) ;
#2322=FACE_OUTER_BOUND ( 'NONE', #40191, .T. ) ;
#2324=CARTESIAN_POINT ( 'NONE',  ( 1.015142113812069313, 3.267716535433071279, -0.4724409448818889246 ) ) ;
#2325=VECTOR ( 'NONE', #18352, 39.37007874015748143 ) ;
#2326=EDGE_CURVE ( 'NONE', #24313, #42844, #6294, .T. ) ;
#2327=CARTESIAN_POINT ( 'NONE',  ( -1.091055626815042201, 0.000000000000000000, 1.377952755905504256 ) ) ;
#2328=CARTESIAN_POINT ( 'NONE',  ( 0.000000000000000000, 3.346456692913386100, 0.000000000000000000 ) ) ;
#2329=VECTOR ( 'NONE', #27569, 39.37007874015748143 ) ;
#2330=ORIENTED_EDGE ( 'NONE', *, *, #10631, .F. ) ;
#2331=ORIENTED_EDGE ( 'NONE', *, *, #15545, .F. ) ;
#2332=LINE ( 'NONE', #21444, #31544 ) ;
#2333=DIRECTION ( 'NONE',  ( 1.000000000000000000, 0.000000000000000000, -3.469446951953613696E-16 ) ) ;
#2334=DIRECTION ( 'NONE',  ( -0.000000000000000000, 1.000000000000000000, -0.000000000000000000 ) ) ;
#2335=EDGE_CURVE ( 'NONE', #36771, #7345, #22042, .T. ) ;
#2336=VECTOR ( 'NONE', #44604, 39.37007874015748143 ) ;
#2339=FACE_OUTER_BOUND ( 'NONE', #23939, .T. ) ;
#2340=EDGE_CURVE ( 'NONE', #47312, #25798, #28682, .T. ) ;
#2342=DIRECTION ( 'NONE',  ( -0.000000000000000000, 1.000000000000000000, -0.000000000000000000 ) ) ;
#2343=ORIENTED_EDGE ( 'NONE', *, *, #47528, .T. ) ;
#2347=EDGE_CURVE ( 'NONE', #44092, #23693, #38049, .T. ) ;
#2348=ORIENTED_EDGE ( 'NONE', *, *, #46632, .F. ) ;
#2349=DIRECTION ( 'NONE',  ( -0.000000000000000000, 1.000000000000000000, -0.000000000000000000 ) ) ;
#2350=VECTOR ( 'NONE', #50356, 39.37007874015748143 ) ;
#2353=DIRECTION ( 'NONE',  ( -0.000000000000000000, 1.000000000000000000, -0.000000000000000000 ) ) ;
#2355=ORIENTED_EDGE ( 'NONE', *, *, #3937, .T. ) ;
#2356=CLOSED_SHELL ( 'NONE', ( #48906, #33438, #3352, #23489, #38798, #12613, #1981, #26148, #45748, #32793, #12742, #47076, #17850, #46605, #13479, #44502, #33285, #18234, #19127, #22021, #1480, #20482, #22830, #45082, #41414, #8100, #5929, #9918, #825, #50557, #44636, #30340, #28705, #12764, #21875, #47533, #45573, #25579, #15596, #31809, #34099, #38632, #6964, #18519, #44071, #39087, #23040, #33571, #18845, #18917, #37640, #46903, #9983, #33504, #2127, #15569, #2083, #33592, #39274, #5546, #34130, #19212, #31291, #38017, #4876, #25682, #43758, #16134, #16170, #9431, #28778, #43961, #2085, #26636, #18257, #6200, #34720, #775, #24407, #34198, #42232, #32434, #5569, #25162, #30401, #17856, #31203, #17915, #3481, #20071, #28587, #42465, #39654, #34993, #30420, #21098, #2698, #42048, #30562, #44384, #5391, #12837, #17054, #34703, #8375, #42617, #46749, #21853, #16069, #14643, #39384, #46636, #7569, #38342, #14997, #3409, #18562, #15145, #33341, #3105, #26843, #3967, #9846, #10082, #26131, #4000, #13671, #30915, #23445, #9440, #5133, #2048, #27527, #173, #40582, #2377, #11057, #17916, #3378, #14604, #3713, #3390, #4834, #18792, #30859, #39290, #22194, #33106, #42623, #20890, #48977, #36657, #48033, #47615, #33939, #31416, #25433, #38146, #2209, #20013, #10874, #50094, #8881, #31151, #48660, #37316, #9075, #46348, #26351, #40740, #17521, #24730, #31141, #17072, #29773, #3070, #48590, #48557, #9441, #50843, #42390, #45308, #38379, #2181, #2716, #35796, #39765, #25482, #17485, #10709, #50625, #9002, #13678, #43478, #43962, #9939, #3462, #23778, #14717, #753, #203, #34493, #45780, #30642, #471, #1204, #41578, #8077, #2248, #12560, #27165, #15081, #37079, #30569, #20091, #16434, #38690, #38963, #35766, #4814, #35861, #33467, #22466, #20315, #10653, #39987, #44440, #44090, #27902, #10876, #29798, #41071, #20491, #46484, #12153, #19611, #10108, #891, #14633, #34325, #234, #23534, #10336, #28573, #34842, #38184, #47721, #20702, #12672, #40361, #3541, #39784, #925, #35353, #40157, #50494, #8349, #3238, #11887, #25414, #29922, #16528, #13514, #20262, #36506, #30652, #33249, #32624, #20008, #13260, #13351, #33972, #38011, #10941, #1949, #1150, #49776, #33728, #10972, #45339, #7755, #34248, #3038, #31478, #29576, #37103, #32334, #1142, #11478, #9495, #32702, #50278, #19526, #28565, #44002, #3057, #49762, #974, #34038, #19250, #20207, #35173, #22127, #11032, #28335, #10969, #25900, #19948, #44725, #5781, #47819, #35017, #26992, #5351, #31619, #15619, #41880, #40798, #15405, #34217, #13994, #14252, #683, #14409, #13867, #35753, #28352, #33817, #43255, #4447, #42579, #50558, #38517, #26728, #20173, #49349, #11665, #16917, #3421, #35470, #22846, #13508, #27282, #48429, #25684, #36381, #11983, #2371, #34708, #21693, #10195, #43898, #47711, #27889, #47492, #35299, #25772, #5766, #20796, #3643, #29338, #42051, #21358, #8078, #36063, #7219, #46393, #11991, #43767, #9202, #5190, #25485, #49049, #18678, #29047, #23066, #31360, #42987, #45139, #41201, #47730, #26501, #4625, #42855, #12665, #49892, #20722, #39574, #10635, #23757, #36282, #21379, #8946, #27413, #39648, #15086, #29414, #562, #11389, #32263, #48150, #18746, #1537, #10314, #29919, #31231, #27620, #12380, #9570, #20374, #9530, #40960, #49584, #39855, #45547, #11913, #34733, #35497, #28576, #30934, #14959, #23447, #8303, #44927, #709, #24170, #24973, #7273, #14835, #1674, #4383, #15873, #44353, #20405, #18787, #30875, #16371, #27319, #8701, #39001, #18387, #7722, #28909, #16632, #42212, #26783, #14124, #39596, #50654, #39440, #21764, #40392, #7066, #14383, #41319, #50216, #36345, #30077, #19831, #27344, #1536, #24933, #11795, #2138, #13386, #15700, #4156, #26325, #8707, #21903, #40940, #21022, #48131, #29866, #39350, #38462, #19051, #13931, #40501, #11668, #42176, #8301, #11576, #27033, #36934, #22885, #43332, #7155, #12634, #11919, #20247, #4358, #39935, #12373, #6141, #31328, #37384, #28391, #18563, #21606, #36571, #9047, #35520, #31549, #22273, #33111, #31008, #26898, #50783, #36080, #253, #9987, #9625, #9490, #19303, #39501, #9363, #44267, #28272, #30453, #47971, #26725, #40834, #35153, #39636, #22061, #1476, #47912, #2661, #28017, #18640, #9827, #41292, #31802, #28074, #34009, #2450, #23220, #37377, #44215, #32329, #33950, #20855, #35781, #27354, #25999, #4441, #6336, #46847, #48944, #16718, #44547, #37215, #23646, #37989, #34959, #41110, #51029, #40577, #36991, #1384, #33847, #17052, #25144, #7742, #45418, #46514, #21946, #1889, #25779, #37584, #24232, #18713, #25902, #19044, #40674, #1020, #14121, #50836, #1787, #19818, #19958, #27400, #8756, #45078, #50790, #16273, #9019, #23540, #44258, #31781, #26982, #41673, #34609, #12055, #27925, #12115, #37946, #15474, #12478, #47665, #18259, #21003, #18932, #12923, #35876, #43084, #12030, #14615, #30010, #17007, #13509, #35001, #23256, #41003, #25267, #20687, #28925, #29403, #36713, #41868, #20833, #4323, #14503, #8668, #30626, #32080, #37631, #20644, #32516, #5805, #46734, #17527, #12435, #31770, #42526, #38364, #44298, #11038, #6641, #7024, #10689, #16493, #33701, #6636, #892, #46065, #37707, #2672, #5479, #5866, #38118, #31035, #22796, #10259, #19016, #1826, #38093, #8608, #30587, #31748, #44086, #26078, #24935, #10240, #48299, #91, #44846, #39543, #18142, #40676, #7142, #44886, #44143, #33607, #13389, #11463, #48811, #32523, #20986, #11965, #3683, #41132, #11402, #33025, #15343, #4746, #9333, #36837, #23836, #9367, #19871, #36898, #600, #34142, #34886, #29136, #27257, #21718, #15548, #37985, #29941, #25516, #35727, #50248, #34960, #50459, #15953, #38640, #26035, #19586, #22599, #45576, #48178, #29213, #10978, #43217, #10114, #16292, #47599, #43796, #30143, #35402, #49243, #34806, #3837, #45963, #33046, #18002, #38993, #25676, #18432, #15015, #31392, #29068, #36440, #25502, #19835, #15597, #25231, #39023, #25845, #17747, #38221, #24870, #18408, #27127, #35281, #44726, #37840, #21835, #42749, #14742, #6558, #29564, #10164, #15470, #8815, #38282, #30825, #49195, #33858, #48965, #3629, #45282, #18106, #49612, #41155, #30708, #22367, #861, #16598, #41346, #50197, #49107, #33398, #38100, #16725, #40128, #49053, #24789, #34208, #9990, #37508, #25841, #18690, #48257, #6734, #1401, #23008, #13383, #23734, #31512, #15810, #38090, #15828, #14510, #12713, #21762, #26347, #9610, #6686, #50521, #38965, #4325, #29303, #39065, #12485, #43147, #13550, #32026, #8470, #39849, #6023, #29003, #37289, #3234, #3189, #31516, #4992, #3817, #11333, #1754, #14605, #44722, #27270, #25616, #30973, #48053, #33472, #11878, #6552, #45181, #31352, #40362, #12940, #27780, #6386, #4874, #41446, #46166, #21683, #3331, #24623, #22290, #9658, #11343, #16991, #27681, #14320, #5905, #11169, #40837, #4742, #12134, #18922, #48671, #43786, #34889, #1744, #39183, #45367, #6049, #20282, #29496, #24718, #3525, #22917, #49766, #49652, #23911, #11630, #25438, #46627, #41136, #42565, #50339, #44867, #31197, #23468, #47620, #21151, #16820 ) ) ;
#2357=VECTOR ( 'NONE', #18556, 39.37007874015748143 ) ;
#2358=CARTESIAN_POINT ( 'NONE',  ( 0.000000000000000000, 3.267716535433071279, -2.047244094488181343 ) ) ;
#2359=DIRECTION ( 'NONE',  ( -1.000000000000000000, 0.000000000000000000, 0.000000000000000000 ) ) ;
#2361=AXIS2_PLACEMENT_3D ( 'NONE', #39911, #16682, #410 ) ;
#2362=EDGE_LOOP ( 'NONE', ( #8292, #35201, #32595, #34940 ) ) ;
#2363=EDGE_LOOP ( 'NONE', ( #41631, #27503, #21057, #35997 ) ) ;
#2365=ORIENTED_EDGE ( 'NONE', *, *, #43765, .T. ) ;
#2366=ORIENTED_EDGE ( 'NONE', *, *, #9528, .F. ) ;
#2367=CARTESIAN_POINT ( 'NONE',  ( -0.8182917201112819283, 3.267716535433071279, -0.7874015748031467643 ) ) ;
#2368=CARTESIAN_POINT ( 'NONE',  ( 0.000000000000000000, 3.267716535433071279, 0.000000000000000000 ) ) ;
#2370=VECTOR ( 'NONE', #14345, 39.37007874015748143 ) ;
#2371=ADVANCED_FACE ( 'NONE', ( #10919 ), #10673, .F. ) ;
#2373=VECTOR ( 'NONE', #34773, 39.37007874015748143 ) ;
#2374=DIRECTION ( 'NONE',  ( 1.734723475976806848E-16, 0.000000000000000000, 1.000000000000000000 ) ) ;
#2376=FACE_OUTER_BOUND ( 'NONE', #15482, .T. ) ;
#2377=ADVANCED_FACE ( 'NONE', ( #22539 ), #7051, .F. ) ;
#2378=ORIENTED_EDGE ( 'NONE', *, *, #31728, .F. ) ;
#2380=CARTESIAN_POINT ( 'NONE',  ( -1.636583440222564301, 3.346456692913386100, 1.574803149606291530 ) ) ;
#2381=DIRECTION ( 'NONE',  ( -3.469446951953613696E-16, 0.000000000000000000, -1.000000000000000000 ) ) ;
#2382=ORIENTED_EDGE ( 'NONE', *, *, #21414, .F. ) ;
#2383=VERTEX_POINT ( 'NONE', #41911 ) ;
#2384=DIRECTION ( 'NONE',  ( -3.469446951953613696E-16, 0.000000000000000000, -1.000000000000000000 ) ) ;
#2385=VECTOR ( 'NONE', #37297, 39.37007874015748143 ) ;
#2388=VERTEX_POINT ( 'NONE', #34424 ) ;
#2389=ORIENTED_EDGE ( 'NONE', *, *, #49200, .F. ) ;
#2392=CARTESIAN_POINT ( 'NONE',  ( 1.560669927219590525, 0.000000000000000000, -0.03937007874015908959 ) ) ;
#2393=CARTESIAN_POINT ( 'NONE',  ( -1.091055626815042201, 3.346456692913386100, 0.9448818897637749625 ) ) ;
#2394=VECTOR ( 'NONE', #3697, 39.37007874015748143 ) ;
#2395=VECTOR ( 'NONE', #37002, 39.37007874015748143 ) ;
#2401=PLANE ( 'NONE',  #27041 ) ;
#2402=ORIENTED_EDGE ( 'NONE', *, *, #11322, .T. ) ;
#2404=CARTESIAN_POINT ( 'NONE',  ( 0.5455278134075211005, 3.346456692913386100, 0.1181102362204701633 ) ) ;
#2406=DIRECTION ( 'NONE',  ( 1.734723475976806848E-16, 0.000000000000000000, 1.000000000000000000 ) ) ;
#2407=EDGE_CURVE ( 'NONE', #44829, #16948, #50113, .T. ) ;
#2408=ORIENTED_EDGE ( 'NONE', *, *, #43800, .T. ) ;
#2409=DIRECTION ( 'NONE',  ( -0.000000000000000000, 0.000000000000000000, 1.000000000000000000 ) ) ;
#2413=DIRECTION ( 'NONE',  ( -3.469446951953613696E-16, 0.000000000000000000, -1.000000000000000000 ) ) ;
#2414=ORIENTED_EDGE ( 'NONE', *, *, #41235, .F. ) ;
#2415=EDGE_CURVE ( 'NONE', #26163, #39867, #34918, .T. ) ;
#2416=DIRECTION ( 'NONE',  ( -1.000000000000000000, 0.000000000000000000, 0.000000000000000000 ) ) ;
#2418=EDGE_LOOP ( 'NONE', ( #45602, #5149, #345, #16611 ) ) ;
#2420=LINE ( 'NONE', #13530, #47160 ) ;
#2425=CARTESIAN_POINT ( 'NONE',  ( -2.182111253630085290, 3.346456692913386100, -6.146657985744592735E-16 ) ) ;
#2427=VECTOR ( 'NONE', #24583, 39.37007874015748143 ) ;
#2428=ORIENTED_EDGE ( 'NONE', *, *, #44263, .T. ) ;
#2429=ORIENTED_EDGE ( 'NONE', *, *, #48141, .F. ) ;
#2430=PLANE ( 'NONE',  #15788 ) ;
#2431=DIRECTION ( 'NONE',  ( -1.000000000000000000, -0.000000000000000000, -0.000000000000000000 ) ) ;
#2433=FACE_OUTER_BOUND ( 'NONE', #29874, .T. ) ;
#2434=CARTESIAN_POINT ( 'NONE',  ( 0.000000000000000000, 3.267716535433071279, 1.259842519685033357 ) ) ;
#2435=LINE ( 'NONE', #6308, #49167 ) ;
#2436=EDGE_CURVE ( 'NONE', #4899, #1768, #42657, .T. ) ;
#2437=AXIS2_PLACEMENT_3D ( 'NONE', #42873, #3648, #27633 ) ;
#2438=ORIENTED_EDGE ( 'NONE', *, *, #12627, .F. ) ;
#2439=ORIENTED_EDGE ( 'NONE', *, *, #47362, .T. ) ;
#2441=PLANE ( 'NONE',  #10980 ) ;
#2442=LINE ( 'NONE', #23069, #27797 ) ;
#2446=AXIS2_PLACEMENT_3D ( 'NONE', #44744, #29779, #49357 ) ;
#2448=DIRECTION ( 'NONE',  ( 1.000000000000000000, -0.000000000000000000, 0.000000000000000000 ) ) ;
#2449=ORIENTED_EDGE ( 'NONE', *, *, #41484, .T. ) ;
#2450=ADVANCED_FACE ( 'NONE', ( #19911 ), #15046, .F. ) ;
#2454=VECTOR ( 'NONE', #29535, 39.37007874015748143 ) ;
#2455=CARTESIAN_POINT ( 'NONE',  ( -1.195183497228115035E-16, 0.000000000000000000, -0.9448818897637765168 ) ) ;
#2457=CARTESIAN_POINT ( 'NONE',  ( -1.439733046521776583, 3.346456692913386100, 1.574803149606291530 ) ) ;
#2458=ORIENTED_EDGE ( 'NONE', *, *, #17814, .F. ) ;
#2461=CARTESIAN_POINT ( 'NONE',  ( 0.7423782071083088185, 3.267716535433071279, -2.575641807848710687E-16 ) ) ;
#2462=VERTEX_POINT ( 'NONE', #23539 ) ;
#2463=EDGE_LOOP ( 'NONE', ( #36514, #44449, #11945, #18136 ) ) ;
#2464=LINE ( 'NONE', #11218, #15398 ) ;
#2465=CARTESIAN_POINT ( 'NONE',  ( 0.5455278134075211005, 3.346456692913386100, -1.141732283464564013 ) ) ;
#2467=DIRECTION ( 'NONE',  ( 0.000000000000000000, 0.000000000000000000, -1.000000000000000000 ) ) ;
#2469=CARTESIAN_POINT ( 'NONE',  ( 0.2727639067037604947, 0.000000000000000000, -0.1574803149606298636 ) ) ;
#2470=CARTESIAN_POINT ( 'NONE',  ( 0.5455278134075211005, 3.346456692913386100, -1.456692913385822630 ) ) ;
#2471=VERTEX_POINT ( 'NONE', #35429 ) ;
#2472=CARTESIAN_POINT ( 'NONE',  ( -0.6214413264104945434, 0.000000000000000000, 2.047244094488179567 ) ) ;
#2473=LINE ( 'NONE', #25960, #39681 ) ;
#2474=AXIS2_PLACEMENT_3D ( 'NONE', #2328, #5431, #10328 ) ;
#2475=VERTEX_POINT ( 'NONE', #46994 ) ;
#2477=EDGE_CURVE ( 'NONE', #17837, #8483, #23045, .T. ) ;
#2478=DIRECTION ( 'NONE',  ( -3.469446951953613696E-16, 0.000000000000000000, -1.000000000000000000 ) ) ;
#2479=ORIENTED_EDGE ( 'NONE', *, *, #48125, .T. ) ;
#2480=DIRECTION ( 'NONE',  ( -0.000000000000000000, 1.000000000000000000, -0.000000000000000000 ) ) ;
#2481=EDGE_CURVE ( 'NONE', #31368, #3488, #27410, .T. ) ;
#2484=CARTESIAN_POINT ( 'NONE',  ( 0.5455278134075212115, 0.000000000000000000, 0.3149606299212576177 ) ) ;
#2485=VERTEX_POINT ( 'NONE', #47508 ) ;
#2486=DIRECTION ( 'NONE',  ( 1.734723475976806848E-16, -0.000000000000000000, 1.000000000000000000 ) ) ;
#2487=VECTOR ( 'NONE', #3680, 39.37007874015748143 ) ;
#2488=ORIENTED_EDGE ( 'NONE', *, *, #37151, .F. ) ;
#2489=FACE_BOUND ( 'NONE', #33894, .T. ) ;
#2491=CARTESIAN_POINT ( 'NONE',  ( -1.166969139818015533, 3.346456692913386100, 1.102362204724404160 ) ) ;
#2493=EDGE_LOOP ( 'NONE', ( #47521, #11946, #18669, #38887 ) ) ;
#2494=EDGE_LOOP ( 'NONE', ( #14837, #42039, #15228, #6702 ) ) ;
#2495=CARTESIAN_POINT ( 'NONE',  ( 0.4696143004045478797, 3.267716535433071279, 0.2755905511810994302 ) ) ;
#2496=EDGE_CURVE ( 'NONE', #2241, #11767, #15297, .T. ) ;
#2497=DIRECTION ( 'NONE',  ( -0.000000000000000000, 0.000000000000000000, 1.000000000000000000 ) ) ;
#2501=ORIENTED_EDGE ( 'NONE', *, *, #36403, .T. ) ;
#2502=CARTESIAN_POINT ( 'NONE',  ( 0.8182917201112819283, 3.346456692913386100, -0.7874015748031473194 ) ) ;
#2504=DIRECTION ( 'NONE',  ( 1.000000000000000000, 0.000000000000000000, 0.000000000000000000 ) ) ;
#2507=EDGE_CURVE ( 'NONE', #27595, #23374, #27923, .T. ) ;
#2509=ORIENTED_EDGE ( 'NONE', *, *, #5915, .T. ) ;
#2510=ORIENTED_EDGE ( 'NONE', *, *, #37730, .F. ) ;
#2511=VECTOR ( 'NONE', #47422, 39.37007874015748143 ) ;
#2513=VERTEX_POINT ( 'NONE', #30794 ) ;
#2514=ORIENTED_EDGE ( 'NONE', *, *, #9698, .T. ) ;
#2515=CARTESIAN_POINT ( 'NONE',  ( -1.363819533518803473, 3.346456692913386100, -0.1574803149606300023 ) ) ;
#2516=ORIENTED_EDGE ( 'NONE', *, *, #37449, .T. ) ;
#2517=LINE ( 'NONE', #6131, #6491 ) ;
#2520=DIRECTION ( 'NONE',  ( 0.000000000000000000, 0.000000000000000000, 1.000000000000000000 ) ) ;
#2522=ORIENTED_EDGE ( 'NONE', *, *, #2990, .T. ) ;
#2526=DIRECTION ( 'NONE',  ( 0.000000000000000000, -1.000000000000000000, 0.000000000000000000 ) ) ;
#2530=VERTEX_POINT ( 'NONE', #46506 ) ;
#2531=CARTESIAN_POINT ( 'NONE',  ( 2.088192093915797631, 3.346456692913386100, 0.2755905511810994302 ) ) ;
#2533=EDGE_CURVE ( 'NONE', #32050, #39562, #3426, .T. ) ;
#2537=CARTESIAN_POINT ( 'NONE',  ( 0.7423782071083084855, 0.000000000000000000, -1.889763779527552812 ) ) ;
#2538=EDGE_CURVE ( 'NONE', #20750, #13112, #16574, .T. ) ;
#2539=DIRECTION ( 'NONE',  ( -0.000000000000000000, 1.000000000000000000, -0.000000000000000000 ) ) ;
#2540=AXIS2_PLACEMENT_3D ( 'NONE', #46306, #2467, #34218 ) ;
#2547=VERTEX_POINT ( 'NONE', #29913 ) ;
#2548=ORIENTED_EDGE ( 'NONE', *, *, #44835, .T. ) ;
#2549=DIRECTION ( 'NONE',  ( -0.000000000000000000, 1.000000000000000000, -0.000000000000000000 ) ) ;
#2551=CARTESIAN_POINT ( 'NONE',  ( 0.5455278134075217666, 0.000000000000000000, 1.889763779527550369 ) ) ;
#2552=VECTOR ( 'NONE', #28318, 39.37007874015748143 ) ;
#2554=ORIENTED_EDGE ( 'NONE', *, *, #25354, .F. ) ;
#2555=DIRECTION ( 'NONE',  ( -0.000000000000000000, 1.000000000000000000, -0.000000000000000000 ) ) ;
#2556=EDGE_CURVE ( 'NONE', #12830, #11574, #48021, .T. ) ;
#2558=DIRECTION ( 'NONE',  ( 1.000000000000000000, 0.000000000000000000, 0.000000000000000000 ) ) ;
#2559=ORIENTED_EDGE ( 'NONE', *, *, #23506, .F. ) ;
#2561=EDGE_CURVE ( 'NONE', #23674, #14569, #33805, .T. ) ;
#2563=FACE_BOUND ( 'NONE', #35204, .T. ) ;
#2566=DIRECTION ( 'NONE',  ( -1.000000000000000000, 0.000000000000000000, -0.000000000000000000 ) ) ;
#2567=VERTEX_POINT ( 'NONE', #28429 ) ;
#2571=ORIENTED_EDGE ( 'NONE', *, *, #24158, .F. ) ;
#2576=LINE ( 'NONE', #25557, #15910 ) ;
#2579=LINE ( 'NONE', #44910, #42834 ) ;
#2580=ORIENTED_EDGE ( 'NONE', *, *, #820, .F. ) ;
#2582=CARTESIAN_POINT ( 'NONE',  ( 0.2727639067037602172, 3.346456692913386100, -2.148105963102950877 ) ) ;
#2583=CARTESIAN_POINT ( 'NONE',  ( -0.6214413264104945434, 0.000000000000000000, -1.929133858267710000 ) ) ;
#2586=CARTESIAN_POINT ( 'NONE',  ( 1.015142113812069091, 3.267716535433071279, -1.614173228346451605 ) ) ;
#2588=VECTOR ( 'NONE', #14851, 39.37007874015748143 ) ;
#2589=DIRECTION ( 'NONE',  ( 1.734723475976806848E-16, -0.000000000000000000, 1.000000000000000000 ) ) ;
#2590=DIRECTION ( 'NONE',  ( -3.469446951953613696E-16, 0.000000000000000000, -1.000000000000000000 ) ) ;
#2591=EDGE_CURVE ( 'NONE', #39943, #48506, #44180, .T. ) ;
#2593=DIRECTION ( 'NONE',  ( -1.000000000000000000, 0.000000000000000000, 0.000000000000000000 ) ) ;
#2596=ORIENTED_EDGE ( 'NONE', *, *, #39324, .T. ) ;
#2597=EDGE_CURVE ( 'NONE', #12774, #42097, #17170, .T. ) ;
#2599=CARTESIAN_POINT ( 'NONE',  ( -1.439733046521776583, 3.267716535433071279, 1.537421584259135443 ) ) ;
#2601=EDGE_CURVE ( 'NONE', #32050, #50372, #6478, .T. ) ;
#2602=VERTEX_POINT ( 'NONE', #819 ) ;
#2603=LINE ( 'NONE', #42096, #19617 ) ;
#2604=ORIENTED_EDGE ( 'NONE', *, *, #46888, .F. ) ;
#2605=VECTOR ( 'NONE', #37851, 39.37007874015748143 ) ;
#2606=DIRECTION ( 'NONE',  ( 1.000000000000000000, -0.000000000000000000, 0.000000000000000000 ) ) ;
#2608=AXIS2_PLACEMENT_3D ( 'NONE', #18998, #15884, #11759 ) ;
#2610=ORIENTED_EDGE ( 'NONE', *, *, #40646, .F. ) ;
#2612=VECTOR ( 'NONE', #17528, 39.37007874015748143 ) ;
#2614=ORIENTED_EDGE ( 'NONE', *, *, #34073, .F. ) ;
#2615=ORIENTED_EDGE ( 'NONE', *, *, #12126, .F. ) ;
#2618=DIRECTION ( 'NONE',  ( -1.000000000000000000, 0.000000000000000000, -0.000000000000000000 ) ) ;
#2620=DIRECTION ( 'NONE',  ( -0.000000000000000000, 1.000000000000000000, -0.000000000000000000 ) ) ;
#2621=CARTESIAN_POINT ( 'NONE',  ( -1.091055626815042201, 3.267716535433071279, 1.062992125984246083 ) ) ;
#2622=AXIS2_PLACEMENT_3D ( 'NONE', #46495, #11164, #35672 ) ;
#2623=ORIENTED_EDGE ( 'NONE', *, *, #1211, .F. ) ;
#2625=FACE_OUTER_BOUND ( 'NONE', #19248, .T. ) ;
#2627=EDGE_LOOP ( 'NONE', ( #34197, #13549, #40584, #24964 ) ) ;
#2629=DIRECTION ( 'NONE',  ( -0.000000000000000000, 1.000000000000000000, -0.000000000000000000 ) ) ;
#2630=CARTESIAN_POINT ( 'NONE',  ( -1.363819533518803029, 0.000000000000000000, 0.4724409448818871482 ) ) ;
#2631=ORIENTED_EDGE ( 'NONE', *, *, #13029, .T. ) ;
#2632=EDGE_LOOP ( 'NONE', ( #19838, #19520, #47143, #50541 ) ) ;
#2635=DIRECTION ( 'NONE',  ( -0.000000000000000000, 1.000000000000000000, -0.000000000000000000 ) ) ;
#2636=DIRECTION ( 'NONE',  ( -1.000000000000000000, 0.000000000000000000, -0.000000000000000000 ) ) ;
#2642=ORIENTED_EDGE ( 'NONE', *, *, #20952, .T. ) ;
#2644=LINE ( 'NONE', #18391, #26774 ) ;
#2645=AXIS2_PLACEMENT_3D ( 'NONE', #23311, #43176, #38573 ) ;
#2647=CARTESIAN_POINT ( 'NONE',  ( -1.166969139818016199, 3.346456692913386100, -0.9842519685039344823 ) ) ;
#2648=AXIS2_PLACEMENT_3D ( 'NONE', #26799, #42292, #18811 ) ;
#2649=CARTESIAN_POINT ( 'NONE',  ( -0.6214413264104939882, 0.000000000000000000, 1.220472440944875281 ) ) ;
#2650=ORIENTED_EDGE ( 'NONE', *, *, #27329, .F. ) ;
#2653=VECTOR ( 'NONE', #29557, 39.37007874015748143 ) ;
#2654=LINE ( 'NONE', #15034, #19100 ) ;
#2656=ORIENTED_EDGE ( 'NONE', *, *, #21895, .T. ) ;
#2657=AXIS2_PLACEMENT_3D ( 'NONE', #3801, #26776, #19279 ) ;
#2658=LINE ( 'NONE', #10664, #24883 ) ;
#2660=CARTESIAN_POINT ( 'NONE',  ( 1.363819533518803251, 0.000000000000000000, 0.2755905511810996522 ) ) ;
#2661=ADVANCED_FACE ( 'NONE', ( #5908 ), #43920, .F. ) ;
#2662=ORIENTED_EDGE ( 'NONE', *, *, #41443, .F. ) ;
#2663=EDGE_CURVE ( 'NONE', #31145, #39431, #12433, .T. ) ;
#2664=CARTESIAN_POINT ( 'NONE',  ( 2.378961647330872786, 3.267716535433071279, -1.161035397307311917E-15 ) ) ;
#2665=ORIENTED_EDGE ( 'NONE', *, *, #21611, .F. ) ;
#2668=CARTESIAN_POINT ( 'NONE',  ( -1.091055626815042645, 0.000000000000000000, 1.692913385826762873 ) ) ;
#2669=CARTESIAN_POINT ( 'NONE',  ( 1.015142113812069091, 3.267716535433071279, -3.521981712565030910E-16 ) ) ;
#2672=ADVANCED_FACE ( 'NONE', ( #21658 ), #2041, .F. ) ;
#2674=ORIENTED_EDGE ( 'NONE', *, *, #19897, .F. ) ;
#2675=DIRECTION ( 'NONE',  ( -3.469446951953613696E-16, 0.000000000000000000, -1.000000000000000000 ) ) ;
#2677=VERTEX_POINT ( 'NONE', #6170 ) ;
#2678=FACE_OUTER_BOUND ( 'NONE', #15132, .T. ) ;
#2679=CARTESIAN_POINT ( 'NONE',  ( 0.8182917201112819283, 3.267716535433071279, 0.2755905511810994302 ) ) ;
#2680=CARTESIAN_POINT ( 'NONE',  ( 0.7423782071083085965, 3.346456692913386100, 0.7480314960629872445 ) ) ;
#2681=ORIENTED_EDGE ( 'NONE', *, *, #39283, .F. ) ;
#2683=ORIENTED_EDGE ( 'NONE', *, *, #29505, .T. ) ;
#2686=EDGE_CURVE ( 'NONE', #3807, #4133, #21919, .T. ) ;
#2687=LINE ( 'NONE', #42175, #23899 ) ;
#2691=FACE_BOUND ( 'NONE', #4794, .T. ) ;
#2692=EDGE_LOOP ( 'NONE', ( #31759, #49098, #33816, #34064 ) ) ;
#2693=CARTESIAN_POINT ( 'NONE',  ( -0.5455278134075216556, 3.267716535433071279, -2.381957271744193250 ) ) ;
#2694=ORIENTED_EDGE ( 'NONE', *, *, #4583, .T. ) ;
#2695=EDGE_LOOP ( 'NONE', ( #5623, #45545, #49439, #35314 ) ) ;
#2698=ADVANCED_FACE ( 'NONE', ( #2802 ), #6928, .F. ) ;
#2702=CARTESIAN_POINT ( 'NONE',  ( 0.000000000000000000, 3.267716535433071279, 0.2755905511810994302 ) ) ;
#2703=LINE ( 'NONE', #49144, #46078 ) ;
#2704=ORIENTED_EDGE ( 'NONE', *, *, #16102, .T. ) ;
#2705=EDGE_CURVE ( 'NONE', #9409, #7396, #46141, .T. ) ;
#2706=ORIENTED_EDGE ( 'NONE', *, *, #24843, .F. ) ;
#2710=DIRECTION ( 'NONE',  ( 0.000000000000000000, -1.000000000000000000, 0.000000000000000000 ) ) ;
#2711=DIRECTION ( 'NONE',  ( 1.000000000000000000, -0.000000000000000000, 0.000000000000000000 ) ) ;
#2713=VERTEX_POINT ( 'NONE', #37928 ) ;
#2714=CARTESIAN_POINT ( 'NONE',  ( -0.5455278134075214336, 0.000000000000000000, -0.6299212598425175669 ) ) ;
#2716=ADVANCED_FACE ( 'NONE', ( #46883 ), #49993, .F. ) ;
#2717=ORIENTED_EDGE ( 'NONE', *, *, #28917, .F. ) ;
#2718=LINE ( 'NONE', #34724, #2588 ) ;
#2723=LINE ( 'NONE', #46070, #30082 ) ;
#2724=EDGE_CURVE ( 'NONE', #25196, #30067, #46639, .T. ) ;
#2725=LINE ( 'NONE', #14603, #23525 ) ;
#2726=VECTOR ( 'NONE', #30564, 39.37007874015748143 ) ;
#2728=ORIENTED_EDGE ( 'NONE', *, *, #47181, .T. ) ;
#2729=CARTESIAN_POINT ( 'NONE',  ( -0.8942052331142552601, 0.000000000000000000, -7.512581982576723358E-16 ) ) ;
#2730=ORIENTED_EDGE ( 'NONE', *, *, #40773, .T. ) ;
#2731=FACE_BOUND ( 'NONE', #13357, .T. ) ;
#2732=CARTESIAN_POINT ( 'NONE',  ( -0.3486774197067334380, 0.000000000000000000, 0.6299212598425164567 ) ) ;
#2733=VECTOR ( 'NONE', #11892, 39.37007874015748143 ) ;
#2734=LINE ( 'NONE', #26471, #39983 ) ;
#2735=LINE ( 'NONE', #17723, #2918 ) ;
#2737=ORIENTED_EDGE ( 'NONE', *, *, #32580, .F. ) ;
#2740=CARTESIAN_POINT ( 'NONE',  ( -1.636583440222564301, 3.267716535433071279, -1.456692913385822186 ) ) ;
#2741=DIRECTION ( 'NONE',  ( -0.000000000000000000, 1.000000000000000000, -0.000000000000000000 ) ) ;
#2742=DIRECTION ( 'NONE',  ( 1.734723475976806848E-16, -0.000000000000000000, 1.000000000000000000 ) ) ;
#2743=DIRECTION ( 'NONE',  ( 0.000000000000000000, 0.000000000000000000, 1.000000000000000000 ) ) ;
#2744=ORIENTED_EDGE ( 'NONE', *, *, #7404, .F. ) ;
#2745=VERTEX_POINT ( 'NONE', #3055 ) ;
#2746=DIRECTION ( 'NONE',  ( -0.000000000000000000, 1.000000000000000000, -0.000000000000000000 ) ) ;
#2747=EDGE_CURVE ( 'NONE', #43721, #6632, #45887, .T. ) ;
#2749=CARTESIAN_POINT ( 'NONE',  ( 0.2727639067037602172, 3.346456692913386100, -1.929133858267710000 ) ) ;
#2750=ORIENTED_EDGE ( 'NONE', *, *, #47124, .F. ) ;
#2751=CARTESIAN_POINT ( 'NONE',  ( 1.015142113812069313, 3.267716535433071279, 0.1574803149606286423 ) ) ;
#2752=VERTEX_POINT ( 'NONE', #14928 ) ;
#2753=VERTEX_POINT ( 'NONE', #10795 ) ;
#2754=EDGE_CURVE ( 'NONE', #3488, #51000, #14678, .T. ) ;
#2758=ORIENTED_EDGE ( 'NONE', *, *, #18868, .T. ) ;
#2759=DIRECTION ( 'NONE',  ( 1.734723475976806848E-16, -0.000000000000000000, 1.000000000000000000 ) ) ;
#2760=AXIS2_PLACEMENT_3D ( 'NONE', #17106, #41615, #20974 ) ;
#2761=ORIENTED_EDGE ( 'NONE', *, *, #15896, .T. ) ;
#2762=VECTOR ( 'NONE', #2856, 39.37007874015748143 ) ;
#2763=DIRECTION ( 'NONE',  ( 1.734723475976806848E-16, 0.000000000000000000, 1.000000000000000000 ) ) ;
#2765=VECTOR ( 'NONE', #3754, 39.37007874015748143 ) ;
#2769=DIRECTION ( 'NONE',  ( 5.175581015019631661E-17, -0.9063077870366510469, 0.4226182617406972208 ) ) ;
#2770=FACE_OUTER_BOUND ( 'NONE', #15780, .T. ) ;
#2775=CARTESIAN_POINT ( 'NONE',  ( -1.091055626815042645, 3.346456692913386100, -1.259842519685034690 ) ) ;
#2776=CARTESIAN_POINT ( 'NONE',  ( 1.560669927219590525, 3.346456692913386100, -0.6692913385826764205 ) ) ;
#2777=EDGE_CURVE ( 'NONE', #42794, #19022, #7185, .T. ) ;
#2778=VERTEX_POINT ( 'NONE', #22926 ) ;
#2779=DIRECTION ( 'NONE',  ( 0.000000000000000000, -1.000000000000000000, 0.000000000000000000 ) ) ;
#2780=CARTESIAN_POINT ( 'NONE',  ( 1.015142113812069313, 3.267716535433071279, -1.102362204724405714 ) ) ;
#2782=CARTESIAN_POINT ( 'NONE',  ( -0.8942052331142547050, 0.000000000000000000, 1.259842519685033357 ) ) ;
#2785=CARTESIAN_POINT ( 'NONE',  ( -0.5455278134075214336, 3.346456692913386100, -1.141732283464563791 ) ) ;
#2786=EDGE_CURVE ( 'NONE', #11424, #14385, #19042, .T. ) ;
#2788=EDGE_CURVE ( 'NONE', #18489, #46962, #42284, .T. ) ;
#2789=CARTESIAN_POINT ( 'NONE',  ( 1.833433833923351353, 3.346456692913386100, -0.6299212598425181220 ) ) ;
#2790=ORIENTED_EDGE ( 'NONE', *, *, #43736, .T. ) ;
#2791=FACE_OUTER_BOUND ( 'NONE', #36958, .T. ) ;
#2793=DIRECTION ( 'NONE',  ( 1.000000000000000000, 0.000000000000000000, 0.000000000000000000 ) ) ;
#2795=DIRECTION ( 'NONE',  ( 1.734723475976806848E-16, -0.000000000000000000, 1.000000000000000000 ) ) ;
#2796=ORIENTED_EDGE ( 'NONE', *, *, #45299, .T. ) ;
#2800=ORIENTED_EDGE ( 'NONE', *, *, #6201, .T. ) ;
#2801=VECTOR ( 'NONE', #44909, 39.37007874015748143 ) ;
#2802=FACE_OUTER_BOUND ( 'NONE', #12291, .T. ) ;
#2803=VERTEX_POINT ( 'NONE', #18294 ) ;
#2804=DIRECTION ( 'NONE',  ( -1.000000000000000000, -0.000000000000000000, -0.000000000000000000 ) ) ;
#2805=AXIS2_PLACEMENT_3D ( 'NONE', #30159, #38173, #18543 ) ;
#2806=DIRECTION ( 'NONE',  ( -0.000000000000000000, 1.000000000000000000, -0.000000000000000000 ) ) ;
#2811=DIRECTION ( 'NONE',  ( -0.000000000000000000, 1.000000000000000000, -0.000000000000000000 ) ) ;
#2812=VECTOR ( 'NONE', #22468, 39.37007874015748143 ) ;
#2813=CARTESIAN_POINT ( 'NONE',  ( 1.636583440222563857, 0.000000000000000000, -1.161035397307311917E-15 ) ) ;
#2814=EDGE_LOOP ( 'NONE', ( #41167, #32354, #23924, #9809 ) ) ;
#2815=ORIENTED_EDGE ( 'NONE', *, *, #298, .T. ) ;
#2816=LINE ( 'NONE', #29927, #16627 ) ;
#2817=FACE_BOUND ( 'NONE', #22157, .T. ) ;
#2818=ORIENTED_EDGE ( 'NONE', *, *, #26777, .F. ) ;
#2819=CARTESIAN_POINT ( 'NONE',  ( 0.2727639067037610499, 0.000000000000000000, 1.102362204724404160 ) ) ;
#2820=CARTESIAN_POINT ( 'NONE',  ( 2.076281802138679300, 3.267716535433071279, -0.3543307086614178592 ) ) ;
#2821=EDGE_CURVE ( 'NONE', #1831, #22006, #14423, .T. ) ;
#2822=VERTEX_POINT ( 'NONE', #26294 ) ;
#2823=ORIENTED_EDGE ( 'NONE', *, *, #10811, .F. ) ;
#2824=CARTESIAN_POINT ( 'NONE',  ( -0.8182917201112818173, 3.267716535433071279, 1.419509857074483292E-16 ) ) ;
#2825=EDGE_CURVE ( 'NONE', #38085, #18489, #42040, .T. ) ;
#2830=ORIENTED_EDGE ( 'NONE', *, *, #23546, .T. ) ;
#2833=DIRECTION ( 'NONE',  ( -0.000000000000000000, 1.000000000000000000, -0.000000000000000000 ) ) ;
#2836=FACE_OUTER_BOUND ( 'NONE', #27778, .T. ) ;
#2837=PLANE ( 'NONE',  #45935 ) ;
#2838=VECTOR ( 'NONE', #24868, 39.37007874015748143 ) ;
#2839=LINE ( 'NONE', #29444, #14263 ) ;
#2840=EDGE_CURVE ( 'NONE', #1425, #25537, #35818, .T. ) ;
#2842=VECTOR ( 'NONE', #47643, 39.37007874015748143 ) ;
#2845=EDGE_CURVE ( 'NONE', #16391, #11818, #4579, .T. ) ;
#2848=CIRCLE ( 'NONE', #9450, 2.952755905511811552 ) ;
#2849=ORIENTED_EDGE ( 'NONE', *, *, #23615, .F. ) ;
#2850=LINE ( 'NONE', #38726, #12680 ) ;
#2851=DIRECTION ( 'NONE',  ( -0.000000000000000000, 1.000000000000000000, -0.000000000000000000 ) ) ;
#2853=EDGE_CURVE ( 'NONE', #1578, #12830, #23940, .T. ) ;
#2854=VERTEX_POINT ( 'NONE', #447 ) ;
#2855=ORIENTED_EDGE ( 'NONE', *, *, #43113, .F. ) ;
#2856=DIRECTION ( 'NONE',  ( -1.000000000000000000, -0.000000000000000000, -0.000000000000000000 ) ) ;
#2857=DIRECTION ( 'NONE',  ( -1.000000000000000000, -0.000000000000000000, -0.000000000000000000 ) ) ;
#2859=ORIENTED_EDGE ( 'NONE', *, *, #12292, .F. ) ;
#2860=CARTESIAN_POINT ( 'NONE',  ( 0.000000000000000000, 3.267716535433071279, -0.03937007874015881204 ) ) ;
#2861=ORIENTED_EDGE ( 'NONE', *, *, #45624, .F. ) ;
#2862=CARTESIAN_POINT ( 'NONE',  ( 1.363819533518803029, 3.346456692913386100, -1.299212598425193210 ) ) ;
#2863=CARTESIAN_POINT ( 'NONE',  ( 0.8182917201112819283, 0.000000000000000000, 0.4724409448818868706 ) ) ;
#2864=ORIENTED_EDGE ( 'NONE', *, *, #5171, .F. ) ;
#2867=VECTOR ( 'NONE', #49148, 39.37007874015748143 ) ;
#2868=ORIENTED_EDGE ( 'NONE', *, *, #21726, .T. ) ;
#2869=VERTEX_POINT ( 'NONE', #50989 ) ;
#2875=AXIS2_PLACEMENT_3D ( 'NONE', #21279, #21789, #13790 ) ;
#2876=EDGE_LOOP ( 'NONE', ( #31617, #49159, #47406, #47144 ) ) ;
#2877=FACE_OUTER_BOUND ( 'NONE', #39614, .T. ) ;
#2878=LINE ( 'NONE', #30248, #21744 ) ;
#2879=CARTESIAN_POINT ( 'NONE',  ( -0.2727639067037611054, 3.267716535433071279, -2.244094488188968395 ) ) ;
#2882=EDGE_CURVE ( 'NONE', #10927, #9086, #12324, .T. ) ;
#2883=VECTOR ( 'NONE', #27287, 39.37007874015748143 ) ;
#2884=EDGE_CURVE ( 'NONE', #13726, #31313, #19796, .T. ) ;
#2885=ORIENTED_EDGE ( 'NONE', *, *, #3547, .F. ) ;
#2886=ORIENTED_EDGE ( 'NONE', *, *, #18926, .F. ) ;
#2888=EDGE_CURVE ( 'NONE', #50909, #6728, #4319, .T. ) ;
#2889=DIRECTION ( 'NONE',  ( -3.469446951953613696E-16, 0.000000000000000000, -1.000000000000000000 ) ) ;
#2891=LINE ( 'NONE', #19131, #26344 ) ;
#2892=ORIENTED_EDGE ( 'NONE', *, *, #18984, .F. ) ;
#2896=EDGE_LOOP ( 'NONE', ( #11511, #30166, #37758, #3468 ) ) ;
#2898=DIRECTION ( 'NONE',  ( 1.000000000000000000, -0.000000000000000000, 0.000000000000000000 ) ) ;
#2905=DIRECTION ( 'NONE',  ( -0.000000000000000000, 0.000000000000000000, 1.000000000000000000 ) ) ;
#2908=EDGE_CURVE ( 'NONE', #19682, #37143, #20049, .T. ) ;
#2909=VECTOR ( 'NONE', #33784, 39.37007874015748143 ) ;
#2911=VECTOR ( 'NONE', #27412, 39.37007874015748143 ) ;
#2913=CARTESIAN_POINT ( 'NONE',  ( 0.2727639067037610499, 0.000000000000000000, 1.732283464566921172 ) ) ;
#2914=DIRECTION ( 'NONE',  ( -1.000000000000000000, 0.000000000000000000, 1.734723475976806848E-16 ) ) ;
#2915=CARTESIAN_POINT ( 'NONE',  ( 0.000000000000000000, 3.346456692913386100, 0.000000000000000000 ) ) ;
#2918=VECTOR ( 'NONE', #6863, 39.37007874015748143 ) ;
#2919=VERTEX_POINT ( 'NONE', #32470 ) ;
#2920=CARTESIAN_POINT ( 'NONE',  ( 4.268512490100411402E-16, 0.000000000000000000, 1.889763779527550369 ) ) ;
#2922=VERTEX_POINT ( 'NONE', #48161 ) ;
#2923=CARTESIAN_POINT ( 'NONE',  ( -1.439733046521776139, 3.267716535433071279, 4.995077429881866871E-16 ) ) ;
#2926=CARTESIAN_POINT ( 'NONE',  ( 0.1968503937007877735, 3.346456692913386100, 2.007874015748021268 ) ) ;
#2927=CARTESIAN_POINT ( 'NONE',  ( 0.000000000000000000, 3.346456692913386100, 0.000000000000000000 ) ) ;
#2928=ORIENTED_EDGE ( 'NONE', *, *, #1306, .T. ) ;
#2929=EDGE_LOOP ( 'NONE', ( #48498, #46715, #10632, #31822 ) ) ;
#2931=FACE_OUTER_BOUND ( 'NONE', #46094, .T. ) ;
#2932=CARTESIAN_POINT ( 'NONE',  ( -0.3486774197067334380, 0.000000000000000000, 1.574803149606291974 ) ) ;
#2934=LINE ( 'NONE', #43165, #19836 ) ;
#2935=DIRECTION ( 'NONE',  ( 1.734723475976806848E-16, -0.000000000000000000, 1.000000000000000000 ) ) ;
#2936=DIRECTION ( 'NONE',  ( -1.000000000000000000, 0.000000000000000000, 1.734723475976806848E-16 ) ) ;
#2937=ORIENTED_EDGE ( 'NONE', *, *, #19497, .F. ) ;
#2939=CARTESIAN_POINT ( 'NONE',  ( 0.000000000000000000, 3.267716535433071279, -0.9842519685039348154 ) ) ;
#2940=PLANE ( 'NONE',  #27436 ) ;
#2941=FACE_OUTER_BOUND ( 'NONE', #42130, .T. ) ;
#2944=CARTESIAN_POINT ( 'NONE',  ( 0.000000000000000000, 3.346456692913386100, 0.000000000000000000 ) ) ;
#2947=EDGE_CURVE ( 'NONE', #2091, #45399, #27055, .T. ) ;
#2948=VECTOR ( 'NONE', #6704, 39.37007874015748143 ) ;
#2949=DIRECTION ( 'NONE',  ( 1.000000000000000000, -0.000000000000000000, 0.000000000000000000 ) ) ;
#2950=ORIENTED_EDGE ( 'NONE', *, *, #11989, .F. ) ;
#2952=CARTESIAN_POINT ( 'NONE',  ( -3.927031490892378253E-16, 3.346456692913386100, -1.889763779527552146 ) ) ;
#2954=VECTOR ( 'NONE', #26237, 39.37007874015748143 ) ;
#2955=EDGE_CURVE ( 'NONE', #28023, #10001, #47392, .T. ) ;
#2956=CARTESIAN_POINT ( 'NONE',  ( 1.091055626815042645, 3.346456692913386100, -0.6299212598425181220 ) ) ;
#2959=CARTESIAN_POINT ( 'NONE',  ( 0.000000000000000000, 3.346456692913386100, 0.000000000000000000 ) ) ;
#2960=EDGE_CURVE ( 'NONE', #29593, #41945, #40210, .T. ) ;
#2961=CARTESIAN_POINT ( 'NONE',  ( -0.2727639067037602172, 0.000000000000000000, 1.102362204724404160 ) ) ;
#2962=ORIENTED_EDGE ( 'NONE', *, *, #44917, .T. ) ;
#2964=ORIENTED_EDGE ( 'NONE', *, *, #34389, .T. ) ;
#2965=CARTESIAN_POINT ( 'NONE',  ( -0.07591351300297333182, 3.346456692913386100, -0.4724409448818883694 ) ) ;
#2966=CARTESIAN_POINT ( 'NONE',  ( 2.106197740627111514, 3.267716535433071279, -0.9842519685039348154 ) ) ;
#2967=EDGE_CURVE ( 'NONE', #10846, #6843, #27291, .T. ) ;
#2968=FACE_OUTER_BOUND ( 'NONE', #1001, .T. ) ;
#2969=FACE_OUTER_BOUND ( 'NONE', #29696, .T. ) ;
#2970=PLANE ( 'NONE',  #15481 ) ;
#2971=ORIENTED_EDGE ( 'NONE', *, *, #34380, .T. ) ;
#2972=LINE ( 'NONE', #2714, #19200 ) ;
#2973=EDGE_CURVE ( 'NONE', #41852, #6627, #24198, .T. ) ;
#2974=DIRECTION ( 'NONE',  ( 1.000000000000000000, 0.000000000000000000, 0.000000000000000000 ) ) ;
#2975=ORIENTED_EDGE ( 'NONE', *, *, #30199, .F. ) ;
#2976=PLANE ( 'NONE',  #5867 ) ;
#2977=DIRECTION ( 'NONE',  ( -3.469446951953613696E-16, 0.000000000000000000, -1.000000000000000000 ) ) ;
#2978=ORIENTED_EDGE ( 'NONE', *, *, #2980, .T. ) ;
#2979=FACE_OUTER_BOUND ( 'NONE', #5943, .T. ) ;
#2980=EDGE_CURVE ( 'NONE', #22076, #22611, #4838, .T. ) ;
#2982=FACE_OUTER_BOUND ( 'NONE', #9514, .T. ) ;
#2983=CARTESIAN_POINT ( 'NONE',  ( 0.000000000000000000, 3.267716535433071279, 0.000000000000000000 ) ) ;
#2984=VECTOR ( 'NONE', #37724, 39.37007874015748143 ) ;
#2985=VECTOR ( 'NONE', #18006, 39.37007874015748143 ) ;
#2988=VERTEX_POINT ( 'NONE', #1719 ) ;
#2989=FACE_BOUND ( 'NONE', #1345, .T. ) ;
#2990=EDGE_CURVE ( 'NONE', #48375, #11317, #32985, .T. ) ;
#2991=VECTOR ( 'NONE', #47268, 39.37007874015748143 ) ;
#2993=DIRECTION ( 'NONE',  ( 1.000000000000000000, -0.000000000000000000, 0.000000000000000000 ) ) ;
#2994=AXIS2_PLACEMENT_3D ( 'NONE', #331, #11697, #23564 ) ;
#2995=VECTOR ( 'NONE', #38127, 39.37007874015748143 ) ;
#2998=DIRECTION ( 'NONE',  ( 1.000000000000000000, -0.000000000000000000, 0.000000000000000000 ) ) ;
#2999=PLANE ( 'NONE',  #7327 ) ;
#3000=EDGE_CURVE ( 'NONE', #5416, #8542, #33236, .T. ) ;
#3005=ORIENTED_EDGE ( 'NONE', *, *, #39189, .T. ) ;
#3006=ORIENTED_EDGE ( 'NONE', *, *, #37184, .F. ) ;
#3007=DIRECTION ( 'NONE',  ( -3.469446951953613696E-16, 0.000000000000000000, -1.000000000000000000 ) ) ;
#3008=CARTESIAN_POINT ( 'NONE',  ( 2.182111253630085290, 3.346456692913386100, 0.3149606299212573401 ) ) ;
#3010=DIRECTION ( 'NONE',  ( -1.000000000000000000, 0.000000000000000000, -0.000000000000000000 ) ) ;
#3012=ORIENTED_EDGE ( 'NONE', *, *, #26199, .F. ) ;
#3013=EDGE_CURVE ( 'NONE', #14432, #17810, #1215, .T. ) ;
#3014=VECTOR ( 'NONE', #8179, 39.37007874015748143 ) ;
#3015=EDGE_LOOP ( 'NONE', ( #4364, #35256, #17032, #19002 ) ) ;
#3016=VERTEX_POINT ( 'NONE', #36847 ) ;
#3017=LINE ( 'NONE', #3516, #539 ) ;
#3018=EDGE_CURVE ( 'NONE', #13176, #3567, #41229, .T. ) ;
#3019=VECTOR ( 'NONE', #7593, 39.37007874015748143 ) ;
#3021=LINE ( 'NONE', #11524, #17188 ) ;
#3022=DIRECTION ( 'NONE',  ( -3.469446951953613696E-16, 0.000000000000000000, -1.000000000000000000 ) ) ;
#3024=LINE ( 'NONE', #22392, #28878 ) ;
#3025=VECTOR ( 'NONE', #40345, 39.37007874015748143 ) ;
#3029=CARTESIAN_POINT ( 'NONE',  ( 1.287906020515830141, 3.267716535433071279, -0.9448818897637765168 ) ) ;
#3030=DIRECTION ( 'NONE',  ( 1.000000000000000000, 0.000000000000000000, 0.000000000000000000 ) ) ;
#3032=CARTESIAN_POINT ( 'NONE',  ( 0.7423782071083087075, 0.000000000000000000, -0.3149606299212593941 ) ) ;
#3033=VERTEX_POINT ( 'NONE', #9979 ) ;
#3035=DIRECTION ( 'NONE',  ( -3.469446951953613696E-16, 0.000000000000000000, -1.000000000000000000 ) ) ;
#3036=VERTEX_POINT ( 'NONE', #21097 ) ;
#3038=ADVANCED_FACE ( 'NONE', ( #9216 ), #5598, .F. ) ;
#3039=CARTESIAN_POINT ( 'NONE',  ( 0.8182917201112819283, 3.346456692913386100, -0.03937007874015881204 ) ) ;
#3040=LINE ( 'NONE', #7171, #42231 ) ;
#3041=EDGE_LOOP ( 'NONE', ( #43908, #38007, #8061, #47649 ) ) ;
#3043=EDGE_CURVE ( 'NONE', #19314, #50260, #45214, .T. ) ;
#3046=EDGE_CURVE ( 'NONE', #40619, #41687, #48916, .T. ) ;
#3049=ORIENTED_EDGE ( 'NONE', *, *, #27749, .F. ) ;
#3050=EDGE_CURVE ( 'NONE', #26629, #49397, #13857, .T. ) ;
#3052=VECTOR ( 'NONE', #32500, 39.37007874015748143 ) ;
#3053=ORIENTED_EDGE ( 'NONE', *, *, #38808, .F. ) ;
#3055=CARTESIAN_POINT ( 'NONE',  ( 2.378961647330872786, 3.267716535433071279, 0.4330708661417287386 ) ) ;
#3057=ADVANCED_FACE ( 'NONE', ( #21859 ), #37101, .F. ) ;
#3059=CARTESIAN_POINT ( 'NONE',  ( -1.439733046521777027, 0.000000000000000000, -0.8267716535433052849 ) ) ;
#3060=EDGE_LOOP ( 'NONE', ( #35581, #1737, #1454, #39950 ) ) ;
#3061=LINE ( 'NONE', #33557, #6644 ) ;
#3065=VERTEX_POINT ( 'NONE', #25468 ) ;
#3067=CARTESIAN_POINT ( 'NONE',  ( 0.000000000000000000, 3.267716535433071279, -0.3149606299212589500 ) ) ;
#3068=FACE_BOUND ( 'NONE', #5329, .T. ) ;
#3070=ADVANCED_FACE ( 'NONE', ( #44819 ), #20837, .F. ) ;
#3072=ORIENTED_EDGE ( 'NONE', *, *, #45485, .F. ) ;
#3074=EDGE_CURVE ( 'NONE', #35684, #49197, #17473, .T. ) ;
#3075=CARTESIAN_POINT ( 'NONE',  ( 0.1968503937007870241, 0.000000000000000000, -2.204724409448811429 ) ) ;
#3079=DIRECTION ( 'NONE',  ( -1.000000000000000000, 0.000000000000000000, -0.000000000000000000 ) ) ;
#3080=ORIENTED_EDGE ( 'NONE', *, *, #39447, .F. ) ;
#3081=FACE_OUTER_BOUND ( 'NONE', #25459, .T. ) ;
#3082=CARTESIAN_POINT ( 'NONE',  ( 0.000000000000000000, 3.267716535433071279, 0.000000000000000000 ) ) ;
#3083=VECTOR ( 'NONE', #15575, 39.37007874015748143 ) ;
#3084=AXIS2_PLACEMENT_3D ( 'NONE', #32579, #27655, #28165 ) ;
#3085=CARTESIAN_POINT ( 'NONE',  ( 1.560669927219590747, 3.267716535433071279, -0.7874015748031473194 ) ) ;
#3086=VERTEX_POINT ( 'NONE', #45072 ) ;
#3087=ORIENTED_EDGE ( 'NONE', *, *, #6730, .T. ) ;
#3095=CARTESIAN_POINT ( 'NONE',  ( -0.2727639067037611054, 3.346456692913386100, -2.088563196121306476 ) ) ;
#3098=VECTOR ( 'NONE', #24688, 39.37007874015748143 ) ;
#3099=ORIENTED_EDGE ( 'NONE', *, *, #48780, .F. ) ;
#3100=EDGE_LOOP ( 'NONE', ( #662, #12203, #29239, #4476 ) ) ;
#3103=EDGE_CURVE ( 'NONE', #10488, #3716, #29608, .T. ) ;
#3105=ADVANCED_FACE ( 'NONE', ( #44318 ), #5086, .F. ) ;
#3107=ORIENTED_EDGE ( 'NONE', *, *, #7943, .F. ) ;
#3108=CARTESIAN_POINT ( 'NONE',  ( -1.363819533518803473, 3.267716535433071279, 1.850393700787392293 ) ) ;
#3109=ORIENTED_EDGE ( 'NONE', *, *, #2561, .F. ) ;
#3110=DIRECTION ( 'NONE',  ( -0.000000000000000000, 0.000000000000000000, 1.000000000000000000 ) ) ;
#3114=VERTEX_POINT ( 'NONE', #2495 ) ;
#3116=VERTEX_POINT ( 'NONE', #38618 ) ;
#3118=LINE ( 'NONE', #8209, #14111 ) ;
#3120=DIRECTION ( 'NONE',  ( 1.000000000000000000, 0.000000000000000000, 0.000000000000000000 ) ) ;
#3121=FACE_OUTER_BOUND ( 'NONE', #40793, .T. ) ;
#3122=VECTOR ( 'NONE', #12651, 39.37007874015748143 ) ;
#3123=EDGE_CURVE ( 'NONE', #10682, #13031, #19235, .T. ) ;
#3124=ORIENTED_EDGE ( 'NONE', *, *, #27710, .T. ) ;
#3125=EDGE_CURVE ( 'NONE', #50633, #39173, #22867, .T. ) ;
#3126=CARTESIAN_POINT ( 'NONE',  ( 1.363819533518803251, 3.267716535433071279, -0.4724409448818889246 ) ) ;
#3128=LINE ( 'NONE', #18372, #47554 ) ;
#3133=EDGE_CURVE ( 'NONE', #15165, #40291, #26259, .T. ) ;
#3134=ORIENTED_EDGE ( 'NONE', *, *, #37768, .F. ) ;
#3137=CONICAL_SURFACE ( 'NONE', #5614, 2.493791675044291445, 0.4363323129985800519 ) ;
#3138=LINE ( 'NONE', #15011, #21833 ) ;
#3139=DIRECTION ( 'NONE',  ( -1.000000000000000000, 0.000000000000000000, -0.000000000000000000 ) ) ;
#3140=CARTESIAN_POINT ( 'NONE',  ( -2.182111253630085290, 3.267716535433071279, 3.785359618865289765E-16 ) ) ;
#3141=DIRECTION ( 'NONE',  ( -3.469446951953613696E-16, 0.000000000000000000, -1.000000000000000000 ) ) ;
#3144=CARTESIAN_POINT ( 'NONE',  ( 0.8182917201112819283, 3.346456692913386100, -0.6692913385826764205 ) ) ;
#3145=CARTESIAN_POINT ( 'NONE',  ( 0.2727639067037604392, 3.346456692913386100, -0.3543307086614173040 ) ) ;
#3149=VECTOR ( 'NONE', #15678, 39.37007874015748143 ) ;
#3152=CARTESIAN_POINT ( 'NONE',  ( 0.000000000000000000, 3.267716535433071279, 0.000000000000000000 ) ) ;
#3154=CARTESIAN_POINT ( 'NONE',  ( 0.000000000000000000, 3.267716535433071279, -0.9448818897637765168 ) ) ;
#3156=VECTOR ( 'NONE', #2196, 39.37007874015748143 ) ;
#3157=CARTESIAN_POINT ( 'NONE',  ( -1.863748091109392879, 3.346456692913386100, 1.102362204724404160 ) ) ;
#3161=DIRECTION ( 'NONE',  ( 1.734723475976806848E-16, 0.000000000000000000, 1.000000000000000000 ) ) ;
#3162=DIRECTION ( 'NONE',  ( 0.000000000000000000, 0.000000000000000000, 1.000000000000000000 ) ) ;
#3163=ORIENTED_EDGE ( 'NONE', *, *, #16884, .F. ) ;
#3167=EDGE_CURVE ( 'NONE', #22305, #31088, #14871, .T. ) ;
#3169=DIRECTION ( 'NONE',  ( -1.000000000000000000, 0.000000000000000000, 0.000000000000000000 ) ) ;
#3177=LINE ( 'NONE', #30799, #1292 ) ;
#3179=VERTEX_POINT ( 'NONE', #2740 ) ;
#3180=VERTEX_POINT ( 'NONE', #49932 ) ;
#3181=CARTESIAN_POINT ( 'NONE',  ( -1.053808008129011320, 3.267716535433071279, 2.204724409448808764 ) ) ;
#3182=CARTESIAN_POINT ( 'NONE',  ( 0.000000000000000000, 3.346456692913386100, -2.493791675044291445 ) ) ;
#3183=ORIENTED_EDGE ( 'NONE', *, *, #22189, .F. ) ;
#3184=DIRECTION ( 'NONE',  ( 1.734723475976806848E-16, 0.000000000000000000, 1.000000000000000000 ) ) ;
#3185=CARTESIAN_POINT ( 'NONE',  ( 1.363819533518803251, 3.346456692913386100, 1.417322834645662777 ) ) ;
#3187=ORIENTED_EDGE ( 'NONE', *, *, #41641, .T. ) ;
#3188=ORIENTED_EDGE ( 'NONE', *, *, #14731, .F. ) ;
#3189=ADVANCED_FACE ( 'NONE', ( #6870 ), #42730, .F. ) ;
#3190=LINE ( 'NONE', #26929, #18061 ) ;
#3191=LINE ( 'NONE', #50375, #24172 ) ;
#3192=AXIS2_PLACEMENT_3D ( 'NONE', #31897, #12262, #43737 ) ;
#3194=EDGE_LOOP ( 'NONE', ( #4997, #14927, #17748, #13431 ) ) ;
#3195=DIRECTION ( 'NONE',  ( 1.734723475976806848E-16, -0.000000000000000000, 1.000000000000000000 ) ) ;
#3196=DIRECTION ( 'NONE',  ( -0.000000000000000000, 1.000000000000000000, -0.000000000000000000 ) ) ;
#3197=ORIENTED_EDGE ( 'NONE', *, *, #35942, .T. ) ;
#3201=EDGE_LOOP ( 'NONE', ( #15679, #26156, #28563, #16403 ) ) ;
#3202=CARTESIAN_POINT ( 'NONE',  ( 1.636583440222563857, 0.000000000000000000, -0.3149606299212596716 ) ) ;
#3205=CIRCLE ( 'NONE', #11416, 2.165354330708661568 ) ;
#3206=DIRECTION ( 'NONE',  ( 1.734723475976806848E-16, -0.000000000000000000, 1.000000000000000000 ) ) ;
#3208=DIRECTION ( 'NONE',  ( -0.000000000000000000, 1.000000000000000000, -0.000000000000000000 ) ) ;
#3212=CARTESIAN_POINT ( 'NONE',  ( 0.7423782071083087075, 0.000000000000000000, 0.3149606299212576177 ) ) ;
#3215=FACE_OUTER_BOUND ( 'NONE', #8236, .T. ) ;
#3217=CARTESIAN_POINT ( 'NONE',  ( 0.1968503937007878568, 0.000000000000000000, 1.889763779527550369 ) ) ;
#3218=LINE ( 'NONE', #39096, #4223 ) ;
#3219=ORIENTED_EDGE ( 'NONE', *, *, #8414, .T. ) ;
#3220=LINE ( 'NONE', #22097, #38051 ) ;
#3221=DIRECTION ( 'NONE',  ( 1.000000000000000000, -0.000000000000000000, 0.000000000000000000 ) ) ;
#3222=PLANE ( 'NONE',  #38669 ) ;
#3225=CARTESIAN_POINT ( 'NONE',  ( 0.000000000000000000, 3.267716535433071279, -0.6299212598425181220 ) ) ;
#3226=CARTESIAN_POINT ( 'NONE',  ( -1.091055626815042645, 0.000000000000000000, -1.574803149606293529 ) ) ;
#3227=CARTESIAN_POINT ( 'NONE',  ( 1.363819533518803251, 3.346456692913386100, 0.4724409448818871482 ) ) ;
#3229=EDGE_CURVE ( 'NONE', #46970, #23957, #46085, .T. ) ;
#3231=FACE_OUTER_BOUND ( 'NONE', #20858, .T. ) ;
#3232=ORIENTED_EDGE ( 'NONE', *, *, #48206, .T. ) ;
#3233=FACE_BOUND ( 'NONE', #24083, .T. ) ;
#3234=ADVANCED_FACE ( 'NONE', ( #25982 ), #2999, .F. ) ;
#3235=VECTOR ( 'NONE', #50891, 39.37007874015748143 ) ;
#3237=DIRECTION ( 'NONE',  ( 1.734723475976806848E-16, -0.000000000000000000, 1.000000000000000000 ) ) ;
#3238=ADVANCED_FACE ( 'NONE', ( #33994 ), #45829, .F. ) ;
#3239=EDGE_CURVE ( 'NONE', #33931, #46747, #26235, .T. ) ;
#3242=VERTEX_POINT ( 'NONE', #38124 ) ;
#3244=CARTESIAN_POINT ( 'NONE',  ( -1.091055626815042201, 0.000000000000000000, 1.062992125984246083 ) ) ;
#3245=DIRECTION ( 'NONE',  ( 1.000000000000000000, 0.000000000000000000, 0.000000000000000000 ) ) ;
#3246=DIRECTION ( 'NONE',  ( -1.000000000000000000, 0.000000000000000000, -0.000000000000000000 ) ) ;
#3247=VECTOR ( 'NONE', #34664, 39.37007874015748143 ) ;
#3248=LINE ( 'NONE', #35000, #18658 ) ;
#3249=B_SPLINE_CURVE_WITH_KNOTS ( 'NONE', 3,
 ( #11330, #50265, #7211, #27571 ),
 .UNSPECIFIED., .F., .F.,
 ( 4, 4 ),
 ( 7.244828104690220634E-07, 0.005111537570788880769 ),
 .UNSPECIFIED. ) ;
#3252=EDGE_CURVE ( 'NONE', #49628, #11104, #7623, .T. ) ;
#3253=VERTEX_POINT ( 'NONE', #12003 ) ;
#3254=FACE_OUTER_BOUND ( 'NONE', #46091, .T. ) ;
#3255=DIRECTION ( 'NONE',  ( -1.000000000000000000, 0.000000000000000000, 0.000000000000000000 ) ) ;
#3256=VERTEX_POINT ( 'NONE', #31629 ) ;
#3257=EDGE_CURVE ( 'NONE', #47679, #37198, #8131, .T. ) ;
#3259=VERTEX_POINT ( 'NONE', #27232 ) ;
#3260=VERTEX_POINT ( 'NONE', #43227 ) ;
#3261=VECTOR ( 'NONE', #44884, 39.37007874015748143 ) ;
#3262=EDGE_CURVE ( 'NONE', #11733, #6435, #11501, .T. ) ;
#3263=ORIENTED_EDGE ( 'NONE', *, *, #41239, .F. ) ;
#3264=ORIENTED_EDGE ( 'NONE', *, *, #18392, .F. ) ;
#3265=PLANE ( 'NONE',  #502 ) ;
#3268=CARTESIAN_POINT ( 'NONE',  ( 1.363819533518803251, 0.000000000000000000, 1.220472440944875281 ) ) ;
#3269=EDGE_CURVE ( 'NONE', #18410, #37571, #7874, .T. ) ;
#3270=CARTESIAN_POINT ( 'NONE',  ( 0.000000000000000000, 3.267716535433071279, -0.7874015748031470974 ) ) ;
#3272=CARTESIAN_POINT ( 'NONE',  ( 0.1968503937007872462, 3.267716535433071279, -0.5118110236220465570 ) ) ;
#3275=ORIENTED_EDGE ( 'NONE', *, *, #42395, .T. ) ;
#3277=CARTESIAN_POINT ( 'NONE',  ( 0.2727639067037604947, 3.346456692913386100, -1.102362204724405714 ) ) ;
#3279=CARTESIAN_POINT ( 'NONE',  ( -0.8182917201112814842, 3.267716535433071279, 0.9055118110236167750 ) ) ;
#3280=DIRECTION ( 'NONE',  ( 1.734723475976806848E-16, 0.000000000000000000, 1.000000000000000000 ) ) ;
#3281=EDGE_LOOP ( 'NONE', ( #24899, #13152, #5466, #50344 ) ) ;
#3283=CARTESIAN_POINT ( 'NONE',  ( -2.182111253630085290, 0.000000000000000000, 0.4330708661417290162 ) ) ;
#3287=LINE ( 'NONE', #10782, #11717 ) ;
#3289=CARTESIAN_POINT ( 'NONE',  ( -1.363819533518803473, 3.267716535433071279, 1.732283464566920950 ) ) ;
#3292=LINE ( 'NONE', #22166, #10569 ) ;
#3294=LINE ( 'NONE', #39427, #2883 ) ;
#3295=EDGE_CURVE ( 'NONE', #43929, #43549, #35752, .T. ) ;
#3296=AXIS2_PLACEMENT_3D ( 'NONE', #40923, #37052, #25671 ) ;
#3299=DIRECTION ( 'NONE',  ( 1.000000000000000000, 0.000000000000000000, 0.000000000000000000 ) ) ;
#3301=ORIENTED_EDGE ( 'NONE', *, *, #35809, .F. ) ;
#3303=ORIENTED_EDGE ( 'NONE', *, *, #30368, .F. ) ;
#3306=ORIENTED_EDGE ( 'NONE', *, *, #7095, .F. ) ;
#3307=VECTOR ( 'NONE', #48691, 39.37007874015748143 ) ;
#3312=ORIENTED_EDGE ( 'NONE', *, *, #30981, .T. ) ;
#3313=ORIENTED_EDGE ( 'NONE', *, *, #17274, .T. ) ;
#3315=FACE_BOUND ( 'NONE', #49368, .T. ) ;
#3316=EDGE_LOOP ( 'NONE', ( #44463, #23044, #2855, #2192 ) ) ;
#3317=VECTOR ( 'NONE', #47653, 39.37007874015748143 ) ;
#3318=CARTESIAN_POINT ( 'NONE',  ( 0.7423782071083087075, 3.267716535433071279, -0.6299212598425181220 ) ) ;
#3322=VERTEX_POINT ( 'NONE', #382 ) ;
#3325=EDGE_LOOP ( 'NONE', ( #27783, #36487, #10237, #666 ) ) ;
#3328=ORIENTED_EDGE ( 'NONE', *, *, #42838, .T. ) ;
#3330=PLANE ( 'NONE',  #30772 ) ;
#3331=ADVANCED_FACE ( 'NONE', ( #32150 ), #35501, .F. ) ;
#3332=LINE ( 'NONE', #34339, #33001 ) ;
#3333=ORIENTED_EDGE ( 'NONE', *, *, #37981, .F. ) ;
#3334=ORIENTED_EDGE ( 'NONE', *, *, #23127, .F. ) ;
#3339=CARTESIAN_POINT ( 'NONE',  ( 1.287906020515829919, 3.267716535433071279, -2.076684646723067296 ) ) ;
#3340=EDGE_CURVE ( 'NONE', #46657, #25764, #40149, .T. ) ;
#3341=PLANE ( 'NONE',  #28912 ) ;
#3345=CARTESIAN_POINT ( 'NONE',  ( 0.5455278134075211005, 3.346456692913386100, -0.1968503937007880511 ) ) ;
#3347=CARTESIAN_POINT ( 'NONE',  ( -0.07591351300297333182, 0.000000000000000000, -0.1574803149606301411 ) ) ;
#3349=VECTOR ( 'NONE', #36535, 39.37007874015748143 ) ;
#3350=ORIENTED_EDGE ( 'NONE', *, *, #14027, .F. ) ;
#3352=ADVANCED_FACE ( 'NONE', ( #28249 ), #40308, .F. ) ;
#3353=CARTESIAN_POINT ( 'NONE',  ( -0.8942052331142547050, 3.267716535433071279, 1.377952755905504256 ) ) ;
#3359=LINE ( 'NONE', #51045, #26267 ) ;
#3360=EDGE_CURVE ( 'NONE', #47112, #12259, #50674, .T. ) ;
#3361=VERTEX_POINT ( 'NONE', #40910 ) ;
#3365=LINE ( 'NONE', #34616, #14011 ) ;
#3366=ORIENTED_EDGE ( 'NONE', *, *, #41324, .F. ) ;
#3368=ORIENTED_EDGE ( 'NONE', *, *, #23732, .T. ) ;
#3369=ORIENTED_EDGE ( 'NONE', *, *, #49867, .F. ) ;
#3370=DIRECTION ( 'NONE',  ( -1.000000000000000000, -0.000000000000000000, -0.000000000000000000 ) ) ;
#3371=CARTESIAN_POINT ( 'NONE',  ( 0.4696143004045476577, 3.346456692913386100, -2.113816876263008293 ) ) ;
#3373=AXIS2_PLACEMENT_3D ( 'NONE', #21134, #2270, #18018 ) ;
#3375=AXIS2_PLACEMENT_3D ( 'NONE', #24468, #40218, #36342 ) ;
#3376=LINE ( 'NONE', #27116, #23718 ) ;
#3378=ADVANCED_FACE ( 'NONE', ( #5536 ), #12777, .F. ) ;
#3379=VERTEX_POINT ( 'NONE', #36781 ) ;
#3380=LINE ( 'NONE', #19121, #12555 ) ;
#3381=ORIENTED_EDGE ( 'NONE', *, *, #22347, .T. ) ;
#3382=ORIENTED_EDGE ( 'NONE', *, *, #7527, .T. ) ;
#3385=EDGE_CURVE ( 'NONE', #31518, #29992, #9154, .T. ) ;
#3388=VECTOR ( 'NONE', #10526, 39.37007874015748143 ) ;
#3390=ADVANCED_FACE ( 'NONE', ( #20770 ), #9413, .F. ) ;
#3391=EDGE_CURVE ( 'NONE', #15612, #22693, #28507, .T. ) ;
#3396=EDGE_CURVE ( 'NONE', #45413, #1213, #1659, .T. ) ;
#3398=DIRECTION ( 'NONE',  ( -0.000000000000000000, 1.000000000000000000, -0.000000000000000000 ) ) ;
#3399=EDGE_LOOP ( 'NONE', ( #29587, #39428, #39387, #24580 ) ) ;
#3403=LINE ( 'NONE', #283, #4457 ) ;
#3405=DIRECTION ( 'NONE',  ( 1.734723475976806848E-16, -0.000000000000000000, 1.000000000000000000 ) ) ;
#3406=VERTEX_POINT ( 'NONE', #25157 ) ;
#3407=LINE ( 'NONE', #50586, #38273 ) ;
#3409=ADVANCED_FACE ( 'NONE', ( #45014 ), #1407, .F. ) ;
#3410=VECTOR ( 'NONE', #26959, 39.37007874015748143 ) ;
#3411=ORIENTED_EDGE ( 'NONE', *, *, #10906, .F. ) ;
#3412=CARTESIAN_POINT ( 'NONE',  ( -1.166969139818015533, 0.000000000000000000, 0.7874015748031456541 ) ) ;
#3413=EDGE_CURVE ( 'NONE', #26317, #49645, #13288, .T. ) ;
#3415=DIRECTION ( 'NONE',  ( -3.469446951953613696E-16, 0.000000000000000000, -1.000000000000000000 ) ) ;
#3418=EDGE_CURVE ( 'NONE', #4264, #31838, #33173, .T. ) ;
#3420=AXIS2_PLACEMENT_3D ( 'NONE', #28248, #12776, #39369 ) ;
#3421=ADVANCED_FACE ( 'NONE', ( #21287 ), #37041, .F. ) ;
#3422=ORIENTED_EDGE ( 'NONE', *, *, #35506, .T. ) ;
#3424=VECTOR ( 'NONE', #10867, 39.37007874015748143 ) ;
#3425=VERTEX_POINT ( 'NONE', #24902 ) ;
#3426=LINE ( 'NONE', #29404, #34492 ) ;
#3427=VERTEX_POINT ( 'NONE', #21536 ) ;
#3428=VECTOR ( 'NONE', #16887, 39.37007874015748143 ) ;
#3430=CARTESIAN_POINT ( 'NONE',  ( -1.909347346926324462, 0.000000000000000000, 1.102362204724404160 ) ) ;
#3432=ORIENTED_EDGE ( 'NONE', *, *, #50034, .F. ) ;
#3433=ORIENTED_EDGE ( 'NONE', *, *, #46228, .F. ) ;
#3434=ORIENTED_EDGE ( 'NONE', *, *, #33399, .F. ) ;
#3435=DIRECTION ( 'NONE',  ( -1.000000000000000000, 0.000000000000000000, 0.000000000000000000 ) ) ;
#3437=ORIENTED_EDGE ( 'NONE', *, *, #19119, .F. ) ;
#3439=LINE ( 'NONE', #22810, #25603 ) ;
#3440=CARTESIAN_POINT ( 'NONE',  ( -0.8182917201112819283, 3.346456692913386100, -0.3543307086614175816 ) ) ;
#3441=DIRECTION ( 'NONE',  ( 1.734723475976806848E-16, -0.000000000000000000, 1.000000000000000000 ) ) ;
#3443=ORIENTED_EDGE ( 'NONE', *, *, #35989, .F. ) ;
#3444=DIRECTION ( 'NONE',  ( -0.000000000000000000, 1.000000000000000000, -0.000000000000000000 ) ) ;
#3449=ORIENTED_EDGE ( 'NONE', *, *, #29863, .T. ) ;
#3450=CARTESIAN_POINT ( 'NONE',  ( 0.2727639067037610499, 3.346456692913386100, 1.417322834645662777 ) ) ;
#3451=ORIENTED_EDGE ( 'NONE', *, *, #41715, .F. ) ;
#3452=ORIENTED_EDGE ( 'NONE', *, *, #20598, .F. ) ;
#3453=CARTESIAN_POINT ( 'NONE',  ( -0.3486774197067339376, 3.267716535433071279, 0.3149606299212577287 ) ) ;
#3454=LINE ( 'NONE', #46784, #1987 ) ;
#3455=CIRCLE ( 'NONE', #29848, 2.106299212598425008 ) ;
#3456=CARTESIAN_POINT ( 'NONE',  ( 4.268512490100411402E-16, 3.346456692913386100, 2.204724409448808764 ) ) ;
#3458=EDGE_CURVE ( 'NONE', #21434, #51008, #1916, .T. ) ;
#3461=VERTEX_POINT ( 'NONE', #5278 ) ;
#3462=ADVANCED_FACE ( 'NONE', ( #21033 ), #36273, .F. ) ;
#3465=EDGE_CURVE ( 'NONE', #9737, #7396, #49116, .T. ) ;
#3466=VECTOR ( 'NONE', #9545, 39.37007874015748143 ) ;
#3468=ORIENTED_EDGE ( 'NONE', *, *, #20957, .F. ) ;
#3469=LINE ( 'NONE', #30079, #7948 ) ;
#3471=LINE ( 'NONE', #19207, #400 ) ;
#3473=DIRECTION ( 'NONE',  ( 1.000000000000000000, -0.000000000000000000, 0.000000000000000000 ) ) ;
#3477=EDGE_CURVE ( 'NONE', #713, #42090, #41413, .T. ) ;
#3478=FACE_OUTER_BOUND ( 'NONE', #50517, .T. ) ;
#3480=DIRECTION ( 'NONE',  ( -1.000000000000000000, 0.000000000000000000, -0.000000000000000000 ) ) ;
#3481=ADVANCED_FACE ( 'NONE', ( #32405 ), #8897, .T. ) ;
#3482=PLANE ( 'NONE',  #22035 ) ;
#3483=CARTESIAN_POINT ( 'NONE',  ( 2.083034095169011428E-16, 3.267716535433071279, -3.613488146149790065E-32 ) ) ;
#3484=DIRECTION ( 'NONE',  ( -1.000000000000000000, 0.000000000000000000, 1.734723475976806848E-16 ) ) ;
#3485=DIRECTION ( 'NONE',  ( -1.000000000000000000, 0.000000000000000000, 1.734723475976806848E-16 ) ) ;
#3486=DIRECTION ( 'NONE',  ( -0.000000000000000000, 0.000000000000000000, 1.000000000000000000 ) ) ;
#3487=EDGE_CURVE ( 'NONE', #23037, #44686, #50366, .T. ) ;
#3488=VERTEX_POINT ( 'NONE', #49371 ) ;
#3489=DIRECTION ( 'NONE',  ( -1.000000000000000000, 0.000000000000000000, 1.734723475976806848E-16 ) ) ;
#3492=VECTOR ( 'NONE', #37440, 39.37007874015748143 ) ;
#3493=LINE ( 'NONE', #10736, #35856 ) ;
#3495=VECTOR ( 'NONE', #39892, 39.37007874015748143 ) ;
#3496=VERTEX_POINT ( 'NONE', #10681 ) ;
#3497=ORIENTED_EDGE ( 'NONE', *, *, #31581, .F. ) ;
#3498=DIRECTION ( 'NONE',  ( -1.000000000000000000, 0.000000000000000000, -0.000000000000000000 ) ) ;
#3500=VECTOR ( 'NONE', #136, 39.37007874015748143 ) ;
#3501=DIRECTION ( 'NONE',  ( -0.000000000000000000, 1.000000000000000000, -0.000000000000000000 ) ) ;
#3503=CARTESIAN_POINT ( 'NONE',  ( 0.8182917201112817063, 0.000000000000000000, -1.929133858267711110 ) ) ;
#3508=CARTESIAN_POINT ( 'NONE',  ( -1.712496953225537633, 3.346456692913386100, 1.417322834645662333 ) ) ;
#3509=CARTESIAN_POINT ( 'NONE',  ( 1.560669927219590747, 3.346456692913386100, -0.7874015748031473194 ) ) ;
#3513=VERTEX_POINT ( 'NONE', #11185 ) ;
#3515=ORIENTED_EDGE ( 'NONE', *, *, #39388, .F. ) ;
#3516=CARTESIAN_POINT ( 'NONE',  ( -2.182111253630085734, 3.346456692913386100, -0.6299212598425177889 ) ) ;
#3517=VERTEX_POINT ( 'NONE', #29793 ) ;
#3519=EDGE_CURVE ( 'NONE', #32787, #8317, #14809, .T. ) ;
#3520=CARTESIAN_POINT ( 'NONE',  ( 0.8182917201112819283, 0.000000000000000000, 0.5905511811023579360 ) ) ;
#3521=EDGE_CURVE ( 'NONE', #23961, #31953, #33668, .T. ) ;
#3523=EDGE_CURVE ( 'NONE', #24076, #46112, #26420, .T. ) ;
#3524=CARTESIAN_POINT ( 'NONE',  ( 0.000000000000000000, 3.346456692913386100, 0.000000000000000000 ) ) ;
#3525=ADVANCED_FACE ( 'NONE', ( #6039 ), #14293, .F. ) ;
#3526=CARTESIAN_POINT ( 'NONE',  ( -2.438548951736695170, 3.267716535433071279, 0.1574803149606286423 ) ) ;
#3527=AXIS2_PLACEMENT_3D ( 'NONE', #1928, #49626, #25413 ) ;
#3529=LINE ( 'NONE', #7159, #22167 ) ;
#3531=LINE ( 'NONE', #19268, #5197 ) ;
#3532=LINE ( 'NONE', #3277, #44800 ) ;
#3533=VECTOR ( 'NONE', #13915, 39.37007874015748143 ) ;
#3534=PLANE ( 'NONE',  #37566 ) ;
#3535=DIRECTION ( 'NONE',  ( 1.000000000000000000, 0.000000000000000000, 0.000000000000000000 ) ) ;
#3537=VECTOR ( 'NONE', #8739, 39.37007874015748143 ) ;
#3539=CARTESIAN_POINT ( 'NONE',  ( -0.5455278134075214336, 0.000000000000000000, -0.9448818897637762948 ) ) ;
#3540=EDGE_CURVE ( 'NONE', #10643, #2988, #49866, .T. ) ;
#3541=ADVANCED_FACE ( 'NONE', ( #30554 ), #42417, .F. ) ;
#3543=ORIENTED_EDGE ( 'NONE', *, *, #2114, .T. ) ;
#3544=DIRECTION ( 'NONE',  ( 1.734723475976806848E-16, 0.000000000000000000, 1.000000000000000000 ) ) ;
#3546=AXIS2_PLACEMENT_3D ( 'NONE', #45049, #9452, #25194 ) ;
#3547=EDGE_CURVE ( 'NONE', #35065, #1059, #22304, .T. ) ;
#3549=ORIENTED_EDGE ( 'NONE', *, *, #28158, .T. ) ;
#3550=CARTESIAN_POINT ( 'NONE',  ( 0.5455278134075217666, 3.346456692913386100, 2.204724409448808764 ) ) ;
#3553=DIRECTION ( 'NONE',  ( -1.000000000000000000, -0.000000000000000000, -0.000000000000000000 ) ) ;
#3554=EDGE_LOOP ( 'NONE', ( #48173, #3583, #23201, #8706 ) ) ;
#3555=VERTEX_POINT ( 'NONE', #42165 ) ;
#3556=VERTEX_POINT ( 'NONE', #34184 ) ;
#3557=CARTESIAN_POINT ( 'NONE',  ( -0.6214413264104945434, 3.346456692913386100, 0.1574803149606285035 ) ) ;
#3561=EDGE_CURVE ( 'NONE', #38385, #47240, #6803, .T. ) ;
#3562=ORIENTED_EDGE ( 'NONE', *, *, #12927, .F. ) ;
#3563=CARTESIAN_POINT ( 'NONE',  ( -1.091055626815042645, 3.267716535433071279, 1.692913385826762873 ) ) ;
#3564=ORIENTED_EDGE ( 'NONE', *, *, #45234, .T. ) ;
#3565=DIRECTION ( 'NONE',  ( 1.000000000000000000, 0.000000000000000000, 0.000000000000000000 ) ) ;
#3566=ORIENTED_EDGE ( 'NONE', *, *, #21671, .T. ) ;
#3567=VERTEX_POINT ( 'NONE', #7061 ) ;
#3568=PLANE ( 'NONE',  #38882 ) ;
#3572=AXIS2_PLACEMENT_3D ( 'NONE', #50770, #8231, #39470 ) ;
#3573=LINE ( 'NONE', #42806, #31171 ) ;
#3575=EDGE_LOOP ( 'NONE', ( #27214, #47899, #22258, #36873 ) ) ;
#3576=VERTEX_POINT ( 'NONE', #22548 ) ;
#3583=ORIENTED_EDGE ( 'NONE', *, *, #26390, .T. ) ;
#3585=EDGE_CURVE ( 'NONE', #18861, #32922, #34434, .T. ) ;
#3588=EDGE_CURVE ( 'NONE', #20835, #34165, #10426, .T. ) ;
#3590=ORIENTED_EDGE ( 'NONE', *, *, #10962, .F. ) ;
#3593=DIRECTION ( 'NONE',  ( 1.000000000000000000, 0.000000000000000000, -3.469446951953613696E-16 ) ) ;
#3597=CARTESIAN_POINT ( 'NONE',  ( 0.2727639067037604392, 3.346456692913386100, -0.6692913385826760875 ) ) ;
#3601=ORIENTED_EDGE ( 'NONE', *, *, #43604, .F. ) ;
#3602=DIRECTION ( 'NONE',  ( -3.469446951953613696E-16, 0.000000000000000000, -1.000000000000000000 ) ) ;
#3603=EDGE_CURVE ( 'NONE', #10927, #39048, #49616, .T. ) ;
#3605=ORIENTED_EDGE ( 'NONE', *, *, #50952, .T. ) ;
#3608=DIRECTION ( 'NONE',  ( 0.000000000000000000, 0.000000000000000000, -1.000000000000000000 ) ) ;
#3609=VECTOR ( 'NONE', #39850, 39.37007874015748143 ) ;
#3612=EDGE_CURVE ( 'NONE', #7991, #42344, #27933, .T. ) ;
#3613=VECTOR ( 'NONE', #45933, 39.37007874015748143 ) ;
#3614=DIRECTION ( 'NONE',  ( -0.000000000000000000, 1.000000000000000000, -0.000000000000000000 ) ) ;
#3616=CARTESIAN_POINT ( 'NONE',  ( 1.287906020515830141, 3.346456692913386100, -0.3149606299212596716 ) ) ;
#3618=ORIENTED_EDGE ( 'NONE', *, *, #32168, .F. ) ;
#3619=CARTESIAN_POINT ( 'NONE',  ( 1.560669927219590747, 3.267716535433071279, 0.1574803149606283648 ) ) ;
#3620=CARTESIAN_POINT ( 'NONE',  ( 1.091055626815043311, 3.267716535433071279, 1.801691980386208591 ) ) ;
#3621=EDGE_LOOP ( 'NONE', ( #25946, #12998, #32695, #4252 ) ) ;
#3623=VERTEX_POINT ( 'NONE', #8064 ) ;
#3624=ORIENTED_EDGE ( 'NONE', *, *, #3018, .F. ) ;
#3625=EDGE_CURVE ( 'NONE', #2745, #9409, #3943, .T. ) ;
#3626=DIRECTION ( 'NONE',  ( 1.734723475976806848E-16, 0.000000000000000000, 1.000000000000000000 ) ) ;
#3628=PLANE ( 'NONE',  #27657 ) ;
#3629=ADVANCED_FACE ( 'NONE', ( #47520 ), #57, .F. ) ;
#3630=VERTEX_POINT ( 'NONE', #46763 ) ;
#3631=DIRECTION ( 'NONE',  ( -0.000000000000000000, 1.000000000000000000, -0.000000000000000000 ) ) ;
#3635=( GEOMETRIC_REPRESENTATION_CONTEXT ( 3 ) GLOBAL_UNCERTAINTY_ASSIGNED_CONTEXT ( ( #9692 ) ) GLOBAL_UNIT_ASSIGNED_CONTEXT ( ( #40606, #40097, #4471 ) ) REPRESENTATION_CONTEXT ( 'NONE', 'WORKASPACE' ) );
#3636=CIRCLE ( 'NONE', #32514, 2.106299212598425008 ) ;
#3637=ORIENTED_EDGE ( 'NONE', *, *, #17816, .F. ) ;
#3638=AXIS2_PLACEMENT_3D ( 'NONE', #40107, #32888, #13503 ) ;
#3640=AXIS2_PLACEMENT_3D ( 'NONE', #11990, #366, #31879 ) ;
#3641=EDGE_LOOP ( 'NONE', ( #22144, #21599, #17873, #31217 ) ) ;
#3643=ADVANCED_FACE ( 'NONE', ( #313 ), #47006, .F. ) ;
#3644=VECTOR ( 'NONE', #6973, 39.37007874015748143 ) ;
#3645=FACE_OUTER_BOUND ( 'NONE', #6197, .T. ) ;
#3646=DIRECTION ( 'NONE',  ( 1.734723475976806848E-16, -0.000000000000000000, 1.000000000000000000 ) ) ;
#3648=DIRECTION ( 'NONE',  ( 0.000000000000000000, 0.000000000000000000, -1.000000000000000000 ) ) ;
#3649=ORIENTED_EDGE ( 'NONE', *, *, #50062, .F. ) ;
#3650=ORIENTED_EDGE ( 'NONE', *, *, #5987, .T. ) ;
#3651=AXIS2_PLACEMENT_3D ( 'NONE', #25769, #18974, #50413 ) ;
#3654=VERTEX_POINT ( 'NONE', #11683 ) ;
#3655=CARTESIAN_POINT ( 'NONE',  ( 0.000000000000000000, 3.267716535433071279, 1.535433070866133898 ) ) ;
#3656=DIRECTION ( 'NONE',  ( -1.000000000000000000, -0.000000000000000000, -0.000000000000000000 ) ) ;
#3657=DIRECTION ( 'NONE',  ( 0.000000000000000000, 0.000000000000000000, 1.000000000000000000 ) ) ;
#3659=DIRECTION ( 'NONE',  ( 0.000000000000000000, 0.000000000000000000, 1.000000000000000000 ) ) ;
#3660=EDGE_LOOP ( 'NONE', ( #47399, #50190, #35334, #34817 ) ) ;
#3661=PLANE ( 'NONE',  #4422 ) ;
#3662=LINE ( 'NONE', #40314, #23565 ) ;
#3665=LINE ( 'NONE', #42891, #48406 ) ;
#3666=CARTESIAN_POINT ( 'NONE',  ( 1.091055626815042645, 0.000000000000000000, -0.5118110236220471121 ) ) ;
#3668=ORIENTED_EDGE ( 'NONE', *, *, #19340, .T. ) ;
#3669=EDGE_CURVE ( 'NONE', #36331, #3242, #4192, .T. ) ;
#3671=EDGE_LOOP ( 'NONE', ( #2580, #45277, #17784, #49267 ) ) ;
#3672=AXIS2_PLACEMENT_3D ( 'NONE', #44920, #41330, #45930 ) ;
#3673=CARTESIAN_POINT ( 'NONE',  ( -2.258024766633058622, 3.267716535433071279, 0.1574803149606286423 ) ) ;
#3674=ORIENTED_EDGE ( 'NONE', *, *, #4993, .T. ) ;
#3676=EDGE_CURVE ( 'NONE', #1152, #23942, #43512, .T. ) ;
#3677=AXIS2_PLACEMENT_3D ( 'NONE', #42783, #38675, #22669 ) ;
#3678=VERTEX_POINT ( 'NONE', #39050 ) ;
#3679=DIRECTION ( 'NONE',  ( -3.469446951953613696E-16, 0.000000000000000000, -1.000000000000000000 ) ) ;
#3680=DIRECTION ( 'NONE',  ( -3.469446951953613696E-16, 0.000000000000000000, -1.000000000000000000 ) ) ;
#3681=DIRECTION ( 'NONE',  ( -0.000000000000000000, 0.000000000000000000, 1.000000000000000000 ) ) ;
#3682=EDGE_CURVE ( 'NONE', #472, #10946, #12195, .T. ) ;
#3683=ADVANCED_FACE ( 'NONE', ( #43162 ), #3689, .F. ) ;
#3685=ORIENTED_EDGE ( 'NONE', *, *, #14361, .F. ) ;
#3686=ORIENTED_EDGE ( 'NONE', *, *, #42836, .F. ) ;
#3688=VECTOR ( 'NONE', #3553, 39.37007874015748143 ) ;
#3689=PLANE ( 'NONE',  #34561 ) ;
#3690=VERTEX_POINT ( 'NONE', #7812 ) ;
#3691=EDGE_LOOP ( 'NONE', ( #24160, #4989, #38301, #44971 ) ) ;
#3692=DIRECTION ( 'NONE',  ( 1.734723475976806848E-16, -0.000000000000000000, 1.000000000000000000 ) ) ;
#3693=CARTESIAN_POINT ( 'NONE',  ( 1.909347346926324462, 3.346456692913386100, -0.9842519685039348154 ) ) ;
#3695=VERTEX_POINT ( 'NONE', #23551 ) ;
#3696=ORIENTED_EDGE ( 'NONE', *, *, #36115, .F. ) ;
#3697=DIRECTION ( 'NONE',  ( 1.000000000000000000, 0.000000000000000000, 0.000000000000000000 ) ) ;
#3699=DIRECTION ( 'NONE',  ( -0.000000000000000000, 1.000000000000000000, -0.000000000000000000 ) ) ;
#3701=EDGE_LOOP ( 'NONE', ( #43866, #27919, #49186, #28211 ) ) ;
#3702=LINE ( 'NONE', #35198, #21595 ) ;
#3703=LINE ( 'NONE', #7828, #19443 ) ;
#3704=ORIENTED_EDGE ( 'NONE', *, *, #9337, .F. ) ;
#3707=ORIENTED_EDGE ( 'NONE', *, *, #9473, .T. ) ;
#3711=LINE ( 'NONE', #47288, #13233 ) ;
#3712=CARTESIAN_POINT ( 'NONE',  ( 1.560669927219590303, 3.346456692913386100, -1.732283464566923170 ) ) ;
#3713=ADVANCED_FACE ( 'NONE', ( #24068 ), #20184, .F. ) ;
#3714=DIRECTION ( 'NONE',  ( 1.000000000000000000, -0.000000000000000000, 0.000000000000000000 ) ) ;
#3715=EDGE_LOOP ( 'NONE', ( #30235, #14422, #22333, #17458 ) ) ;
#3716=VERTEX_POINT ( 'NONE', #38807 ) ;
#3717=AXIS2_PLACEMENT_3D ( 'NONE', #37204, #33080, #48766 ) ;
#3718=VECTOR ( 'NONE', #4453, 39.37007874015748143 ) ;
#3719=VECTOR ( 'NONE', #35606, 39.37007874015748143 ) ;
#3721=DIRECTION ( 'NONE',  ( -3.469446951953613696E-16, 0.000000000000000000, -1.000000000000000000 ) ) ;
#3723=AXIS2_PLACEMENT_3D ( 'NONE', #37097, #44815, #1715 ) ;
#3725=CARTESIAN_POINT ( 'NONE',  ( 0.8182917201112817063, 3.267716535433071279, -1.417322834645664331 ) ) ;
#3728=DIRECTION ( 'NONE',  ( -3.469446951953613696E-16, 0.000000000000000000, -1.000000000000000000 ) ) ;
#3731=LINE ( 'NONE', #39100, #38885 ) ;
#3732=DIRECTION ( 'NONE',  ( -0.000000000000000000, 1.000000000000000000, -0.000000000000000000 ) ) ;
#3734=ORIENTED_EDGE ( 'NONE', *, *, #24644, .T. ) ;
#3735=CARTESIAN_POINT ( 'NONE',  ( -2.258024766633058622, 3.267716535433071279, 7.834097144030835427E-16 ) ) ;
#3739=DIRECTION ( 'NONE',  ( -3.469446951953613696E-16, 0.000000000000000000, -1.000000000000000000 ) ) ;
#3741=DIRECTION ( 'NONE',  ( -0.000000000000000000, 1.000000000000000000, -0.000000000000000000 ) ) ;
#3742=DIRECTION ( 'NONE',  ( -0.000000000000000000, 1.000000000000000000, -0.000000000000000000 ) ) ;
#3743=CARTESIAN_POINT ( 'NONE',  ( -0.07591351300297348448, 3.267716535433071279, 2.633779063002574070E-17 ) ) ;
#3745=EDGE_CURVE ( 'NONE', #41713, #17882, #47698, .T. ) ;
#3746=EDGE_CURVE ( 'NONE', #31869, #50064, #28185, .T. ) ;
#3747=ORIENTED_EDGE ( 'NONE', *, *, #17184, .F. ) ;
#3748=ORIENTED_EDGE ( 'NONE', *, *, #30790, .T. ) ;
#3749=DIRECTION ( 'NONE',  ( 0.000000000000000000, 0.000000000000000000, -1.000000000000000000 ) ) ;
#3750=VECTOR ( 'NONE', #4048, 39.37007874015748143 ) ;
#3752=AXIS2_PLACEMENT_3D ( 'NONE', #20387, #47713, #4388 ) ;
#3753=ORIENTED_EDGE ( 'NONE', *, *, #19086, .F. ) ;
#3754=DIRECTION ( 'NONE',  ( -1.000000000000000000, -0.000000000000000000, -0.000000000000000000 ) ) ;
#3755=CARTESIAN_POINT ( 'NONE',  ( -1.091055626815042201, 3.346456692913386100, 1.377952755905504256 ) ) ;
#3758=EDGE_CURVE ( 'NONE', #39512, #39570, #9341, .T. ) ;
#3759=DIRECTION ( 'NONE',  ( 1.734723475976806848E-16, -0.000000000000000000, 1.000000000000000000 ) ) ;
#3760=EDGE_LOOP ( 'NONE', ( #49814, #40533, #15984, #36563 ) ) ;
#3761=DIRECTION ( 'NONE',  ( -0.000000000000000000, 1.000000000000000000, -0.000000000000000000 ) ) ;
#3763=AXIS2_PLACEMENT_3D ( 'NONE', #36663, #28644, #43870 ) ;
#3764=CARTESIAN_POINT ( 'NONE',  ( -0.8942052331142547050, 0.000000000000000000, 0.7480314960629874665 ) ) ;
#3765=AXIS2_PLACEMENT_3D ( 'NONE', #50856, #39044, #15797 ) ;
#3766=ORIENTED_EDGE ( 'NONE', *, *, #19246, .T. ) ;
#3768=ORIENTED_EDGE ( 'NONE', *, *, #19726, .F. ) ;
#3769=VERTEX_POINT ( 'NONE', #41103 ) ;
#3770=EDGE_CURVE ( 'NONE', #35404, #47863, #5209, .T. ) ;
#3771=PLANE ( 'NONE',  #39908 ) ;
#3774=EDGE_LOOP ( 'NONE', ( #12550, #6789, #27025, #48731 ) ) ;
#3775=LINE ( 'NONE', #27255, #40948 ) ;
#3776=EDGE_CURVE ( 'NONE', #25971, #20686, #17599, .T. ) ;
#3777=ORIENTED_EDGE ( 'NONE', *, *, #27813, .T. ) ;
#3778=EDGE_CURVE ( 'NONE', #45969, #47335, #12968, .T. ) ;
#3779=DIRECTION ( 'NONE',  ( 1.000000000000000000, 0.000000000000000000, -3.469446951953613696E-16 ) ) ;
#3780=EDGE_CURVE ( 'NONE', #4026, #14569, #28699, .T. ) ;
#3787=VERTEX_POINT ( 'NONE', #830 ) ;
#3788=LINE ( 'NONE', #26510, #8486 ) ;
#3789=VECTOR ( 'NONE', #42313, 39.37007874015748143 ) ;
#3792=PLANE ( 'NONE',  #34747 ) ;
#3797=DIRECTION ( 'NONE',  ( 1.734723475976806848E-16, -0.000000000000000000, 1.000000000000000000 ) ) ;
#3801=CARTESIAN_POINT ( 'NONE',  ( 0.2727639067037610499, 0.000000000000000000, 2.047244094488179567 ) ) ;
#3802=EDGE_LOOP ( 'NONE', ( #46498, #34553, #37375, #19055 ) ) ;
#3803=DIRECTION ( 'NONE',  ( 1.734723475976806848E-16, -0.000000000000000000, 1.000000000000000000 ) ) ;
#3805=DIRECTION ( 'NONE',  ( 0.000000000000000000, -1.000000000000000000, 0.000000000000000000 ) ) ;
#3806=DIRECTION ( 'NONE',  ( 1.734723475976806848E-16, -0.000000000000000000, 1.000000000000000000 ) ) ;
#3807=VERTEX_POINT ( 'NONE', #5727 ) ;
#3808=EDGE_CURVE ( 'NONE', #30118, #50026, #1596, .T. ) ;
#3810=ORIENTED_EDGE ( 'NONE', *, *, #41193, .T. ) ;
#3811=EDGE_CURVE ( 'NONE', #28015, #21029, #44446, .T. ) ;
#3814=CARTESIAN_POINT ( 'NONE',  ( -0.2727639067037607723, 3.346456692913386100, -0.7874015748031470974 ) ) ;
#3815=CARTESIAN_POINT ( 'NONE',  ( -0.8182917201112819283, 0.000000000000000000, -1.417322834645664331 ) ) ;
#3816=EDGE_LOOP ( 'NONE', ( #43733, #22905, #38181, #38699 ) ) ;
#3817=ADVANCED_FACE ( 'NONE', ( #32599 ), #33110, .F. ) ;
#3818=CARTESIAN_POINT ( 'NONE',  ( 0.7423782071083085965, 3.267716535433071279, -2.575641807848709701E-16 ) ) ;
#3819=ORIENTED_EDGE ( 'NONE', *, *, #34136, .T. ) ;
#3820=FACE_OUTER_BOUND ( 'NONE', #48296, .T. ) ;
#3823=ORIENTED_EDGE ( 'NONE', *, *, #40980, .T. ) ;
#3824=EDGE_LOOP ( 'NONE', ( #2343, #47409, #48934, #14906 ) ) ;
#3825=VECTOR ( 'NONE', #28028, 39.37007874015748143 ) ;
#3826=CARTESIAN_POINT ( 'NONE',  ( -1.363819533518803029, 0.000000000000000000, 0.4724409448818871482 ) ) ;
#3828=AXIS2_PLACEMENT_3D ( 'NONE', #2368, #33368, #21736 ) ;
#3831=AXIS2_PLACEMENT_3D ( 'NONE', #34207, #26196, #49894 ) ;
#3832=VERTEX_POINT ( 'NONE', #36207 ) ;
#3833=ORIENTED_EDGE ( 'NONE', *, *, #33179, .F. ) ;
#3837=ADVANCED_FACE ( 'NONE', ( #44689 ), #25090, .F. ) ;
#3842=ORIENTED_EDGE ( 'NONE', *, *, #49454, .F. ) ;
#3845=CARTESIAN_POINT ( 'NONE',  ( 0.000000000000000000, 3.267716535433071279, -1.259842519685034468 ) ) ;
#3847=ORIENTED_EDGE ( 'NONE', *, *, #35594, .T. ) ;
#3849=CARTESIAN_POINT ( 'NONE',  ( -0.3486774197067340486, 3.346456692913386100, 2.007874015748021268 ) ) ;
#3850=LINE ( 'NONE', #50274, #13802 ) ;
#3851=DIRECTION ( 'NONE',  ( 1.734723475976806848E-16, -0.000000000000000000, 1.000000000000000000 ) ) ;
#3852=LINE ( 'NONE', #35352, #48226 ) ;
#3857=CARTESIAN_POINT ( 'NONE',  ( -1.712496953225537188, 3.267716535433071279, 0.4724409448818871482 ) ) ;
#3858=ORIENTED_EDGE ( 'NONE', *, *, #43191, .T. ) ;
#3859=VECTOR ( 'NONE', #47105, 39.37007874015748143 ) ;
#3861=ORIENTED_EDGE ( 'NONE', *, *, #42894, .T. ) ;
#3862=DIRECTION ( 'NONE',  ( -1.000000000000000000, -0.000000000000000000, -0.000000000000000000 ) ) ;
#3865=ORIENTED_EDGE ( 'NONE', *, *, #16176, .T. ) ;
#3867=EDGE_CURVE ( 'NONE', #42867, #24046, #40843, .T. ) ;
#3868=LINE ( 'NONE', #12123, #41938 ) ;
#3870=ORIENTED_EDGE ( 'NONE', *, *, #31340, .T. ) ;
#3871=CARTESIAN_POINT ( 'NONE',  ( -1.363819533518803029, 0.000000000000000000, 1.417322834645662777 ) ) ;
#3873=EDGE_CURVE ( 'NONE', #39604, #32922, #48030, .T. ) ;
#3874=CARTESIAN_POINT ( 'NONE',  ( 0.5455278134075212115, 0.000000000000000000, -6.146657985744592735E-16 ) ) ;
#3875=CARTESIAN_POINT ( 'NONE',  ( -0.5455278134075217666, 3.267716535433071279, 9.463399047163231808E-17 ) ) ;
#3877=EDGE_CURVE ( 'NONE', #32968, #13111, #6494, .T. ) ;
#3881=ORIENTED_EDGE ( 'NONE', *, *, #627, .F. ) ;
#3882=FACE_OUTER_BOUND ( 'NONE', #42788, .T. ) ;
#3885=ORIENTED_EDGE ( 'NONE', *, *, #29445, .T. ) ;
#3886=PLANE ( 'NONE',  #27023 ) ;
#3887=EDGE_CURVE ( 'NONE', #1038, #1681, #18362, .T. ) ;
#3888=LINE ( 'NONE', #8267, #42325 ) ;
#3890=AXIS2_PLACEMENT_3D ( 'NONE', #7105, #22850, #38603 ) ;
#3892=DIRECTION ( 'NONE',  ( -1.000000000000000000, 0.000000000000000000, 0.000000000000000000 ) ) ;
#3893=AXIS2_PLACEMENT_3D ( 'NONE', #36818, #13579, #41703 ) ;
#3896=EDGE_LOOP ( 'NONE', ( #1827, #1530, #6855, #28080 ) ) ;
#3898=CARTESIAN_POINT ( 'NONE',  ( -1.636583440222564301, 3.346456692913386100, 1.377952755905504256 ) ) ;
#3901=FACE_OUTER_BOUND ( 'NONE', #34242, .T. ) ;
#3906=FACE_OUTER_BOUND ( 'NONE', #30984, .T. ) ;
#3907=VECTOR ( 'NONE', #49773, 39.37007874015748143 ) ;
#3908=ORIENTED_EDGE ( 'NONE', *, *, #34418, .T. ) ;
#3909=CARTESIAN_POINT ( 'NONE',  ( -0.8182917201112814842, 0.000000000000000000, 1.535433070866133898 ) ) ;
#3910=EDGE_CURVE ( 'NONE', #42214, #28697, #34115, .T. ) ;
#3912=LINE ( 'NONE', #14330, #46996 ) ;
#3913=DIRECTION ( 'NONE',  ( -0.000000000000000000, 1.000000000000000000, -0.000000000000000000 ) ) ;
#3916=ORIENTED_EDGE ( 'NONE', *, *, #7955, .F. ) ;
#3920=ORIENTED_EDGE ( 'NONE', *, *, #47904, .T. ) ;
#3921=CARTESIAN_POINT ( 'NONE',  ( 1.363819533518803029, 3.267716535433071279, -1.102362204724405714 ) ) ;
#3922=DIRECTION ( 'NONE',  ( -3.469446951953613696E-16, 0.000000000000000000, -1.000000000000000000 ) ) ;
#3924=AXIS2_PLACEMENT_3D ( 'NONE', #44499, #40641, #29011 ) ;
#3927=ORIENTED_EDGE ( 'NONE', *, *, #3877, .T. ) ;
#3928=DIRECTION ( 'NONE',  ( -3.469446951953613696E-16, 0.000000000000000000, -1.000000000000000000 ) ) ;
#3932=ORIENTED_EDGE ( 'NONE', *, *, #16184, .T. ) ;
#3934=CARTESIAN_POINT ( 'NONE',  ( -0.8942052331142547050, 0.000000000000000000, 1.377952755905504256 ) ) ;
#3935=DIRECTION ( 'NONE',  ( 1.000000000000000000, 0.000000000000000000, 0.000000000000000000 ) ) ;
#3937=EDGE_CURVE ( 'NONE', #43163, #47500, #21986, .T. ) ;
#3939=VERTEX_POINT ( 'NONE', #45443 ) ;
#3941=ORIENTED_EDGE ( 'NONE', *, *, #16193, .F. ) ;
#3942=DIRECTION ( 'NONE',  ( -1.000000000000000000, 0.000000000000000000, 1.734723475976806848E-16 ) ) ;
#3943=LINE ( 'NONE', #39813, #15607 ) ;
#3945=ORIENTED_EDGE ( 'NONE', *, *, #28787, .F. ) ;
#3946=CARTESIAN_POINT ( 'NONE',  ( 1.636583440222563635, 0.000000000000000000, -0.9448818897637765168 ) ) ;
#3948=CARTESIAN_POINT ( 'NONE',  ( -1.166969139818015755, 3.346456692913386100, -0.03937007874015868020 ) ) ;
#3950=EDGE_LOOP ( 'NONE', ( #20624, #45570, #50015, #38903 ) ) ;
#3951=ORIENTED_EDGE ( 'NONE', *, *, #47694, .F. ) ;
#3952=CARTESIAN_POINT ( 'NONE',  ( 0.000000000000000000, 3.267716535433071279, 0.000000000000000000 ) ) ;
#3954=LINE ( 'NONE', #27433, #18752 ) ;
#3957=FACE_OUTER_BOUND ( 'NONE', #17099, .T. ) ;
#3958=VERTEX_POINT ( 'NONE', #34618 ) ;
#3959=CARTESIAN_POINT ( 'NONE',  ( 0.2727639067037610499, 3.267716535433071279, 2.362204724409437961 ) ) ;
#3960=VERTEX_POINT ( 'NONE', #30491 ) ;
#3961=ORIENTED_EDGE ( 'NONE', *, *, #47366, .T. ) ;
#3962=DIRECTION ( 'NONE',  ( 1.000000000000000000, 0.000000000000000000, 0.000000000000000000 ) ) ;
#3964=DIRECTION ( 'NONE',  ( -0.000000000000000000, 1.000000000000000000, -0.000000000000000000 ) ) ;
#3965=VECTOR ( 'NONE', #19290, 39.37007874015748143 ) ;
#3966=VECTOR ( 'NONE', #2033, 39.37007874015748143 ) ;
#3967=ADVANCED_FACE ( 'NONE', ( #6992 ), #49801, .F. ) ;
#3969=DIRECTION ( 'NONE',  ( 1.734723475976806848E-16, -0.000000000000000000, 1.000000000000000000 ) ) ;
#3970=EDGE_LOOP ( 'NONE', ( #33240, #8455, #14326, #5955 ) ) ;
#3973=ORIENTED_EDGE ( 'NONE', *, *, #41734, .F. ) ;
#3974=DIRECTION ( 'NONE',  ( 1.000000000000000000, 0.000000000000000000, -3.469446951953613696E-16 ) ) ;
#3977=AXIS2_PLACEMENT_3D ( 'NONE', #36450, #28943, #33609 ) ;
#3979=VECTOR ( 'NONE', #43515, 39.37007874015748143 ) ;
#3980=DIRECTION ( 'NONE',  ( 0.000000000000000000, 0.000000000000000000, -1.000000000000000000 ) ) ;
#3981=DIRECTION ( 'NONE',  ( -1.000000000000000000, 0.000000000000000000, -0.000000000000000000 ) ) ;
#3982=ORIENTED_EDGE ( 'NONE', *, *, #44828, .T. ) ;
#3984=EDGE_CURVE ( 'NONE', #20840, #1905, #42349, .T. ) ;
#3985=AXIS2_PLACEMENT_3D ( 'NONE', #41141, #37268, #17635 ) ;
#3987=EDGE_CURVE ( 'NONE', #721, #6366, #13731, .T. ) ;
#3988=ORIENTED_EDGE ( 'NONE', *, *, #29359, .T. ) ;
#3989=CARTESIAN_POINT ( 'NONE',  ( 0.1968503937007878568, 3.346456692913386100, 2.204724409448808764 ) ) ;
#3990=DIRECTION ( 'NONE',  ( 1.734723475976806848E-16, 0.000000000000000000, 1.000000000000000000 ) ) ;
#3992=ORIENTED_EDGE ( 'NONE', *, *, #39130, .F. ) ;
#3993=LINE ( 'NONE', #19724, #14384 ) ;
#3994=CARTESIAN_POINT ( 'NONE',  ( -0.3486774197067339376, 0.000000000000000000, -0.3149606299212593941 ) ) ;
#3995=DIRECTION ( 'NONE',  ( -0.000000000000000000, 1.000000000000000000, -0.000000000000000000 ) ) ;
#3997=DIRECTION ( 'NONE',  ( 0.000000000000000000, 0.000000000000000000, -1.000000000000000000 ) ) ;
#3998=ORIENTED_EDGE ( 'NONE', *, *, #40975, .T. ) ;
#4000=ADVANCED_FACE ( 'NONE', ( #22742 ), #25594, .F. ) ;
#4001=LINE ( 'NONE', #1139, #10322 ) ;
#4002=CARTESIAN_POINT ( 'NONE',  ( 0.8182917201112824834, 3.267716535433071279, 2.004783788421103718 ) ) ;
#4003=AXIS2_PLACEMENT_3D ( 'NONE', #15120, #41733, #30108 ) ;
#4005=VERTEX_POINT ( 'NONE', #38246 ) ;
#4006=ORIENTED_EDGE ( 'NONE', *, *, #43960, .T. ) ;
#4007=CARTESIAN_POINT ( 'NONE',  ( 1.287906020515830141, 3.267716535433071279, -4.468321617281355077E-16 ) ) ;
#4010=VERTEX_POINT ( 'NONE', #11616 ) ;
#4011=DIRECTION ( 'NONE',  ( -1.000000000000000000, 0.000000000000000000, 0.000000000000000000 ) ) ;
#4012=VECTOR ( 'NONE', #43087, 39.37007874015748143 ) ;
#4016=VECTOR ( 'NONE', #36539, 39.37007874015748143 ) ;
#4017=CIRCLE ( 'NONE', #32894, 2.952755905511811552 ) ;
#4018=VERTEX_POINT ( 'NONE', #23236 ) ;
#4019=DIRECTION ( 'NONE',  ( 1.000000000000000000, 0.000000000000000000, 0.000000000000000000 ) ) ;
#4020=CARTESIAN_POINT ( 'NONE',  ( 0.2727639067037610499, 3.267716535433071279, 1.417322834645662777 ) ) ;
#4022=VECTOR ( 'NONE', #10588, 39.37007874015748143 ) ;
#4023=LINE ( 'NONE', #47598, #18270 ) ;
#4024=VERTEX_POINT ( 'NONE', #27357 ) ;
#4025=CARTESIAN_POINT ( 'NONE',  ( -0.07591351300297359550, 3.346456692913386100, -2.047244094488181343 ) ) ;
#4026=VERTEX_POINT ( 'NONE', #47457 ) ;
#4027=VERTEX_POINT ( 'NONE', #12131 ) ;
#4028=VECTOR ( 'NONE', #38410, 39.37007874015748143 ) ;
#4029=CARTESIAN_POINT ( 'NONE',  ( 0.4696143004045479352, 3.346456692913386100, -0.7874015748031473194 ) ) ;
#4030=ORIENTED_EDGE ( 'NONE', *, *, #7842, .T. ) ;
#4032=EDGE_LOOP ( 'NONE', ( #21578, #15959, #12852, #31525 ) ) ;
#4033=CARTESIAN_POINT ( 'NONE',  ( 0.1968503937007874405, 3.346456692913386100, 0.000000000000000000 ) ) ;
#4036=DIRECTION ( 'NONE',  ( 1.000000000000000000, 0.000000000000000000, -3.469446951953613696E-16 ) ) ;
#4039=EDGE_CURVE ( 'NONE', #25208, #18779, #43098, .T. ) ;
#4041=EDGE_CURVE ( 'NONE', #36033, #23187, #24000, .T. ) ;
#4043=EDGE_CURVE ( 'NONE', #10848, #31608, #35123, .T. ) ;
#4044=CARTESIAN_POINT ( 'NONE',  ( 1.833433833923351353, 3.346456692913386100, -1.036830145017913596 ) ) ;
#4048=DIRECTION ( 'NONE',  ( 1.000000000000000000, -0.000000000000000000, 0.000000000000000000 ) ) ;
#4049=DIRECTION ( 'NONE',  ( 0.000000000000000000, 0.000000000000000000, -1.000000000000000000 ) ) ;
#4051=AXIS2_PLACEMENT_3D ( 'NONE', #37497, #18117, #13482 ) ;
#4052=VECTOR ( 'NONE', #9368, 39.37007874015748143 ) ;
#4054=CARTESIAN_POINT ( 'NONE',  ( 0.000000000000000000, 3.267716535433071279, -0.7874015748031473194 ) ) ;
#4056=EDGE_LOOP ( 'NONE', ( #43439, #30094, #557, #43054 ) ) ;
#4057=DIRECTION ( 'NONE',  ( 1.000000000000000000, -0.000000000000000000, 0.000000000000000000 ) ) ;
#4059=AXIS2_PLACEMENT_3D ( 'NONE', #46751, #46256, #14543 ) ;
#4061=LINE ( 'NONE', #47380, #44682 ) ;
#4062=EDGE_CURVE ( 'NONE', #27577, #8496, #42605, .T. ) ;
#4063=VECTOR ( 'NONE', #47311, 39.37007874015748143 ) ;
#4065=DIRECTION ( 'NONE',  ( 1.734723475976806848E-16, 0.000000000000000000, 1.000000000000000000 ) ) ;
#4066=CARTESIAN_POINT ( 'NONE',  ( -1.166969139818015533, 3.267716535433071279, 4.048737525165544183E-16 ) ) ;
#4069=DIRECTION ( 'NONE',  ( 1.734723475976806848E-16, -0.000000000000000000, 1.000000000000000000 ) ) ;
#4070=ORIENTED_EDGE ( 'NONE', *, *, #17207, .F. ) ;
#4072=EDGE_LOOP ( 'NONE', ( #15699, #44834, #5868, #20971 ) ) ;
#4073=VERTEX_POINT ( 'NONE', #31252 ) ;
#4074=DIRECTION ( 'NONE',  ( -1.000000000000000000, -0.000000000000000000, -0.000000000000000000 ) ) ;
#4080=DIRECTION ( 'NONE',  ( 1.000000000000000000, 0.000000000000000000, 0.000000000000000000 ) ) ;
#4081=VECTOR ( 'NONE', #22240, 39.37007874015748143 ) ;
#4082=ORIENTED_EDGE ( 'NONE', *, *, #37733, .T. ) ;
#4083=CARTESIAN_POINT ( 'NONE',  ( -0.8182917201112819283, 0.000000000000000000, -0.6692913385826760875 ) ) ;
#4086=ORIENTED_EDGE ( 'NONE', *, *, #2884, .F. ) ;
#4087=CARTESIAN_POINT ( 'NONE',  ( -1.909347346926324462, 0.000000000000000000, 0.9055118110236167750 ) ) ;
#4091=CARTESIAN_POINT ( 'NONE',  ( 1.636583440222563857, 3.267716535433071279, 0.1181102362204701633 ) ) ;
#4092=ORIENTED_EDGE ( 'NONE', *, *, #12545, .F. ) ;
#4094=CARTESIAN_POINT ( 'NONE',  ( 1.015142113812069091, 0.000000000000000000, -1.732283464566923614 ) ) ;
#4095=DIRECTION ( 'NONE',  ( 0.000000000000000000, 0.000000000000000000, -1.000000000000000000 ) ) ;
#4097=CIRCLE ( 'NONE', #45278, 2.165354330708661568 ) ;
#4098=CARTESIAN_POINT ( 'NONE',  ( -0.2727639067037602172, 3.346456692913386100, 0.7874015748031456541 ) ) ;
#4099=ORIENTED_EDGE ( 'NONE', *, *, #43031, .F. ) ;
#4100=LINE ( 'NONE', #8477, #6304 ) ;
#4101=DIRECTION ( 'NONE',  ( 0.000000000000000000, 1.000000000000000000, 0.000000000000000000 ) ) ;
#4106=CARTESIAN_POINT ( 'NONE',  ( 1.015142113812069313, 0.000000000000000000, -0.7874015748031473194 ) ) ;
#4107=CARTESIAN_POINT ( 'NONE',  ( 0.000000000000000000, 3.267716535433071279, 1.692913385826762873 ) ) ;
#4109=LINE ( 'NONE', #19830, #242 ) ;
#4111=EDGE_CURVE ( 'NONE', #23557, #42367, #247, .T. ) ;
#4112=DIRECTION ( 'NONE',  ( -3.469446951953613696E-16, 0.000000000000000000, -1.000000000000000000 ) ) ;
#4114=VECTOR ( 'NONE', #47597, 39.37007874015748143 ) ;
#4115=VERTEX_POINT ( 'NONE', #27107 ) ;
#4117=VERTEX_POINT ( 'NONE', #7497 ) ;
#4118=LINE ( 'NONE', #36123, #10223 ) ;
#4119=ORIENTED_EDGE ( 'NONE', *, *, #42928, .F. ) ;
#4124=ORIENTED_EDGE ( 'NONE', *, *, #32936, .F. ) ;
#4125=LINE ( 'NONE', #11861, #50931 ) ;
#4129=VECTOR ( 'NONE', #8057, 39.37007874015748143 ) ;
#4130=ORIENTED_EDGE ( 'NONE', *, *, #8855, .T. ) ;
#4131=CARTESIAN_POINT ( 'NONE',  ( -2.182111253630085734, 3.346456692913386100, -0.8267716535433052849 ) ) ;
#4132=CARTESIAN_POINT ( 'NONE',  ( 1.363819533518803251, 0.000000000000000000, -0.6692913385826764205 ) ) ;
#4133=VERTEX_POINT ( 'NONE', #19106 ) ;
#4134=DIRECTION ( 'NONE',  ( -1.000000000000000000, -0.000000000000000000, -0.000000000000000000 ) ) ;
#4135=ORIENTED_EDGE ( 'NONE', *, *, #1568, .T. ) ;
#4136=VERTEX_POINT ( 'NONE', #50547 ) ;
#4139=FACE_OUTER_BOUND ( 'NONE', #44805, .T. ) ;
#4141=FACE_OUTER_BOUND ( 'NONE', #49980, .T. ) ;
#4142=CARTESIAN_POINT ( 'NONE',  ( -0.5455278134075208785, 3.267716535433071279, 1.062992125984246083 ) ) ;
#4143=ORIENTED_EDGE ( 'NONE', *, *, #12176, .T. ) ;
#4144=CARTESIAN_POINT ( 'NONE',  ( -2.182111253630085734, 3.346456692913386100, -0.9448818897637762948 ) ) ;
#4145=ORIENTED_EDGE ( 'NONE', *, *, #47823, .F. ) ;
#4147=ORIENTED_EDGE ( 'NONE', *, *, #6845, .T. ) ;
#4149=VECTOR ( 'NONE', #18770, 39.37007874015748143 ) ;
#4151=VECTOR ( 'NONE', #21889, 39.37007874015748143 ) ;
#4152=FACE_OUTER_BOUND ( 'NONE', #40839, .T. ) ;
#4153=LINE ( 'NONE', #24289, #9875 ) ;
#4154=ORIENTED_EDGE ( 'NONE', *, *, #42271, .T. ) ;
#4156=ADVANCED_FACE ( 'NONE', ( #15243 ), #30994, .F. ) ;
#4157=FACE_OUTER_BOUND ( 'NONE', #6053, .T. ) ;
#4158=EDGE_CURVE ( 'NONE', #16832, #4956, #17041, .T. ) ;
#4159=DIRECTION ( 'NONE',  ( 1.000000000000000000, -0.000000000000000000, 0.000000000000000000 ) ) ;
#4161=ORIENTED_EDGE ( 'NONE', *, *, #50443, .F. ) ;
#4162=DIRECTION ( 'NONE',  ( 1.000000000000000000, -0.000000000000000000, 0.000000000000000000 ) ) ;
#4165=LINE ( 'NONE', #19385, #41577 ) ;
#4168=ORIENTED_EDGE ( 'NONE', *, *, #44598, .T. ) ;
#4169=CARTESIAN_POINT ( 'NONE',  ( 0.8182917201112819283, 3.346456692913386100, -0.7874015748031473194 ) ) ;
#4170=ORIENTED_EDGE ( 'NONE', *, *, #621, .F. ) ;
#4171=VERTEX_POINT ( 'NONE', #29152 ) ;
#4172=DIRECTION ( 'NONE',  ( 1.000000000000000000, 0.000000000000000000, 0.000000000000000000 ) ) ;
#4176=ORIENTED_EDGE ( 'NONE', *, *, #20331, .F. ) ;
#4178=ORIENTED_EDGE ( 'NONE', *, *, #22215, .T. ) ;
#4183=AXIS2_PLACEMENT_3D ( 'NONE', #19581, #30967, #46177 ) ;
#4184=CARTESIAN_POINT ( 'NONE',  ( 1.443330927545150910, 3.346456692913386100, -1.614173228346452715 ) ) ;
#4185=CARTESIAN_POINT ( 'NONE',  ( -0.3486774197067334935, 3.267716535433071279, 1.209717811016577352E-16 ) ) ;
#4186=DIRECTION ( 'NONE',  ( -1.000000000000000000, 0.000000000000000000, 0.000000000000000000 ) ) ;
#4190=ORIENTED_EDGE ( 'NONE', *, *, #41792, .T. ) ;
#4192=LINE ( 'NONE', #47773, #32918 ) ;
#4193=VERTEX_POINT ( 'NONE', #4646 ) ;
#4195=FACE_OUTER_BOUND ( 'NONE', #2202, .T. ) ;
#4197=VECTOR ( 'NONE', #8456, 39.37007874015748143 ) ;
#4198=CARTESIAN_POINT ( 'NONE',  ( -1.091055626815042201, 0.000000000000000000, 0.3149606299212580063 ) ) ;
#4201=ORIENTED_EDGE ( 'NONE', *, *, #32144, .F. ) ;
#4202=ORIENTED_EDGE ( 'NONE', *, *, #7548, .T. ) ;
#4203=DIRECTION ( 'NONE',  ( 1.000000000000000000, -0.000000000000000000, 0.000000000000000000 ) ) ;
#4204=DIRECTION ( 'NONE',  ( -3.469446951953613696E-16, 0.000000000000000000, -1.000000000000000000 ) ) ;
#4205=VERTEX_POINT ( 'NONE', #32018 ) ;
#4206=PLANE ( 'NONE',  #27353 ) ;
#4208=ORIENTED_EDGE ( 'NONE', *, *, #34073, .T. ) ;
#4210=EDGE_LOOP ( 'NONE', ( #24378, #44238, #9921, #46517 ) ) ;
#4211=EDGE_LOOP ( 'NONE', ( #23107, #32326, #33615 ) ) ;
#4215=CARTESIAN_POINT ( 'NONE',  ( 0.7423782071083085965, 3.267716535433071279, -0.5118110236220467790 ) ) ;
#4216=ORIENTED_EDGE ( 'NONE', *, *, #42960, .T. ) ;
#4220=CARTESIAN_POINT ( 'NONE',  ( -1.909347346926324462, 3.346456692913386100, 0.4724409448818871482 ) ) ;
#4221=LINE ( 'NONE', #20481, #17694 ) ;
#4223=VECTOR ( 'NONE', #38600, 39.37007874015748143 ) ;
#4224=VECTOR ( 'NONE', #44692, 39.37007874015748143 ) ;
#4227=DIRECTION ( 'NONE',  ( 0.000000000000000000, -1.000000000000000000, 0.000000000000000000 ) ) ;
#4228=DIRECTION ( 'NONE',  ( -1.000000000000000000, -0.000000000000000000, -0.000000000000000000 ) ) ;
#4229=ORIENTED_EDGE ( 'NONE', *, *, #49705, .F. ) ;
#4230=CARTESIAN_POINT ( 'NONE',  ( 1.560669927219590747, 3.267716535433071279, 0.7874015748031454320 ) ) ;
#4233=VECTOR ( 'NONE', #27784, 39.37007874015748143 ) ;
#4234=LINE ( 'NONE', #48075, #5939 ) ;
#4237=LINE ( 'NONE', #28230, #6539 ) ;
#4239=CARTESIAN_POINT ( 'NONE',  ( 0.000000000000000000, 3.267716535433071279, 0.1181102362204703021 ) ) ;
#4242=VERTEX_POINT ( 'NONE', #16521 ) ;
#4243=CARTESIAN_POINT ( 'NONE',  ( 0.2727639067037602172, 3.346456692913386100, -2.047244094488182231 ) ) ;
#4244=CARTESIAN_POINT ( 'NONE',  ( -1.439733046521776139, 3.267716535433071279, 0.9448818897637749625 ) ) ;
#4245=VERTEX_POINT ( 'NONE', #28379 ) ;
#4246=CARTESIAN_POINT ( 'NONE',  ( 1.091055626815042645, 0.000000000000000000, -0.1968503937007883287 ) ) ;
#4247=DIRECTION ( 'NONE',  ( -1.000000000000000000, 0.000000000000000000, 1.734723475976806848E-16 ) ) ;
#4248=CARTESIAN_POINT ( 'NONE',  ( 0.5455278134075211005, 0.000000000000000000, 0.1181102362204701633 ) ) ;
#4249=DIRECTION ( 'NONE',  ( -3.469446951953613696E-16, 0.000000000000000000, -1.000000000000000000 ) ) ;
#4250=EDGE_CURVE ( 'NONE', #38635, #16977, #48225, .T. ) ;
#4252=ORIENTED_EDGE ( 'NONE', *, *, #18350, .F. ) ;
#4253=DIRECTION ( 'NONE',  ( -1.000000000000000000, -0.000000000000000000, -0.000000000000000000 ) ) ;
#4256=CARTESIAN_POINT ( 'NONE',  ( 0.1968503937007877735, 0.000000000000000000, 1.062992125984246083 ) ) ;
#4258=CARTESIAN_POINT ( 'NONE',  ( 1.287906020515829919, 3.346456692913386100, -1.574803149606294417 ) ) ;
#4260=AXIS2_PLACEMENT_3D ( 'NONE', #17896, #14021, #29767 ) ;
#4262=ORIENTED_EDGE ( 'NONE', *, *, #13481, .F. ) ;
#4264=VERTEX_POINT ( 'NONE', #13412 ) ;
#4266=CARTESIAN_POINT ( 'NONE',  ( 0.8182917201112819283, 3.267716535433071279, -0.7874015748031473194 ) ) ;
#4267=CARTESIAN_POINT ( 'NONE',  ( -3.927031490892378253E-16, 0.000000000000000000, -1.889763779527552146 ) ) ;
#4268=DIRECTION ( 'NONE',  ( -0.000000000000000000, 0.000000000000000000, 1.000000000000000000 ) ) ;
#4269=VECTOR ( 'NONE', #20769, 39.37007874015748143 ) ;
#4270=FACE_BOUND ( 'NONE', #38038, .T. ) ;
#4272=EDGE_CURVE ( 'NONE', #25200, #36052, #32274, .T. ) ;
#4275=VECTOR ( 'NONE', #12336, 39.37007874015748143 ) ;
#4276=EDGE_LOOP ( 'NONE', ( #9969, #35120, #9857, #37603 ) ) ;
#4280=ORIENTED_EDGE ( 'NONE', *, *, #28499, .T. ) ;
#4281=VERTEX_POINT ( 'NONE', #47968 ) ;
#4283=VERTEX_POINT ( 'NONE', #40009 ) ;
#4288=CARTESIAN_POINT ( 'NONE',  ( 1.363819533518803251, 3.346456692913386100, 0.5905511811023579360 ) ) ;
#4290=EDGE_CURVE ( 'NONE', #34106, #45399, #24522, .T. ) ;
#4292=LINE ( 'NONE', #12814, #7235 ) ;
#4295=DIRECTION ( 'NONE',  ( -3.469446951953613696E-16, 0.000000000000000000, -1.000000000000000000 ) ) ;
#4296=LINE ( 'NONE', #7914, #41342 ) ;
#4297=ORIENTED_EDGE ( 'NONE', *, *, #48309, .T. ) ;
#4298=VECTOR ( 'NONE', #15008, 39.37007874015748143 ) ;
#4299=LINE ( 'NONE', #12046, #4233 ) ;
#4300=LINE ( 'NONE', #36829, #45881 ) ;
#4301=ORIENTED_EDGE ( 'NONE', *, *, #12217, .T. ) ;
#4302=DIRECTION ( 'NONE',  ( 0.000000000000000000, -1.000000000000000000, 0.000000000000000000 ) ) ;
#4303=CARTESIAN_POINT ( 'NONE',  ( -0.8942052331142552601, 3.346456692913386100, -1.771653543307081025 ) ) ;
#4305=VECTOR ( 'NONE', #2300, 39.37007874015748143 ) ;
#4307=DIRECTION ( 'NONE',  ( 1.734723475976806848E-16, -0.000000000000000000, 1.000000000000000000 ) ) ;
#4308=VERTEX_POINT ( 'NONE', #41544 ) ;
#4309=CARTESIAN_POINT ( 'NONE',  ( -0.2727639067037610499, 3.346456692913386100, -2.047244094488181343 ) ) ;
#4310=DIRECTION ( 'NONE',  ( -3.469446951953613696E-16, 0.000000000000000000, -1.000000000000000000 ) ) ;
#4311=VECTOR ( 'NONE', #35045, 39.37007874015748143 ) ;
#4312=CARTESIAN_POINT ( 'NONE',  ( 1.636583440222563857, 3.267716535433071279, -0.1968503937007886062 ) ) ;
#4317=VERTEX_POINT ( 'NONE', #21670 ) ;
#4319=LINE ( 'NONE', #16456, #3149 ) ;
#4320=ORIENTED_EDGE ( 'NONE', *, *, #48554, .T. ) ;
#4321=DIRECTION ( 'NONE',  ( 1.000000000000000000, 0.000000000000000000, 0.000000000000000000 ) ) ;
#4322=ORIENTED_EDGE ( 'NONE', *, *, #40942, .F. ) ;
#4323=ADVANCED_FACE ( 'NONE', ( #46151 ), #49748, .F. ) ;
#4324=LINE ( 'NONE', #34808, #5829 ) ;
#4325=ADVANCED_FACE ( 'NONE', ( #38193 ), #18564, .F. ) ;
#4326=VERTEX_POINT ( 'NONE', #6177 ) ;
#4330=EDGE_LOOP ( 'NONE', ( #34319, #32586, #45334 ) ) ;
#4332=ORIENTED_EDGE ( 'NONE', *, *, #28935, .F. ) ;
#4333=VECTOR ( 'NONE', #34072, 39.37007874015748143 ) ;
#4335=ORIENTED_EDGE ( 'NONE', *, *, #50061, .T. ) ;
#4336=ORIENTED_EDGE ( 'NONE', *, *, #14243, .F. ) ;
#4338=CARTESIAN_POINT ( 'NONE',  ( 0.8182917201112824834, 3.346456692913386100, 1.417322834645662777 ) ) ;
#4340=DIRECTION ( 'NONE',  ( -3.469446951953613696E-16, 0.000000000000000000, -1.000000000000000000 ) ) ;
#4342=VECTOR ( 'NONE', #44875, 39.37007874015748143 ) ;
#4344=EDGE_LOOP ( 'NONE', ( #44004, #46277, #43108, #24705 ) ) ;
#4345=LINE ( 'NONE', #4861, #13673 ) ;
#4347=EDGE_CURVE ( 'NONE', #45218, #45413, #37172, .T. ) ;
#4348=VECTOR ( 'NONE', #799, 39.37007874015748143 ) ;
#4349=DIRECTION ( 'NONE',  ( -1.000000000000000000, 0.000000000000000000, 0.000000000000000000 ) ) ;
#4351=EDGE_CURVE ( 'NONE', #21756, #17988, #1788, .T. ) ;
#4353=EDGE_CURVE ( 'NONE', #24511, #32825, #25536, .T. ) ;
#4354=VERTEX_POINT ( 'NONE', #14431 ) ;
#4355=EDGE_LOOP ( 'NONE', ( #10570, #34602, #20342, #27729 ) ) ;
#4356=CARTESIAN_POINT ( 'NONE',  ( -1.636583440222563635, 3.346456692913386100, -4.780733988912460139E-16 ) ) ;
#4358=ADVANCED_FACE ( 'NONE', ( #10804 ), #45640, .F. ) ;
#4360=CARTESIAN_POINT ( 'NONE',  ( -1.909347346926324462, 3.346456692913386100, 0.5905511811023582691 ) ) ;
#4361=DIRECTION ( 'NONE',  ( -1.000000000000000000, -0.000000000000000000, -0.000000000000000000 ) ) ;
#4362=DIRECTION ( 'NONE',  ( 1.000000000000000000, 0.000000000000000000, -3.469446951953613696E-16 ) ) ;
#4363=DIRECTION ( 'NONE',  ( 0.000000000000000000, 0.000000000000000000, -1.000000000000000000 ) ) ;
#4364=ORIENTED_EDGE ( 'NONE', *, *, #18295, .F. ) ;
#4365=DIRECTION ( 'NONE',  ( -3.469446951953613696E-16, 0.000000000000000000, -1.000000000000000000 ) ) ;
#4366=ORIENTED_EDGE ( 'NONE', *, *, #24690, .F. ) ;
#4367=CARTESIAN_POINT ( 'NONE',  ( 0.1968503937007871074, 3.267716535433071279, -6.829619984160646953E-17 ) ) ;
#4369=DIRECTION ( 'NONE',  ( -3.469446951953613696E-16, 0.000000000000000000, -1.000000000000000000 ) ) ;
#4370=CARTESIAN_POINT ( 'NONE',  ( -1.363819533518803473, 0.000000000000000000, 1.732283464566920950 ) ) ;
#4371=LINE ( 'NONE', #757, #10281 ) ;
#4373=VECTOR ( 'NONE', #25167, 39.37007874015748143 ) ;
#4374=LINE ( 'NONE', #19597, #13087 ) ;
#4376=DIRECTION ( 'NONE',  ( 0.000000000000000000, 0.000000000000000000, -1.000000000000000000 ) ) ;
#4377=ORIENTED_EDGE ( 'NONE', *, *, #11605, .T. ) ;
#4378=AXIS2_PLACEMENT_3D ( 'NONE', #38212, #45915, #45155 ) ;
#4379=VECTOR ( 'NONE', #12877, 39.37007874015748143 ) ;
#4380=DIRECTION ( 'NONE',  ( 0.000000000000000000, -1.000000000000000000, 0.000000000000000000 ) ) ;
#4383=ADVANCED_FACE ( 'NONE', ( #30177 ), #45896, .F. ) ;
#4384=VECTOR ( 'NONE', #14902, 39.37007874015748143 ) ;
#4385=CARTESIAN_POINT ( 'NONE',  ( -2.182111253630085734, 0.000000000000000000, -0.9448818897637762948 ) ) ;
#4386=ORIENTED_EDGE ( 'NONE', *, *, #41782, .T. ) ;
#4387=ORIENTED_EDGE ( 'NONE', *, *, #35758, .T. ) ;
#4388=DIRECTION ( 'NONE',  ( -3.469446951953613696E-16, 0.000000000000000000, -1.000000000000000000 ) ) ;
#4389=DIRECTION ( 'NONE',  ( 1.734723475976806848E-16, -0.000000000000000000, 1.000000000000000000 ) ) ;
#4391=VERTEX_POINT ( 'NONE', #26303 ) ;
#4393=CARTESIAN_POINT ( 'NONE',  ( 1.928732080931637505, 3.267716535433071279, -0.9842519685039348154 ) ) ;
#4394=ORIENTED_EDGE ( 'NONE', *, *, #48750, .T. ) ;
#4396=ORIENTED_EDGE ( 'NONE', *, *, #16620, .F. ) ;
#4397=ORIENTED_EDGE ( 'NONE', *, *, #36947, .F. ) ;
#4398=EDGE_CURVE ( 'NONE', #35324, #54, #33561, .T. ) ;
#4400=ORIENTED_EDGE ( 'NONE', *, *, #31199, .F. ) ;
#4402=CARTESIAN_POINT ( 'NONE',  ( 0.5455278134075208785, 3.346456692913386100, -1.771653543307081025 ) ) ;
#4403=EDGE_CURVE ( 'NONE', #34006, #2513, #50004, .T. ) ;
#4407=ORIENTED_EDGE ( 'NONE', *, *, #5980, .F. ) ;
#4408=ORIENTED_EDGE ( 'NONE', *, *, #15177, .F. ) ;
#4410=DIRECTION ( 'NONE',  ( 1.000000000000000000, 0.000000000000000000, -3.469446951953613696E-16 ) ) ;
#4411=EDGE_CURVE ( 'NONE', #2304, #32620, #41296, .T. ) ;
#4415=FACE_OUTER_BOUND ( 'NONE', #22786, .T. ) ;
#4416=AXIS2_PLACEMENT_3D ( 'NONE', #26818, #23709, #34338 ) ;
#4417=PLANE ( 'NONE',  #34674 ) ;
#4418=VECTOR ( 'NONE', #6652, 39.37007874015748143 ) ;
#4420=DIRECTION ( 'NONE',  ( 0.000000000000000000, 0.000000000000000000, 1.000000000000000000 ) ) ;
#4421=DIRECTION ( 'NONE',  ( -0.000000000000000000, 1.000000000000000000, -0.000000000000000000 ) ) ;
#4422=AXIS2_PLACEMENT_3D ( 'NONE', #26644, #41896, #14782 ) ;
#4423=ORIENTED_EDGE ( 'NONE', *, *, #26996, .T. ) ;
#4425=ORIENTED_EDGE ( 'NONE', *, *, #46859, .F. ) ;
#4426=ORIENTED_EDGE ( 'NONE', *, *, #20054, .F. ) ;
#4427=LINE ( 'NONE', #50840, #47126 ) ;
#4428=CARTESIAN_POINT ( 'NONE',  ( 4.439252989704605840E-17, 3.267716535433071279, -7.700876377040806239E-33 ) ) ;
#4429=FACE_OUTER_BOUND ( 'NONE', #13558, .T. ) ;
#4432=DIRECTION ( 'NONE',  ( 0.000000000000000000, 0.000000000000000000, -1.000000000000000000 ) ) ;
#4433=ORIENTED_EDGE ( 'NONE', *, *, #48477, .F. ) ;
#4435=ORIENTED_EDGE ( 'NONE', *, *, #25989, .F. ) ;
#4438=CARTESIAN_POINT ( 'NONE',  ( -0.8182917201112814842, 3.346456692913386100, 1.732283464566921172 ) ) ;
#4440=VECTOR ( 'NONE', #46537, 39.37007874015748143 ) ;
#4441=ADVANCED_FACE ( 'NONE', ( #907 ), #38440, .F. ) ;
#4446=VECTOR ( 'NONE', #5941, 39.37007874015748143 ) ;
#4447=ADVANCED_FACE ( 'NONE', ( #15882 ), #30683, .F. ) ;
#4449=EDGE_LOOP ( 'NONE', ( #19705, #22223, #42604, #15059 ) ) ;
#4450=VERTEX_POINT ( 'NONE', #27752 ) ;
#4451=VECTOR ( 'NONE', #44869, 39.37007874015748143 ) ;
#4452=DIRECTION ( 'NONE',  ( 1.000000000000000000, 0.000000000000000000, -3.469446951953613696E-16 ) ) ;
#4453=DIRECTION ( 'NONE',  ( -0.000000000000000000, 1.000000000000000000, -0.000000000000000000 ) ) ;
#4454=FACE_OUTER_BOUND ( 'NONE', #12224, .T. ) ;
#4455=EDGE_CURVE ( 'NONE', #7592, #728, #20000, .T. ) ;
#4456=VECTOR ( 'NONE', #24118, 39.37007874015748143 ) ;
#4457=VECTOR ( 'NONE', #19142, 39.37007874015748143 ) ;
#4458=VERTEX_POINT ( 'NONE', #20267 ) ;
#4460=CARTESIAN_POINT ( 'NONE',  ( -0.2727639067037607723, 0.000000000000000000, 2.362204724409437961 ) ) ;
#4464=LINE ( 'NONE', #13239, #511 ) ;
#4465=VECTOR ( 'NONE', #26834, 39.37007874015748143 ) ;
#4468=ORIENTED_EDGE ( 'NONE', *, *, #29204, .F. ) ;
#4469=ORIENTED_EDGE ( 'NONE', *, *, #16035, .T. ) ;
#4470=CARTESIAN_POINT ( 'NONE',  ( 0.000000000000000000, 3.267716535433071279, 0.000000000000000000 ) ) ;
#4471=( NAMED_UNIT ( * ) SI_UNIT ( $, .STERADIAN. ) SOLID_ANGLE_UNIT ( ) );
#4472=CARTESIAN_POINT ( 'NONE',  ( -0.07591351300297363713, 3.346456692913386100, -2.164023224473873963 ) ) ;
#4476=ORIENTED_EDGE ( 'NONE', *, *, #30434, .F. ) ;
#4479=ORIENTED_EDGE ( 'NONE', *, *, #40507, .T. ) ;
#4480=DIRECTION ( 'NONE',  ( -3.469446951953613696E-16, 0.000000000000000000, -1.000000000000000000 ) ) ;
#4482=CARTESIAN_POINT ( 'NONE',  ( 1.909347346926324684, 3.346456692913386100, 0.7874015748031456541 ) ) ;
#4486=ORIENTED_EDGE ( 'NONE', *, *, #7459, .T. ) ;
#4488=DIRECTION ( 'NONE',  ( -3.469446951953613696E-16, 0.000000000000000000, -1.000000000000000000 ) ) ;
#4493=VECTOR ( 'NONE', #36064, 39.37007874015748143 ) ;
#4494=VERTEX_POINT ( 'NONE', #8145 ) ;
#4495=CARTESIAN_POINT ( 'NONE',  ( 3.927031490892378253E-16, 0.000000000000000000, 0.7480314960629874665 ) ) ;
#4500=CARTESIAN_POINT ( 'NONE',  ( 0.7423782071083090406, 3.267716535433071279, -2.575641807848711180E-16 ) ) ;
#4502=ORIENTED_EDGE ( 'NONE', *, *, #17563, .F. ) ;
#4503=DIRECTION ( 'NONE',  ( -3.469446951953613696E-16, 0.000000000000000000, -1.000000000000000000 ) ) ;
#4504=CARTESIAN_POINT ( 'NONE',  ( 0.000000000000000000, 3.267716535433071279, -0.9448818897637760728 ) ) ;
#4505=ORIENTED_EDGE ( 'NONE', *, *, #49246, .T. ) ;
#4507=DIRECTION ( 'NONE',  ( 0.000000000000000000, 0.000000000000000000, -1.000000000000000000 ) ) ;
#4508=DIRECTION ( 'NONE',  ( 1.000000000000000000, 0.000000000000000000, -3.469446951953613696E-16 ) ) ;
#4510=ORIENTED_EDGE ( 'NONE', *, *, #32632, .T. ) ;
#4511=ORIENTED_EDGE ( 'NONE', *, *, #25455, .F. ) ;
#4512=CARTESIAN_POINT ( 'NONE',  ( -0.8182917201112819283, 3.346456692913386100, -1.929133858267710000 ) ) ;
#4515=ORIENTED_EDGE ( 'NONE', *, *, #23402, .F. ) ;
#4516=DIRECTION ( 'NONE',  ( -0.000000000000000000, 0.000000000000000000, 1.000000000000000000 ) ) ;
#4518=LINE ( 'NONE', #40657, #19517 ) ;
#4519=EDGE_CURVE ( 'NONE', #22792, #29967, #23891, .T. ) ;
#4520=DIRECTION ( 'NONE',  ( -0.000000000000000000, 1.000000000000000000, -0.000000000000000000 ) ) ;
#4521=VERTEX_POINT ( 'NONE', #39637 ) ;
#4524=LINE ( 'NONE', #48616, #32893 ) ;
#4525=DIRECTION ( 'NONE',  ( -0.000000000000000000, 1.000000000000000000, -0.000000000000000000 ) ) ;
#4526=DIRECTION ( 'NONE',  ( -0.000000000000000000, 1.000000000000000000, -0.000000000000000000 ) ) ;
#4527=EDGE_CURVE ( 'NONE', #3556, #19885, #39893, .T. ) ;
#4528=CARTESIAN_POINT ( 'NONE',  ( -0.8942052331142549271, 3.267716535433071279, 3.102397620449222481E-16 ) ) ;
#4529=FACE_BOUND ( 'NONE', #20717, .T. ) ;
#4531=VERTEX_POINT ( 'NONE', #24406 ) ;
#4532=CARTESIAN_POINT ( 'NONE',  ( 0.4696143004045478797, 3.346456692913386100, -1.299212598425193210 ) ) ;
#4533=VECTOR ( 'NONE', #47486, 39.37007874015748143 ) ;
#4535=ORIENTED_EDGE ( 'NONE', *, *, #51038, .F. ) ;
#4538=EDGE_CURVE ( 'NONE', #44975, #13922, #36030, .T. ) ;
#4540=ORIENTED_EDGE ( 'NONE', *, *, #42347, .F. ) ;
#4541=DIRECTION ( 'NONE',  ( 1.734723475976806848E-16, 0.000000000000000000, 1.000000000000000000 ) ) ;
#4542=VERTEX_POINT ( 'NONE', #7197 ) ;
#4543=VECTOR ( 'NONE', #5428, 39.37007874015748143 ) ;
#4544=EDGE_CURVE ( 'NONE', #46747, #30154, #32161, .T. ) ;
#4547=FACE_OUTER_BOUND ( 'NONE', #15560, .T. ) ;
#4548=EDGE_CURVE ( 'NONE', #38358, #19280, #50250, .T. ) ;
#4550=CARTESIAN_POINT ( 'NONE',  ( 1.636583440222563857, 0.000000000000000000, -1.161035397307311917E-15 ) ) ;
#4551=CARTESIAN_POINT ( 'NONE',  ( 0.2727639067037604947, 3.346456692913386100, -0.4724409448818886470 ) ) ;
#4552=ORIENTED_EDGE ( 'NONE', *, *, #49393, .F. ) ;
#4553=LINE ( 'NONE', #40183, #20037 ) ;
#4556=PLANE ( 'NONE',  #31462 ) ;
#4557=VERTEX_POINT ( 'NONE', #22936 ) ;
#4560=VERTEX_POINT ( 'NONE', #19053 ) ;
#4562=LINE ( 'NONE', #9200, #33372 ) ;
#4564=VECTOR ( 'NONE', #12878, 39.37007874015748143 ) ;
#4565=CIRCLE ( 'NONE', #40828, 2.165354330708661568 ) ;
#4568=ORIENTED_EDGE ( 'NONE', *, *, #4999, .T. ) ;
#4570=ORIENTED_EDGE ( 'NONE', *, *, #38283, .F. ) ;
#4571=CARTESIAN_POINT ( 'NONE',  ( 0.8182917201112819283, 0.000000000000000000, 0.2755905511810994302 ) ) ;
#4573=CARTESIAN_POINT ( 'NONE',  ( 1.636583440222563857, 0.000000000000000000, -0.6299212598425181220 ) ) ;
#4574=LINE ( 'NONE', #700, #30081 ) ;
#4575=CARTESIAN_POINT ( 'NONE',  ( -0.6214413264104945434, 3.267716535433071279, 1.850393700787391849 ) ) ;
#4576=VECTOR ( 'NONE', #46325, 39.37007874015748143 ) ;
#4578=ORIENTED_EDGE ( 'NONE', *, *, #47765, .T. ) ;
#4579=LINE ( 'NONE', #43290, #41928 ) ;
#4580=ORIENTED_EDGE ( 'NONE', *, *, #16038, .F. ) ;
#4583=EDGE_CURVE ( 'NONE', #21352, #2302, #17931, .T. ) ;
#4585=ORIENTED_EDGE ( 'NONE', *, *, #34516, .F. ) ;
#4587=EDGE_CURVE ( 'NONE', #30787, #38385, #5800, .T. ) ;
#4588=DIRECTION ( 'NONE',  ( 1.734723475976806848E-16, -0.000000000000000000, 1.000000000000000000 ) ) ;
#4592=LINE ( 'NONE', #50141, #38621 ) ;
#4593=ORIENTED_EDGE ( 'NONE', *, *, #12916, .T. ) ;
#4594=VERTEX_POINT ( 'NONE', #13300 ) ;
#4595=DIRECTION ( 'NONE',  ( 0.000000000000000000, 1.000000000000000000, 0.000000000000000000 ) ) ;
#4596=CARTESIAN_POINT ( 'NONE',  ( 0.4696143004045484903, 3.346456692913386100, 1.417322834645662777 ) ) ;
#4598=ORIENTED_EDGE ( 'NONE', *, *, #28757, .T. ) ;
#4599=FACE_OUTER_BOUND ( 'NONE', #24311, .T. ) ;
#4601=ORIENTED_EDGE ( 'NONE', *, *, #1670, .F. ) ;
#4602=CARTESIAN_POINT ( 'NONE',  ( -0.2727639067037608278, 3.267716535433071279, -1.929133858267710000 ) ) ;
#4603=DIRECTION ( 'NONE',  ( -0.000000000000000000, 1.000000000000000000, -0.000000000000000000 ) ) ;
#4604=AXIS2_PLACEMENT_3D ( 'NONE', #11127, #7257, #38750 ) ;
#4605=EDGE_CURVE ( 'NONE', #47393, #3807, #9678, .T. ) ;
#4608=ORIENTED_EDGE ( 'NONE', *, *, #1514, .F. ) ;
#4611=LINE ( 'NONE', #12875, #33601 ) ;
#4613=CARTESIAN_POINT ( 'NONE',  ( 0.000000000000000000, 3.267716535433071279, 1.102362204724404160 ) ) ;
#4614=EDGE_CURVE ( 'NONE', #45913, #41125, #1418, .T. ) ;
#4616=EDGE_CURVE ( 'NONE', #767, #37842, #48561, .T. ) ;
#4617=DIRECTION ( 'NONE',  ( -0.000000000000000000, 1.000000000000000000, -0.000000000000000000 ) ) ;
#4618=ORIENTED_EDGE ( 'NONE', *, *, #42271, .F. ) ;
#4619=EDGE_CURVE ( 'NONE', #38729, #35081, #5547, .T. ) ;
#4621=ORIENTED_EDGE ( 'NONE', *, *, #6100, .F. ) ;
#4623=EDGE_CURVE ( 'NONE', #16455, #42424, #29289, .T. ) ;
#4624=ORIENTED_EDGE ( 'NONE', *, *, #17940, .T. ) ;
#4625=ADVANCED_FACE ( 'NONE', ( #1929 ), #32939, .F. ) ;
#4626=CARTESIAN_POINT ( 'NONE',  ( 0.4696143004045484903, 3.346456692913386100, 1.732283464566921172 ) ) ;
#4627=LINE ( 'NONE', #31239, #44315 ) ;
#4630=EDGE_LOOP ( 'NONE', ( #49682, #44069, #5586, #18424 ) ) ;
#4633=VECTOR ( 'NONE', #42318, 39.37007874015748143 ) ;
#4634=FACE_BOUND ( 'NONE', #1357, .T. ) ;
#4638=AXIS2_PLACEMENT_3D ( 'NONE', #28443, #16589, #23817 ) ;
#4639=ORIENTED_EDGE ( 'NONE', *, *, #6480, .F. ) ;
#4640=EDGE_CURVE ( 'NONE', #15732, #49030, #5289, .T. ) ;
#4641=DIRECTION ( 'NONE',  ( -0.000000000000000000, 1.000000000000000000, -0.000000000000000000 ) ) ;
#4642=CARTESIAN_POINT ( 'NONE',  ( -1.909347346926324462, 0.000000000000000000, 0.7874015748031456541 ) ) ;
#4643=VECTOR ( 'NONE', #19186, 39.37007874015748143 ) ;
#4644=EDGE_CURVE ( 'NONE', #26747, #16466, #21299, .T. ) ;
#4646=CARTESIAN_POINT ( 'NONE',  ( 0.2727639067037604947, 3.346456692913386100, -1.417322834645664331 ) ) ;
#4647=EDGE_CURVE ( 'NONE', #12127, #31145, #37309, .T. ) ;
#4649=ORIENTED_EDGE ( 'NONE', *, *, #42333, .F. ) ;
#4650=CARTESIAN_POINT ( 'NONE',  ( -1.091055626815042645, 3.267716535433071279, 1.892679809432644882E-16 ) ) ;
#4652=FACE_BOUND ( 'NONE', #16284, .T. ) ;
#4653=PLANE ( 'NONE',  #8051 ) ;
#4654=DIRECTION ( 'NONE',  ( 1.000000000000000000, 0.000000000000000000, -3.469446951953613696E-16 ) ) ;
#4655=ORIENTED_EDGE ( 'NONE', *, *, #41993, .T. ) ;
#4656=LINE ( 'NONE', #4910, #38145 ) ;
#4658=EDGE_LOOP ( 'NONE', ( #23084, #488, #50548, #21795 ) ) ;
#4660=ORIENTED_EDGE ( 'NONE', *, *, #5059, .F. ) ;
#4661=LINE ( 'NONE', #44651, #33418 ) ;
#4666=EDGE_LOOP ( 'NONE', ( #6025, #42875, #14834, #956, #15069 ) ) ;
#4667=ORIENTED_EDGE ( 'NONE', *, *, #26158, .T. ) ;
#4671=VECTOR ( 'NONE', #41444, 39.37007874015748143 ) ;
#4672=DIRECTION ( 'NONE',  ( -0.000000000000000000, 1.000000000000000000, -0.000000000000000000 ) ) ;
#4673=CARTESIAN_POINT ( 'NONE',  ( -1.166969139818015977, 3.346456692913386100, 2.047244094488179567 ) ) ;
#4676=LINE ( 'NONE', #31095, #28393 ) ;
#4678=EDGE_CURVE ( 'NONE', #40155, #17243, #9423, .T. ) ;
#4682=VECTOR ( 'NONE', #21803, 39.37007874015748143 ) ;
#4683=ORIENTED_EDGE ( 'NONE', *, *, #28707, .T. ) ;
#4684=LINE ( 'NONE', #23523, #332 ) ;
#4688=DIRECTION ( 'NONE',  ( 1.734723475976806848E-16, -0.000000000000000000, 1.000000000000000000 ) ) ;
#4691=ORIENTED_EDGE ( 'NONE', *, *, #27332, .T. ) ;
#4692=ORIENTED_EDGE ( 'NONE', *, *, #5980, .T. ) ;
#4694=EDGE_CURVE ( 'NONE', #39809, #45998, #24664, .T. ) ;
#4695=ORIENTED_EDGE ( 'NONE', *, *, #29732, .F. ) ;
#4696=CARTESIAN_POINT ( 'NONE',  ( 1.636583440222563857, 3.346456692913386100, 0.9448818897637746295 ) ) ;
#4697=VERTEX_POINT ( 'NONE', #48362 ) ;
#4698=FACE_OUTER_BOUND ( 'NONE', #48020, .T. ) ;
#4701=DIRECTION ( 'NONE',  ( -3.469446951953613696E-16, 0.000000000000000000, -1.000000000000000000 ) ) ;
#4702=VECTOR ( 'NONE', #48332, 39.37007874015748143 ) ;
#4703=EDGE_CURVE ( 'NONE', #13831, #26074, #2185, .T. ) ;
#4705=EDGE_LOOP ( 'NONE', ( #23065, #5618, #6144, #25093 ) ) ;
#4706=ORIENTED_EDGE ( 'NONE', *, *, #2561, .T. ) ;
#4707=VECTOR ( 'NONE', #39660, 39.37007874015748143 ) ;
#4709=EDGE_CURVE ( 'NONE', #36526, #41290, #38069, .T. ) ;
#4710=VERTEX_POINT ( 'NONE', #46280 ) ;
#4711=ORIENTED_EDGE ( 'NONE', *, *, #9306, .F. ) ;
#4712=CARTESIAN_POINT ( 'NONE',  ( 1.015142113812069979, 0.000000000000000000, 2.047244094488179567 ) ) ;
#4713=DIRECTION ( 'NONE',  ( 1.000000000000000000, 0.000000000000000000, 0.000000000000000000 ) ) ;
#4714=LINE ( 'NONE', #28958, #17040 ) ;
#4715=ORIENTED_EDGE ( 'NONE', *, *, #49401, .T. ) ;
#4716=LINE ( 'NONE', #32869, #24658 ) ;
#4719=DIRECTION ( 'NONE',  ( 1.734723475976806848E-16, 0.000000000000000000, 1.000000000000000000 ) ) ;
#4720=VERTEX_POINT ( 'NONE', #26430 ) ;
#4721=PLANE ( 'NONE',  #36443 ) ;
#4722=PLANE ( 'NONE',  #11211 ) ;
#4724=PLANE ( 'NONE',  #22481 ) ;
#4725=VERTEX_POINT ( 'NONE', #49877 ) ;
#4727=CARTESIAN_POINT ( 'NONE',  ( -0.8942052331142552601, 3.346456692913386100, -1.259842519685034690 ) ) ;
#4733=ORIENTED_EDGE ( 'NONE', *, *, #33318, .F. ) ;
#4735=LINE ( 'NONE', #12735, #5304 ) ;
#4736=ORIENTED_EDGE ( 'NONE', *, *, #46551, .F. ) ;
#4739=VECTOR ( 'NONE', #8586, 39.37007874015748143 ) ;
#4740=VECTOR ( 'NONE', #8813, 39.37007874015748143 ) ;
#4742=ADVANCED_FACE ( 'NONE', ( #26932 ), #10940, .F. ) ;
#4744=PLANE ( 'NONE',  #48457 ) ;
#4745=ORIENTED_EDGE ( 'NONE', *, *, #48073, .T. ) ;
#4746=ADVANCED_FACE ( 'NONE', ( #2941 ), #30059, .F. ) ;
#4747=LINE ( 'NONE', #16880, #43955 ) ;
#4748=CARTESIAN_POINT ( 'NONE',  ( -1.636583440222563635, 3.346456692913386100, -4.780733988912460139E-16 ) ) ;
#4751=CARTESIAN_POINT ( 'NONE',  ( 0.8182917201112819283, 0.000000000000000000, -0.9842519685039348154 ) ) ;
#4752=CARTESIAN_POINT ( 'NONE',  ( 1.091055626815042645, 3.346456692913386100, -8.878505979408855953E-16 ) ) ;
#4753=DIRECTION ( 'NONE',  ( 1.734723475976806848E-16, -0.000000000000000000, 1.000000000000000000 ) ) ;
#4754=ORIENTED_EDGE ( 'NONE', *, *, #34362, .T. ) ;
#4758=ORIENTED_EDGE ( 'NONE', *, *, #16062, .F. ) ;
#4759=FACE_BOUND ( 'NONE', #20727, .T. ) ;
#4763=CARTESIAN_POINT ( 'NONE',  ( 0.2727639067037604947, 3.346456692913386100, -1.102362204724405714 ) ) ;
#4764=DIRECTION ( 'NONE',  ( 0.000000000000000000, 0.000000000000000000, -1.000000000000000000 ) ) ;
#4765=EDGE_CURVE ( 'NONE', #25411, #1059, #2687, .T. ) ;
#4767=DIRECTION ( 'NONE',  ( 1.000000000000000000, 0.000000000000000000, 0.000000000000000000 ) ) ;
#4770=LINE ( 'NONE', #24650, #39721 ) ;
#4774=CARTESIAN_POINT ( 'NONE',  ( 2.182111253630085290, 3.267716535433071279, 0.4330708661417287386 ) ) ;
#4775=CARTESIAN_POINT ( 'NONE',  ( 0.7423782071083084855, 3.346456692913386100, -1.889763779527552812 ) ) ;
#4777=CARTESIAN_POINT ( 'NONE',  ( -1.166969139818015977, 0.000000000000000000, -0.1574803149606300023 ) ) ;
#4778=VERTEX_POINT ( 'NONE', #22561 ) ;
#4780=LINE ( 'NONE', #40417, #17217 ) ;
#4782=CIRCLE ( 'NONE', #3924, 2.165354330708661568 ) ;
#4783=AXIS2_PLACEMENT_3D ( 'NONE', #1773, #17023, #28624 ) ;
#4784=DIRECTION ( 'NONE',  ( -0.000000000000000000, 1.000000000000000000, -0.000000000000000000 ) ) ;
#4786=FACE_BOUND ( 'NONE', #11575, .T. ) ;
#4787=VERTEX_POINT ( 'NONE', #18696 ) ;
#4788=LINE ( 'NONE', #20788, #43868 ) ;
#4789=EDGE_LOOP ( 'NONE', ( #40226, #11929, #47735, #7814 ) ) ;
#4790=AXIS2_PLACEMENT_3D ( 'NONE', #20127, #36150, #32029 ) ;
#4791=ORIENTED_EDGE ( 'NONE', *, *, #25202, .T. ) ;
#4792=LINE ( 'NONE', #915, #41567 ) ;
#4794=EDGE_LOOP ( 'NONE', ( #31580, #12070, #23326, #33820 ) ) ;
#4796=DIRECTION ( 'NONE',  ( 0.000000000000000000, 1.000000000000000000, 0.000000000000000000 ) ) ;
#4798=EDGE_LOOP ( 'NONE', ( #33515, #45814, #10272, #15915 ) ) ;
#4799=VECTOR ( 'NONE', #20488, 39.37007874015748143 ) ;
#4800=CARTESIAN_POINT ( 'NONE',  ( -2.182111253630085290, 3.346456692913386100, 0.1181102362204704270 ) ) ;
#4807=CARTESIAN_POINT ( 'NONE',  ( -0.5455278134075214336, 3.346456692913386100, -0.1968503937007883287 ) ) ;
#4811=DIRECTION ( 'NONE',  ( 1.000000000000000000, 0.000000000000000000, 0.000000000000000000 ) ) ;
#4812=DIRECTION ( 'NONE',  ( -1.000000000000000000, 0.000000000000000000, -0.000000000000000000 ) ) ;
#4813=CARTESIAN_POINT ( 'NONE',  ( -1.636583440222563635, 3.267716535433071279, 0.9448818897637749625 ) ) ;
#4814=ADVANCED_FACE ( 'NONE', ( #38570 ), #22315, .F. ) ;
#4816=ORIENTED_EDGE ( 'NONE', *, *, #1617, .F. ) ;
#4817=LINE ( 'NONE', #39668, #42158 ) ;
#4818=CARTESIAN_POINT ( 'NONE',  ( 1.833433833923351353, 0.000000000000000000, -0.3149606299212596716 ) ) ;
#4821=AXIS2_PLACEMENT_3D ( 'NONE', #27546, #44058, #8705 ) ;
#4823=DIRECTION ( 'NONE',  ( 1.734723475976806848E-16, -0.000000000000000000, 1.000000000000000000 ) ) ;
#4824=LINE ( 'NONE', #43274, #42481 ) ;
#4825=EDGE_LOOP ( 'NONE', ( #34619, #13350, #25148, #7372 ) ) ;
#4826=VECTOR ( 'NONE', #42932, 39.37007874015748143 ) ;
#4827=CARTESIAN_POINT ( 'NONE',  ( -1.909347346926324462, 3.346456692913386100, -0.3543307086614171930 ) ) ;
#4829=FACE_BOUND ( 'NONE', #48392, .T. ) ;
#4830=FACE_OUTER_BOUND ( 'NONE', #19761, .T. ) ;
#4832=VECTOR ( 'NONE', #49293, 39.37007874015748143 ) ;
#4833=CARTESIAN_POINT ( 'NONE',  ( -1.536664496436148184E-16, 3.346456692913386100, -1.141732283464564013 ) ) ;
#4834=ADVANCED_FACE ( 'NONE', ( #46528 ), #25930, .F. ) ;
#4835=DIRECTION ( 'NONE',  ( 1.000000000000000000, 0.000000000000000000, 0.000000000000000000 ) ) ;
#4836=ORIENTED_EDGE ( 'NONE', *, *, #10212, .T. ) ;
#4837=ORIENTED_EDGE ( 'NONE', *, *, #28460, .F. ) ;
#4838=LINE ( 'NONE', #23419, #26230 ) ;
#4839=ORIENTED_EDGE ( 'NONE', *, *, #42619, .F. ) ;
#4840=EDGE_CURVE ( 'NONE', #6948, #30730, #2442, .T. ) ;
#4845=ORIENTED_EDGE ( 'NONE', *, *, #45343, .T. ) ;
#4846=EDGE_CURVE ( 'NONE', #17653, #49899, #38820, .T. ) ;
#4847=DIRECTION ( 'NONE',  ( -0.000000000000000000, 1.000000000000000000, -0.000000000000000000 ) ) ;
#4849=ORIENTED_EDGE ( 'NONE', *, *, #5408, .F. ) ;
#4850=FACE_OUTER_BOUND ( 'NONE', #5432, .T. ) ;
#4852=EDGE_CURVE ( 'NONE', #4778, #1584, #22060, .T. ) ;
#4853=CARTESIAN_POINT ( 'NONE',  ( 1.015142113812069313, 3.346456692913386100, -0.6692913385826764205 ) ) ;
#4854=AXIS2_PLACEMENT_3D ( 'NONE', #3244, #14360, #10491 ) ;
#4856=VERTEX_POINT ( 'NONE', #28197 ) ;
#4859=LINE ( 'NONE', #20601, #46838 ) ;
#4860=ORIENTED_EDGE ( 'NONE', *, *, #19366, .F. ) ;
#4861=CARTESIAN_POINT ( 'NONE',  ( 0.000000000000000000, 3.267716535433071279, -1.574803149606294417 ) ) ;
#4862=CARTESIAN_POINT ( 'NONE',  ( -2.182111253630085734, 0.000000000000000000, -0.8267716535433052849 ) ) ;
#4863=VECTOR ( 'NONE', #42173, 39.37007874015748143 ) ;
#4864=VECTOR ( 'NONE', #34557, 39.37007874015748143 ) ;
#4865=CARTESIAN_POINT ( 'NONE',  ( -0.07591351300297333182, 3.346456692913386100, -1.417322834645664331 ) ) ;
#4866=ORIENTED_EDGE ( 'NONE', *, *, #49393, .T. ) ;
#4867=CARTESIAN_POINT ( 'NONE',  ( 2.017116292511733189, 3.346456692913386100, -0.7874015748031473194 ) ) ;
#4869=CARTESIAN_POINT ( 'NONE',  ( -0.6214413264104945434, 3.267716535433071279, 2.156057715732901026E-16 ) ) ;
#4871=VECTOR ( 'NONE', #15786, 39.37007874015748143 ) ;
#4872=DIRECTION ( 'NONE',  ( 1.000000000000000000, 0.000000000000000000, 0.000000000000000000 ) ) ;
#4873=DIRECTION ( 'NONE',  ( 1.000000000000000000, -0.000000000000000000, 0.000000000000000000 ) ) ;
#4874=ADVANCED_FACE ( 'NONE', ( #16337 ), #43174, .F. ) ;
#4876=ADVANCED_FACE ( 'NONE', ( #8333 ), #589, .F. ) ;
#4877=VERTEX_POINT ( 'NONE', #39575 ) ;
#4878=EDGE_CURVE ( 'NONE', #49034, #6476, #12456, .T. ) ;
#4879=FACE_OUTER_BOUND ( 'NONE', #34844, .T. ) ;
#4880=ORIENTED_EDGE ( 'NONE', *, *, #43802, .T. ) ;
#4884=DIRECTION ( 'NONE',  ( 1.000000000000000000, -0.000000000000000000, 0.000000000000000000 ) ) ;
#4885=FACE_OUTER_BOUND ( 'NONE', #44431, .T. ) ;
#4886=CARTESIAN_POINT ( 'NONE',  ( -0.5455278134075216556, 3.346456692913386100, -2.204724409448810540 ) ) ;
#4887=ORIENTED_EDGE ( 'NONE', *, *, #29758, .T. ) ;
#4888=CARTESIAN_POINT ( 'NONE',  ( 3.256118103108526111E-16, 3.267716535433071279, 2.443628662382284489 ) ) ;
#4889=FACE_BOUND ( 'NONE', #16339, .T. ) ;
#4890=VERTEX_POINT ( 'NONE', #46775 ) ;
#4892=EDGE_LOOP ( 'NONE', ( #8482, #11764, #26805, #8017 ) ) ;
#4893=AXIS2_PLACEMENT_3D ( 'NONE', #7088, #11709, #42696 ) ;
#4894=FACE_OUTER_BOUND ( 'NONE', #50074, .T. ) ;
#4895=DIRECTION ( 'NONE',  ( -1.000000000000000000, 0.000000000000000000, 0.000000000000000000 ) ) ;
#4896=EDGE_CURVE ( 'NONE', #24628, #1125, #31575, .T. ) ;
#4899=VERTEX_POINT ( 'NONE', #11694 ) ;
#4900=ORIENTED_EDGE ( 'NONE', *, *, #25123, .T. ) ;
#4901=DIRECTION ( 'NONE',  ( -1.000000000000000000, 0.000000000000000000, 0.000000000000000000 ) ) ;
#4902=LINE ( 'NONE', #20646, #3466 ) ;
#4903=FACE_BOUND ( 'NONE', #5937, .T. ) ;
#4905=EDGE_CURVE ( 'NONE', #8911, #43312, #27945, .T. ) ;
#4908=EDGE_CURVE ( 'NONE', #12085, #29688, #31323, .T. ) ;
#4910=CARTESIAN_POINT ( 'NONE',  ( 0.000000000000000000, 3.267716535433071279, 0.4330708661417290162 ) ) ;
#4912=EDGE_CURVE ( 'NONE', #23868, #47925, #7574, .T. ) ;
#4913=ORIENTED_EDGE ( 'NONE', *, *, #766, .T. ) ;
#4917=DIRECTION ( 'NONE',  ( -3.469446951953613696E-16, 0.000000000000000000, -1.000000000000000000 ) ) ;
#4918=DIRECTION ( 'NONE',  ( -3.469446951953613696E-16, 0.000000000000000000, -1.000000000000000000 ) ) ;
#4919=VECTOR ( 'NONE', #27865, 39.37007874015748143 ) ;
#4920=DIRECTION ( 'NONE',  ( 1.000000000000000000, 0.000000000000000000, -3.469446951953613696E-16 ) ) ;
#4922=EDGE_LOOP ( 'NONE', ( #13627, #35055, #24672, #46414 ) ) ;
#4923=ORIENTED_EDGE ( 'NONE', *, *, #42368, .T. ) ;
#4926=CARTESIAN_POINT ( 'NONE',  ( 0.4696143004045484348, 3.346456692913386100, 1.535433070866133898 ) ) ;
#4927=CARTESIAN_POINT ( 'NONE',  ( -1.439733046521776139, 0.000000000000000000, 0.3149606299212578953 ) ) ;
#4929=EDGE_CURVE ( 'NONE', #37360, #49076, #7823, .T. ) ;
#4930=CIRCLE ( 'NONE', #8214, 2.165354330708661568 ) ;
#4931=DIRECTION ( 'NONE',  ( 1.734723475976806848E-16, -0.000000000000000000, 1.000000000000000000 ) ) ;
#4933=EDGE_CURVE ( 'NONE', #3787, #4283, #3954, .T. ) ;
#4935=DIRECTION ( 'NONE',  ( -1.000000000000000000, -0.000000000000000000, -0.000000000000000000 ) ) ;
#4936=ORIENTED_EDGE ( 'NONE', *, *, #17932, .F. ) ;
#4938=CARTESIAN_POINT ( 'NONE',  ( 0.7423782071083084855, 0.000000000000000000, -1.889763779527552812 ) ) ;
#4939=AXIS2_PLACEMENT_3D ( 'NONE', #25913, #42661, #34427 ) ;
#4940=EDGE_LOOP ( 'NONE', ( #17995, #32729, #45783, #12798 ) ) ;
#4942=LINE ( 'NONE', #44171, #5125 ) ;
#4943=DIRECTION ( 'NONE',  ( 1.734723475976806848E-16, -0.000000000000000000, 1.000000000000000000 ) ) ;
#4944=CARTESIAN_POINT ( 'NONE',  ( 1.909347346926324462, 0.000000000000000000, -0.7874015748031473194 ) ) ;
#4945=ORIENTED_EDGE ( 'NONE', *, *, #1555, .T. ) ;
#4946=ORIENTED_EDGE ( 'NONE', *, *, #10906, .T. ) ;
#4947=DIRECTION ( 'NONE',  ( 1.734723475976806848E-16, 0.000000000000000000, 1.000000000000000000 ) ) ;
#4948=EDGE_LOOP ( 'NONE', ( #8306, #20787, #23073, #40405 ) ) ;
#4949=ORIENTED_EDGE ( 'NONE', *, *, #18847, .F. ) ;
#4950=LINE ( 'NONE', #1844, #7880 ) ;
#4951=FACE_OUTER_BOUND ( 'NONE', #7570, .T. ) ;
#4953=EDGE_CURVE ( 'NONE', #42837, #31796, #12207, .T. ) ;
#4954=ORIENTED_EDGE ( 'NONE', *, *, #18206, .T. ) ;
#4955=ORIENTED_EDGE ( 'NONE', *, *, #20729, .T. ) ;
#4956=VERTEX_POINT ( 'NONE', #16079 ) ;
#4958=ORIENTED_EDGE ( 'NONE', *, *, #3669, .T. ) ;
#4959=VERTEX_POINT ( 'NONE', #31072 ) ;
#4960=DIRECTION ( 'NONE',  ( -0.000000000000000000, 1.000000000000000000, -0.000000000000000000 ) ) ;
#4961=LINE ( 'NONE', #43932, #48308 ) ;
#4962=PLANE ( 'NONE',  #31893 ) ;
#4963=EDGE_CURVE ( 'NONE', #47752, #32071, #35960, .T. ) ;
#4964=VECTOR ( 'NONE', #38649, 39.37007874015748143 ) ;
#4966=AXIS2_PLACEMENT_3D ( 'NONE', #18451, #24982, #10451 ) ;
#4967=EDGE_CURVE ( 'NONE', #5543, #45211, #19427, .T. ) ;
#4968=CARTESIAN_POINT ( 'NONE',  ( -2.454875160333845674, 3.189042514953126961, -0.3543307086614173040 ) ) ;
#4969=CARTESIAN_POINT ( 'NONE',  ( -0.5455278134075213226, 3.267716535433071279, 9.463399047163221947E-17 ) ) ;
#4970=CARTESIAN_POINT ( 'NONE',  ( 0.4696143004045479352, 0.000000000000000000, 0.1574803149606283648 ) ) ;
#4972=ORIENTED_EDGE ( 'NONE', *, *, #958, .T. ) ;
#4973=LINE ( 'NONE', #8588, #159 ) ;
#4974=CARTESIAN_POINT ( 'NONE',  ( -1.636583440222563635, 0.000000000000000000, 0.3149606299212578953 ) ) ;
#4975=CARTESIAN_POINT ( 'NONE',  ( -0.8942052331142552601, 0.000000000000000000, 2.204724409448808764 ) ) ;
#4977=ORIENTED_EDGE ( 'NONE', *, *, #22978, .F. ) ;
#4978=AXIS2_PLACEMENT_3D ( 'NONE', #17290, #9027, #48987 ) ;
#4979=FACE_OUTER_BOUND ( 'NONE', #4892, .T. ) ;
#4983=EDGE_CURVE ( 'NONE', #17988, #4450, #11447, .T. ) ;
#4987=CARTESIAN_POINT ( 'NONE',  ( -1.439733046521777027, 3.346456692913386100, -0.8267716535433052849 ) ) ;
#4988=EDGE_CURVE ( 'NONE', #36614, #35430, #39064, .T. ) ;
#4989=ORIENTED_EDGE ( 'NONE', *, *, #43374, .T. ) ;
#4990=CARTESIAN_POINT ( 'NONE',  ( -2.103998301714549157, 3.346456692913386100, -0.5118110236220464460 ) ) ;
#4991=DIRECTION ( 'NONE',  ( -1.000000000000000000, 0.000000000000000000, 1.734723475976806848E-16 ) ) ;
#4992=ADVANCED_FACE ( 'NONE', ( #25606 ), #9096, .F. ) ;
#4993=EDGE_CURVE ( 'NONE', #20171, #43099, #17107, .T. ) ;
#4994=DIRECTION ( 'NONE',  ( 1.000000000000000000, 0.000000000000000000, 0.000000000000000000 ) ) ;
#4995=LINE ( 'NONE', #47043, #31837 ) ;
#4996=CARTESIAN_POINT ( 'NONE',  ( 0.4696143004045484903, 3.346456692913386100, 1.102362204724404160 ) ) ;
#4997=ORIENTED_EDGE ( 'NONE', *, *, #18346, .F. ) ;
#4999=EDGE_CURVE ( 'NONE', #26233, #16054, #16856, .T. ) ;
#5000=DIRECTION ( 'NONE',  ( -0.000000000000000000, 1.000000000000000000, -0.000000000000000000 ) ) ;
#5001=VECTOR ( 'NONE', #8288, 39.37007874015748143 ) ;
#5002=ORIENTED_EDGE ( 'NONE', *, *, #5384, .T. ) ;
#5006=DIRECTION ( 'NONE',  ( -1.000000000000000000, -0.000000000000000000, -0.000000000000000000 ) ) ;
#5007=ORIENTED_EDGE ( 'NONE', *, *, #26540, .F. ) ;
#5008=CARTESIAN_POINT ( 'NONE',  ( -2.182111253630085290, 3.346456692913386100, -0.3149606299212589500 ) ) ;
#5009=LINE ( 'NONE', #36512, #7695 ) ;
#5012=LINE ( 'NONE', #16383, #7371 ) ;
#5013=VECTOR ( 'NONE', #40471, 39.37007874015748143 ) ;
#5014=LINE ( 'NONE', #44247, #23280 ) ;
#5016=DIRECTION ( 'NONE',  ( -1.000000000000000000, 0.000000000000000000, 1.734723475976806848E-16 ) ) ;
#5018=CARTESIAN_POINT ( 'NONE',  ( -1.794796351285542491, 3.346456692913386100, 1.102362204724404160 ) ) ;
#5023=ORIENTED_EDGE ( 'NONE', *, *, #40851, .F. ) ;
#5024=LINE ( 'NONE', #4007, #47086 ) ;
#5025=DIRECTION ( 'NONE',  ( 0.000000000000000000, 0.000000000000000000, -1.000000000000000000 ) ) ;
#5026=ORIENTED_EDGE ( 'NONE', *, *, #691, .T. ) ;
#5027=CARTESIAN_POINT ( 'NONE',  ( -0.3486774197067334380, 3.267716535433071279, 0.9448818897637749625 ) ) ;
#5028=LINE ( 'NONE', #5281, #21937 ) ;
#5030=DIRECTION ( 'NONE',  ( -3.469446951953613696E-16, 0.000000000000000000, -1.000000000000000000 ) ) ;
#5032=ORIENTED_EDGE ( 'NONE', *, *, #13516, .T. ) ;
#5033=EDGE_CURVE ( 'NONE', #10946, #14069, #28711, .T. ) ;
#5034=DIRECTION ( 'NONE',  ( 1.000000000000000000, 0.000000000000000000, 0.000000000000000000 ) ) ;
#5035=DIRECTION ( 'NONE',  ( -3.469446951953613696E-16, 0.000000000000000000, -1.000000000000000000 ) ) ;
#5037=ORIENTED_EDGE ( 'NONE', *, *, #17363, .F. ) ;
#5039=EDGE_CURVE ( 'NONE', #41221, #39372, #48552, .T. ) ;
#5040=FACE_BOUND ( 'NONE', #4798, .T. ) ;
#5043=ORIENTED_EDGE ( 'NONE', *, *, #16110, .F. ) ;
#5046=AXIS2_PLACEMENT_3D ( 'NONE', #21702, #6717, #17323 ) ;
#5047=VECTOR ( 'NONE', #45197, 39.37007874015748143 ) ;
#5048=VERTEX_POINT ( 'NONE', #24849 ) ;
#5049=ORIENTED_EDGE ( 'NONE', *, *, #36805, .F. ) ;
#5050=PLANE ( 'NONE',  #18695 ) ;
#5052=VERTEX_POINT ( 'NONE', #29485 ) ;
#5053=VECTOR ( 'NONE', #30244, 39.37007874015748143 ) ;
#5054=EDGE_CURVE ( 'NONE', #373, #17272, #40598, .T. ) ;
#5055=DIRECTION ( 'NONE',  ( -0.000000000000000000, 0.000000000000000000, 1.000000000000000000 ) ) ;
#5057=LINE ( 'NONE', #47356, #47300 ) ;
#5058=VECTOR ( 'NONE', #38162, 39.37007874015748143 ) ;
#5059=EDGE_CURVE ( 'NONE', #35559, #28822, #9353, .T. ) ;
#5060=DIRECTION ( 'NONE',  ( -1.000000000000000000, 0.000000000000000000, -0.000000000000000000 ) ) ;
#5061=CARTESIAN_POINT ( 'NONE',  ( 1.015142113812069313, 3.346456692913386100, -0.7874015748031473194 ) ) ;
#5062=CARTESIAN_POINT ( 'NONE',  ( 0.1968503937007874405, 0.000000000000000000, 0.000000000000000000 ) ) ;
#5063=ORIENTED_EDGE ( 'NONE', *, *, #10594, .F. ) ;
#5064=CARTESIAN_POINT ( 'NONE',  ( -0.6214413264104939882, 3.346456692913386100, 1.417322834645662777 ) ) ;
#5065=EDGE_CURVE ( 'NONE', #54, #45803, #12979, .T. ) ;
#5068=LINE ( 'NONE', #9963, #42952 ) ;
#5069=CARTESIAN_POINT ( 'NONE',  ( -0.3486774197067339376, 3.267716535433071279, -0.9448818897637762948 ) ) ;
#5073=LINE ( 'NONE', #20036, #44933 ) ;
#5076=ORIENTED_EDGE ( 'NONE', *, *, #50492, .F. ) ;
#5077=FACE_BOUND ( 'NONE', #25467, .T. ) ;
#5082=CARTESIAN_POINT ( 'NONE',  ( 0.000000000000000000, 3.346456692913386100, 0.000000000000000000 ) ) ;
#5083=AXIS2_PLACEMENT_3D ( 'NONE', #7374, #641, #28505 ) ;
#5084=ORIENTED_EDGE ( 'NONE', *, *, #17746, .T. ) ;
#5085=ORIENTED_EDGE ( 'NONE', *, *, #16592, .F. ) ;
#5086=PLANE ( 'NONE',  #13114 ) ;
#5088=AXIS2_PLACEMENT_3D ( 'NONE', #13618, #44075, #29355 ) ;
#5089=DIRECTION ( 'NONE',  ( -0.000000000000000000, 0.000000000000000000, 1.000000000000000000 ) ) ;
#5091=LINE ( 'NONE', #32476, #2552 ) ;
#5093=ORIENTED_EDGE ( 'NONE', *, *, #41636, .T. ) ;
#5094=DIRECTION ( 'NONE',  ( -0.000000000000000000, 0.000000000000000000, 1.000000000000000000 ) ) ;
#5096=EDGE_CURVE ( 'NONE', #11186, #7899, #40853, .T. ) ;
#5097=ORIENTED_EDGE ( 'NONE', *, *, #917, .T. ) ;
#5098=EDGE_CURVE ( 'NONE', #29929, #41791, #33122, .T. ) ;
#5099=PLANE ( 'NONE',  #50394 ) ;
#5100=VERTEX_POINT ( 'NONE', #29225 ) ;
#5102=EDGE_CURVE ( 'NONE', #31043, #19694, #36730, .T. ) ;
#5103=EDGE_LOOP ( 'NONE', ( #630, #39990, #49805, #12724 ) ) ;
#5104=ORIENTED_EDGE ( 'NONE', *, *, #6795, .T. ) ;
#5105=LINE ( 'NONE', #16735, #24006 ) ;
#5106=VERTEX_POINT ( 'NONE', #28963 ) ;
#5107=CARTESIAN_POINT ( 'NONE',  ( -0.07591351300297340121, 3.267716535433071279, -0.03937007874015908959 ) ) ;
#5109=CARTESIAN_POINT ( 'NONE',  ( -0.8182917201112819283, 3.267716535433071279, 1.419509857074483292E-16 ) ) ;
#5113=CARTESIAN_POINT ( 'NONE',  ( -0.5455278134075214336, 3.346456692913386100, 2.007874015748021268 ) ) ;
#5114=ORIENTED_EDGE ( 'NONE', *, *, #17469, .T. ) ;
#5119=LINE ( 'NONE', #36622, #1029 ) ;
#5120=CARTESIAN_POINT ( 'NONE',  ( -0.2727639067037608278, 0.000000000000000000, -0.9842519685039344823 ) ) ;
#5122=VECTOR ( 'NONE', #17177, 39.37007874015748143 ) ;
#5123=CARTESIAN_POINT ( 'NONE',  ( 2.052631463899901920, 3.346456692913386100, -0.4724409448818889246 ) ) ;
#5125=VECTOR ( 'NONE', #12952, 39.37007874015748143 ) ;
#5127=ORIENTED_EDGE ( 'NONE', *, *, #41999, .T. ) ;
#5128=DIRECTION ( 'NONE',  ( -3.469446951953613696E-16, 0.000000000000000000, -1.000000000000000000 ) ) ;
#5131=LINE ( 'NONE', #41273, #8629 ) ;
#5133=ADVANCED_FACE ( 'NONE', ( #5737 ), #9866, .F. ) ;
#5134=DIRECTION ( 'NONE',  ( 0.000000000000000000, 0.000000000000000000, 1.000000000000000000 ) ) ;
#5135=FACE_OUTER_BOUND ( 'NONE', #30795, .T. ) ;
#5136=CARTESIAN_POINT ( 'NONE',  ( -1.636583440222563635, 0.000000000000000000, 0.6299212598425164567 ) ) ;
#5138=LINE ( 'NONE', #16511, #26885 ) ;
#5139=ORIENTED_EDGE ( 'NONE', *, *, #23479, .T. ) ;
#5141=FACE_BOUND ( 'NONE', #15625, .T. ) ;
#5144=ORIENTED_EDGE ( 'NONE', *, *, #39737, .T. ) ;
#5146=DIRECTION ( 'NONE',  ( -1.000000000000000000, 0.000000000000000000, -0.000000000000000000 ) ) ;
#5147=VECTOR ( 'NONE', #14113, 39.37007874015748143 ) ;
#5149=ORIENTED_EDGE ( 'NONE', *, *, #24398, .T. ) ;
#5151=VERTEX_POINT ( 'NONE', #44200 ) ;
#5154=LINE ( 'NONE', #17296, #47090 ) ;
#5155=FACE_BOUND ( 'NONE', #9383, .T. ) ;
#5156=EDGE_CURVE ( 'NONE', #33305, #43110, #8843, .T. ) ;
#5157=VECTOR ( 'NONE', #16491, 39.37007874015748143 ) ;
#5160=PLANE ( 'NONE',  #8571 ) ;
#5161=EDGE_CURVE ( 'NONE', #36537, #13304, #6755, .T. ) ;
#5162=EDGE_CURVE ( 'NONE', #47679, #50505, #18121, .T. ) ;
#5163=ORIENTED_EDGE ( 'NONE', *, *, #45852, .T. ) ;
#5165=VERTEX_POINT ( 'NONE', #45962 ) ;
#5166=ORIENTED_EDGE ( 'NONE', *, *, #18903, .F. ) ;
#5168=VERTEX_POINT ( 'NONE', #37753 ) ;
#5170=PLANE ( 'NONE',  #7698 ) ;
#5171=EDGE_CURVE ( 'NONE', #11955, #30948, #10630, .T. ) ;
#5172=DIRECTION ( 'NONE',  ( 1.000000000000000000, 0.000000000000000000, 0.000000000000000000 ) ) ;
#5173=DIRECTION ( 'NONE',  ( -1.000000000000000000, 0.000000000000000000, -0.000000000000000000 ) ) ;
#5174=VERTEX_POINT ( 'NONE', #49563 ) ;
#5175=VERTEX_POINT ( 'NONE', #26369 ) ;
#5177=DIRECTION ( 'NONE',  ( -3.469446951953613696E-16, 0.000000000000000000, -1.000000000000000000 ) ) ;
#5180=DIRECTION ( 'NONE',  ( 1.000000000000000000, 0.000000000000000000, 0.000000000000000000 ) ) ;
#5181=CARTESIAN_POINT ( 'NONE',  ( 1.015142113812069313, 3.346456692913386100, -1.102362204724405714 ) ) ;
#5183=EDGE_CURVE ( 'NONE', #4787, #18808, #42115, .T. ) ;
#5184=DIRECTION ( 'NONE',  ( 1.000000000000000000, 0.000000000000000000, 0.000000000000000000 ) ) ;
#5188=LINE ( 'NONE', #6218, #2984 ) ;
#5189=EDGE_LOOP ( 'NONE', ( #27153, #29663, #29166, #50793 ) ) ;
#5190=ADVANCED_FACE ( 'NONE', ( #2376 ), #26617, .F. ) ;
#5191=AXIS2_PLACEMENT_3D ( 'NONE', #29944, #13693, #44907 ) ;
#5192=ORIENTED_EDGE ( 'NONE', *, *, #6673, .F. ) ;
#5193=VECTOR ( 'NONE', #3851, 39.37007874015748143 ) ;
#5194=DIRECTION ( 'NONE',  ( 1.000000000000000000, 0.000000000000000000, 0.000000000000000000 ) ) ;
#5195=CARTESIAN_POINT ( 'NONE',  ( 1.560669927219590303, 0.000000000000000000, -1.417322834645665219 ) ) ;
#5197=VECTOR ( 'NONE', #35033, 39.37007874015748143 ) ;
#5198=EDGE_CURVE ( 'NONE', #47008, #18423, #22500, .T. ) ;
#5199=ORIENTED_EDGE ( 'NONE', *, *, #36575, .T. ) ;
#5202=ORIENTED_EDGE ( 'NONE', *, *, #3385, .F. ) ;
#5203=EDGE_CURVE ( 'NONE', #25675, #40849, #45455, .T. ) ;
#5204=FACE_OUTER_BOUND ( 'NONE', #32993, .T. ) ;
#5206=ORIENTED_EDGE ( 'NONE', *, *, #50818, .T. ) ;
#5207=VERTEX_POINT ( 'NONE', #2879 ) ;
#5209=LINE ( 'NONE', #25344, #24683 ) ;
#5212=CARTESIAN_POINT ( 'NONE',  ( 1.909347346926324684, 3.346456692913386100, 1.021348170950612033 ) ) ;
#5216=VERTEX_POINT ( 'NONE', #33881 ) ;
#5217=DIRECTION ( 'NONE',  ( 1.000000000000000000, 0.000000000000000000, 0.000000000000000000 ) ) ;
#5218=CARTESIAN_POINT ( 'NONE',  ( -0.5455278134075214336, 3.346456692913386100, -1.574803149606293529 ) ) ;
#5220=EDGE_CURVE ( 'NONE', #39958, #44569, #38005, .T. ) ;
#5221=ORIENTED_EDGE ( 'NONE', *, *, #12536, .F. ) ;
#5222=FACE_OUTER_BOUND ( 'NONE', #33682, .T. ) ;
#5223=VECTOR ( 'NONE', #7754, 39.37007874015748143 ) ;
#5224=CARTESIAN_POINT ( 'NONE',  ( -0.6214413264104939882, 0.000000000000000000, 0.9055118110236167750 ) ) ;
#5225=DIRECTION ( 'NONE',  ( 0.000000000000000000, 1.000000000000000000, 0.000000000000000000 ) ) ;
#5226=ORIENTED_EDGE ( 'NONE', *, *, #15675, .T. ) ;
#5227=AXIS2_PLACEMENT_3D ( 'NONE', #6980, #10849, #26587 ) ;
#5228=ORIENTED_EDGE ( 'NONE', *, *, #22310, .F. ) ;
#5230=DIRECTION ( 'NONE',  ( -1.000000000000000000, 0.000000000000000000, 0.000000000000000000 ) ) ;
#5231=AXIS2_PLACEMENT_3D ( 'NONE', #3082, #35086, #26570 ) ;
#5232=CIRCLE ( 'NONE', #282, 2.106299212598425008 ) ;
#5234=LINE ( 'NONE', #49328, #36864 ) ;
#5235=CARTESIAN_POINT ( 'NONE',  ( 0.7423782071083087075, 0.000000000000000000, -0.9448818897637765168 ) ) ;
#5237=ORIENTED_EDGE ( 'NONE', *, *, #49263, .F. ) ;
#5238=VECTOR ( 'NONE', #21001, 39.37007874015748143 ) ;
#5239=CARTESIAN_POINT ( 'NONE',  ( 1.015142113812069313, 3.346456692913386100, -0.1574803149606301411 ) ) ;
#5240=ORIENTED_EDGE ( 'NONE', *, *, #39388, .T. ) ;
#5242=LINE ( 'NONE', #44977, #16014 ) ;
#5243=EDGE_CURVE ( 'NONE', #22183, #15854, #3128, .T. ) ;
#5244=DIRECTION ( 'NONE',  ( -1.000000000000000000, 0.000000000000000000, 1.734723475976806848E-16 ) ) ;
#5245=CARTESIAN_POINT ( 'NONE',  ( -0.3486774197067341041, 3.267716535433071279, 1.209717811016579571E-16 ) ) ;
#5248=DIRECTION ( 'NONE',  ( -3.469446951953613696E-16, 0.000000000000000000, -1.000000000000000000 ) ) ;
#5249=LINE ( 'NONE', #5510, #45476 ) ;
#5250=EDGE_CURVE ( 'NONE', #21513, #17057, #46217, .T. ) ;
#5252=LINE ( 'NONE', #28997, #34760 ) ;
#5254=LINE ( 'NONE', #6283, #8009 ) ;
#5256=ORIENTED_EDGE ( 'NONE', *, *, #43702, .T. ) ;
#5259=FACE_OUTER_BOUND ( 'NONE', #32846, .T. ) ;
#5262=ORIENTED_EDGE ( 'NONE', *, *, #10542, .T. ) ;
#5267=LINE ( 'NONE', #1648, #18784 ) ;
#5269=VECTOR ( 'NONE', #47746, 39.37007874015748143 ) ;
#5271=LINE ( 'NONE', #20760, #15628 ) ;
#5273=CARTESIAN_POINT ( 'NONE',  ( -1.091055626815042201, 3.346456692913386100, 1.259842519685033357 ) ) ;
#5274=EDGE_LOOP ( 'NONE', ( #8670, #5023, #37442, #29473 ) ) ;
#5275=ORIENTED_EDGE ( 'NONE', *, *, #17950, .F. ) ;
#5277=AXIS2_PLACEMENT_3D ( 'NONE', #16561, #24305, #8808 ) ;
#5278=CARTESIAN_POINT ( 'NONE',  ( -2.082617625631827174, 3.346456692913386100, 0.3149606299212578953 ) ) ;
#5279=ORIENTED_EDGE ( 'NONE', *, *, #36053, .F. ) ;
#5280=DIRECTION ( 'NONE',  ( -3.469446951953613696E-16, 0.000000000000000000, -1.000000000000000000 ) ) ;
#5281=CARTESIAN_POINT ( 'NONE',  ( 1.560669927219591191, 3.267716535433071279, -5.414661521997678257E-16 ) ) ;
#5284=CARTESIAN_POINT ( 'NONE',  ( -1.166969139818015977, 0.000000000000000000, -1.102362204724405270 ) ) ;
#5286=ORIENTED_EDGE ( 'NONE', *, *, #5558, .F. ) ;
#5287=DIRECTION ( 'NONE',  ( -1.000000000000000000, 0.000000000000000000, 0.000000000000000000 ) ) ;
#5289=LINE ( 'NONE', #49380, #41236 ) ;
#5293=FACE_BOUND ( 'NONE', #48183, .T. ) ;
#5295=EDGE_CURVE ( 'NONE', #1759, #12892, #29653, .T. ) ;
#5297=ORIENTED_EDGE ( 'NONE', *, *, #22713, .T. ) ;
#5299=DIRECTION ( 'NONE',  ( -0.000000000000000000, 1.000000000000000000, -0.000000000000000000 ) ) ;
#5300=EDGE_LOOP ( 'NONE', ( #2251, #17374, #13821, #1024 ) ) ;
#5301=PLANE ( 'NONE',  #35156 ) ;
#5302=ORIENTED_EDGE ( 'NONE', *, *, #21065, .T. ) ;
#5303=AXIS2_PLACEMENT_3D ( 'NONE', #29437, #47988, #20922 ) ;
#5304=VECTOR ( 'NONE', #44224, 39.37007874015748143 ) ;
#5305=LINE ( 'NONE', #42377, #8148 ) ;
#5306=FACE_OUTER_BOUND ( 'NONE', #50047, .T. ) ;
#5307=DIRECTION ( 'NONE',  ( 1.000000000000000000, 0.000000000000000000, 0.000000000000000000 ) ) ;
#5308=VECTOR ( 'NONE', #12060, 39.37007874015748143 ) ;
#5309=VECTOR ( 'NONE', #40757, 39.37007874015748143 ) ;
#5311=B_SPLINE_CURVE_WITH_KNOTS ( 'NONE', 3,
 ( #37586, #17953, #41202, #40945 ),
 .UNSPECIFIED., .F., .F.,
 ( 4, 4 ),
 ( 0.03860485074691297896, 0.04008437576871594354 ),
 .UNSPECIFIED. ) ;
#5312=PLANE ( 'NONE',  #31393 ) ;
#5314=DIRECTION ( 'NONE',  ( 1.000000000000000000, 0.000000000000000000, 0.000000000000000000 ) ) ;
#5316=ORIENTED_EDGE ( 'NONE', *, *, #46102, .F. ) ;
#5317=LINE ( 'NONE', #25700, #44774 ) ;
#5318=CARTESIAN_POINT ( 'NONE',  ( 1.909347346926324684, 3.267716535433071279, -0.4724409448818889246 ) ) ;
#5319=ORIENTED_EDGE ( 'NONE', *, *, #37509, .T. ) ;
#5322=LINE ( 'NONE', #12307, #46679 ) ;
#5323=VERTEX_POINT ( 'NONE', #41522 ) ;
#5324=DIRECTION ( 'NONE',  ( 1.000000000000000000, 0.000000000000000000, 0.000000000000000000 ) ) ;
#5325=EDGE_CURVE ( 'NONE', #10605, #13662, #13145, .T. ) ;
#5326=LINE ( 'NONE', #21077, #7803 ) ;
#5327=EDGE_CURVE ( 'NONE', #39217, #47188, #5652, .T. ) ;
#5329=EDGE_LOOP ( 'NONE', ( #47541, #13338, #10578, #9171 ) ) ;
#5330=CARTESIAN_POINT ( 'NONE',  ( 0.1968503937007873017, 3.346456692913386100, 0.6299212598425161236 ) ) ;
#5332=FACE_BOUND ( 'NONE', #33690, .T. ) ;
#5333=CARTESIAN_POINT ( 'NONE',  ( 0.1968503937007872462, 3.267716535433071279, 0.1181102362204701633 ) ) ;
#5334=EDGE_CURVE ( 'NONE', #2753, #32787, #43452, .T. ) ;
#5335=CARTESIAN_POINT ( 'NONE',  ( 1.636583440222563857, 3.346456692913386100, 0.9448818897637746295 ) ) ;
#5336=DIRECTION ( 'NONE',  ( 1.000000000000000000, -0.000000000000000000, 0.000000000000000000 ) ) ;
#5337=ORIENTED_EDGE ( 'NONE', *, *, #34389, .F. ) ;
#5338=ORIENTED_EDGE ( 'NONE', *, *, #39768, .T. ) ;
#5340=CARTESIAN_POINT ( 'NONE',  ( -0.07591351300297277671, 0.000000000000000000, 0.7874015748031456541 ) ) ;
#5341=EDGE_LOOP ( 'NONE', ( #30961, #25210, #24135, #3080 ) ) ;
#5343=EDGE_CURVE ( 'NONE', #7654, #22523, #25266, .T. ) ;
#5344=CARTESIAN_POINT ( 'NONE',  ( 1.909347346926324684, 3.267716535433071279, -3.312189666507128175E-16 ) ) ;
#5346=VECTOR ( 'NONE', #19733, 39.37007874015748143 ) ;
#5347=DIRECTION ( 'NONE',  ( 1.734723475976806848E-16, 0.000000000000000000, 1.000000000000000000 ) ) ;
#5348=EDGE_CURVE ( 'NONE', #30262, #18933, #17021, .T. ) ;
#5349=VERTEX_POINT ( 'NONE', #6156 ) ;
#5350=PLANE ( 'NONE',  #21669 ) ;
#5351=ADVANCED_FACE ( 'NONE', ( #49226 ), #29392, .F. ) ;
#5353=AXIS2_PLACEMENT_3D ( 'NONE', #42784, #15927, #43028 ) ;
#5354=ORIENTED_EDGE ( 'NONE', *, *, #11069, .F. ) ;
#5355=EDGE_CURVE ( 'NONE', #3576, #41125, #40510, .T. ) ;
#5358=ORIENTED_EDGE ( 'NONE', *, *, #14860, .F. ) ;
#5359=EDGE_CURVE ( 'NONE', #2219, #44295, #45374, .T. ) ;
#5360=ORIENTED_EDGE ( 'NONE', *, *, #3125, .F. ) ;
#5361=ORIENTED_EDGE ( 'NONE', *, *, #22534, .F. ) ;
#5362=CARTESIAN_POINT ( 'NONE',  ( -0.5455278134075208785, 3.267716535433071279, 1.692913385826762873 ) ) ;
#5363=DIRECTION ( 'NONE',  ( 1.000000000000000000, -0.000000000000000000, 0.000000000000000000 ) ) ;
#5364=ORIENTED_EDGE ( 'NONE', *, *, #30856, .T. ) ;
#5366=EDGE_LOOP ( 'NONE', ( #35640, #9215, #9161, #29939 ) ) ;
#5368=CARTESIAN_POINT ( 'NONE',  ( 0.5455278134075208785, 3.346456692913386100, -1.889763779527552812 ) ) ;
#5369=B_SPLINE_CURVE_WITH_KNOTS ( 'NONE', 3,
 ( #38557, #42164, #6802, #3181 ),
 .UNSPECIFIED., .F., .F.,
 ( 4, 4 ),
 ( 0.03795604549884937229, 0.03924238266445750911 ),
 .UNSPECIFIED. ) ;
#5371=DIRECTION ( 'NONE',  ( 1.734723475976806848E-16, -0.000000000000000000, 1.000000000000000000 ) ) ;
#5372=DIRECTION ( 'NONE',  ( 1.734723475976806848E-16, 0.000000000000000000, 1.000000000000000000 ) ) ;
#5375=DIRECTION ( 'NONE',  ( -1.000000000000000000, 0.000000000000000000, -0.000000000000000000 ) ) ;
#5376=DIRECTION ( 'NONE',  ( -1.000000000000000000, 0.000000000000000000, 1.734723475976806848E-16 ) ) ;
#5379=CARTESIAN_POINT ( 'NONE',  ( -1.636583440222563635, 3.346456692913386100, -0.1968503937007879123 ) ) ;
#5384=EDGE_CURVE ( 'NONE', #44282, #2677, #33031, .T. ) ;
#5386=ORIENTED_EDGE ( 'NONE', *, *, #49263, .T. ) ;
#5387=CARTESIAN_POINT ( 'NONE',  ( 0.000000000000000000, 0.000000000000000000, 0.000000000000000000 ) ) ;
#5388=EDGE_CURVE ( 'NONE', #48506, #47496, #17520, .T. ) ;
#5389=ORIENTED_EDGE ( 'NONE', *, *, #50451, .T. ) ;
#5390=DIRECTION ( 'NONE',  ( -0.000000000000000000, 1.000000000000000000, -0.000000000000000000 ) ) ;
#5391=ADVANCED_FACE ( 'NONE', ( #48212 ), #12887, .F. ) ;
#5392=CARTESIAN_POINT ( 'NONE',  ( -0.8942052331142547050, 3.346456692913386100, 0.4330708661417290162 ) ) ;
#5393=DIRECTION ( 'NONE',  ( 1.734723475976806848E-16, -0.000000000000000000, 1.000000000000000000 ) ) ;
#5394=LINE ( 'NONE', #17278, #24282 ) ;
#5396=EDGE_LOOP ( 'NONE', ( #3777, #3072, #27859 ) ) ;
#5397=CARTESIAN_POINT ( 'NONE',  ( 0.000000000000000000, 3.267716535433071279, 0.4330708661417290162 ) ) ;
#5399=VERTEX_POINT ( 'NONE', #20880 ) ;
#5401=ORIENTED_EDGE ( 'NONE', *, *, #39602, .T. ) ;
#5402=CARTESIAN_POINT ( 'NONE',  ( -0.07591351300297337346, 3.267716535433071279, 2.633779063002570064E-17 ) ) ;
#5403=FACE_OUTER_BOUND ( 'NONE', #18199, .T. ) ;
#5405=CARTESIAN_POINT ( 'NONE',  ( -1.091055626815042867, 3.267716535433071279, 1.892679809432645129E-16 ) ) ;
#5407=AXIS2_PLACEMENT_3D ( 'NONE', #31730, #16494, #7974 ) ;
#5408=EDGE_CURVE ( 'NONE', #22325, #18373, #19032, .T. ) ;
#5409=ORIENTED_EDGE ( 'NONE', *, *, #6278, .T. ) ;
#5411=VECTOR ( 'NONE', #38708, 39.37007874015748143 ) ;
#5413=CARTESIAN_POINT ( 'NONE',  ( -0.2727639067037602172, 0.000000000000000000, 0.7874015748031456541 ) ) ;
#5414=CARTESIAN_POINT ( 'NONE',  ( -0.8942052331142552601, 3.267716535433071279, -1.456692913385822186 ) ) ;
#5415=FACE_BOUND ( 'NONE', #16739, .T. ) ;
#5416=VERTEX_POINT ( 'NONE', #46629 ) ;
#5417=VECTOR ( 'NONE', #19101, 39.37007874015748143 ) ;
#5418=DIRECTION ( 'NONE',  ( -1.000000000000000000, 0.000000000000000000, 0.000000000000000000 ) ) ;
#5421=ORIENTED_EDGE ( 'NONE', *, *, #26158, .F. ) ;
#5423=VECTOR ( 'NONE', #12187, 39.37007874015748143 ) ;
#5424=DIRECTION ( 'NONE',  ( 1.000000000000000000, 0.000000000000000000, 0.000000000000000000 ) ) ;
#5427=ORIENTED_EDGE ( 'NONE', *, *, #20800, .F. ) ;
#5428=DIRECTION ( 'NONE',  ( 1.000000000000000000, 0.000000000000000000, 0.000000000000000000 ) ) ;
#5431=DIRECTION ( 'NONE',  ( 0.000000000000000000, -1.000000000000000000, 0.000000000000000000 ) ) ;
#5432=EDGE_LOOP ( 'NONE', ( #12568, #43738, #18292, #7640, #49921 ) ) ;
#5434=DIRECTION ( 'NONE',  ( -0.000000000000000000, 1.000000000000000000, -0.000000000000000000 ) ) ;
#5435=CARTESIAN_POINT ( 'NONE',  ( 1.287906020515829919, 3.346456692913386100, -1.456692913385822630 ) ) ;
#5437=DIRECTION ( 'NONE',  ( -0.000000000000000000, 1.000000000000000000, -0.000000000000000000 ) ) ;
#5438=DIRECTION ( 'NONE',  ( -3.469446951953613696E-16, 0.000000000000000000, -1.000000000000000000 ) ) ;
#5439=DIRECTION ( 'NONE',  ( -0.000000000000000000, 1.000000000000000000, -0.000000000000000000 ) ) ;
#5441=CARTESIAN_POINT ( 'NONE',  ( 0.000000000000000000, 3.346456692913386100, 0.000000000000000000 ) ) ;
#5442=EDGE_CURVE ( 'NONE', #42803, #9319, #22913, .T. ) ;
#5443=ORIENTED_EDGE ( 'NONE', *, *, #8590, .T. ) ;
#5444=AXIS2_PLACEMENT_3D ( 'NONE', #38534, #6779, #34158 ) ;
#5448=AXIS2_PLACEMENT_3D ( 'NONE', #17441, #17951, #13317 ) ;
#5449=ORIENTED_EDGE ( 'NONE', *, *, #30336, .F. ) ;
#5451=EDGE_CURVE ( 'NONE', #46412, #45936, #14154, .T. ) ;
#5452=ORIENTED_EDGE ( 'NONE', *, *, #44665, .T. ) ;
#5453=FACE_OUTER_BOUND ( 'NONE', #44923, .T. ) ;
#5455=EDGE_CURVE ( 'NONE', #3016, #39431, #30921, .T. ) ;
#5456=VECTOR ( 'NONE', #25933, 39.37007874015748143 ) ;
#5460=ORIENTED_EDGE ( 'NONE', *, *, #22631, .T. ) ;
#5461=FACE_OUTER_BOUND ( 'NONE', #13168, .T. ) ;
#5462=ORIENTED_EDGE ( 'NONE', *, *, #50380, .T. ) ;
#5464=CARTESIAN_POINT ( 'NONE',  ( -2.142325647309101022, 3.346456692913386100, 0.3149606299212578953 ) ) ;
#5466=ORIENTED_EDGE ( 'NONE', *, *, #45239, .F. ) ;
#5467=VERTEX_POINT ( 'NONE', #18032 ) ;
#5469=CARTESIAN_POINT ( 'NONE',  ( 0.000000000000000000, 3.267716535433071279, 0.000000000000000000 ) ) ;
#5471=ORIENTED_EDGE ( 'NONE', *, *, #7047, .T. ) ;
#5473=CARTESIAN_POINT ( 'NONE',  ( -1.985260859929297794, 3.267716535433071279, 6.887757239314512246E-16 ) ) ;
#5476=ORIENTED_EDGE ( 'NONE', *, *, #24195, .F. ) ;
#5477=LINE ( 'NONE', #36984, #14738 ) ;
#5478=CARTESIAN_POINT ( 'NONE',  ( -0.5455278134075208785, 3.346456692913386100, 0.9448818897637749625 ) ) ;
#5479=ADVANCED_FACE ( 'NONE', ( #2791 ), #30157, .F. ) ;
#5480=CARTESIAN_POINT ( 'NONE',  ( -2.061297163897529483, 3.346456692913386100, 0.4330708661417290162 ) ) ;
#5482=ORIENTED_EDGE ( 'NONE', *, *, #4347, .F. ) ;
#5483=CARTESIAN_POINT ( 'NONE',  ( 1.909347346926324684, 0.000000000000000000, 0.1574803149606280872 ) ) ;
#5484=DIRECTION ( 'NONE',  ( 0.000000000000000000, 0.000000000000000000, -1.000000000000000000 ) ) ;
#5485=VECTOR ( 'NONE', #23379, 39.37007874015748143 ) ;
#5486=VECTOR ( 'NONE', #13826, 39.37007874015748143 ) ;
#5487=CARTESIAN_POINT ( 'NONE',  ( 0.4696143004045484903, 0.000000000000000000, 1.732283464566921172 ) ) ;
#5488=ORIENTED_EDGE ( 'NONE', *, *, #39318, .T. ) ;
#5489=ORIENTED_EDGE ( 'NONE', *, *, #36807, .T. ) ;
#5492=VECTOR ( 'NONE', #30050, 39.37007874015748143 ) ;
#5493=LINE ( 'NONE', #21240, #44537 ) ;
#5494=VECTOR ( 'NONE', #10790, 39.37007874015748143 ) ;
#5495=DIRECTION ( 'NONE',  ( -0.000000000000000000, 1.000000000000000000, -0.000000000000000000 ) ) ;
#5497=ORIENTED_EDGE ( 'NONE', *, *, #27556, .F. ) ;
#5500=DIRECTION ( 'NONE',  ( -0.000000000000000000, 1.000000000000000000, -0.000000000000000000 ) ) ;
#5501=ORIENTED_EDGE ( 'NONE', *, *, #5701, .T. ) ;
#5502=DIRECTION ( 'NONE',  ( 1.000000000000000000, 0.000000000000000000, -3.469446951953613696E-16 ) ) ;
#5503=CARTESIAN_POINT ( 'NONE',  ( -0.07591351300297333182, 3.346456692913386100, 2.362204724409437961 ) ) ;
#5504=LINE ( 'NONE', #1113, #29147 ) ;
#5506=LINE ( 'NONE', #21765, #13707 ) ;
#5507=CARTESIAN_POINT ( 'NONE',  ( 1.363819533518803029, 0.000000000000000000, -1.102362204724405714 ) ) ;
#5509=CARTESIAN_POINT ( 'NONE',  ( -1.712496953225538077, 3.267716535433071279, 5.941417334598193996E-16 ) ) ;
#5510=CARTESIAN_POINT ( 'NONE',  ( 1.287906020515830585, 3.346456692913386100, 1.574803149606291974 ) ) ;
#5512=EDGE_LOOP ( 'NONE', ( #5226, #25154, #10758, #5497 ) ) ;
#5513=FACE_OUTER_BOUND ( 'NONE', #12305, .T. ) ;
#5515=DIRECTION ( 'NONE',  ( 1.000000000000000000, -0.000000000000000000, 0.000000000000000000 ) ) ;
#5516=EDGE_CURVE ( 'NONE', #28782, #4720, #26028, .T. ) ;
#5518=VECTOR ( 'NONE', #20562, 39.37007874015748143 ) ;
#5519=CARTESIAN_POINT ( 'NONE',  ( -0.2727639067037602172, 3.267716535433071279, 1.102362204724404160 ) ) ;
#5523=VERTEX_POINT ( 'NONE', #26779 ) ;
#5524=CARTESIAN_POINT ( 'NONE',  ( 0.7423782071083084855, 3.267716535433071279, -2.034117492951036166 ) ) ;
#5526=ORIENTED_EDGE ( 'NONE', *, *, #22982, .T. ) ;
#5527=LINE ( 'NONE', #21278, #32807 ) ;
#5528=DIRECTION ( 'NONE',  ( 0.000000000000000000, 0.000000000000000000, 1.000000000000000000 ) ) ;
#5529=DIRECTION ( 'NONE',  ( -3.469446951953613696E-16, 0.000000000000000000, -1.000000000000000000 ) ) ;
#5530=LINE ( 'NONE', #33679, #21094 ) ;
#5531=VECTOR ( 'NONE', #18890, 39.37007874015748143 ) ;
#5532=LINE ( 'NONE', #37549, #27912 ) ;
#5534=ORIENTED_EDGE ( 'NONE', *, *, #6836, .T. ) ;
#5536=FACE_OUTER_BOUND ( 'NONE', #42874, .T. ) ;
#5537=ORIENTED_EDGE ( 'NONE', *, *, #24850, .T. ) ;
#5540=DIRECTION ( 'NONE',  ( -0.000000000000000000, 0.000000000000000000, 1.000000000000000000 ) ) ;
#5541=LINE ( 'NONE', #10371, #11636 ) ;
#5542=ORIENTED_EDGE ( 'NONE', *, *, #22942, .F. ) ;
#5543=VERTEX_POINT ( 'NONE', #3289 ) ;
#5544=LINE ( 'NONE', #36791, #36968 ) ;
#5546=ADVANCED_FACE ( 'NONE', ( #34042 ), #34793, .F. ) ;
#5547=LINE ( 'NONE', #40665, #50233 ) ;
#5548=ORIENTED_EDGE ( 'NONE', *, *, #28138, .F. ) ;
#5549=LINE ( 'NONE', #28264, #23198 ) ;
#5550=FACE_BOUND ( 'NONE', #45091, .T. ) ;
#5551=ORIENTED_EDGE ( 'NONE', *, *, #45589, .T. ) ;
#5552=CARTESIAN_POINT ( 'NONE',  ( 1.636583440222563857, 0.000000000000000000, -0.1968503937007886062 ) ) ;
#5553=ORIENTED_EDGE ( 'NONE', *, *, #15762, .F. ) ;
#5555=CARTESIAN_POINT ( 'NONE',  ( 0.2727639067037604947, 3.346456692913386100, 0.1574803149606283648 ) ) ;
#5557=AXIS2_PLACEMENT_3D ( 'NONE', #14501, #26117, #14239 ) ;
#5558=EDGE_CURVE ( 'NONE', #18488, #26431, #19789, .T. ) ;
#5559=VECTOR ( 'NONE', #19967, 39.37007874015748143 ) ;
#5561=FACE_OUTER_BOUND ( 'NONE', #41020, .T. ) ;
#5562=DIRECTION ( 'NONE',  ( -1.000000000000000000, 0.000000000000000000, 0.000000000000000000 ) ) ;
#5563=ORIENTED_EDGE ( 'NONE', *, *, #25909, .F. ) ;
#5564=VECTOR ( 'NONE', #931, 39.37007874015748143 ) ;
#5565=EDGE_CURVE ( 'NONE', #15453, #33477, #15923, .T. ) ;
#5566=DIRECTION ( 'NONE',  ( 1.734723475976806848E-16, 0.000000000000000000, 1.000000000000000000 ) ) ;
#5567=DIRECTION ( 'NONE',  ( 0.000000000000000000, -1.000000000000000000, 0.000000000000000000 ) ) ;
#5569=ADVANCED_FACE ( 'NONE', ( #32201 ), #43536, .F. ) ;
#5570=DIRECTION ( 'NONE',  ( -1.000000000000000000, 0.000000000000000000, -0.000000000000000000 ) ) ;
#5572=DIRECTION ( 'NONE',  ( -1.000000000000000000, 0.000000000000000000, 1.734723475976806848E-16 ) ) ;
#5573=ORIENTED_EDGE ( 'NONE', *, *, #29977, .T. ) ;
#5574=DIRECTION ( 'NONE',  ( -1.000000000000000000, 0.000000000000000000, 0.000000000000000000 ) ) ;
#5575=VECTOR ( 'NONE', #17446, 39.37007874015748143 ) ;
#5576=DIRECTION ( 'NONE',  ( -0.000000000000000000, 1.000000000000000000, -0.000000000000000000 ) ) ;
#5578=ORIENTED_EDGE ( 'NONE', *, *, #44701, .T. ) ;
#5579=CARTESIAN_POINT ( 'NONE',  ( 2.378961647330872786, 3.346456692913386100, -1.161035397307311917E-15 ) ) ;
#5580=CARTESIAN_POINT ( 'NONE',  ( 0.5455278134075217666, 3.346456692913386100, 2.204724409448808764 ) ) ;
#5581=EDGE_LOOP ( 'NONE', ( #49168, #3951, #14563, #20212 ) ) ;
#5582=CARTESIAN_POINT ( 'NONE',  ( -0.2727639067037602172, 3.346456692913386100, 2.047244094488179567 ) ) ;
#5585=CARTESIAN_POINT ( 'NONE',  ( -1.985260859929297794, 3.267716535433071279, 0.1181102362204704270 ) ) ;
#5586=ORIENTED_EDGE ( 'NONE', *, *, #39418, .T. ) ;
#5589=FACE_BOUND ( 'NONE', #5621, .T. ) ;
#5591=FACE_OUTER_BOUND ( 'NONE', #2418, .T. ) ;
#5596=VERTEX_POINT ( 'NONE', #23669 ) ;
#5597=ORIENTED_EDGE ( 'NONE', *, *, #18684, .F. ) ;
#5598=PLANE ( 'NONE',  #47664 ) ;
#5601=CARTESIAN_POINT ( 'NONE',  ( 0.000000000000000000, 3.267716535433071279, -7.512581982576723358E-16 ) ) ;
#5602=VERTEX_POINT ( 'NONE', #39423 ) ;
#5603=CARTESIAN_POINT ( 'NONE',  ( -1.091055626815042645, 0.000000000000000000, 1.889763779527550147 ) ) ;
#5606=DIRECTION ( 'NONE',  ( -1.000000000000000000, 0.000000000000000000, 1.734723475976806848E-16 ) ) ;
#5607=EDGE_CURVE ( 'NONE', #15116, #19912, #39679, .T. ) ;
#5608=VECTOR ( 'NONE', #10818, 39.37007874015748143 ) ;
#5609=FACE_OUTER_BOUND ( 'NONE', #18671, .T. ) ;
#5612=ORIENTED_EDGE ( 'NONE', *, *, #44908, .T. ) ;
#5614=AXIS2_PLACEMENT_3D ( 'NONE', #14017, #45481, #37777 ) ;
#5616=EDGE_CURVE ( 'NONE', #18320, #7706, #50726, .T. ) ;
#5617=ORIENTED_EDGE ( 'NONE', *, *, #4353, .F. ) ;
#5618=ORIENTED_EDGE ( 'NONE', *, *, #26359, .T. ) ;
#5619=DIRECTION ( 'NONE',  ( -3.469446951953613696E-16, 0.000000000000000000, -1.000000000000000000 ) ) ;
#5620=EDGE_CURVE ( 'NONE', #22725, #35907, #47640, .T. ) ;
#5621=EDGE_LOOP ( 'NONE', ( #11871, #35566, #49419, #4006 ) ) ;
#5622=CARTESIAN_POINT ( 'NONE',  ( 0.2727639067037607168, 3.267716535433071279, -4.731699523581612823E-17 ) ) ;
#5623=ORIENTED_EDGE ( 'NONE', *, *, #32381, .F. ) ;
#5624=CARTESIAN_POINT ( 'NONE',  ( -0.2727639067037607723, 3.346456692913386100, 2.362204724409437961 ) ) ;
#5625=VECTOR ( 'NONE', #19664, 39.37007874015748143 ) ;
#5627=ORIENTED_EDGE ( 'NONE', *, *, #3867, .T. ) ;
#5628=CARTESIAN_POINT ( 'NONE',  ( 0.000000000000000000, 3.267716535433071279, 0.7874015748031456541 ) ) ;
#5630=ORIENTED_EDGE ( 'NONE', *, *, #556, .T. ) ;
#5631=CARTESIAN_POINT ( 'NONE',  ( -0.5455278134075214336, 3.346456692913386100, 2.007874015748021268 ) ) ;
#5632=DIRECTION ( 'NONE',  ( -3.469446951953613696E-16, 0.000000000000000000, -1.000000000000000000 ) ) ;
#5633=AXIS2_PLACEMENT_3D ( 'NONE', #31452, #47148, #7953 ) ;
#5634=EDGE_CURVE ( 'NONE', #26534, #660, #43281, .T. ) ;
#5636=CARTESIAN_POINT ( 'NONE',  ( 0.7423782071083087075, 3.346456692913386100, -6.146657985744592735E-16 ) ) ;
#5638=VECTOR ( 'NONE', #20379, 39.37007874015748143 ) ;
#5639=EDGE_CURVE ( 'NONE', #19400, #26179, #35047, .T. ) ;
#5640=CARTESIAN_POINT ( 'NONE',  ( 0.000000000000000000, 3.346456692913386100, 0.000000000000000000 ) ) ;
#5641=ORIENTED_EDGE ( 'NONE', *, *, #39675, .T. ) ;
#5642=DIRECTION ( 'NONE',  ( -3.469446951953613696E-16, 0.000000000000000000, -1.000000000000000000 ) ) ;
#5643=CARTESIAN_POINT ( 'NONE',  ( 1.015142113812069979, 3.346456692913386100, 1.732283464566921172 ) ) ;
#5646=ORIENTED_EDGE ( 'NONE', *, *, #23323, .T. ) ;
#5647=CARTESIAN_POINT ( 'NONE',  ( 1.687984952120843207, 3.346456692913386100, -1.259842519685035800 ) ) ;
#5648=EDGE_CURVE ( 'NONE', #30555, #2803, #8444, .T. ) ;
#5649=EDGE_CURVE ( 'NONE', #43058, #23763, #11545, .T. ) ;
#5651=ORIENTED_EDGE ( 'NONE', *, *, #914, .F. ) ;
#5652=LINE ( 'NONE', #9521, #10499 ) ;
#5654=LINE ( 'NONE', #48214, #29508 ) ;
#5655=PLANE ( 'NONE',  #41610 ) ;
#5656=DIRECTION ( 'NONE',  ( 0.000000000000000000, 0.000000000000000000, 1.000000000000000000 ) ) ;
#5657=ORIENTED_EDGE ( 'NONE', *, *, #15972, .F. ) ;
#5659=FACE_BOUND ( 'NONE', #821, .T. ) ;
#5661=VERTEX_POINT ( 'NONE', #31421 ) ;
#5663=VERTEX_POINT ( 'NONE', #47123 ) ;
#5664=CARTESIAN_POINT ( 'NONE',  ( 1.363819533518803029, 0.000000000000000000, -1.929133858267710666 ) ) ;
#5665=DIRECTION ( 'NONE',  ( 0.000000000000000000, -1.000000000000000000, 0.000000000000000000 ) ) ;
#5666=AXIS2_PLACEMENT_3D ( 'NONE', #16907, #44756, #1151 ) ;
#5667=CARTESIAN_POINT ( 'NONE',  ( -2.106299212598425008, 3.267716535433071279, -6.146657985744592735E-16 ) ) ;
#5669=VERTEX_POINT ( 'NONE', #7926 ) ;
#5670=VERTEX_POINT ( 'NONE', #12316 ) ;
#5671=DIRECTION ( 'NONE',  ( -0.000000000000000000, 1.000000000000000000, -0.000000000000000000 ) ) ;
#5673=FACE_BOUND ( 'NONE', #43440, .T. ) ;
#5674=ORIENTED_EDGE ( 'NONE', *, *, #27184, .F. ) ;
#5678=DIRECTION ( 'NONE',  ( -3.469446951953613696E-16, 0.000000000000000000, -1.000000000000000000 ) ) ;
#5679=EDGE_CURVE ( 'NONE', #12398, #21285, #24191, .T. ) ;
#5680=ORIENTED_EDGE ( 'NONE', *, *, #50176, .F. ) ;
#5681=EDGE_LOOP ( 'NONE', ( #278, #27334, #44209, #46752 ) ) ;
#5684=EDGE_CURVE ( 'NONE', #23466, #8911, #36069, .T. ) ;
#5685=EDGE_CURVE ( 'NONE', #122, #48282, #3439, .T. ) ;
#5689=VECTOR ( 'NONE', #5515, 39.37007874015748143 ) ;
#5691=ORIENTED_EDGE ( 'NONE', *, *, #39666, .F. ) ;
#5694=CARTESIAN_POINT ( 'NONE',  ( 0.000000000000000000, 3.267716535433071279, -1.299212598425193210 ) ) ;
#5696=ORIENTED_EDGE ( 'NONE', *, *, #4983, .T. ) ;
#5698=CARTESIAN_POINT ( 'NONE',  ( -2.182111253630085290, 0.000000000000000000, 0.6299212598425164567 ) ) ;
#5700=DIRECTION ( 'NONE',  ( -0.000000000000000000, 0.000000000000000000, 1.000000000000000000 ) ) ;
#5701=EDGE_CURVE ( 'NONE', #51000, #29752, #50616, .T. ) ;
#5702=LINE ( 'NONE', #21448, #9504 ) ;
#5703=EDGE_CURVE ( 'NONE', #35551, #13057, #29735, .T. ) ;
#5704=DIRECTION ( 'NONE',  ( 1.000000000000000000, -0.000000000000000000, 0.000000000000000000 ) ) ;
#5705=VECTOR ( 'NONE', #45193, 39.37007874015748143 ) ;
#5706=DIRECTION ( 'NONE',  ( -1.000000000000000000, 0.000000000000000000, 1.734723475976806848E-16 ) ) ;
#5707=ORIENTED_EDGE ( 'NONE', *, *, #46799, .T. ) ;
#5708=CARTESIAN_POINT ( 'NONE',  ( -2.182111253630085290, 0.000000000000000000, -0.3149606299212589500 ) ) ;
#5710=EDGE_CURVE ( 'NONE', #15688, #17158, #2934, .T. ) ;
#5712=EDGE_LOOP ( 'NONE', ( #6613, #41284, #13089, #11024 ) ) ;
#5714=FACE_OUTER_BOUND ( 'NONE', #3774, .T. ) ;
#5715=FACE_OUTER_BOUND ( 'NONE', #1698, .T. ) ;
#5717=AXIS2_PLACEMENT_3D ( 'NONE', #28753, #29265, #14032 ) ;
#5719=DIRECTION ( 'NONE',  ( 1.000000000000000000, 0.000000000000000000, 0.000000000000000000 ) ) ;
#5720=AXIS2_PLACEMENT_3D ( 'NONE', #10160, #25151, #40899 ) ;
#5722=CARTESIAN_POINT ( 'NONE',  ( 0.8182917201112819283, 0.000000000000000000, 0.4724409448818868706 ) ) ;
#5723=CARTESIAN_POINT ( 'NONE',  ( -1.439733046521776583, 0.000000000000000000, -0.3149606299212592275 ) ) ;
#5724=ORIENTED_EDGE ( 'NONE', *, *, #12990, .T. ) ;
#5725=EDGE_LOOP ( 'NONE', ( #47606, #9789, #8859, #23830 ) ) ;
#5726=VERTEX_POINT ( 'NONE', #18934 ) ;
#5727=CARTESIAN_POINT ( 'NONE',  ( -0.07591351300297340121, 3.346456692913386100, -1.929133858267710000 ) ) ;
#5728=ORIENTED_EDGE ( 'NONE', *, *, #36362, .T. ) ;
#5729=ORIENTED_EDGE ( 'NONE', *, *, #21994, .F. ) ;
#5730=DIRECTION ( 'NONE',  ( 1.000000000000000000, -0.000000000000000000, 0.000000000000000000 ) ) ;
#5731=CARTESIAN_POINT ( 'NONE',  ( -1.166969139818015977, 3.346456692913386100, 2.047244094488179567 ) ) ;
#5732=CARTESIAN_POINT ( 'NONE',  ( 0.8182917201112821504, 3.267716535433071279, -1.419509857074483539E-16 ) ) ;
#5733=ORIENTED_EDGE ( 'NONE', *, *, #43765, .F. ) ;
#5734=DIRECTION ( 'NONE',  ( 0.000000000000000000, 0.000000000000000000, 1.000000000000000000 ) ) ;
#5736=AXIS2_PLACEMENT_3D ( 'NONE', #45136, #21418, #5916 ) ;
#5737=FACE_OUTER_BOUND ( 'NONE', #38102, .T. ) ;
#5740=LINE ( 'NONE', #45715, #17804 ) ;
#5741=EDGE_CURVE ( 'NONE', #3513, #50909, #35188, .T. ) ;
#5743=DIRECTION ( 'NONE',  ( -3.469446951953613696E-16, 0.000000000000000000, -1.000000000000000000 ) ) ;
#5744=EDGE_LOOP ( 'NONE', ( #9518, #12886, #4336, #50309 ) ) ;
#5747=AXIS2_PLACEMENT_3D ( 'NONE', #44407, #24799, #1300 ) ;
#5754=VECTOR ( 'NONE', #24384, 39.37007874015748143 ) ;
#5755=VERTEX_POINT ( 'NONE', #30556 ) ;
#5756=CARTESIAN_POINT ( 'NONE',  ( -0.2727639067037610499, 3.267716535433071279, -2.047244094488181343 ) ) ;
#5761=CARTESIAN_POINT ( 'NONE',  ( -2.454875160333845674, 3.346456692913386100, -0.1574803149606298636 ) ) ;
#5762=DIRECTION ( 'NONE',  ( -3.469446951953613696E-16, 0.000000000000000000, -1.000000000000000000 ) ) ;
#5763=ORIENTED_EDGE ( 'NONE', *, *, #22322, .F. ) ;
#5765=FACE_OUTER_BOUND ( 'NONE', #15794, .T. ) ;
#5766=ADVANCED_FACE ( 'NONE', ( #7318 ), #7566, .F. ) ;
#5767=FACE_OUTER_BOUND ( 'NONE', #50441, .T. ) ;
#5768=ORIENTED_EDGE ( 'NONE', *, *, #18494, .T. ) ;
#5770=DIRECTION ( 'NONE',  ( -1.000000000000000000, 0.000000000000000000, 1.734723475976806848E-16 ) ) ;
#5771=DIRECTION ( 'NONE',  ( -0.000000000000000000, 1.000000000000000000, -0.000000000000000000 ) ) ;
#5774=LINE ( 'NONE', #49096, #26710 ) ;
#5775=DIRECTION ( 'NONE',  ( 0.000000000000000000, 0.000000000000000000, -1.000000000000000000 ) ) ;
#5776=ORIENTED_EDGE ( 'NONE', *, *, #46908, .F. ) ;
#5779=VERTEX_POINT ( 'NONE', #31315 ) ;
#5780=DIRECTION ( 'NONE',  ( 1.000000000000000000, 0.000000000000000000, 0.000000000000000000 ) ) ;
#5781=ADVANCED_FACE ( 'NONE', ( #47010 ), #15566, .F. ) ;
#5782=VECTOR ( 'NONE', #26819, 39.37007874015748143 ) ;
#5783=CARTESIAN_POINT ( 'NONE',  ( 0.5455278134075211005, 3.346456692913386100, -0.5118110236220467790 ) ) ;
#5784=DIRECTION ( 'NONE',  ( -1.000000000000000000, 0.000000000000000000, -0.000000000000000000 ) ) ;
#5786=VECTOR ( 'NONE', #29746, 39.37007874015748143 ) ;
#5789=EDGE_LOOP ( 'NONE', ( #6881, #12510, #39083, #29734 ) ) ;
#5790=CARTESIAN_POINT ( 'NONE',  ( 0.5455278134075211005, 3.267716535433071279, -0.5118110236220467790 ) ) ;
#5791=DIRECTION ( 'NONE',  ( -1.000000000000000000, 0.000000000000000000, -0.000000000000000000 ) ) ;
#5793=CARTESIAN_POINT ( 'NONE',  ( 0.000000000000000000, 3.346456692913386100, 0.000000000000000000 ) ) ;
#5794=CARTESIAN_POINT ( 'NONE',  ( -1.712496953225537633, 3.346456692913386100, 1.226315847645293999 ) ) ;
#5795=LINE ( 'NONE', #49375, #50791 ) ;
#5796=ORIENTED_EDGE ( 'NONE', *, *, #11004, .F. ) ;
#5797=ORIENTED_EDGE ( 'NONE', *, *, #4678, .F. ) ;
#5799=CARTESIAN_POINT ( 'NONE',  ( 0.4696143004045484348, 3.267716535433071279, 1.535433070866133898 ) ) ;
#5800=LINE ( 'NONE', #21548, #14841 ) ;
#5802=LENGTH_MEASURE_WITH_UNIT ( LENGTH_MEASURE( 0.02539999999999999897 ), #14821 );
#5803=FACE_BOUND ( 'NONE', #26604, .T. ) ;
#5805=ADVANCED_FACE ( 'NONE', ( #23554 ), #39309, .F. ) ;
#5806=CARTESIAN_POINT ( 'NONE',  ( 0.8182917201112824834, 3.267716535433071279, 1.732283464566921172 ) ) ;
#5807=ORIENTED_EDGE ( 'NONE', *, *, #21141, .T. ) ;
#5808=ORIENTED_EDGE ( 'NONE', *, *, #37373, .F. ) ;
#5811=EDGE_CURVE ( 'NONE', #44964, #12754, #35442, .T. ) ;
#5813=VERTEX_POINT ( 'NONE', #10931 ) ;
#5814=DIRECTION ( 'NONE',  ( 1.734723475976806848E-16, 0.000000000000000000, 1.000000000000000000 ) ) ;
#5815=EDGE_CURVE ( 'NONE', #22677, #17201, #38811, .T. ) ;
#5816=LINE ( 'NONE', #41196, #22191 ) ;
#5817=VERTEX_POINT ( 'NONE', #32602 ) ;
#5818=LINE ( 'NONE', #9697, #31059 ) ;
#5819=LINE ( 'NONE', #21572, #50595 ) ;
#5820=VECTOR ( 'NONE', #49902, 39.37007874015748143 ) ;
#5821=VECTOR ( 'NONE', #25519, 39.37007874015748143 ) ;
#5823=DIRECTION ( 'NONE',  ( 0.000000000000000000, 0.000000000000000000, -1.000000000000000000 ) ) ;
#5825=CARTESIAN_POINT ( 'NONE',  ( 0.000000000000000000, 3.346456692913386100, 0.000000000000000000 ) ) ;
#5828=EDGE_CURVE ( 'NONE', #13249, #13554, #16588, .T. ) ;
#5829=VECTOR ( 'NONE', #43039, 39.37007874015748143 ) ;
#5830=CARTESIAN_POINT ( 'NONE',  ( 0.4696143004045479352, 3.346456692913386100, -1.102362204724405714 ) ) ;
#5831=VERTEX_POINT ( 'NONE', #12972 ) ;
#5832=CARTESIAN_POINT ( 'NONE',  ( 1.560669927219590525, 0.000000000000000000, -0.6692913385826764205 ) ) ;
#5833=LINE ( 'NONE', #45552, #19540 ) ;
#5837=LINE ( 'NONE', #37088, #1955 ) ;
#5841=ORIENTED_EDGE ( 'NONE', *, *, #49708, .T. ) ;
#5842=FACE_BOUND ( 'NONE', #11615, .T. ) ;
#5843=EDGE_CURVE ( 'NONE', #18933, #11499, #35693, .T. ) ;
#5845=LINE ( 'NONE', #41726, #404 ) ;
#5847=ORIENTED_EDGE ( 'NONE', *, *, #38387, .F. ) ;
#5849=DIRECTION ( 'NONE',  ( -0.000000000000000000, 0.000000000000000000, 1.000000000000000000 ) ) ;
#5850=VERTEX_POINT ( 'NONE', #5212 ) ;
#5852=DIRECTION ( 'NONE',  ( -3.469446951953613696E-16, 0.000000000000000000, -1.000000000000000000 ) ) ;
#5853=ORIENTED_EDGE ( 'NONE', *, *, #45204, .T. ) ;
#5854=EDGE_CURVE ( 'NONE', #33436, #28782, #27936, .T. ) ;
#5857=VECTOR ( 'NONE', #23691, 39.37007874015748143 ) ;
#5858=ORIENTED_EDGE ( 'NONE', *, *, #30748, .F. ) ;
#5859=DIRECTION ( 'NONE',  ( 1.000000000000000000, 0.000000000000000000, 0.000000000000000000 ) ) ;
#5860=CARTESIAN_POINT ( 'NONE',  ( -1.363819533518803029, 3.346456692913386100, 0.4724409448818871482 ) ) ;
#5861=ORIENTED_EDGE ( 'NONE', *, *, #3603, .T. ) ;
#5862=PLANE ( 'NONE',  #13352 ) ;
#5866=ADVANCED_FACE ( 'NONE', ( #48543 ), #28442, .F. ) ;
#5867=AXIS2_PLACEMENT_3D ( 'NONE', #26215, #19215, #37853 ) ;
#5868=ORIENTED_EDGE ( 'NONE', *, *, #33209, .F. ) ;
#5869=ORIENTED_EDGE ( 'NONE', *, *, #19464, .F. ) ;
#5870=DIRECTION ( 'NONE',  ( -1.000000000000000000, 0.000000000000000000, -0.000000000000000000 ) ) ;
#5871=EDGE_CURVE ( 'NONE', #26807, #44408, #43676, .T. ) ;
#5873=CARTESIAN_POINT ( 'NONE',  ( 1.560669927219590303, 3.346456692913386100, -1.501022570047217508 ) ) ;
#5874=LINE ( 'NONE', #25245, #2985 ) ;
#5876=ORIENTED_EDGE ( 'NONE', *, *, #11732, .T. ) ;
#5879=ORIENTED_EDGE ( 'NONE', *, *, #25978, .T. ) ;
#5880=CARTESIAN_POINT ( 'NONE',  ( -0.6214413264104939882, 3.267716535433071279, 2.156057715732899300E-16 ) ) ;
#5883=DIRECTION ( 'NONE',  ( 0.000000000000000000, 0.000000000000000000, -1.000000000000000000 ) ) ;
#5886=PLANE ( 'NONE',  #22385 ) ;
#5887=DIRECTION ( 'NONE',  ( -0.000000000000000000, 1.000000000000000000, -0.000000000000000000 ) ) ;
#5892=VECTOR ( 'NONE', #25661, 39.37007874015748143 ) ;
#5893=VERTEX_POINT ( 'NONE', #1083 ) ;
#5894=LINE ( 'NONE', #45116, #1190 ) ;
#5896=ORIENTED_EDGE ( 'NONE', *, *, #14795, .F. ) ;
#5899=CARTESIAN_POINT ( 'NONE',  ( -0.2727639067037602172, 0.000000000000000000, 0.7874015748031456541 ) ) ;
#5900=PLANE ( 'NONE',  #4783 ) ;
#5901=EDGE_CURVE ( 'NONE', #14542, #34665, #28702, .T. ) ;
#5902=CARTESIAN_POINT ( 'NONE',  ( -1.091055626815042201, 3.267716535433071279, 0.7480314960629874665 ) ) ;
#5903=CARTESIAN_POINT ( 'NONE',  ( 0.1968503937007873850, 3.346456692913386100, -0.1968503937007874405 ) ) ;
#5904=VERTEX_POINT ( 'NONE', #39816 ) ;
#5905=ADVANCED_FACE ( 'NONE', ( #44450 ), #318, .F. ) ;
#5906=PLANE ( 'NONE',  #13346 ) ;
#5908=FACE_OUTER_BOUND ( 'NONE', #13539, .T. ) ;
#5911=LINE ( 'NONE', #23806, #8735 ) ;
#5912=ORIENTED_EDGE ( 'NONE', *, *, #8437, .T. ) ;
#5915=EDGE_CURVE ( 'NONE', #37376, #45969, #20451, .T. ) ;
#5916=DIRECTION ( 'NONE',  ( 1.734723475976806848E-16, 0.000000000000000000, 1.000000000000000000 ) ) ;
#5919=CARTESIAN_POINT ( 'NONE',  ( 1.909347346926324462, 3.346456692913386100, -0.7874015748031473194 ) ) ;
#5920=FACE_BOUND ( 'NONE', #20077, .T. ) ;
#5922=EDGE_CURVE ( 'NONE', #13777, #29680, #9088, .T. ) ;
#5923=CIRCLE ( 'NONE', #43862, 2.165354330708661568 ) ;
#5925=CARTESIAN_POINT ( 'NONE',  ( -1.195183497228115035E-16, 0.000000000000000000, 0.6299212598425161236 ) ) ;
#5927=ORIENTED_EDGE ( 'NONE', *, *, #29010, .F. ) ;
#5929=ADVANCED_FACE ( 'NONE', ( #4195 ), #43931, .F. ) ;
#5932=DIRECTION ( 'NONE',  ( -0.000000000000000000, 1.000000000000000000, -0.000000000000000000 ) ) ;
#5933=ORIENTED_EDGE ( 'NONE', *, *, #724, .T. ) ;
#5937=EDGE_LOOP ( 'NONE', ( #37341, #37558, #43902, #25835 ) ) ;
#5939=VECTOR ( 'NONE', #39349, 39.37007874015748143 ) ;
#5941=DIRECTION ( 'NONE',  ( -3.469446951953613696E-16, 0.000000000000000000, -1.000000000000000000 ) ) ;
#5942=PLANE ( 'NONE',  #42045 ) ;
#5943=EDGE_LOOP ( 'NONE', ( #27980, #17491, #3263, #43050 ) ) ;
#5944=ORIENTED_EDGE ( 'NONE', *, *, #17774, .T. ) ;
#5945=CARTESIAN_POINT ( 'NONE',  ( -1.091055626815042645, 0.000000000000000000, -1.259842519685034690 ) ) ;
#5947=FACE_OUTER_BOUND ( 'NONE', #26998, .T. ) ;
#5948=CARTESIAN_POINT ( 'NONE',  ( -0.6214413264104939882, 3.267716535433071279, 2.156057715732899300E-16 ) ) ;
#5949=CARTESIAN_POINT ( 'NONE',  ( 0.8182917201112819283, 0.000000000000000000, 0.9055118110236164419 ) ) ;
#5950=DIRECTION ( 'NONE',  ( -1.000000000000000000, -0.000000000000000000, -0.000000000000000000 ) ) ;
#5951=FACE_OUTER_BOUND ( 'NONE', #7357, .T. ) ;
#5952=VERTEX_POINT ( 'NONE', #17857 ) ;
#5954=CARTESIAN_POINT ( 'NONE',  ( -0.5455278134075208785, 3.346456692913386100, 1.259842519685033357 ) ) ;
#5955=ORIENTED_EDGE ( 'NONE', *, *, #6740, .T. ) ;
#5956=VERTEX_POINT ( 'NONE', #25597 ) ;
#5957=VECTOR ( 'NONE', #11076, 39.37007874015748143 ) ;
#5958=DIRECTION ( 'NONE',  ( -3.469446951953613696E-16, 0.000000000000000000, -1.000000000000000000 ) ) ;
#5959=EDGE_CURVE ( 'NONE', #39288, #19595, #9345, .T. ) ;
#5960=ORIENTED_EDGE ( 'NONE', *, *, #8419, .F. ) ;
#5962=AXIS2_PLACEMENT_3D ( 'NONE', #15128, #14878, #23630 ) ;
#5963=ORIENTED_EDGE ( 'NONE', *, *, #5741, .F. ) ;
#5964=LINE ( 'NONE', #24824, #22119 ) ;
#5966=EDGE_LOOP ( 'NONE', ( #35133, #49690, #35452, #22345 ) ) ;
#5967=EDGE_CURVE ( 'NONE', #26524, #8104, #5977, .T. ) ;
#5968=VECTOR ( 'NONE', #47121, 39.37007874015748143 ) ;
#5969=CARTESIAN_POINT ( 'NONE',  ( 1.536664496436137830E-16, 3.267716535433071279, -2.665687976667846366E-32 ) ) ;
#5972=VERTEX_POINT ( 'NONE', #2367 ) ;
#5973=ORIENTED_EDGE ( 'NONE', *, *, #34789, .F. ) ;
#5975=ORIENTED_EDGE ( 'NONE', *, *, #17589, .F. ) ;
#5976=EDGE_LOOP ( 'NONE', ( #28466, #48268, #15483, #21224 ) ) ;
#5977=LINE ( 'NONE', #26110, #35554 ) ;
#5979=DIRECTION ( 'NONE',  ( -0.000000000000000000, 0.000000000000000000, 1.000000000000000000 ) ) ;
#5980=EDGE_CURVE ( 'NONE', #26348, #26976, #44950, .T. ) ;
#5982=EDGE_CURVE ( 'NONE', #39976, #17373, #2109, .T. ) ;
#5983=CARTESIAN_POINT ( 'NONE',  ( -0.3486774197067339376, 3.267716535433071279, -0.3149606299212593941 ) ) ;
#5986=ORIENTED_EDGE ( 'NONE', *, *, #28757, .F. ) ;
#5987=EDGE_CURVE ( 'NONE', #36398, #38696, #33620, .T. ) ;
#5989=PLANE ( 'NONE',  #1325 ) ;
#5992=ORIENTED_EDGE ( 'NONE', *, *, #17751, .F. ) ;
#5994=EDGE_CURVE ( 'NONE', #30196, #31565, #21989, .T. ) ;
#5995=LINE ( 'NONE', #33387, #28880 ) ;
#5996=VECTOR ( 'NONE', #723, 39.37007874015748143 ) ;
#5997=LINE ( 'NONE', #12991, #22009 ) ;
#5999=EDGE_LOOP ( 'NONE', ( #41647, #41341, #49136, #46808 ) ) ;
#6000=ORIENTED_EDGE ( 'NONE', *, *, #30748, .T. ) ;
#6001=VECTOR ( 'NONE', #40083, 39.37007874015748143 ) ;
#6003=VECTOR ( 'NONE', #31844, 39.37007874015748143 ) ;
#6008=VECTOR ( 'NONE', #40894, 39.37007874015748143 ) ;
#6009=CARTESIAN_POINT ( 'NONE',  ( 0.000000000000000000, 3.267716535433071279, -1.929133858267710000 ) ) ;
#6010=DIRECTION ( 'NONE',  ( -0.000000000000000000, 1.000000000000000000, -0.000000000000000000 ) ) ;
#6011=CARTESIAN_POINT ( 'NONE',  ( 1.909347346926324684, 3.346456692913386100, 1.021348170950612033 ) ) ;
#6013=EDGE_LOOP ( 'NONE', ( #41931, #34504, #31022, #6925 ) ) ;
#6015=LINE ( 'NONE', #21770, #12002 ) ;
#6019=LINE ( 'NONE', #44737, #34384 ) ;
#6020=CARTESIAN_POINT ( 'NONE',  ( 0.000000000000000000, 0.000000000000000000, 0.000000000000000000 ) ) ;
#6021=VERTEX_POINT ( 'NONE', #49807 ) ;
#6022=DIRECTION ( 'NONE',  ( 1.000000000000000000, -0.000000000000000000, 0.000000000000000000 ) ) ;
#6023=ADVANCED_FACE ( 'NONE', ( #17351 ), #6498, .F. ) ;
#6024=EDGE_CURVE ( 'NONE', #50505, #19595, #24831, .T. ) ;
#6025=ORIENTED_EDGE ( 'NONE', *, *, #49042, .T. ) ;
#6028=EDGE_LOOP ( 'NONE', ( #14691, #38744, #24735, #6724 ) ) ;
#6031=DIRECTION ( 'NONE',  ( 1.000000000000000000, 0.000000000000000000, -3.469446951953613696E-16 ) ) ;
#6032=DIRECTION ( 'NONE',  ( 1.000000000000000000, 0.000000000000000000, -3.469446951953613696E-16 ) ) ;
#6036=ORIENTED_EDGE ( 'NONE', *, *, #10565, .F. ) ;
#6037=ORIENTED_EDGE ( 'NONE', *, *, #24860, .F. ) ;
#6038=LINE ( 'NONE', #41666, #20739 ) ;
#6039=FACE_OUTER_BOUND ( 'NONE', #26490, .T. ) ;
#6041=VECTOR ( 'NONE', #34480, 39.37007874015748143 ) ;
#6043=FACE_OUTER_BOUND ( 'NONE', #36783, .T. ) ;
#6045=VECTOR ( 'NONE', #33890, 39.37007874015748143 ) ;
#6046=VECTOR ( 'NONE', #2334, 39.37007874015748143 ) ;
#6047=EDGE_LOOP ( 'NONE', ( #45707, #36004, #37839, #38313 ) ) ;
#6049=ADVANCED_FACE ( 'NONE', ( #49554 ), #29983, .F. ) ;
#6050=FACE_OUTER_BOUND ( 'NONE', #9018, .T. ) ;
#6051=CARTESIAN_POINT ( 'NONE',  ( 0.5455278134075211005, 0.000000000000000000, -0.1968503937007880511 ) ) ;
#6053=EDGE_LOOP ( 'NONE', ( #15231, #37592, #23070, #1158 ) ) ;
#6054=LINE ( 'NONE', #41428, #46293 ) ;
#6055=DIRECTION ( 'NONE',  ( -0.000000000000000000, 1.000000000000000000, -0.000000000000000000 ) ) ;
#6056=VECTOR ( 'NONE', #31100, 39.37007874015748143 ) ;
#6057=ORIENTED_EDGE ( 'NONE', *, *, #10565, .T. ) ;
#6058=EDGE_CURVE ( 'NONE', #12607, #46834, #1600, .T. ) ;
#6059=LINE ( 'NONE', #45275, #31502 ) ;
#6060=ORIENTED_EDGE ( 'NONE', *, *, #18524, .F. ) ;
#6062=PLANE ( 'NONE',  #45184 ) ;
#6066=CARTESIAN_POINT ( 'NONE',  ( 1.909347346926324462, 3.267716535433071279, -3.312189666507127188E-16 ) ) ;
#6067=ORIENTED_EDGE ( 'NONE', *, *, #9777, .T. ) ;
#6068=EDGE_CURVE ( 'NONE', #24438, #37496, #48795, .T. ) ;
#6069=DIRECTION ( 'NONE',  ( -3.469446951953613696E-16, 0.000000000000000000, -1.000000000000000000 ) ) ;
#6072=VECTOR ( 'NONE', #1606, 39.37007874015748143 ) ;
#6074=CARTESIAN_POINT ( 'NONE',  ( -2.082617625631827174, 3.346456692913386100, -0.3149606299212589500 ) ) ;
#6075=VERTEX_POINT ( 'NONE', #25095 ) ;
#6076=FACE_OUTER_BOUND ( 'NONE', #42864, .T. ) ;
#6077=AXIS2_PLACEMENT_3D ( 'NONE', #23471, #11603, #4369 ) ;
#6079=LINE ( 'NONE', #33473, #37222 ) ;
#6080=VECTOR ( 'NONE', #32152, 39.37007874015748143 ) ;
#6081=VECTOR ( 'NONE', #16296, 39.37007874015748143 ) ;
#6082=ORIENTED_EDGE ( 'NONE', *, *, #1111, .F. ) ;
#6083=DIRECTION ( 'NONE',  ( -3.469446951953613696E-16, 0.000000000000000000, -1.000000000000000000 ) ) ;
#6084=LINE ( 'NONE', #13331, #25304 ) ;
#6086=DIRECTION ( 'NONE',  ( 1.000000000000000000, 0.000000000000000000, 0.000000000000000000 ) ) ;
#6087=CARTESIAN_POINT ( 'NONE',  ( -0.2727639067037602727, 0.000000000000000000, 1.220472440944875281 ) ) ;
#6091=EDGE_CURVE ( 'NONE', #37886, #50549, #40846, .T. ) ;
#6092=ORIENTED_EDGE ( 'NONE', *, *, #34640, .T. ) ;
#6093=PLANE ( 'NONE',  #46904 ) ;
#6094=ORIENTED_EDGE ( 'NONE', *, *, #21292, .F. ) ;
#6095=FACE_BOUND ( 'NONE', #14236, .T. ) ;
#6096=EDGE_CURVE ( 'NONE', #2778, #1395, #36979, .T. ) ;
#6098=PLANE ( 'NONE',  #1251 ) ;
#6099=CARTESIAN_POINT ( 'NONE',  ( -0.5455278134075214336, 3.267716535433071279, -1.771653543307081025 ) ) ;
#6100=EDGE_CURVE ( 'NONE', #39431, #16156, #12334, .T. ) ;
#6103=VERTEX_POINT ( 'NONE', #6997 ) ;
#6104=CARTESIAN_POINT ( 'NONE',  ( -0.3486774197067340486, 0.000000000000000000, -0.5118110236220467790 ) ) ;
#6105=ORIENTED_EDGE ( 'NONE', *, *, #24701, .T. ) ;
#6107=ORIENTED_EDGE ( 'NONE', *, *, #521, .F. ) ;
#6108=PLANE ( 'NONE',  #12450 ) ;
#6109=EDGE_CURVE ( 'NONE', #4531, #7644, #35574, .T. ) ;
#6110=VERTEX_POINT ( 'NONE', #20327 ) ;
#6113=VECTOR ( 'NONE', #41053, 39.37007874015748143 ) ;
#6114=DIRECTION ( 'NONE',  ( -0.000000000000000000, 1.000000000000000000, -0.000000000000000000 ) ) ;
#6118=EDGE_CURVE ( 'NONE', #43312, #1319, #11813, .T. ) ;
#6122=ORIENTED_EDGE ( 'NONE', *, *, #50686, .F. ) ;
#6127=ORIENTED_EDGE ( 'NONE', *, *, #45646, .T. ) ;
#6129=VECTOR ( 'NONE', #11599, 39.37007874015748143 ) ;
#6131=CARTESIAN_POINT ( 'NONE',  ( 0.000000000000000000, 3.267716535433071279, 1.889763779527550369 ) ) ;
#6132=EDGE_CURVE ( 'NONE', #46532, #33705, #26332, .T. ) ;
#6133=DIRECTION ( 'NONE',  ( 1.734723475976806848E-16, -0.000000000000000000, 1.000000000000000000 ) ) ;
#6134=CARTESIAN_POINT ( 'NONE',  ( -0.8942052331142547050, 3.346456692913386100, 0.9448818897637749625 ) ) ;
#6135=ORIENTED_EDGE ( 'NONE', *, *, #44796, .F. ) ;
#6136=CARTESIAN_POINT ( 'NONE',  ( 0.000000000000000000, 3.267716535433071279, 0.000000000000000000 ) ) ;
#6138=EDGE_LOOP ( 'NONE', ( #17800, #34391, #42656, #77 ) ) ;
#6139=LINE ( 'NONE', #45102, #8478 ) ;
#6141=ADVANCED_FACE ( 'NONE', ( #35322 ), #47656, .F. ) ;
#6142=DIRECTION ( 'NONE',  ( 0.000000000000000000, -1.000000000000000000, 0.000000000000000000 ) ) ;
#6143=DIRECTION ( 'NONE',  ( -3.469446951953613696E-16, 0.000000000000000000, -1.000000000000000000 ) ) ;
#6144=ORIENTED_EDGE ( 'NONE', *, *, #38281, .T. ) ;
#6146=LINE ( 'NONE', #41770, #1387 ) ;
#6147=VERTEX_POINT ( 'NONE', #18624 ) ;
#6150=VECTOR ( 'NONE', #5230, 39.37007874015748143 ) ;
#6151=ORIENTED_EDGE ( 'NONE', *, *, #5039, .T. ) ;
#6153=VECTOR ( 'NONE', #39848, 39.37007874015748143 ) ;
#6154=VECTOR ( 'NONE', #34647, 39.37007874015748143 ) ;
#6156=CARTESIAN_POINT ( 'NONE',  ( 1.287906020515829919, 3.346456692913386100, -1.771653543307081691 ) ) ;
#6157=VECTOR ( 'NONE', #176, 39.37007874015748143 ) ;
#6158=EDGE_CURVE ( 'NONE', #9586, #39809, #3118, .T. ) ;
#6160=AXIS2_PLACEMENT_3D ( 'NONE', #22159, #38412, #29901 ) ;
#6163=CARTESIAN_POINT ( 'NONE',  ( 2.106197740627111514, 3.201134874551266218, -1.299212598425194320 ) ) ;
#6168=EDGE_LOOP ( 'NONE', ( #49039, #12519, #19039, #29374 ) ) ;
#6170=CARTESIAN_POINT ( 'NONE',  ( -1.712496953225537633, 3.346456692913386100, -0.4724409448818884805 ) ) ;
#6171=ORIENTED_EDGE ( 'NONE', *, *, #30468, .F. ) ;
#6172=DIRECTION ( 'NONE',  ( -0.000000000000000000, 1.000000000000000000, -0.000000000000000000 ) ) ;
#6173=FACE_OUTER_BOUND ( 'NONE', #43064, .T. ) ;
#6175=DIRECTION ( 'NONE',  ( -1.000000000000000000, 0.000000000000000000, 0.000000000000000000 ) ) ;
#6176=PLANE ( 'NONE',  #19952 ) ;
#6177=CARTESIAN_POINT ( 'NONE',  ( -2.258024766633058622, 3.346456692913386100, 0.1574803149606286423 ) ) ;
#6178=ORIENTED_EDGE ( 'NONE', *, *, #48714, .T. ) ;
#6179=ORIENTED_EDGE ( 'NONE', *, *, #42519, .T. ) ;
#6181=FACE_BOUND ( 'NONE', #21381, .T. ) ;
#6182=ORIENTED_EDGE ( 'NONE', *, *, #28798, .F. ) ;
#6183=CARTESIAN_POINT ( 'NONE',  ( 0.000000000000000000, 3.267716535433071279, 0.7480314960629874665 ) ) ;
#6184=DIRECTION ( 'NONE',  ( 0.000000000000000000, 0.000000000000000000, -1.000000000000000000 ) ) ;
#6186=ORIENTED_EDGE ( 'NONE', *, *, #6497, .T. ) ;
#6187=EDGE_LOOP ( 'NONE', ( #18313, #4578, #5933, #16681 ) ) ;
#6188=CARTESIAN_POINT ( 'NONE',  ( -2.454875160333845674, 3.346456692913386100, 0.1574803149606286423 ) ) ;
#6189=ORIENTED_EDGE ( 'NONE', *, *, #36575, .F. ) ;
#6190=VECTOR ( 'NONE', #6529, 39.37007874015748143 ) ;
#6191=DIRECTION ( 'NONE',  ( 0.000000000000000000, -1.000000000000000000, 0.000000000000000000 ) ) ;
#6193=VECTOR ( 'NONE', #24750, 39.37007874015748143 ) ;
#6194=ORIENTED_EDGE ( 'NONE', *, *, #16760, .F. ) ;
#6197=EDGE_LOOP ( 'NONE', ( #25392, #40367, #38788, #18172 ) ) ;
#6198=DIRECTION ( 'NONE',  ( 0.000000000000000000, 0.000000000000000000, -1.000000000000000000 ) ) ;
#6199=LINE ( 'NONE', #45409, #7660 ) ;
#6200=ADVANCED_FACE ( 'NONE', ( #16207 ), #20059, .F. ) ;
#6201=EDGE_CURVE ( 'NONE', #50682, #20750, #31963, .T. ) ;
#6202=CARTESIAN_POINT ( 'NONE',  ( 0.2727639067037602172, 0.000000000000000000, -2.244094488188969727 ) ) ;
#6203=LINE ( 'NONE', #26073, #37897 ) ;
#6204=ORIENTED_EDGE ( 'NONE', *, *, #18202, .F. ) ;
#6205=ORIENTED_EDGE ( 'NONE', *, *, #23127, .T. ) ;
#6206=VECTOR ( 'NONE', #6555, 39.37007874015748143 ) ;
#6207=DIRECTION ( 'NONE',  ( -0.000000000000000000, 1.000000000000000000, -0.000000000000000000 ) ) ;
#6215=CARTESIAN_POINT ( 'NONE',  ( 0.1968503937007873017, 3.346456692913386100, -1.259842519685035134 ) ) ;
#6216=ORIENTED_EDGE ( 'NONE', *, *, #49010, .T. ) ;
#6217=DIRECTION ( 'NONE',  ( -3.469446951953613696E-16, 0.000000000000000000, -1.000000000000000000 ) ) ;
#6218=CARTESIAN_POINT ( 'NONE',  ( 1.091055626815043311, 3.346456692913386100, 1.870389530743258755 ) ) ;
#6219=ORIENTED_EDGE ( 'NONE', *, *, #5828, .F. ) ;
#6222=DIRECTION ( 'NONE',  ( 1.000000000000000000, -0.000000000000000000, 0.000000000000000000 ) ) ;
#6223=ORIENTED_EDGE ( 'NONE', *, *, #17480, .T. ) ;
#6224=EDGE_CURVE ( 'NONE', #4877, #29154, #50999, .T. ) ;
#6225=VECTOR ( 'NONE', #41144, 39.37007874015748143 ) ;
#6227=VERTEX_POINT ( 'NONE', #48924 ) ;
#6228=LINE ( 'NONE', #41593, #8921 ) ;
#6229=VECTOR ( 'NONE', #26102, 39.37007874015748143 ) ;
#6231=CARTESIAN_POINT ( 'NONE',  ( 0.2727639067037604947, 3.346456692913386100, -0.7874015748031473194 ) ) ;
#6232=CARTESIAN_POINT ( 'NONE',  ( 1.091055626815042423, 3.267716535433071279, -1.456692913385822630 ) ) ;
#6233=AXIS2_PLACEMENT_3D ( 'NONE', #27870, #23752, #47462 ) ;
#6236=ORIENTED_EDGE ( 'NONE', *, *, #33273, .F. ) ;
#6237=VECTOR ( 'NONE', #3237, 39.37007874015748143 ) ;
#6241=DIRECTION ( 'NONE',  ( 1.734723475976806848E-16, 0.000000000000000000, 1.000000000000000000 ) ) ;
#6242=DIRECTION ( 'NONE',  ( -0.000000000000000000, 1.000000000000000000, -0.000000000000000000 ) ) ;
#6243=LINE ( 'NONE', #14235, #45895 ) ;
#6244=ORIENTED_EDGE ( 'NONE', *, *, #24518, .T. ) ;
#6245=LINE ( 'NONE', #6506, #46077 ) ;
#6247=CARTESIAN_POINT ( 'NONE',  ( 1.909347346926324684, 3.346456692913386100, 0.7874015748031456541 ) ) ;
#6249=FACE_OUTER_BOUND ( 'NONE', #38560, .T. ) ;
#6250=DIRECTION ( 'NONE',  ( -1.000000000000000000, 0.000000000000000000, 0.000000000000000000 ) ) ;
#6251=PLANE ( 'NONE',  #1763 ) ;
#6253=EDGE_LOOP ( 'NONE', ( #7730, #26426, #44255, #12733 ) ) ;
#6254=CARTESIAN_POINT ( 'NONE',  ( -0.2727639067037611054, 3.346456692913386100, -2.148105963102950877 ) ) ;
#6255=EDGE_CURVE ( 'NONE', #11567, #34201, #40725, .T. ) ;
#6257=LINE ( 'NONE', #3140, #5531 ) ;
#6259=ORIENTED_EDGE ( 'NONE', *, *, #48985, .F. ) ;
#6260=ORIENTED_EDGE ( 'NONE', *, *, #22999, .F. ) ;
#6263=VECTOR ( 'NONE', #18733, 39.37007874015748143 ) ;
#6264=CARTESIAN_POINT ( 'NONE',  ( -1.712496953225537633, 0.000000000000000000, 1.417322834645662333 ) ) ;
#6266=ORIENTED_EDGE ( 'NONE', *, *, #25856, .T. ) ;
#6270=VECTOR ( 'NONE', #592, 39.37007874015748143 ) ;
#6271=CARTESIAN_POINT ( 'NONE',  ( -2.182111253630085734, 0.000000000000000000, -0.6299212598425177889 ) ) ;
#6272=CARTESIAN_POINT ( 'NONE',  ( 0.2727639067037604947, 3.267716535433071279, 0.7874015748031454320 ) ) ;
#6274=VECTOR ( 'NONE', #16580, 39.37007874015748143 ) ;
#6275=EDGE_LOOP ( 'NONE', ( #11530, #27050, #40743, #24401 ) ) ;
#6276=FACE_OUTER_BOUND ( 'NONE', #22961, .T. ) ;
#6278=EDGE_CURVE ( 'NONE', #1290, #26492, #28581, .T. ) ;
#6280=ORIENTED_EDGE ( 'NONE', *, *, #18103, .F. ) ;
#6281=DIRECTION ( 'NONE',  ( 1.000000000000000000, 0.000000000000000000, 0.000000000000000000 ) ) ;
#6283=CARTESIAN_POINT ( 'NONE',  ( 1.966928503432568975, 3.346456692913386100, 0.9055118110236164419 ) ) ;
#6285=ORIENTED_EDGE ( 'NONE', *, *, #46946, .F. ) ;
#6286=EDGE_CURVE ( 'NONE', #48366, #24319, #44827, .T. ) ;
#6287=DIRECTION ( 'NONE',  ( 1.734723475976806848E-16, 0.000000000000000000, 1.000000000000000000 ) ) ;
#6288=EDGE_CURVE ( 'NONE', #4024, #49804, #24725, .T. ) ;
#6289=EDGE_CURVE ( 'NONE', #20175, #25737, #24970, .T. ) ;
#6291=DIRECTION ( 'NONE',  ( -0.000000000000000000, 0.000000000000000000, 1.000000000000000000 ) ) ;
#6293=VERTEX_POINT ( 'NONE', #32996 ) ;
#6294=LINE ( 'NONE', #14800, #13046 ) ;
#6295=CARTESIAN_POINT ( 'NONE',  ( 0.000000000000000000, 2.344748451760389596, -2.874015748031496731 ) ) ;
#6296=DIRECTION ( 'NONE',  ( -3.469446951953613696E-16, 0.000000000000000000, -1.000000000000000000 ) ) ;
#6299=ORIENTED_EDGE ( 'NONE', *, *, #5096, .T. ) ;
#6300=ORIENTED_EDGE ( 'NONE', *, *, #5616, .T. ) ;
#6301=DIRECTION ( 'NONE',  ( 1.000000000000000000, 0.000000000000000000, 0.000000000000000000 ) ) ;
#6304=VECTOR ( 'NONE', #16998, 39.37007874015748143 ) ;
#6306=LINE ( 'NONE', #48858, #1183 ) ;
#6307=CARTESIAN_POINT ( 'NONE',  ( 0.000000000000000000, 3.267716535433071279, -1.259842519685035134 ) ) ;
#6308=CARTESIAN_POINT ( 'NONE',  ( 2.182111253630085290, 3.267716535433071279, -3.785359618865289765E-16 ) ) ;
#6309=CIRCLE ( 'NONE', #38448, 2.165354330708661568 ) ;
#6310=ORIENTED_EDGE ( 'NONE', *, *, #44784, .T. ) ;
#6312=CARTESIAN_POINT ( 'NONE',  ( -1.909347346926324906, 3.346456692913386100, 1.220472440944875059 ) ) ;
#6313=DIRECTION ( 'NONE',  ( -0.000000000000000000, 1.000000000000000000, -0.000000000000000000 ) ) ;
#6314=VECTOR ( 'NONE', #29305, 39.37007874015748143 ) ;
#6319=LINE ( 'NONE', #22065, #18654 ) ;
#6321=ORIENTED_EDGE ( 'NONE', *, *, #44854, .T. ) ;
#6322=LINE ( 'NONE', #21554, #33995 ) ;
#6325=DIRECTION ( 'NONE',  ( 1.000000000000000000, 0.000000000000000000, 0.000000000000000000 ) ) ;
#6328=ORIENTED_EDGE ( 'NONE', *, *, #1012, .F. ) ;
#6329=CARTESIAN_POINT ( 'NONE',  ( -1.909347346926324906, 0.000000000000000000, -0.7874015748031470974 ) ) ;
#6333=EDGE_CURVE ( 'NONE', #47259, #5956, #13359, .T. ) ;
#6334=ORIENTED_EDGE ( 'NONE', *, *, #18126, .T. ) ;
#6335=CARTESIAN_POINT ( 'NONE',  ( -1.636583440222563635, 3.346456692913386100, -0.1968503937007879123 ) ) ;
#6336=ADVANCED_FACE ( 'NONE', ( #5609 ), #32742, .F. ) ;
#6337=DIRECTION ( 'NONE',  ( 1.000000000000000000, 0.000000000000000000, 0.000000000000000000 ) ) ;
#6338=CIRCLE ( 'NONE', #41785, 2.165354330708661568 ) ;
#6339=LINE ( 'NONE', #22086, #37999 ) ;
#6340=DIRECTION ( 'NONE',  ( 1.734723475976806848E-16, 0.000000000000000000, 1.000000000000000000 ) ) ;
#6341=CARTESIAN_POINT ( 'NONE',  ( -1.439733046521776583, 3.267716535433071279, -1.617383112398506295 ) ) ;
#6343=CARTESIAN_POINT ( 'NONE',  ( -0.3486774197067334935, 0.000000000000000000, 1.062992125984246083 ) ) ;
#6344=AXIS2_PLACEMENT_3D ( 'NONE', #44786, #21571, #25692 ) ;
#6345=DIRECTION ( 'NONE',  ( 1.734723475976806848E-16, 0.000000000000000000, 1.000000000000000000 ) ) ;
#6346=ORIENTED_EDGE ( 'NONE', *, *, #10074, .F. ) ;
#6349=CARTESIAN_POINT ( 'NONE',  ( 1.833433833923351353, 0.000000000000000000, -0.9448818897637765168 ) ) ;
#6350=ORIENTED_EDGE ( 'NONE', *, *, #14354, .T. ) ;
#6351=CARTESIAN_POINT ( 'NONE',  ( -0.2727639067037607723, 0.000000000000000000, -1.102362204724405714 ) ) ;
#6352=AXIS2_PLACEMENT_3D ( 'NONE', #43377, #39009, #43882 ) ;
#6353=LINE ( 'NONE', #49417, #22550 ) ;
#6355=VECTOR ( 'NONE', #3441, 39.37007874015748143 ) ;
#6357=ORIENTED_EDGE ( 'NONE', *, *, #3745, .T. ) ;
#6358=DIRECTION ( 'NONE',  ( 1.000000000000000000, 0.000000000000000000, -3.469446951953613696E-16 ) ) ;
#6359=ORIENTED_EDGE ( 'NONE', *, *, #3625, .T. ) ;
#6360=FACE_BOUND ( 'NONE', #50352, .T. ) ;
#6364=LINE ( 'NONE', #29851, #30122 ) ;
#6365=ORIENTED_EDGE ( 'NONE', *, *, #629, .F. ) ;
#6366=VERTEX_POINT ( 'NONE', #17483 ) ;
#6367=DIRECTION ( 'NONE',  ( 1.000000000000000000, 0.000000000000000000, 0.000000000000000000 ) ) ;
#6368=CARTESIAN_POINT ( 'NONE',  ( 1.363819533518803695, 0.000000000000000000, 1.535433070866133898 ) ) ;
#6372=DIRECTION ( 'NONE',  ( 1.000000000000000000, 0.000000000000000000, 0.000000000000000000 ) ) ;
#6373=VECTOR ( 'NONE', #2117, 39.37007874015748143 ) ;
#6374=VECTOR ( 'NONE', #10973, 39.37007874015748143 ) ;
#6375=DIRECTION ( 'NONE',  ( 0.000000000000000000, 1.000000000000000000, 0.000000000000000000 ) ) ;
#6376=VECTOR ( 'NONE', #24687, 39.37007874015748143 ) ;
#6378=CARTESIAN_POINT ( 'NONE',  ( 0.8182917201112824834, 3.346456692913386100, 2.004783788421103718 ) ) ;
#6380=ORIENTED_EDGE ( 'NONE', *, *, #3682, .T. ) ;
#6382=EDGE_LOOP ( 'NONE', ( #6674, #14163, #48326, #19794 ) ) ;
#6383=ORIENTED_EDGE ( 'NONE', *, *, #45134, .F. ) ;
#6384=DIRECTION ( 'NONE',  ( 1.000000000000000000, 0.000000000000000000, 0.000000000000000000 ) ) ;
#6386=ADVANCED_FACE ( 'NONE', ( #28322 ), #44072, .F. ) ;
#6388=ORIENTED_EDGE ( 'NONE', *, *, #7469, .F. ) ;
#6390=DIRECTION ( 'NONE',  ( -0.000000000000000000, 1.000000000000000000, -0.000000000000000000 ) ) ;
#6391=CARTESIAN_POINT ( 'NONE',  ( 1.287906020515830141, 0.000000000000000000, 1.259842519685033357 ) ) ;
#6392=EDGE_CURVE ( 'NONE', #26276, #43980, #34003, .T. ) ;
#6395=CARTESIAN_POINT ( 'NONE',  ( 2.106197740627111958, 3.267716535433071279, -7.307341331430321661E-16 ) ) ;
#6396=DIRECTION ( 'NONE',  ( 1.734723475976806848E-16, 0.000000000000000000, 1.000000000000000000 ) ) ;
#6399=CARTESIAN_POINT ( 'NONE',  ( -1.166969139818016199, 3.267716535433071279, -1.929133858267710000 ) ) ;
#6400=DIRECTION ( 'NONE',  ( -0.000000000000000000, 1.000000000000000000, -0.000000000000000000 ) ) ;
#6405=EDGE_CURVE ( 'NONE', #10848, #3242, #37622, .T. ) ;
#6409=VECTOR ( 'NONE', #42360, 39.37007874015748143 ) ;
#6412=ORIENTED_EDGE ( 'NONE', *, *, #29170, .F. ) ;
#6413=EDGE_CURVE ( 'NONE', #19556, #45614, #38380, .T. ) ;
#6414=VECTOR ( 'NONE', #14754, 39.37007874015748143 ) ;
#6417=CARTESIAN_POINT ( 'NONE',  ( 1.287906020515830585, 0.000000000000000000, 1.889763779527550369 ) ) ;
#6418=CARTESIAN_POINT ( 'NONE',  ( 1.909347346926324462, 3.267716535433071279, -1.102362204724406602 ) ) ;
#6419=DIRECTION ( 'NONE',  ( -1.000000000000000000, 0.000000000000000000, 0.000000000000000000 ) ) ;
#6420=FACE_OUTER_BOUND ( 'NONE', #46991, .T. ) ;
#6421=ORIENTED_EDGE ( 'NONE', *, *, #8905, .T. ) ;
#6422=DIRECTION ( 'NONE',  ( 0.000000000000000000, 0.000000000000000000, -1.000000000000000000 ) ) ;
#6423=EDGE_LOOP ( 'NONE', ( #15930, #4900, #3819, #49354, #12414 ) ) ;
#6424=ORIENTED_EDGE ( 'NONE', *, *, #13516, .F. ) ;
#6426=EDGE_LOOP ( 'NONE', ( #44265, #38596, #35419, #50765 ) ) ;
#6427=CARTESIAN_POINT ( 'NONE',  ( 0.000000000000000000, 3.267716535433071279, -0.7874015748031467643 ) ) ;
#6428=AXIS2_PLACEMENT_3D ( 'NONE', #46803, #11719, #30338 ) ;
#6429=PLANE ( 'NONE',  #35091 ) ;
#6431=ORIENTED_EDGE ( 'NONE', *, *, #39130, .T. ) ;
#6435=VERTEX_POINT ( 'NONE', #2749 ) ;
#6436=ORIENTED_EDGE ( 'NONE', *, *, #2754, .T. ) ;
#6437=FACE_OUTER_BOUND ( 'NONE', #16229, .T. ) ;
#6438=FACE_BOUND ( 'NONE', #13813, .T. ) ;
#6440=CARTESIAN_POINT ( 'NONE',  ( -1.439733046521776361, 3.346456692913386100, 0.7480314960629874665 ) ) ;
#6441=DIRECTION ( 'NONE',  ( -0.000000000000000000, 1.000000000000000000, -0.000000000000000000 ) ) ;
#6442=AXIS2_PLACEMENT_3D ( 'NONE', #30544, #10416, #30292 ) ;
#6444=VECTOR ( 'NONE', #50476, 39.37007874015748143 ) ;
#6445=ORIENTED_EDGE ( 'NONE', *, *, #23852, .T. ) ;
#6446=ORIENTED_EDGE ( 'NONE', *, *, #36929, .T. ) ;
#6449=VERTEX_POINT ( 'NONE', #41992 ) ;
#6451=AXIS2_PLACEMENT_3D ( 'NONE', #28205, #44708, #9104 ) ;
#6453=PLANE ( 'NONE',  #9543 ) ;
#6455=LINE ( 'NONE', #26323, #23354 ) ;
#6457=EDGE_CURVE ( 'NONE', #20260, #32968, #14370, .T. ) ;
#6458=CARTESIAN_POINT ( 'NONE',  ( 1.953585199828834940, 3.346456692913386100, -0.7874015748031473194 ) ) ;
#6460=CARTESIAN_POINT ( 'NONE',  ( -0.07591351300297333182, 0.000000000000000000, -0.7874015748031470974 ) ) ;
#6461=AXIS2_PLACEMENT_3D ( 'NONE', #44782, #4095, #47153 ) ;
#6462=ORIENTED_EDGE ( 'NONE', *, *, #47253, .T. ) ;
#6463=ORIENTED_EDGE ( 'NONE', *, *, #34764, .T. ) ;
#6464=LINE ( 'NONE', #2582, #48010 ) ;
#6467=VECTOR ( 'NONE', #25632, 39.37007874015748143 ) ;
#6470=CARTESIAN_POINT ( 'NONE',  ( 1.909347346926324684, 3.346456692913386100, 0.9055118110236164419 ) ) ;
#6471=LINE ( 'NONE', #3095, #35787 ) ;
#6473=LINE ( 'NONE', #30972, #2812 ) ;
#6474=DIRECTION ( 'NONE',  ( 1.000000000000000000, 0.000000000000000000, 0.000000000000000000 ) ) ;
#6475=EDGE_LOOP ( 'NONE', ( #36449, #39268, #7132, #48029 ) ) ;
#6476=VERTEX_POINT ( 'NONE', #6629 ) ;
#6478=CIRCLE ( 'NONE', #22140, 2.165354330708661568 ) ;
#6479=VERTEX_POINT ( 'NONE', #18755 ) ;
#6480=EDGE_CURVE ( 'NONE', #7243, #4778, #14879, .T. ) ;
#6481=B_SPLINE_CURVE_WITH_KNOTS ( 'NONE', 3,
 ( #37720, #21963, #17827, #9573 ),
 .UNSPECIFIED., .F., .F.,
 ( 4, 4 ),
 ( 0.02665634820260516513, 0.02770374167893049910 ),
 .UNSPECIFIED. ) ;
#6482=ORIENTED_EDGE ( 'NONE', *, *, #16410, .T. ) ;
#6483=DIRECTION ( 'NONE',  ( -0.000000000000000000, 1.000000000000000000, -0.000000000000000000 ) ) ;
#6484=VECTOR ( 'NONE', #28886, 39.37007874015748143 ) ;
#6485=EDGE_CURVE ( 'NONE', #13805, #10560, #33501, .T. ) ;
#6486=ORIENTED_EDGE ( 'NONE', *, *, #21549, .F. ) ;
#6487=AXIS2_PLACEMENT_3D ( 'NONE', #25166, #17419, #24662 ) ;
#6489=CARTESIAN_POINT ( 'NONE',  ( -1.636583440222564301, 0.000000000000000000, -1.574803149606293307 ) ) ;
#6491=VECTOR ( 'NONE', #2003, 39.37007874015748143 ) ;
#6494=LINE ( 'NONE', #49551, #19722 ) ;
#6495=ORIENTED_EDGE ( 'NONE', *, *, #30047, .F. ) ;
#6497=EDGE_CURVE ( 'NONE', #23861, #16084, #46342, .T. ) ;
#6498=PLANE ( 'NONE',  #22372 ) ;
#6499=CARTESIAN_POINT ( 'NONE',  ( 0.8182917201112819283, 0.000000000000000000, -0.1574803149606301411 ) ) ;
#6500=DIRECTION ( 'NONE',  ( -3.469446951953613696E-16, 0.000000000000000000, -1.000000000000000000 ) ) ;
#6502=VECTOR ( 'NONE', #3797, 39.37007874015748143 ) ;
#6503=EDGE_CURVE ( 'NONE', #4956, #37208, #34257, .T. ) ;
#6504=VERTEX_POINT ( 'NONE', #11005 ) ;
#6506=CARTESIAN_POINT ( 'NONE',  ( -1.363819533518803473, 0.000000000000000000, -1.732283464566922726 ) ) ;
#6507=CARTESIAN_POINT ( 'NONE',  ( -1.439733046521776139, 0.000000000000000000, 0.9448818897637749625 ) ) ;
#6509=ORIENTED_EDGE ( 'NONE', *, *, #33749, .T. ) ;
#6511=CARTESIAN_POINT ( 'NONE',  ( -2.142325647309101022, 3.346456692913386100, -0.3149606299212589500 ) ) ;
#6512=DIRECTION ( 'NONE',  ( 1.000000000000000000, 0.000000000000000000, 0.000000000000000000 ) ) ;
#6513=ORIENTED_EDGE ( 'NONE', *, *, #13321, .T. ) ;
#6514=ORIENTED_EDGE ( 'NONE', *, *, #22921, .F. ) ;
#6517=CARTESIAN_POINT ( 'NONE',  ( -1.363819533518803029, 3.346456692913386100, 1.102362204724404160 ) ) ;
#6518=AXIS2_PLACEMENT_3D ( 'NONE', #48606, #36528, #33431 ) ;
#6519=DIRECTION ( 'NONE',  ( -0.000000000000000000, 1.000000000000000000, -0.000000000000000000 ) ) ;
#6521=EDGE_CURVE ( 'NONE', #19510, #6110, #38040, .T. ) ;
#6522=DIRECTION ( 'NONE',  ( 0.000000000000000000, -1.000000000000000000, 0.000000000000000000 ) ) ;
#6527=ORIENTED_EDGE ( 'NONE', *, *, #37396, .T. ) ;
#6528=CARTESIAN_POINT ( 'NONE',  ( -1.363819533518803473, 3.346456692913386100, -0.9842519685039344823 ) ) ;
#6529=DIRECTION ( 'NONE',  ( 1.000000000000000000, -0.000000000000000000, 0.000000000000000000 ) ) ;
#6532=VECTOR ( 'NONE', #540, 39.37007874015748143 ) ;
#6534=CARTESIAN_POINT ( 'NONE',  ( 0.8182917201112819283, 3.346456692913386100, -0.9842519685039348154 ) ) ;
#6537=DIRECTION ( 'NONE',  ( -0.000000000000000000, 1.000000000000000000, -0.000000000000000000 ) ) ;
#6539=VECTOR ( 'NONE', #5006, 39.37007874015748143 ) ;
#6540=CARTESIAN_POINT ( 'NONE',  ( 2.106197740627111958, 3.267716535433071279, 0.9055118110236164419 ) ) ;
#6544=CARTESIAN_POINT ( 'NONE',  ( 0.7423782071083087075, 3.267716535433071279, 0.9448818897637746295 ) ) ;
#6545=EDGE_LOOP ( 'NONE', ( #39801, #14153, #16070, #25236 ) ) ;
#6548=ORIENTED_EDGE ( 'NONE', *, *, #38395, .T. ) ;
#6549=DIRECTION ( 'NONE',  ( -1.000000000000000000, -0.000000000000000000, -0.000000000000000000 ) ) ;
#6550=ORIENTED_EDGE ( 'NONE', *, *, #38906, .F. ) ;
#6552=ADVANCED_FACE ( 'NONE', ( #42237 ), #43236, .F. ) ;
#6553=LINE ( 'NONE', #11177, #47383 ) ;
#6554=CARTESIAN_POINT ( 'NONE',  ( -0.8182917201112819283, 0.000000000000000000, -1.614173228346451605 ) ) ;
#6555=DIRECTION ( 'NONE',  ( -3.469446951953613696E-16, 0.000000000000000000, -1.000000000000000000 ) ) ;
#6556=EDGE_CURVE ( 'NONE', #19562, #36908, #27244, .T. ) ;
#6558=ADVANCED_FACE ( 'NONE', ( #42984 ), #20001, .F. ) ;
#6559=ORIENTED_EDGE ( 'NONE', *, *, #4527, .F. ) ;
#6560=ORIENTED_EDGE ( 'NONE', *, *, #10814, .T. ) ;
#6561=DIRECTION ( 'NONE',  ( -1.000000000000000000, -0.000000000000000000, -0.000000000000000000 ) ) ;
#6562=DIRECTION ( 'NONE',  ( -0.000000000000000000, 1.000000000000000000, -0.000000000000000000 ) ) ;
#6563=EDGE_LOOP ( 'NONE', ( #35935, #11011, #2704, #50121 ) ) ;
#6564=DIRECTION ( 'NONE',  ( -0.000000000000000000, 1.000000000000000000, -0.000000000000000000 ) ) ;
#6566=FACE_OUTER_BOUND ( 'NONE', #41120, .T. ) ;
#6568=ORIENTED_EDGE ( 'NONE', *, *, #17395, .T. ) ;
#6569=ORIENTED_EDGE ( 'NONE', *, *, #40933, .F. ) ;
#6570=LINE ( 'NONE', #2939, #19698 ) ;
#6571=CARTESIAN_POINT ( 'NONE',  ( -0.8182917201112814842, 3.346456692913386100, 0.4724409448818872592 ) ) ;
#6572=CARTESIAN_POINT ( 'NONE',  ( 0.2727639067037604947, 3.346456692913386100, 0.1574803149606283648 ) ) ;
#6573=ORIENTED_EDGE ( 'NONE', *, *, #334, .T. ) ;
#6578=DIRECTION ( 'NONE',  ( 1.000000000000000000, 0.000000000000000000, 0.000000000000000000 ) ) ;
#6580=ORIENTED_EDGE ( 'NONE', *, *, #2189, .F. ) ;
#6581=EDGE_CURVE ( 'NONE', #37657, #41218, #12017, .T. ) ;
#6582=VECTOR ( 'NONE', #30538, 39.37007874015748143 ) ;
#6584=CARTESIAN_POINT ( 'NONE',  ( 1.560669927219591413, 3.346456692913386100, 1.732283464566921172 ) ) ;
#6585=EDGE_CURVE ( 'NONE', #35311, #29664, #11510, .T. ) ;
#6586=CARTESIAN_POINT ( 'NONE',  ( 1.560669927219591413, 0.000000000000000000, 1.732283464566921172 ) ) ;
#6588=EDGE_CURVE ( 'NONE', #27292, #49048, #4023, .T. ) ;
#6591=DIRECTION ( 'NONE',  ( -1.000000000000000000, 0.000000000000000000, 0.000000000000000000 ) ) ;
#6592=ORIENTED_EDGE ( 'NONE', *, *, #24832, .F. ) ;
#6593=EDGE_CURVE ( 'NONE', #12364, #41352, #31134, .T. ) ;
#6594=EDGE_LOOP ( 'NONE', ( #22079, #20118, #6216, #40919 ) ) ;
#6595=DIRECTION ( 'NONE',  ( -1.000000000000000000, 0.000000000000000000, 1.734723475976806848E-16 ) ) ;
#6596=VECTOR ( 'NONE', #42049, 39.37007874015748143 ) ;
#6600=VERTEX_POINT ( 'NONE', #7637 ) ;
#6601=CARTESIAN_POINT ( 'NONE',  ( 1.833433833923351353, 3.267716535433071279, -6.361001426713998480E-16 ) ) ;
#6603=EDGE_LOOP ( 'NONE', ( #18318, #19202, #34390, #28044 ) ) ;
#6606=ORIENTED_EDGE ( 'NONE', *, *, #6556, .F. ) ;
#6609=DIRECTION ( 'NONE',  ( -1.000000000000000000, 0.000000000000000000, -0.000000000000000000 ) ) ;
#6612=VECTOR ( 'NONE', #33864, 39.37007874015748143 ) ;
#6613=ORIENTED_EDGE ( 'NONE', *, *, #42330, .T. ) ;
#6614=DIRECTION ( 'NONE',  ( 0.000000000000000000, 1.000000000000000000, 0.000000000000000000 ) ) ;
#6615=CARTESIAN_POINT ( 'NONE',  ( -1.712496953225537633, 3.346456692913386100, 1.226315847645293999 ) ) ;
#6616=CARTESIAN_POINT ( 'NONE',  ( 1.287906020515830141, 3.267716535433071279, 0.9448818897637746295 ) ) ;
#6617=LINE ( 'NONE', #33489, #49045 ) ;
#6618=EDGE_CURVE ( 'NONE', #1749, #41218, #39125, .T. ) ;
#6619=EDGE_CURVE ( 'NONE', #50789, #29175, #19499, .T. ) ;
#6620=VERTEX_POINT ( 'NONE', #35007 ) ;
#6621=EDGE_LOOP ( 'NONE', ( #32138, #36021, #47509, #6953 ) ) ;
#6622=CARTESIAN_POINT ( 'NONE',  ( 0.000000000000000000, 3.267716535433071279, -0.5118110236220464460 ) ) ;
#6623=DIRECTION ( 'NONE',  ( -0.000000000000000000, 0.000000000000000000, 1.000000000000000000 ) ) ;
#6624=CARTESIAN_POINT ( 'NONE',  ( -0.8182917201112819283, 3.267716535433071279, -1.299212598425193210 ) ) ;
#6627=VERTEX_POINT ( 'NONE', #35262 ) ;
#6629=CARTESIAN_POINT ( 'NONE',  ( -0.2727639067037602172, 3.346456692913386100, 1.732283464566921172 ) ) ;
#6630=ORIENTED_EDGE ( 'NONE', *, *, #197, .T. ) ;
#6631=FACE_OUTER_BOUND ( 'NONE', #10807, .T. ) ;
#6632=VERTEX_POINT ( 'NONE', #35512 ) ;
#6633=ORIENTED_EDGE ( 'NONE', *, *, #47490, .T. ) ;
#6634=EDGE_CURVE ( 'NONE', #11355, #15591, #31641, .T. ) ;
#6636=ADVANCED_FACE ( 'NONE', ( #23125 ), #22879, .F. ) ;
#6637=VECTOR ( 'NONE', #49326, 39.37007874015748143 ) ;
#6638=ORIENTED_EDGE ( 'NONE', *, *, #43768, .F. ) ;
#6640=DIRECTION ( 'NONE',  ( 1.734723475976806848E-16, -0.000000000000000000, 1.000000000000000000 ) ) ;
#6641=ADVANCED_FACE ( 'NONE', ( #15635 ), #34753, .F. ) ;
#6642=EDGE_CURVE ( 'NONE', #30226, #448, #16148, .T. ) ;
#6644=VECTOR ( 'NONE', #45387, 39.37007874015748143 ) ;
#6645=PLANE ( 'NONE',  #34508 ) ;
#6646=DIRECTION ( 'NONE',  ( 1.734723475976806848E-16, 0.000000000000000000, 1.000000000000000000 ) ) ;
#6650=ORIENTED_EDGE ( 'NONE', *, *, #25617, .F. ) ;
#6652=DIRECTION ( 'NONE',  ( -1.000000000000000000, -0.000000000000000000, -0.000000000000000000 ) ) ;
#6654=CARTESIAN_POINT ( 'NONE',  ( 1.287906020515830141, 0.000000000000000000, 0.9448818897637746295 ) ) ;
#6655=ORIENTED_EDGE ( 'NONE', *, *, #3257, .F. ) ;
#6657=CARTESIAN_POINT ( 'NONE',  ( -0.3486774197067334380, 3.346456692913386100, 1.574803149606291974 ) ) ;
#6658=ORIENTED_EDGE ( 'NONE', *, *, #3867, .F. ) ;
#6659=DIRECTION ( 'NONE',  ( 1.000000000000000000, 0.000000000000000000, -3.469446951953613696E-16 ) ) ;
#6660=DIRECTION ( 'NONE',  ( 0.000000000000000000, -1.000000000000000000, 0.000000000000000000 ) ) ;
#6662=LINE ( 'NONE', #46129, #31506 ) ;
#6663=ORIENTED_EDGE ( 'NONE', *, *, #41226, .F. ) ;
#6666=VECTOR ( 'NONE', #6143, 39.37007874015748143 ) ;
#6667=DIRECTION ( 'NONE',  ( -0.000000000000000000, 0.000000000000000000, 1.000000000000000000 ) ) ;
#6669=LINE ( 'NONE', #2034, #36674 ) ;
#6670=DIRECTION ( 'NONE',  ( 1.000000000000000000, 0.000000000000000000, -3.469446951953613696E-16 ) ) ;
#6671=ORIENTED_EDGE ( 'NONE', *, *, #8530, .T. ) ;
#6672=FACE_OUTER_BOUND ( 'NONE', #1321, .T. ) ;
#6673=EDGE_CURVE ( 'NONE', #40629, #47658, #38634, .T. ) ;
#6674=ORIENTED_EDGE ( 'NONE', *, *, #28625, .F. ) ;
#6675=ORIENTED_EDGE ( 'NONE', *, *, #43250, .F. ) ;
#6677=DIRECTION ( 'NONE',  ( -3.469446951953613696E-16, 0.000000000000000000, -1.000000000000000000 ) ) ;
#6681=CARTESIAN_POINT ( 'NONE',  ( -1.363819533518803029, 0.000000000000000000, 0.2755905511810996522 ) ) ;
#6683=EDGE_CURVE ( 'NONE', #35776, #46240, #12525, .T. ) ;
#6684=FACE_OUTER_BOUND ( 'NONE', #23916, .T. ) ;
#6685=CARTESIAN_POINT ( 'NONE',  ( -0.3486774197067339376, 3.346456692913386100, 2.137096964226333107 ) ) ;
#6686=ADVANCED_FACE ( 'NONE', ( #24916 ), #32162, .F. ) ;
#6687=DIRECTION ( 'NONE',  ( -0.000000000000000000, 0.000000000000000000, 1.000000000000000000 ) ) ;
#6688=ORIENTED_EDGE ( 'NONE', *, *, #34875, .T. ) ;
#6689=EDGE_LOOP ( 'NONE', ( #4598, #3449, #43877, #45964 ) ) ;
#6690=DIRECTION ( 'NONE',  ( 1.734723475976806848E-16, -0.000000000000000000, 1.000000000000000000 ) ) ;
#6691=FACE_BOUND ( 'NONE', #50479, .T. ) ;
#6693=LINE ( 'NONE', #22442, #24568 ) ;
#6694=EDGE_CURVE ( 'NONE', #50136, #4308, #5549, .T. ) ;
#6695=CARTESIAN_POINT ( 'NONE',  ( -1.636583440222563857, 3.267716535433071279, 2.839019714148966584E-16 ) ) ;
#6696=ORIENTED_EDGE ( 'NONE', *, *, #46603, .T. ) ;
#6697=ORIENTED_EDGE ( 'NONE', *, *, #22634, .F. ) ;
#6698=CARTESIAN_POINT ( 'NONE',  ( -0.2727639067037602172, 0.000000000000000000, 0.7874015748031456541 ) ) ;
#6701=VERTEX_POINT ( 'NONE', #40925 ) ;
#6702=ORIENTED_EDGE ( 'NONE', *, *, #13344, .T. ) ;
#6703=VERTEX_POINT ( 'NONE', #36544 ) ;
#6704=DIRECTION ( 'NONE',  ( -3.469446951953613696E-16, 0.000000000000000000, -1.000000000000000000 ) ) ;
#6707=AXIS2_PLACEMENT_3D ( 'NONE', #36087, #42353, #27810 ) ;
#6708=FACE_OUTER_BOUND ( 'NONE', #18918, .T. ) ;
#6709=ORIENTED_EDGE ( 'NONE', *, *, #15651, .T. ) ;
#6710=ORIENTED_EDGE ( 'NONE', *, *, #48426, .F. ) ;
#6711=DIRECTION ( 'NONE',  ( 1.000000000000000000, 0.000000000000000000, 0.000000000000000000 ) ) ;
#6712=CARTESIAN_POINT ( 'NONE',  ( -0.07591351300297333182, 0.000000000000000000, -1.102362204724405714 ) ) ;
#6713=LINE ( 'NONE', #45667, #6046 ) ;
#6714=AXIS2_PLACEMENT_3D ( 'NONE', #26362, #14234, #6500 ) ;
#6717=DIRECTION ( 'NONE',  ( -1.000000000000000000, 0.000000000000000000, 1.734723475976806848E-16 ) ) ;
#6718=VECTOR ( 'NONE', #26273, 39.37007874015748143 ) ;
#6720=DIRECTION ( 'NONE',  ( 0.000000000000000000, -1.000000000000000000, 0.000000000000000000 ) ) ;
#6723=LINE ( 'NONE', #45678, #45848 ) ;
#6724=ORIENTED_EDGE ( 'NONE', *, *, #7443, .F. ) ;
#6725=ORIENTED_EDGE ( 'NONE', *, *, #24426, .T. ) ;
#6726=CARTESIAN_POINT ( 'NONE',  ( 1.015142113812069979, 0.000000000000000000, 2.047244094488179567 ) ) ;
#6727=CARTESIAN_POINT ( 'NONE',  ( 1.363819533518803029, 0.000000000000000000, -1.732283464566923170 ) ) ;
#6728=VERTEX_POINT ( 'NONE', #29291 ) ;
#6730=EDGE_CURVE ( 'NONE', #29593, #44975, #44771, .T. ) ;
#6732=CARTESIAN_POINT ( 'NONE',  ( 0.2727639067037604947, 3.346456692913386100, -1.102362204724405714 ) ) ;
#6733=ORIENTED_EDGE ( 'NONE', *, *, #3050, .T. ) ;
#6734=ADVANCED_FACE ( 'NONE', ( #20532 ), #44523, .F. ) ;
#6737=FACE_OUTER_BOUND ( 'NONE', #17726, .T. ) ;
#6738=VECTOR ( 'NONE', #20784, 39.37007874015748143 ) ;
#6740=EDGE_CURVE ( 'NONE', #11491, #45764, #24149, .T. ) ;
#6742=VECTOR ( 'NONE', #18549, 39.37007874015748143 ) ;
#6743=DIRECTION ( 'NONE',  ( -0.000000000000000000, 1.000000000000000000, -0.000000000000000000 ) ) ;
#6745=VERTEX_POINT ( 'NONE', #13302 ) ;
#6747=CARTESIAN_POINT ( 'NONE',  ( -2.182111253630085290, 3.346456692913386100, -0.1968503937007880511 ) ) ;
#6751=ORIENTED_EDGE ( 'NONE', *, *, #10988, .T. ) ;
#6755=LINE ( 'NONE', #6247, #28648 ) ;
#6756=VERTEX_POINT ( 'NONE', #28522 ) ;
#6758=EDGE_CURVE ( 'NONE', #39701, #12754, #32419, .T. ) ;
#6760=VERTEX_POINT ( 'NONE', #32943 ) ;
#6764=CARTESIAN_POINT ( 'NONE',  ( 1.091055626815042645, 0.000000000000000000, -1.141732283464564013 ) ) ;
#6767=CARTESIAN_POINT ( 'NONE',  ( -1.195183497228115035E-16, 0.000000000000000000, -1.574803149606293529 ) ) ;
#6771=EDGE_CURVE ( 'NONE', #20825, #22703, #9425, .T. ) ;
#6772=LINE ( 'NONE', #45985, #6190 ) ;
#6775=DIRECTION ( 'NONE',  ( 1.000000000000000000, 0.000000000000000000, -3.469446951953613696E-16 ) ) ;
#6777=ORIENTED_EDGE ( 'NONE', *, *, #46551, .T. ) ;
#6778=CARTESIAN_POINT ( 'NONE',  ( 1.287906020515829919, 3.346456692913386100, -1.740706023381844547 ) ) ;
#6779=DIRECTION ( 'NONE',  ( 1.000000000000000000, 0.000000000000000000, -3.469446951953613696E-16 ) ) ;
#6782=LINE ( 'NONE', #22526, #7583 ) ;
#6783=EDGE_CURVE ( 'NONE', #2471, #9083, #21301, .T. ) ;
#6784=ORIENTED_EDGE ( 'NONE', *, *, #27773, .F. ) ;
#6788=CARTESIAN_POINT ( 'NONE',  ( 3.927031490892378253E-16, 3.267716535433071279, 2.007874015748021268 ) ) ;
#6789=ORIENTED_EDGE ( 'NONE', *, *, #3984, .T. ) ;
#6790=FACE_OUTER_BOUND ( 'NONE', #46621, .T. ) ;
#6793=EDGE_LOOP ( 'NONE', ( #24498, #39832, #8666, #18929 ) ) ;
#6795=EDGE_CURVE ( 'NONE', #34431, #35644, #16920, .T. ) ;
#6797=PLANE ( 'NONE',  #14863 ) ;
#6798=FACE_OUTER_BOUND ( 'NONE', #40928, .T. ) ;
#6799=EDGE_CURVE ( 'NONE', #28822, #37178, #1676, .T. ) ;
#6800=ORIENTED_EDGE ( 'NONE', *, *, #9588, .F. ) ;
#6801=ORIENTED_EDGE ( 'NONE', *, *, #41999, .F. ) ;
#6802=CARTESIAN_POINT ( 'NONE',  ( -1.066305685425808392, 3.256158526051301738, 2.204724409448808764 ) ) ;
#6803=LINE ( 'NONE', #33684, #29622 ) ;
#6804=ORIENTED_EDGE ( 'NONE', *, *, #4709, .T. ) ;
#6806=DIRECTION ( 'NONE',  ( 1.734723475976806848E-16, -0.000000000000000000, 1.000000000000000000 ) ) ;
#6807=CARTESIAN_POINT ( 'NONE',  ( 1.636583440222563857, 3.267716535433071279, -0.3149606299212596716 ) ) ;
#6810=VECTOR ( 'NONE', #33826, 39.37007874015748143 ) ;
#6814=DIRECTION ( 'NONE',  ( 0.000000000000000000, 0.000000000000000000, -1.000000000000000000 ) ) ;
#6816=ORIENTED_EDGE ( 'NONE', *, *, #18990, .F. ) ;
#6818=VECTOR ( 'NONE', #18242, 39.37007874015748143 ) ;
#6821=CARTESIAN_POINT ( 'NONE',  ( 0.5455278134075211005, 3.346456692913386100, -0.5118110236220467790 ) ) ;
#6823=VECTOR ( 'NONE', #46780, 39.37007874015748143 ) ;
#6824=VERTEX_POINT ( 'NONE', #38326 ) ;
#6827=VECTOR ( 'NONE', #42634, 39.37007874015748143 ) ;
#6828=VECTOR ( 'NONE', #13699, 39.37007874015748143 ) ;
#6832=CARTESIAN_POINT ( 'NONE',  ( -0.5455278134075214336, 0.000000000000000000, -0.3149606299212593941 ) ) ;
#6833=VERTEX_POINT ( 'NONE', #41680 ) ;
#6834=EDGE_LOOP ( 'NONE', ( #37257, #31467, #21374, #3303 ) ) ;
#6835=CARTESIAN_POINT ( 'NONE',  ( 0.7423782071083092626, 3.346456692913386100, 1.574803149606291974 ) ) ;
#6836=EDGE_CURVE ( 'NONE', #29967, #22951, #45520, .T. ) ;
#6837=DIRECTION ( 'NONE',  ( -1.000000000000000000, 0.000000000000000000, 0.000000000000000000 ) ) ;
#6839=EDGE_CURVE ( 'NONE', #35448, #23722, #49383, .T. ) ;
#6841=DIRECTION ( 'NONE',  ( -3.469446951953613696E-16, 0.000000000000000000, -1.000000000000000000 ) ) ;
#6842=CARTESIAN_POINT ( 'NONE',  ( -0.8182917201112821504, 3.267716535433071279, 1.940849049717691344 ) ) ;
#6843=VERTEX_POINT ( 'NONE', #1931 ) ;
#6844=LINE ( 'NONE', #15096, #12644 ) ;
#6845=EDGE_CURVE ( 'NONE', #50043, #16378, #13811, .T. ) ;
#6847=ORIENTED_EDGE ( 'NONE', *, *, #4878, .F. ) ;
#6849=LINE ( 'NONE', #46314, #6374 ) ;
#6850=ORIENTED_EDGE ( 'NONE', *, *, #2415, .F. ) ;
#6852=CARTESIAN_POINT ( 'NONE',  ( 1.091055626815042645, 3.267716535433071279, -8.878505979408855953E-16 ) ) ;
#6853=PLANE ( 'NONE',  #7875 ) ;
#6854=VECTOR ( 'NONE', #13552, 39.37007874015748143 ) ;
#6855=ORIENTED_EDGE ( 'NONE', *, *, #44442, .F. ) ;
#6856=DIRECTION ( 'NONE',  ( 1.000000000000000000, 0.000000000000000000, -3.469446951953613696E-16 ) ) ;
#6858=FACE_BOUND ( 'NONE', #26318, .T. ) ;
#6859=AXIS2_PLACEMENT_3D ( 'NONE', #26625, #23507, #23769 ) ;
#6860=EDGE_CURVE ( 'NONE', #48901, #11981, #10185, .T. ) ;
#6861=VECTOR ( 'NONE', #23717, 39.37007874015748143 ) ;
#6862=CARTESIAN_POINT ( 'NONE',  ( 1.015142113812069313, 3.267716535433071279, -0.03937007874015881204 ) ) ;
#6863=DIRECTION ( 'NONE',  ( 0.000000000000000000, -1.000000000000000000, 0.000000000000000000 ) ) ;
#6866=ORIENTED_EDGE ( 'NONE', *, *, #668, .F. ) ;
#6867=LINE ( 'NONE', #6622, #24875 ) ;
#6868=AXIS2_PLACEMENT_3D ( 'NONE', #16949, #28036, #24176 ) ;
#6870=FACE_OUTER_BOUND ( 'NONE', #25046, .T. ) ;
#6871=DIRECTION ( 'NONE',  ( 0.000000000000000000, -1.000000000000000000, 0.000000000000000000 ) ) ;
#6876=CARTESIAN_POINT ( 'NONE',  ( 0.7423782071083091516, 0.000000000000000000, 1.062992125984246083 ) ) ;
#6877=CARTESIAN_POINT ( 'NONE',  ( -0.5455278134075214336, 0.000000000000000000, -1.889763779527552146 ) ) ;
#6878=ORIENTED_EDGE ( 'NONE', *, *, #23808, .F. ) ;
#6879=LINE ( 'NONE', #34260, #10099 ) ;
#6881=ORIENTED_EDGE ( 'NONE', *, *, #45196, .F. ) ;
#6883=ORIENTED_EDGE ( 'NONE', *, *, #10077, .T. ) ;
#6885=VECTOR ( 'NONE', #15751, 39.37007874015748143 ) ;
#6888=CARTESIAN_POINT ( 'NONE',  ( -0.8942052331142552601, 3.346456692913386100, -0.8267716535433052849 ) ) ;
#6890=VECTOR ( 'NONE', #40623, 39.37007874015748143 ) ;
#6892=EDGE_CURVE ( 'NONE', #15453, #13805, #6054, .T. ) ;
#6894=EDGE_CURVE ( 'NONE', #26463, #12576, #17934, .T. ) ;
#6895=MANIFOLD_SOLID_BREP ( 'Extrude-Thin1', #2356 ) ;
#6896=CARTESIAN_POINT ( 'NONE',  ( 0.8182917201112817063, 3.346456692913386100, -1.417322834645664331 ) ) ;
#6899=ORIENTED_EDGE ( 'NONE', *, *, #21441, .F. ) ;
#6901=DIRECTION ( 'NONE',  ( 0.000000000000000000, -1.000000000000000000, 0.000000000000000000 ) ) ;
#6906=DIRECTION ( 'NONE',  ( 1.000000000000000000, 0.000000000000000000, 0.000000000000000000 ) ) ;
#6907=ORIENTED_EDGE ( 'NONE', *, *, #46295, .F. ) ;
#6908=LINE ( 'NONE', #25765, #9778 ) ;
#6909=LINE ( 'NONE', #29388, #25954 ) ;
#6911=LINE ( 'NONE', #42531, #16677 ) ;
#6912=EDGE_CURVE ( 'NONE', #17493, #7739, #49629, .T. ) ;
#6913=ORIENTED_EDGE ( 'NONE', *, *, #49537, .T. ) ;
#6916=PLANE ( 'NONE',  #20430 ) ;
#6918=LINE ( 'NONE', #39169, #11093 ) ;
#6919=DIRECTION ( 'NONE',  ( 0.000000000000000000, 0.000000000000000000, -1.000000000000000000 ) ) ;
#6920=ORIENTED_EDGE ( 'NONE', *, *, #24494, .T. ) ;
#6922=EDGE_CURVE ( 'NONE', #37613, #49793, #11198, .T. ) ;
#6923=CARTESIAN_POINT ( 'NONE',  ( 0.8182917201112819283, 3.346456692913386100, -0.7874015748031473194 ) ) ;
#6924=VECTOR ( 'NONE', #43243, 39.37007874015748143 ) ;
#6925=ORIENTED_EDGE ( 'NONE', *, *, #36655, .F. ) ;
#6927=AXIS2_PLACEMENT_3D ( 'NONE', #41562, #34081, #49767 ) ;
#6928=PLANE ( 'NONE',  #45986 ) ;
#6930=ORIENTED_EDGE ( 'NONE', *, *, #3561, .T. ) ;
#6931=CARTESIAN_POINT ( 'NONE',  ( -6.488138984952753334E-17, 3.267716535433071279, 1.125512701259787342E-32 ) ) ;
#6932=VECTOR ( 'NONE', #2539, 39.37007874015748143 ) ;
#6933=CARTESIAN_POINT ( 'NONE',  ( -0.5455278134075214336, 3.267716535433071279, 0.1181102362204703021 ) ) ;
#6934=ORIENTED_EDGE ( 'NONE', *, *, #48301, .T. ) ;
#6936=CIRCLE ( 'NONE', #25065, 2.106299212598425008 ) ;
#6937=PLANE ( 'NONE',  #14892 ) ;
#6942=ORIENTED_EDGE ( 'NONE', *, *, #42151, .T. ) ;
#6943=DIRECTION ( 'NONE',  ( 1.734723475976806848E-16, 0.000000000000000000, 1.000000000000000000 ) ) ;
#6944=FACE_BOUND ( 'NONE', #10930, .T. ) ;
#6945=ORIENTED_EDGE ( 'NONE', *, *, #19650, .F. ) ;
#6948=VERTEX_POINT ( 'NONE', #11696 ) ;
#6953=ORIENTED_EDGE ( 'NONE', *, *, #14103, .F. ) ;
#6955=DIRECTION ( 'NONE',  ( -0.000000000000000000, 1.000000000000000000, -0.000000000000000000 ) ) ;
#6956=LINE ( 'NONE', #27069, #24762 ) ;
#6957=EDGE_LOOP ( 'NONE', ( #2868, #29903, #20791, #36682 ) ) ;
#6958=ORIENTED_EDGE ( 'NONE', *, *, #16939, .F. ) ;
#6961=CARTESIAN_POINT ( 'NONE',  ( 0.2727639067037610499, 0.000000000000000000, 1.732283464566921172 ) ) ;
#6964=ADVANCED_FACE ( 'NONE', ( #27688 ), #15577, .F. ) ;
#6967=DIRECTION ( 'NONE',  ( 1.734723475976806848E-16, -0.000000000000000000, 1.000000000000000000 ) ) ;
#6969=AXIS2_PLACEMENT_3D ( 'NONE', #12119, #32259, #48464 ) ;
#6970=CARTESIAN_POINT ( 'NONE',  ( 0.1968503937007873017, 0.000000000000000000, 0.6299212598425161236 ) ) ;
#6971=AXIS2_PLACEMENT_3D ( 'NONE', #48648, #36833, #13334 ) ;
#6972=CARTESIAN_POINT ( 'NONE',  ( 1.909347346926324684, 0.000000000000000000, -0.4724409448818889246 ) ) ;
#6973=DIRECTION ( 'NONE',  ( -0.000000000000000000, 1.000000000000000000, -0.000000000000000000 ) ) ;
#6976=LINE ( 'NONE', #3347, #18479 ) ;
#6977=FACE_OUTER_BOUND ( 'NONE', #23746, .T. ) ;
#6979=ORIENTED_EDGE ( 'NONE', *, *, #23803, .T. ) ;
#6980=CARTESIAN_POINT ( 'NONE',  ( -1.909347346926324462, 0.000000000000000000, 0.7874015748031456541 ) ) ;
#6981=CARTESIAN_POINT ( 'NONE',  ( 1.909347346926324462, 3.346456692913386100, -0.7874015748031473194 ) ) ;
#6982=EDGE_CURVE ( 'NONE', #29807, #3259, #15818, .T. ) ;
#6983=EDGE_LOOP ( 'NONE', ( #44641, #14949, #36735, #17001 ) ) ;
#6986=EDGE_LOOP ( 'NONE', ( #5452, #45151, #28019, #35832 ) ) ;
#6987=CARTESIAN_POINT ( 'NONE',  ( -1.862188077367287642, 3.267716535433071279, -0.9842519685039344823 ) ) ;
#6990=PLANE ( 'NONE',  #25542 ) ;
#6991=VERTEX_POINT ( 'NONE', #35453 ) ;
#6992=FACE_OUTER_BOUND ( 'NONE', #35517, .T. ) ;
#6995=ORIENTED_EDGE ( 'NONE', *, *, #8696, .T. ) ;
#6997=CARTESIAN_POINT ( 'NONE',  ( -1.794796351285541602, 3.346456692913386100, -1.102362204724405492 ) ) ;
#6999=CARTESIAN_POINT ( 'NONE',  ( 1.091055626815043311, 3.346456692913386100, 1.574803149606291974 ) ) ;
#7000=CARTESIAN_POINT ( 'NONE',  ( -1.909347346926324462, 0.000000000000000000, -0.1574803149606297248 ) ) ;
#7004=CARTESIAN_POINT ( 'NONE',  ( -1.712496953225537633, 3.267716535433071279, -0.6692913385826758654 ) ) ;
#7009=EDGE_LOOP ( 'NONE', ( #42719, #34929, #15640, #49501 ) ) ;
#7011=DIRECTION ( 'NONE',  ( -1.000000000000000000, -0.000000000000000000, -0.000000000000000000 ) ) ;
#7012=DIRECTION ( 'NONE',  ( 0.000000000000000000, 0.000000000000000000, -1.000000000000000000 ) ) ;
#7013=CARTESIAN_POINT ( 'NONE',  ( -1.363819533518803029, 0.000000000000000000, 1.417322834645662777 ) ) ;
#7014=CARTESIAN_POINT ( 'NONE',  ( 1.833433833923351353, 3.267716535433071279, 0.4330708661417290162 ) ) ;
#7017=EDGE_CURVE ( 'NONE', #47774, #29685, #3702, .T. ) ;
#7021=ORIENTED_EDGE ( 'NONE', *, *, #24627, .T. ) ;
#7022=CARTESIAN_POINT ( 'NONE',  ( -1.439733046521776361, 3.267716535433071279, 4.995077429881866871E-16 ) ) ;
#7024=ADVANCED_FACE ( 'NONE', ( #43435 ), #4206, .F. ) ;
#7025=EDGE_CURVE ( 'NONE', #37496, #13662, #30568, .T. ) ;
#7030=ORIENTED_EDGE ( 'NONE', *, *, #16659, .F. ) ;
#7031=VECTOR ( 'NONE', #2269, 39.37007874015748143 ) ;
#7034=VECTOR ( 'NONE', #23239, 39.37007874015748143 ) ;
#7039=ORIENTED_EDGE ( 'NONE', *, *, #15683, .F. ) ;
#7040=CARTESIAN_POINT ( 'NONE',  ( -2.258024766633058622, 3.267716535433071279, -0.1574803149606298636 ) ) ;
#7041=CARTESIAN_POINT ( 'NONE',  ( -1.985260859929297794, 0.000000000000000000, -0.5118110236220464460 ) ) ;
#7042=EDGE_CURVE ( 'NONE', #43305, #50744, #7074, .T. ) ;
#7043=CARTESIAN_POINT ( 'NONE',  ( 0.000000000000000000, 3.267716535433071279, 0.000000000000000000 ) ) ;
#7044=ORIENTED_EDGE ( 'NONE', *, *, #1185, .F. ) ;
#7045=CARTESIAN_POINT ( 'NONE',  ( 1.287906020515829919, 3.346456692913386100, -1.574803149606294417 ) ) ;
#7046=VECTOR ( 'NONE', #1141, 39.37007874015748143 ) ;
#7047=EDGE_CURVE ( 'NONE', #16270, #20260, #12209, .T. ) ;
#7048=ORIENTED_EDGE ( 'NONE', *, *, #23337, .T. ) ;
#7049=LINE ( 'NONE', #38546, #1509 ) ;
#7050=ORIENTED_EDGE ( 'NONE', *, *, #35108, .F. ) ;
#7051=PLANE ( 'NONE',  #43493 ) ;
#7053=LINE ( 'NONE', #2669, #8697 ) ;
#7055=DIRECTION ( 'NONE',  ( 1.000000000000000000, 0.000000000000000000, 0.000000000000000000 ) ) ;
#7058=EDGE_LOOP ( 'NONE', ( #7366, #20579, #43241, #40992 ) ) ;
#7059=ORIENTED_EDGE ( 'NONE', *, *, #1186, .F. ) ;
#7061=CARTESIAN_POINT ( 'NONE',  ( -0.5455278134075214336, 3.346456692913386100, 2.204724409448808764 ) ) ;
#7065=DIRECTION ( 'NONE',  ( 1.000000000000000000, 0.000000000000000000, 0.000000000000000000 ) ) ;
#7066=ADVANCED_FACE ( 'NONE', ( #24852 ), #40087, .F. ) ;
#7069=ORIENTED_EDGE ( 'NONE', *, *, #26161, .F. ) ;
#7070=LINE ( 'NONE', #46278, #29599 ) ;
#7074=LINE ( 'NONE', #36732, #10894 ) ;
#7075=DIRECTION ( 'NONE',  ( -0.000000000000000000, 1.000000000000000000, -0.000000000000000000 ) ) ;
#7076=VECTOR ( 'NONE', #15283, 39.37007874015748143 ) ;
#7078=AXIS2_PLACEMENT_3D ( 'NONE', #29842, #16959, #28817 ) ;
#7079=CARTESIAN_POINT ( 'NONE',  ( 1.560669927219590747, 3.346456692913386100, 1.102362204724403938 ) ) ;
#7080=ORIENTED_EDGE ( 'NONE', *, *, #45335, .F. ) ;
#7085=PLANE ( 'NONE',  #10757 ) ;
#7087=DIRECTION ( 'NONE',  ( 0.000000000000000000, -1.000000000000000000, 0.000000000000000000 ) ) ;
#7088=CARTESIAN_POINT ( 'NONE',  ( -0.6214413264104945434, 0.000000000000000000, -1.102362204724405492 ) ) ;
#7089=EDGE_LOOP ( 'NONE', ( #19755, #48060, #18455, #49071 ) ) ;
#7090=VECTOR ( 'NONE', #30040, 39.37007874015748143 ) ;
#7093=CARTESIAN_POINT ( 'NONE',  ( -0.2727639067037608278, 3.267716535433071279, -0.9842519685039344823 ) ) ;
#7094=CARTESIAN_POINT ( 'NONE',  ( -1.909347346926324462, 3.346456692913386100, -0.1574803149606297248 ) ) ;
#7095=EDGE_CURVE ( 'NONE', #18320, #43157, #44203, .T. ) ;
#7097=EDGE_CURVE ( 'NONE', #37613, #48933, #9355, .T. ) ;
#7098=DIRECTION ( 'NONE',  ( -0.000000000000000000, 1.000000000000000000, -0.000000000000000000 ) ) ;
#7100=ORIENTED_EDGE ( 'NONE', *, *, #32168, .T. ) ;
#7101=LINE ( 'NONE', #18723, #44809 ) ;
#7102=DIRECTION ( 'NONE',  ( -0.000000000000000000, 0.000000000000000000, 1.000000000000000000 ) ) ;
#7104=LINE ( 'NONE', #45804, #26496 ) ;
#7105=CARTESIAN_POINT ( 'NONE',  ( 2.378961647330872786, 0.000000000000000000, -1.161035397307311917E-15 ) ) ;
#7108=CARTESIAN_POINT ( 'NONE',  ( 1.091055626815042645, 3.346456692913386100, -0.9448818897637765168 ) ) ;
#7109=CARTESIAN_POINT ( 'NONE',  ( -0.2727639067037607723, 3.267716535433071279, 0.1574803149606283648 ) ) ;
#7110=DIRECTION ( 'NONE',  ( -0.000000000000000000, 1.000000000000000000, -0.000000000000000000 ) ) ;
#7111=AXIS2_PLACEMENT_3D ( 'NONE', #48935, #29625, #6384 ) ;
#7114=LINE ( 'NONE', #22606, #45271 ) ;
#7116=CARTESIAN_POINT ( 'NONE',  ( 0.000000000000000000, 3.267716535433071279, 0.000000000000000000 ) ) ;
#7117=VECTOR ( 'NONE', #20452, 39.37007874015748143 ) ;
#7120=VECTOR ( 'NONE', #22256, 39.37007874015748143 ) ;
#7121=EDGE_CURVE ( 'NONE', #9684, #43163, #4973, .T. ) ;
#7122=AXIS2_PLACEMENT_3D ( 'NONE', #3815, #7936, #35317 ) ;
#7127=LINE ( 'NONE', #34998, #25023 ) ;
#7128=PLANE ( 'NONE',  #48269 ) ;
#7129=CARTESIAN_POINT ( 'NONE',  ( -2.182111253630085290, 0.000000000000000000, -0.3149606299212589500 ) ) ;
#7132=ORIENTED_EDGE ( 'NONE', *, *, #15216, .F. ) ;
#7134=CARTESIAN_POINT ( 'NONE',  ( -0.3486774197067334380, 3.267716535433071279, 1.209717811016577106E-16 ) ) ;
#7135=EDGE_CURVE ( 'NONE', #11168, #15727, #20977, .T. ) ;
#7138=EDGE_CURVE ( 'NONE', #21275, #43635, #32611, .T. ) ;
#7139=FACE_OUTER_BOUND ( 'NONE', #3575, .T. ) ;
#7140=ORIENTED_EDGE ( 'NONE', *, *, #48831, .F. ) ;
#7141=ORIENTED_EDGE ( 'NONE', *, *, #7346, .T. ) ;
#7142=ADVANCED_FACE ( 'NONE', ( #5222 ), #25108, .F. ) ;
#7144=VECTOR ( 'NONE', #42522, 39.37007874015748143 ) ;
#7145=ORIENTED_EDGE ( 'NONE', *, *, #15216, .T. ) ;
#7146=ORIENTED_EDGE ( 'NONE', *, *, #1847, .T. ) ;
#7147=LINE ( 'NONE', #38390, #30215 ) ;
#7148=AXIS2_PLACEMENT_3D ( 'NONE', #48190, #40492, #43581 ) ;
#7150=CARTESIAN_POINT ( 'NONE',  ( -1.439733046521777027, 0.000000000000000000, -1.771653543307080581 ) ) ;
#7153=VECTOR ( 'NONE', #10706, 39.37007874015748143 ) ;
#7154=DIRECTION ( 'NONE',  ( 1.000000000000000000, 0.000000000000000000, 0.000000000000000000 ) ) ;
#7155=ADVANCED_FACE ( 'NONE', ( #24081 ), #4721, .F. ) ;
#7159=CARTESIAN_POINT ( 'NONE',  ( 0.2727639067037604947, 3.346456692913386100, -1.417322834645664331 ) ) ;
#7160=VERTEX_POINT ( 'NONE', #846 ) ;
#7161=DIRECTION ( 'NONE',  ( 1.734723475976806848E-16, -0.000000000000000000, 1.000000000000000000 ) ) ;
#7162=LINE ( 'NONE', #26765, #3609 ) ;
#7164=DIRECTION ( 'NONE',  ( 1.000000000000000000, 0.000000000000000000, -3.469446951953613696E-16 ) ) ;
#7165=ORIENTED_EDGE ( 'NONE', *, *, #23474, .T. ) ;
#7166=CARTESIAN_POINT ( 'NONE',  ( 4.268512490100411402E-16, 0.000000000000000000, 1.574803149606291974 ) ) ;
#7169=LINE ( 'NONE', #42524, #1556 ) ;
#7170=PLANE ( 'NONE',  #11095 ) ;
#7171=CARTESIAN_POINT ( 'NONE',  ( 0.000000000000000000, 3.267716535433071279, 1.220472440944875281 ) ) ;
#7173=DIRECTION ( 'NONE',  ( -1.000000000000000000, 0.000000000000000000, -0.000000000000000000 ) ) ;
#7174=FACE_OUTER_BOUND ( 'NONE', #47667, .T. ) ;
#7177=CARTESIAN_POINT ( 'NONE',  ( 0.1968503937007872462, 0.000000000000000000, -1.771653543307081025 ) ) ;
#7178=ORIENTED_EDGE ( 'NONE', *, *, #5811, .T. ) ;
#7179=VECTOR ( 'NONE', #34228, 39.37007874015748143 ) ;
#7181=DIRECTION ( 'NONE',  ( -0.000000000000000000, 1.000000000000000000, -0.000000000000000000 ) ) ;
#7183=VERTEX_POINT ( 'NONE', #12458 ) ;
#7185=LINE ( 'NONE', #50733, #13882 ) ;
#7186=ORIENTED_EDGE ( 'NONE', *, *, #9271, .F. ) ;
#7188=DIRECTION ( 'NONE',  ( 1.000000000000000000, 0.000000000000000000, 0.000000000000000000 ) ) ;
#7189=VERTEX_POINT ( 'NONE', #41618 ) ;
#7193=VECTOR ( 'NONE', #6519, 39.37007874015748143 ) ;
#7194=DIRECTION ( 'NONE',  ( 1.000000000000000000, -0.000000000000000000, 0.000000000000000000 ) ) ;
#7195=EDGE_CURVE ( 'NONE', #49909, #50260, #13745, .T. ) ;
#7197=CARTESIAN_POINT ( 'NONE',  ( 0.9834642517162937025, 3.267716535433071279, -1.929133858267711110 ) ) ;
#7198=EDGE_LOOP ( 'NONE', ( #50483, #28223, #29089, #4124 ) ) ;
#7199=ORIENTED_EDGE ( 'NONE', *, *, #25766, .T. ) ;
#7201=FACE_BOUND ( 'NONE', #14502, .T. ) ;
#7204=ORIENTED_EDGE ( 'NONE', *, *, #21473, .F. ) ;
#7205=ORIENTED_EDGE ( 'NONE', *, *, #15341, .F. ) ;
#7207=DIRECTION ( 'NONE',  ( -3.469446951953613696E-16, 0.000000000000000000, -1.000000000000000000 ) ) ;
#7208=CARTESIAN_POINT ( 'NONE',  ( 0.000000000000000000, 3.267716535433071279, 1.850393700787392293 ) ) ;
#7209=ORIENTED_EDGE ( 'NONE', *, *, #20895, .F. ) ;
#7210=EDGE_CURVE ( 'NONE', #10793, #21434, #48803, .T. ) ;
#7211=CARTESIAN_POINT ( 'NONE',  ( -2.454875160333845674, 3.223653470355286377, -0.2239369375554250974 ) ) ;
#7212=ORIENTED_EDGE ( 'NONE', *, *, #20793, .T. ) ;
#7213=LINE ( 'NONE', #18583, #32667 ) ;
#7214=DIRECTION ( 'NONE',  ( -0.000000000000000000, 0.000000000000000000, 1.000000000000000000 ) ) ;
#7215=EDGE_CURVE ( 'NONE', #46654, #16378, #5923, .T. ) ;
#7216=VECTOR ( 'NONE', #1348, 39.37007874015748143 ) ;
#7219=ADVANCED_FACE ( 'NONE', ( #6249 ), #33883, .F. ) ;
#7220=EDGE_LOOP ( 'NONE', ( #26836, #26223, #27133, #40613 ) ) ;
#7221=EDGE_LOOP ( 'NONE', ( #6696, #21794, #19276, #11106 ) ) ;
#7223=DIRECTION ( 'NONE',  ( 0.000000000000000000, -1.000000000000000000, 0.000000000000000000 ) ) ;
#7224=CARTESIAN_POINT ( 'NONE',  ( 1.560669927219590525, 3.346456692913386100, -0.9842519685039348154 ) ) ;
#7228=FACE_OUTER_BOUND ( 'NONE', #17541, .T. ) ;
#7229=DIRECTION ( 'NONE',  ( 1.000000000000000000, 0.000000000000000000, 0.000000000000000000 ) ) ;
#7230=CARTESIAN_POINT ( 'NONE',  ( -0.5455278134075214336, 3.267716535433071279, -1.574803149606293529 ) ) ;
#7233=CARTESIAN_POINT ( 'NONE',  ( -0.6214413264104938772, 3.267716535433071279, 2.156057715732898561E-16 ) ) ;
#7234=CARTESIAN_POINT ( 'NONE',  ( -0.5455278134075214336, 3.346456692913386100, -1.259842519685035134 ) ) ;
#7235=VECTOR ( 'NONE', #17197, 39.37007874015748143 ) ;
#7236=EDGE_LOOP ( 'NONE', ( #46073, #26255, #2571, #47838 ) ) ;
#7240=EDGE_LOOP ( 'NONE', ( #32311, #12957, #13491, #24534 ) ) ;
#7243=VERTEX_POINT ( 'NONE', #1610 ) ;
#7244=DIRECTION ( 'NONE',  ( 0.000000000000000000, 0.000000000000000000, -1.000000000000000000 ) ) ;
#7251=DIRECTION ( 'NONE',  ( 1.000000000000000000, 0.000000000000000000, 0.000000000000000000 ) ) ;
#7257=DIRECTION ( 'NONE',  ( -0.000000000000000000, 0.000000000000000000, 1.000000000000000000 ) ) ;
#7258=VECTOR ( 'NONE', #28901, 39.37007874015748143 ) ;
#7259=ORIENTED_EDGE ( 'NONE', *, *, #19669, .F. ) ;
#7260=PLANE ( 'NONE',  #30330 ) ;
#7261=PLANE ( 'NONE',  #23347 ) ;
#7262=ORIENTED_EDGE ( 'NONE', *, *, #33865, .T. ) ;
#7263=VECTOR ( 'NONE', #20074, 39.37007874015748143 ) ;
#7264=DIRECTION ( 'NONE',  ( -3.469446951953613696E-16, 0.000000000000000000, -1.000000000000000000 ) ) ;
#7266=ORIENTED_EDGE ( 'NONE', *, *, #47229, .F. ) ;
#7269=VECTOR ( 'NONE', #3405, 39.37007874015748143 ) ;
#7271=CARTESIAN_POINT ( 'NONE',  ( 0.5455278134075211005, 3.267716535433071279, -1.456692913385822630 ) ) ;
#7272=LINE ( 'NONE', #23014, #39836 ) ;
#7273=ADVANCED_FACE ( 'NONE', ( #26371 ), #33124, .F. ) ;
#7276=ORIENTED_EDGE ( 'NONE', *, *, #24575, .T. ) ;
#7277=ORIENTED_EDGE ( 'NONE', *, *, #14972, .F. ) ;
#7278=EDGE_CURVE ( 'NONE', #6632, #19367, #49819, .T. ) ;
#7279=DIRECTION ( 'NONE',  ( 1.000000000000000000, 0.000000000000000000, -3.469446951953613696E-16 ) ) ;
#7281=LINE ( 'NONE', #22271, #1879 ) ;
#7282=DIRECTION ( 'NONE',  ( 0.000000000000000000, 1.000000000000000000, 0.000000000000000000 ) ) ;
#7283=VECTOR ( 'NONE', #34555, 39.37007874015748143 ) ;
#7285=PLANE ( 'NONE',  #21150 ) ;
#7286=PLANE ( 'NONE',  #43514 ) ;
#7287=VERTEX_POINT ( 'NONE', #29227 ) ;
#7288=DIRECTION ( 'NONE',  ( -1.000000000000000000, 0.000000000000000000, 0.000000000000000000 ) ) ;
#7290=VECTOR ( 'NONE', #47542, 39.37007874015748143 ) ;
#7291=ORIENTED_EDGE ( 'NONE', *, *, #23341, .T. ) ;
#7292=AXIS2_PLACEMENT_3D ( 'NONE', #43347, #11864, #23996 ) ;
#7293=FACE_OUTER_BOUND ( 'NONE', #33107, .T. ) ;
#7294=LINE ( 'NONE', #34911, #34416 ) ;
#7295=CARTESIAN_POINT ( 'NONE',  ( 0.2727639067037610499, 3.267716535433071279, 1.732283464566921172 ) ) ;
#7296=VERTEX_POINT ( 'NONE', #44961 ) ;
#7297=VECTOR ( 'NONE', #48434, 39.37007874015748143 ) ;
#7298=FACE_OUTER_BOUND ( 'NONE', #26721, .T. ) ;
#7300=PLANE ( 'NONE',  #4059 ) ;
#7301=ORIENTED_EDGE ( 'NONE', *, *, #10806, .T. ) ;
#7302=VECTOR ( 'NONE', #16442, 39.37007874015748143 ) ;
#7306=CARTESIAN_POINT ( 'NONE',  ( -1.909347346926324906, 3.346456692913386100, -1.299212598425193210 ) ) ;
#7308=LINE ( 'NONE', #11431, #20270 ) ;
#7309=EDGE_LOOP ( 'NONE', ( #49828, #43211, #718, #25288 ) ) ;
#7310=EDGE_CURVE ( 'NONE', #1759, #38943, #45207, .T. ) ;
#7311=ORIENTED_EDGE ( 'NONE', *, *, #20561, .T. ) ;
#7314=DIRECTION ( 'NONE',  ( 1.734723475976806848E-16, -0.000000000000000000, 1.000000000000000000 ) ) ;
#7315=EDGE_CURVE ( 'NONE', #17605, #29278, #11880, .T. ) ;
#7316=ORIENTED_EDGE ( 'NONE', *, *, #42078, .T. ) ;
#7317=ORIENTED_EDGE ( 'NONE', *, *, #17402, .F. ) ;
#7318=FACE_OUTER_BOUND ( 'NONE', #26608, .T. ) ;
#7319=LINE ( 'NONE', #23060, #46655 ) ;
#7320=CARTESIAN_POINT ( 'NONE',  ( -0.2727639067037607723, 0.000000000000000000, 0.4724409448818869817 ) ) ;
#7322=EDGE_CURVE ( 'NONE', #5467, #19694, #11382, .T. ) ;
#7323=VERTEX_POINT ( 'NONE', #39252 ) ;
#7324=ORIENTED_EDGE ( 'NONE', *, *, #20107, .T. ) ;
#7325=FACE_OUTER_BOUND ( 'NONE', #23473, .T. ) ;
#7326=DIRECTION ( 'NONE',  ( 1.734723475976806848E-16, 0.000000000000000000, 1.000000000000000000 ) ) ;
#7327=AXIS2_PLACEMENT_3D ( 'NONE', #50182, #6623, #6367 ) ;
#7328=DIRECTION ( 'NONE',  ( 1.000000000000000000, 0.000000000000000000, 0.000000000000000000 ) ) ;
#7329=EDGE_CURVE ( 'NONE', #47752, #46412, #46464, .T. ) ;
#7330=EDGE_LOOP ( 'NONE', ( #21924, #44507, #49002, #48547, #29006 ) ) ;
#7331=DIRECTION ( 'NONE',  ( 0.000000000000000000, 0.000000000000000000, -1.000000000000000000 ) ) ;
#7332=ORIENTED_EDGE ( 'NONE', *, *, #50373, .F. ) ;
#7333=CARTESIAN_POINT ( 'NONE',  ( 0.000000000000000000, 3.346456692913386100, 0.000000000000000000 ) ) ;
#7335=VERTEX_POINT ( 'NONE', #35134 ) ;
#7336=CARTESIAN_POINT ( 'NONE',  ( -0.07591351300297333182, 3.346456692913386100, -0.1574803149606301411 ) ) ;
#7337=CARTESIAN_POINT ( 'NONE',  ( -0.8942052331142552601, 3.267716535433071279, 2.007874015748021268 ) ) ;
#7338=VECTOR ( 'NONE', #25928, 39.37007874015748143 ) ;
#7339=VECTOR ( 'NONE', #6172, 39.37007874015748143 ) ;
#7345=VERTEX_POINT ( 'NONE', #42862 ) ;
#7346=EDGE_CURVE ( 'NONE', #22651, #33992, #35389, .T. ) ;
#7347=AXIS2_PLACEMENT_3D ( 'NONE', #25386, #49850, #17390 ) ;
#7348=ORIENTED_EDGE ( 'NONE', *, *, #50118, .F. ) ;
#7349=CARTESIAN_POINT ( 'NONE',  ( 0.1968503937007878291, 3.346456692913386100, 2.097080421798980687 ) ) ;
#7350=LINE ( 'NONE', #34965, #31689 ) ;
#7352=CARTESIAN_POINT ( 'NONE',  ( 9.902948977032876513E-17, 3.267716535433071279, -1.717887807185943447E-32 ) ) ;
#7353=ORIENTED_EDGE ( 'NONE', *, *, #18990, .T. ) ;
#7355=EDGE_CURVE ( 'NONE', #16989, #33135, #24090, .T. ) ;
#7356=DIRECTION ( 'NONE',  ( 1.000000000000000000, 0.000000000000000000, -3.469446951953613696E-16 ) ) ;
#7357=EDGE_LOOP ( 'NONE', ( #46284, #22099, #24070, #34534 ) ) ;
#7358=LINE ( 'NONE', #38850, #50399 ) ;
#7359=DIRECTION ( 'NONE',  ( 1.734723475976806848E-16, -0.000000000000000000, 1.000000000000000000 ) ) ;
#7361=FACE_OUTER_BOUND ( 'NONE', #21589, .T. ) ;
#7362=LINE ( 'NONE', #23601, #29964 ) ;
#7364=ORIENTED_EDGE ( 'NONE', *, *, #39375, .F. ) ;
#7365=CARTESIAN_POINT ( 'NONE',  ( -0.2727639067037602172, 0.000000000000000000, 1.732283464566921172 ) ) ;
#7366=ORIENTED_EDGE ( 'NONE', *, *, #49012, .T. ) ;
#7367=LINE ( 'NONE', #23108, #19571 ) ;
#7370=CARTESIAN_POINT ( 'NONE',  ( 0.1968503937007871074, 3.267716535433071279, -6.829619984160646953E-17 ) ) ;
#7371=VECTOR ( 'NONE', #15613, 39.37007874015748143 ) ;
#7372=ORIENTED_EDGE ( 'NONE', *, *, #40594, .F. ) ;
#7373=ORIENTED_EDGE ( 'NONE', *, *, #5620, .T. ) ;
#7374=CARTESIAN_POINT ( 'NONE',  ( -0.2727639067037607723, 0.000000000000000000, 0.4724409448818869817 ) ) ;
#7375=DIRECTION ( 'NONE',  ( -1.000000000000000000, 0.000000000000000000, 1.734723475976806848E-16 ) ) ;
#7376=EDGE_CURVE ( 'NONE', #15755, #49388, #23248, .T. ) ;
#7377=LINE ( 'NONE', #43229, #49704 ) ;
#7379=AXIS2_PLACEMENT_3D ( 'NONE', #7043, #27404, #22789 ) ;
#7382=PLANE ( 'NONE',  #29745 ) ;
#7384=EDGE_CURVE ( 'NONE', #43635, #22497, #23007, .T. ) ;
#7386=LINE ( 'NONE', #7134, #47152 ) ;
#7389=ORIENTED_EDGE ( 'NONE', *, *, #7697, .T. ) ;
#7391=ORIENTED_EDGE ( 'NONE', *, *, #13146, .F. ) ;
#7394=VECTOR ( 'NONE', #40160, 39.37007874015748143 ) ;
#7396=VERTEX_POINT ( 'NONE', #50076 ) ;
#7397=DIRECTION ( 'NONE',  ( -3.469446951953613696E-16, 0.000000000000000000, -1.000000000000000000 ) ) ;
#7400=LINE ( 'NONE', #42998, #36154 ) ;
#7402=PLANE ( 'NONE',  #25901 ) ;
#7403=AXIS2_PLACEMENT_3D ( 'NONE', #14196, #34082, #29947 ) ;
#7404=EDGE_CURVE ( 'NONE', #45000, #27097, #45514, .T. ) ;
#7406=DIRECTION ( 'NONE',  ( 0.000000000000000000, 0.000000000000000000, -1.000000000000000000 ) ) ;
#7409=CARTESIAN_POINT ( 'NONE',  ( 0.000000000000000000, 3.267716535433071279, -6.146657985744592735E-16 ) ) ;
#7410=CARTESIAN_POINT ( 'NONE',  ( -0.8182917201112819283, 0.000000000000000000, -0.1574803149606301411 ) ) ;
#7411=AXIS2_PLACEMENT_3D ( 'NONE', #18358, #45946, #34369 ) ;
#7412=DIRECTION ( 'NONE',  ( -3.469446951953613696E-16, 0.000000000000000000, -1.000000000000000000 ) ) ;
#7415=ORIENTED_EDGE ( 'NONE', *, *, #49599, .T. ) ;
#7416=CARTESIAN_POINT ( 'NONE',  ( 1.560669927219590747, 3.346456692913386100, 0.1574803149606283648 ) ) ;
#7418=VERTEX_POINT ( 'NONE', #50316 ) ;
#7421=EDGE_CURVE ( 'NONE', #14850, #9971, #3380, .T. ) ;
#7423=ORIENTED_EDGE ( 'NONE', *, *, #31093, .T. ) ;
#7424=CARTESIAN_POINT ( 'NONE',  ( -0.2727639067037608278, 0.000000000000000000, -0.03937007874015908959 ) ) ;
#7425=EDGE_CURVE ( 'NONE', #4026, #48864, #46712, .T. ) ;
#7427=LINE ( 'NONE', #31177, #29219 ) ;
#7429=ORIENTED_EDGE ( 'NONE', *, *, #47549, .F. ) ;
#7431=ORIENTED_EDGE ( 'NONE', *, *, #48755, .T. ) ;
#7432=ORIENTED_EDGE ( 'NONE', *, *, #15908, .F. ) ;
#7434=ORIENTED_EDGE ( 'NONE', *, *, #40449, .F. ) ;
#7436=CARTESIAN_POINT ( 'NONE',  ( -1.636583440222564301, 3.267716535433071279, -1.259842519685034468 ) ) ;
#7439=DIRECTION ( 'NONE',  ( -0.000000000000000000, 1.000000000000000000, -0.000000000000000000 ) ) ;
#7441=VERTEX_POINT ( 'NONE', #8524 ) ;
#7442=CYLINDRICAL_SURFACE ( 'NONE', #2648, 2.106299212598425008 ) ;
#7443=EDGE_CURVE ( 'NONE', #41084, #12747, #524, .T. ) ;
#7445=EDGE_LOOP ( 'NONE', ( #18188, #11432, #12901, #657 ) ) ;
#7446=FACE_OUTER_BOUND ( 'NONE', #27167, .T. ) ;
#7447=EDGE_LOOP ( 'NONE', ( #11875, #14325, #46459, #50683 ) ) ;
#7449=CARTESIAN_POINT ( 'NONE',  ( -1.166969139818016199, 0.000000000000000000, -1.929133858267710000 ) ) ;
#7450=ORIENTED_EDGE ( 'NONE', *, *, #735, .T. ) ;
#7452=DIRECTION ( 'NONE',  ( -0.000000000000000000, 1.000000000000000000, -0.000000000000000000 ) ) ;
#7453=DIRECTION ( 'NONE',  ( 1.000000000000000000, 0.000000000000000000, 0.000000000000000000 ) ) ;
#7455=DIRECTION ( 'NONE',  ( -0.000000000000000000, 1.000000000000000000, -0.000000000000000000 ) ) ;
#7458=PLANE ( 'NONE',  #4416 ) ;
#7459=EDGE_CURVE ( 'NONE', #18552, #35065, #12145, .T. ) ;
#7460=DIRECTION ( 'NONE',  ( 1.734723475976806848E-16, 0.000000000000000000, 1.000000000000000000 ) ) ;
#7464=APPLICATION_CONTEXT ( 'automotive_design' ) ;
#7466=CARTESIAN_POINT ( 'NONE',  ( -1.166969139818015977, 0.000000000000000000, -0.7874015748031470974 ) ) ;
#7467=FACE_OUTER_BOUND ( 'NONE', #44777, .T. ) ;
#7468=CARTESIAN_POINT ( 'NONE',  ( -1.712496953225537411, 3.267716535433071279, 5.941417334598190051E-16 ) ) ;
#7469=EDGE_CURVE ( 'NONE', #23187, #8950, #39763, .T. ) ;
#7471=VECTOR ( 'NONE', #44031, 39.37007874015748143 ) ;
#7472=AXIS2_PLACEMENT_3D ( 'NONE', #14811, #11686, #34685 ) ;
#7473=EDGE_CURVE ( 'NONE', #17100, #21759, #12920, .T. ) ;
#7474=CARTESIAN_POINT ( 'NONE',  ( -2.454875160333845674, 3.189042514953126961, -0.3543307086614173040 ) ) ;
#7477=VERTEX_POINT ( 'NONE', #27881 ) ;
#7478=DIRECTION ( 'NONE',  ( 1.734723475976806848E-16, 0.000000000000000000, 1.000000000000000000 ) ) ;
#7479=VECTOR ( 'NONE', #47907, 39.37007874015748143 ) ;
#7482=LINE ( 'NONE', #46933, #37421 ) ;
#7484=VERTEX_POINT ( 'NONE', #16012 ) ;
#7485=EDGE_CURVE ( 'NONE', #37048, #47504, #4656, .T. ) ;
#7487=DIRECTION ( 'NONE',  ( 1.000000000000000000, 0.000000000000000000, -3.469446951953613696E-16 ) ) ;
#7488=ORIENTED_EDGE ( 'NONE', *, *, #29260, .T. ) ;
#7489=CARTESIAN_POINT ( 'NONE',  ( -0.2727639067037602727, 3.346456692913386100, 0.9055118110236167750 ) ) ;
#7490=ORIENTED_EDGE ( 'NONE', *, *, #42857, .F. ) ;
#7495=EDGE_CURVE ( 'NONE', #7692, #6991, #32286, .T. ) ;
#7496=ORIENTED_EDGE ( 'NONE', *, *, #27487, .T. ) ;
#7497=CARTESIAN_POINT ( 'NONE',  ( -1.712496953225537188, 3.267716535433071279, -0.1574803149606297248 ) ) ;
#7498=VERTEX_POINT ( 'NONE', #44139 ) ;
#7502=DIRECTION ( 'NONE',  ( 1.000000000000000000, 0.000000000000000000, 0.000000000000000000 ) ) ;
#7506=VECTOR ( 'NONE', #20966, 39.37007874015748143 ) ;
#7507=PLANE ( 'NONE',  #47605 ) ;
#7512=ORIENTED_EDGE ( 'NONE', *, *, #5679, .F. ) ;
#7513=VECTOR ( 'NONE', #42355, 39.37007874015748143 ) ;
#7515=DIRECTION ( 'NONE',  ( 1.000000000000000000, 0.000000000000000000, 0.000000000000000000 ) ) ;
#7516=VECTOR ( 'NONE', #31936, 39.37007874015748143 ) ;
#7517=DIRECTION ( 'NONE',  ( 1.000000000000000000, 0.000000000000000000, 0.000000000000000000 ) ) ;
#7518=DIRECTION ( 'NONE',  ( 1.000000000000000000, 0.000000000000000000, 0.000000000000000000 ) ) ;
#7519=CARTESIAN_POINT ( 'NONE',  ( 0.000000000000000000, 3.267716535433071279, 0.000000000000000000 ) ) ;
#7520=ORIENTED_EDGE ( 'NONE', *, *, #33139, .F. ) ;
#7522=CARTESIAN_POINT ( 'NONE',  ( 0.2727639067037602172, 3.267716535433071279, -2.244094488188969727 ) ) ;
#7523=DIRECTION ( 'NONE',  ( -0.000000000000000000, 1.000000000000000000, -0.000000000000000000 ) ) ;
#7524=ORIENTED_EDGE ( 'NONE', *, *, #4583, .F. ) ;
#7525=CARTESIAN_POINT ( 'NONE',  ( -1.363819533518803473, 0.000000000000000000, 2.047244094488179567 ) ) ;
#7526=PLANE ( 'NONE',  #11119 ) ;
#7527=EDGE_CURVE ( 'NONE', #36336, #46441, #36668, .T. ) ;
#7528=EDGE_CURVE ( 'NONE', #4542, #35067, #11738, .T. ) ;
#7529=CARTESIAN_POINT ( 'NONE',  ( 0.000000000000000000, 3.267716535433071279, 0.000000000000000000 ) ) ;
#7531=CARTESIAN_POINT ( 'NONE',  ( 1.909347346926324684, 3.267716535433071279, 1.102362204724403938 ) ) ;
#7532=LINE ( 'NONE', #45990, #17997 ) ;
#7533=EDGE_LOOP ( 'NONE', ( #32206, #19321, #34891, #42182 ) ) ;
#7534=CARTESIAN_POINT ( 'NONE',  ( 1.363819533518803251, 3.346456692913386100, 0.2755905511810996522 ) ) ;
#7535=LINE ( 'NONE', #23275, #19433 ) ;
#7536=VECTOR ( 'NONE', #16950, 39.37007874015748143 ) ;
#7537=ORIENTED_EDGE ( 'NONE', *, *, #8663, .T. ) ;
#7539=CARTESIAN_POINT ( 'NONE',  ( -2.097080421798980687, 3.346456692913386100, -0.1968503937007880511 ) ) ;
#7541=DIRECTION ( 'NONE',  ( -0.000000000000000000, 1.000000000000000000, -0.000000000000000000 ) ) ;
#7545=ORIENTED_EDGE ( 'NONE', *, *, #33311, .T. ) ;
#7546=FACE_OUTER_BOUND ( 'NONE', #14457, .T. ) ;
#7548=EDGE_CURVE ( 'NONE', #29935, #15133, #40286, .T. ) ;
#7551=ORIENTED_EDGE ( 'NONE', *, *, #31581, .T. ) ;
#7552=VECTOR ( 'NONE', #31605, 39.37007874015748143 ) ;
#7553=CARTESIAN_POINT ( 'NONE',  ( 0.2727639067037610499, 0.000000000000000000, 1.102362204724404160 ) ) ;
#7556=DIRECTION ( 'NONE',  ( -0.000000000000000000, 1.000000000000000000, -0.000000000000000000 ) ) ;
#7557=EDGE_CURVE ( 'NONE', #39081, #9101, #28905, .T. ) ;
#7558=VERTEX_POINT ( 'NONE', #23761 ) ;
#7559=ORIENTED_EDGE ( 'NONE', *, *, #25261, .T. ) ;
#7563=EDGE_CURVE ( 'NONE', #20150, #30476, #19870, .T. ) ;
#7564=VERTEX_POINT ( 'NONE', #37186 ) ;
#7565=ORIENTED_EDGE ( 'NONE', *, *, #43024, .F. ) ;
#7566=PLANE ( 'NONE',  #33070 ) ;
#7567=CARTESIAN_POINT ( 'NONE',  ( 1.560669927219590747, 3.346456692913386100, -0.7874015748031473194 ) ) ;
#7568=CARTESIAN_POINT ( 'NONE',  ( -1.536664496436148184E-16, 3.346456692913386100, 0.1181102362204701633 ) ) ;
#7569=ADVANCED_FACE ( 'NONE', ( #29428 ), #25298, .F. ) ;
#7570=EDGE_LOOP ( 'NONE', ( #24201, #32730, #30048, #11757 ) ) ;
#7571=VERTEX_POINT ( 'NONE', #1802 ) ;
#7572=CARTESIAN_POINT ( 'NONE',  ( 2.059322335531026837, 3.346456692913386100, -0.6692913385826764205 ) ) ;
#7573=DIRECTION ( 'NONE',  ( -1.000000000000000000, -0.000000000000000000, -0.000000000000000000 ) ) ;
#7574=LINE ( 'NONE', #19687, #17943 ) ;
#7575=ORIENTED_EDGE ( 'NONE', *, *, #26322, .F. ) ;
#7577=ORIENTED_EDGE ( 'NONE', *, *, #27685, .F. ) ;
#7579=ORIENTED_EDGE ( 'NONE', *, *, #20305, .F. ) ;
#7580=EDGE_LOOP ( 'NONE', ( #49385, #34554, #24325, #6697 ) ) ;
#7582=LINE ( 'NONE', #26691, #25866 ) ;
#7583=VECTOR ( 'NONE', #33905, 39.37007874015748143 ) ;
#7585=VECTOR ( 'NONE', #42431, 39.37007874015748143 ) ;
#7589=EDGE_LOOP ( 'NONE', ( #35385, #19970, #16934, #11085 ) ) ;
#7590=VECTOR ( 'NONE', #37936, 39.37007874015748143 ) ;
#7592=VERTEX_POINT ( 'NONE', #45148 ) ;
#7593=DIRECTION ( 'NONE',  ( 0.000000000000000000, -1.000000000000000000, 0.000000000000000000 ) ) ;
#7594=DIRECTION ( 'NONE',  ( 1.000000000000000000, 0.000000000000000000, 0.000000000000000000 ) ) ;
#7595=VECTOR ( 'NONE', #40567, 39.37007874015748143 ) ;
#7596=EDGE_CURVE ( 'NONE', #9369, #9748, #17554, .T. ) ;
#7597=PLANE ( 'NONE',  #13825 ) ;
#7599=EDGE_LOOP ( 'NONE', ( #38048, #10678, #20373 ) ) ;
#7600=EDGE_CURVE ( 'NONE', #24676, #34367, #25043, .T. ) ;
#7602=LINE ( 'NONE', #23092, #25683 ) ;
#7606=DIRECTION ( 'NONE',  ( -0.000000000000000000, 1.000000000000000000, -0.000000000000000000 ) ) ;
#7607=LINE ( 'NONE', #18973, #4063 ) ;
#7608=CARTESIAN_POINT ( 'NONE',  ( 0.2727639067037609943, 3.346456692913386100, 1.535433070866133898 ) ) ;
#7609=DIRECTION ( 'NONE',  ( 1.734723475976806848E-16, -0.000000000000000000, 1.000000000000000000 ) ) ;
#7610=FACE_OUTER_BOUND ( 'NONE', #25668, .T. ) ;
#7611=ORIENTED_EDGE ( 'NONE', *, *, #5634, .T. ) ;
#7612=CARTESIAN_POINT ( 'NONE',  ( -1.636583440222563635, 3.346456692913386100, 0.9448818897637749625 ) ) ;
#7613=ORIENTED_EDGE ( 'NONE', *, *, #14616, .T. ) ;
#7617=EDGE_CURVE ( 'NONE', #35577, #26630, #10063, .T. ) ;
#7618=DIRECTION ( 'NONE',  ( 1.000000000000000000, 0.000000000000000000, 0.000000000000000000 ) ) ;
#7619=CIRCLE ( 'NONE', #36488, 2.165354330708661568 ) ;
#7621=ORIENTED_EDGE ( 'NONE', *, *, #4111, .F. ) ;
#7622=DIRECTION ( 'NONE',  ( -1.000000000000000000, 0.000000000000000000, 0.000000000000000000 ) ) ;
#7623=LINE ( 'NONE', #47328, #25451 ) ;
#7625=EDGE_CURVE ( 'NONE', #25938, #17945, #21684, .T. ) ;
#7628=DIRECTION ( 'NONE',  ( -1.000000000000000000, 0.000000000000000000, 0.000000000000000000 ) ) ;
#7629=CARTESIAN_POINT ( 'NONE',  ( -0.2727639067037608278, 3.267716535433071279, -0.03937007874015908959 ) ) ;
#7630=CARTESIAN_POINT ( 'NONE',  ( 1.363819533518803029, 3.346456692913386100, -1.102362204724405714 ) ) ;
#7631=VECTOR ( 'NONE', #37138, 39.37007874015748143 ) ;
#7633=AXIS2_PLACEMENT_3D ( 'NONE', #5945, #10080, #6711 ) ;
#7634=ORIENTED_EDGE ( 'NONE', *, *, #41930, .T. ) ;
#7637=CARTESIAN_POINT ( 'NONE',  ( -2.182111253630085290, 3.267716535433071279, -0.1968503937007880511 ) ) ;
#7638=ORIENTED_EDGE ( 'NONE', *, *, #38082, .T. ) ;
#7639=CARTESIAN_POINT ( 'NONE',  ( 1.015142113812069979, 3.346456692913386100, 1.417322834645662777 ) ) ;
#7640=ORIENTED_EDGE ( 'NONE', *, *, #27711, .F. ) ;
#7643=ORIENTED_EDGE ( 'NONE', *, *, #43693, .T. ) ;
#7644=VERTEX_POINT ( 'NONE', #1551 ) ;
#7646=ORIENTED_EDGE ( 'NONE', *, *, #12257, .F. ) ;
#7647=CARTESIAN_POINT ( 'NONE',  ( 1.015142113812069313, 3.267716535433071279, -1.299212598425193210 ) ) ;
#7648=DIRECTION ( 'NONE',  ( 1.734723475976806848E-16, -0.000000000000000000, 1.000000000000000000 ) ) ;
#7649=CARTESIAN_POINT ( 'NONE',  ( -0.2727639067037611054, 3.346456692913386100, -2.244094488188968395 ) ) ;
#7651=VECTOR ( 'NONE', #24663, 39.37007874015748143 ) ;
#7653=FACE_OUTER_BOUND ( 'NONE', #18067, .T. ) ;
#7654=VERTEX_POINT ( 'NONE', #45652 ) ;
#7655=EDGE_CURVE ( 'NONE', #42444, #5670, #44898, .T. ) ;
#7656=CARTESIAN_POINT ( 'NONE',  ( -1.712496953225537633, 3.346456692913386100, 1.417322834645662333 ) ) ;
#7658=CARTESIAN_POINT ( 'NONE',  ( 4.268512490100411402E-16, 3.267716535433071279, 1.259842519685033357 ) ) ;
#7660=VECTOR ( 'NONE', #37957, 39.37007874015748143 ) ;
#7661=AXIS2_PLACEMENT_3D ( 'NONE', #37459, #14201, #33333 ) ;
#7663=DIRECTION ( 'NONE',  ( -1.000000000000000000, 0.000000000000000000, 0.000000000000000000 ) ) ;
#7665=PLANE ( 'NONE',  #13742 ) ;
#7667=DIRECTION ( 'NONE',  ( 1.734723475976806848E-16, -0.000000000000000000, 1.000000000000000000 ) ) ;
#7668=EDGE_CURVE ( 'NONE', #20338, #38076, #37699, .T. ) ;
#7670=VECTOR ( 'NONE', #46114, 39.37007874015748143 ) ;
#7671=CARTESIAN_POINT ( 'NONE',  ( -0.5455278134075208785, 0.000000000000000000, 0.4330708661417290162 ) ) ;
#7672=ORIENTED_EDGE ( 'NONE', *, *, #49775, .F. ) ;
#7673=DIRECTION ( 'NONE',  ( -0.000000000000000000, 1.000000000000000000, -0.000000000000000000 ) ) ;
#7674=CARTESIAN_POINT ( 'NONE',  ( 1.091055626815042645, 3.346456692913386100, 0.6299212598425161236 ) ) ;
#7677=DIRECTION ( 'NONE',  ( -0.000000000000000000, 0.000000000000000000, 1.000000000000000000 ) ) ;
#7678=VERTEX_POINT ( 'NONE', #49261 ) ;
#7679=ORIENTED_EDGE ( 'NONE', *, *, #17911, .F. ) ;
#7681=DIRECTION ( 'NONE',  ( 1.734723475976806848E-16, -0.000000000000000000, 1.000000000000000000 ) ) ;
#7684=CARTESIAN_POINT ( 'NONE',  ( -2.043170538425928662, 3.346456692913386100, -0.5118110236220464460 ) ) ;
#7686=ORIENTED_EDGE ( 'NONE', *, *, #44788, .F. ) ;
#7687=PLANE ( 'NONE',  #8285 ) ;
#7688=VERTEX_POINT ( 'NONE', #25549 ) ;
#7689=EDGE_CURVE ( 'NONE', #30948, #29664, #13941, .T. ) ;
#7690=LINE ( 'NONE', #42799, #23235 ) ;
#7692=VERTEX_POINT ( 'NONE', #14443 ) ;
#7694=DIRECTION ( 'NONE',  ( 0.000000000000000000, 0.000000000000000000, -1.000000000000000000 ) ) ;
#7695=VECTOR ( 'NONE', #28748, 39.37007874015748143 ) ;
#7697=EDGE_CURVE ( 'NONE', #34149, #13984, #30191, .T. ) ;
#7698=AXIS2_PLACEMENT_3D ( 'NONE', #12659, #20403, #20658 ) ;
#7700=CARTESIAN_POINT ( 'NONE',  ( 1.091055626815042645, 3.267716535433071279, 0.3149606299212578953 ) ) ;
#7703=LINE ( 'NONE', #42811, #1019 ) ;
#7704=VECTOR ( 'NONE', #19148, 39.37007874015748143 ) ;
#7706=VERTEX_POINT ( 'NONE', #13427 ) ;
#7707=LINE ( 'NONE', #51015, #35272 ) ;
#7711=DIRECTION ( 'NONE',  ( -3.469446951953613696E-16, 0.000000000000000000, -1.000000000000000000 ) ) ;
#7713=VERTEX_POINT ( 'NONE', #14946 ) ;
#7714=FACE_OUTER_BOUND ( 'NONE', #5512, .T. ) ;
#7715=DIRECTION ( 'NONE',  ( -1.000000000000000000, 0.000000000000000000, 0.000000000000000000 ) ) ;
#7716=DIRECTION ( 'NONE',  ( 1.000000000000000000, 0.000000000000000000, 0.000000000000000000 ) ) ;
#7719=EDGE_CURVE ( 'NONE', #45211, #50302, #17536, .T. ) ;
#7720=DIRECTION ( 'NONE',  ( 0.000000000000000000, -1.000000000000000000, 0.000000000000000000 ) ) ;
#7721=EDGE_LOOP ( 'NONE', ( #50629, #44839, #30146, #42831 ) ) ;
#7722=ADVANCED_FACE ( 'NONE', ( #38453 ), #50261, .F. ) ;
#7723=CARTESIAN_POINT ( 'NONE',  ( 0.000000000000000000, 3.267716535433071279, 0.000000000000000000 ) ) ;
#7726=CARTESIAN_POINT ( 'NONE',  ( 0.2727639067037602172, 0.000000000000000000, -1.732283464566922726 ) ) ;
#7728=ORIENTED_EDGE ( 'NONE', *, *, #11383, .F. ) ;
#7730=ORIENTED_EDGE ( 'NONE', *, *, #9136, .T. ) ;
#7732=VECTOR ( 'NONE', #4365, 39.37007874015748143 ) ;
#7733=CARTESIAN_POINT ( 'NONE',  ( -2.258024766633058622, 0.000000000000000000, 0.1574803149606286423 ) ) ;
#7734=ORIENTED_EDGE ( 'NONE', *, *, #5054, .F. ) ;
#7736=CARTESIAN_POINT ( 'NONE',  ( 0.000000000000000000, 3.267716535433071279, -0.3543307086614175816 ) ) ;
#7738=PLANE ( 'NONE',  #31176 ) ;
#7739=VERTEX_POINT ( 'NONE', #50506 ) ;
#7741=LINE ( 'NONE', #8256, #46187 ) ;
#7742=ADVANCED_FACE ( 'NONE', ( #30698 ), #34819, .F. ) ;
#7743=ORIENTED_EDGE ( 'NONE', *, *, #14506, .T. ) ;
#7744=CARTESIAN_POINT ( 'NONE',  ( -0.6214413264104940993, 3.267716535433071279, 2.156057715732899547E-16 ) ) ;
#7745=ORIENTED_EDGE ( 'NONE', *, *, #33854, .F. ) ;
#7746=ORIENTED_EDGE ( 'NONE', *, *, #2141, .F. ) ;
#7749=FACE_OUTER_BOUND ( 'NONE', #44443, .T. ) ;
#7752=EDGE_CURVE ( 'NONE', #19355, #23628, #18824, .T. ) ;
#7754=DIRECTION ( 'NONE',  ( -3.469446951953613696E-16, 0.000000000000000000, -1.000000000000000000 ) ) ;
#7755=ADVANCED_FACE ( 'NONE', ( #22948 ), #42307, .F. ) ;
#7756=EDGE_LOOP ( 'NONE', ( #576, #38498, #14120, #5630 ) ) ;
#7758=VECTOR ( 'NONE', #28539, 39.37007874015748143 ) ;
#7760=ORIENTED_EDGE ( 'NONE', *, *, #36473, .T. ) ;
#7762=ORIENTED_EDGE ( 'NONE', *, *, #8355, .T. ) ;
#7763=VECTOR ( 'NONE', #37043, 39.37007874015748143 ) ;
#7764=ORIENTED_EDGE ( 'NONE', *, *, #36020, .F. ) ;
#7765=EDGE_CURVE ( 'NONE', #42413, #39696, #11326, .T. ) ;
#7767=VECTOR ( 'NONE', #38724, 39.37007874015748143 ) ;
#7768=LINE ( 'NONE', #35394, #16776 ) ;
#7769=CARTESIAN_POINT ( 'NONE',  ( 2.017116292511733633, 3.346456692913386100, 0.7874015748031456541 ) ) ;
#7770=FACE_OUTER_BOUND ( 'NONE', #13531, .T. ) ;
#7771=VERTEX_POINT ( 'NONE', #23189 ) ;
#7772=ORIENTED_EDGE ( 'NONE', *, *, #34386, .F. ) ;
#7774=DIRECTION ( 'NONE',  ( -0.000000000000000000, 1.000000000000000000, -0.000000000000000000 ) ) ;
#7776=VERTEX_POINT ( 'NONE', #38702 ) ;
#7777=DIRECTION ( 'NONE',  ( -1.000000000000000000, 0.000000000000000000, 0.000000000000000000 ) ) ;
#7779=DIRECTION ( 'NONE',  ( 1.734723475976806848E-16, -0.000000000000000000, 1.000000000000000000 ) ) ;
#7780=EDGE_CURVE ( 'NONE', #46932, #8029, #7703, .T. ) ;
#7783=FACE_OUTER_BOUND ( 'NONE', #20573, .T. ) ;
#7784=LINE ( 'NONE', #28613, #10591 ) ;
#7786=EDGE_CURVE ( 'NONE', #20580, #912, #22446, .T. ) ;
#7787=LINE ( 'NONE', #27648, #47281 ) ;
#7788=DIRECTION ( 'NONE',  ( -0.000000000000000000, 1.000000000000000000, -0.000000000000000000 ) ) ;
#7791=FACE_OUTER_BOUND ( 'NONE', #43242, .T. ) ;
#7792=LINE ( 'NONE', #12171, #2277 ) ;
#7796=ORIENTED_EDGE ( 'NONE', *, *, #10349, .F. ) ;
#7797=VECTOR ( 'NONE', #4931, 39.37007874015748143 ) ;
#7799=ORIENTED_EDGE ( 'NONE', *, *, #50183, .F. ) ;
#7801=VECTOR ( 'NONE', #8699, 39.37007874015748143 ) ;
#7802=ORIENTED_EDGE ( 'NONE', *, *, #1102, .T. ) ;
#7803=VECTOR ( 'NONE', #1452, 39.37007874015748143 ) ;
#7806=CARTESIAN_POINT ( 'NONE',  ( -1.909347346926324462, 3.267716535433071279, 1.102362204724404160 ) ) ;
#7808=ORIENTED_EDGE ( 'NONE', *, *, #11920, .F. ) ;
#7809=ORIENTED_EDGE ( 'NONE', *, *, #30209, .F. ) ;
#7810=CARTESIAN_POINT ( 'NONE',  ( 0.000000000000000000, 3.267716535433071279, 0.000000000000000000 ) ) ;
#7812=CARTESIAN_POINT ( 'NONE',  ( 1.363819533518803251, 3.346456692913386100, -0.6692913385826764205 ) ) ;
#7814=ORIENTED_EDGE ( 'NONE', *, *, #42838, .F. ) ;
#7816=DIRECTION ( 'NONE',  ( 1.000000000000000000, 0.000000000000000000, 0.000000000000000000 ) ) ;
#7817=CARTESIAN_POINT ( 'NONE',  ( -1.636583440222564301, 3.346456692913386100, -1.456692913385822186 ) ) ;
#7818=ORIENTED_EDGE ( 'NONE', *, *, #8208, .F. ) ;
#7820=EDGE_CURVE ( 'NONE', #46097, #43386, #14215, .T. ) ;
#7821=CARTESIAN_POINT ( 'NONE',  ( 2.021817418930639931, 3.267716535433071279, 0.5905511811023582691 ) ) ;
#7822=CARTESIAN_POINT ( 'NONE',  ( 0.5455278134075212115, 3.267716535433071279, -9.463399047163220715E-17 ) ) ;
#7823=LINE ( 'NONE', #8076, #50022 ) ;
#7825=VERTEX_POINT ( 'NONE', #38205 ) ;
#7826=CARTESIAN_POINT ( 'NONE',  ( -1.091055626815042645, 3.346456692913386100, -0.3149606299212593941 ) ) ;
#7828=CARTESIAN_POINT ( 'NONE',  ( 0.4696143004045484348, 0.000000000000000000, 1.535433070866133898 ) ) ;
#7829=ORIENTED_EDGE ( 'NONE', *, *, #38413, .T. ) ;
#7830=CARTESIAN_POINT ( 'NONE',  ( 1.091055626815043311, 3.267716535433071279, 1.377952755905504256 ) ) ;
#7831=ORIENTED_EDGE ( 'NONE', *, *, #34026, .F. ) ;
#7832=ORIENTED_EDGE ( 'NONE', *, *, #23387, .F. ) ;
#7835=CARTESIAN_POINT ( 'NONE',  ( 0.4696143004045478797, 3.267716535433071279, -0.03937007874015908959 ) ) ;
#7836=CARTESIAN_POINT ( 'NONE',  ( -0.8182917201112817063, 3.267716535433071279, 1.419509857074483046E-16 ) ) ;
#7837=CARTESIAN_POINT ( 'NONE',  ( 1.909347346926324684, 3.346456692913386100, 0.5905511811023582691 ) ) ;
#7840=VECTOR ( 'NONE', #16005, 39.37007874015748143 ) ;
#7841=VECTOR ( 'NONE', #50281, 39.37007874015748143 ) ;
#7842=EDGE_CURVE ( 'NONE', #9971, #34006, #15701, .T. ) ;
#7843=ORIENTED_EDGE ( 'NONE', *, *, #13485, .F. ) ;
#7844=CARTESIAN_POINT ( 'NONE',  ( -0.2727639067037602172, 3.346456692913386100, 1.417322834645662777 ) ) ;
#7846=AXIS2_PLACEMENT_3D ( 'NONE', #29336, #45068, #33488 ) ;
#7847=EDGE_CURVE ( 'NONE', #19800, #3259, #34332, .T. ) ;
#7848=EDGE_CURVE ( 'NONE', #27397, #12593, #22694, .T. ) ;
#7851=VECTOR ( 'NONE', #30359, 39.37007874015748143 ) ;
#7852=ORIENTED_EDGE ( 'NONE', *, *, #49180, .T. ) ;
#7857=ORIENTED_EDGE ( 'NONE', *, *, #35304, .F. ) ;
#7859=CARTESIAN_POINT ( 'NONE',  ( -1.909347346926324462, 3.346456692913386100, 0.4724409448818871482 ) ) ;
#7860=ORIENTED_EDGE ( 'NONE', *, *, #48881, .T. ) ;
#7861=DIRECTION ( 'NONE',  ( 0.000000000000000000, 0.000000000000000000, 1.000000000000000000 ) ) ;
#7862=DIRECTION ( 'NONE',  ( 1.000000000000000000, 0.000000000000000000, -3.469446951953613696E-16 ) ) ;
#7863=CARTESIAN_POINT ( 'NONE',  ( -0.8942052331142551491, 3.267716535433071279, 3.102397620449222974E-16 ) ) ;
#7864=EDGE_LOOP ( 'NONE', ( #16020, #39466 ) ) ;
#7865=LINE ( 'NONE', #47318, #8183 ) ;
#7867=LINE ( 'NONE', #11241, #16307 ) ;
#7868=PLANE ( 'NONE',  #23494 ) ;
#7871=ORIENTED_EDGE ( 'NONE', *, *, #39283, .T. ) ;
#7872=DIRECTION ( 'NONE',  ( -1.000000000000000000, -0.000000000000000000, -0.000000000000000000 ) ) ;
#7873=VECTOR ( 'NONE', #38404, 39.37007874015748143 ) ;
#7874=LINE ( 'NONE', #23621, #13926 ) ;
#7875=AXIS2_PLACEMENT_3D ( 'NONE', #46814, #38607, #34233 ) ;
#7876=ORIENTED_EDGE ( 'NONE', *, *, #9113, .T. ) ;
#7877=DIRECTION ( 'NONE',  ( -3.469446951953613696E-16, 0.000000000000000000, -1.000000000000000000 ) ) ;
#7878=FACE_OUTER_BOUND ( 'NONE', #50725, .T. ) ;
#7879=CARTESIAN_POINT ( 'NONE',  ( -0.8942052331142552601, 3.346456692913386100, 1.889763779527550147 ) ) ;
#7880=VECTOR ( 'NONE', #28946, 39.37007874015748143 ) ;
#7881=DIRECTION ( 'NONE',  ( -0.000000000000000000, 0.000000000000000000, 1.000000000000000000 ) ) ;
#7883=ORIENTED_EDGE ( 'NONE', *, *, #19205, .T. ) ;
#7884=PLANE ( 'NONE',  #5962 ) ;
#7886=DIRECTION ( 'NONE',  ( 1.734723475976806848E-16, -0.000000000000000000, 1.000000000000000000 ) ) ;
#7887=EDGE_CURVE ( 'NONE', #34340, #30894, #47923, .T. ) ;
#7888=VECTOR ( 'NONE', #34428, 39.37007874015748143 ) ;
#7890=EDGE_CURVE ( 'NONE', #50120, #42995, #23959, .T. ) ;
#7892=ORIENTED_EDGE ( 'NONE', *, *, #13702, .F. ) ;
#7893=ORIENTED_EDGE ( 'NONE', *, *, #46858, .T. ) ;
#7895=EDGE_CURVE ( 'NONE', #40070, #3116, #39967, .T. ) ;
#7896=ORIENTED_EDGE ( 'NONE', *, *, #13694, .F. ) ;
#7897=ORIENTED_EDGE ( 'NONE', *, *, #19589, .T. ) ;
#7898=CARTESIAN_POINT ( 'NONE',  ( 2.106333035502527373, 3.267716535433071279, 0.006892066987321476823 ) ) ;
#7899=VERTEX_POINT ( 'NONE', #4338 ) ;
#7900=FACE_OUTER_BOUND ( 'NONE', #36084, .T. ) ;
#7902=LINE ( 'NONE', #6458, #17651 ) ;
#7904=DIRECTION ( 'NONE',  ( -1.000000000000000000, -0.000000000000000000, -0.000000000000000000 ) ) ;
#7905=LINE ( 'NONE', #23654, #13782 ) ;
#7907=VECTOR ( 'NONE', #9066, 39.37007874015748143 ) ;
#7908=VERTEX_POINT ( 'NONE', #31456 ) ;
#7912=DIRECTION ( 'NONE',  ( -0.000000000000000000, 1.000000000000000000, -0.000000000000000000 ) ) ;
#7913=VECTOR ( 'NONE', #20898, 39.37007874015748143 ) ;
#7914=CARTESIAN_POINT ( 'NONE',  ( 0.000000000000000000, 3.267716535433071279, -0.1968503937007883287 ) ) ;
#7915=ORIENTED_EDGE ( 'NONE', *, *, #27459, .F. ) ;
#7917=LINE ( 'NONE', #23662, #10459 ) ;
#7919=CARTESIAN_POINT ( 'NONE',  ( 1.636583440222563635, 0.000000000000000000, -1.259842519685035800 ) ) ;
#7922=CARTESIAN_POINT ( 'NONE',  ( 0.000000000000000000, 3.346456692913386100, 0.000000000000000000 ) ) ;
#7924=LINE ( 'NONE', #47889, #39758 ) ;
#7926=CARTESIAN_POINT ( 'NONE',  ( -0.8942052331142552601, 3.267716535433071279, 2.204724409448808764 ) ) ;
#7929=LINE ( 'NONE', #35556, #50650 ) ;
#7930=VERTEX_POINT ( 'NONE', #44081 ) ;
#7932=ORIENTED_EDGE ( 'NONE', *, *, #28615, .F. ) ;
#7935=CARTESIAN_POINT ( 'NONE',  ( -0.3486774197067334380, 3.346456692913386100, 1.259842519685033357 ) ) ;
#7936=DIRECTION ( 'NONE',  ( -0.000000000000000000, 0.000000000000000000, 1.000000000000000000 ) ) ;
#7937=ORIENTED_EDGE ( 'NONE', *, *, #17240, .T. ) ;
#7939=ORIENTED_EDGE ( 'NONE', *, *, #4403, .F. ) ;
#7941=VECTOR ( 'NONE', #32897, 39.37007874015748143 ) ;
#7942=DIRECTION ( 'NONE',  ( -1.000000000000000000, 0.000000000000000000, -0.000000000000000000 ) ) ;
#7943=EDGE_CURVE ( 'NONE', #31137, #28697, #39677, .T. ) ;
#7944=VECTOR ( 'NONE', #2000, 39.37007874015748143 ) ;
#7945=ORIENTED_EDGE ( 'NONE', *, *, #22132, .F. ) ;
#7946=EDGE_CURVE ( 'NONE', #16727, #33477, #43307, .T. ) ;
#7947=ORIENTED_EDGE ( 'NONE', *, *, #2601, .F. ) ;
#7948=VECTOR ( 'NONE', #18457, 39.37007874015748143 ) ;
#7949=DIRECTION ( 'NONE',  ( 1.000000000000000000, 0.000000000000000000, 0.000000000000000000 ) ) ;
#7950=VERTEX_POINT ( 'NONE', #16219 ) ;
#7951=VECTOR ( 'NONE', #21802, 39.37007874015748143 ) ;
#7952=EDGE_CURVE ( 'NONE', #2129, #43946, #17430, .T. ) ;
#7953=DIRECTION ( 'NONE',  ( 1.000000000000000000, 0.000000000000000000, 0.000000000000000000 ) ) ;
#7955=EDGE_CURVE ( 'NONE', #34623, #27824, #43818, .T. ) ;
#7961=ORIENTED_EDGE ( 'NONE', *, *, #32530, .F. ) ;
#7962=FACE_OUTER_BOUND ( 'NONE', #10402, .T. ) ;
#7963=ORIENTED_EDGE ( 'NONE', *, *, #3746, .F. ) ;
#7964=CARTESIAN_POINT ( 'NONE',  ( -1.439733046521777027, 0.000000000000000000, -1.456692913385822186 ) ) ;
#7965=CARTESIAN_POINT ( 'NONE',  ( 0.7423782071083085965, 0.000000000000000000, -0.5118110236220467790 ) ) ;
#7968=ORIENTED_EDGE ( 'NONE', *, *, #48026, .T. ) ;
#7969=ORIENTED_EDGE ( 'NONE', *, *, #9843, .T. ) ;
#7970=LINE ( 'NONE', #4106, #36857 ) ;
#7971=LINE ( 'NONE', #8230, #22054 ) ;
#7972=CARTESIAN_POINT ( 'NONE',  ( 2.106197740627112402, 3.346456692913386100, 1.102362204724403938 ) ) ;
#7973=EDGE_CURVE ( 'NONE', #14952, #41410, #5105, .T. ) ;
#7974=DIRECTION ( 'NONE',  ( 1.000000000000000000, 0.000000000000000000, 0.000000000000000000 ) ) ;
#7976=CARTESIAN_POINT ( 'NONE',  ( -1.909347346926324462, 3.346456692913386100, 0.1574803149606286423 ) ) ;
#7977=ORIENTED_EDGE ( 'NONE', *, *, #44895, .F. ) ;
#7981=ORIENTED_EDGE ( 'NONE', *, *, #24462, .T. ) ;
#7982=CIRCLE ( 'NONE', #47519, 2.106299212598425008 ) ;
#7983=LINE ( 'NONE', #27086, #32490 ) ;
#7984=VERTEX_POINT ( 'NONE', #48181 ) ;
#7987=CARTESIAN_POINT ( 'NONE',  ( 0.5455278134075217666, 3.346456692913386100, 2.204724409448808764 ) ) ;
#7988=VECTOR ( 'NONE', #24350, 39.37007874015748143 ) ;
#7989=ORIENTED_EDGE ( 'NONE', *, *, #21926, .F. ) ;
#7990=FACE_OUTER_BOUND ( 'NONE', #16358, .T. ) ;
#7991=VERTEX_POINT ( 'NONE', #8982 ) ;
#7992=DIRECTION ( 'NONE',  ( -1.000000000000000000, 0.000000000000000000, -0.000000000000000000 ) ) ;
#7994=LINE ( 'NONE', #31493, #33486 ) ;
#7995=PLANE ( 'NONE',  #852 ) ;
#7999=ORIENTED_EDGE ( 'NONE', *, *, #15303, .F. ) ;
#8000=DIRECTION ( 'NONE',  ( 0.000000000000000000, 0.000000000000000000, -1.000000000000000000 ) ) ;
#8001=CARTESIAN_POINT ( 'NONE',  ( -1.091055626815042645, 3.346456692913386100, -0.6299212598425177889 ) ) ;
#8006=CARTESIAN_POINT ( 'NONE',  ( 0.000000000000000000, 3.267716535433071279, 0.000000000000000000 ) ) ;
#8007=EDGE_CURVE ( 'NONE', #50330, #3253, #31713, .T. ) ;
#8008=VECTOR ( 'NONE', #21741, 39.37007874015748143 ) ;
#8009=VECTOR ( 'NONE', #26153, 39.37007874015748143 ) ;
#8013=VECTOR ( 'NONE', #16430, 39.37007874015748143 ) ;
#8015=ORIENTED_EDGE ( 'NONE', *, *, #30753, .F. ) ;
#8017=ORIENTED_EDGE ( 'NONE', *, *, #27428, .F. ) ;
#8022=CARTESIAN_POINT ( 'NONE',  ( -1.057143431661237143, 3.267716535433071279, -1.889763779527552146 ) ) ;
#8025=ORIENTED_EDGE ( 'NONE', *, *, #42509, .T. ) ;
#8028=VECTOR ( 'NONE', #20740, 39.37007874015748143 ) ;
#8029=VERTEX_POINT ( 'NONE', #46043 ) ;
#8030=PLANE ( 'NONE',  #15244 ) ;
#8041=EDGE_LOOP ( 'NONE', ( #24581, #25787, #15777, #34823 ) ) ;
#8043=DIRECTION ( 'NONE',  ( -0.000000000000000000, 0.000000000000000000, 1.000000000000000000 ) ) ;
#8044=CARTESIAN_POINT ( 'NONE',  ( -0.8942052331142547050, 0.000000000000000000, 0.3149606299212580063 ) ) ;
#8045=AXIS2_PLACEMENT_3D ( 'NONE', #23353, #31369, #8381 ) ;
#8047=AXIS2_PLACEMENT_3D ( 'NONE', #5195, #36700, #36961 ) ;
#8049=ORIENTED_EDGE ( 'NONE', *, *, #23122, .T. ) ;
#8050=CARTESIAN_POINT ( 'NONE',  ( 0.2727639067037610499, 3.267716535433071279, 2.047244094488179567 ) ) ;
#8051=AXIS2_PLACEMENT_3D ( 'NONE', #35893, #47718, #16265 ) ;
#8052=EDGE_LOOP ( 'NONE', ( #6663, #22607, #35357, #23238, #48627, #37852, #44649, #43879, #23264, #23352, #36701, #27154, #40826, #39942, #10052, #4860, #22017, #7745, #46650, #24523, #18057, #9542, #39720, #22452, #3334, #17340, #8025, #14254, #3012, #42557, #21084, #30543, #36026, #13099, #7100, #41282, #19848, #44426, #30671, #43579, #24835, #32151, #1609, #36667, #13374, #11635, #193, #12040, #50655, #38572, #47450, #34740, #18928, #39539, #50559, #5847, #20745, #5992, #16831, #32355, #34050, #40578, #30168, #5316, #22450, #35771, #43490, #37623, #26101, #23010, #34926 ) ) ;
#8056=LINE ( 'NONE', #27665, #12009 ) ;
#8057=DIRECTION ( 'NONE',  ( 1.734723475976806848E-16, -0.000000000000000000, 1.000000000000000000 ) ) ;
#8060=VERTEX_POINT ( 'NONE', #38334 ) ;
#8061=ORIENTED_EDGE ( 'NONE', *, *, #24349, .T. ) ;
#8063=CARTESIAN_POINT ( 'NONE',  ( 1.091055626815042645, 3.267716535433071279, -1.892679809432644882E-16 ) ) ;
#8064=CARTESIAN_POINT ( 'NONE',  ( 1.363819533518803029, 3.267716535433071279, -1.732283464566923170 ) ) ;
#8066=EDGE_LOOP ( 'NONE', ( #11629, #39282, #19670, #47003 ) ) ;
#8068=CARTESIAN_POINT ( 'NONE',  ( 0.000000000000000000, 3.267716535433071279, 2.204724409448808764 ) ) ;
#8069=CARTESIAN_POINT ( 'NONE',  ( 0.8182917201112819283, 3.346456692913386100, 1.102362204724403938 ) ) ;
#8071=EDGE_CURVE ( 'NONE', #46953, #1801, #38080, .T. ) ;
#8073=ORIENTED_EDGE ( 'NONE', *, *, #49907, .T. ) ;
#8075=LINE ( 'NONE', #7822, #19185 ) ;
#8076=CARTESIAN_POINT ( 'NONE',  ( -0.3486774197067340486, 0.000000000000000000, -0.1968503937007883287 ) ) ;
#8077=ADVANCED_FACE ( 'NONE', ( #30070 ), #7085, .F. ) ;
#8078=ADVANCED_FACE ( 'NONE', ( #22831 ), #29815, .F. ) ;
#8081=ORIENTED_EDGE ( 'NONE', *, *, #26701, .F. ) ;
#8083=CARTESIAN_POINT ( 'NONE',  ( -0.6214413264104945434, 3.346456692913386100, -1.299212598425193210 ) ) ;
#8084=ORIENTED_EDGE ( 'NONE', *, *, #34914, .F. ) ;
#8085=ORIENTED_EDGE ( 'NONE', *, *, #28181, .F. ) ;
#8088=CARTESIAN_POINT ( 'NONE',  ( -1.166969139818016643, 3.267716535433071279, 4.048737525165548620E-16 ) ) ;
#8090=CARTESIAN_POINT ( 'NONE',  ( 1.363819533518803695, 0.000000000000000000, 1.535433070866133898 ) ) ;
#8091=LINE ( 'NONE', #46297, #3235 ) ;
#8092=ORIENTED_EDGE ( 'NONE', *, *, #28651, .T. ) ;
#8093=EDGE_LOOP ( 'NONE', ( #42746, #22562, #2330, #43246 ) ) ;
#8095=VERTEX_POINT ( 'NONE', #9233 ) ;
#8097=CARTESIAN_POINT ( 'NONE',  ( -1.636583440222563635, 0.000000000000000000, 1.259842519685033357 ) ) ;
#8099=VECTOR ( 'NONE', #37983, 39.37007874015748143 ) ;
#8100=ADVANCED_FACE ( 'NONE', ( #30578 ), #21115, .F. ) ;
#8101=VECTOR ( 'NONE', #44338, 39.37007874015748143 ) ;
#8102=FACE_OUTER_BOUND ( 'NONE', #45746, .T. ) ;
#8103=DIRECTION ( 'NONE',  ( -1.000000000000000000, -0.000000000000000000, -0.000000000000000000 ) ) ;
#8104=VERTEX_POINT ( 'NONE', #22073 ) ;
#8105=CARTESIAN_POINT ( 'NONE',  ( 2.106197740627112402, 3.346456692913386100, -0.02067487291359444701 ) ) ;
#8106=VECTOR ( 'NONE', #41638, 39.37007874015748143 ) ;
#8109=ORIENTED_EDGE ( 'NONE', *, *, #23002, .F. ) ;
#8110=FACE_OUTER_BOUND ( 'NONE', #30275, .T. ) ;
#8111=EDGE_CURVE ( 'NONE', #36377, #29102, #49891, .T. ) ;
#8113=CARTESIAN_POINT ( 'NONE',  ( -1.363819533518803473, 0.000000000000000000, 1.850393700787392293 ) ) ;
#8115=EDGE_CURVE ( 'NONE', #17096, #25478, #38581, .T. ) ;
#8117=CARTESIAN_POINT ( 'NONE',  ( -1.985260859929297572, 3.346456692913386100, 0.6299212598425164567 ) ) ;
#8120=CARTESIAN_POINT ( 'NONE',  ( 0.2727639067037604947, 0.000000000000000000, 0.7874015748031454320 ) ) ;
#8123=PLANE ( 'NONE',  #37773 ) ;
#8124=LINE ( 'NONE', #48091, #5346 ) ;
#8127=VECTOR ( 'NONE', #40653, 39.37007874015748143 ) ;
#8129=ORIENTED_EDGE ( 'NONE', *, *, #28104, .F. ) ;
#8130=CARTESIAN_POINT ( 'NONE',  ( 1.636583440222563857, 3.267716535433071279, -0.5118110236220471121 ) ) ;
#8131=LINE ( 'NONE', #23880, #36177 ) ;
#8133=LINE ( 'NONE', #4256, #14299 ) ;
#8137=EDGE_CURVE ( 'NONE', #42344, #26476, #48431, .T. ) ;
#8138=DIRECTION ( 'NONE',  ( 1.000000000000000000, -0.000000000000000000, 0.000000000000000000 ) ) ;
#8139=AXIS2_PLACEMENT_3D ( 'NONE', #21230, #41614, #9863 ) ;
#8140=VECTOR ( 'NONE', #16773, 39.37007874015748143 ) ;
#8141=ORIENTED_EDGE ( 'NONE', *, *, #11180, .F. ) ;
#8142=ORIENTED_EDGE ( 'NONE', *, *, #29445, .F. ) ;
#8143=ORIENTED_EDGE ( 'NONE', *, *, #11830, .F. ) ;
#8144=LINE ( 'NONE', #43492, #3495 ) ;
#8145=CARTESIAN_POINT ( 'NONE',  ( 1.091055626815042645, 3.346456692913386100, -0.8267716535433055070 ) ) ;
#8146=EDGE_CURVE ( 'NONE', #2168, #40155, #1488, .T. ) ;
#8148=VECTOR ( 'NONE', #17439, 39.37007874015748143 ) ;
#8149=CARTESIAN_POINT ( 'NONE',  ( -1.909347346926324906, 3.346456692913386100, -0.7874015748031470974 ) ) ;
#8151=FACE_BOUND ( 'NONE', #42238, .T. ) ;
#8152=VERTEX_POINT ( 'NONE', #7835 ) ;
#8154=CARTESIAN_POINT ( 'NONE',  ( 2.106197740627112402, 3.267716535433071279, -0.02067487291359444701 ) ) ;
#8157=VECTOR ( 'NONE', #42267, 39.37007874015748143 ) ;
#8158=CARTESIAN_POINT ( 'NONE',  ( 1.636583440222563857, 3.267716535433071279, 0.9448818897637746295 ) ) ;
#8160=ORIENTED_EDGE ( 'NONE', *, *, #50307, .T. ) ;
#8161=DIRECTION ( 'NONE',  ( 1.000000000000000000, 0.000000000000000000, 0.000000000000000000 ) ) ;
#8162=ORIENTED_EDGE ( 'NONE', *, *, #1010, .T. ) ;
#8163=LINE ( 'NONE', #20803, #45190 ) ;
#8167=DIRECTION ( 'NONE',  ( -3.469446951953613696E-16, 0.000000000000000000, -1.000000000000000000 ) ) ;
#8168=LINE ( 'NONE', #44293, #17905 ) ;
#8171=DIRECTION ( 'NONE',  ( -0.000000000000000000, 0.000000000000000000, 1.000000000000000000 ) ) ;
#8172=LINE ( 'NONE', #39664, #44932 ) ;
#8174=VECTOR ( 'NONE', #1087, 39.37007874015748143 ) ;
#8176=ORIENTED_EDGE ( 'NONE', *, *, #23901, .F. ) ;
#8177=DIRECTION ( 'NONE',  ( 0.000000000000000000, 0.000000000000000000, -1.000000000000000000 ) ) ;
#8178=EDGE_CURVE ( 'NONE', #7571, #10927, #34957, .T. ) ;
#8179=DIRECTION ( 'NONE',  ( -0.000000000000000000, 1.000000000000000000, -0.000000000000000000 ) ) ;
#8181=DIRECTION ( 'NONE',  ( -0.000000000000000000, 1.000000000000000000, -0.000000000000000000 ) ) ;
#8182=FACE_OUTER_BOUND ( 'NONE', #39609, .T. ) ;
#8183=VECTOR ( 'NONE', #883, 39.37007874015748143 ) ;
#8185=CARTESIAN_POINT ( 'NONE',  ( 1.833433833923351353, 3.346456692913386100, 0.9448818897637746295 ) ) ;
#8186=CARTESIAN_POINT ( 'NONE',  ( 0.8182917201112819283, 3.346456692913386100, 0.7874015748031454320 ) ) ;
#8187=AXIS2_PLACEMENT_3D ( 'NONE', #6020, #25643, #33155 ) ;
#8189=ORIENTED_EDGE ( 'NONE', *, *, #38275, .T. ) ;
#8193=DIRECTION ( 'NONE',  ( 1.734723475976806848E-16, 0.000000000000000000, 1.000000000000000000 ) ) ;
#8195=VERTEX_POINT ( 'NONE', #27195 ) ;
#8196=ORIENTED_EDGE ( 'NONE', *, *, #30976, .T. ) ;
#8198=VERTEX_POINT ( 'NONE', #35712 ) ;
#8199=DIRECTION ( 'NONE',  ( -1.000000000000000000, 0.000000000000000000, 0.000000000000000000 ) ) ;
#8200=EDGE_CURVE ( 'NONE', #35993, #5779, #31357, .T. ) ;
#8202=ORIENTED_EDGE ( 'NONE', *, *, #23994, .T. ) ;
#8204=EDGE_CURVE ( 'NONE', #37100, #27093, #11210, .T. ) ;
#8205=VECTOR ( 'NONE', #6743, 39.37007874015748143 ) ;
#8208=EDGE_CURVE ( 'NONE', #1491, #33429, #50389, .T. ) ;
#8209=CARTESIAN_POINT ( 'NONE',  ( 0.000000000000000000, 3.267716535433071279, -1.299212598425193210 ) ) ;
#8211=EDGE_CURVE ( 'NONE', #28900, #739, #31337, .T. ) ;
#8213=ORIENTED_EDGE ( 'NONE', *, *, #27994, .T. ) ;
#8214=AXIS2_PLACEMENT_3D ( 'NONE', #7519, #38765, #19631 ) ;
#8217=ORIENTED_EDGE ( 'NONE', *, *, #6799, .T. ) ;
#8218=CARTESIAN_POINT ( 'NONE',  ( 0.000000000000000000, 3.346456692913386100, 0.000000000000000000 ) ) ;
#8221=VECTOR ( 'NONE', #37034, 39.37007874015748143 ) ;
#8222=PLANE ( 'NONE',  #43543 ) ;
#8225=LINE ( 'NONE', #16743, #38231 ) ;
#8226=CARTESIAN_POINT ( 'NONE',  ( 0.4696143004045478242, 3.267716535433071279, -1.629301903132387013E-16 ) ) ;
#8227=VERTEX_POINT ( 'NONE', #12218 ) ;
#8228=ORIENTED_EDGE ( 'NONE', *, *, #41925, .F. ) ;
#8230=CARTESIAN_POINT ( 'NONE',  ( 1.015142113812069757, 3.267716535433071279, -3.521981712565033375E-16 ) ) ;
#8231=DIRECTION ( 'NONE',  ( -0.000000000000000000, 0.000000000000000000, 1.000000000000000000 ) ) ;
#8234=CARTESIAN_POINT ( 'NONE',  ( 0.000000000000000000, 3.267716535433071279, -0.3543307086614178592 ) ) ;
#8235=VECTOR ( 'NONE', #41425, 39.37007874015748143 ) ;
#8236=EDGE_LOOP ( 'NONE', ( #49712, #36416, #7524, #42488 ) ) ;
#8239=ORIENTED_EDGE ( 'NONE', *, *, #18132, .T. ) ;
#8240=DIRECTION ( 'NONE',  ( 1.734723475976806848E-16, -0.000000000000000000, 1.000000000000000000 ) ) ;
#8242=EDGE_LOOP ( 'NONE', ( #46959, #14470, #27188, #6878 ) ) ;
#8243=EDGE_CURVE ( 'NONE', #36726, #12169, #39587, .T. ) ;
#8245=VECTOR ( 'NONE', #20863, 39.37007874015748143 ) ;
#8246=DIRECTION ( 'NONE',  ( 0.000000000000000000, -1.000000000000000000, 0.000000000000000000 ) ) ;
#8247=VECTOR ( 'NONE', #10955, 39.37007874015748143 ) ;
#8248=CARTESIAN_POINT ( 'NONE',  ( 0.4696143004045476577, 3.346456692913386100, -2.047244094488182231 ) ) ;
#8251=ORIENTED_EDGE ( 'NONE', *, *, #4840, .F. ) ;
#8254=VERTEX_POINT ( 'NONE', #43692 ) ;
#8255=CARTESIAN_POINT ( 'NONE',  ( 0.5455278134075217666, 0.000000000000000000, 1.574803149606291974 ) ) ;
#8256=CARTESIAN_POINT ( 'NONE',  ( -1.091055626815043089, 3.267716535433071279, 1.892679809432645376E-16 ) ) ;
#8259=EDGE_LOOP ( 'NONE', ( #48408, #16044, #26021, #38677 ) ) ;
#8261=EDGE_CURVE ( 'NONE', #28015, #16004, #3711, .T. ) ;
#8262=LINE ( 'NONE', #47460, #34247 ) ;
#8263=CARTESIAN_POINT ( 'NONE',  ( 1.833433833923351353, 3.346456692913386100, -1.161035397307311917E-15 ) ) ;
#8264=CARTESIAN_POINT ( 'NONE',  ( 1.015142113812069091, 3.346456692913386100, -1.929133858267711110 ) ) ;
#8265=ORIENTED_EDGE ( 'NONE', *, *, #8115, .T. ) ;
#8267=CARTESIAN_POINT ( 'NONE',  ( 2.378961647330872786, 3.346456692913386100, -0.3149606299212596716 ) ) ;
#8268=ORIENTED_EDGE ( 'NONE', *, *, #2538, .T. ) ;
#8270=EDGE_LOOP ( 'NONE', ( #44960, #16277, #19900, #18913 ) ) ;
#8271=ORIENTED_EDGE ( 'NONE', *, *, #47454, .F. ) ;
#8273=EDGE_CURVE ( 'NONE', #33135, #8060, #43443, .T. ) ;
#8274=ORIENTED_EDGE ( 'NONE', *, *, #19445, .T. ) ;
#8275=LINE ( 'NONE', #21181, #48172 ) ;
#8276=AXIS2_PLACEMENT_3D ( 'NONE', #33204, #5823, #5570 ) ;
#8278=VECTOR ( 'NONE', #24588, 39.37007874015748143 ) ;
#8279=CARTESIAN_POINT ( 'NONE',  ( -2.182111253630085734, 3.346456692913386100, -0.6299212598425177889 ) ) ;
#8282=EDGE_LOOP ( 'NONE', ( #26342, #15270, #20596, #8983 ) ) ;
#8285=AXIS2_PLACEMENT_3D ( 'NONE', #27045, #42547, #19049 ) ;
#8286=EDGE_LOOP ( 'NONE', ( #35499, #50782, #4758, #37635 ) ) ;
#8287=CARTESIAN_POINT ( 'NONE',  ( 1.560669927219591191, 3.267716535433071279, 1.535433070866133898 ) ) ;
#8288=DIRECTION ( 'NONE',  ( 1.000000000000000000, -0.000000000000000000, 0.000000000000000000 ) ) ;
#8289=CARTESIAN_POINT ( 'NONE',  ( -1.636583440222564301, 3.346456692913386100, -1.574803149606293307 ) ) ;
#8290=DIRECTION ( 'NONE',  ( 1.000000000000000000, 0.000000000000000000, 0.000000000000000000 ) ) ;
#8291=LINE ( 'NONE', #29645, #38474 ) ;
#8292=ORIENTED_EDGE ( 'NONE', *, *, #25337, .T. ) ;
#8293=FACE_OUTER_BOUND ( 'NONE', #13684, .T. ) ;
#8295=ORIENTED_EDGE ( 'NONE', *, *, #20272, .T. ) ;
#8297=ORIENTED_EDGE ( 'NONE', *, *, #46727, .T. ) ;
#8298=DIRECTION ( 'NONE',  ( -3.469446951953613696E-16, 0.000000000000000000, -1.000000000000000000 ) ) ;
#8299=DIRECTION ( 'NONE',  ( 1.000000000000000000, 0.000000000000000000, 0.000000000000000000 ) ) ;
#8300=LINE ( 'NONE', #20162, #35417 ) ;
#8301=ADVANCED_FACE ( 'NONE', ( #48056 ), #13497, .F. ) ;
#8303=ADVANCED_FACE ( 'NONE', ( #1101 ), #13246, .F. ) ;
#8304=EDGE_LOOP ( 'NONE', ( #16043, #6568, #8557, #46945 ) ) ;
#8305=PLANE ( 'NONE',  #17183 ) ;
#8306=ORIENTED_EDGE ( 'NONE', *, *, #11546, .F. ) ;
#8308=VERTEX_POINT ( 'NONE', #8856 ) ;
#8310=DIRECTION ( 'NONE',  ( -1.000000000000000000, 0.000000000000000000, 1.734723475976806848E-16 ) ) ;
#8311=FACE_OUTER_BOUND ( 'NONE', #1082, .T. ) ;
#8312=PLANE ( 'NONE',  #21944 ) ;
#8313=VECTOR ( 'NONE', #1478, 39.37007874015748143 ) ;
#8317=VERTEX_POINT ( 'NONE', #4472 ) ;
#8322=ORIENTED_EDGE ( 'NONE', *, *, #13328, .T. ) ;
#8324=DIRECTION ( 'NONE',  ( 1.000000000000000000, 0.000000000000000000, 0.000000000000000000 ) ) ;
#8325=CARTESIAN_POINT ( 'NONE',  ( -0.6214413264104945434, 0.000000000000000000, 1.850393700787391849 ) ) ;
#8326=VECTOR ( 'NONE', #34253, 39.37007874015748143 ) ;
#8327=LINE ( 'NONE', #20453, #9630 ) ;
#8329=CARTESIAN_POINT ( 'NONE',  ( 1.909347346926324684, 0.000000000000000000, 0.9055118110236164419 ) ) ;
#8331=FACE_OUTER_BOUND ( 'NONE', #29926, .T. ) ;
#8332=EDGE_CURVE ( 'NONE', #13971, #36157, #32879, .T. ) ;
#8333=FACE_OUTER_BOUND ( 'NONE', #45394, .T. ) ;
#8334=ORIENTED_EDGE ( 'NONE', *, *, #724, .F. ) ;
#8336=CARTESIAN_POINT ( 'NONE',  ( -0.07591351300297340121, 3.346456692913386100, -0.03937007874015908959 ) ) ;
#8337=ORIENTED_EDGE ( 'NONE', *, *, #259, .T. ) ;
#8338=DIRECTION ( 'NONE',  ( -3.469446951953613696E-16, 0.000000000000000000, -1.000000000000000000 ) ) ;
#8340=ORIENTED_EDGE ( 'NONE', *, *, #22432, .T. ) ;
#8341=CARTESIAN_POINT ( 'NONE',  ( 1.833433833923351353, 3.267716535433071279, 0.6299212598425164567 ) ) ;
#8346=DIRECTION ( 'NONE',  ( 1.734723475976806848E-16, 0.000000000000000000, 1.000000000000000000 ) ) ;
#8349=ADVANCED_FACE ( 'NONE', ( #9106 ), #25114, .F. ) ;
#8353=FACE_OUTER_BOUND ( 'NONE', #13137, .T. ) ;
#8355=EDGE_CURVE ( 'NONE', #28387, #17641, #40100, .T. ) ;
#8356=VECTOR ( 'NONE', #5576, 39.37007874015748143 ) ;
#8357=STYLED_ITEM('',(#51073),#6895);
#8358=DIRECTION ( 'NONE',  ( -0.000000000000000000, 0.000000000000000000, 1.000000000000000000 ) ) ;
#8360=AXIS2_PLACEMENT_3D ( 'NONE', #23360, #3749, #3498 ) ;
#8363=DIRECTION ( 'NONE',  ( 1.000000000000000000, 0.000000000000000000, -3.469446951953613696E-16 ) ) ;
#8364=VECTOR ( 'NONE', #32801, 39.37007874015748143 ) ;
#8367=ORIENTED_EDGE ( 'NONE', *, *, #7557, .T. ) ;
#8368=VECTOR ( 'NONE', #22652, 39.37007874015748143 ) ;
#8369=CARTESIAN_POINT ( 'NONE',  ( -1.439733046521777027, 3.267716535433071279, -0.5118110236220466680 ) ) ;
#8372=ORIENTED_EDGE ( 'NONE', *, *, #33980, .T. ) ;
#8375=ADVANCED_FACE ( 'NONE', ( #12729 ), #16867, .F. ) ;
#8376=DIRECTION ( 'NONE',  ( -3.469446951953613696E-16, 0.000000000000000000, -1.000000000000000000 ) ) ;
#8377=ORIENTED_EDGE ( 'NONE', *, *, #31867, .F. ) ;
#8378=DIRECTION ( 'NONE',  ( 1.000000000000000000, 0.000000000000000000, 0.000000000000000000 ) ) ;
#8380=ORIENTED_EDGE ( 'NONE', *, *, #6091, .F. ) ;
#8381=DIRECTION ( 'NONE',  ( -1.000000000000000000, 0.000000000000000000, -0.000000000000000000 ) ) ;
#8383=CARTESIAN_POINT ( 'NONE',  ( -1.363819533518803473, 0.000000000000000000, -1.732283464566922726 ) ) ;
#8384=LINE ( 'NONE', #24128, #29310 ) ;
#8386=EDGE_LOOP ( 'NONE', ( #32552, #44770, #478, #41189 ) ) ;
#8389=ORIENTED_EDGE ( 'NONE', *, *, #14958, .T. ) ;
#8390=FACE_OUTER_BOUND ( 'NONE', #1680, .T. ) ;
#8391=DIRECTION ( 'NONE',  ( 1.734723475976806848E-16, -0.000000000000000000, 1.000000000000000000 ) ) ;
#8392=PLANE ( 'NONE',  #43394 ) ;
#8393=VECTOR ( 'NONE', #40628, 39.37007874015748143 ) ;
#8394=CARTESIAN_POINT ( 'NONE',  ( -0.8182917201112814842, 3.267716535433071279, 0.5905511811023582691 ) ) ;
#8395=VERTEX_POINT ( 'NONE', #24858 ) ;
#8397=ORIENTED_EDGE ( 'NONE', *, *, #2663, .T. ) ;
#8398=DIRECTION ( 'NONE',  ( -1.000000000000000000, 0.000000000000000000, -0.000000000000000000 ) ) ;
#8399=CARTESIAN_POINT ( 'NONE',  ( 0.000000000000000000, 3.346456692913386100, 0.000000000000000000 ) ) ;
#8400=EDGE_CURVE ( 'NONE', #15891, #29593, #28461, .T. ) ;
#8403=VECTOR ( 'NONE', #4253, 39.37007874015748143 ) ;
#8404=FACE_BOUND ( 'NONE', #32621, .T. ) ;
#8405=ORIENTED_EDGE ( 'NONE', *, *, #14954, .T. ) ;
#8407=EDGE_LOOP ( 'NONE', ( #45369, #47611, #11434 ) ) ;
#8409=VERTEX_POINT ( 'NONE', #48566 ) ;
#8414=EDGE_CURVE ( 'NONE', #39500, #1960, #40861, .T. ) ;
#8416=EDGE_LOOP ( 'NONE', ( #590, #23683, #47336, #13951 ) ) ;
#8419=EDGE_CURVE ( 'NONE', #22619, #37657, #28971, .T. ) ;
#8421=LINE ( 'NONE', #20547, #14518 ) ;
#8422=DIRECTION ( 'NONE',  ( 1.000000000000000000, 0.000000000000000000, 0.000000000000000000 ) ) ;
#8423=FACE_OUTER_BOUND ( 'NONE', #18140, .T. ) ;
#8424=PLANE ( 'NONE',  #50814 ) ;
#8425=CARTESIAN_POINT ( 'NONE',  ( -2.258024766633058622, 0.000000000000000000, -0.3543307086614173040 ) ) ;
#8426=EDGE_LOOP ( 'NONE', ( #40229, #42066, #25234, #12585 ) ) ;
#8427=LINE ( 'NONE', #20291, #40669 ) ;
#8429=CARTESIAN_POINT ( 'NONE',  ( 1.363819533518803029, 3.346456692913386100, -1.417322834645665219 ) ) ;
#8430=EDGE_CURVE ( 'NONE', #36606, #50546, #5493, .T. ) ;
#8433=CARTESIAN_POINT ( 'NONE',  ( 0.4696143004045478797, 0.000000000000000000, -0.9842519685039348154 ) ) ;
#8435=CARTESIAN_POINT ( 'NONE',  ( -1.166969139818016199, 3.267716535433071279, 1.850393700787392293 ) ) ;
#8437=EDGE_CURVE ( 'NONE', #27664, #32071, #49824, .T. ) ;
#8438=LINE ( 'NONE', #20567, #16924 ) ;
#8440=EDGE_CURVE ( 'NONE', #9489, #14486, #34140, .T. ) ;
#8442=DIRECTION ( 'NONE',  ( -0.000000000000000000, 1.000000000000000000, -0.000000000000000000 ) ) ;
#8443=VERTEX_POINT ( 'NONE', #18379 ) ;
#8444=LINE ( 'NONE', #35808, #28915 ) ;
#8446=VECTOR ( 'NONE', #45312, 39.37007874015748143 ) ;
#8448=CARTESIAN_POINT ( 'NONE',  ( 0.7423782071083092626, 3.267716535433071279, 1.259842519685033357 ) ) ;
#8449=EDGE_CURVE ( 'NONE', #1768, #42073, #26127, .T. ) ;
#8452=DIRECTION ( 'NONE',  ( 1.734723475976806848E-16, -0.000000000000000000, 1.000000000000000000 ) ) ;
#8454=PLANE ( 'NONE',  #16971 ) ;
#8455=ORIENTED_EDGE ( 'NONE', *, *, #14625, .T. ) ;
#8456=DIRECTION ( 'NONE',  ( -0.000000000000000000, 1.000000000000000000, -0.000000000000000000 ) ) ;
#8457=EDGE_LOOP ( 'NONE', ( #35607, #29361, #26607, #24156 ) ) ;
#8458=LINE ( 'NONE', #24206, #34820 ) ;
#8463=VECTOR ( 'NONE', #45400, 39.37007874015748143 ) ;
#8464=CARTESIAN_POINT ( 'NONE',  ( 1.560669927219590303, 3.213780742542635238, -1.912925693120431481 ) ) ;
#8465=EDGE_CURVE ( 'NONE', #40849, #6366, #5995, .T. ) ;
#8466=EDGE_CURVE ( 'NONE', #50824, #32285, #37507, .T. ) ;
#8468=ORIENTED_EDGE ( 'NONE', *, *, #18862, .T. ) ;
#8469=CARTESIAN_POINT ( 'NONE',  ( 0.5455278134075212115, 0.000000000000000000, 0.3149606299212576177 ) ) ;
#8470=ADVANCED_FACE ( 'NONE', ( #14511 ), #41878, .F. ) ;
#8474=AXIS2_PLACEMENT_3D ( 'NONE', #22005, #18125, #41621 ) ;
#8475=CARTESIAN_POINT ( 'NONE',  ( 0.5455278134075208785, 3.346456692913386100, -1.771653543307081025 ) ) ;
#8477=CARTESIAN_POINT ( 'NONE',  ( -0.5455278134075214336, 0.000000000000000000, -1.141732283464563791 ) ) ;
#8478=VECTOR ( 'NONE', #29889, 39.37007874015748143 ) ;
#8480=PLANE ( 'NONE',  #47226 ) ;
#8481=CARTESIAN_POINT ( 'NONE',  ( 0.5455278134075208785, 0.000000000000000000, -2.086614173228340086 ) ) ;
#8482=ORIENTED_EDGE ( 'NONE', *, *, #32297, .T. ) ;
#8483=VERTEX_POINT ( 'NONE', #49065 ) ;
#8484=DIRECTION ( 'NONE',  ( -0.000000000000000000, 1.000000000000000000, -0.000000000000000000 ) ) ;
#8485=CARTESIAN_POINT ( 'NONE',  ( 1.909347346926324684, 3.267716535433071279, -0.3543307086614178592 ) ) ;
#8486=VECTOR ( 'NONE', #43262, 39.37007874015748143 ) ;
#8487=LINE ( 'NONE', #36882, #29107 ) ;
#8488=EDGE_CURVE ( 'NONE', #18819, #24456, #25618, .T. ) ;
#8490=CARTESIAN_POINT ( 'NONE',  ( -1.985260859929297572, 3.267716535433071279, 6.887757239314511260E-16 ) ) ;
#8493=ORIENTED_EDGE ( 'NONE', *, *, #38275, .F. ) ;
#8496=VERTEX_POINT ( 'NONE', #45466 ) ;
#8499=ORIENTED_EDGE ( 'NONE', *, *, #28777, .F. ) ;
#8501=DIRECTION ( 'NONE',  ( -1.000000000000000000, -0.000000000000000000, -0.000000000000000000 ) ) ;
#8502=CARTESIAN_POINT ( 'NONE',  ( -1.909347346926324906, 3.267716535433071279, 3.312189666507128668E-16 ) ) ;
#8505=VECTOR ( 'NONE', #20195, 39.37007874015748143 ) ;
#8508=LINE ( 'NONE', #16253, #40248 ) ;
#8509=EDGE_LOOP ( 'NONE', ( #50853, #40651, #23512, #2282 ) ) ;
#8512=DIRECTION ( 'NONE',  ( -1.000000000000000000, 0.000000000000000000, 1.734723475976806848E-16 ) ) ;
#8515=CARTESIAN_POINT ( 'NONE',  ( 0.2727639067037609943, 0.000000000000000000, 1.535433070866133898 ) ) ;
#8516=ORIENTED_EDGE ( 'NONE', *, *, #12609, .F. ) ;
#8517=ORIENTED_EDGE ( 'NONE', *, *, #48486, .F. ) ;
#8518=CARTESIAN_POINT ( 'NONE',  ( 1.091055626815043311, 3.346456692913386100, 1.889763779527550369 ) ) ;
#8519=CARTESIAN_POINT ( 'NONE',  ( -2.454875160333845674, 3.346456692913386100, -0.3543307086614173040 ) ) ;
#8520=FACE_OUTER_BOUND ( 'NONE', #42216, .T. ) ;
#8521=LINE ( 'NONE', #28385, #42698 ) ;
#8523=ORIENTED_EDGE ( 'NONE', *, *, #38565, .T. ) ;
#8524=CARTESIAN_POINT ( 'NONE',  ( -1.363819533518803473, 3.267716535433071279, -0.3543307086614174151 ) ) ;
#8526=EDGE_CURVE ( 'NONE', #681, #31838, #25876, .T. ) ;
#8527=ORIENTED_EDGE ( 'NONE', *, *, #28273, .T. ) ;
#8528=EDGE_LOOP ( 'NONE', ( #44862, #14861, #1224, #44192 ) ) ;
#8530=EDGE_CURVE ( 'NONE', #41536, #5523, #22008, .T. ) ;
#8534=CARTESIAN_POINT ( 'NONE',  ( -1.166969139818015533, 3.267716535433071279, 4.048737525165544183E-16 ) ) ;
#8535=CARTESIAN_POINT ( 'NONE',  ( 0.8182917201112819283, 3.346456692913386100, -0.4724409448818889246 ) ) ;
#8536=ORIENTED_EDGE ( 'NONE', *, *, #47037, .T. ) ;
#8537=ORIENTED_EDGE ( 'NONE', *, *, #4290, .F. ) ;
#8538=DIRECTION ( 'NONE',  ( -1.000000000000000000, 0.000000000000000000, 1.734723475976806848E-16 ) ) ;
#8539=CARTESIAN_POINT ( 'NONE',  ( -1.166969139818015977, 0.000000000000000000, -1.102362204724405270 ) ) ;
#8540=DIRECTION ( 'NONE',  ( 1.000000000000000000, 0.000000000000000000, 0.000000000000000000 ) ) ;
#8542=VERTEX_POINT ( 'NONE', #6254 ) ;
#8543=DIRECTION ( 'NONE',  ( -0.000000000000000000, 0.000000000000000000, 1.000000000000000000 ) ) ;
#8544=AXIS2_PLACEMENT_3D ( 'NONE', #19991, #38868, #42732 ) ;
#8545=FACE_OUTER_BOUND ( 'NONE', #10694, .T. ) ;
#8546=VECTOR ( 'NONE', #26266, 39.37007874015748143 ) ;
#8547=EDGE_CURVE ( 'NONE', #41687, #13480, #30513, .T. ) ;
#8548=CARTESIAN_POINT ( 'NONE',  ( -1.363819533518803473, 3.346456692913386100, 1.535433070866133232 ) ) ;
#8549=DIRECTION ( 'NONE',  ( 1.000000000000000000, -0.000000000000000000, 0.000000000000000000 ) ) ;
#8550=LINE ( 'NONE', #11652, #25235 ) ;
#8552=ORIENTED_EDGE ( 'NONE', *, *, #30856, .F. ) ;
#8555=EDGE_CURVE ( 'NONE', #14497, #15505, #18131, .T. ) ;
#8557=ORIENTED_EDGE ( 'NONE', *, *, #31699, .F. ) ;
#8559=LINE ( 'NONE', #24309, #18785 ) ;
#8560=CARTESIAN_POINT ( 'NONE',  ( -1.712496953225537633, 0.000000000000000000, -0.9842519685039344823 ) ) ;
#8561=ORIENTED_EDGE ( 'NONE', *, *, #17495, .T. ) ;
#8562=VERTEX_POINT ( 'NONE', #37254 ) ;
#8564=ORIENTED_EDGE ( 'NONE', *, *, #28751, .F. ) ;
#8565=DIRECTION ( 'NONE',  ( -1.000000000000000000, -0.000000000000000000, -0.000000000000000000 ) ) ;
#8566=ORIENTED_EDGE ( 'NONE', *, *, #13570, .T. ) ;
#8569=DIRECTION ( 'NONE',  ( 1.734723475976806848E-16, -0.000000000000000000, 1.000000000000000000 ) ) ;
#8570=ORIENTED_EDGE ( 'NONE', *, *, #15651, .F. ) ;
#8571=AXIS2_PLACEMENT_3D ( 'NONE', #5925, #21680, #13938 ) ;
#8573=ORIENTED_EDGE ( 'NONE', *, *, #45343, .F. ) ;
#8577=VERTEX_POINT ( 'NONE', #49571 ) ;
#8578=CARTESIAN_POINT ( 'NONE',  ( -0.07591351300297333182, 0.000000000000000000, 0.1574803149606283648 ) ) ;
#8579=LINE ( 'NONE', #47524, #21159 ) ;
#8583=VERTEX_POINT ( 'NONE', #17620 ) ;
#8584=LINE ( 'NONE', #842, #28773 ) ;
#8585=LINE ( 'NONE', #4969, #8505 ) ;
#8586=DIRECTION ( 'NONE',  ( -0.000000000000000000, 1.000000000000000000, -0.000000000000000000 ) ) ;
#8587=ORIENTED_EDGE ( 'NONE', *, *, #8414, .F. ) ;
#8588=CARTESIAN_POINT ( 'NONE',  ( 1.363819533518803251, 0.000000000000000000, 1.102362204724403938 ) ) ;
#8589=DIRECTION ( 'NONE',  ( 1.734723475976806848E-16, -0.000000000000000000, 1.000000000000000000 ) ) ;
#8590=EDGE_CURVE ( 'NONE', #39122, #44945, #13752, .T. ) ;
#8592=EDGE_CURVE ( 'NONE', #6504, #30555, #9876, .T. ) ;
#8594=VERTEX_POINT ( 'NONE', #11641 ) ;
#8596=DIRECTION ( 'NONE',  ( -1.000000000000000000, 0.000000000000000000, 0.000000000000000000 ) ) ;
#8597=EDGE_CURVE ( 'NONE', #12593, #50064, #7272, .T. ) ;
#8599=LINE ( 'NONE', #81, #45893 ) ;
#8600=EDGE_CURVE ( 'NONE', #20045, #14432, #7768, .T. ) ;
#8602=ORIENTED_EDGE ( 'NONE', *, *, #27240, .T. ) ;
#8603=ORIENTED_EDGE ( 'NONE', *, *, #22757, .F. ) ;
#8604=FACE_OUTER_BOUND ( 'NONE', #43171, .T. ) ;
#8606=PLANE ( 'NONE',  #31881 ) ;
#8607=DIRECTION ( 'NONE',  ( -1.000000000000000000, 0.000000000000000000, 0.000000000000000000 ) ) ;
#8608=ADVANCED_FACE ( 'NONE', ( #47215 ), #16023, .F. ) ;
#8611=DIRECTION ( 'NONE',  ( -3.469446951953613696E-16, 0.000000000000000000, -1.000000000000000000 ) ) ;
#8614=VECTOR ( 'NONE', #46236, 39.37007874015748143 ) ;
#8615=PLANE ( 'NONE',  #29151 ) ;
#8617=VECTOR ( 'NONE', #8698, 39.37007874015748143 ) ;
#8618=PLANE ( 'NONE',  #27349 ) ;
#8621=DIRECTION ( 'NONE',  ( 1.000000000000000000, 0.000000000000000000, 0.000000000000000000 ) ) ;
#8625=ORIENTED_EDGE ( 'NONE', *, *, #22011, .F. ) ;
#8626=CARTESIAN_POINT ( 'NONE',  ( 1.909347346926324462, 3.346456692913386100, -0.7874015748031473194 ) ) ;
#8627=CARTESIAN_POINT ( 'NONE',  ( 1.363819533518803473, 3.267716535433071279, -2.365849761790805980E-16 ) ) ;
#8629=VECTOR ( 'NONE', #21646, 39.37007874015748143 ) ;
#8631=CARTESIAN_POINT ( 'NONE',  ( 1.909347346926324684, 0.000000000000000000, 1.102362204724403938 ) ) ;
#8633=ORIENTED_EDGE ( 'NONE', *, *, #16320, .F. ) ;
#8636=CARTESIAN_POINT ( 'NONE',  ( -1.636583440222563635, 0.000000000000000000, 0.7480314960629874665 ) ) ;
#8637=PLANE ( 'NONE',  #39536 ) ;
#8641=CARTESIAN_POINT ( 'NONE',  ( -1.363819533518803473, 0.000000000000000000, -0.6692913385826760875 ) ) ;
#8644=LINE ( 'NONE', #9156, #28327 ) ;
#8645=CARTESIAN_POINT ( 'NONE',  ( 0.5455278134075216556, 3.267716535433071279, 2.007874015748021268 ) ) ;
#8648=ORIENTED_EDGE ( 'NONE', *, *, #44263, .F. ) ;
#8651=CARTESIAN_POINT ( 'NONE',  ( 0.000000000000000000, 3.267716535433071279, -1.141732283464564013 ) ) ;
#8654=FACE_BOUND ( 'NONE', #36413, .T. ) ;
#8656=ORIENTED_EDGE ( 'NONE', *, *, #22719, .T. ) ;
#8657=CARTESIAN_POINT ( 'NONE',  ( 0.000000000000000000, 3.267716535433071279, -0.5118110236220471121 ) ) ;
#8658=VECTOR ( 'NONE', #38023, 39.37007874015748143 ) ;
#8660=VERTEX_POINT ( 'NONE', #35141 ) ;
#8661=CARTESIAN_POINT ( 'NONE',  ( -2.182111253630085290, 3.267716535433071279, 0.3149606299212578953 ) ) ;
#8663=EDGE_CURVE ( 'NONE', #36157, #15505, #31522, .T. ) ;
#8664=EDGE_CURVE ( 'NONE', #12716, #23414, #31012, .T. ) ;
#8666=ORIENTED_EDGE ( 'NONE', *, *, #22921, .T. ) ;
#8667=CARTESIAN_POINT ( 'NONE',  ( -0.2727639067037607723, 0.000000000000000000, -1.732283464566922726 ) ) ;
#8668=ADVANCED_FACE ( 'NONE', ( #31780 ), #15264, .F. ) ;
#8670=ORIENTED_EDGE ( 'NONE', *, *, #19464, .T. ) ;
#8672=LINE ( 'NONE', #44288, #9774 ) ;
#8674=DIRECTION ( 'NONE',  ( 1.000000000000000000, 0.000000000000000000, 0.000000000000000000 ) ) ;
#8675=PLANE ( 'NONE',  #14885 ) ;
#8676=CARTESIAN_POINT ( 'NONE',  ( 1.909347346926324684, 3.346456692913386100, 0.7874015748031456541 ) ) ;
#8677=CARTESIAN_POINT ( 'NONE',  ( -1.363819533518803473, 0.000000000000000000, 1.535433070866133232 ) ) ;
#8678=ORIENTED_EDGE ( 'NONE', *, *, #44287, .T. ) ;
#8681=CARTESIAN_POINT ( 'NONE',  ( 0.1968503937007873850, 3.267716535433071279, -0.1968503937007874405 ) ) ;
#8683=DIRECTION ( 'NONE',  ( 1.000000000000000000, 0.000000000000000000, 0.000000000000000000 ) ) ;
#8684=CARTESIAN_POINT ( 'NONE',  ( -0.3486774197067336045, 3.267716535433071279, 1.209717811016577845E-16 ) ) ;
#8686=CARTESIAN_POINT ( 'NONE',  ( -0.6214413264104945434, 3.346456692913386100, -1.417322834645664331 ) ) ;
#8689=CARTESIAN_POINT ( 'NONE',  ( 4.268512490100411402E-16, 3.346456692913386100, 0.9448818897637749625 ) ) ;
#8692=ORIENTED_EDGE ( 'NONE', *, *, #11893, .F. ) ;
#8693=DIRECTION ( 'NONE',  ( 0.000000000000000000, -1.000000000000000000, 0.000000000000000000 ) ) ;
#8694=VERTEX_POINT ( 'NONE', #15761 ) ;
#8696=EDGE_CURVE ( 'NONE', #2462, #43721, #11392, .T. ) ;
#8697=VECTOR ( 'NONE', #3679, 39.37007874015748143 ) ;
#8698=DIRECTION ( 'NONE',  ( -0.000000000000000000, 1.000000000000000000, -0.000000000000000000 ) ) ;
#8699=DIRECTION ( 'NONE',  ( -0.000000000000000000, 1.000000000000000000, -0.000000000000000000 ) ) ;
#8700=LINE ( 'NONE', #40204, #43251 ) ;
#8701=ADVANCED_FACE ( 'NONE', ( #3645 ), #46474, .F. ) ;
#8702=AXIS2_PLACEMENT_3D ( 'NONE', #29602, #45318, #25721 ) ;
#8703=ORIENTED_EDGE ( 'NONE', *, *, #11287, .F. ) ;
#8704=ORIENTED_EDGE ( 'NONE', *, *, #15285, .F. ) ;
#8705=DIRECTION ( 'NONE',  ( 1.000000000000000000, 0.000000000000000000, 0.000000000000000000 ) ) ;
#8706=ORIENTED_EDGE ( 'NONE', *, *, #35063, .F. ) ;
#8707=ADVANCED_FACE ( 'NONE', ( #39008 ), #15517, .F. ) ;
#8708=CARTESIAN_POINT ( 'NONE',  ( -0.8182917201112819283, 3.267716535433071279, 0.1574803149606285035 ) ) ;
#8709=ORIENTED_EDGE ( 'NONE', *, *, #33461, .F. ) ;
#8710=EDGE_CURVE ( 'NONE', #32803, #47925, #23255, .T. ) ;
#8711=DIRECTION ( 'NONE',  ( -3.469446951953613696E-16, 0.000000000000000000, -1.000000000000000000 ) ) ;
#8713=CARTESIAN_POINT ( 'NONE',  ( 0.1968503937007873017, 3.346456692913386100, -0.3149606299212591165 ) ) ;
#8716=CARTESIAN_POINT ( 'NONE',  ( 0.000000000000000000, 3.267716535433071279, -2.244094488188969727 ) ) ;
#8717=ORIENTED_EDGE ( 'NONE', *, *, #6683, .F. ) ;
#8718=EDGE_CURVE ( 'NONE', #46669, #27924, #35646, .T. ) ;
#8720=EDGE_LOOP ( 'NONE', ( #26797, #39532, #47455, #16905 ) ) ;
#8721=ORIENTED_EDGE ( 'NONE', *, *, #45834, .T. ) ;
#8722=EDGE_CURVE ( 'NONE', #18090, #20587, #1041, .T. ) ;
#8723=EDGE_CURVE ( 'NONE', #46164, #34660, #17061, .T. ) ;
#8724=DIRECTION ( 'NONE',  ( -0.000000000000000000, 1.000000000000000000, -0.000000000000000000 ) ) ;
#8726=ORIENTED_EDGE ( 'NONE', *, *, #23448, .T. ) ;
#8728=VECTOR ( 'NONE', #44381, 39.37007874015748143 ) ;
#8730=CARTESIAN_POINT ( 'NONE',  ( 0.5455278134075211005, 3.267716535433071279, -1.141732283464564013 ) ) ;
#8731=DIRECTION ( 'NONE',  ( -0.000000000000000000, 1.000000000000000000, -0.000000000000000000 ) ) ;
#8734=ORIENTED_EDGE ( 'NONE', *, *, #16855, .F. ) ;
#8735=VECTOR ( 'NONE', #43666, 39.37007874015748143 ) ;
#8736=CARTESIAN_POINT ( 'NONE',  ( 1.560669927219590747, 0.000000000000000000, 1.102362204724403938 ) ) ;
#8737=DIRECTION ( 'NONE',  ( 1.000000000000000000, -0.000000000000000000, 0.000000000000000000 ) ) ;
#8739=DIRECTION ( 'NONE',  ( 1.000000000000000000, 0.000000000000000000, 0.000000000000000000 ) ) ;
#8740=LINE ( 'NONE', #24747, #26810 ) ;
#8741=LINE ( 'NONE', #32246, #20689 ) ;
#8743=ORIENTED_EDGE ( 'NONE', *, *, #40634, .F. ) ;
#8744=EDGE_CURVE ( 'NONE', #50070, #46776, #45596, .T. ) ;
#8747=DIRECTION ( 'NONE',  ( 0.000000000000000000, -0.000000000000000000, -1.000000000000000000 ) ) ;
#8749=EDGE_CURVE ( 'NONE', #50070, #26751, #36937, .T. ) ;
#8750=FACE_OUTER_BOUND ( 'NONE', #9935, .T. ) ;
#8751=CARTESIAN_POINT ( 'NONE',  ( 0.8182917201112824834, 3.346456692913386100, 1.732283464566921172 ) ) ;
#8752=EDGE_CURVE ( 'NONE', #46970, #912, #25834, .T. ) ;
#8754=LINE ( 'NONE', #13657, #11245 ) ;
#8755=ORIENTED_EDGE ( 'NONE', *, *, #30047, .T. ) ;
#8756=ADVANCED_FACE ( 'NONE', ( #12403 ), #20141, .F. ) ;
#8757=AXIS2_PLACEMENT_3D ( 'NONE', #27643, #36181, #23783 ) ;
#8758=DIRECTION ( 'NONE',  ( 1.000000000000000000, 0.000000000000000000, -3.469446951953613696E-16 ) ) ;
#8759=VECTOR ( 'NONE', #1487, 39.37007874015748143 ) ;
#8761=VECTOR ( 'NONE', #3022, 39.37007874015748143 ) ;
#8764=VECTOR ( 'NONE', #29730, 39.37007874015748143 ) ;
#8765=VERTEX_POINT ( 'NONE', #9304 ) ;
#8766=CARTESIAN_POINT ( 'NONE',  ( 1.091055626815042645, 3.346456692913386100, 0.7480314960629872445 ) ) ;
#8767=LINE ( 'NONE', #24520, #23955 ) ;
#8768=VECTOR ( 'NONE', #50232, 39.37007874015748143 ) ;
#8770=AXIS2_PLACEMENT_3D ( 'NONE', #49183, #13861, #45831 ) ;
#8772=ORIENTED_EDGE ( 'NONE', *, *, #41715, .T. ) ;
#8775=DIRECTION ( 'NONE',  ( -0.000000000000000000, 1.000000000000000000, -0.000000000000000000 ) ) ;
#8778=DIRECTION ( 'NONE',  ( -1.000000000000000000, 0.000000000000000000, -0.000000000000000000 ) ) ;
#8780=ORIENTED_EDGE ( 'NONE', *, *, #34627, .F. ) ;
#8782=CARTESIAN_POINT ( 'NONE',  ( 0.4696143004045481018, 3.267716535433071279, -1.629301903132388246E-16 ) ) ;
#8784=EDGE_LOOP ( 'NONE', ( #24882, #9743, #16857, #27576 ) ) ;
#8785=VERTEX_POINT ( 'NONE', #4402 ) ;
#8788=CARTESIAN_POINT ( 'NONE',  ( -1.712496953225537188, 3.267716535433071279, 5.941417334598190051E-16 ) ) ;
#8791=DIRECTION ( 'NONE',  ( -1.000000000000000000, 0.000000000000000000, 0.000000000000000000 ) ) ;
#8793=ORIENTED_EDGE ( 'NONE', *, *, #20165, .T. ) ;
#8796=VECTOR ( 'NONE', #38714, 39.37007874015748143 ) ;
#8798=VECTOR ( 'NONE', #5567, 39.37007874015748143 ) ;
#8799=DIRECTION ( 'NONE',  ( -1.000000000000000000, 0.000000000000000000, 0.000000000000000000 ) ) ;
#8800=CARTESIAN_POINT ( 'NONE',  ( -1.363819533518803473, 3.346456692913386100, -1.605145679676863057 ) ) ;
#8804=DIRECTION ( 'NONE',  ( -1.000000000000000000, 0.000000000000000000, -0.000000000000000000 ) ) ;
#8806=VECTOR ( 'NONE', #35190, 39.37007874015748143 ) ;
#8808=DIRECTION ( 'NONE',  ( 1.000000000000000000, 0.000000000000000000, 0.000000000000000000 ) ) ;
#8811=ORIENTED_EDGE ( 'NONE', *, *, #6799, .F. ) ;
#8812=CARTESIAN_POINT ( 'NONE',  ( -1.712496953225537633, 3.267716535433071279, 1.417322834645662333 ) ) ;
#8813=DIRECTION ( 'NONE',  ( -1.000000000000000000, 0.000000000000000000, 0.000000000000000000 ) ) ;
#8814=FACE_OUTER_BOUND ( 'NONE', #30517, .T. ) ;
#8815=ADVANCED_FACE ( 'NONE', ( #40548 ), #5170, .F. ) ;
#8818=EDGE_CURVE ( 'NONE', #1340, #35947, #35903, .T. ) ;
#8819=ORIENTED_EDGE ( 'NONE', *, *, #34591, .F. ) ;
#8821=VERTEX_POINT ( 'NONE', #530 ) ;
#8824=ORIENTED_EDGE ( 'NONE', *, *, #50451, .F. ) ;
#8825=CARTESIAN_POINT ( 'NONE',  ( -1.909347346926324906, 0.000000000000000000, -1.299212598425193210 ) ) ;
#8827=CARTESIAN_POINT ( 'NONE',  ( -0.2727639067037602172, 3.346456692913386100, 1.732283464566921172 ) ) ;
#8828=AXIS2_PLACEMENT_3D ( 'NONE', #37786, #14276, #28999 ) ;
#8829=ORIENTED_EDGE ( 'NONE', *, *, #38718, .T. ) ;
#8830=EDGE_LOOP ( 'NONE', ( #1598, #37943, #35775, #2230 ) ) ;
#8832=CARTESIAN_POINT ( 'NONE',  ( -0.5455278134075216556, 3.346456692913386100, -2.204724409448810540 ) ) ;
#8834=ORIENTED_EDGE ( 'NONE', *, *, #15962, .F. ) ;
#8836=LINE ( 'NONE', #32603, #44213 ) ;
#8837=CARTESIAN_POINT ( 'NONE',  ( -0.8942052331142552601, 3.346456692913386100, 2.204724409448808764 ) ) ;
#8839=EDGE_LOOP ( 'NONE', ( #1232, #37953, #48018, #48319 ) ) ;
#8840=EDGE_CURVE ( 'NONE', #45259, #24676, #24286, .T. ) ;
#8841=DIRECTION ( 'NONE',  ( 1.000000000000000000, 0.000000000000000000, 0.000000000000000000 ) ) ;
#8842=CARTESIAN_POINT ( 'NONE',  ( 0.4696143004045478797, 0.000000000000000000, -0.3543307086614173040 ) ) ;
#8843=LINE ( 'NONE', #13995, #12142 ) ;
#8844=ORIENTED_EDGE ( 'NONE', *, *, #27196, .T. ) ;
#8845=DIRECTION ( 'NONE',  ( 0.000000000000000000, 0.000000000000000000, -1.000000000000000000 ) ) ;
#8846=CARTESIAN_POINT ( 'NONE',  ( -2.103998301714549157, 3.267716535433071279, -0.5118110236220464460 ) ) ;
#8849=FACE_OUTER_BOUND ( 'NONE', #12535, .T. ) ;
#8850=EDGE_LOOP ( 'NONE', ( #22844, #27179, #40350, #525 ) ) ;
#8855=EDGE_CURVE ( 'NONE', #29456, #28387, #40293, .T. ) ;
#8856=CARTESIAN_POINT ( 'NONE',  ( -1.439733046521777027, 3.346456692913386100, -0.5118110236220466680 ) ) ;
#8857=DIRECTION ( 'NONE',  ( -3.469446951953613696E-16, 0.000000000000000000, -1.000000000000000000 ) ) ;
#8858=CARTESIAN_POINT ( 'NONE',  ( -0.5455278134075214336, 3.267716535433071279, 9.463399047163224412E-17 ) ) ;
#8859=ORIENTED_EDGE ( 'NONE', *, *, #1186, .T. ) ;
#8860=ORIENTED_EDGE ( 'NONE', *, *, #45843, .T. ) ;
#8861=CARTESIAN_POINT ( 'NONE',  ( 0.2727639067037604392, 3.267716535433071279, -1.614173228346451605 ) ) ;
#8862=VERTEX_POINT ( 'NONE', #13948 ) ;
#8863=PLANE ( 'NONE',  #28584 ) ;
#8864=DIRECTION ( 'NONE',  ( -0.000000000000000000, 1.000000000000000000, -0.000000000000000000 ) ) ;
#8865=VECTOR ( 'NONE', #36986, 39.37007874015748143 ) ;
#8866=VECTOR ( 'NONE', #293, 39.37007874015748143 ) ;
#8868=CARTESIAN_POINT ( 'NONE',  ( 4.268512490100411402E-16, 0.000000000000000000, 1.259842519685033357 ) ) ;
#8869=DIRECTION ( 'NONE',  ( -0.000000000000000000, 1.000000000000000000, -0.000000000000000000 ) ) ;
#8870=ORIENTED_EDGE ( 'NONE', *, *, #3987, .T. ) ;
#8872=FACE_OUTER_BOUND ( 'NONE', #43122, .T. ) ;
#8874=PLANE ( 'NONE',  #28177 ) ;
#8878=FACE_OUTER_BOUND ( 'NONE', #14737, .T. ) ;
#8879=DIRECTION ( 'NONE',  ( 1.734723475976806848E-16, 0.000000000000000000, 1.000000000000000000 ) ) ;
#8880=LINE ( 'NONE', #50917, #44028 ) ;
#8881=ADVANCED_FACE ( 'NONE', ( #21952 ), #29692, .F. ) ;
#8882=EDGE_CURVE ( 'NONE', #12300, #4494, #6455, .T. ) ;
#8884=CARTESIAN_POINT ( 'NONE',  ( -0.8942052331142552601, 3.346456692913386100, -1.889763779527552146 ) ) ;
#8885=CARTESIAN_POINT ( 'NONE',  ( -0.5455278134075214336, 3.267716535433071279, -0.1968503937007883287 ) ) ;
#8888=DIRECTION ( 'NONE',  ( 1.734723475976806848E-16, -0.000000000000000000, 1.000000000000000000 ) ) ;
#8889=EDGE_CURVE ( 'NONE', #37676, #36095, #6199, .T. ) ;
#8890=DIRECTION ( 'NONE',  ( 0.000000000000000000, 1.000000000000000000, 0.000000000000000000 ) ) ;
#8891=CARTESIAN_POINT ( 'NONE',  ( 1.833433833923351353, 3.346456692913386100, 0.3149606299212576177 ) ) ;
#8895=ORIENTED_EDGE ( 'NONE', *, *, #40283, .T. ) ;
#8896=CARTESIAN_POINT ( 'NONE',  ( -0.3486774197067334935, 3.346456692913386100, 1.692913385826762873 ) ) ;
#8897=CYLINDRICAL_SURFACE ( 'NONE', #16390, 2.952755905511811552 ) ;
#8899=LINE ( 'NONE', #48100, #16808 ) ;
#8901=PLANE ( 'NONE',  #42598 ) ;
#8902=LINE ( 'NONE', #31902, #22383 ) ;
#8903=ORIENTED_EDGE ( 'NONE', *, *, #37373, .T. ) ;
#8904=EDGE_LOOP ( 'NONE', ( #12784, #37164, #36281, #40491 ) ) ;
#8905=EDGE_CURVE ( 'NONE', #28960, #13304, #10073, .T. ) ;
#8906=DIRECTION ( 'NONE',  ( 1.000000000000000000, 0.000000000000000000, -3.469446951953613696E-16 ) ) ;
#8908=VECTOR ( 'NONE', #43474, 39.37007874015748143 ) ;
#8909=VECTOR ( 'NONE', #17523, 39.37007874015748143 ) ;
#8910=DIRECTION ( 'NONE',  ( 1.734723475976806848E-16, -0.000000000000000000, 1.000000000000000000 ) ) ;
#8911=VERTEX_POINT ( 'NONE', #2324 ) ;
#8913=FACE_BOUND ( 'NONE', #722, .T. ) ;
#8914=EDGE_LOOP ( 'NONE', ( #45865, #44511, #14367, #9220 ) ) ;
#8916=CARTESIAN_POINT ( 'NONE',  ( 0.000000000000000000, 3.267716535433071279, 0.000000000000000000 ) ) ;
#8917=EDGE_LOOP ( 'NONE', ( #30355, #13109, #1790, #22317 ) ) ;
#8921=VECTOR ( 'NONE', #22985, 39.37007874015748143 ) ;
#8923=VERTEX_POINT ( 'NONE', #9819 ) ;
#8924=DIRECTION ( 'NONE',  ( -1.000000000000000000, -0.000000000000000000, -0.000000000000000000 ) ) ;
#8925=VECTOR ( 'NONE', #23703, 39.37007874015748143 ) ;
#8928=DIRECTION ( 'NONE',  ( 1.000000000000000000, -0.000000000000000000, 0.000000000000000000 ) ) ;
#8929=EDGE_CURVE ( 'NONE', #706, #12462, #33069, .T. ) ;
#8930=DIRECTION ( 'NONE',  ( 1.000000000000000000, -0.000000000000000000, 0.000000000000000000 ) ) ;
#8933=DIRECTION ( 'NONE',  ( 0.000000000000000000, 0.000000000000000000, -1.000000000000000000 ) ) ;
#8934=DIRECTION ( 'NONE',  ( 1.734723475976806848E-16, -0.000000000000000000, 1.000000000000000000 ) ) ;
#8935=ORIENTED_EDGE ( 'NONE', *, *, #27640, .F. ) ;
#8936=CARTESIAN_POINT ( 'NONE',  ( 0.2727639067037609943, 3.346456692913386100, 0.9055118110236167750 ) ) ;
#8937=LINE ( 'NONE', #43264, #28945 ) ;
#8938=EDGE_LOOP ( 'NONE', ( #31193, #14617, #7266, #9470 ) ) ;
#8939=CARTESIAN_POINT ( 'NONE',  ( 1.833433833923351353, 3.346456692913386100, -0.1968503937007886062 ) ) ;
#8941=ORIENTED_EDGE ( 'NONE', *, *, #18487, .F. ) ;
#8942=DIRECTION ( 'NONE',  ( -0.000000000000000000, 1.000000000000000000, -0.000000000000000000 ) ) ;
#8943=VECTOR ( 'NONE', #18803, 39.37007874015748143 ) ;
#8946=ADVANCED_FACE ( 'NONE', ( #22455 ), #33832, .F. ) ;
#8947=ORIENTED_EDGE ( 'NONE', *, *, #36408, .T. ) ;
#8948=AXIS2_PLACEMENT_3D ( 'NONE', #43183, #19192, #3962 ) ;
#8950=VERTEX_POINT ( 'NONE', #45658 ) ;
#8951=FACE_BOUND ( 'NONE', #11720, .T. ) ;
#8952=EDGE_CURVE ( 'NONE', #33042, #41687, #10325, .T. ) ;
#8953=DIRECTION ( 'NONE',  ( 1.734723475976806848E-16, 0.000000000000000000, 1.000000000000000000 ) ) ;
#8955=VECTOR ( 'NONE', #30677, 39.37007874015748143 ) ;
#8958=EDGE_CURVE ( 'NONE', #36771, #3425, #48754, .T. ) ;
#8959=EDGE_CURVE ( 'NONE', #26189, #21459, #2576, .T. ) ;
#8961=ORIENTED_EDGE ( 'NONE', *, *, #40611, .T. ) ;
#8962=VERTEX_POINT ( 'NONE', #29169 ) ;
#8963=CARTESIAN_POINT ( 'NONE',  ( -0.2727639067037610499, 3.346456692913386100, -2.047244094488181343 ) ) ;
#8964=ORIENTED_EDGE ( 'NONE', *, *, #43080, .T. ) ;
#8965=VECTOR ( 'NONE', #2480, 39.37007874015748143 ) ;
#8967=VERTEX_POINT ( 'NONE', #34080 ) ;
#8968=CARTESIAN_POINT ( 'NONE',  ( -1.985260859929297572, 3.346456692913386100, 0.6299212598425164567 ) ) ;
#8971=ORIENTED_EDGE ( 'NONE', *, *, #47467, .F. ) ;
#8972=PLANE ( 'NONE',  #25752 ) ;
#8974=EDGE_CURVE ( 'NONE', #44686, #36221, #29105, .T. ) ;
#8975=CARTESIAN_POINT ( 'NONE',  ( -2.454875160333845674, 0.000000000000000000, 0.1574803149606286423 ) ) ;
#8976=EDGE_LOOP ( 'NONE', ( #19644, #23737, #2438, #28678 ) ) ;
#8978=VECTOR ( 'NONE', #12841, 39.37007874015748143 ) ;
#8980=ORIENTED_EDGE ( 'NONE', *, *, #27, .F. ) ;
#8982=CARTESIAN_POINT ( 'NONE',  ( -0.5455278134075214336, 3.267716535433071279, -1.141732283464563791 ) ) ;
#8983=ORIENTED_EDGE ( 'NONE', *, *, #4709, .F. ) ;
#8984=CARTESIAN_POINT ( 'NONE',  ( 0.5455278134075212115, 0.000000000000000000, -0.9448818897637765168 ) ) ;
#8986=ORIENTED_EDGE ( 'NONE', *, *, #20762, .F. ) ;
#8987=DIRECTION ( 'NONE',  ( -0.000000000000000000, 1.000000000000000000, -0.000000000000000000 ) ) ;
#8988=CARTESIAN_POINT ( 'NONE',  ( -0.6214413264104945434, 3.267716535433071279, -0.03937007874015895081 ) ) ;
#8989=VECTOR ( 'NONE', #48799, 39.37007874015748143 ) ;
#8992=LINE ( 'NONE', #476, #2511 ) ;
#8994=VERTEX_POINT ( 'NONE', #41065 ) ;
#8995=CARTESIAN_POINT ( 'NONE',  ( -0.2727639067037602727, 3.346456692913386100, 1.220472440944875281 ) ) ;
#8997=CARTESIAN_POINT ( 'NONE',  ( 0.7423782071083087075, 0.000000000000000000, 0.6299212598425161236 ) ) ;
#8998=PLANE ( 'NONE',  #49672 ) ;
#8999=EDGE_CURVE ( 'NONE', #21605, #1831, #1923, .T. ) ;
#9002=ADVANCED_FACE ( 'NONE', ( #50269 ), #3330, .F. ) ;
#9004=LINE ( 'NONE', #24241, #19357 ) ;
#9005=ORIENTED_EDGE ( 'NONE', *, *, #10519, .F. ) ;
#9008=EDGE_LOOP ( 'NONE', ( #32200, #31912, #18041, #30567 ) ) ;
#9009=FACE_BOUND ( 'NONE', #16333, .T. ) ;
#9011=DIRECTION ( 'NONE',  ( -0.000000000000000000, 0.000000000000000000, 1.000000000000000000 ) ) ;
#9014=CARTESIAN_POINT ( 'NONE',  ( 1.091055626815042423, 0.000000000000000000, -1.771653543307081691 ) ) ;
#9015=DIRECTION ( 'NONE',  ( -1.000000000000000000, 0.000000000000000000, 1.734723475976806848E-16 ) ) ;
#9016=FACE_OUTER_BOUND ( 'NONE', #21534, .T. ) ;
#9017=AXIS2_PLACEMENT_3D ( 'NONE', #31312, #16325, #47261 ) ;
#9018=EDGE_LOOP ( 'NONE', ( #4880, #37174, #273, #32861 ) ) ;
#9019=ADVANCED_FACE ( 'NONE', ( #22956 ), #7458, .F. ) ;
#9023=CARTESIAN_POINT ( 'NONE',  ( -1.166969139818015533, 0.000000000000000000, 1.417322834645662777 ) ) ;
#9024=ORIENTED_EDGE ( 'NONE', *, *, #28463, .T. ) ;
#9025=VECTOR ( 'NONE', #49573, 39.37007874015748143 ) ;
#9026=CARTESIAN_POINT ( 'NONE',  ( -1.195183497228115035E-16, 0.000000000000000000, -1.259842519685035134 ) ) ;
#9027=DIRECTION ( 'NONE',  ( -1.000000000000000000, 0.000000000000000000, 1.734723475976806848E-16 ) ) ;
#9028=VECTOR ( 'NONE', #18481, 39.37007874015748143 ) ;
#9029=CARTESIAN_POINT ( 'NONE',  ( 1.636583440222563635, 3.346456692913386100, -1.259842519685035800 ) ) ;
#9030=ORIENTED_EDGE ( 'NONE', *, *, #22981, .T. ) ;
#9033=CARTESIAN_POINT ( 'NONE',  ( -1.439733046521776361, 3.346456692913386100, 0.1181102362204704270 ) ) ;
#9034=FACE_BOUND ( 'NONE', #47534, .T. ) ;
#9035=AXIS2_PLACEMENT_3D ( 'NONE', #27915, #19904, #11917 ) ;
#9037=CARTESIAN_POINT ( 'NONE',  ( -0.8182917201112814842, 0.000000000000000000, 1.417322834645662777 ) ) ;
#9039=ORIENTED_EDGE ( 'NONE', *, *, #14212, .F. ) ;
#9041=VERTEX_POINT ( 'NONE', #38709 ) ;
#9042=ORIENTED_EDGE ( 'NONE', *, *, #20849, .T. ) ;
#9043=EDGE_CURVE ( 'NONE', #36095, #24457, #39057, .T. ) ;
#9045=CARTESIAN_POINT ( 'NONE',  ( 1.091055626815043311, 3.267716535433071279, 1.692913385826762873 ) ) ;
#9046=DIRECTION ( 'NONE',  ( 0.000000000000000000, 0.000000000000000000, 1.000000000000000000 ) ) ;
#9047=ADVANCED_FACE ( 'NONE', ( #34830 ), #30958, .F. ) ;
#9049=EDGE_CURVE ( 'NONE', #16457, #22729, #13495, .T. ) ;
#9050=DIRECTION ( 'NONE',  ( -3.469446951953613696E-16, 0.000000000000000000, -1.000000000000000000 ) ) ;
#9051=CARTESIAN_POINT ( 'NONE',  ( 0.000000000000000000, 3.267716535433071279, -1.102362204724405714 ) ) ;
#9055=CARTESIAN_POINT ( 'NONE',  ( 1.833433833923350909, 3.267716535433071279, 1.152076279655074087 ) ) ;
#9056=DIRECTION ( 'NONE',  ( -3.469446951953613696E-16, 0.000000000000000000, -1.000000000000000000 ) ) ;
#9057=CARTESIAN_POINT ( 'NONE',  ( 0.1968503937007873017, 0.000000000000000000, 0.6299212598425161236 ) ) ;
#9059=LINE ( 'NONE', #1571, #47815 ) ;
#9060=AXIS2_PLACEMENT_3D ( 'NONE', #8481, #11834, #24230 ) ;
#9063=LINE ( 'NONE', #21199, #40732 ) ;
#9064=ORIENTED_EDGE ( 'NONE', *, *, #40711, .T. ) ;
#9065=LINE ( 'NONE', #9578, #44841 ) ;
#9066=DIRECTION ( 'NONE',  ( 1.734723475976806848E-16, -0.000000000000000000, 1.000000000000000000 ) ) ;
#9068=ORIENTED_EDGE ( 'NONE', *, *, #39495, .T. ) ;
#9069=EDGE_CURVE ( 'NONE', #35441, #16692, #14956, .T. ) ;
#9070=ORIENTED_EDGE ( 'NONE', *, *, #2538, .F. ) ;
#9073=ORIENTED_EDGE ( 'NONE', *, *, #27462, .T. ) ;
#9074=EDGE_CURVE ( 'NONE', #37676, #13035, #27317, .T. ) ;
#9075=ADVANCED_FACE ( 'NONE', ( #15461 ), #11583, .F. ) ;
#9076=VERTEX_POINT ( 'NONE', #31463 ) ;
#9078=EDGE_LOOP ( 'NONE', ( #8755, #22675, #17088, #27288 ) ) ;
#9079=ORIENTED_EDGE ( 'NONE', *, *, #13434, .T. ) ;
#9080=CARTESIAN_POINT ( 'NONE',  ( 0.000000000000000000, 3.267716535433071279, 0.5905511811023582691 ) ) ;
#9081=DIRECTION ( 'NONE',  ( 1.000000000000000000, 0.000000000000000000, -3.469446951953613696E-16 ) ) ;
#9083=VERTEX_POINT ( 'NONE', #11334 ) ;
#9084=ORIENTED_EDGE ( 'NONE', *, *, #39592, .F. ) ;
#9085=DIRECTION ( 'NONE',  ( -3.469446951953613696E-16, 0.000000000000000000, -1.000000000000000000 ) ) ;
#9086=VERTEX_POINT ( 'NONE', #43062 ) ;
#9087=ORIENTED_EDGE ( 'NONE', *, *, #13398, .T. ) ;
#9088=LINE ( 'NONE', #36723, #44600 ) ;
#9089=DIRECTION ( 'NONE',  ( -0.000000000000000000, 0.000000000000000000, 1.000000000000000000 ) ) ;
#9090=DIRECTION ( 'NONE',  ( -0.000000000000000000, 0.000000000000000000, 1.000000000000000000 ) ) ;
#9091=VECTOR ( 'NONE', #39463, 39.37007874015748143 ) ;
#9092=ORIENTED_EDGE ( 'NONE', *, *, #1904, .F. ) ;
#9093=VECTOR ( 'NONE', #12466, 39.37007874015748143 ) ;
#9095=LINE ( 'NONE', #5478, #6072 ) ;
#9096=PLANE ( 'NONE',  #11335 ) ;
#9097=ORIENTED_EDGE ( 'NONE', *, *, #30234, .T. ) ;
#9099=FACE_OUTER_BOUND ( 'NONE', #48031, .T. ) ;
#9101=VERTEX_POINT ( 'NONE', #27067 ) ;
#9102=ORIENTED_EDGE ( 'NONE', *, *, #40136, .T. ) ;
#9103=VECTOR ( 'NONE', #10046, 39.37007874015748143 ) ;
#9104=DIRECTION ( 'NONE',  ( -1.000000000000000000, 0.000000000000000000, -0.000000000000000000 ) ) ;
#9105=CARTESIAN_POINT ( 'NONE',  ( 0.5455278134075208785, 0.000000000000000000, -1.574803149606293529 ) ) ;
#9106=FACE_OUTER_BOUND ( 'NONE', #33349, .T. ) ;
#9108=EDGE_CURVE ( 'NONE', #34031, #40030, #42314, .T. ) ;
#9109=DIRECTION ( 'NONE',  ( -0.000000000000000000, 1.000000000000000000, -0.000000000000000000 ) ) ;
#9110=DIRECTION ( 'NONE',  ( -0.000000000000000000, 1.000000000000000000, -0.000000000000000000 ) ) ;
#9111=VERTEX_POINT ( 'NONE', #11833 ) ;
#9112=ORIENTED_EDGE ( 'NONE', *, *, #142, .F. ) ;
#9113=EDGE_CURVE ( 'NONE', #36589, #8562, #51019, .T. ) ;
#9116=LINE ( 'NONE', #17631, #38159 ) ;
#9117=DIRECTION ( 'NONE',  ( 0.000000000000000000, 0.000000000000000000, -1.000000000000000000 ) ) ;
#9119=CARTESIAN_POINT ( 'NONE',  ( 0.000000000000000000, 3.313179664429866556, -2.422428857167389982 ) ) ;
#9124=CARTESIAN_POINT ( 'NONE',  ( 0.7423782071083084855, 3.267716535433071279, -1.889763779527552812 ) ) ;
#9125=EDGE_CURVE ( 'NONE', #48261, #11767, #36103, .T. ) ;
#9128=ORIENTED_EDGE ( 'NONE', *, *, #31110, .F. ) ;
#9130=EDGE_CURVE ( 'NONE', #29370, #45283, #213, .T. ) ;
#9132=LINE ( 'NONE', #12240, #4702 ) ;
#9135=CARTESIAN_POINT ( 'NONE',  ( -1.091055626815042645, 3.346456692913386100, -2.086614173228339641 ) ) ;
#9136=EDGE_CURVE ( 'NONE', #46482, #30180, #28601, .T. ) ;
#9137=CARTESIAN_POINT ( 'NONE',  ( 0.4696143004045483793, 3.267716535433071279, -1.629301903132388985E-16 ) ) ;
#9138=EDGE_CURVE ( 'NONE', #36547, #12398, #28341, .T. ) ;
#9139=EDGE_LOOP ( 'NONE', ( #3163, #248 ) ) ;
#9140=CARTESIAN_POINT ( 'NONE',  ( 0.7423782071083082634, 3.267716535433071279, -1.771653543307081025 ) ) ;
#9142=DIRECTION ( 'NONE',  ( -1.000000000000000000, 0.000000000000000000, 0.000000000000000000 ) ) ;
#9144=EDGE_CURVE ( 'NONE', #19095, #8962, #42334, .T. ) ;
#9145=FACE_OUTER_BOUND ( 'NONE', #35424, .T. ) ;
#9147=CARTESIAN_POINT ( 'NONE',  ( -1.712496953225537633, 3.267716535433071279, -0.4724409448818884805 ) ) ;
#9148=DIRECTION ( 'NONE',  ( 0.000000000000000000, 0.000000000000000000, 1.000000000000000000 ) ) ;
#9149=DIRECTION ( 'NONE',  ( 0.000000000000000000, 0.000000000000000000, -1.000000000000000000 ) ) ;
#9150=ORIENTED_EDGE ( 'NONE', *, *, #5384, .F. ) ;
#9151=EDGE_LOOP ( 'NONE', ( #44943, #41085, #26564, #5646 ) ) ;
#9152=CARTESIAN_POINT ( 'NONE',  ( 0.4696143004045479352, 3.346456692913386100, 0.7874015748031454320 ) ) ;
#9154=LINE ( 'NONE', #13033, #9797 ) ;
#9155=ORIENTED_EDGE ( 'NONE', *, *, #31235, .F. ) ;
#9156=CARTESIAN_POINT ( 'NONE',  ( 0.8182917201112819283, 0.000000000000000000, -0.7874015748031473194 ) ) ;
#9157=CARTESIAN_POINT ( 'NONE',  ( 1.363819533518803251, 0.000000000000000000, -0.7874015748031473194 ) ) ;
#9158=DIRECTION ( 'NONE',  ( 1.000000000000000000, 0.000000000000000000, -3.469446951953613696E-16 ) ) ;
#9159=DIRECTION ( 'NONE',  ( 0.000000000000000000, 0.000000000000000000, -1.000000000000000000 ) ) ;
#9161=ORIENTED_EDGE ( 'NONE', *, *, #47787, .F. ) ;
#9164=DIRECTION ( 'NONE',  ( -1.000000000000000000, 0.000000000000000000, 0.000000000000000000 ) ) ;
#9165=CARTESIAN_POINT ( 'NONE',  ( -2.454875160333845674, 3.232777166330581320, 0.1574803149606286423 ) ) ;
#9167=DIRECTION ( 'NONE',  ( 1.000000000000000000, 0.000000000000000000, -3.469446951953613696E-16 ) ) ;
#9168=FACE_BOUND ( 'NONE', #7533, .T. ) ;
#9171=ORIENTED_EDGE ( 'NONE', *, *, #45402, .F. ) ;
#9172=ORIENTED_EDGE ( 'NONE', *, *, #33648, .T. ) ;
#9174=VECTOR ( 'NONE', #14204, 39.37007874015748143 ) ;
#9175=VECTOR ( 'NONE', #21225, 39.37007874015748143 ) ;
#9176=ORIENTED_EDGE ( 'NONE', *, *, #40309, .F. ) ;
#9180=EDGE_CURVE ( 'NONE', #31704, #10848, #12096, .T. ) ;
#9181=EDGE_CURVE ( 'NONE', #30078, #14009, #8225, .T. ) ;
#9184=CARTESIAN_POINT ( 'NONE',  ( 0.2727639067037604392, 3.346456692913386100, -0.6692913385826760875 ) ) ;
#9186=DIRECTION ( 'NONE',  ( -3.469446951953613696E-16, 0.000000000000000000, -1.000000000000000000 ) ) ;
#9188=CARTESIAN_POINT ( 'NONE',  ( 4.268512490100411402E-16, 3.346456692913386100, 0.9448818897637749625 ) ) ;
#9191=ORIENTED_EDGE ( 'NONE', *, *, #32370, .F. ) ;
#9193=DIRECTION ( 'NONE',  ( 1.000000000000000000, 0.000000000000000000, -3.469446951953613696E-16 ) ) ;
#9195=CARTESIAN_POINT ( 'NONE',  ( -1.363819533518803029, 0.000000000000000000, 1.417322834645662777 ) ) ;
#9197=PLANE ( 'NONE',  #27763 ) ;
#9198=ORIENTED_EDGE ( 'NONE', *, *, #44323, .T. ) ;
#9199=CARTESIAN_POINT ( 'NONE',  ( -2.102985103392958077, 3.346456692913386100, 0.1181102362204704270 ) ) ;
#9200=CARTESIAN_POINT ( 'NONE',  ( 1.636583440222563635, 3.267716535433071279, -2.839019714148966584E-16 ) ) ;
#9202=ADVANCED_FACE ( 'NONE', ( #16484 ), #8480, .F. ) ;
#9203=EDGE_CURVE ( 'NONE', #43398, #17597, #40234, .T. ) ;
#9204=ORIENTED_EDGE ( 'NONE', *, *, #18050, .T. ) ;
#9205=DIRECTION ( 'NONE',  ( 0.000000000000000000, 1.000000000000000000, 0.000000000000000000 ) ) ;
#9206=ORIENTED_EDGE ( 'NONE', *, *, #36351, .T. ) ;
#9207=FACE_BOUND ( 'NONE', #17094, .T. ) ;
#9209=AXIS2_PLACEMENT_3D ( 'NONE', #14848, #33971, #2974 ) ;
#9212=LINE ( 'NONE', #17467, #23465 ) ;
#9214=VERTEX_POINT ( 'NONE', #8988 ) ;
#9215=ORIENTED_EDGE ( 'NONE', *, *, #37477, .T. ) ;
#9216=FACE_OUTER_BOUND ( 'NONE', #41309, .T. ) ;
#9218=VECTOR ( 'NONE', #25796, 39.37007874015748143 ) ;
#9219=DIRECTION ( 'NONE',  ( 1.734723475976806848E-16, -0.000000000000000000, 1.000000000000000000 ) ) ;
#9220=ORIENTED_EDGE ( 'NONE', *, *, #36311, .F. ) ;
#9221=LINE ( 'NONE', #16721, #42121 ) ;
#9222=VERTEX_POINT ( 'NONE', #15961 ) ;
#9225=DIRECTION ( 'NONE',  ( 0.000000000000000000, 0.000000000000000000, -1.000000000000000000 ) ) ;
#9227=LINE ( 'NONE', #28844, #43837 ) ;
#9228=ORIENTED_EDGE ( 'NONE', *, *, #45974, .F. ) ;
#9229=EDGE_LOOP ( 'NONE', ( #46804, #46714, #33245, #1498 ) ) ;
#9230=VERTEX_POINT ( 'NONE', #12604 ) ;
#9231=ORIENTED_EDGE ( 'NONE', *, *, #38783, .T. ) ;
#9233=CARTESIAN_POINT ( 'NONE',  ( -1.091055626815042645, 3.346456692913386100, -1.771653543307081025 ) ) ;
#9235=EDGE_CURVE ( 'NONE', #30696, #1746, #39373, .T. ) ;
#9238=DIRECTION ( 'NONE',  ( -3.469446951953613696E-16, 0.000000000000000000, -1.000000000000000000 ) ) ;
#9239=EDGE_LOOP ( 'NONE', ( #11923, #27867, #34400, #18915 ) ) ;
#9240=CARTESIAN_POINT ( 'NONE',  ( -1.536664496436148184E-16, 3.267716535433071279, 0.4330708661417287386 ) ) ;
#9241=EDGE_CURVE ( 'NONE', #40528, #12432, #27234, .T. ) ;
#9242=VECTOR ( 'NONE', #36222, 39.37007874015748143 ) ;
#9243=EDGE_CURVE ( 'NONE', #21615, #5817, #8133, .T. ) ;
#9245=CARTESIAN_POINT ( 'NONE',  ( -1.363819533518803029, 3.267716535433071279, 0.4724409448818871482 ) ) ;
#9246=EDGE_LOOP ( 'NONE', ( #13296, #11006, #43603, #4301 ) ) ;
#9248=DIRECTION ( 'NONE',  ( -0.000000000000000000, 1.000000000000000000, -0.000000000000000000 ) ) ;
#9249=DIRECTION ( 'NONE',  ( -1.000000000000000000, 0.000000000000000000, 1.734723475976806848E-16 ) ) ;
#9250=LINE ( 'NONE', #36881, #30736 ) ;
#9251=PLANE ( 'NONE',  #26639 ) ;
#9252=VECTOR ( 'NONE', #50944, 39.37007874015748143 ) ;
#9253=CARTESIAN_POINT ( 'NONE',  ( -2.097080421798980687, 3.346456692913386100, -0.1968503937007880511 ) ) ;
#9254=CARTESIAN_POINT ( 'NONE',  ( -1.091055626815042645, 3.267716535433071279, -1.771653543307081025 ) ) ;
#9258=ORIENTED_EDGE ( 'NONE', *, *, #10466, .T. ) ;
#9261=ORIENTED_EDGE ( 'NONE', *, *, #48062, .F. ) ;
#9262=CARTESIAN_POINT ( 'NONE',  ( 0.000000000000000000, 3.267716535433071279, 0.1181102362204704270 ) ) ;
#9264=EDGE_LOOP ( 'NONE', ( #25332, #4092, #13393, #38139 ) ) ;
#9265=CARTESIAN_POINT ( 'NONE',  ( 0.000000000000000000, 3.267716535433071279, 0.000000000000000000 ) ) ;
#9267=LINE ( 'NONE', #25774, #48438 ) ;
#9268=FACE_OUTER_BOUND ( 'NONE', #14176, .T. ) ;
#9269=DIRECTION ( 'NONE',  ( -3.469446951953613696E-16, 0.000000000000000000, -1.000000000000000000 ) ) ;
#9271=EDGE_CURVE ( 'NONE', #43549, #7899, #7377, .T. ) ;
#9273=FACE_BOUND ( 'NONE', #43750, .T. ) ;
#9274=ORIENTED_EDGE ( 'NONE', *, *, #46181, .T. ) ;
#9275=DIRECTION ( 'NONE',  ( -0.000000000000000000, 0.000000000000000000, 1.000000000000000000 ) ) ;
#9276=EDGE_CURVE ( 'NONE', #19355, #41467, #7127, .T. ) ;
#9281=CARTESIAN_POINT ( 'NONE',  ( -2.182111253630085290, 0.000000000000000000, -0.1968503937007880511 ) ) ;
#9282=AXIS2_PLACEMENT_3D ( 'NONE', #17989, #40986, #41739 ) ;
#9284=ORIENTED_EDGE ( 'NONE', *, *, #33519, .T. ) ;
#9285=VERTEX_POINT ( 'NONE', #50676 ) ;
#9286=CARTESIAN_POINT ( 'NONE',  ( 0.1968503937007873017, 0.000000000000000000, 0.3149606299212576177 ) ) ;
#9288=PLANE ( 'NONE',  #47940 ) ;
#9289=FACE_BOUND ( 'NONE', #47875, .T. ) ;
#9291=VECTOR ( 'NONE', #20613, 39.37007874015748143 ) ;
#9292=VECTOR ( 'NONE', #25147, 39.37007874015748143 ) ;
#9294=CARTESIAN_POINT ( 'NONE',  ( -1.636583440222564301, 3.346456692913386100, 1.417869535855831753 ) ) ;
#9295=ORIENTED_EDGE ( 'NONE', *, *, #1171, .T. ) ;
#9297=CARTESIAN_POINT ( 'NONE',  ( 0.000000000000000000, 3.267716535433071279, -1.102362204724405714 ) ) ;
#9298=DIRECTION ( 'NONE',  ( 1.000000000000000000, 0.000000000000000000, -3.469446951953613696E-16 ) ) ;
#9300=ORIENTED_EDGE ( 'NONE', *, *, #35855, .F. ) ;
#9301=ORIENTED_EDGE ( 'NONE', *, *, #14211, .F. ) ;
#9302=LINE ( 'NONE', #16796, #29263 ) ;
#9303=EDGE_CURVE ( 'NONE', #42740, #10110, #38620, .T. ) ;
#9304=CARTESIAN_POINT ( 'NONE',  ( -0.07591351300297333182, 3.346456692913386100, -1.102362204724405714 ) ) ;
#9306=EDGE_CURVE ( 'NONE', #26179, #23113, #11251, .T. ) ;
#9307=DIRECTION ( 'NONE',  ( -3.469446951953613696E-16, 0.000000000000000000, -1.000000000000000000 ) ) ;
#9311=CARTESIAN_POINT ( 'NONE',  ( -0.8942052331142549271, 3.267716535433071279, 3.102397620449222481E-16 ) ) ;
#9312=LINE ( 'NONE', #16287, #44724 ) ;
#9314=CARTESIAN_POINT ( 'NONE',  ( 1.363819533518803695, 3.346456692913386100, 1.681890501046755748 ) ) ;
#9315=DIRECTION ( 'NONE',  ( -1.000000000000000000, -0.000000000000000000, -0.000000000000000000 ) ) ;
#9317=FACE_OUTER_BOUND ( 'NONE', #6957, .T. ) ;
#9319=VERTEX_POINT ( 'NONE', #39628 ) ;
#9321=CARTESIAN_POINT ( 'NONE',  ( -0.5455278134075214336, 0.000000000000000000, -0.5118110236220467790 ) ) ;
#9325=VECTOR ( 'NONE', #49523, 39.37007874015748143 ) ;
#9327=CARTESIAN_POINT ( 'NONE',  ( 0.7423782071083087075, 3.346456692913386100, 0.9448818897637746295 ) ) ;
#9328=ORIENTED_EDGE ( 'NONE', *, *, #74, .F. ) ;
#9329=EDGE_CURVE ( 'NONE', #17641, #13815, #42483, .T. ) ;
#9330=VECTOR ( 'NONE', #5574, 39.37007874015748143 ) ;
#9332=CARTESIAN_POINT ( 'NONE',  ( 0.7423782071083092626, 3.346456692913386100, 1.889763779527550369 ) ) ;
#9333=ADVANCED_FACE ( 'NONE', ( #34744 ), #43485, .F. ) ;
#9335=LINE ( 'NONE', #29465, #21086 ) ;
#9337=EDGE_CURVE ( 'NONE', #6293, #24410, #50184, .T. ) ;
#9339=VERTEX_POINT ( 'NONE', #14872 ) ;
#9341=LINE ( 'NONE', #1338, #32096 ) ;
#9343=ORIENTED_EDGE ( 'NONE', *, *, #21324, .T. ) ;
#9344=EDGE_CURVE ( 'NONE', #20959, #28842, #30615, .T. ) ;
#9345=LINE ( 'NONE', #41857, #16581 ) ;
#9346=CARTESIAN_POINT ( 'NONE',  ( -1.712496953225537188, 3.267716535433071279, 0.7874015748031456541 ) ) ;
#9348=EDGE_CURVE ( 'NONE', #46386, #7678, #39118, .T. ) ;
#9351=CARTESIAN_POINT ( 'NONE',  ( 0.4696143004045479352, 3.346456692913386100, -0.4724409448818886470 ) ) ;
#9353=LINE ( 'NONE', #32871, #8008 ) ;
#9354=EDGE_LOOP ( 'NONE', ( #34514, #19954, #32951, #4161 ) ) ;
#9355=LINE ( 'NONE', #28965, #9242 ) ;
#9357=DIRECTION ( 'NONE',  ( 1.000000000000000000, 0.000000000000000000, -3.469446951953613696E-16 ) ) ;
#9359=ORIENTED_EDGE ( 'NONE', *, *, #28762, .F. ) ;
#9360=AXIS2_PLACEMENT_3D ( 'NONE', #37025, #18854, #21519 ) ;
#9362=VECTOR ( 'NONE', #39716, 39.37007874015748143 ) ;
#9363=ADVANCED_FACE ( 'NONE', ( #50930 ), #31378, .F. ) ;
#9364=AXIS2_PLACEMENT_3D ( 'NONE', #41138, #44981, #25375 ) ;
#9365=DIRECTION ( 'NONE',  ( 1.000000000000000000, 0.000000000000000000, 0.000000000000000000 ) ) ;
#9366=PLANE ( 'NONE',  #23651 ) ;
#9367=ADVANCED_FACE ( 'NONE', ( #23623 ), #35503, .F. ) ;
#9368=DIRECTION ( 'NONE',  ( -1.000000000000000000, 0.000000000000000000, 0.000000000000000000 ) ) ;
#9369=VERTEX_POINT ( 'NONE', #31631 ) ;
#9370=VERTEX_POINT ( 'NONE', #5027 ) ;
#9371=CIRCLE ( 'NONE', #16780, 2.165354330708661568 ) ;
#9376=DIRECTION ( 'NONE',  ( 0.000000000000000000, 0.000000000000000000, 1.000000000000000000 ) ) ;
#9377=PLANE ( 'NONE',  #11820 ) ;
#9378=CARTESIAN_POINT ( 'NONE',  ( 0.4696143004045479352, 3.346456692913386100, -1.417322834645664331 ) ) ;
#9379=CARTESIAN_POINT ( 'NONE',  ( -1.909347346926324462, 3.346456692913386100, 1.021348170950612255 ) ) ;
#9380=ORIENTED_EDGE ( 'NONE', *, *, #4250, .T. ) ;
#9382=CARTESIAN_POINT ( 'NONE',  ( -2.156388021673881994, 3.267716535433071279, -0.1968503937007880511 ) ) ;
#9383=EDGE_LOOP ( 'NONE', ( #453, #3562, #48651, #21350 ) ) ;
#9384=DIRECTION ( 'NONE',  ( 1.000000000000000000, 0.000000000000000000, -3.469446951953613696E-16 ) ) ;
#9386=CARTESIAN_POINT ( 'NONE',  ( -0.2727639067037602727, 3.346456692913386100, 0.5905511811023582691 ) ) ;
#9388=EDGE_CURVE ( 'NONE', #31953, #25971, #20772, .T. ) ;
#9390=FACE_OUTER_BOUND ( 'NONE', #10165, .T. ) ;
#9391=VECTOR ( 'NONE', #5299, 39.37007874015748143 ) ;
#9392=AXIS2_PLACEMENT_3D ( 'NONE', #28662, #4920, #9050 ) ;
#9394=EDGE_LOOP ( 'NONE', ( #11823, #40480, #1, #26241 ) ) ;
#9395=AXIS2_PLACEMENT_3D ( 'NONE', #36382, #17522, #36641 ) ;
#9397=CARTESIAN_POINT ( 'NONE',  ( 0.1968503937007869686, 3.267716535433071279, -2.086614173228339641 ) ) ;
#9398=EDGE_LOOP ( 'NONE', ( #30659, #17226, #30583, #18401 ) ) ;
#9399=PLANE ( 'NONE',  #48405 ) ;
#9400=AXIS2_PLACEMENT_3D ( 'NONE', #41920, #45765, #45260 ) ;
#9403=LINE ( 'NONE', #21529, #2454 ) ;
#9405=EDGE_CURVE ( 'NONE', #26688, #16323, #9415, .T. ) ;
#9406=EDGE_CURVE ( 'NONE', #49431, #49218, #8644, .T. ) ;
#9407=EDGE_CURVE ( 'NONE', #30647, #8095, #644, .T. ) ;
#9408=DIRECTION ( 'NONE',  ( 1.734723475976806848E-16, -0.000000000000000000, 1.000000000000000000 ) ) ;
#9409=VERTEX_POINT ( 'NONE', #4774 ) ;
#9410=ORIENTED_EDGE ( 'NONE', *, *, #46387, .F. ) ;
#9411=LINE ( 'NONE', #40907, #40540 ) ;
#9413=PLANE ( 'NONE',  #24647 ) ;
#9414=ORIENTED_EDGE ( 'NONE', *, *, #39709, .F. ) ;
#9415=LINE ( 'NONE', #40655, #50533 ) ;
#9416=CARTESIAN_POINT ( 'NONE',  ( 2.083268748869757658, 3.267716535433071279, 0.5905511811023582691 ) ) ;
#9417=DIRECTION ( 'NONE',  ( 1.734723475976806848E-16, -0.000000000000000000, 1.000000000000000000 ) ) ;
#9418=CARTESIAN_POINT ( 'NONE',  ( 0.1968503937007873017, 0.000000000000000000, -1.259842519685035134 ) ) ;
#9419=VERTEX_POINT ( 'NONE', #28000 ) ;
#9420=ORIENTED_EDGE ( 'NONE', *, *, #23986, .F. ) ;
#9423=LINE ( 'NONE', #17421, #9903 ) ;
#9424=ORIENTED_EDGE ( 'NONE', *, *, #4878, .T. ) ;
#9425=LINE ( 'NONE', #17174, #38081 ) ;
#9426=FACE_BOUND ( 'NONE', #28835, .T. ) ;
#9427=ORIENTED_EDGE ( 'NONE', *, *, #443, .F. ) ;
#9429=VERTEX_POINT ( 'NONE', #16396 ) ;
#9430=ORIENTED_EDGE ( 'NONE', *, *, #25037, .T. ) ;
#9431=ADVANCED_FACE ( 'NONE', ( #20521 ), #32927, .F. ) ;
#9435=CARTESIAN_POINT ( 'NONE',  ( -1.363819533518803029, 3.346456692913386100, 0.7874015748031456541 ) ) ;
#9436=EDGE_CURVE ( 'NONE', #8029, #5151, #8899, .T. ) ;
#9437=LINE ( 'NONE', #19819, #21269 ) ;
#9438=ORIENTED_EDGE ( 'NONE', *, *, #15241, .F. ) ;
#9439=VECTOR ( 'NONE', #7594, 39.37007874015748143 ) ;
#9440=ADVANCED_FACE ( 'NONE', ( #16655 ), #36530, .F. ) ;
#9441=ADVANCED_FACE ( 'NONE', ( #1409 ), #1153, .F. ) ;
#9442=VECTOR ( 'NONE', #49172, 39.37007874015748143 ) ;
#9443=LINE ( 'NONE', #10203, #34354 ) ;
#9444=DIRECTION ( 'NONE',  ( 0.000000000000000000, 0.000000000000000000, 1.000000000000000000 ) ) ;
#9445=VECTOR ( 'NONE', #32464, 39.37007874015748143 ) ;
#9446=VECTOR ( 'NONE', #10274, 39.37007874015748143 ) ;
#9448=CARTESIAN_POINT ( 'NONE',  ( -0.5455278134075214336, 3.267716535433071279, 0.3149606299212577287 ) ) ;
#9450=AXIS2_PLACEMENT_3D ( 'NONE', #21907, #43212, #7861 ) ;
#9452=DIRECTION ( 'NONE',  ( -0.000000000000000000, 0.000000000000000000, 1.000000000000000000 ) ) ;
#9453=LINE ( 'NONE', #32966, #16618 ) ;
#9456=CARTESIAN_POINT ( 'NONE',  ( 0.000000000000000000, 3.346456692913386100, 0.000000000000000000 ) ) ;
#9457=ORIENTED_EDGE ( 'NONE', *, *, #38300, .T. ) ;
#9458=CARTESIAN_POINT ( 'NONE',  ( 0.000000000000000000, 3.267716535433071279, -1.141732283464563569 ) ) ;
#9459=CARTESIAN_POINT ( 'NONE',  ( -2.182111253630085290, 3.346456692913386100, 0.6299212598425164567 ) ) ;
#9460=DIRECTION ( 'NONE',  ( -3.469446951953613696E-16, 0.000000000000000000, -1.000000000000000000 ) ) ;
#9462=FACE_OUTER_BOUND ( 'NONE', #40465, .T. ) ;
#9464=FACE_BOUND ( 'NONE', #30535, .T. ) ;
#9466=DIRECTION ( 'NONE',  ( -1.000000000000000000, 0.000000000000000000, -0.000000000000000000 ) ) ;
#9468=EDGE_CURVE ( 'NONE', #42898, #10781, #12514, .T. ) ;
#9470=ORIENTED_EDGE ( 'NONE', *, *, #49012, .F. ) ;
#9472=VECTOR ( 'NONE', #6967, 39.37007874015748143 ) ;
#9473=EDGE_CURVE ( 'NONE', #11679, #18573, #44512, .T. ) ;
#9474=DIRECTION ( 'NONE',  ( 0.000000000000000000, 0.000000000000000000, -1.000000000000000000 ) ) ;
#9477=DIRECTION ( 'NONE',  ( -3.469446951953613696E-16, 0.000000000000000000, -1.000000000000000000 ) ) ;
#9480=CIRCLE ( 'NONE', #46549, 2.443628662382284489 ) ;
#9481=LINE ( 'NONE', #17478, #34719 ) ;
#9483=CARTESIAN_POINT ( 'NONE',  ( -1.195183497228115035E-16, 3.346456692913386100, -0.6299212598425177889 ) ) ;
#9484=CARTESIAN_POINT ( 'NONE',  ( 0.5455278134075212115, 3.346456692913386100, -0.3149606299212593941 ) ) ;
#9485=VECTOR ( 'NONE', #3806, 39.37007874015748143 ) ;
#9486=EDGE_LOOP ( 'NONE', ( #26994, #31080, #26940, #50442 ) ) ;
#9487=PLANE ( 'NONE',  #26525 ) ;
#9489=VERTEX_POINT ( 'NONE', #43739 ) ;
#9490=ADVANCED_FACE ( 'NONE', ( #8390 ), #24137, .F. ) ;
#9492=ORIENTED_EDGE ( 'NONE', *, *, #30003, .T. ) ;
#9495=ADVANCED_FACE ( 'NONE', ( #37299 ), #25664, .F. ) ;
#9496=ORIENTED_EDGE ( 'NONE', *, *, #24447, .T. ) ;
#9498=ORIENTED_EDGE ( 'NONE', *, *, #40164, .T. ) ;
#9499=CARTESIAN_POINT ( 'NONE',  ( -1.363819533518803473, 3.267716535433071279, 1.605145679676863057 ) ) ;
#9500=CARTESIAN_POINT ( 'NONE',  ( 0.000000000000000000, 3.267716535433071279, -4.780733988912460139E-16 ) ) ;
#9501=ORIENTED_EDGE ( 'NONE', *, *, #17975, .F. ) ;
#9502=DIRECTION ( 'NONE',  ( 1.000000000000000000, -0.000000000000000000, 0.000000000000000000 ) ) ;
#9503=LINE ( 'NONE', #21129, #42632 ) ;
#9504=VECTOR ( 'NONE', #41327, 39.37007874015748143 ) ;
#9506=CARTESIAN_POINT ( 'NONE',  ( -2.082617625631827174, 3.267716535433071279, 0.3149606299212578953 ) ) ;
#9508=AXIS2_PLACEMENT_3D ( 'NONE', #37996, #14749, #2618 ) ;
#9510=VECTOR ( 'NONE', #33102, 39.37007874015748143 ) ;
#9514=EDGE_LOOP ( 'NONE', ( #38908, #29346, #28515, #19624 ) ) ;
#9515=LINE ( 'NONE', #47234, #47616 ) ;
#9516=CARTESIAN_POINT ( 'NONE',  ( -0.8182917201112819283, 3.346456692913386100, -0.03937007874015895081 ) ) ;
#9517=VECTOR ( 'NONE', #4249, 39.37007874015748143 ) ;
#9518=ORIENTED_EDGE ( 'NONE', *, *, #29852, .T. ) ;
#9520=ORIENTED_EDGE ( 'NONE', *, *, #47845, .F. ) ;
#9521=CARTESIAN_POINT ( 'NONE',  ( 0.4696143004045479352, 3.346456692913386100, -1.102362204724405714 ) ) ;
#9522=CARTESIAN_POINT ( 'NONE',  ( -0.07591351300297359550, 3.267716535433071279, -2.047244094488181343 ) ) ;
#9523=LINE ( 'NONE', #37410, #11367 ) ;
#9524=FACE_OUTER_BOUND ( 'NONE', #8242, .T. ) ;
#9525=DIRECTION ( 'NONE',  ( -0.000000000000000000, 1.000000000000000000, -0.000000000000000000 ) ) ;
#9526=ORIENTED_EDGE ( 'NONE', *, *, #4411, .T. ) ;
#9527=LINE ( 'NONE', #5397, #48005 ) ;
#9528=EDGE_CURVE ( 'NONE', #26747, #19657, #29544, .T. ) ;
#9529=FACE_BOUND ( 'NONE', #50221, .T. ) ;
#9530=ADVANCED_FACE ( 'NONE', ( #21289 ), #1919, .F. ) ;
#9531=ORIENTED_EDGE ( 'NONE', *, *, #7315, .T. ) ;
#9532=CARTESIAN_POINT ( 'NONE',  ( 0.8182917201112819283, 3.346456692913386100, 0.7874015748031454320 ) ) ;
#9534=EDGE_CURVE ( 'NONE', #47091, #33606, #6306, .T. ) ;
#9535=DIRECTION ( 'NONE',  ( -3.469446951953613696E-16, 0.000000000000000000, -1.000000000000000000 ) ) ;
#9536=PLANE ( 'NONE',  #20636 ) ;
#9537=CARTESIAN_POINT ( 'NONE',  ( -1.439733046521776139, 3.346456692913386100, 0.3149606299212578953 ) ) ;
#9538=EDGE_CURVE ( 'NONE', #17338, #27824, #29282, .T. ) ;
#9541=ORIENTED_EDGE ( 'NONE', *, *, #27302, .T. ) ;
#9542=ORIENTED_EDGE ( 'NONE', *, *, #11293, .F. ) ;
#9543=AXIS2_PLACEMENT_3D ( 'NONE', #22205, #6198, #49268 ) ;
#9545=DIRECTION ( 'NONE',  ( 1.734723475976806848E-16, -0.000000000000000000, 1.000000000000000000 ) ) ;
#9546=FACE_BOUND ( 'NONE', #32531, .T. ) ;
#9548=VECTOR ( 'NONE', #2741, 39.37007874015748143 ) ;
#9549=FACE_OUTER_BOUND ( 'NONE', #30064, .T. ) ;
#9551=DIRECTION ( 'NONE',  ( -1.000000000000000000, 0.000000000000000000, 1.734723475976806848E-16 ) ) ;
#9552=CIRCLE ( 'NONE', #18616, 2.106299212598425008 ) ;
#9556=AXIS2_PLACEMENT_3D ( 'NONE', #49996, #41794, #42545 ) ;
#9557=PLANE ( 'NONE',  #36940 ) ;
#9558=EDGE_CURVE ( 'NONE', #13466, #24951, #30304, .T. ) ;
#9560=ORIENTED_EDGE ( 'NONE', *, *, #1789, .F. ) ;
#9562=LINE ( 'NONE', #13692, #2132 ) ;
#9564=DIRECTION ( 'NONE',  ( 0.000000000000000000, 1.000000000000000000, 0.000000000000000000 ) ) ;
#9565=CARTESIAN_POINT ( 'NONE',  ( 0.000000000000000000, 3.267716535433071279, -0.1968503937007883287 ) ) ;
#9566=VERTEX_POINT ( 'NONE', #9671 ) ;
#9569=FACE_OUTER_BOUND ( 'NONE', #26308, .T. ) ;
#9570=ADVANCED_FACE ( 'NONE', ( #2433 ), #49869, .F. ) ;
#9571=LINE ( 'NONE', #21700, #1246 ) ;
#9572=CARTESIAN_POINT ( 'NONE',  ( 1.015142113812069091, 3.239993870794025010, -2.236998478663746237 ) ) ;
#9573=CARTESIAN_POINT ( 'NONE',  ( 2.378961647330872342, 3.230577599468342775, 0.6299212598425161236 ) ) ;
#9576=ORIENTED_EDGE ( 'NONE', *, *, #40523, .T. ) ;
#9578=CARTESIAN_POINT ( 'NONE',  ( -1.363819533518803251, 3.267716535433071279, 2.365849761790805487E-16 ) ) ;
#9579=LINE ( 'NONE', #25322, #35148 ) ;
#9580=VECTOR ( 'NONE', #45854, 39.37007874015748143 ) ;
#9581=EDGE_LOOP ( 'NONE', ( #36830, #7291, #2971, #24938 ) ) ;
#9582=ORIENTED_EDGE ( 'NONE', *, *, #43445, .F. ) ;
#9585=AXIS2_PLACEMENT_3D ( 'NONE', #48045, #28451, #16859 ) ;
#9586=VERTEX_POINT ( 'NONE', #26422 ) ;
#9587=VECTOR ( 'NONE', #19238, 39.37007874015748143 ) ;
#9588=EDGE_CURVE ( 'NONE', #25851, #3960, #14047, .T. ) ;
#9592=EDGE_CURVE ( 'NONE', #42497, #15363, #29795, .T. ) ;
#9593=CARTESIAN_POINT ( 'NONE',  ( -0.8182917201112814842, 0.000000000000000000, 0.4724409448818872592 ) ) ;
#9594=PLANE ( 'NONE',  #34648 ) ;
#9596=EDGE_CURVE ( 'NONE', #33624, #11338, #21801, .T. ) ;
#9597=ORIENTED_EDGE ( 'NONE', *, *, #25347, .F. ) ;
#9599=ORIENTED_EDGE ( 'NONE', *, *, #48812, .T. ) ;
#9602=ORIENTED_EDGE ( 'NONE', *, *, #44732, .T. ) ;
#9604=CARTESIAN_POINT ( 'NONE',  ( -0.2727639067037605503, 3.267716535433071279, 4.731699523581609741E-17 ) ) ;
#9605=FACE_OUTER_BOUND ( 'NONE', #21955, .T. ) ;
#9608=ORIENTED_EDGE ( 'NONE', *, *, #28638, .F. ) ;
#9610=ADVANCED_FACE ( 'NONE', ( #2678 ), #49618, .F. ) ;
#9611=LINE ( 'NONE', #1347, #46428 ) ;
#9613=VECTOR ( 'NONE', #49719, 39.37007874015748143 ) ;
#9614=EDGE_LOOP ( 'NONE', ( #40749, #45921, #12646, #10329 ) ) ;
#9615=CARTESIAN_POINT ( 'NONE',  ( -1.712496953225537411, 3.267716535433071279, 5.941417334598190051E-16 ) ) ;
#9617=VECTOR ( 'NONE', #42329, 39.37007874015748143 ) ;
#9619=DIRECTION ( 'NONE',  ( -0.000000000000000000, 0.000000000000000000, 1.000000000000000000 ) ) ;
#9621=ORIENTED_EDGE ( 'NONE', *, *, #41930, .F. ) ;
#9622=EDGE_LOOP ( 'NONE', ( #20950, #19500, #50234, #3543 ) ) ;
#9623=DIRECTION ( 'NONE',  ( 1.734723475976806848E-16, 0.000000000000000000, 1.000000000000000000 ) ) ;
#9624=VECTOR ( 'NONE', #42189, 39.37007874015748143 ) ;
#9625=ADVANCED_FACE ( 'NONE', ( #38062 ), #33176, .F. ) ;
#9627=CARTESIAN_POINT ( 'NONE',  ( 2.651794250122221246E-16, 3.346456692913386100, 2.165354330708661568 ) ) ;
#9628=ORIENTED_EDGE ( 'NONE', *, *, #19122, .T. ) ;
#9629=ORIENTED_EDGE ( 'NONE', *, *, #46169, .F. ) ;
#9630=VECTOR ( 'NONE', #35956, 39.37007874015748143 ) ;
#9632=ORIENTED_EDGE ( 'NONE', *, *, #29883, .T. ) ;
#9634=EDGE_CURVE ( 'NONE', #17559, #46164, #17659, .T. ) ;
#9635=CARTESIAN_POINT ( 'NONE',  ( 0.2727639067037609943, 3.267716535433071279, 1.850393700787392293 ) ) ;
#9636=CARTESIAN_POINT ( 'NONE',  ( -0.2727639067037607723, 0.000000000000000000, -1.732283464566922726 ) ) ;
#9637=DIRECTION ( 'NONE',  ( -0.000000000000000000, 1.000000000000000000, -0.000000000000000000 ) ) ;
#9638=LINE ( 'NONE', #9893, #44366 ) ;
#9639=VERTEX_POINT ( 'NONE', #15611 ) ;
#9641=DIRECTION ( 'NONE',  ( -1.000000000000000000, -0.000000000000000000, -0.000000000000000000 ) ) ;
#9642=EDGE_CURVE ( 'NONE', #10831, #5151, #47058, .T. ) ;
#9644=EDGE_CURVE ( 'NONE', #24556, #795, #24377, .T. ) ;
#9645=ORIENTED_EDGE ( 'NONE', *, *, #6413, .T. ) ;
#9646=PLANE ( 'NONE',  #41358 ) ;
#9653=ORIENTED_EDGE ( 'NONE', *, *, #1373, .T. ) ;
#9654=CARTESIAN_POINT ( 'NONE',  ( 1.363819533518804139, 3.346456692913386100, 1.605145679676863057 ) ) ;
#9657=DIRECTION ( 'NONE',  ( -1.000000000000000000, 0.000000000000000000, -0.000000000000000000 ) ) ;
#9658=ADVANCED_FACE ( 'NONE', ( #11730 ), #881, .F. ) ;
#9659=CARTESIAN_POINT ( 'NONE',  ( 2.182111253630085290, 3.346456692913386100, -1.161035397307311917E-15 ) ) ;
#9661=DIRECTION ( 'NONE',  ( -0.000000000000000000, 1.000000000000000000, -0.000000000000000000 ) ) ;
#9662=VECTOR ( 'NONE', #26627, 39.37007874015748143 ) ;
#9663=EDGE_CURVE ( 'NONE', #16084, #19545, #39105, .T. ) ;
#9664=EDGE_CURVE ( 'NONE', #6110, #13500, #19727, .T. ) ;
#9668=DIRECTION ( 'NONE',  ( 1.000000000000000000, -0.000000000000000000, 0.000000000000000000 ) ) ;
#9669=CARTESIAN_POINT ( 'NONE',  ( 0.2727639067037609943, 0.000000000000000000, 1.220472440944875281 ) ) ;
#9670=ORIENTED_EDGE ( 'NONE', *, *, #49110, .T. ) ;
#9671=CARTESIAN_POINT ( 'NONE',  ( 0.7423782071083092626, 3.346456692913386100, 2.034117492951036166 ) ) ;
#9672=DIRECTION ( 'NONE',  ( 0.000000000000000000, 0.000000000000000000, 1.000000000000000000 ) ) ;
#9673=CARTESIAN_POINT ( 'NONE',  ( -0.5455278134075214336, 3.346456692913386100, -8.878505979408855953E-16 ) ) ;
#9674=EDGE_LOOP ( 'NONE', ( #27930, #38105, #11908, #41490 ) ) ;
#9675=ORIENTED_EDGE ( 'NONE', *, *, #29122, .T. ) ;
#9677=FACE_OUTER_BOUND ( 'NONE', #23019, .T. ) ;
#9678=LINE ( 'NONE', #9934, #34626 ) ;
#9679=VERTEX_POINT ( 'NONE', #43214 ) ;
#9681=FACE_BOUND ( 'NONE', #26677, .T. ) ;
#9683=CARTESIAN_POINT ( 'NONE',  ( 0.000000000000000000, 3.267716535433071279, -0.9448818897637762948 ) ) ;
#9684=VERTEX_POINT ( 'NONE', #36001 ) ;
#9685=ORIENTED_EDGE ( 'NONE', *, *, #23762, .T. ) ;
#9687=VECTOR ( 'NONE', #42923, 39.37007874015748143 ) ;
#9688=VECTOR ( 'NONE', #4943, 39.37007874015748143 ) ;
#9689=EDGE_CURVE ( 'NONE', #49800, #45211, #32134, .T. ) ;
#9690=ORIENTED_EDGE ( 'NONE', *, *, #11607, .T. ) ;
#9691=CARTESIAN_POINT ( 'NONE',  ( 2.106333035502527373, 3.267716535433071279, -0.006892066987323136953 ) ) ;
#9692=UNCERTAINTY_MEASURE_WITH_UNIT (LENGTH_MEASURE( 1.000000000000000082E-05 ), #40606, 'distance_accuracy_value', 'NONE');
#9694=ORIENTED_EDGE ( 'NONE', *, *, #37789, .F. ) ;
#9695=AXIS2_PLACEMENT_3D ( 'NONE', #12548, #8933, #1188 ) ;
#9696=CARTESIAN_POINT ( 'NONE',  ( 1.363819533518803251, 3.267716535433071279, -2.365849761790805487E-16 ) ) ;
#9697=CARTESIAN_POINT ( 'NONE',  ( -0.07591351300297359550, 0.000000000000000000, -2.047244094488181343 ) ) ;
#9698=EDGE_CURVE ( 'NONE', #4856, #129, #43467, .T. ) ;
#9704=LINE ( 'NONE', #49151, #36895 ) ;
#9705=DIRECTION ( 'NONE',  ( -0.000000000000000000, 1.000000000000000000, -0.000000000000000000 ) ) ;
#9706=VERTEX_POINT ( 'NONE', #47315 ) ;
#9708=VECTOR ( 'NONE', #44034, 39.37007874015748143 ) ;
#9709=DIRECTION ( 'NONE',  ( -0.000000000000000000, 1.000000000000000000, -0.000000000000000000 ) ) ;
#9710=ORIENTED_EDGE ( 'NONE', *, *, #10282, .F. ) ;
#9711=LINE ( 'NONE', #25704, #18249 ) ;
#9713=EDGE_LOOP ( 'NONE', ( #42348, #47257, #47704, #23063 ) ) ;
#9714=CARTESIAN_POINT ( 'NONE',  ( -1.636583440222563635, 0.000000000000000000, -4.780733988912460139E-16 ) ) ;
#9718=PLANE ( 'NONE',  #7078 ) ;
#9719=EDGE_LOOP ( 'NONE', ( #44400, #39810, #3637, #48353 ) ) ;
#9720=CARTESIAN_POINT ( 'NONE',  ( 0.4696143004045484903, 3.346456692913386100, 1.732283464566921172 ) ) ;
#9721=ORIENTED_EDGE ( 'NONE', *, *, #43640, .T. ) ;
#9722=FACE_BOUND ( 'NONE', #7058, .T. ) ;
#9725=CARTESIAN_POINT ( 'NONE',  ( -0.5455278134075217666, 3.226699998040866824, -2.401574803149598036 ) ) ;
#9726=PLANE ( 'NONE',  #50688 ) ;
#9728=EDGE_CURVE ( 'NONE', #37378, #681, #40127, .T. ) ;
#9730=ORIENTED_EDGE ( 'NONE', *, *, #31062, .F. ) ;
#9736=LINE ( 'NONE', #5601, #12908 ) ;
#9737=VERTEX_POINT ( 'NONE', #12497 ) ;
#9738=DIRECTION ( 'NONE',  ( 0.000000000000000000, -1.000000000000000000, 0.000000000000000000 ) ) ;
#9739=ORIENTED_EDGE ( 'NONE', *, *, #9144, .T. ) ;
#9740=DIRECTION ( 'NONE',  ( 0.000000000000000000, 0.000000000000000000, -1.000000000000000000 ) ) ;
#9743=ORIENTED_EDGE ( 'NONE', *, *, #37633, .F. ) ;
#9748=VERTEX_POINT ( 'NONE', #28235 ) ;
#9750=CARTESIAN_POINT ( 'NONE',  ( -1.712496953225537188, 3.267716535433071279, 0.9055118110236167750 ) ) ;
#9752=CARTESIAN_POINT ( 'NONE',  ( 0.2727639067037608278, 3.267716535433071279, -4.731699523581614055E-17 ) ) ;
#9754=EDGE_CURVE ( 'NONE', #47970, #3256, #8880, .T. ) ;
#9755=AXIS2_PLACEMENT_3D ( 'NONE', #15437, #46388, #6677 ) ;
#9756=DIRECTION ( 'NONE',  ( -1.000000000000000000, -0.000000000000000000, -0.000000000000000000 ) ) ;
#9758=EDGE_CURVE ( 'NONE', #26688, #18090, #45243, .T. ) ;
#9760=DIRECTION ( 'NONE',  ( -1.000000000000000000, -0.000000000000000000, -0.000000000000000000 ) ) ;
#9761=VERTEX_POINT ( 'NONE', #49097 ) ;
#9763=DIRECTION ( 'NONE',  ( 0.000000000000000000, -1.000000000000000000, 0.000000000000000000 ) ) ;
#9764=VECTOR ( 'NONE', #39962, 39.37007874015748143 ) ;
#9765=CARTESIAN_POINT ( 'NONE',  ( 2.052631463899902364, 3.346456692913386100, 0.4724409448818868706 ) ) ;
#9768=VECTOR ( 'NONE', #1587, 39.37007874015748143 ) ;
#9769=LINE ( 'NONE', #10270, #50322 ) ;
#9773=LINE ( 'NONE', #38166, #29221 ) ;
#9774=VECTOR ( 'NONE', #8928, 39.37007874015748143 ) ;
#9775=ORIENTED_EDGE ( 'NONE', *, *, #25050, .T. ) ;
#9776=PLANE ( 'NONE',  #12723 ) ;
#9777=EDGE_CURVE ( 'NONE', #22951, #42620, #29262, .T. ) ;
#9778=VECTOR ( 'NONE', #26277, 39.37007874015748143 ) ;
#9781=CARTESIAN_POINT ( 'NONE',  ( 0.000000000000000000, 3.267716535433071279, 1.574803149606291974 ) ) ;
#9782=DIRECTION ( 'NONE',  ( 1.000000000000000000, 0.000000000000000000, 0.000000000000000000 ) ) ;
#9784=CARTESIAN_POINT ( 'NONE',  ( -1.909347346926324462, 3.346456692913386100, 0.7874015748031456541 ) ) ;
#9785=CARTESIAN_POINT ( 'NONE',  ( 1.636583440222563635, 3.267716535433071279, -1.417869535855832419 ) ) ;
#9786=ORIENTED_EDGE ( 'NONE', *, *, #3074, .T. ) ;
#9789=ORIENTED_EDGE ( 'NONE', *, *, #44271, .T. ) ;
#9792=EDGE_LOOP ( 'NONE', ( #10253, #43810, #42418, #50671 ) ) ;
#9793=LINE ( 'NONE', #28375, #8140 ) ;
#9797=VECTOR ( 'NONE', #44509, 39.37007874015748143 ) ;
#9799=DIRECTION ( 'NONE',  ( -3.469446951953613696E-16, 0.000000000000000000, -1.000000000000000000 ) ) ;
#9800=ORIENTED_EDGE ( 'NONE', *, *, #43317, .T. ) ;
#9801=EDGE_LOOP ( 'NONE', ( #35003, #3961, #35492, #34361, #9560 ) ) ;
#9803=FACE_BOUND ( 'NONE', #5396, .T. ) ;
#9804=VERTEX_POINT ( 'NONE', #41154 ) ;
#9805=VECTOR ( 'NONE', #10116, 39.37007874015748143 ) ;
#9807=LINE ( 'NONE', #48488, #7258 ) ;
#9809=ORIENTED_EDGE ( 'NONE', *, *, #20404, .F. ) ;
#9811=AXIS2_PLACEMENT_3D ( 'NONE', #10645, #48883, #5566 ) ;
#9813=DIRECTION ( 'NONE',  ( -0.000000000000000000, 0.000000000000000000, 1.000000000000000000 ) ) ;
#9814=EDGE_LOOP ( 'NONE', ( #8389, #27039, #10738, #6057 ) ) ;
#9815=ORIENTED_EDGE ( 'NONE', *, *, #46915, .T. ) ;
#9816=VECTOR ( 'NONE', #44490, 39.37007874015748143 ) ;
#9817=ORIENTED_EDGE ( 'NONE', *, *, #46169, .T. ) ;
#9818=CARTESIAN_POINT ( 'NONE',  ( -1.712496953225537633, 3.346456692913386100, -0.7874015748031470974 ) ) ;
#9819=CARTESIAN_POINT ( 'NONE',  ( -2.182111253630085290, 3.346456692913386100, -6.146657985744592735E-16 ) ) ;
#9821=FACE_OUTER_BOUND ( 'NONE', #44459, .T. ) ;
#9823=VERTEX_POINT ( 'NONE', #17649 ) ;
#9825=CARTESIAN_POINT ( 'NONE',  ( -1.166969139818015977, 3.346456692913386100, -1.732283464566922726 ) ) ;
#9826=CARTESIAN_POINT ( 'NONE',  ( -2.182111253630085290, 3.346456692913386100, 0.4330708661417290162 ) ) ;
#9827=ADVANCED_FACE ( 'NONE', ( #9390 ), #25142, .F. ) ;
#9828=CARTESIAN_POINT ( 'NONE',  ( -0.07591351300297333182, 3.346456692913386100, -0.4724409448818883694 ) ) ;
#9829=CARTESIAN_POINT ( 'NONE',  ( -1.091055626815042645, 0.000000000000000000, -1.889763779527552146 ) ) ;
#9830=EDGE_CURVE ( 'NONE', #40779, #20338, #9906, .T. ) ;
#9832=PLANE ( 'NONE',  #25984 ) ;
#9833=VECTOR ( 'NONE', #17348, 39.37007874015748143 ) ;
#9834=CARTESIAN_POINT ( 'NONE',  ( -0.6214413264104945434, 0.000000000000000000, -1.732283464566922726 ) ) ;
#9836=CARTESIAN_POINT ( 'NONE',  ( 1.091055626815042645, 0.000000000000000000, -8.878505979408855953E-16 ) ) ;
#9837=CARTESIAN_POINT ( 'NONE',  ( 1.363819533518803251, 0.000000000000000000, -0.4724409448818889246 ) ) ;
#9838=ORIENTED_EDGE ( 'NONE', *, *, #13783, .T. ) ;
#9839=ORIENTED_EDGE ( 'NONE', *, *, #24793, .T. ) ;
#9840=VECTOR ( 'NONE', #342, 39.37007874015748143 ) ;
#9841=PLANE ( 'NONE',  #50432 ) ;
#9842=CARTESIAN_POINT ( 'NONE',  ( 0.000000000000000000, 3.267716535433071279, 0.4724409448818871482 ) ) ;
#9843=EDGE_CURVE ( 'NONE', #26214, #9586, #44494, .T. ) ;
#9844=VERTEX_POINT ( 'NONE', #45494 ) ;
#9845=CIRCLE ( 'NONE', #23025, 2.106299212598425008 ) ;
#9846=ADVANCED_FACE ( 'NONE', ( #5259 ), #2156, .F. ) ;
#9847=ORIENTED_EDGE ( 'NONE', *, *, #964, .T. ) ;
#9848=DIRECTION ( 'NONE',  ( -1.000000000000000000, -0.000000000000000000, -0.000000000000000000 ) ) ;
#9849=AXIS2_PLACEMENT_3D ( 'NONE', #50235, #4508, #31890 ) ;
#9850=EDGE_LOOP ( 'NONE', ( #45217, #6436, #17883, #15294 ) ) ;
#9851=LINE ( 'NONE', #9080, #37574 ) ;
#9852=CARTESIAN_POINT ( 'NONE',  ( -0.2727639067037602727, 0.000000000000000000, 1.535433070866133898 ) ) ;
#9853=ORIENTED_EDGE ( 'NONE', *, *, #34224, .T. ) ;
#9854=ORIENTED_EDGE ( 'NONE', *, *, #40719, .T. ) ;
#9855=DIRECTION ( 'NONE',  ( -1.000000000000000000, 0.000000000000000000, -0.000000000000000000 ) ) ;
#9857=ORIENTED_EDGE ( 'NONE', *, *, #25337, .F. ) ;
#9858=DIRECTION ( 'NONE',  ( -1.000000000000000000, 0.000000000000000000, 1.734723475976806848E-16 ) ) ;
#9859=DIRECTION ( 'NONE',  ( -1.000000000000000000, 0.000000000000000000, 1.734723475976806848E-16 ) ) ;
#9860=FACE_OUTER_BOUND ( 'NONE', #35124, .T. ) ;
#9861=EDGE_CURVE ( 'NONE', #1626, #13831, #21520, .T. ) ;
#9862=ORIENTED_EDGE ( 'NONE', *, *, #79, .F. ) ;
#9863=DIRECTION ( 'NONE',  ( -3.469446951953613696E-16, 0.000000000000000000, -1.000000000000000000 ) ) ;
#9864=DIRECTION ( 'NONE',  ( -1.000000000000000000, -0.000000000000000000, -0.000000000000000000 ) ) ;
#9866=PLANE ( 'NONE',  #15462 ) ;
#9870=DIRECTION ( 'NONE',  ( 1.734723475976806848E-16, -0.000000000000000000, 1.000000000000000000 ) ) ;
#9871=CARTESIAN_POINT ( 'NONE',  ( 1.287906020515830141, 0.000000000000000000, -0.9448818897637765168 ) ) ;
#9875=VECTOR ( 'NONE', #32299, 39.37007874015748143 ) ;
#9876=LINE ( 'NONE', #43116, #34900 ) ;
#9877=DIRECTION ( 'NONE',  ( -3.469446951953613696E-16, 0.000000000000000000, -1.000000000000000000 ) ) ;
#9878=LINE ( 'NONE', #9627, #2395 ) ;
#9880=VERTEX_POINT ( 'NONE', #21015 ) ;
#9883=AXIS2_PLACEMENT_3D ( 'NONE', #36712, #9081, #13468 ) ;
#9890=EDGE_CURVE ( 'NONE', #31232, #31458, #1642, .T. ) ;
#9891=LINE ( 'NONE', #9119, #1959 ) ;
#9892=CARTESIAN_POINT ( 'NONE',  ( 0.000000000000000000, 3.267716535433071279, -0.1574803149606301411 ) ) ;
#9893=CARTESIAN_POINT ( 'NONE',  ( -1.712496953225537633, 3.346456692913386100, -0.4724409448818884805 ) ) ;
#9895=LINE ( 'NONE', #5509, #11826 ) ;
#9897=DIRECTION ( 'NONE',  ( -3.469446951953613696E-16, 0.000000000000000000, -1.000000000000000000 ) ) ;
#9898=ORIENTED_EDGE ( 'NONE', *, *, #3523, .T. ) ;
#9899=DIRECTION ( 'NONE',  ( 1.000000000000000000, -0.000000000000000000, 0.000000000000000000 ) ) ;
#9901=EDGE_CURVE ( 'NONE', #3787, #38012, #33158, .T. ) ;
#9902=CARTESIAN_POINT ( 'NONE',  ( -1.636583440222564301, 3.346456692913386100, -1.141732283464563791 ) ) ;
#9903=VECTOR ( 'NONE', #32680, 39.37007874015748143 ) ;
#9904=EDGE_LOOP ( 'NONE', ( #42997, #45037, #37994, #22120 ) ) ;
#9905=PLANE ( 'NONE',  #24213 ) ;
#9906=LINE ( 'NONE', #1389, #12714 ) ;
#9908=ORIENTED_EDGE ( 'NONE', *, *, #49462, .T. ) ;
#9910=CARTESIAN_POINT ( 'NONE',  ( 0.000000000000000000, 3.267716535433071279, 1.417322834645662777 ) ) ;
#9912=DIRECTION ( 'NONE',  ( -0.000000000000000000, 1.000000000000000000, -0.000000000000000000 ) ) ;
#9913=VECTOR ( 'NONE', #41004, 39.37007874015748854 ) ;
#9914=DIRECTION ( 'NONE',  ( 0.000000000000000000, 0.000000000000000000, -1.000000000000000000 ) ) ;
#9917=AXIS2_PLACEMENT_3D ( 'NONE', #32617, #28207, #48310 ) ;
#9918=ADVANCED_FACE ( 'NONE', ( #7298 ), #46007, .F. ) ;
#9919=CARTESIAN_POINT ( 'NONE',  ( -1.363819533518803473, 3.346456692913386100, 1.732283464566920950 ) ) ;
#9921=ORIENTED_EDGE ( 'NONE', *, *, #38311, .F. ) ;
#9922=LINE ( 'NONE', #48605, #1803 ) ;
#9923=CARTESIAN_POINT ( 'NONE',  ( 2.378961647330872786, 0.000000000000000000, 0.6299212598425161236 ) ) ;
#9924=ORIENTED_EDGE ( 'NONE', *, *, #8744, .F. ) ;
#9925=CARTESIAN_POINT ( 'NONE',  ( -1.166969139818015977, 3.346456692913386100, -1.102362204724405270 ) ) ;
#9926=CARTESIAN_POINT ( 'NONE',  ( 1.287906020515830141, 3.346456692913386100, -0.8267716535433055070 ) ) ;
#9927=VECTOR ( 'NONE', #15494, 39.37007874015748143 ) ;
#9928=DIRECTION ( 'NONE',  ( -0.000000000000000000, 1.000000000000000000, -0.000000000000000000 ) ) ;
#9930=ORIENTED_EDGE ( 'NONE', *, *, #7355, .F. ) ;
#9931=VERTEX_POINT ( 'NONE', #2664 ) ;
#9932=DIRECTION ( 'NONE',  ( 1.734723475976806848E-16, -0.000000000000000000, 1.000000000000000000 ) ) ;
#9933=CARTESIAN_POINT ( 'NONE',  ( -1.091055626815042201, 3.267716535433071279, 0.6299212598425164567 ) ) ;
#9934=CARTESIAN_POINT ( 'NONE',  ( -0.07591351300297333182, 3.346456692913386100, -1.732283464566922726 ) ) ;
#9935=EDGE_LOOP ( 'NONE', ( #13690, #21229, #42137, #10843 ) ) ;
#9937=CARTESIAN_POINT ( 'NONE',  ( 1.761123562704338452, 3.267716535433071279, 1.259842519685033135 ) ) ;
#9939=ADVANCED_FACE ( 'NONE', ( #10669 ), #23039, .F. ) ;
#9940=LINE ( 'NONE', #29809, #24922 ) ;
#9944=CARTESIAN_POINT ( 'NONE',  ( -1.636583440222563635, 3.267716535433071279, 0.4330708661417290162 ) ) ;
#9946=PLANE ( 'NONE',  #49164 ) ;
#9947=LINE ( 'NONE', #14584, #45263 ) ;
#9948=VERTEX_POINT ( 'NONE', #232 ) ;
#9949=PLANE ( 'NONE',  #6344 ) ;
#9950=CARTESIAN_POINT ( 'NONE',  ( 0.5455278134075212115, 3.346456692913386100, -0.6299212598425181220 ) ) ;
#9952=VECTOR ( 'NONE', #7154, 39.37007874015748143 ) ;
#9953=VECTOR ( 'NONE', #5390, 39.37007874015748143 ) ;
#9955=EDGE_CURVE ( 'NONE', #4281, #37443, #11170, .T. ) ;
#9956=PLANE ( 'NONE',  #11305 ) ;
#9958=ORIENTED_EDGE ( 'NONE', *, *, #1312, .F. ) ;
#9960=CIRCLE ( 'NONE', #25649, 2.106299212598425008 ) ;
#9961=CARTESIAN_POINT ( 'NONE',  ( 1.363819533518803251, 3.346456692913386100, 1.102362204724403938 ) ) ;
#9963=CARTESIAN_POINT ( 'NONE',  ( 0.1968503937007873017, 3.346456692913386100, -0.6299212598425177889 ) ) ;
#9965=ORIENTED_EDGE ( 'NONE', *, *, #30428, .T. ) ;
#9966=DIRECTION ( 'NONE',  ( 1.000000000000000000, 0.000000000000000000, 0.000000000000000000 ) ) ;
#9967=CARTESIAN_POINT ( 'NONE',  ( 0.000000000000000000, 3.267716535433071279, -0.6692913385826758654 ) ) ;
#9968=LINE ( 'NONE', #14095, #26842 ) ;
#9969=ORIENTED_EDGE ( 'NONE', *, *, #14418, .F. ) ;
#9970=DIRECTION ( 'NONE',  ( -0.000000000000000000, 0.000000000000000000, 1.000000000000000000 ) ) ;
#9971=VERTEX_POINT ( 'NONE', #41652 ) ;
#9972=FACE_BOUND ( 'NONE', #49839, .T. ) ;
#9974=FACE_OUTER_BOUND ( 'NONE', #23580, .T. ) ;
#9975=DIRECTION ( 'NONE',  ( 1.734723475976806848E-16, 0.000000000000000000, 1.000000000000000000 ) ) ;
#9976=EDGE_CURVE ( 'NONE', #16878, #16143, #38544, .T. ) ;
#9977=ORIENTED_EDGE ( 'NONE', *, *, #521, .T. ) ;
#9978=ORIENTED_EDGE ( 'NONE', *, *, #9138, .T. ) ;
#9979=CARTESIAN_POINT ( 'NONE',  ( 1.636583440222563857, 3.346456692913386100, -0.1968503937007886062 ) ) ;
#9980=ORIENTED_EDGE ( 'NONE', *, *, #5203, .T. ) ;
#9982=EDGE_LOOP ( 'NONE', ( #48726, #8217, #16459, #33175 ) ) ;
#9983=ADVANCED_FACE ( 'NONE', ( #45747 ), #34166, .F. ) ;
#9985=CARTESIAN_POINT ( 'NONE',  ( 0.4696143004045484903, 3.346456692913386100, 1.417322834645662777 ) ) ;
#9987=ADVANCED_FACE ( 'NONE', ( #6790 ), #22535, .F. ) ;
#9989=LINE ( 'NONE', #25735, #6818 ) ;
#9990=ADVANCED_FACE ( 'NONE', ( #30789 ), #38297, .F. ) ;
#9991=CARTESIAN_POINT ( 'NONE',  ( 0.000000000000000000, 3.267716535433071279, 0.000000000000000000 ) ) ;
#9992=VERTEX_POINT ( 'NONE', #7045 ) ;
#9994=PLANE ( 'NONE',  #20790 ) ;
#9995=ORIENTED_EDGE ( 'NONE', *, *, #26322, .T. ) ;
#9996=AXIS2_PLACEMENT_3D ( 'NONE', #23751, #43102, #7502 ) ;
#9998=EDGE_CURVE ( 'NONE', #23774, #34452, #34667, .T. ) ;
#10001=VERTEX_POINT ( 'NONE', #15042 ) ;
#10002=ORIENTED_EDGE ( 'NONE', *, *, #26537, .T. ) ;
#10005=FACE_OUTER_BOUND ( 'NONE', #45838, .T. ) ;
#10007=EDGE_CURVE ( 'NONE', #4959, #50129, #26901, .T. ) ;
#10010=ORIENTED_EDGE ( 'NONE', *, *, #37245, .F. ) ;
#10011=FACE_OUTER_BOUND ( 'NONE', #19107, .T. ) ;
#10015=DIRECTION ( 'NONE',  ( 1.734723475976806848E-16, 0.000000000000000000, 1.000000000000000000 ) ) ;
#10016=LINE ( 'NONE', #25757, #8546 ) ;
#10017=CARTESIAN_POINT ( 'NONE',  ( -0.3486774197067340486, 3.267716535433071279, -0.8267716535433049518 ) ) ;
#10019=AXIS2_PLACEMENT_3D ( 'NONE', #43524, #4049, #36056 ) ;
#10021=LINE ( 'NONE', #18022, #47871 ) ;
#10023=ORIENTED_EDGE ( 'NONE', *, *, #14789, .T. ) ;
#10024=LINE ( 'NONE', #22406, #30414 ) ;
#10026=AXIS2_PLACEMENT_3D ( 'NONE', #48978, #13659, #45125 ) ;
#10027=ORIENTED_EDGE ( 'NONE', *, *, #37872, .F. ) ;
#10028=DIRECTION ( 'NONE',  ( 1.000000000000000000, 0.000000000000000000, 0.000000000000000000 ) ) ;
#10029=VECTOR ( 'NONE', #39756, 39.37007874015748143 ) ;
#10030=VERTEX_POINT ( 'NONE', #43851 ) ;
#10033=VECTOR ( 'NONE', #42461, 39.37007874015748143 ) ;
#10034=FACE_OUTER_BOUND ( 'NONE', #20653, .T. ) ;
#10035=CARTESIAN_POINT ( 'NONE',  ( 0.4696143004045476577, 3.267716535433071279, -2.053280005709960054 ) ) ;
#10036=DIRECTION ( 'NONE',  ( 1.734723475976806848E-16, -0.000000000000000000, 1.000000000000000000 ) ) ;
#10041=DIRECTION ( 'NONE',  ( -3.469446951953613696E-16, 0.000000000000000000, -1.000000000000000000 ) ) ;
#10042=ORIENTED_EDGE ( 'NONE', *, *, #1789, .T. ) ;
#10043=LINE ( 'NONE', #41793, #26271 ) ;
#10044=CARTESIAN_POINT ( 'NONE',  ( -1.057143431661240696, 3.267716535433071279, 1.889763779527550147 ) ) ;
#10045=ORIENTED_EDGE ( 'NONE', *, *, #11461, .T. ) ;
#10046=DIRECTION ( 'NONE',  ( 1.734723475976806848E-16, -0.000000000000000000, 1.000000000000000000 ) ) ;
#10047=EDGE_CURVE ( 'NONE', #16283, #19691, #47441, .T. ) ;
#10049=EDGE_CURVE ( 'NONE', #31344, #10330, #22632, .T. ) ;
#10050=EDGE_CURVE ( 'NONE', #14916, #329, #4371, .T. ) ;
#10052=ORIENTED_EDGE ( 'NONE', *, *, #38861, .T. ) ;
#10053=VERTEX_POINT ( 'NONE', #16510 ) ;
#10054=CARTESIAN_POINT ( 'NONE',  ( 1.636583440222563857, 3.346456692913386100, 0.6299212598425164567 ) ) ;
#10055=FACE_BOUND ( 'NONE', #11787, .T. ) ;
#10060=LINE ( 'NONE', #28647, #15941 ) ;
#10061=ORIENTED_EDGE ( 'NONE', *, *, #3521, .F. ) ;
#10062=ORIENTED_EDGE ( 'NONE', *, *, #25973, .T. ) ;
#10063=LINE ( 'NONE', #33316, #16693 ) ;
#10064=AXIS2_PLACEMENT_3D ( 'NONE', #34809, #50742, #11064 ) ;
#10065=CARTESIAN_POINT ( 'NONE',  ( -1.195183497228115035E-16, 0.000000000000000000, -0.6299212598425177889 ) ) ;
#10067=ORIENTED_EDGE ( 'NONE', *, *, #5639, .T. ) ;
#10068=VECTOR ( 'NONE', #18567, 39.37007874015748143 ) ;
#10070=ORIENTED_EDGE ( 'NONE', *, *, #9596, .T. ) ;
#10071=LINE ( 'NONE', #37704, #2948 ) ;
#10072=AXIS2_PLACEMENT_3D ( 'NONE', #28049, #39421, #32721 ) ;
#10073=LINE ( 'NONE', #41314, #36533 ) ;
#10074=EDGE_CURVE ( 'NONE', #4308, #27306, #16248, .T. ) ;
#10075=DIRECTION ( 'NONE',  ( -0.000000000000000000, 1.000000000000000000, -0.000000000000000000 ) ) ;
#10077=EDGE_CURVE ( 'NONE', #7418, #10769, #1266, .T. ) ;
#10078=ORIENTED_EDGE ( 'NONE', *, *, #3910, .T. ) ;
#10079=ORIENTED_EDGE ( 'NONE', *, *, #36924, .F. ) ;
#10080=DIRECTION ( 'NONE',  ( -0.000000000000000000, 0.000000000000000000, 1.000000000000000000 ) ) ;
#10081=LINE ( 'NONE', #45924, #17222 ) ;
#10082=ADVANCED_FACE ( 'NONE', ( #28368 ), #32782, .F. ) ;
#10084=DIRECTION ( 'NONE',  ( 0.000000000000000000, -1.000000000000000000, 0.000000000000000000 ) ) ;
#10087=LINE ( 'NONE', #33597, #31661 ) ;
#10088=EDGE_LOOP ( 'NONE', ( #32910, #45559, #37090, #6569 ) ) ;
#10090=DIRECTION ( 'NONE',  ( -0.000000000000000000, 0.000000000000000000, 1.000000000000000000 ) ) ;
#10094=CARTESIAN_POINT ( 'NONE',  ( -0.5455278134075214336, 3.346456692913386100, -0.5118110236220467790 ) ) ;
#10095=ORIENTED_EDGE ( 'NONE', *, *, #42637, .T. ) ;
#10096=VECTOR ( 'NONE', #40723, 39.37007874015748143 ) ;
#10099=VECTOR ( 'NONE', #42240, 39.37007874015748143 ) ;
#10102=CARTESIAN_POINT ( 'NONE',  ( 0.6363476328836782381, 3.267716535433071279, 2.007874015748021268 ) ) ;
#10103=LINE ( 'NONE', #47452, #33852 ) ;
#10104=ORIENTED_EDGE ( 'NONE', *, *, #11801, .F. ) ;
#10106=ORIENTED_EDGE ( 'NONE', *, *, #40205, .F. ) ;
#10107=CARTESIAN_POINT ( 'NONE',  ( 1.909347346926324462, 0.000000000000000000, -1.299212598425194320 ) ) ;
#10108=ADVANCED_FACE ( 'NONE', ( #27854 ), #24254, .F. ) ;
#10109=ORIENTED_EDGE ( 'NONE', *, *, #11920, .T. ) ;
#10110=VERTEX_POINT ( 'NONE', #8248 ) ;
#10111=CARTESIAN_POINT ( 'NONE',  ( 0.000000000000000000, 3.267716535433071279, 1.417322834645662777 ) ) ;
#10112=CARTESIAN_POINT ( 'NONE',  ( 2.100403847690402337, 3.346456692913386100, -0.1574803149606304187 ) ) ;
#10113=LINE ( 'NONE', #17604, #1289 ) ;
#10114=ADVANCED_FACE ( 'NONE', ( #9268 ), #39997, .F. ) ;
#10115=ORIENTED_EDGE ( 'NONE', *, *, #34026, .T. ) ;
#10116=DIRECTION ( 'NONE',  ( -3.469446951953613696E-16, 0.000000000000000000, -1.000000000000000000 ) ) ;
#10118=CARTESIAN_POINT ( 'NONE',  ( 0.7423782071083087075, 0.000000000000000000, -1.259842519685035134 ) ) ;
#10119=ORIENTED_EDGE ( 'NONE', *, *, #23423, .T. ) ;
#10120=CARTESIAN_POINT ( 'NONE',  ( 0.000000000000000000, 3.267716535433071279, 0.7874015748031456541 ) ) ;
#10121=LINE ( 'NONE', #21745, #44174 ) ;
#10126=EDGE_CURVE ( 'NONE', #38943, #49919, #25013, .T. ) ;
#10127=DIRECTION ( 'NONE',  ( 0.000000000000000000, 0.000000000000000000, -1.000000000000000000 ) ) ;
#10131=AXIS2_PLACEMENT_3D ( 'NONE', #34943, #30816, #7326 ) ;
#10133=CARTESIAN_POINT ( 'NONE',  ( 1.636583440222563635, 3.346456692913386100, -1.456692913385823296 ) ) ;
#10134=AXIS2_PLACEMENT_3D ( 'NONE', #47792, #21236, #48558 ) ;
#10137=CARTESIAN_POINT ( 'NONE',  ( -0.2727639067037608278, 0.000000000000000000, 0.2755905511810995412 ) ) ;
#10138=AXIS2_PLACEMENT_3D ( 'NONE', #32242, #42880, #24997 ) ;
#10141=DIRECTION ( 'NONE',  ( 1.000000000000000000, 0.000000000000000000, 0.000000000000000000 ) ) ;
#10142=LINE ( 'NONE', #44983, #25396 ) ;
#10145=CARTESIAN_POINT ( 'NONE',  ( 0.5455278134075212115, 3.346456692913386100, -0.3149606299212593941 ) ) ;
#10146=CARTESIAN_POINT ( 'NONE',  ( 4.268512490100411402E-16, 0.000000000000000000, 2.204724409448808764 ) ) ;
#10147=CARTESIAN_POINT ( 'NONE',  ( -0.5455278134075216556, 3.346456692913386100, -2.401574803149598036 ) ) ;
#10148=ORIENTED_EDGE ( 'NONE', *, *, #5198, .T. ) ;
#10149=FACE_OUTER_BOUND ( 'NONE', #28883, .T. ) ;
#10151=PLANE ( 'NONE',  #19707 ) ;
#10152=ORIENTED_EDGE ( 'NONE', *, *, #46168, .T. ) ;
#10153=CARTESIAN_POINT ( 'NONE',  ( 1.636583440222563635, 0.000000000000000000, -1.259842519685035800 ) ) ;
#10155=CARTESIAN_POINT ( 'NONE',  ( -2.182111253630085290, 0.000000000000000000, -0.3149606299212589500 ) ) ;
#10156=CARTESIAN_POINT ( 'NONE',  ( 4.268512490100411402E-16, 0.000000000000000000, 2.204724409448808764 ) ) ;
#10157=ORIENTED_EDGE ( 'NONE', *, *, #34871, .T. ) ;
#10158=CARTESIAN_POINT ( 'NONE',  ( -0.8182917201112819283, 3.346456692913386100, 1.850393700787391849 ) ) ;
#10159=DIRECTION ( 'NONE',  ( -0.000000000000000000, 1.000000000000000000, -0.000000000000000000 ) ) ;
#10160=CARTESIAN_POINT ( 'NONE',  ( 0.8182917201112819283, 0.000000000000000000, -0.4724409448818889246 ) ) ;
#10161=CARTESIAN_POINT ( 'NONE',  ( -1.636583440222564301, 0.000000000000000000, -0.8267716535433052849 ) ) ;
#10164=ADVANCED_FACE ( 'NONE', ( #4885 ), #28881, .F. ) ;
#10165=EDGE_LOOP ( 'NONE', ( #49448, #22974, #36214, #49549 ) ) ;
#10169=EDGE_CURVE ( 'NONE', #34201, #41731, #5394, .T. ) ;
#10171=VECTOR ( 'NONE', #41716, 39.37007874015748143 ) ;
#10172=CARTESIAN_POINT ( 'NONE',  ( 0.8182917201112819283, 0.000000000000000000, -0.1574803149606301411 ) ) ;
#10175=EDGE_CURVE ( 'NONE', #10682, #20840, #32005, .T. ) ;
#10179=VERTEX_POINT ( 'NONE', #29395 ) ;
#10180=DIRECTION ( 'NONE',  ( -1.000000000000000000, 0.000000000000000000, 0.000000000000000000 ) ) ;
#10181=CARTESIAN_POINT ( 'NONE',  ( 0.000000000000000000, 3.267716535433071279, -1.614173228346451605 ) ) ;
#10182=DIRECTION ( 'NONE',  ( -1.000000000000000000, 0.000000000000000000, 0.000000000000000000 ) ) ;
#10183=EDGE_CURVE ( 'NONE', #29009, #37485, #37919, .T. ) ;
#10185=LINE ( 'NONE', #17680, #48739 ) ;
#10186=DIRECTION ( 'NONE',  ( 1.000000000000000000, 0.000000000000000000, 0.000000000000000000 ) ) ;
#10187=VECTOR ( 'NONE', #5248, 39.37007874015748143 ) ;
#10189=CARTESIAN_POINT ( 'NONE',  ( 0.000000000000000000, 3.267716535433071279, -1.732283464566923614 ) ) ;
#10190=ORIENTED_EDGE ( 'NONE', *, *, #23870, .T. ) ;
#10193=DIRECTION ( 'NONE',  ( 1.734723475976806848E-16, -0.000000000000000000, 1.000000000000000000 ) ) ;
#10195=ADVANCED_FACE ( 'NONE', ( #48974 ), #5655, .F. ) ;
#10197=CARTESIAN_POINT ( 'NONE',  ( 0.8182917201112819283, 0.000000000000000000, 0.4724409448818868706 ) ) ;
#10199=CARTESIAN_POINT ( 'NONE',  ( -0.3486774197067336045, 3.267716535433071279, 1.209717811016577845E-16 ) ) ;
#10200=ORIENTED_EDGE ( 'NONE', *, *, #29464, .F. ) ;
#10203=CARTESIAN_POINT ( 'NONE',  ( 0.4696143004045484903, 3.346456692913386100, 2.362204724409437961 ) ) ;
#10204=CARTESIAN_POINT ( 'NONE',  ( -0.3486774197067339376, 0.000000000000000000, -0.9448818897637762948 ) ) ;
#10207=DIRECTION ( 'NONE',  ( -0.000000000000000000, 1.000000000000000000, -0.000000000000000000 ) ) ;
#10208=DIRECTION ( 'NONE',  ( -0.000000000000000000, 1.000000000000000000, -0.000000000000000000 ) ) ;
#10209=EDGE_LOOP ( 'NONE', ( #23126, #30022, #42685 ) ) ;
#10212=EDGE_CURVE ( 'NONE', #13102, #19845, #21912, .T. ) ;
#10213=CARTESIAN_POINT ( 'NONE',  ( 1.015142113812069313, 3.346456692913386100, 1.102362204724403938 ) ) ;
#10215=VECTOR ( 'NONE', #19018, 39.37007874015748143 ) ;
#10217=CARTESIAN_POINT ( 'NONE',  ( 0.000000000000000000, 3.346456692913386100, 0.000000000000000000 ) ) ;
#10218=CARTESIAN_POINT ( 'NONE',  ( 1.091055626815042645, 3.267716535433071279, -0.9448818897637765168 ) ) ;
#10220=CARTESIAN_POINT ( 'NONE',  ( 1.833433833923351353, 0.000000000000000000, -0.6299212598425181220 ) ) ;
#10221=DIRECTION ( 'NONE',  ( -3.469446951953613696E-16, 0.000000000000000000, -1.000000000000000000 ) ) ;
#10223=VECTOR ( 'NONE', #23984, 39.37007874015748143 ) ;
#10225=CARTESIAN_POINT ( 'NONE',  ( 1.091055626815043311, 0.000000000000000000, 1.692913385826762873 ) ) ;
#10229=CARTESIAN_POINT ( 'NONE',  ( 1.560669927219590525, 3.346456692913386100, 1.220472440944875281 ) ) ;
#10230=LINE ( 'NONE', #46080, #11171 ) ;
#10234=DIRECTION ( 'NONE',  ( 1.734723475976806848E-16, -0.000000000000000000, 1.000000000000000000 ) ) ;
#10237=ORIENTED_EDGE ( 'NONE', *, *, #32088, .F. ) ;
#10238=EDGE_CURVE ( 'NONE', #42166, #44618, #6669, .T. ) ;
#10239=LINE ( 'NONE', #41480, #8326 ) ;
#10240=ADVANCED_FACE ( 'NONE', ( #9524 ), #29657, .F. ) ;
#10242=CARTESIAN_POINT ( 'NONE',  ( 0.1968503937007877735, 0.000000000000000000, 2.007874015748021268 ) ) ;
#10245=AXIS2_PLACEMENT_3D ( 'NONE', #1182, #28283, #8674 ) ;
#10246=VERTEX_POINT ( 'NONE', #5902 ) ;
#10247=DIRECTION ( 'NONE',  ( -3.469446951953613696E-16, 0.000000000000000000, -1.000000000000000000 ) ) ;
#10248=ORIENTED_EDGE ( 'NONE', *, *, #30175, .T. ) ;
#10249=ORIENTED_EDGE ( 'NONE', *, *, #34309, .T. ) ;
#10250=VECTOR ( 'NONE', #37555, 39.37007874015748143 ) ;
#10251=VECTOR ( 'NONE', #46427, 39.37007874015748143 ) ;
#10252=ORIENTED_EDGE ( 'NONE', *, *, #30848, .F. ) ;
#10253=ORIENTED_EDGE ( 'NONE', *, *, #1473, .T. ) ;
#10254=LINE ( 'NONE', #17745, #14554 ) ;
#10255=VECTOR ( 'NONE', #20622, 39.37007874015748143 ) ;
#10256=ORIENTED_EDGE ( 'NONE', *, *, #16427, .T. ) ;
#10257=CARTESIAN_POINT ( 'NONE',  ( -1.091055626815042645, 0.000000000000000000, 1.889763779527550147 ) ) ;
#10259=ADVANCED_FACE ( 'NONE', ( #42033 ), #25522, .F. ) ;
#10260=DIRECTION ( 'NONE',  ( 1.000000000000000000, -0.000000000000000000, 0.000000000000000000 ) ) ;
#10261=CARTESIAN_POINT ( 'NONE',  ( 0.8182917201112817063, 3.346456692913386100, -2.244094488188969283 ) ) ;
#10262=DIRECTION ( 'NONE',  ( -1.000000000000000000, -0.000000000000000000, -0.000000000000000000 ) ) ;
#10263=ORIENTED_EDGE ( 'NONE', *, *, #10433, .F. ) ;
#10264=PLANE ( 'NONE',  #19194 ) ;
#10265=LINE ( 'NONE', #14137, #32485 ) ;
#10266=DIRECTION ( 'NONE',  ( 0.000000000000000000, 0.000000000000000000, -1.000000000000000000 ) ) ;
#10267=EDGE_CURVE ( 'NONE', #575, #49569, #18287, .T. ) ;
#10268=LINE ( 'NONE', #13892, #27284 ) ;
#10269=VERTEX_POINT ( 'NONE', #13912 ) ;
#10270=CARTESIAN_POINT ( 'NONE',  ( 1.015142113812069979, 3.346456692913386100, 1.912654141836395372 ) ) ;
#10272=ORIENTED_EDGE ( 'NONE', *, *, #31159, .F. ) ;
#10273=DIRECTION ( 'NONE',  ( -1.000000000000000000, -0.000000000000000000, -0.000000000000000000 ) ) ;
#10274=DIRECTION ( 'NONE',  ( -1.000000000000000000, 0.000000000000000000, 0.000000000000000000 ) ) ;
#10275=ORIENTED_EDGE ( 'NONE', *, *, #40978, .T. ) ;
#10276=CIRCLE ( 'NONE', #49802, 2.165354330708661568 ) ;
#10278=VECTOR ( 'NONE', #30011, 39.37007874015748143 ) ;
#10279=VERTEX_POINT ( 'NONE', #10035 ) ;
#10281=VECTOR ( 'NONE', #35870, 39.37007874015748143 ) ;
#10282=EDGE_CURVE ( 'NONE', #36917, #47149, #25271, .T. ) ;
#10283=DIRECTION ( 'NONE',  ( -1.000000000000000000, -0.000000000000000000, -0.000000000000000000 ) ) ;
#10284=VECTOR ( 'NONE', #19029, 39.37007874015748143 ) ;
#10286=DIRECTION ( 'NONE',  ( -3.469446951953613696E-16, 0.000000000000000000, -1.000000000000000000 ) ) ;
#10288=ORIENTED_EDGE ( 'NONE', *, *, #23615, .T. ) ;
#10289=CARTESIAN_POINT ( 'NONE',  ( 0.5455278134075216556, 0.000000000000000000, 1.062992125984246083 ) ) ;
#10292=ORIENTED_EDGE ( 'NONE', *, *, #8555, .T. ) ;
#10293=DIRECTION ( 'NONE',  ( -1.000000000000000000, -0.000000000000000000, -0.000000000000000000 ) ) ;
#10294=ORIENTED_EDGE ( 'NONE', *, *, #1975, .F. ) ;
#10295=LINE ( 'NONE', #2551, #7339 ) ;
#10296=FACE_OUTER_BOUND ( 'NONE', #38923, .T. ) ;
#10299=LINE ( 'NONE', #21664, #30558 ) ;
#10304=DIRECTION ( 'NONE',  ( 1.000000000000000000, 0.000000000000000000, 0.000000000000000000 ) ) ;
#10306=ORIENTED_EDGE ( 'NONE', *, *, #50314, .F. ) ;
#10308=FACE_BOUND ( 'NONE', #23809, .T. ) ;
#10310=LINE ( 'NONE', #49253, #27840 ) ;
#10311=CARTESIAN_POINT ( 'NONE',  ( -1.909347346926324906, 0.000000000000000000, 1.220472440944875059 ) ) ;
#10312=ORIENTED_EDGE ( 'NONE', *, *, #28531, .T. ) ;
#10314=ADVANCED_FACE ( 'NONE', ( #49729 ), #14415, .F. ) ;
#10315=CARTESIAN_POINT ( 'NONE',  ( -1.909347346926324462, 3.346456692913386100, 1.102362204724404160 ) ) ;
#10316=VECTOR ( 'NONE', #11903, 39.37007874015748143 ) ;
#10318=VECTOR ( 'NONE', #18625, 39.37007874015748143 ) ;
#10319=ORIENTED_EDGE ( 'NONE', *, *, #7310, .F. ) ;
#10320=VECTOR ( 'NONE', #42826, 39.37007874015748143 ) ;
#10322=VECTOR ( 'NONE', #16900, 39.37007874015748143 ) ;
#10323=ORIENTED_EDGE ( 'NONE', *, *, #5703, .T. ) ;
#10324=CARTESIAN_POINT ( 'NONE',  ( -1.166969139818015533, 0.000000000000000000, 1.102362204724404160 ) ) ;
#10325=LINE ( 'NONE', #26069, #46403 ) ;
#10326=CARTESIAN_POINT ( 'NONE',  ( 0.5455278134075211005, 3.267716535433071279, 0.1181102362204701633 ) ) ;
#10327=EDGE_CURVE ( 'NONE', #33404, #44569, #11045, .T. ) ;
#10328=DIRECTION ( 'NONE',  ( 1.000000000000000000, 0.000000000000000000, 0.000000000000000000 ) ) ;
#10329=ORIENTED_EDGE ( 'NONE', *, *, #47676, .F. ) ;
#10330=VERTEX_POINT ( 'NONE', #10789 ) ;
#10331=VECTOR ( 'NONE', #4767, 39.37007874015748143 ) ;
#10332=DIRECTION ( 'NONE',  ( 1.000000000000000000, 0.000000000000000000, 0.000000000000000000 ) ) ;
#10333=CARTESIAN_POINT ( 'NONE',  ( 1.287906020515830585, 3.346456692913386100, 1.377952755905504256 ) ) ;
#10336=ADVANCED_FACE ( 'NONE', ( #11549 ), #26784, .F. ) ;
#10338=EDGE_CURVE ( 'NONE', #19488, #35545, #42278, .T. ) ;
#10339=LINE ( 'NONE', #21704, #32549 ) ;
#10342=VERTEX_POINT ( 'NONE', #38421 ) ;
#10343=PLANE ( 'NONE',  #11065 ) ;
#10348=ORIENTED_EDGE ( 'NONE', *, *, #44650, .F. ) ;
#10349=EDGE_CURVE ( 'NONE', #18986, #26807, #7427, .T. ) ;
#10350=VECTOR ( 'NONE', #29119, 39.37007874015748143 ) ;
#10352=ORIENTED_EDGE ( 'NONE', *, *, #29430, .T. ) ;
#10353=CARTESIAN_POINT ( 'NONE',  ( -0.8182917201112818173, 3.267716535433071279, 1.419509857074483292E-16 ) ) ;
#10356=ORIENTED_EDGE ( 'NONE', *, *, #24977, .T. ) ;
#10358=DIRECTION ( 'NONE',  ( 1.734723475976806848E-16, -0.000000000000000000, 1.000000000000000000 ) ) ;
#10359=VECTOR ( 'NONE', #21991, 39.37007874015748143 ) ;
#10364=VECTOR ( 'NONE', #50, 39.37007874015748143 ) ;
#10365=CARTESIAN_POINT ( 'NONE',  ( -0.5455278134075216556, 0.000000000000000000, -2.204724409448810540 ) ) ;
#10366=EDGE_CURVE ( 'NONE', #47863, #20926, #6918, .T. ) ;
#10367=ORIENTED_EDGE ( 'NONE', *, *, #36639, .T. ) ;
#10369=DIRECTION ( 'NONE',  ( -3.469446951953613696E-16, 0.000000000000000000, -1.000000000000000000 ) ) ;
#10371=CARTESIAN_POINT ( 'NONE',  ( 1.363819533518803251, 3.346456692913386100, 0.7874015748031454320 ) ) ;
#10373=ORIENTED_EDGE ( 'NONE', *, *, #3000, .F. ) ;
#10375=PLANE ( 'NONE',  #26665 ) ;
#10376=CARTESIAN_POINT ( 'NONE',  ( 0.8182917201112819283, 0.000000000000000000, -0.03937007874015881204 ) ) ;
#10379=CARTESIAN_POINT ( 'NONE',  ( -0.5455278134075214336, 3.346456692913386100, -0.9448818897637762948 ) ) ;
#10380=CARTESIAN_POINT ( 'NONE',  ( -0.3486774197067339376, 3.346456692913386100, -1.889763779527552146 ) ) ;
#10381=VERTEX_POINT ( 'NONE', #11797 ) ;
#10382=ORIENTED_EDGE ( 'NONE', *, *, #30272, .T. ) ;
#10385=CARTESIAN_POINT ( 'NONE',  ( 0.5455278134075216556, 3.346456692913386100, 1.062992125984246083 ) ) ;
#10388=EDGE_LOOP ( 'NONE', ( #48399, #30929, #49194, #48877 ) ) ;
#10389=ORIENTED_EDGE ( 'NONE', *, *, #14789, .F. ) ;
#10390=VECTOR ( 'NONE', #37210, 39.37007874015748143 ) ;
#10394=DIRECTION ( 'NONE',  ( -3.469446951953613696E-16, 0.000000000000000000, -1.000000000000000000 ) ) ;
#10395=AXIS2_PLACEMENT_3D ( 'NONE', #20639, #1017, #13406 ) ;
#10399=EDGE_CURVE ( 'NONE', #19912, #3116, #34300, .T. ) ;
#10402=EDGE_LOOP ( 'NONE', ( #40253, #4335, #50610, #44018 ) ) ;
#10403=DIRECTION ( 'NONE',  ( 1.000000000000000000, -0.000000000000000000, 0.000000000000000000 ) ) ;
#10406=VERTEX_POINT ( 'NONE', #46380 ) ;
#10407=LINE ( 'NONE', #14788, #42196 ) ;
#10410=VERTEX_POINT ( 'NONE', #49985 ) ;
#10411=DIRECTION ( 'NONE',  ( -1.000000000000000000, 0.000000000000000000, -0.000000000000000000 ) ) ;
#10412=ORIENTED_EDGE ( 'NONE', *, *, #32177, .F. ) ;
#10413=PLANE ( 'NONE',  #48526 ) ;
#10415=ORIENTED_EDGE ( 'NONE', *, *, #23474, .F. ) ;
#10416=DIRECTION ( 'NONE',  ( 0.000000000000000000, 1.000000000000000000, 0.000000000000000000 ) ) ;
#10420=CARTESIAN_POINT ( 'NONE',  ( 0.000000000000000000, 3.346456692913386100, 0.000000000000000000 ) ) ;
#10421=VECTOR ( 'NONE', #14266, 39.37007874015748143 ) ;
#10422=ORIENTED_EDGE ( 'NONE', *, *, #6839, .F. ) ;
#10423=ORIENTED_EDGE ( 'NONE', *, *, #30942, .T. ) ;
#10424=CARTESIAN_POINT ( 'NONE',  ( 0.2727639067037609943, 3.346456692913386100, 1.220472440944875281 ) ) ;
#10425=VECTOR ( 'NONE', #29096, 39.37007874015748143 ) ;
#10426=LINE ( 'NONE', #38558, #45253 ) ;
#10427=VECTOR ( 'NONE', #28857, 39.37007874015748143 ) ;
#10429=ORIENTED_EDGE ( 'NONE', *, *, #8840, .F. ) ;
#10431=CARTESIAN_POINT ( 'NONE',  ( -1.166969139818016199, 0.000000000000000000, -1.614173228346451605 ) ) ;
#10433=EDGE_CURVE ( 'NONE', #49700, #43929, #14922, .T. ) ;
#10434=VECTOR ( 'NONE', #37044, 39.37007874015748143 ) ;
#10435=ORIENTED_EDGE ( 'NONE', *, *, #44360, .F. ) ;
#10436=ORIENTED_EDGE ( 'NONE', *, *, #9049, .F. ) ;
#10437=CARTESIAN_POINT ( 'NONE',  ( 3.927031490892378253E-16, 3.346456692913386100, 1.692913385826762873 ) ) ;
#10438=CARTESIAN_POINT ( 'NONE',  ( -3.927031490892378253E-16, 3.346456692913386100, -2.204724409448811429 ) ) ;
#10439=VECTOR ( 'NONE', #46294, 39.37007874015748143 ) ;
#10440=DIRECTION ( 'NONE',  ( 1.000000000000000000, 0.000000000000000000, 0.000000000000000000 ) ) ;
#10441=ORIENTED_EDGE ( 'NONE', *, *, #16818, .T. ) ;
#10443=LINE ( 'NONE', #26185, #40875 ) ;
#10444=VECTOR ( 'NONE', #1411, 39.37007874015748143 ) ;
#10446=LINE ( 'NONE', #45525, #27361 ) ;
#10447=VERTEX_POINT ( 'NONE', #4833 ) ;
#10448=VERTEX_POINT ( 'NONE', #4312 ) ;
#10451=DIRECTION ( 'NONE',  ( -1.000000000000000000, 0.000000000000000000, -0.000000000000000000 ) ) ;
#10452=ORIENTED_EDGE ( 'NONE', *, *, #24585, .T. ) ;
#10454=CARTESIAN_POINT ( 'NONE',  ( -1.712496953225537633, 0.000000000000000000, -0.7874015748031470974 ) ) ;
#10455=EDGE_LOOP ( 'NONE', ( #38513, #10710, #3916, #46771 ) ) ;
#10457=DIRECTION ( 'NONE',  ( 1.734723475976806848E-16, 0.000000000000000000, 1.000000000000000000 ) ) ;
#10459=VECTOR ( 'NONE', #32451, 39.37007874015748143 ) ;
#10462=LINE ( 'NONE', #16366, #15357 ) ;
#10465=EDGE_LOOP ( 'NONE', ( #30673, #47985, #1808, #39662 ) ) ;
#10466=EDGE_CURVE ( 'NONE', #12085, #47811, #439, .T. ) ;
#10467=CARTESIAN_POINT ( 'NONE',  ( -0.07591351300297359550, 0.000000000000000000, -2.047244094488181343 ) ) ;
#10468=DIRECTION ( 'NONE',  ( -3.469446951953613696E-16, 0.000000000000000000, -1.000000000000000000 ) ) ;
#10469=EDGE_CURVE ( 'NONE', #9339, #35392, #36071, .T. ) ;
#10474=CARTESIAN_POINT ( 'NONE',  ( -2.165354330708661568, 3.346456692913386100, -6.146657985744592735E-16 ) ) ;
#10475=VECTOR ( 'NONE', #20142, 39.37007874015748143 ) ;
#10478=FACE_OUTER_BOUND ( 'NONE', #1853, .T. ) ;
#10479=VECTOR ( 'NONE', #21737, 39.37007874015748143 ) ;
#10480=ORIENTED_EDGE ( 'NONE', *, *, #48467, .T. ) ;
#10482=ORIENTED_EDGE ( 'NONE', *, *, #6100, .T. ) ;
#10483=FACE_BOUND ( 'NONE', #37007, .T. ) ;
#10485=CARTESIAN_POINT ( 'NONE',  ( 1.560669927219590303, 3.346456692913386100, -1.929133858267710666 ) ) ;
#10486=EDGE_CURVE ( 'NONE', #16772, #4281, #32203, .T. ) ;
#10487=LINE ( 'NONE', #49174, #7851 ) ;
#10488=VERTEX_POINT ( 'NONE', #12834 ) ;
#10489=ORIENTED_EDGE ( 'NONE', *, *, #27716, .T. ) ;
#10490=FACE_OUTER_BOUND ( 'NONE', #32850, .T. ) ;
#10491=DIRECTION ( 'NONE',  ( -1.000000000000000000, 0.000000000000000000, -0.000000000000000000 ) ) ;
#10493=DIRECTION ( 'NONE',  ( 1.000000000000000000, 0.000000000000000000, 0.000000000000000000 ) ) ;
#10497=ORIENTED_EDGE ( 'NONE', *, *, #44380, .F. ) ;
#10498=LINE ( 'NONE', #2242, #46358 ) ;
#10499=VECTOR ( 'NONE', #2283, 39.37007874015748143 ) ;
#10502=VECTOR ( 'NONE', #32184, 39.37007874015748143 ) ;
#10506=ORIENTED_EDGE ( 'NONE', *, *, #35719, .T. ) ;
#10507=EDGE_CURVE ( 'NONE', #37481, #1147, #20576, .T. ) ;
#10510=DIRECTION ( 'NONE',  ( 1.000000000000000000, 0.000000000000000000, -3.469446951953613696E-16 ) ) ;
#10511=EDGE_LOOP ( 'NONE', ( #42615, #23896, #11800, #2124 ) ) ;
#10512=VECTOR ( 'NONE', #7715, 39.37007874015748143 ) ;
#10513=DIRECTION ( 'NONE',  ( -0.000000000000000000, 1.000000000000000000, -0.000000000000000000 ) ) ;
#10514=CARTESIAN_POINT ( 'NONE',  ( -0.6214413264104942103, 3.267716535433071279, 2.156057715732900040E-16 ) ) ;
#10515=DIRECTION ( 'NONE',  ( -0.000000000000000000, 1.000000000000000000, -0.000000000000000000 ) ) ;
#10519=EDGE_CURVE ( 'NONE', #39188, #37274, #44312, .T. ) ;
#10520=CARTESIAN_POINT ( 'NONE',  ( -0.8182917201112814842, 3.346456692913386100, 1.102362204724404160 ) ) ;
#10521=DIRECTION ( 'NONE',  ( -0.000000000000000000, 1.000000000000000000, -0.000000000000000000 ) ) ;
#10522=LINE ( 'NONE', #30399, #19389 ) ;
#10526=DIRECTION ( 'NONE',  ( -3.469446951953613696E-16, 0.000000000000000000, -1.000000000000000000 ) ) ;
#10527=EDGE_CURVE ( 'NONE', #23763, #11950, #31948, .T. ) ;
#10528=DIRECTION ( 'NONE',  ( -0.000000000000000000, 1.000000000000000000, -0.000000000000000000 ) ) ;
#10529=ORIENTED_EDGE ( 'NONE', *, *, #28625, .T. ) ;
#10531=VECTOR ( 'NONE', #12502, 39.37007874015748143 ) ;
#10532=VECTOR ( 'NONE', #37979, 39.37007874015748143 ) ;
#10533=EDGE_CURVE ( 'NONE', #32010, #31869, #39937, .T. ) ;
#10534=DIRECTION ( 'NONE',  ( 1.000000000000000000, -0.000000000000000000, 0.000000000000000000 ) ) ;
#10535=VERTEX_POINT ( 'NONE', #16968 ) ;
#10536=CIRCLE ( 'NONE', #31206, 2.165354330708661568 ) ;
#10537=ORIENTED_EDGE ( 'NONE', *, *, #31782, .F. ) ;
#10539=DIRECTION ( 'NONE',  ( 0.000000000000000000, 0.000000000000000000, -1.000000000000000000 ) ) ;
#10540=FACE_OUTER_BOUND ( 'NONE', #49697, .T. ) ;
#10542=EDGE_CURVE ( 'NONE', #11695, #15891, #35555, .T. ) ;
#10543=PLANE ( 'NONE',  #31892 ) ;
#10544=VERTEX_POINT ( 'NONE', #47385 ) ;
#10547=ORIENTED_EDGE ( 'NONE', *, *, #815, .T. ) ;
#10548=VERTEX_POINT ( 'NONE', #20043 ) ;
#10549=DIRECTION ( 'NONE',  ( -3.469446951953613696E-16, 0.000000000000000000, -1.000000000000000000 ) ) ;
#10550=ORIENTED_EDGE ( 'NONE', *, *, #9113, .F. ) ;
#10554=LINE ( 'NONE', #3059, #22740 ) ;
#10556=DIRECTION ( 'NONE',  ( -0.000000000000000000, 1.000000000000000000, -0.000000000000000000 ) ) ;
#10558=LINE ( 'NONE', #49495, #15833 ) ;
#10560=VERTEX_POINT ( 'NONE', #28053 ) ;
#10561=ORIENTED_EDGE ( 'NONE', *, *, #5710, .T. ) ;
#10563=FACE_BOUND ( 'NONE', #47647, .T. ) ;
#10564=ORIENTED_EDGE ( 'NONE', *, *, #33072, .T. ) ;
#10565=EDGE_CURVE ( 'NONE', #26163, #40779, #4574, .T. ) ;
#10566=CARTESIAN_POINT ( 'NONE',  ( 2.069629837364519886, 3.267716535433071279, -1.299212598425194320 ) ) ;
#10568=VECTOR ( 'NONE', #39804, 39.37007874015748143 ) ;
#10569=VECTOR ( 'NONE', #11300, 39.37007874015748143 ) ;
#10570=ORIENTED_EDGE ( 'NONE', *, *, #3910, .F. ) ;
#10572=DIRECTION ( 'NONE',  ( 1.000000000000000000, 0.000000000000000000, -3.469446951953613696E-16 ) ) ;
#10574=EDGE_CURVE ( 'NONE', #47459, #4557, #44052, .T. ) ;
#10575=EDGE_LOOP ( 'NONE', ( #48532, #27670, #44801, #4745 ) ) ;
#10578=ORIENTED_EDGE ( 'NONE', *, *, #37477, .F. ) ;
#10579=EDGE_CURVE ( 'NONE', #31953, #47312, #46109, .T. ) ;
#10580=DIRECTION ( 'NONE',  ( -1.000000000000000000, 0.000000000000000000, 1.734723475976806848E-16 ) ) ;
#10582=VECTOR ( 'NONE', #18670, 39.37007874015748143 ) ;
#10583=DIRECTION ( 'NONE',  ( -3.469446951953613696E-16, 0.000000000000000000, -1.000000000000000000 ) ) ;
#10587=DIRECTION ( 'NONE',  ( 0.000000000000000000, -1.000000000000000000, 0.000000000000000000 ) ) ;
#10588=DIRECTION ( 'NONE',  ( -0.000000000000000000, 1.000000000000000000, -0.000000000000000000 ) ) ;
#10591=VECTOR ( 'NONE', #5128, 39.37007874015748143 ) ;
#10594=EDGE_CURVE ( 'NONE', #33946, #8577, #1974, .T. ) ;
#10596=EDGE_CURVE ( 'NONE', #24456, #25931, #2233, .T. ) ;
#10597=DIRECTION ( 'NONE',  ( 1.000000000000000000, 0.000000000000000000, 0.000000000000000000 ) ) ;
#10599=LINE ( 'NONE', #14209, #13542 ) ;
#10600=CARTESIAN_POINT ( 'NONE',  ( 0.000000000000000000, 3.267716535433071279, -0.6692913385826764205 ) ) ;
#10602=ORIENTED_EDGE ( 'NONE', *, *, #35063, .T. ) ;
#10603=DIRECTION ( 'NONE',  ( 0.000000000000000000, 1.000000000000000000, 0.000000000000000000 ) ) ;
#10605=VERTEX_POINT ( 'NONE', #14101 ) ;
#10606=EDGE_LOOP ( 'NONE', ( #30530, #48957, #5986, #18579 ) ) ;
#10607=LINE ( 'NONE', #38241, #29563 ) ;
#10609=ORIENTED_EDGE ( 'NONE', *, *, #28866, .F. ) ;
#10613=CARTESIAN_POINT ( 'NONE',  ( -2.182111253630085290, 3.346456692913386100, -0.1968503937007880511 ) ) ;
#10614=EDGE_CURVE ( 'NONE', #8862, #37378, #40972, .T. ) ;
#10615=VECTOR ( 'NONE', #42128, 39.37007874015748143 ) ;
#10618=ORIENTED_EDGE ( 'NONE', *, *, #3780, .T. ) ;
#10619=ORIENTED_EDGE ( 'NONE', *, *, #40773, .F. ) ;
#10620=CARTESIAN_POINT ( 'NONE',  ( -2.182111253630085290, 3.267716535433071279, 3.785359618865289765E-16 ) ) ;
#10622=CARTESIAN_POINT ( 'NONE',  ( 1.363819533518803251, 0.000000000000000000, 1.417322834645662777 ) ) ;
#10623=LINE ( 'NONE', #25599, #10359 ) ;
#10625=EDGE_CURVE ( 'NONE', #11936, #20750, #41224, .T. ) ;
#10626=ORIENTED_EDGE ( 'NONE', *, *, #15201, .T. ) ;
#10629=LINE ( 'NONE', #42113, #39866 ) ;
#10630=LINE ( 'NONE', #29738, #609 ) ;
#10631=EDGE_CURVE ( 'NONE', #12457, #41521, #30103, .T. ) ;
#10632=ORIENTED_EDGE ( 'NONE', *, *, #29666, .F. ) ;
#10635=ADVANCED_FACE ( 'NONE', ( #5591 ), #6098, .F. ) ;
#10636=EDGE_LOOP ( 'NONE', ( #34302, #25402, #34335, #27275 ) ) ;
#10637=VERTEX_POINT ( 'NONE', #21089 ) ;
#10640=VECTOR ( 'NONE', #32339, 39.37007874015748143 ) ;
#10641=CARTESIAN_POINT ( 'NONE',  ( 0.000000000000000000, 3.267716535433071279, 1.692913385826762873 ) ) ;
#10642=LINE ( 'NONE', #17624, #47705 ) ;
#10643=VERTEX_POINT ( 'NONE', #45567 ) ;
#10644=ORIENTED_EDGE ( 'NONE', *, *, #34449, .F. ) ;
#10645=CARTESIAN_POINT ( 'NONE',  ( -0.8182917201112819283, 0.000000000000000000, 2.047244094488179567 ) ) ;
#10646=LINE ( 'NONE', #10133, #24314 ) ;
#10647=ORIENTED_EDGE ( 'NONE', *, *, #25800, .T. ) ;
#10648=LINE ( 'NONE', #26388, #35669 ) ;
#10649=CARTESIAN_POINT ( 'NONE',  ( 0.000000000000000000, 3.267716535433071279, -2.204724409448810540 ) ) ;
#10650=EDGE_CURVE ( 'NONE', #43639, #8308, #49173, .T. ) ;
#10652=VECTOR ( 'NONE', #1943, 39.37007874015748143 ) ;
#10653=ADVANCED_FACE ( 'NONE', ( #25463 ), #18229, .F. ) ;
#10654=VECTOR ( 'NONE', #30354, 39.37007874015748143 ) ;
#10656=CARTESIAN_POINT ( 'NONE',  ( -1.712496953225537188, 0.000000000000000000, -0.1574803149606297248 ) ) ;
#10657=PLANE ( 'NONE',  #11388 ) ;
#10658=VERTEX_POINT ( 'NONE', #10229 ) ;
#10659=CARTESIAN_POINT ( 'NONE',  ( -1.363819533518803473, 3.267716535433071279, 1.681890501046756192 ) ) ;
#10662=DIRECTION ( 'NONE',  ( 0.000000000000000000, 0.000000000000000000, 1.000000000000000000 ) ) ;
#10663=ORIENTED_EDGE ( 'NONE', *, *, #11, .T. ) ;
#10664=CARTESIAN_POINT ( 'NONE',  ( -0.07591351300297348448, 3.267716535433071279, 2.633779063002574070E-17 ) ) ;
#10666=CARTESIAN_POINT ( 'NONE',  ( -0.3486774197067334380, 0.000000000000000000, 0.9448818897637749625 ) ) ;
#10667=ORIENTED_EDGE ( 'NONE', *, *, #29358, .T. ) ;
#10668=EDGE_CURVE ( 'NONE', #7899, #46993, #1459, .T. ) ;
#10669=FACE_OUTER_BOUND ( 'NONE', #26939, .T. ) ;
#10670=VERTEX_POINT ( 'NONE', #10485 ) ;
#10672=ORIENTED_EDGE ( 'NONE', *, *, #23252, .F. ) ;
#10673=PLANE ( 'NONE',  #45144 ) ;
#10676=DIRECTION ( 'NONE',  ( 0.000000000000000000, -1.000000000000000000, 0.000000000000000000 ) ) ;
#10677=VECTOR ( 'NONE', #18110, 39.37007874015748143 ) ;
#10678=ORIENTED_EDGE ( 'NONE', *, *, #21417, .F. ) ;
#10679=ORIENTED_EDGE ( 'NONE', *, *, #36350, .T. ) ;
#10680=CARTESIAN_POINT ( 'NONE',  ( -1.536664496436148184E-16, 3.346456692913386100, -1.141732283464564013 ) ) ;
#10681=CARTESIAN_POINT ( 'NONE',  ( -1.593029370565769431, 3.267716535433071279, 1.377952755905504256 ) ) ;
#10682=VERTEX_POINT ( 'NONE', #25975 ) ;
#10683=DIRECTION ( 'NONE',  ( 1.734723475976806848E-16, -0.000000000000000000, 1.000000000000000000 ) ) ;
#10684=LINE ( 'NONE', #38317, #23609 ) ;
#10685=CARTESIAN_POINT ( 'NONE',  ( -1.363819533518803029, 3.267716535433071279, 2.365849761790804994E-16 ) ) ;
#10686=VECTOR ( 'NONE', #35649, 39.37007874015748143 ) ;
#10687=ORIENTED_EDGE ( 'NONE', *, *, #16855, .T. ) ;
#10688=ORIENTED_EDGE ( 'NONE', *, *, #51039, .F. ) ;
#10689=ADVANCED_FACE ( 'NONE', ( #9974 ), #17219, .F. ) ;
#10692=CARTESIAN_POINT ( 'NONE',  ( 1.560669927219590747, 0.000000000000000000, 0.7874015748031454320 ) ) ;
#10693=EDGE_CURVE ( 'NONE', #16832, #46970, #5845, .T. ) ;
#10694=EDGE_LOOP ( 'NONE', ( #22739, #13405, #20032, #48237, #48472 ) ) ;
#10695=CARTESIAN_POINT ( 'NONE',  ( 1.015142113812069091, 3.346456692913386100, -1.845530509571139399 ) ) ;
#10697=LINE ( 'NONE', #45776, #12015 ) ;
#10698=ORIENTED_EDGE ( 'NONE', *, *, #1783, .T. ) ;
#10699=CARTESIAN_POINT ( 'NONE',  ( 1.560669927219590747, 3.346456692913386100, 1.414498409778230492 ) ) ;
#10700=VERTEX_POINT ( 'NONE', #22108 ) ;
#10701=ORIENTED_EDGE ( 'NONE', *, *, #19402, .F. ) ;
#10702=AXIS2_PLACEMENT_3D ( 'NONE', #4944, #16568, #43402 ) ;
#10706=DIRECTION ( 'NONE',  ( -0.000000000000000000, 1.000000000000000000, -0.000000000000000000 ) ) ;
#10709=ADVANCED_FACE ( 'NONE', ( #41471 ), #13599, .F. ) ;
#10710=ORIENTED_EDGE ( 'NONE', *, *, #9538, .T. ) ;
#10711=DIRECTION ( 'NONE',  ( -1.000000000000000000, 0.000000000000000000, 1.734723475976806848E-16 ) ) ;
#10716=EDGE_CURVE ( 'NONE', #31608, #26125, #15369, .T. ) ;
#10717=LINE ( 'NONE', #41957, #26160 ) ;
#10718=DIRECTION ( 'NONE',  ( -3.469446951953613696E-16, 0.000000000000000000, -1.000000000000000000 ) ) ;
#10719=ORIENTED_EDGE ( 'NONE', *, *, #48004, .F. ) ;
#10720=CARTESIAN_POINT ( 'NONE',  ( 1.363819533518803251, 3.346456692913386100, -0.1574803149606304187 ) ) ;
#10722=LINE ( 'NONE', #31101, #44637 ) ;
#10723=VECTOR ( 'NONE', #24741, 39.37007874015748143 ) ;
#10724=ORIENTED_EDGE ( 'NONE', *, *, #3103, .F. ) ;
#10725=LINE ( 'NONE', #22849, #49528 ) ;
#10731=EDGE_LOOP ( 'NONE', ( #8633, #18588, #39422, #25079 ) ) ;
#10732=DIRECTION ( 'NONE',  ( -3.469446951953613696E-16, 0.000000000000000000, -1.000000000000000000 ) ) ;
#10735=FACE_BOUND ( 'NONE', #44607, .T. ) ;
#10736=CARTESIAN_POINT ( 'NONE',  ( 0.000000000000000000, 3.267716535433071279, -1.259842519685034690 ) ) ;
#10737=CARTESIAN_POINT ( 'NONE',  ( -1.636583440222564301, 3.346456692913386100, -1.771653543307080581 ) ) ;
#10738=ORIENTED_EDGE ( 'NONE', *, *, #13683, .T. ) ;
#10739=VERTEX_POINT ( 'NONE', #46819 ) ;
#10740=PLANE ( 'NONE',  #27323 ) ;
#10742=FACE_OUTER_BOUND ( 'NONE', #39963, .T. ) ;
#10744=LINE ( 'NONE', #30372, #10798 ) ;
#10745=ORIENTED_EDGE ( 'NONE', *, *, #17782, .F. ) ;
#10747=CARTESIAN_POINT ( 'NONE',  ( 1.560669927219590303, 0.000000000000000000, -1.614173228346452715 ) ) ;
#10749=EDGE_CURVE ( 'NONE', #5755, #23656, #46079, .T. ) ;
#10750=VERTEX_POINT ( 'NONE', #6616 ) ;
#10752=CARTESIAN_POINT ( 'NONE',  ( -0.8942052331142552601, 3.346456692913386100, -1.456692913385822186 ) ) ;
#10753=ORIENTED_EDGE ( 'NONE', *, *, #2112, .F. ) ;
#10755=EDGE_CURVE ( 'NONE', #7825, #28628, #26228, .T. ) ;
#10757=AXIS2_PLACEMENT_3D ( 'NONE', #26192, #49641, #33005 ) ;
#10758=ORIENTED_EDGE ( 'NONE', *, *, #9276, .F. ) ;
#10761=VECTOR ( 'NONE', #50545, 39.37007874015748143 ) ;
#10763=CARTESIAN_POINT ( 'NONE',  ( -0.07591351300297333182, 3.267716535433071279, 0.4724409448818869817 ) ) ;
#10764=EDGE_CURVE ( 'NONE', #1038, #4027, #31118, .T. ) ;
#10769=VERTEX_POINT ( 'NONE', #18982 ) ;
#10770=LINE ( 'NONE', #22898, #4384 ) ;
#10772=EDGE_CURVE ( 'NONE', #23541, #35962, #11495, .T. ) ;
#10773=DIRECTION ( 'NONE',  ( 1.000000000000000000, 0.000000000000000000, 0.000000000000000000 ) ) ;
#10774=FACE_OUTER_BOUND ( 'NONE', #26658, .T. ) ;
#10778=ORIENTED_EDGE ( 'NONE', *, *, #46603, .F. ) ;
#10779=CARTESIAN_POINT ( 'NONE',  ( -0.8182917201112823724, 3.267716535433071279, 1.419509857074484278E-16 ) ) ;
#10781=VERTEX_POINT ( 'NONE', #38860 ) ;
#10782=CARTESIAN_POINT ( 'NONE',  ( -0.8942052331142552601, 3.267716535433071279, 3.102397620449223960E-16 ) ) ;
#10783=ORIENTED_EDGE ( 'NONE', *, *, #21437, .T. ) ;
#10785=DIRECTION ( 'NONE',  ( 0.000000000000000000, 0.000000000000000000, -1.000000000000000000 ) ) ;
#10786=CONICAL_SURFACE ( 'NONE', #43755, 2.493791675044291445, 0.4363323129985800519 ) ;
#10787=DIRECTION ( 'NONE',  ( -1.000000000000000000, -0.000000000000000000, -0.000000000000000000 ) ) ;
#10788=VECTOR ( 'NONE', #8324, 39.37007874015748143 ) ;
#10789=CARTESIAN_POINT ( 'NONE',  ( -2.043170538425928662, 3.267716535433071279, -0.5118110236220464460 ) ) ;
#10790=DIRECTION ( 'NONE',  ( -0.000000000000000000, 1.000000000000000000, -0.000000000000000000 ) ) ;
#10792=CARTESIAN_POINT ( 'NONE',  ( -1.536664496436148184E-16, 0.000000000000000000, -1.141732283464564013 ) ) ;
#10793=VERTEX_POINT ( 'NONE', #49925 ) ;
#10794=ORIENTED_EDGE ( 'NONE', *, *, #5203, .F. ) ;
#10795=CARTESIAN_POINT ( 'NONE',  ( 0.000000000000000000, 3.267716535433071279, -2.165354330708661568 ) ) ;
#10797=CARTESIAN_POINT ( 'NONE',  ( 1.363819533518803695, 0.000000000000000000, 1.732283464566921172 ) ) ;
#10798=VECTOR ( 'NONE', #25988, 39.37007874015748143 ) ;
#10799=CARTESIAN_POINT ( 'NONE',  ( 0.2727639067037602172, 0.000000000000000000, -1.732283464566922726 ) ) ;
#10801=CARTESIAN_POINT ( 'NONE',  ( 0.000000000000000000, 3.267716535433071279, 0.5905511811023582691 ) ) ;
#10802=LINE ( 'NONE', #21415, #17501 ) ;
#10803=EDGE_CURVE ( 'NONE', #41904, #30696, #3493, .T. ) ;
#10804=FACE_OUTER_BOUND ( 'NONE', #16122, .T. ) ;
#10805=ORIENTED_EDGE ( 'NONE', *, *, #8710, .T. ) ;
#10806=EDGE_CURVE ( 'NONE', #19754, #40954, #41979, .T. ) ;
#10807=EDGE_LOOP ( 'NONE', ( #43918, #25663, #4143, #14508 ) ) ;
#10809=FACE_BOUND ( 'NONE', #26272, .T. ) ;
#10810=EDGE_LOOP ( 'NONE', ( #37929, #43182, #32461, #10918 ) ) ;
#10811=EDGE_CURVE ( 'NONE', #38065, #38012, #38116, .T. ) ;
#10812=LINE ( 'NONE', #35071, #22080 ) ;
#10814=EDGE_CURVE ( 'NONE', #23656, #44436, #2734, .T. ) ;
#10815=ORIENTED_EDGE ( 'NONE', *, *, #7786, .T. ) ;
#10816=ORIENTED_EDGE ( 'NONE', *, *, #18813, .T. ) ;
#10818=DIRECTION ( 'NONE',  ( -1.000000000000000000, 0.000000000000000000, 0.000000000000000000 ) ) ;
#10820=VECTOR ( 'NONE', #47411, 39.37007874015748143 ) ;
#10822=DIRECTION ( 'NONE',  ( 0.000000000000000000, 0.000000000000000000, -1.000000000000000000 ) ) ;
#10824=DIRECTION ( 'NONE',  ( 1.000000000000000000, 0.000000000000000000, 0.000000000000000000 ) ) ;
#10826=EDGE_CURVE ( 'NONE', #33365, #15732, #50922, .T. ) ;
#10829=DIRECTION ( 'NONE',  ( 1.000000000000000000, -0.000000000000000000, 0.000000000000000000 ) ) ;
#10830=ORIENTED_EDGE ( 'NONE', *, *, #50156, .F. ) ;
#10831=VERTEX_POINT ( 'NONE', #6862 ) ;
#10836=VECTOR ( 'NONE', #32278, 39.37007874015748143 ) ;
#10837=LINE ( 'NONE', #26333, #9472 ) ;
#10839=VECTOR ( 'NONE', #26769, 39.37007874015748143 ) ;
#10841=EDGE_CURVE ( 'NONE', #31518, #41767, #18485, .T. ) ;
#10842=PLANE ( 'NONE',  #44030 ) ;
#10843=ORIENTED_EDGE ( 'NONE', *, *, #18207, .F. ) ;
#10844=CARTESIAN_POINT ( 'NONE',  ( 1.636583440222563857, 3.346456692913386100, 1.574803149606291974 ) ) ;
#10845=LINE ( 'NONE', #10600, #19473 ) ;
#10846=VERTEX_POINT ( 'NONE', #38362 ) ;
#10847=EDGE_CURVE ( 'NONE', #26492, #50693, #26726, .T. ) ;
#10848=VERTEX_POINT ( 'NONE', #43989 ) ;
#10849=DIRECTION ( 'NONE',  ( -1.000000000000000000, 0.000000000000000000, 1.734723475976806848E-16 ) ) ;
#10850=CARTESIAN_POINT ( 'NONE',  ( -1.195183497228115035E-16, 3.267716535433071279, -1.574803149606293529 ) ) ;
#10852=VERTEX_POINT ( 'NONE', #11996 ) ;
#10853=LINE ( 'NONE', #42600, #33659 ) ;
#10854=ORIENTED_EDGE ( 'NONE', *, *, #27350, .T. ) ;
#10856=CARTESIAN_POINT ( 'NONE',  ( -1.985260859929297572, 0.000000000000000000, 0.6299212598425164567 ) ) ;
#10857=DIRECTION ( 'NONE',  ( -1.000000000000000000, 0.000000000000000000, -0.000000000000000000 ) ) ;
#10859=VERTEX_POINT ( 'NONE', #32396 ) ;
#10860=AXIS2_PLACEMENT_3D ( 'NONE', #8641, #1148, #24133 ) ;
#10861=DIRECTION ( 'NONE',  ( 1.000000000000000000, -0.000000000000000000, 0.000000000000000000 ) ) ;
#10866=CIRCLE ( 'NONE', #19909, 2.106299212598425008 ) ;
#10867=DIRECTION ( 'NONE',  ( -0.000000000000000000, 1.000000000000000000, -0.000000000000000000 ) ) ;
#10868=CARTESIAN_POINT ( 'NONE',  ( 1.091055626815043311, 3.346456692913386100, 1.692913385826762873 ) ) ;
#10869=EDGE_CURVE ( 'NONE', #11499, #12204, #24643, .T. ) ;
#10870=VECTOR ( 'NONE', #32643, 39.37007874015748143 ) ;
#10873=DIRECTION ( 'NONE',  ( 1.734723475976806848E-16, 0.000000000000000000, 1.000000000000000000 ) ) ;
#10874=ADVANCED_FACE ( 'NONE', ( #24383 ), #27479, .F. ) ;
#10876=ADVANCED_FACE ( 'NONE', ( #28242 ), #43728, .F. ) ;
#10877=VERTEX_POINT ( 'NONE', #36519 ) ;
#10878=DIRECTION ( 'NONE',  ( 0.000000000000000000, -1.000000000000000000, 0.000000000000000000 ) ) ;
#10879=VERTEX_POINT ( 'NONE', #39364 ) ;
#10880=ORIENTED_EDGE ( 'NONE', *, *, #7042, .F. ) ;
#10884=DIRECTION ( 'NONE',  ( -0.000000000000000000, 1.000000000000000000, -0.000000000000000000 ) ) ;
#10886=LINE ( 'NONE', #43379, #47743 ) ;
#10887=ORIENTED_EDGE ( 'NONE', *, *, #41135, .T. ) ;
#10888=VERTEX_POINT ( 'NONE', #44250 ) ;
#10889=FACE_OUTER_BOUND ( 'NONE', #40006, .T. ) ;
#10892=CARTESIAN_POINT ( 'NONE',  ( -1.363819533518803473, 3.267716535433071279, 2.365849761790805980E-16 ) ) ;
#10893=LINE ( 'NONE', #15276, #36669 ) ;
#10894=VECTOR ( 'NONE', #28713, 39.37007874015748143 ) ;
#10896=FACE_OUTER_BOUND ( 'NONE', #43016, .T. ) ;
#10898=VECTOR ( 'NONE', #6561, 39.37007874015748143 ) ;
#10899=DIRECTION ( 'NONE',  ( 0.000000000000000000, 0.000000000000000000, -1.000000000000000000 ) ) ;
#10900=ORIENTED_EDGE ( 'NONE', *, *, #33293, .F. ) ;
#10901=CARTESIAN_POINT ( 'NONE',  ( 0.000000000000000000, 3.346456692913386100, -2.165354330708661568 ) ) ;
#10902=CARTESIAN_POINT ( 'NONE',  ( 1.636583440222563635, 3.267716535433071279, -1.259842519685035800 ) ) ;
#10903=VECTOR ( 'NONE', #47088, 39.37007874015748143 ) ;
#10906=EDGE_CURVE ( 'NONE', #19583, #11836, #40139, .T. ) ;
#10907=ORIENTED_EDGE ( 'NONE', *, *, #22411, .T. ) ;
#10908=VECTOR ( 'NONE', #8442, 39.37007874015748143 ) ;
#10911=CARTESIAN_POINT ( 'NONE',  ( 0.000000000000000000, 3.267716535433071279, 0.000000000000000000 ) ) ;
#10912=ORIENTED_EDGE ( 'NONE', *, *, #11911, .F. ) ;
#10913=EDGE_CURVE ( 'NONE', #47308, #46754, #4001, .T. ) ;
#10915=EDGE_CURVE ( 'NONE', #8923, #25574, #8124, .T. ) ;
#10918=ORIENTED_EDGE ( 'NONE', *, *, #45843, .F. ) ;
#10919=FACE_OUTER_BOUND ( 'NONE', #19552, .T. ) ;
#10920=ORIENTED_EDGE ( 'NONE', *, *, #47434, .F. ) ;
#10924=CARTESIAN_POINT ( 'NONE',  ( -1.363819533518803473, 3.346456692913386100, -1.929133858267710000 ) ) ;
#10927=VERTEX_POINT ( 'NONE', #39620 ) ;
#10930=EDGE_LOOP ( 'NONE', ( #47146, #17646, #2488, #23129 ) ) ;
#10931=CARTESIAN_POINT ( 'NONE',  ( 0.8182917201112819283, 3.267716535433071279, -0.9842519685039348154 ) ) ;
#10932=DIRECTION ( 'NONE',  ( -3.469446951953613696E-16, 0.000000000000000000, -1.000000000000000000 ) ) ;
#10934=EDGE_CURVE ( 'NONE', #13877, #47112, #32657, .T. ) ;
#10935=EDGE_LOOP ( 'NONE', ( #23057, #36298, #2737, #45953 ) ) ;
#10939=LINE ( 'NONE', #6571, #15902 ) ;
#10940=PLANE ( 'NONE',  #16498 ) ;
#10941=ADVANCED_FACE ( 'NONE', ( #43222 ), #7868, .F. ) ;
#10943=DIRECTION ( 'NONE',  ( -3.469446951953613696E-16, 0.000000000000000000, -1.000000000000000000 ) ) ;
#10944=VECTOR ( 'NONE', #37110, 39.37007874015748143 ) ;
#10946=VERTEX_POINT ( 'NONE', #12770 ) ;
#10947=DIRECTION ( 'NONE',  ( -1.000000000000000000, 0.000000000000000000, -0.000000000000000000 ) ) ;
#10948=EDGE_LOOP ( 'NONE', ( #40425, #44746, #21812, #18456 ) ) ;
#10949=AXIS2_PLACEMENT_3D ( 'NONE', #48218, #8758, #32008 ) ;
#10950=EDGE_LOOP ( 'NONE', ( #26174, #5853, #27893, #13086 ) ) ;
#10951=DIRECTION ( 'NONE',  ( 1.734723475976806848E-16, -0.000000000000000000, 1.000000000000000000 ) ) ;
#10952=LINE ( 'NONE', #31334, #30840 ) ;
#10954=VECTOR ( 'NONE', #22212, 39.37007874015748143 ) ;
#10955=DIRECTION ( 'NONE',  ( -3.469446951953613696E-16, 0.000000000000000000, -1.000000000000000000 ) ) ;
#10958=ORIENTED_EDGE ( 'NONE', *, *, #1216, .F. ) ;
#10962=EDGE_CURVE ( 'NONE', #24780, #46834, #9480, .T. ) ;
#10964=CARTESIAN_POINT ( 'NONE',  ( 0.2727639067037604947, 0.000000000000000000, 0.7874015748031454320 ) ) ;
#10965=DIRECTION ( 'NONE',  ( 0.000000000000000000, 0.000000000000000000, -1.000000000000000000 ) ) ;
#10966=ORIENTED_EDGE ( 'NONE', *, *, #35654, .F. ) ;
#10967=CARTESIAN_POINT ( 'NONE',  ( -0.2727639067037602172, 3.267716535433071279, 1.417322834645662777 ) ) ;
#10968=CARTESIAN_POINT ( 'NONE',  ( 0.000000000000000000, 3.267716535433071279, 0.9448818897637749625 ) ) ;
#10969=ADVANCED_FACE ( 'NONE', ( #114 ), #35745, .F. ) ;
#10970=ORIENTED_EDGE ( 'NONE', *, *, #10327, .F. ) ;
#10971=DIRECTION ( 'NONE',  ( 1.000000000000000000, 0.000000000000000000, -3.469446951953613696E-16 ) ) ;
#10972=ADVANCED_FACE ( 'NONE', ( #39876 ), #376, .F. ) ;
#10973=DIRECTION ( 'NONE',  ( -1.000000000000000000, -0.000000000000000000, -0.000000000000000000 ) ) ;
#10976=LINE ( 'NONE', #7108, #33382 ) ;
#10978=ADVANCED_FACE ( 'NONE', ( #12251 ), #1397, .F. ) ;
#10979=LINE ( 'NONE', #18478, #468 ) ;
#10980=AXIS2_PLACEMENT_3D ( 'NONE', #6051, #21297, #48617 ) ;
#10982=CARTESIAN_POINT ( 'NONE',  ( 2.182111253630085290, 0.000000000000000000, -0.3149606299212596716 ) ) ;
#10983=ORIENTED_EDGE ( 'NONE', *, *, #19813, .T. ) ;
#10984=FACE_BOUND ( 'NONE', #22744, .T. ) ;
#10987=FACE_OUTER_BOUND ( 'NONE', #40011, .T. ) ;
#10988=EDGE_CURVE ( 'NONE', #7160, #47130, #37290, .T. ) ;
#10990=ORIENTED_EDGE ( 'NONE', *, *, #30882, .F. ) ;
#10991=ORIENTED_EDGE ( 'NONE', *, *, #5994, .F. ) ;
#10995=CARTESIAN_POINT ( 'NONE',  ( 1.833433833923351353, 0.000000000000000000, 0.9448818897637746295 ) ) ;
#10996=FACE_OUTER_BOUND ( 'NONE', #33314, .T. ) ;
#10998=PLANE ( 'NONE',  #49132 ) ;
#11001=ORIENTED_EDGE ( 'NONE', *, *, #13430, .T. ) ;
#11002=LINE ( 'NONE', #26739, #26270 ) ;
#11004=EDGE_CURVE ( 'NONE', #47658, #15712, #33424, .T. ) ;
#11005=CARTESIAN_POINT ( 'NONE',  ( -2.032045338671488288, 3.267716535433071279, 0.7480314960629874665 ) ) ;
#11006=ORIENTED_EDGE ( 'NONE', *, *, #4353, .T. ) ;
#11007=EDGE_CURVE ( 'NONE', #16948, #46637, #33677, .T. ) ;
#11008=LINE ( 'NONE', #22128, #961 ) ;
#11009=ORIENTED_EDGE ( 'NONE', *, *, #668, .T. ) ;
#11010=ORIENTED_EDGE ( 'NONE', *, *, #1071, .F. ) ;
#11011=ORIENTED_EDGE ( 'NONE', *, *, #27773, .T. ) ;
#11013=CARTESIAN_POINT ( 'NONE',  ( -0.3486774197067340486, 0.000000000000000000, -1.456692913385822630 ) ) ;
#11014=VECTOR ( 'NONE', #34124, 39.37007874015748143 ) ;
#11016=DIRECTION ( 'NONE',  ( -3.469446951953613696E-16, 0.000000000000000000, -1.000000000000000000 ) ) ;
#11018=VECTOR ( 'NONE', #6955, 39.37007874015748143 ) ;
#11022=PLANE ( 'NONE',  #46769 ) ;
#11023=AXIS2_PLACEMENT_3D ( 'NONE', #47812, #16370, #28224 ) ;
#11024=ORIENTED_EDGE ( 'NONE', *, *, #22284, .F. ) ;
#11027=DIRECTION ( 'NONE',  ( 1.734723475976806848E-16, 0.000000000000000000, 1.000000000000000000 ) ) ;
#11028=DIRECTION ( 'NONE',  ( 1.734723475976806848E-16, -0.000000000000000000, 1.000000000000000000 ) ) ;
#11029=DIRECTION ( 'NONE',  ( -1.000000000000000000, 0.000000000000000000, 0.000000000000000000 ) ) ;
#11030=ORIENTED_EDGE ( 'NONE', *, *, #48812, .F. ) ;
#11032=ADVANCED_FACE ( 'NONE', ( #2163 ), #17661, .F. ) ;
#11033=CARTESIAN_POINT ( 'NONE',  ( 0.1968503937007873017, 3.267716535433071279, -1.259842519685035134 ) ) ;
#11036=DIRECTION ( 'NONE',  ( -0.000000000000000000, 0.000000000000000000, 1.000000000000000000 ) ) ;
#11037=EDGE_CURVE ( 'NONE', #23942, #3832, #40802, .T. ) ;
#11038=ADVANCED_FACE ( 'NONE', ( #29270 ), #41405, .F. ) ;
#11040=VERTEX_POINT ( 'NONE', #6295 ) ;
#11042=EDGE_CURVE ( 'NONE', #28182, #8765, #33165, .T. ) ;
#11043=CARTESIAN_POINT ( 'NONE',  ( -0.5455278134075214336, 0.000000000000000000, -1.141732283464563791 ) ) ;
#11045=LINE ( 'NONE', #43027, #48969 ) ;
#11046=DIRECTION ( 'NONE',  ( -3.469446951953613696E-16, 0.000000000000000000, -1.000000000000000000 ) ) ;
#11048=DIRECTION ( 'NONE',  ( -3.469446951953613696E-16, 0.000000000000000000, -1.000000000000000000 ) ) ;
#11049=AXIS2_PLACEMENT_3D ( 'NONE', #14317, #1682, #13818 ) ;
#11051=ORIENTED_EDGE ( 'NONE', *, *, #4678, .T. ) ;
#11052=VECTOR ( 'NONE', #12295, 39.37007874015748143 ) ;
#11055=LINE ( 'NONE', #6427, #16401 ) ;
#11057=ADVANCED_FACE ( 'NONE', ( #37033 ), #49362, .F. ) ;
#11059=ORIENTED_EDGE ( 'NONE', *, *, #12544, .T. ) ;
#11060=VECTOR ( 'NONE', #33686, 39.37007874015748143 ) ;
#11061=AXIS2_PLACEMENT_3D ( 'NONE', #9834, #44420, #17075 ) ;
#11063=EDGE_CURVE ( 'NONE', #44945, #34145, #14037, .T. ) ;
#11064=DIRECTION ( 'NONE',  ( -1.000000000000000000, 0.000000000000000000, -0.000000000000000000 ) ) ;
#11065=AXIS2_PLACEMENT_3D ( 'NONE', #22721, #26087, #22224 ) ;
#11067=VERTEX_POINT ( 'NONE', #29785 ) ;
#11068=ORIENTED_EDGE ( 'NONE', *, *, #29464, .T. ) ;
#11069=EDGE_CURVE ( 'NONE', #20587, #25223, #37546, .T. ) ;
#11070=CARTESIAN_POINT ( 'NONE',  ( 0.4696143004045476022, 0.000000000000000000, -1.929133858267710000 ) ) ;
#11071=FACE_BOUND ( 'NONE', #42919, .T. ) ;
#11072=EDGE_LOOP ( 'NONE', ( #41210, #21157, #27378, #36076 ) ) ;
#11073=DIRECTION ( 'NONE',  ( 1.734723475976806848E-16, -0.000000000000000000, 1.000000000000000000 ) ) ;
#11074=VERTEX_POINT ( 'NONE', #45501 ) ;
#11075=ORIENTED_EDGE ( 'NONE', *, *, #41032, .T. ) ;
#11076=DIRECTION ( 'NONE',  ( -3.469446951953613696E-16, 0.000000000000000000, -1.000000000000000000 ) ) ;
#11078=ORIENTED_EDGE ( 'NONE', *, *, #46758, .T. ) ;
#11080=VERTEX_POINT ( 'NONE', #25912 ) ;
#11082=CARTESIAN_POINT ( 'NONE',  ( 4.097771990496411591E-16, 3.346456692913386100, 2.106299212598425008 ) ) ;
#11083=CARTESIAN_POINT ( 'NONE',  ( -0.3486774197067339376, 3.267716535433071279, -1.259842519685035134 ) ) ;
#11085=ORIENTED_EDGE ( 'NONE', *, *, #11162, .F. ) ;
#11087=DIRECTION ( 'NONE',  ( 1.734723475976806848E-16, 0.000000000000000000, 1.000000000000000000 ) ) ;
#11088=CARTESIAN_POINT ( 'NONE',  ( 0.000000000000000000, 3.267716535433071279, 0.6299212598425164567 ) ) ;
#11089=AXIS2_PLACEMENT_3D ( 'NONE', #8097, #4991, #32371 ) ;
#11092=DIRECTION ( 'NONE',  ( 0.000000000000000000, 0.000000000000000000, 1.000000000000000000 ) ) ;
#11093=VECTOR ( 'NONE', #30669, 39.37007874015748143 ) ;
#11095=AXIS2_PLACEMENT_3D ( 'NONE', #50224, #26773, #31417 ) ;
#11096=PLANE ( 'NONE',  #32587 ) ;
#11097=DIRECTION ( 'NONE',  ( -1.000000000000000000, -0.000000000000000000, -0.000000000000000000 ) ) ;
#11099=VECTOR ( 'NONE', #7515, 39.37007874015748143 ) ;
#11100=ORIENTED_EDGE ( 'NONE', *, *, #42723, .T. ) ;
#11104=VERTEX_POINT ( 'NONE', #9659 ) ;
#11106=ORIENTED_EDGE ( 'NONE', *, *, #22656, .F. ) ;
#11109=ORIENTED_EDGE ( 'NONE', *, *, #4967, .F. ) ;
#11110=EDGE_CURVE ( 'NONE', #8562, #47259, #40642, .T. ) ;
#11111=ORIENTED_EDGE ( 'NONE', *, *, #43850, .T. ) ;
#11113=VERTEX_POINT ( 'NONE', #41912 ) ;
#11114=CARTESIAN_POINT ( 'NONE',  ( 0.000000000000000000, 3.267716535433071279, -1.102362204724405714 ) ) ;
#11115=DIRECTION ( 'NONE',  ( -0.000000000000000000, 1.000000000000000000, -0.000000000000000000 ) ) ;
#11116=EDGE_CURVE ( 'NONE', #15892, #12933, #34177, .T. ) ;
#11119=AXIS2_PLACEMENT_3D ( 'NONE', #39019, #33898, #38027 ) ;
#11121=ORIENTED_EDGE ( 'NONE', *, *, #29369, .F. ) ;
#11125=LINE ( 'NONE', #6747, #21891 ) ;
#11127=CARTESIAN_POINT ( 'NONE',  ( 1.636583440222563857, 0.000000000000000000, 0.9448818897637746295 ) ) ;
#11128=VECTOR ( 'NONE', #46572, 39.37007874015748143 ) ;
#11130=CARTESIAN_POINT ( 'NONE',  ( 0.2727639067037604392, 0.000000000000000000, 0.2755905511810994302 ) ) ;
#11131=DIRECTION ( 'NONE',  ( -1.000000000000000000, -0.000000000000000000, -0.000000000000000000 ) ) ;
#11132=ORIENTED_EDGE ( 'NONE', *, *, #7138, .T. ) ;
#11135=ORIENTED_EDGE ( 'NONE', *, *, #26951, .T. ) ;
#11138=EDGE_CURVE ( 'NONE', #40564, #45493, #6553, .T. ) ;
#11139=CARTESIAN_POINT ( 'NONE',  ( -0.07591351300297284610, 3.346456692913386100, 0.5905511811023582691 ) ) ;
#11141=DIRECTION ( 'NONE',  ( -3.469446951953613696E-16, 0.000000000000000000, -1.000000000000000000 ) ) ;
#11142=DIRECTION ( 'NONE',  ( -0.000000000000000000, 1.000000000000000000, -0.000000000000000000 ) ) ;
#11143=VERTEX_POINT ( 'NONE', #34426 ) ;
#11146=LINE ( 'NONE', #15525, #12750 ) ;
#11147=VERTEX_POINT ( 'NONE', #26909 ) ;
#11148=LINE ( 'NONE', #10892, #15874 ) ;
#11150=PLANE ( 'NONE',  #15148 ) ;
#11152=PLANE ( 'NONE',  #38598 ) ;
#11155=CARTESIAN_POINT ( 'NONE',  ( -1.166969139818015533, 3.346456692913386100, 0.1574803149606287811 ) ) ;
#11160=CARTESIAN_POINT ( 'NONE',  ( 0.000000000000000000, 3.267716535433071279, 0.000000000000000000 ) ) ;
#11162=EDGE_CURVE ( 'NONE', #44618, #30787, #49609, .T. ) ;
#11163=ORIENTED_EDGE ( 'NONE', *, *, #46725, .T. ) ;
#11164=DIRECTION ( 'NONE',  ( 1.000000000000000000, 0.000000000000000000, -3.469446951953613696E-16 ) ) ;
#11168=VERTEX_POINT ( 'NONE', #22297 ) ;
#11169=ADVANCED_FACE ( 'NONE', ( #38308 ), #11428, .F. ) ;
#11170=LINE ( 'NONE', #34417, #31659 ) ;
#11171=VECTOR ( 'NONE', #1976, 39.37007874015748143 ) ;
#11172=ORIENTED_EDGE ( 'NONE', *, *, #34666, .F. ) ;
#11174=ORIENTED_EDGE ( 'NONE', *, *, #2821, .F. ) ;
#11176=ORIENTED_EDGE ( 'NONE', *, *, #36049, .F. ) ;
#11177=CARTESIAN_POINT ( 'NONE',  ( 0.000000000000000000, 3.267716535433071279, -2.401574803149598480 ) ) ;
#11180=EDGE_CURVE ( 'NONE', #1205, #34792, #15049, .T. ) ;
#11181=ORIENTED_EDGE ( 'NONE', *, *, #42500, .F. ) ;
#11182=ORIENTED_EDGE ( 'NONE', *, *, #4694, .F. ) ;
#11183=ORIENTED_EDGE ( 'NONE', *, *, #49346, .T. ) ;
#11184=CARTESIAN_POINT ( 'NONE',  ( -1.195183497228115035E-16, 3.346456692913386100, -0.3149606299212591165 ) ) ;
#11185=CARTESIAN_POINT ( 'NONE',  ( -0.5455278134075214336, 3.267716535433071279, -8.878505979408855953E-16 ) ) ;
#11186=VERTEX_POINT ( 'NONE', #39042 ) ;
#11187=EDGE_CURVE ( 'NONE', #1604, #24291, #7053, .T. ) ;
#11189=DIRECTION ( 'NONE',  ( 0.000000000000000000, 0.000000000000000000, -1.000000000000000000 ) ) ;
#11194=FACE_OUTER_BOUND ( 'NONE', #29082, .T. ) ;
#11196=DIRECTION ( 'NONE',  ( -0.000000000000000000, 0.000000000000000000, 1.000000000000000000 ) ) ;
#11197=ORIENTED_EDGE ( 'NONE', *, *, #17268, .T. ) ;
#11198=LINE ( 'NONE', #15320, #22441 ) ;
#11199=PLANE ( 'NONE',  #25246 ) ;
#11201=ORIENTED_EDGE ( 'NONE', *, *, #13743, .T. ) ;
#11202=VECTOR ( 'NONE', #40962, 39.37007874015748143 ) ;
#11203=FACE_OUTER_BOUND ( 'NONE', #11598, .T. ) ;
#11204=ORIENTED_EDGE ( 'NONE', *, *, #21271, .F. ) ;
#11206=FACE_OUTER_BOUND ( 'NONE', #3641, .T. ) ;
#11207=DIRECTION ( 'NONE',  ( -0.000000000000000000, 1.000000000000000000, -0.000000000000000000 ) ) ;
#11209=AXIS2_PLACEMENT_3D ( 'NONE', #15627, #15122, #30874 ) ;
#11210=LINE ( 'NONE', #23835, #34638 ) ;
#11211=AXIS2_PLACEMENT_3D ( 'NONE', #25109, #5484, #1352 ) ;
#11213=CARTESIAN_POINT ( 'NONE',  ( 0.2727639067037604947, 3.346456692913386100, 0.1574803149606283648 ) ) ;
#11217=ORIENTED_EDGE ( 'NONE', *, *, #47904, .F. ) ;
#11218=CARTESIAN_POINT ( 'NONE',  ( 1.909347346926324462, 3.346456692913386100, -0.7874015748031473194 ) ) ;
#11219=CARTESIAN_POINT ( 'NONE',  ( -1.091055626815042645, 3.346456692913386100, -1.889763779527552146 ) ) ;
#11221=DIRECTION ( 'NONE',  ( -1.000000000000000000, 0.000000000000000000, 1.734723475976806848E-16 ) ) ;
#11223=ORIENTED_EDGE ( 'NONE', *, *, #25766, .F. ) ;
#11228=DIRECTION ( 'NONE',  ( -3.469446951953613696E-16, 0.000000000000000000, -1.000000000000000000 ) ) ;
#11232=CARTESIAN_POINT ( 'NONE',  ( 0.000000000000000000, 3.267716535433071279, 0.000000000000000000 ) ) ;
#11233=CARTESIAN_POINT ( 'NONE',  ( -1.166969139818015755, 0.000000000000000000, 1.220472440944875281 ) ) ;
#11236=AXIS2_PLACEMENT_3D ( 'NONE', #9837, #10090, #17833 ) ;
#11237=VECTOR ( 'NONE', #28538, 39.37007874015748143 ) ;
#11239=LINE ( 'NONE', #38110, #37054 ) ;
#11241=CARTESIAN_POINT ( 'NONE',  ( 0.000000000000000000, 3.267716535433071279, 0.6299212598425164567 ) ) ;
#11242=CIRCLE ( 'NONE', #14561, 2.874015748031496731 ) ;
#11243=CARTESIAN_POINT ( 'NONE',  ( -0.6214413264104945434, 3.346456692913386100, -0.4724409448818886470 ) ) ;
#11244=PLANE ( 'NONE',  #49853 ) ;
#11245=VECTOR ( 'NONE', #32260, 39.37007874015748143 ) ;
#11248=ORIENTED_EDGE ( 'NONE', *, *, #44134, .T. ) ;
#11251=LINE ( 'NONE', #26979, #24215 ) ;
#11252=CARTESIAN_POINT ( 'NONE',  ( -1.985260859929297572, 0.000000000000000000, -6.146657985744592735E-16 ) ) ;
#11253=PLANE ( 'NONE',  #2191 ) ;
#11257=CARTESIAN_POINT ( 'NONE',  ( 1.091055626815042645, 3.267716535433071279, -0.6299212598425181220 ) ) ;
#11260=ORIENTED_EDGE ( 'NONE', *, *, #21209, .F. ) ;
#11265=EDGE_CURVE ( 'NONE', #9222, #39032, #8056, .T. ) ;
#11267=AXIS2_PLACEMENT_3D ( 'NONE', #2018, #30148, #38163 ) ;
#11269=ORIENTED_EDGE ( 'NONE', *, *, #47305, .F. ) ;
#11270=CARTESIAN_POINT ( 'NONE',  ( -1.439733046521776139, 3.346456692913386100, 0.9448818897637749625 ) ) ;
#11271=VECTOR ( 'NONE', #50273, 39.37007874015748143 ) ;
#11273=DIRECTION ( 'NONE',  ( -3.469446951953613696E-16, 0.000000000000000000, -1.000000000000000000 ) ) ;
#11276=AXIS2_PLACEMENT_3D ( 'NONE', #12027, #39905, #4541 ) ;
#11279=VECTOR ( 'NONE', #45512, 39.37007874015748143 ) ;
#11280=FACE_OUTER_BOUND ( 'NONE', #14703, .T. ) ;
#11283=DIRECTION ( 'NONE',  ( 1.000000000000000000, -0.000000000000000000, 0.000000000000000000 ) ) ;
#11284=CARTESIAN_POINT ( 'NONE',  ( 0.2727639067037604947, 3.346456692913386100, 0.7874015748031454320 ) ) ;
#11285=CARTESIAN_POINT ( 'NONE',  ( 0.2727639067037602172, 0.000000000000000000, -1.732283464566922726 ) ) ;
#11286=CARTESIAN_POINT ( 'NONE',  ( -1.091055626815042201, 0.000000000000000000, 1.574803149606291974 ) ) ;
#11287=EDGE_CURVE ( 'NONE', #4959, #39171, #36200, .T. ) ;
#11290=DIRECTION ( 'NONE',  ( 1.734723475976806848E-16, -0.000000000000000000, 1.000000000000000000 ) ) ;
#11291=EDGE_LOOP ( 'NONE', ( #40473, #28471, #16129, #3350 ) ) ;
#11293=EDGE_CURVE ( 'NONE', #4560, #48286, #39297, .T. ) ;
#11297=ORIENTED_EDGE ( 'NONE', *, *, #7121, .T. ) ;
#11298=DIRECTION ( 'NONE',  ( -0.000000000000000000, 1.000000000000000000, -0.000000000000000000 ) ) ;
#11300=DIRECTION ( 'NONE',  ( -3.469446951953613696E-16, 0.000000000000000000, -1.000000000000000000 ) ) ;
#11301=CARTESIAN_POINT ( 'NONE',  ( 0.000000000000000000, 3.267716535433071279, 1.220472440944875281 ) ) ;
#11303=EDGE_LOOP ( 'NONE', ( #25179, #26304, #26689, #48105 ) ) ;
#11305=AXIS2_PLACEMENT_3D ( 'NONE', #2469, #45543, #6340 ) ;
#11306=ORIENTED_EDGE ( 'NONE', *, *, #564, .T. ) ;
#11311=DIRECTION ( 'NONE',  ( 1.734723475976806848E-16, 0.000000000000000000, 1.000000000000000000 ) ) ;
#11312=ORIENTED_EDGE ( 'NONE', *, *, #33851, .F. ) ;
#11313=DIRECTION ( 'NONE',  ( -1.000000000000000000, 0.000000000000000000, -0.000000000000000000 ) ) ;
#11314=ORIENTED_EDGE ( 'NONE', *, *, #7459, .F. ) ;
#11315=DIRECTION ( 'NONE',  ( -1.000000000000000000, 0.000000000000000000, 0.000000000000000000 ) ) ;
#11317=VERTEX_POINT ( 'NONE', #23804 ) ;
#11318=FACE_OUTER_BOUND ( 'NONE', #24331, .T. ) ;
#11320=VECTOR ( 'NONE', #15904, 39.37007874015748143 ) ;
#11321=DIRECTION ( 'NONE',  ( 1.000000000000000000, 0.000000000000000000, 0.000000000000000000 ) ) ;
#11322=EDGE_CURVE ( 'NONE', #39188, #65, #19914, .T. ) ;
#11323=EDGE_CURVE ( 'NONE', #31195, #48901, #35431, .T. ) ;
#11326=LINE ( 'NONE', #46659, #23267 ) ;
#11328=LINE ( 'NONE', #43310, #8925 ) ;
#11329=ORIENTED_EDGE ( 'NONE', *, *, #48118, .F. ) ;
#11330=CARTESIAN_POINT ( 'NONE',  ( -2.454875160333845674, 3.189042514953126961, -0.3543307086614173040 ) ) ;
#11332=DIRECTION ( 'NONE',  ( 1.000000000000000000, 0.000000000000000000, 0.000000000000000000 ) ) ;
#11333=ADVANCED_FACE ( 'NONE', ( #4698 ), #39551, .F. ) ;
#11334=CARTESIAN_POINT ( 'NONE',  ( -1.091055626815042201, 3.346456692913386100, 0.1181102362204705658 ) ) ;
#11335=AXIS2_PLACEMENT_3D ( 'NONE', #4970, #1089, #41362 ) ;
#11336=VECTOR ( 'NONE', #43143, 39.37007874015748143 ) ;
#11337=CARTESIAN_POINT ( 'NONE',  ( 0.5455278134075211005, 3.267716535433071279, 0.7480314960629872445 ) ) ;
#11338=VERTEX_POINT ( 'NONE', #44182 ) ;
#11339=VERTEX_POINT ( 'NONE', #28178 ) ;
#11340=LINE ( 'NONE', #6961, #1390 ) ;
#11341=DIRECTION ( 'NONE',  ( -0.000000000000000000, 0.000000000000000000, 1.000000000000000000 ) ) ;
#11342=PLANE ( 'NONE',  #25836 ) ;
#11343=ADVANCED_FACE ( 'NONE', ( #47252 ), #46997, .F. ) ;
#11344=PLANE ( 'NONE',  #5407 ) ;
#11345=CARTESIAN_POINT ( 'NONE',  ( 1.015142113812069979, 3.346456692913386100, 1.912654141836395372 ) ) ;
#11348=CARTESIAN_POINT ( 'NONE',  ( -0.2727639067037608278, 3.267716535433071279, -1.299212598425193210 ) ) ;
#11351=DIRECTION ( 'NONE',  ( 1.000000000000000000, 0.000000000000000000, -3.469446951953613696E-16 ) ) ;
#11352=EDGE_CURVE ( 'NONE', #6103, #31288, #20176, .T. ) ;
#11354=EDGE_CURVE ( 'NONE', #5106, #36537, #31304, .T. ) ;
#11355=VERTEX_POINT ( 'NONE', #48787 ) ;
#11356=VERTEX_POINT ( 'NONE', #40835 ) ;
#11358=CARTESIAN_POINT ( 'NONE',  ( -0.2727639067037607723, 3.346456692913386100, -0.1574803149606301411 ) ) ;
#11359=VERTEX_POINT ( 'NONE', #10102 ) ;
#11362=DIRECTION ( 'NONE',  ( -0.000000000000000000, 0.000000000000000000, 1.000000000000000000 ) ) ;
#11363=EDGE_LOOP ( 'NONE', ( #49647, #42908, #8834, #46019 ) ) ;
#11364=CARTESIAN_POINT ( 'NONE',  ( 0.5455278134075211005, 3.346456692913386100, 0.7480314960629872445 ) ) ;
#11366=VECTOR ( 'NONE', #8888, 39.37007874015748143 ) ;
#11367=VECTOR ( 'NONE', #49476, 39.37007874015748143 ) ;
#11368=VERTEX_POINT ( 'NONE', #25335 ) ;
#11369=DIRECTION ( 'NONE',  ( -0.000000000000000000, 0.000000000000000000, 1.000000000000000000 ) ) ;
#11373=LINE ( 'NONE', #42106, #7513 ) ;
#11374=DIRECTION ( 'NONE',  ( -1.000000000000000000, -0.000000000000000000, -0.000000000000000000 ) ) ;
#11376=EDGE_LOOP ( 'NONE', ( #2157, #46433, #1483, #11963 ) ) ;
#11378=CARTESIAN_POINT ( 'NONE',  ( 3.519654186525858491E-16, 3.346456692913386100, 2.874015748031496731 ) ) ;
#11381=VECTOR ( 'NONE', #7455, 39.37007874015748143 ) ;
#11382=LINE ( 'NONE', #26619, #41382 ) ;
#11383=EDGE_CURVE ( 'NONE', #44874, #31800, #44683, .T. ) ;
#11384=EDGE_CURVE ( 'NONE', #23553, #25851, #9335, .T. ) ;
#11386=ORIENTED_EDGE ( 'NONE', *, *, #21888, .F. ) ;
#11388=AXIS2_PLACEMENT_3D ( 'NONE', #34904, #26642, #43134 ) ;
#11389=ADVANCED_FACE ( 'NONE', ( #21214 ), #37223, .F. ) ;
#11390=VERTEX_POINT ( 'NONE', #36970 ) ;
#11392=LINE ( 'NONE', #42371, #2733 ) ;
#11393=LINE ( 'NONE', #23508, #50788 ) ;
#11394=CARTESIAN_POINT ( 'NONE',  ( 1.287906020515830141, 0.000000000000000000, 0.9448818897637746295 ) ) ;
#11396=ORIENTED_EDGE ( 'NONE', *, *, #35593, .F. ) ;
#11398=CARTESIAN_POINT ( 'NONE',  ( -0.3486774197067334380, 0.000000000000000000, 0.6299212598425164567 ) ) ;
#11400=DIRECTION ( 'NONE',  ( 1.000000000000000000, 0.000000000000000000, 0.000000000000000000 ) ) ;
#11401=FACE_OUTER_BOUND ( 'NONE', #6382, .T. ) ;
#11402=ADVANCED_FACE ( 'NONE', ( #25589 ), #33356, .F. ) ;
#11404=LINE ( 'NONE', #20154, #28366 ) ;
#11405=CARTESIAN_POINT ( 'NONE',  ( 0.8182917201112824834, 3.267716535433071279, 1.535433070866133898 ) ) ;
#11406=FACE_OUTER_BOUND ( 'NONE', #15183, .T. ) ;
#11412=EDGE_CURVE ( 'NONE', #50705, #45906, #9851, .T. ) ;
#11416=AXIS2_PLACEMENT_3D ( 'NONE', #25785, #22176, #46143 ) ;
#11417=CARTESIAN_POINT ( 'NONE',  ( -0.07591351300297284610, 3.267716535433071279, 0.5905511811023582691 ) ) ;
#11418=DIRECTION ( 'NONE',  ( 1.734723475976806848E-16, -0.000000000000000000, 1.000000000000000000 ) ) ;
#11420=VERTEX_POINT ( 'NONE', #48533 ) ;
#11422=ORIENTED_EDGE ( 'NONE', *, *, #5161, .F. ) ;
#11423=LINE ( 'NONE', #42897, #41096 ) ;
#11424=VERTEX_POINT ( 'NONE', #49040 ) ;
#11425=AXIS2_PLACEMENT_3D ( 'NONE', #32715, #26464, #49415 ) ;
#11428=PLANE ( 'NONE',  #18581 ) ;
#11430=VECTOR ( 'NONE', #9760, 39.37007874015748143 ) ;
#11431=CARTESIAN_POINT ( 'NONE',  ( -0.07591351300297333182, 3.346456692913386100, -1.102362204724405714 ) ) ;
#11432=ORIENTED_EDGE ( 'NONE', *, *, #49234, .T. ) ;
#11433=VERTEX_POINT ( 'NONE', #13216 ) ;
#11434=ORIENTED_EDGE ( 'NONE', *, *, #50211, .F. ) ;
#11435=DIRECTION ( 'NONE',  ( 1.000000000000000000, 0.000000000000000000, 0.000000000000000000 ) ) ;
#11437=ORIENTED_EDGE ( 'NONE', *, *, #48016, .T. ) ;
#11438=ORIENTED_EDGE ( 'NONE', *, *, #45234, .F. ) ;
#11440=FACE_OUTER_BOUND ( 'NONE', #12657, .T. ) ;
#11441=DIRECTION ( 'NONE',  ( 1.734723475976806848E-16, 0.000000000000000000, 1.000000000000000000 ) ) ;
#11442=ORIENTED_EDGE ( 'NONE', *, *, #28707, .F. ) ;
#11444=CARTESIAN_POINT ( 'NONE',  ( 0.7423782071083085965, 3.267716535433071279, -1.456692913385822630 ) ) ;
#11447=LINE ( 'NONE', #27183, #9687 ) ;
#11448=EDGE_LOOP ( 'NONE', ( #19058, #3748, #12242, #27453 ) ) ;
#11449=DIRECTION ( 'NONE',  ( -0.000000000000000000, 1.000000000000000000, -0.000000000000000000 ) ) ;
#11452=EDGE_CURVE ( 'NONE', #795, #2123, #4950, .T. ) ;
#11453=LINE ( 'NONE', #39325, #6823 ) ;
#11454=EDGE_LOOP ( 'NONE', ( #29971, #23237, #30711, #22689 ) ) ;
#11456=CARTESIAN_POINT ( 'NONE',  ( 0.000000000000000000, 3.267716535433071279, 1.732283464566920950 ) ) ;
#11457=LINE ( 'NONE', #30831, #39046 ) ;
#11459=CIRCLE ( 'NONE', #49337, 2.106299212598425008 ) ;
#11461=EDGE_CURVE ( 'NONE', #30195, #27463, #37482, .T. ) ;
#11462=CARTESIAN_POINT ( 'NONE',  ( 0.7423782071083082634, 0.000000000000000000, -1.771653543307081025 ) ) ;
#11463=ADVANCED_FACE ( 'NONE', ( #5204 ), #36456, .F. ) ;
#11465=CARTESIAN_POINT ( 'NONE',  ( 0.8182917201112824834, 0.000000000000000000, 1.417322834645662777 ) ) ;
#11466=ORIENTED_EDGE ( 'NONE', *, *, #22284, .T. ) ;
#11469=ORIENTED_EDGE ( 'NONE', *, *, #33103, .F. ) ;
#11471=DIRECTION ( 'NONE',  ( 1.000000000000000000, -0.000000000000000000, 0.000000000000000000 ) ) ;
#11474=CARTESIAN_POINT ( 'NONE',  ( 0.000000000000000000, 3.267716535433071279, -2.047244094488182231 ) ) ;
#11475=LINE ( 'NONE', #35222, #13022 ) ;
#11476=ORIENTED_EDGE ( 'NONE', *, *, #24113, .F. ) ;
#11477=DIRECTION ( 'NONE',  ( -0.000000000000000000, 1.000000000000000000, -0.000000000000000000 ) ) ;
#11478=ADVANCED_FACE ( 'NONE', ( #13727 ), #25846, .F. ) ;
#11479=CARTESIAN_POINT ( 'NONE',  ( -1.166969139818016199, 3.267716535433071279, -0.9842519685039344823 ) ) ;
#11480=ORIENTED_EDGE ( 'NONE', *, *, #43960, .F. ) ;
#11481=CARTESIAN_POINT ( 'NONE',  ( 1.015142113812069979, 3.346456692913386100, 1.220472440944875281 ) ) ;
#11482=CARTESIAN_POINT ( 'NONE',  ( 0.000000000000000000, 3.267716535433071279, -0.1574803149606304187 ) ) ;
#11486=CARTESIAN_POINT ( 'NONE',  ( 0.000000000000000000, 3.267716535433071279, -2.204724409448811429 ) ) ;
#11487=PLANE ( 'NONE',  #26671 ) ;
#11488=CARTESIAN_POINT ( 'NONE',  ( -0.5455278134075208785, 3.346456692913386100, 1.889763779527550369 ) ) ;
#11489=EDGE_LOOP ( 'NONE', ( #47299, #49264, #21843, #18435 ) ) ;
#11491=VERTEX_POINT ( 'NONE', #48280 ) ;
#11494=VECTOR ( 'NONE', #26445, 39.37007874015748143 ) ;
#11495=LINE ( 'NONE', #50420, #50645 ) ;
#11496=CARTESIAN_POINT ( 'NONE',  ( -1.909347346926324906, 0.000000000000000000, -1.102362204724405492 ) ) ;
#11498=VERTEX_POINT ( 'NONE', #40580 ) ;
#11499=VERTEX_POINT ( 'NONE', #30988 ) ;
#11500=LINE ( 'NONE', #42972, #19906 ) ;
#11501=LINE ( 'NONE', #39116, #27092 ) ;
#11502=CARTESIAN_POINT ( 'NONE',  ( 0.000000000000000000, 3.267716535433071279, -0.8267716535433055070 ) ) ;
#11504=VECTOR ( 'NONE', #23873, 39.37007874015748143 ) ;
#11508=CARTESIAN_POINT ( 'NONE',  ( -1.363819533518803029, 3.267716535433071279, 0.1574803149606287811 ) ) ;
#11509=LINE ( 'NONE', #26487, #18348 ) ;
#11510=LINE ( 'NONE', #15386, #42979 ) ;
#11511=ORIENTED_EDGE ( 'NONE', *, *, #18126, .F. ) ;
#11514=ORIENTED_EDGE ( 'NONE', *, *, #46224, .F. ) ;
#11515=CARTESIAN_POINT ( 'NONE',  ( -2.454875160333845674, 3.242921367653845977, -0.03937007874015881204 ) ) ;
#11516=EDGE_CURVE ( 'NONE', #31565, #28182, #49545, .T. ) ;
#11518=VERTEX_POINT ( 'NONE', #18613 ) ;
#11524=CARTESIAN_POINT ( 'NONE',  ( 0.4696143004045479352, 0.000000000000000000, -1.102362204724405714 ) ) ;
#11527=CARTESIAN_POINT ( 'NONE',  ( 0.1968503937007878568, 0.000000000000000000, 2.204724409448808764 ) ) ;
#11529=DIRECTION ( 'NONE',  ( 1.000000000000000000, 0.000000000000000000, -3.469446951953613696E-16 ) ) ;
#11530=ORIENTED_EDGE ( 'NONE', *, *, #48432, .F. ) ;
#11531=CARTESIAN_POINT ( 'NONE',  ( -0.3486774197067339376, 3.346456692913386100, -0.9448818897637762948 ) ) ;
#11532=CARTESIAN_POINT ( 'NONE',  ( 0.4696143004045479352, 3.346456692913386100, -1.417322834645664331 ) ) ;
#11533=VECTOR ( 'NONE', #40581, 39.37007874015748143 ) ;
#11538=CARTESIAN_POINT ( 'NONE',  ( 1.363819533518803251, 3.346456692913386100, 0.1574803149606283648 ) ) ;
#11540=LINE ( 'NONE', #43529, #20492 ) ;
#11541=EDGE_CURVE ( 'NONE', #36491, #42385, #22236, .T. ) ;
#11545=LINE ( 'NONE', #27281, #35522 ) ;
#11546=EDGE_CURVE ( 'NONE', #4710, #43170, #38740, .T. ) ;
#11547=CARTESIAN_POINT ( 'NONE',  ( 0.000000000000000000, 3.267716535433071279, 1.259842519685033357 ) ) ;
#11549=FACE_OUTER_BOUND ( 'NONE', #17347, .T. ) ;
#11550=CARTESIAN_POINT ( 'NONE',  ( -1.363819533518803473, 3.346456692913386100, -0.9842519685039344823 ) ) ;
#11551=ORIENTED_EDGE ( 'NONE', *, *, #27710, .F. ) ;
#11553=VERTEX_POINT ( 'NONE', #50296 ) ;
#11554=ORIENTED_EDGE ( 'NONE', *, *, #43894, .T. ) ;
#11555=CARTESIAN_POINT ( 'NONE',  ( 0.7423782071083084855, 3.267716535433071279, -2.575641807848709208E-16 ) ) ;
#11556=ORIENTED_EDGE ( 'NONE', *, *, #24712, .F. ) ;
#11557=EDGE_CURVE ( 'NONE', #9319, #2383, #14989, .T. ) ;
#11558=LINE ( 'NONE', #47134, #45224 ) ;
#11560=ORIENTED_EDGE ( 'NONE', *, *, #40974, .T. ) ;
#11561=EDGE_CURVE ( 'NONE', #22568, #47433, #30231, .T. ) ;
#11562=VECTOR ( 'NONE', #27263, 39.37007874015748143 ) ;
#11563=CARTESIAN_POINT ( 'NONE',  ( -3.927031490892378253E-16, 0.000000000000000000, -2.204724409448811429 ) ) ;
#11564=VECTOR ( 'NONE', #47544, 39.37007874015748143 ) ;
#11565=ORIENTED_EDGE ( 'NONE', *, *, #15275, .F. ) ;
#11566=DIRECTION ( 'NONE',  ( 1.734723475976806848E-16, -0.000000000000000000, 1.000000000000000000 ) ) ;
#11567=VERTEX_POINT ( 'NONE', #11364 ) ;
#11571=VECTOR ( 'NONE', #27861, 39.37007874015748143 ) ;
#11574=VERTEX_POINT ( 'NONE', #2862 ) ;
#11575=EDGE_LOOP ( 'NONE', ( #35167, #33777, #21563, #4332 ) ) ;
#11576=ADVANCED_FACE ( 'NONE', ( #46448 ), #30738, .F. ) ;
#11578=CARTESIAN_POINT ( 'NONE',  ( -2.454875160333845674, 3.232777166330581320, -0.1574803149606298636 ) ) ;
#11579=ORIENTED_EDGE ( 'NONE', *, *, #19428, .T. ) ;
#11580=CARTESIAN_POINT ( 'NONE',  ( -0.5455278134075208785, 0.000000000000000000, 1.377952755905504256 ) ) ;
#11581=VERTEX_POINT ( 'NONE', #38243 ) ;
#11582=CARTESIAN_POINT ( 'NONE',  ( 0.8182917201112819283, 3.267716535433071279, -0.1574803149606301411 ) ) ;
#11583=PLANE ( 'NONE',  #31620 ) ;
#11584=CARTESIAN_POINT ( 'NONE',  ( -0.3486774197067337711, 3.267716535433071279, 1.209717811016578338E-16 ) ) ;
#11585=EDGE_CURVE ( 'NONE', #11040, #12778, #29302, .T. ) ;
#11589=LINE ( 'NONE', #27325, #24516 ) ;
#11590=CARTESIAN_POINT ( 'NONE',  ( -1.091055626815042201, 3.267716535433071279, 0.4330708661417290162 ) ) ;
#11592=FACE_OUTER_BOUND ( 'NONE', #7198, .T. ) ;
#11597=LINE ( 'NONE', #489, #36609 ) ;
#11598=EDGE_LOOP ( 'NONE', ( #36240, #50614, #16843, #1901 ) ) ;
#11599=DIRECTION ( 'NONE',  ( -3.469446951953613696E-16, 0.000000000000000000, -1.000000000000000000 ) ) ;
#11601=ORIENTED_EDGE ( 'NONE', *, *, #2556, .T. ) ;
#11603=DIRECTION ( 'NONE',  ( 1.000000000000000000, 0.000000000000000000, -3.469446951953613696E-16 ) ) ;
#11604=CARTESIAN_POINT ( 'NONE',  ( 0.000000000000000000, 3.267716535433071279, 1.732283464566921172 ) ) ;
#11605=EDGE_CURVE ( 'NONE', #14773, #31439, #50052, .T. ) ;
#11606=ORIENTED_EDGE ( 'NONE', *, *, #14541, .F. ) ;
#11607=EDGE_CURVE ( 'NONE', #45259, #45523, #18104, .T. ) ;
#11608=EDGE_CURVE ( 'NONE', #21172, #575, #42345, .T. ) ;
#11611=CARTESIAN_POINT ( 'NONE',  ( 1.909347346926324684, 3.346456692913386100, 0.4724409448818868706 ) ) ;
#11615=EDGE_LOOP ( 'NONE', ( #21883, #12922, #35801, #40905 ) ) ;
#11616=CARTESIAN_POINT ( 'NONE',  ( -2.071704270381554913, 3.346456692913386100, -0.6299212598425177889 ) ) ;
#11617=ORIENTED_EDGE ( 'NONE', *, *, #25727, .T. ) ;
#11618=ORIENTED_EDGE ( 'NONE', *, *, #50865, .T. ) ;
#11620=LINE ( 'NONE', #44889, #8364 ) ;
#11621=DIRECTION ( 'NONE',  ( -1.000000000000000000, -0.000000000000000000, -0.000000000000000000 ) ) ;
#11624=ORIENTED_EDGE ( 'NONE', *, *, #10847, .T. ) ;
#11626=VECTOR ( 'NONE', #13108, 39.37007874015748143 ) ;
#11629=ORIENTED_EDGE ( 'NONE', *, *, #31742, .F. ) ;
#11630=ADVANCED_FACE ( 'NONE', ( #15735 ), #32014, .F. ) ;
#11631=DIRECTION ( 'NONE',  ( -3.469446951953613696E-16, 0.000000000000000000, -1.000000000000000000 ) ) ;
#11633=EDGE_CURVE ( 'NONE', #26232, #17597, #15997, .T. ) ;
#11635=ORIENTED_EDGE ( 'NONE', *, *, #40884, .F. ) ;
#11636=VECTOR ( 'NONE', #49809, 39.37007874015748143 ) ;
#11638=ORIENTED_EDGE ( 'NONE', *, *, #7210, .F. ) ;
#11640=AXIS2_PLACEMENT_3D ( 'NONE', #35289, #160, #44041 ) ;
#11641=CARTESIAN_POINT ( 'NONE',  ( -0.07591351300297333182, 3.346456692913386100, -1.417322834645664331 ) ) ;
#11645=ORIENTED_EDGE ( 'NONE', *, *, #17366, .F. ) ;
#11646=ORIENTED_EDGE ( 'NONE', *, *, #23546, .F. ) ;
#11649=DIRECTION ( 'NONE',  ( 1.000000000000000000, 0.000000000000000000, -3.469446951953613696E-16 ) ) ;
#11650=DIRECTION ( 'NONE',  ( -3.469446951953613696E-16, 0.000000000000000000, -1.000000000000000000 ) ) ;
#11652=CARTESIAN_POINT ( 'NONE',  ( -0.8182917201112814842, 0.000000000000000000, 1.102362204724404160 ) ) ;
#11653=DIRECTION ( 'NONE',  ( -0.000000000000000000, 0.000000000000000000, 1.000000000000000000 ) ) ;
#11659=ORIENTED_EDGE ( 'NONE', *, *, #48452, .F. ) ;
#11662=CARTESIAN_POINT ( 'NONE',  ( -0.8182917201112814842, 0.000000000000000000, 1.732283464566921172 ) ) ;
#11665=ADVANCED_FACE ( 'NONE', ( #509 ), #19602, .F. ) ;
#11668=ADVANCED_FACE ( 'NONE', ( #20114 ), #15493, .F. ) ;
#11669=ORIENTED_EDGE ( 'NONE', *, *, #49095, .F. ) ;
#11674=EDGE_CURVE ( 'NONE', #4283, #7287, #7994, .T. ) ;
#11676=CARTESIAN_POINT ( 'NONE',  ( 1.909347346926324684, 0.000000000000000000, 0.5905511811023582691 ) ) ;
#11677=DIRECTION ( 'NONE',  ( 0.000000000000000000, 0.000000000000000000, -1.000000000000000000 ) ) ;
#11678=CARTESIAN_POINT ( 'NONE',  ( -1.909347346926324906, 0.000000000000000000, -0.7874015748031470974 ) ) ;
#11679=VERTEX_POINT ( 'NONE', #35374 ) ;
#11680=EDGE_LOOP ( 'NONE', ( #42931, #15965, #16547, #1635 ) ) ;
#11682=DIRECTION ( 'NONE',  ( -1.000000000000000000, 0.000000000000000000, -0.000000000000000000 ) ) ;
#11683=CARTESIAN_POINT ( 'NONE',  ( -0.8182917201112819283, 3.267716535433071279, -0.9842519685039342603 ) ) ;
#11684=EDGE_LOOP ( 'NONE', ( #40604, #5551, #7989, #50179 ) ) ;
#11685=ORIENTED_EDGE ( 'NONE', *, *, #32856, .F. ) ;
#11686=DIRECTION ( 'NONE',  ( 0.000000000000000000, 0.000000000000000000, -1.000000000000000000 ) ) ;
#11687=FACE_OUTER_BOUND ( 'NONE', #48421, .T. ) ;
#11690=ORIENTED_EDGE ( 'NONE', *, *, #6457, .F. ) ;
#11694=CARTESIAN_POINT ( 'NONE',  ( -1.363819533518803473, 3.267716535433071279, -1.102362204724405270 ) ) ;
#11695=VERTEX_POINT ( 'NONE', #20382 ) ;
#11696=CARTESIAN_POINT ( 'NONE',  ( -2.182111253630085290, 3.346456692913386100, 0.4330708661417290162 ) ) ;
#11697=DIRECTION ( 'NONE',  ( -1.000000000000000000, 0.000000000000000000, 1.734723475976806848E-16 ) ) ;
#11698=ORIENTED_EDGE ( 'NONE', *, *, #23423, .F. ) ;
#11699=EDGE_CURVE ( 'NONE', #44656, #48838, #39234, .T. ) ;
#11700=DIRECTION ( 'NONE',  ( -1.000000000000000000, -0.000000000000000000, -0.000000000000000000 ) ) ;
#11701=VERTEX_POINT ( 'NONE', #24262 ) ;
#11702=ORIENTED_EDGE ( 'NONE', *, *, #42900, .T. ) ;
#11703=LINE ( 'NONE', #11957, #40278 ) ;
#11705=VECTOR ( 'NONE', #37782, 39.37007874015748143 ) ;
#11707=VECTOR ( 'NONE', #11631, 39.37007874015748143 ) ;
#11708=DIRECTION ( 'NONE',  ( -0.000000000000000000, -1.000000000000000000, -0.000000000000000000 ) ) ;
#11709=DIRECTION ( 'NONE',  ( 1.000000000000000000, 0.000000000000000000, -3.469446951953613696E-16 ) ) ;
#11710=ORIENTED_EDGE ( 'NONE', *, *, #2043, .F. ) ;
#11711=ORIENTED_EDGE ( 'NONE', *, *, #6642, .F. ) ;
#11713=VECTOR ( 'NONE', #42745, 39.37007874015748143 ) ;
#11715=CARTESIAN_POINT ( 'NONE',  ( -1.091055626815042645, 3.267716535433071279, 1.801691980386209258 ) ) ;
#11717=VECTOR ( 'NONE', #31172, 39.37007874015748143 ) ;
#11718=CARTESIAN_POINT ( 'NONE',  ( 0.000000000000000000, 2.344748451760389596, 0.000000000000000000 ) ) ;
#11719=DIRECTION ( 'NONE',  ( 0.000000000000000000, 0.000000000000000000, -1.000000000000000000 ) ) ;
#11720=EDGE_LOOP ( 'NONE', ( #30492, #29158, #36509, #13733 ) ) ;
#11722=PLANE ( 'NONE',  #17464 ) ;
#11723=VERTEX_POINT ( 'NONE', #35877 ) ;
#11726=DIRECTION ( 'NONE',  ( -0.000000000000000000, 1.000000000000000000, -0.000000000000000000 ) ) ;
#11728=CARTESIAN_POINT ( 'NONE',  ( 0.1968503937007878568, 3.346456692913386100, 2.156388021673882438 ) ) ;
#11729=DIRECTION ( 'NONE',  ( -1.000000000000000000, 0.000000000000000000, -0.000000000000000000 ) ) ;
#11730=FACE_OUTER_BOUND ( 'NONE', #1776, .T. ) ;
#11731=EDGE_CURVE ( 'NONE', #38209, #20260, #32271, .T. ) ;
#11732=EDGE_CURVE ( 'NONE', #27199, #17243, #31754, .T. ) ;
#11733=VERTEX_POINT ( 'NONE', #27351 ) ;
#11734=DIRECTION ( 'NONE',  ( -0.000000000000000000, 0.000000000000000000, 1.000000000000000000 ) ) ;
#11735=ORIENTED_EDGE ( 'NONE', *, *, #5648, .T. ) ;
#11737=EDGE_CURVE ( 'NONE', #49343, #27036, #47963, .T. ) ;
#11738=CIRCLE ( 'NONE', #15858, 2.165354330708661568 ) ;
#11739=CARTESIAN_POINT ( 'NONE',  ( 1.909347346926324684, 3.346456692913386100, 0.5905511811023582691 ) ) ;
#11742=CIRCLE ( 'NONE', #9282, 2.106299212598425008 ) ;
#11745=DIRECTION ( 'NONE',  ( 1.734723475976806848E-16, -0.000000000000000000, 1.000000000000000000 ) ) ;
#11748=VECTOR ( 'NONE', #1009, 39.37007874015748143 ) ;
#11749=DIRECTION ( 'NONE',  ( 1.000000000000000000, 0.000000000000000000, -3.469446951953613696E-16 ) ) ;
#11750=LINE ( 'NONE', #50932, #36787 ) ;
#11751=LINE ( 'NONE', #50933, #9587 ) ;
#11752=VECTOR ( 'NONE', #991, 39.37007874015748143 ) ;
#11755=VERTEX_POINT ( 'NONE', #3619 ) ;
#11756=EDGE_CURVE ( 'NONE', #29154, #9083, #25282, .T. ) ;
#11757=ORIENTED_EDGE ( 'NONE', *, *, #46574, .F. ) ;
#11759=DIRECTION ( 'NONE',  ( 1.000000000000000000, 0.000000000000000000, 0.000000000000000000 ) ) ;
#11760=ORIENTED_EDGE ( 'NONE', *, *, #14003, .F. ) ;
#11761=EDGE_CURVE ( 'NONE', #39073, #36917, #1531, .T. ) ;
#11762=CARTESIAN_POINT ( 'NONE',  ( -1.909347346926324462, 3.346456692913386100, 1.021348170950612255 ) ) ;
#11763=ORIENTED_EDGE ( 'NONE', *, *, #45329, .F. ) ;
#11764=ORIENTED_EDGE ( 'NONE', *, *, #18809, .T. ) ;
#11765=CARTESIAN_POINT ( 'NONE',  ( 1.953585199828835828, 3.346456692913386100, 0.7874015748031456541 ) ) ;
#11766=ORIENTED_EDGE ( 'NONE', *, *, #38495, .T. ) ;
#11767=VERTEX_POINT ( 'NONE', #44624 ) ;
#11768=PLANE ( 'NONE',  #49958 ) ;
#11769=ORIENTED_EDGE ( 'NONE', *, *, #42264, .F. ) ;
#11770=CARTESIAN_POINT ( 'NONE',  ( 1.015142113812069091, 0.000000000000000000, -1.732283464566923614 ) ) ;
#11773=CARTESIAN_POINT ( 'NONE',  ( 0.7423782071083082634, 3.346456692913386100, -2.086614173228340086 ) ) ;
#11775=VECTOR ( 'NONE', #30058, 39.37007874015748143 ) ;
#11776=DIRECTION ( 'NONE',  ( 1.734723475976806848E-16, -0.000000000000000000, 1.000000000000000000 ) ) ;
#11777=DIRECTION ( 'NONE',  ( -1.000000000000000000, 0.000000000000000000, 1.734723475976806848E-16 ) ) ;
#11778=ORIENTED_EDGE ( 'NONE', *, *, #13043, .F. ) ;
#11779=DIRECTION ( 'NONE',  ( 1.734723475976806848E-16, -0.000000000000000000, 1.000000000000000000 ) ) ;
#11780=CARTESIAN_POINT ( 'NONE',  ( -1.091055626815042645, 3.267716535433071279, -0.6299212598425177889 ) ) ;
#11782=VECTOR ( 'NONE', #22206, 39.37007874015748143 ) ;
#11784=ORIENTED_EDGE ( 'NONE', *, *, #24264, .T. ) ;
#11785=CARTESIAN_POINT ( 'NONE',  ( -0.8942052331142552601, 3.267716535433071279, 1.889763779527550147 ) ) ;
#11787=EDGE_LOOP ( 'NONE', ( #49054, #9261, #5360 ) ) ;
#11792=CARTESIAN_POINT ( 'NONE',  ( 1.091055626815042645, 3.267716535433071279, -0.8267716535433055070 ) ) ;
#11794=DIRECTION ( 'NONE',  ( -1.000000000000000000, 0.000000000000000000, 1.734723475976806848E-16 ) ) ;
#11795=ADVANCED_FACE ( 'NONE', ( #28377 ), #28891, .F. ) ;
#11796=LINE ( 'NONE', #42534, #25871 ) ;
#11797=CARTESIAN_POINT ( 'NONE',  ( 2.106197740627111514, 3.201134874551266218, -1.299212598425194320 ) ) ;
#11798=PLANE ( 'NONE',  #5353 ) ;
#11799=EDGE_CURVE ( 'NONE', #27409, #329, #16777, .T. ) ;
#11800=ORIENTED_EDGE ( 'NONE', *, *, #15285, .T. ) ;
#11801=EDGE_CURVE ( 'NONE', #3259, #13403, #25025, .T. ) ;
#11802=ORIENTED_EDGE ( 'NONE', *, *, #3588, .F. ) ;
#11803=ORIENTED_EDGE ( 'NONE', *, *, #16002, .F. ) ;
#11805=ORIENTED_EDGE ( 'NONE', *, *, #20608, .T. ) ;
#11806=LINE ( 'NONE', #47395, #31212 ) ;
#11808=ORIENTED_EDGE ( 'NONE', *, *, #14954, .F. ) ;
#11809=CARTESIAN_POINT ( 'NONE',  ( 1.091055626815042645, 0.000000000000000000, 0.1181102362204704270 ) ) ;
#11810=ORIENTED_EDGE ( 'NONE', *, *, #29204, .T. ) ;
#11811=LINE ( 'NONE', #4083, #10096 ) ;
#11812=VECTOR ( 'NONE', #37181, 39.37007874015748143 ) ;
#11813=LINE ( 'NONE', #31702, #50310 ) ;
#11816=DIRECTION ( 'NONE',  ( -1.000000000000000000, 0.000000000000000000, -0.000000000000000000 ) ) ;
#11817=VECTOR ( 'NONE', #20234, 39.37007874015748143 ) ;
#11818=VERTEX_POINT ( 'NONE', #33299 ) ;
#11819=AXIS2_PLACEMENT_3D ( 'NONE', #43575, #4101, #27829 ) ;
#11820=AXIS2_PLACEMENT_3D ( 'NONE', #49082, #5244, #36752 ) ;
#11821=CARTESIAN_POINT ( 'NONE',  ( 0.000000000000000000, 3.267716535433071279, 1.574803149606291974 ) ) ;
#11822=EDGE_CURVE ( 'NONE', #12892, #41081, #34250, .T. ) ;
#11823=ORIENTED_EDGE ( 'NONE', *, *, #37478, .T. ) ;
#11824=ORIENTED_EDGE ( 'NONE', *, *, #11412, .T. ) ;
#11826=VECTOR ( 'NONE', #21769, 39.37007874015748143 ) ;
#11828=VERTEX_POINT ( 'NONE', #1276 ) ;
#11830=EDGE_CURVE ( 'NONE', #23434, #15077, #36394, .T. ) ;
#11831=ORIENTED_EDGE ( 'NONE', *, *, #48650, .T. ) ;
#11833=CARTESIAN_POINT ( 'NONE',  ( 1.560669927219590525, 3.267716535433071279, -0.03937007874015908959 ) ) ;
#11834=DIRECTION ( 'NONE',  ( 0.000000000000000000, 0.000000000000000000, -1.000000000000000000 ) ) ;
#11835=EDGE_LOOP ( 'NONE', ( #25811, #50938, #8499, #21645 ) ) ;
#11836=VERTEX_POINT ( 'NONE', #6624 ) ;
#11839=CARTESIAN_POINT ( 'NONE',  ( 1.833433833923351353, 3.346456692913386100, -0.9448818897637765168 ) ) ;
#11844=LINE ( 'NONE', #8234, #28426 ) ;
#11845=ORIENTED_EDGE ( 'NONE', *, *, #38896, .T. ) ;
#11846=DIRECTION ( 'NONE',  ( 0.000000000000000000, 0.000000000000000000, 1.000000000000000000 ) ) ;
#11847=VECTOR ( 'NONE', #44779, 39.37007874015748143 ) ;
#11849=DIRECTION ( 'NONE',  ( -3.469446951953613696E-16, 0.000000000000000000, -1.000000000000000000 ) ) ;
#11851=EDGE_LOOP ( 'NONE', ( #26186, #17368, #17472, #27037 ) ) ;
#11852=VECTOR ( 'NONE', #29004, 39.37007874015748143 ) ;
#11853=EDGE_CURVE ( 'NONE', #24076, #28575, #24774, .T. ) ;
#11854=CARTESIAN_POINT ( 'NONE',  ( -0.07591351300297284610, 3.267716535433071279, 1.850393700787392293 ) ) ;
#11855=VECTOR ( 'NONE', #3913, 39.37007874015748143 ) ;
#11856=LINE ( 'NONE', #39224, #36105 ) ;
#11860=VECTOR ( 'NONE', #25321, 39.37007874015748143 ) ;
#11861=CARTESIAN_POINT ( 'NONE',  ( -1.788632549858358844, 3.346456692913386100, 1.220472440944875059 ) ) ;
#11863=ORIENTED_EDGE ( 'NONE', *, *, #47305, .T. ) ;
#11864=DIRECTION ( 'NONE',  ( 0.000000000000000000, 0.000000000000000000, -1.000000000000000000 ) ) ;
#11865=EDGE_LOOP ( 'NONE', ( #10292, #42063, #12346, #28554 ) ) ;
#11867=CARTESIAN_POINT ( 'NONE',  ( 0.000000000000000000, 3.267716535433071279, -1.574803149606293307 ) ) ;
#11868=ORIENTED_EDGE ( 'NONE', *, *, #40634, .T. ) ;
#11870=ORIENTED_EDGE ( 'NONE', *, *, #38433, .F. ) ;
#11871=ORIENTED_EDGE ( 'NONE', *, *, #24355, .T. ) ;
#11872=DIRECTION ( 'NONE',  ( 1.000000000000000000, 0.000000000000000000, -3.469446951953613696E-16 ) ) ;
#11873=PLANE ( 'NONE',  #9996 ) ;
#11875=ORIENTED_EDGE ( 'NONE', *, *, #48721, .T. ) ;
#11876=CARTESIAN_POINT ( 'NONE',  ( -1.593029370565769431, 3.346456692913386100, 1.377952755905504256 ) ) ;
#11878=ADVANCED_FACE ( 'NONE', ( #4894 ), #17036, .F. ) ;
#11879=ORIENTED_EDGE ( 'NONE', *, *, #25507, .T. ) ;
#11880=LINE ( 'NONE', #30755, #11707 ) ;
#11882=VECTOR ( 'NONE', #23258, 39.37007874015748143 ) ;
#11884=AXIS2_PLACEMENT_3D ( 'NONE', #36746, #21246, #20477 ) ;
#11887=ADVANCED_FACE ( 'NONE', ( #29148 ), #48473, .F. ) ;
#11888=VECTOR ( 'NONE', #3805, 39.37007874015748143 ) ;
#11889=EDGE_LOOP ( 'NONE', ( #40690, #659, #13278, #35686 ) ) ;
#11891=AXIS2_PLACEMENT_3D ( 'NONE', #47690, #28096, #1000 ) ;
#11892=DIRECTION ( 'NONE',  ( 1.000000000000000000, -0.000000000000000000, 0.000000000000000000 ) ) ;
#11893=EDGE_CURVE ( 'NONE', #19488, #17373, #2137, .T. ) ;
#11895=PLANE ( 'NONE',  #43432 ) ;
#11896=CARTESIAN_POINT ( 'NONE',  ( 2.182111253630085290, 0.000000000000000000, 0.1181102362204698858 ) ) ;
#11897=ORIENTED_EDGE ( 'NONE', *, *, #42636, .F. ) ;
#11898=ORIENTED_EDGE ( 'NONE', *, *, #37185, .T. ) ;
#11899=VECTOR ( 'NONE', #46930, 39.37007874015748143 ) ;
#11901=CARTESIAN_POINT ( 'NONE',  ( 1.560669927219590303, 3.267716535433071279, -1.614173228346452715 ) ) ;
#11903=DIRECTION ( 'NONE',  ( -3.469446951953613696E-16, 0.000000000000000000, -1.000000000000000000 ) ) ;
#11905=CARTESIAN_POINT ( 'NONE',  ( 1.363819533518803251, 3.346456692913386100, 0.1574803149606283648 ) ) ;
#11906=LINE ( 'NONE', #284, #28540 ) ;
#11908=ORIENTED_EDGE ( 'NONE', *, *, #1841, .F. ) ;
#11911=EDGE_CURVE ( 'NONE', #15133, #50731, #42975, .T. ) ;
#11912=ORIENTED_EDGE ( 'NONE', *, *, #32691, .T. ) ;
#11913=ADVANCED_FACE ( 'NONE', ( #7878 ), #27491, .F. ) ;
#11916=CARTESIAN_POINT ( 'NONE',  ( 0.1968503937007876903, 3.267716535433071279, -6.829619984160666674E-17 ) ) ;
#11917=DIRECTION ( 'NONE',  ( 1.734723475976806848E-16, 0.000000000000000000, 1.000000000000000000 ) ) ;
#11919=ADVANCED_FACE ( 'NONE', ( #39374 ), #7128, .F. ) ;
#11920=EDGE_CURVE ( 'NONE', #50546, #4697, #11750, .T. ) ;
#11921=AXIS2_PLACEMENT_3D ( 'NONE', #50153, #6595, #14588 ) ;
#11923=ORIENTED_EDGE ( 'NONE', *, *, #37893, .F. ) ;
#11924=VECTOR ( 'NONE', #15770, 39.37007874015748143 ) ;
#11927=CARTESIAN_POINT ( 'NONE',  ( 0.000000000000000000, 3.267716535433071279, -1.102362204724405270 ) ) ;
#11928=VECTOR ( 'NONE', #1907, 39.37007874015748143 ) ;
#11929=ORIENTED_EDGE ( 'NONE', *, *, #36020, .T. ) ;
#11930=DIRECTION ( 'NONE',  ( 0.000000000000000000, -1.000000000000000000, 0.000000000000000000 ) ) ;
#11936=VERTEX_POINT ( 'NONE', #38371 ) ;
#11939=CARTESIAN_POINT ( 'NONE',  ( 1.287906020515830585, 0.000000000000000000, 1.574803149606291974 ) ) ;
#11941=ORIENTED_EDGE ( 'NONE', *, *, #30443, .F. ) ;
#11944=DIRECTION ( 'NONE',  ( -1.000000000000000000, 0.000000000000000000, 0.000000000000000000 ) ) ;
#11945=ORIENTED_EDGE ( 'NONE', *, *, #13972, .F. ) ;
#11946=ORIENTED_EDGE ( 'NONE', *, *, #26701, .T. ) ;
#11947=CARTESIAN_POINT ( 'NONE',  ( 0.5455278134075217666, 3.346456692913386100, 1.259842519685033357 ) ) ;
#11949=DIRECTION ( 'NONE',  ( 0.000000000000000000, 0.000000000000000000, -1.000000000000000000 ) ) ;
#11950=VERTEX_POINT ( 'NONE', #30616 ) ;
#11952=DIRECTION ( 'NONE',  ( 1.734723475976806848E-16, -0.000000000000000000, 1.000000000000000000 ) ) ;
#11953=ORIENTED_EDGE ( 'NONE', *, *, #49831, .T. ) ;
#11954=LINE ( 'NONE', #35202, #43055 ) ;
#11955=VERTEX_POINT ( 'NONE', #7629 ) ;
#11957=CARTESIAN_POINT ( 'NONE',  ( -0.6214413264104945434, 3.346456692913386100, 2.047244094488179567 ) ) ;
#11958=LINE ( 'NONE', #39834, #17692 ) ;
#11960=EDGE_CURVE ( 'NONE', #40968, #42434, #50429, .T. ) ;
#11961=FACE_OUTER_BOUND ( 'NONE', #37239, .T. ) ;
#11962=CARTESIAN_POINT ( 'NONE',  ( 1.287906020515830141, 3.346456692913386100, -8.878505979408855953E-16 ) ) ;
#11963=ORIENTED_EDGE ( 'NONE', *, *, #8437, .F. ) ;
#11964=ORIENTED_EDGE ( 'NONE', *, *, #14695, .F. ) ;
#11965=ADVANCED_FACE ( 'NONE', ( #18744 ), #46086, .F. ) ;
#11966=AXIS2_PLACEMENT_3D ( 'NONE', #46675, #42079, #38471 ) ;
#11969=ORIENTED_EDGE ( 'NONE', *, *, #11541, .T. ) ;
#11970=CARTESIAN_POINT ( 'NONE',  ( -1.985260859929298016, 3.346456692913386100, -0.9448818897637762948 ) ) ;
#11971=CARTESIAN_POINT ( 'NONE',  ( -2.156388021673881994, 3.346456692913386100, -0.1968503937007880511 ) ) ;
#11976=VECTOR ( 'NONE', #36012, 39.37007874015748143 ) ;
#11978=DIRECTION ( 'NONE',  ( 1.000000000000000000, 0.000000000000000000, 0.000000000000000000 ) ) ;
#11981=VERTEX_POINT ( 'NONE', #3755 ) ;
#11982=DIRECTION ( 'NONE',  ( -3.469446951953613696E-16, 0.000000000000000000, -1.000000000000000000 ) ) ;
#11983=ADVANCED_FACE ( 'NONE', ( #10996 ), #42227, .F. ) ;
#11987=CARTESIAN_POINT ( 'NONE',  ( -2.182111253630085290, 3.267716535433071279, -0.5118110236220464460 ) ) ;
#11988=CARTESIAN_POINT ( 'NONE',  ( -1.363819533518803473, 3.346456692913386100, -1.605145679676863057 ) ) ;
#11989=EDGE_CURVE ( 'NONE', #23167, #38385, #19742, .T. ) ;
#11990=CARTESIAN_POINT ( 'NONE',  ( -1.909347346926324906, 0.000000000000000000, -1.102362204724405492 ) ) ;
#11991=ADVANCED_FACE ( 'NONE', ( #10742 ), #38622, .F. ) ;
#11993=CARTESIAN_POINT ( 'NONE',  ( 0.5455278134075208785, 0.000000000000000000, -1.771653543307081025 ) ) ;
#11995=FACE_OUTER_BOUND ( 'NONE', #10950, .T. ) ;
#11996=CARTESIAN_POINT ( 'NONE',  ( -1.363819533518803029, 3.346456692913386100, 0.5905511811023582691 ) ) ;
#11997=DIRECTION ( 'NONE',  ( -1.000000000000000000, 0.000000000000000000, -0.000000000000000000 ) ) ;
#11998=CARTESIAN_POINT ( 'NONE',  ( 1.560669927219590747, 3.267716535433071279, 1.102362204724403938 ) ) ;
#12000=ORIENTED_EDGE ( 'NONE', *, *, #47322, .F. ) ;
#12001=DIRECTION ( 'NONE',  ( -3.469446951953613696E-16, 0.000000000000000000, -1.000000000000000000 ) ) ;
#12002=VECTOR ( 'NONE', #29514, 39.37007874015748143 ) ;
#12003=CARTESIAN_POINT ( 'NONE',  ( -1.439733046521777027, 3.346456692913386100, 1.377952755905504256 ) ) ;
#12004=VECTOR ( 'NONE', #17456, 39.37007874015748143 ) ;
#12006=DIRECTION ( 'NONE',  ( -3.469446951953613696E-16, 0.000000000000000000, -1.000000000000000000 ) ) ;
#12009=VECTOR ( 'NONE', #40067, 39.37007874015748143 ) ;
#12010=CARTESIAN_POINT ( 'NONE',  ( 1.015142113812069757, 3.267716535433071279, -3.521981712565033375E-16 ) ) ;
#12011=VERTEX_POINT ( 'NONE', #50185 ) ;
#12012=VERTEX_POINT ( 'NONE', #46335 ) ;
#12013=ORIENTED_EDGE ( 'NONE', *, *, #33141, .F. ) ;
#12015=VECTOR ( 'NONE', #45273, 39.37007874015748143 ) ;
#12016=DIRECTION ( 'NONE',  ( 1.734723475976806848E-16, 0.000000000000000000, 1.000000000000000000 ) ) ;
#12017=LINE ( 'NONE', #38877, #39717 ) ;
#12018=FACE_BOUND ( 'NONE', #10731, .T. ) ;
#12019=VECTOR ( 'NONE', #8569, 39.37007874015748143 ) ;
#12022=ORIENTED_EDGE ( 'NONE', *, *, #2788, .F. ) ;
#12024=CARTESIAN_POINT ( 'NONE',  ( -2.451020605438007482, 3.251186424478681225, -0.03937007874015881204 ) ) ;
#12027=CARTESIAN_POINT ( 'NONE',  ( -0.2727639067037610499, 0.000000000000000000, -2.047244094488181343 ) ) ;
#12028=EDGE_LOOP ( 'NONE', ( #47185, #40918, #24307, #8085 ) ) ;
#12030=ADVANCED_FACE ( 'NONE', ( #38869 ), #31125, .F. ) ;
#12031=CARTESIAN_POINT ( 'NONE',  ( 0.000000000000000000, 3.267716535433071279, 0.4330708661417287386 ) ) ;
#12034=DIRECTION ( 'NONE',  ( 1.000000000000000000, 0.000000000000000000, -3.469446951953613696E-16 ) ) ;
#12035=VECTOR ( 'NONE', #45989, 39.37007874015748143 ) ;
#12036=DIRECTION ( 'NONE',  ( 1.000000000000000000, 0.000000000000000000, -3.469446951953613696E-16 ) ) ;
#12040=ORIENTED_EDGE ( 'NONE', *, *, #13584, .F. ) ;
#12041=FACE_OUTER_BOUND ( 'NONE', #9622, .T. ) ;
#12042=AXIS2_PLACEMENT_3D ( 'NONE', #6391, #29103, #41254 ) ;
#12043=CARTESIAN_POINT ( 'NONE',  ( -0.5455278134075208785, 3.346456692913386100, 1.889763779527550369 ) ) ;
#12044=CARTESIAN_POINT ( 'NONE',  ( 0.000000000000000000, 3.267716535433071279, -1.929133858267711110 ) ) ;
#12045=ORIENTED_EDGE ( 'NONE', *, *, #15254, .T. ) ;
#12046=CARTESIAN_POINT ( 'NONE',  ( 0.000000000000000000, 3.267716535433071279, 1.535433070866133898 ) ) ;
#12047=EDGE_CURVE ( 'NONE', #4899, #14448, #40656, .T. ) ;
#12051=AXIS2_PLACEMENT_3D ( 'NONE', #12891, #36130, #29134 ) ;
#12052=CARTESIAN_POINT ( 'NONE',  ( -0.8182917201112819283, 0.000000000000000000, -0.1574803149606301411 ) ) ;
#12055=ADVANCED_FACE ( 'NONE', ( #12780 ), #40411, .F. ) ;
#12056=CARTESIAN_POINT ( 'NONE',  ( 1.636583440222563857, 0.000000000000000000, 1.062992125984245639 ) ) ;
#12057=ORIENTED_EDGE ( 'NONE', *, *, #21705, .F. ) ;
#12058=DIRECTION ( 'NONE',  ( -0.000000000000000000, 1.000000000000000000, -0.000000000000000000 ) ) ;
#12060=DIRECTION ( 'NONE',  ( -3.469446951953613696E-16, 0.000000000000000000, -1.000000000000000000 ) ) ;
#12061=CARTESIAN_POINT ( 'NONE',  ( -2.182111253630085290, 0.000000000000000000, 0.6299212598425164567 ) ) ;
#12062=ORIENTED_EDGE ( 'NONE', *, *, #40590, .T. ) ;
#12063=ORIENTED_EDGE ( 'NONE', *, *, #50314, .T. ) ;
#12064=VERTEX_POINT ( 'NONE', #28511 ) ;
#12065=CARTESIAN_POINT ( 'NONE',  ( 0.2727639067037604947, 3.346456692913386100, 0.4724409448818868706 ) ) ;
#12066=VERTEX_POINT ( 'NONE', #35756 ) ;
#12067=LINE ( 'NONE', #7684, #24616 ) ;
#12068=DIRECTION ( 'NONE',  ( -1.000000000000000000, 0.000000000000000000, 1.734723475976806848E-16 ) ) ;
#12070=ORIENTED_EDGE ( 'NONE', *, *, #8663, .F. ) ;
#12072=ORIENTED_EDGE ( 'NONE', *, *, #29948, .T. ) ;
#12073=CARTESIAN_POINT ( 'NONE',  ( 1.015142113812069313, 3.267716535433071279, -3.521981712565032882E-16 ) ) ;
#12074=CIRCLE ( 'NONE', #25274, 2.106299212598425008 ) ;
#12076=VECTOR ( 'NONE', #30638, 39.37007874015748143 ) ;
#12077=ORIENTED_EDGE ( 'NONE', *, *, #49769, .F. ) ;
#12079=VECTOR ( 'NONE', #23086, 39.37007874015748143 ) ;
#12080=CARTESIAN_POINT ( 'NONE',  ( 1.287906020515830141, 3.346456692913386100, 0.3149606299212578953 ) ) ;
#12081=ORIENTED_EDGE ( 'NONE', *, *, #32686, .T. ) ;
#12082=VECTOR ( 'NONE', #6806, 39.37007874015748143 ) ;
#12083=DIRECTION ( 'NONE',  ( -3.469446951953613696E-16, 0.000000000000000000, -1.000000000000000000 ) ) ;
#12084=AXIS2_PLACEMENT_3D ( 'NONE', #40172, #4796, #35777 ) ;
#12085=VERTEX_POINT ( 'NONE', #8645 ) ;
#12086=ORIENTED_EDGE ( 'NONE', *, *, #5348, .F. ) ;
#12090=CARTESIAN_POINT ( 'NONE',  ( 1.363819533518803695, 3.346456692913386100, 1.681890501046755748 ) ) ;
#12093=ORIENTED_EDGE ( 'NONE', *, *, #32283, .F. ) ;
#12095=EDGE_CURVE ( 'NONE', #37382, #36994, #5028, .T. ) ;
#12096=LINE ( 'NONE', #39974, #20065 ) ;
#12097=EDGE_CURVE ( 'NONE', #23181, #13035, #124, .T. ) ;
#12098=EDGE_CURVE ( 'NONE', #3114, #15411, #36531, .T. ) ;
#12099=LINE ( 'NONE', #31985, #45336 ) ;
#12103=DIRECTION ( 'NONE',  ( -3.469446951953613696E-16, 0.000000000000000000, -1.000000000000000000 ) ) ;
#12104=LINE ( 'NONE', #43328, #19229 ) ;
#12106=FACE_OUTER_BOUND ( 'NONE', #21149, .T. ) ;
#12107=CARTESIAN_POINT ( 'NONE',  ( 2.378961647330872786, 3.346456692913386100, 0.3149606299212573401 ) ) ;
#12109=ORIENTED_EDGE ( 'NONE', *, *, #24237, .T. ) ;
#12111=DIRECTION ( 'NONE',  ( -3.469446951953613696E-16, 0.000000000000000000, -1.000000000000000000 ) ) ;
#12114=LINE ( 'NONE', #4367, #6129 ) ;
#12115=ADVANCED_FACE ( 'NONE', ( #16910 ), #32670, .F. ) ;
#12117=LINE ( 'NONE', #15484, #28325 ) ;
#12119=CARTESIAN_POINT ( 'NONE',  ( -0.3486774197067342151, 0.000000000000000000, -2.204724409448810540 ) ) ;
#12120=VECTOR ( 'NONE', #14512, 39.37007874015748143 ) ;
#12123=CARTESIAN_POINT ( 'NONE',  ( -0.5455278134075214336, 0.000000000000000000, -1.259842519685035134 ) ) ;
#12125=FACE_OUTER_BOUND ( 'NONE', #33658, .T. ) ;
#12126=EDGE_CURVE ( 'NONE', #11080, #27247, #39886, .T. ) ;
#12127=VERTEX_POINT ( 'NONE', #23883 ) ;
#12128=CARTESIAN_POINT ( 'NONE',  ( 2.182111253630085290, 0.000000000000000000, 0.3149606299212573401 ) ) ;
#12129=DIRECTION ( 'NONE',  ( 1.000000000000000000, -0.000000000000000000, 0.000000000000000000 ) ) ;
#12131=CARTESIAN_POINT ( 'NONE',  ( 1.636583440222563857, 3.346456692913386100, 0.6299212598425164567 ) ) ;
#12134=ADVANCED_FACE ( 'NONE', ( #16656 ), #39629, .F. ) ;
#12135=DIRECTION ( 'NONE',  ( 1.734723475976806848E-16, -0.000000000000000000, 1.000000000000000000 ) ) ;
#12136=LINE ( 'NONE', #27869, #30632 ) ;
#12137=DIRECTION ( 'NONE',  ( -1.000000000000000000, 0.000000000000000000, 1.734723475976806848E-16 ) ) ;
#12138=EDGE_CURVE ( 'NONE', #1443, #17373, #28253, .T. ) ;
#12141=CARTESIAN_POINT ( 'NONE',  ( -0.8942052331142560373, 3.267716535433071279, 3.102397620449225933E-16 ) ) ;
#12142=VECTOR ( 'NONE', #30249, 39.37007874015748143 ) ;
#12145=LINE ( 'NONE', #39510, #18344 ) ;
#12146=ORIENTED_EDGE ( 'NONE', *, *, #23341, .F. ) ;
#12147=ORIENTED_EDGE ( 'NONE', *, *, #15427, .F. ) ;
#12149=DIRECTION ( 'NONE',  ( -3.469446951953613696E-16, 0.000000000000000000, -1.000000000000000000 ) ) ;
#12150=EDGE_CURVE ( 'NONE', #12012, #20408, #900, .T. ) ;
#12151=CARTESIAN_POINT ( 'NONE',  ( 0.000000000000000000, 3.267716535433071279, 0.000000000000000000 ) ) ;
#12152=DIRECTION ( 'NONE',  ( -0.000000000000000000, 1.000000000000000000, -0.000000000000000000 ) ) ;
#12153=ADVANCED_FACE ( 'NONE', ( #6043 ), #37556, .F. ) ;
#12156=EDGE_LOOP ( 'NONE', ( #32934, #45150, #17157, #16343 ) ) ;
#12157=PLANE ( 'NONE',  #40327 ) ;
#12158=CARTESIAN_POINT ( 'NONE',  ( 0.5455278134075214336, 3.267716535433071279, -9.463399047163224412E-17 ) ) ;
#12160=EDGE_LOOP ( 'NONE', ( #49466, #26596, #6573, #4515 ) ) ;
#12163=CARTESIAN_POINT ( 'NONE',  ( -0.3486774197067339376, 3.346456692913386100, -0.3149606299212593941 ) ) ;
#12164=CARTESIAN_POINT ( 'NONE',  ( 1.818390528211208945, 3.346456692913386100, 1.062992125984245639 ) ) ;
#12165=ORIENTED_EDGE ( 'NONE', *, *, #20123, .F. ) ;
#12166=FACE_OUTER_BOUND ( 'NONE', #2814, .T. ) ;
#12168=ORIENTED_EDGE ( 'NONE', *, *, #8273, .F. ) ;
#12169=VERTEX_POINT ( 'NONE', #41417 ) ;
#12170=PLANE ( 'NONE',  #46338 ) ;
#12171=CARTESIAN_POINT ( 'NONE',  ( -0.3486774197067334380, 0.000000000000000000, 1.259842519685033357 ) ) ;
#12175=VECTOR ( 'NONE', #32319, 39.37007874015748143 ) ;
#12176=EDGE_CURVE ( 'NONE', #17328, #26916, #18177, .T. ) ;
#12177=ORIENTED_EDGE ( 'NONE', *, *, #28654, .T. ) ;
#12178=CARTESIAN_POINT ( 'NONE',  ( -0.5455278134075209895, 3.267716535433071279, 9.463399047163218249E-17 ) ) ;
#12179=VECTOR ( 'NONE', #31196, 39.37007874015748143 ) ;
#12180=ORIENTED_EDGE ( 'NONE', *, *, #24652, .T. ) ;
#12182=EDGE_CURVE ( 'NONE', #36547, #5893, #29022, .T. ) ;
#12184=VECTOR ( 'NONE', #17284, 39.37007874015748143 ) ;
#12186=CARTESIAN_POINT ( 'NONE',  ( -1.091055626815042201, 3.346456692913386100, 0.3149606299212580063 ) ) ;
#12187=DIRECTION ( 'NONE',  ( -3.469446951953613696E-16, 0.000000000000000000, -1.000000000000000000 ) ) ;
#12189=EDGE_CURVE ( 'NONE', #31898, #27834, #41173, .T. ) ;
#12190=VECTOR ( 'NONE', #20341, 39.37007874015748143 ) ;
#12191=ORIENTED_EDGE ( 'NONE', *, *, #48460, .T. ) ;
#12192=ORIENTED_EDGE ( 'NONE', *, *, #3396, .F. ) ;
#12193=VERTEX_POINT ( 'NONE', #33687 ) ;
#12195=LINE ( 'NONE', #19416, #1573 ) ;
#12196=EDGE_LOOP ( 'NONE', ( #41789, #2823, #30735, #35585 ) ) ;
#12198=EDGE_CURVE ( 'NONE', #10769, #34717, #25408, .T. ) ;
#12200=DIRECTION ( 'NONE',  ( -0.000000000000000000, 1.000000000000000000, -0.000000000000000000 ) ) ;
#12203=ORIENTED_EDGE ( 'NONE', *, *, #22125, .T. ) ;
#12204=VERTEX_POINT ( 'NONE', #29796 ) ;
#12207=LINE ( 'NONE', #328, #31131 ) ;
#12208=EDGE_LOOP ( 'NONE', ( #4469, #33411, #9150, #12898 ) ) ;
#12209=LINE ( 'NONE', #24597, #38904 ) ;
#12210=FACE_OUTER_BOUND ( 'NONE', #34318, .T. ) ;
#12211=VERTEX_POINT ( 'NONE', #33933 ) ;
#12212=CARTESIAN_POINT ( 'NONE',  ( -1.166969139818015533, 3.346456692913386100, 1.417322834645662777 ) ) ;
#12213=EDGE_LOOP ( 'NONE', ( #45185, #44678, #9, #31961 ) ) ;
#12214=ORIENTED_EDGE ( 'NONE', *, *, #46265, .F. ) ;
#12215=LINE ( 'NONE', #42438, #17179 ) ;
#12216=DIRECTION ( 'NONE',  ( -0.000000000000000000, 1.000000000000000000, -0.000000000000000000 ) ) ;
#12217=EDGE_CURVE ( 'NONE', #19764, #13466, #17413, .T. ) ;
#12218=CARTESIAN_POINT ( 'NONE',  ( -0.3486774197067334380, 3.267716535433071279, 1.259842519685033357 ) ) ;
#12220=LINE ( 'NONE', #3712, #7988 ) ;
#12221=EDGE_CURVE ( 'NONE', #35595, #26317, #17672, .T. ) ;
#12222=DIRECTION ( 'NONE',  ( -1.000000000000000000, 0.000000000000000000, -0.000000000000000000 ) ) ;
#12224=EDGE_LOOP ( 'NONE', ( #13540, #7611, #12971, #37694 ) ) ;
#12226=ORIENTED_EDGE ( 'NONE', *, *, #31613, .F. ) ;
#12227=CARTESIAN_POINT ( 'NONE',  ( -1.863748091109392213, 3.346456692913386100, -1.102362204724405492 ) ) ;
#12229=AXIS2_PLACEMENT_3D ( 'NONE', #48106, #8906, #40663 ) ;
#12230=VECTOR ( 'NONE', #46195, 39.37007874015748143 ) ;
#12234=ORIENTED_EDGE ( 'NONE', *, *, #34303, .F. ) ;
#12235=CARTESIAN_POINT ( 'NONE',  ( 1.287906020515829919, 3.346456692913386100, -2.086614173228339641 ) ) ;
#12236=VECTOR ( 'NONE', #22598, 39.37007874015748143 ) ;
#12238=ORIENTED_EDGE ( 'NONE', *, *, #18847, .T. ) ;
#12240=CARTESIAN_POINT ( 'NONE',  ( -1.195183497228115035E-16, 0.000000000000000000, -0.3149606299212591165 ) ) ;
#12241=CARTESIAN_POINT ( 'NONE',  ( -2.162130742952123263, 3.267716535433071279, 0.1181102362204704270 ) ) ;
#12242=ORIENTED_EDGE ( 'NONE', *, *, #37118, .F. ) ;
#12245=DIRECTION ( 'NONE',  ( -1.000000000000000000, -0.000000000000000000, -0.000000000000000000 ) ) ;
#12246=ORIENTED_EDGE ( 'NONE', *, *, #20394, .F. ) ;
#12247=FACE_OUTER_BOUND ( 'NONE', #25596, .T. ) ;
#12249=EDGE_LOOP ( 'NONE', ( #24818, #22490, #42629, #40012 ) ) ;
#12250=DIRECTION ( 'NONE',  ( -1.000000000000000000, 0.000000000000000000, 1.734723475976806848E-16 ) ) ;
#12251=FACE_OUTER_BOUND ( 'NONE', #29595, .T. ) ;
#12253=DIRECTION ( 'NONE',  ( 0.000000000000000000, 1.000000000000000000, 0.000000000000000000 ) ) ;
#12254=EDGE_CURVE ( 'NONE', #6843, #20840, #1920, .T. ) ;
#12255=VECTOR ( 'NONE', #20519, 39.37007874015748143 ) ;
#12256=EDGE_CURVE ( 'NONE', #27951, #42606, #11242, .T. ) ;
#12257=EDGE_CURVE ( 'NONE', #38943, #41081, #41671, .T. ) ;
#12258=ORIENTED_EDGE ( 'NONE', *, *, #41598, .T. ) ;
#12259=VERTEX_POINT ( 'NONE', #9416 ) ;
#12262=DIRECTION ( 'NONE',  ( 0.000000000000000000, 0.000000000000000000, -1.000000000000000000 ) ) ;
#12263=ORIENTED_EDGE ( 'NONE', *, *, #15016, .T. ) ;
#12266=DIRECTION ( 'NONE',  ( 1.000000000000000000, 0.000000000000000000, 0.000000000000000000 ) ) ;
#12267=FACE_OUTER_BOUND ( 'NONE', #18013, .T. ) ;
#12268=CIRCLE ( 'NONE', #41133, 2.106299212598425008 ) ;
#12269=AXIS2_PLACEMENT_3D ( 'NONE', #22929, #38683, #35060 ) ;
#12271=EDGE_LOOP ( 'NONE', ( #5084, #28437, #36916, #22743 ) ) ;
#12275=DIRECTION ( 'NONE',  ( -1.000000000000000000, 0.000000000000000000, 1.734723475976806848E-16 ) ) ;
#12277=DIRECTION ( 'NONE',  ( -3.469446951953613696E-16, 0.000000000000000000, -1.000000000000000000 ) ) ;
#12278=FACE_BOUND ( 'NONE', #7236, .T. ) ;
#12279=ORIENTED_EDGE ( 'NONE', *, *, #14913, .F. ) ;
#12280=LINE ( 'NONE', #15638, #49593 ) ;
#12281=ORIENTED_EDGE ( 'NONE', *, *, #21643, .F. ) ;
#12282=ORIENTED_EDGE ( 'NONE', *, *, #36420, .F. ) ;
#12283=EDGE_CURVE ( 'NONE', #43980, #25798, #49120, .T. ) ;
#12284=VECTOR ( 'NONE', #46989, 39.37007874015748143 ) ;
#12286=EDGE_CURVE ( 'NONE', #45498, #24717, #1663, .T. ) ;
#12289=CARTESIAN_POINT ( 'NONE',  ( 0.1968503937007878568, 0.000000000000000000, 1.574803149606291974 ) ) ;
#12291=EDGE_LOOP ( 'NONE', ( #33954, #2964, #12165, #33315 ) ) ;
#12292=EDGE_CURVE ( 'NONE', #7345, #35180, #37810, .T. ) ;
#12295=DIRECTION ( 'NONE',  ( -0.000000000000000000, 1.000000000000000000, -0.000000000000000000 ) ) ;
#12297=DIRECTION ( 'NONE',  ( -1.000000000000000000, 0.000000000000000000, 0.000000000000000000 ) ) ;
#12298=DIRECTION ( 'NONE',  ( -0.000000000000000000, 1.000000000000000000, -0.000000000000000000 ) ) ;
#12299=CARTESIAN_POINT ( 'NONE',  ( -1.091055626815042645, 3.267716535433071279, -1.259842519685034690 ) ) ;
#12300=VERTEX_POINT ( 'NONE', #9926 ) ;
#12301=CARTESIAN_POINT ( 'NONE',  ( -1.909347346926324462, 3.267716535433071279, -0.03937007874015881204 ) ) ;
#12302=FACE_OUTER_BOUND ( 'NONE', #37570, .T. ) ;
#12303=PLANE ( 'NONE',  #24007 ) ;
#12304=VECTOR ( 'NONE', #32883, 39.37007874015748143 ) ;
#12305=EDGE_LOOP ( 'NONE', ( #27322, #24986, #27892, #42989 ) ) ;
#12306=LINE ( 'NONE', #40448, #50358 ) ;
#12307=CARTESIAN_POINT ( 'NONE',  ( 3.927031490892378253E-16, 3.346456692913386100, 2.007874015748021268 ) ) ;
#12308=ORIENTED_EDGE ( 'NONE', *, *, #24812, .T. ) ;
#12312=DIRECTION ( 'NONE',  ( 0.000000000000000000, 0.000000000000000000, -1.000000000000000000 ) ) ;
#12314=VECTOR ( 'NONE', #48849, 39.37007874015748143 ) ;
#12315=ORIENTED_EDGE ( 'NONE', *, *, #9329, .F. ) ;
#12316=CARTESIAN_POINT ( 'NONE',  ( -1.909347346926324462, 3.346456692913386100, 1.102362204724404160 ) ) ;
#12319=DIRECTION ( 'NONE',  ( 1.734723475976806848E-16, -0.000000000000000000, 1.000000000000000000 ) ) ;
#12320=EDGE_CURVE ( 'NONE', #37743, #27124, #25665, .T. ) ;
#12321=ORIENTED_EDGE ( 'NONE', *, *, #6694, .F. ) ;
#12323=EDGE_CURVE ( 'NONE', #39537, #5174, #22811, .T. ) ;
#12324=LINE ( 'NONE', #16197, #19640 ) ;
#12328=EDGE_CURVE ( 'NONE', #17781, #33327, #47011, .T. ) ;
#12330=VECTOR ( 'NONE', #4134, 39.37007874015748143 ) ;
#12331=ORIENTED_EDGE ( 'NONE', *, *, #12098, .F. ) ;
#12332=DIRECTION ( 'NONE',  ( 1.734723475976806848E-16, -0.000000000000000000, 1.000000000000000000 ) ) ;
#12334=LINE ( 'NONE', #34374, #38838 ) ;
#12336=DIRECTION ( 'NONE',  ( 1.734723475976806848E-16, -0.000000000000000000, 1.000000000000000000 ) ) ;
#12337=ORIENTED_EDGE ( 'NONE', *, *, #23854, .F. ) ;
#12340=EDGE_CURVE ( 'NONE', #24, #19538, #10684, .T. ) ;
#12341=ORIENTED_EDGE ( 'NONE', *, *, #8590, .F. ) ;
#12342=EDGE_LOOP ( 'NONE', ( #36452, #8552, #38031, #3432 ) ) ;
#12345=EDGE_CURVE ( 'NONE', #38409, #40420, #34936, .T. ) ;
#12346=ORIENTED_EDGE ( 'NONE', *, *, #12547, .F. ) ;
#12347=CIRCLE ( 'NONE', #16480, 2.106299212598425008 ) ;
#12349=VERTEX_POINT ( 'NONE', #18935 ) ;
#12352=CARTESIAN_POINT ( 'NONE',  ( 0.7423782071083092626, 3.267716535433071279, 1.889763779527550369 ) ) ;
#12353=EDGE_LOOP ( 'NONE', ( #2815, #38020, #45920, #1815 ) ) ;
#12354=ORIENTED_EDGE ( 'NONE', *, *, #24940, .F. ) ;
#12355=DIRECTION ( 'NONE',  ( -3.469446951953613696E-16, 0.000000000000000000, -1.000000000000000000 ) ) ;
#12356=CARTESIAN_POINT ( 'NONE',  ( -1.712496953225537188, 3.267716535433071279, 0.1574803149606286423 ) ) ;
#12358=LINE ( 'NONE', #35095, #49032 ) ;
#12361=VECTOR ( 'NONE', #1673, 39.37007874015748143 ) ;
#12362=ORIENTED_EDGE ( 'NONE', *, *, #26597, .T. ) ;
#12363=PLANE ( 'NONE',  #11891 ) ;
#12364=VERTEX_POINT ( 'NONE', #7567 ) ;
#12365=FACE_OUTER_BOUND ( 'NONE', #26475, .T. ) ;
#12366=EDGE_LOOP ( 'NONE', ( #34236, #35399, #16827, #8743 ) ) ;
#12368=AXIS2_PLACEMENT_3D ( 'NONE', #25750, #17254, #13373 ) ;
#12372=LINE ( 'NONE', #28110, #44717 ) ;
#12373=ADVANCED_FACE ( 'NONE', ( #11687 ), #26423, .F. ) ;
#12374=DIRECTION ( 'NONE',  ( -1.000000000000000000, 0.000000000000000000, 1.734723475976806848E-16 ) ) ;
#12376=ORIENTED_EDGE ( 'NONE', *, *, #41523, .T. ) ;
#12377=DIRECTION ( 'NONE',  ( -0.000000000000000000, 0.000000000000000000, 1.000000000000000000 ) ) ;
#12378=VECTOR ( 'NONE', #18167, 39.37007874015748143 ) ;
#12380=ADVANCED_FACE ( 'NONE', ( #11440 ), #46767, .F. ) ;
#12383=EDGE_CURVE ( 'NONE', #20489, #28082, #19420, .T. ) ;
#12387=ORIENTED_EDGE ( 'NONE', *, *, #9344, .F. ) ;
#12389=LINE ( 'NONE', #35127, #14119 ) ;
#12390=FACE_BOUND ( 'NONE', #9398, .T. ) ;
#12391=CARTESIAN_POINT ( 'NONE',  ( 1.363819533518803251, 3.267716535433071279, 1.220472440944875281 ) ) ;
#12392=EDGE_CURVE ( 'NONE', #31330, #11733, #38562, .T. ) ;
#12393=DIRECTION ( 'NONE',  ( -1.000000000000000000, -0.000000000000000000, -0.000000000000000000 ) ) ;
#12395=DIRECTION ( 'NONE',  ( 1.000000000000000000, 0.000000000000000000, 0.000000000000000000 ) ) ;
#12397=VERTEX_POINT ( 'NONE', #23303 ) ;
#12398=VERTEX_POINT ( 'NONE', #2679 ) ;
#12400=ORIENTED_EDGE ( 'NONE', *, *, #35119, .T. ) ;
#12403=FACE_OUTER_BOUND ( 'NONE', #34330, .T. ) ;
#12404=AXIS2_PLACEMENT_3D ( 'NONE', #7424, #30665, #7173 ) ;
#12406=CARTESIAN_POINT ( 'NONE',  ( 0.8182917201112819283, 0.000000000000000000, -0.7874015748031473194 ) ) ;
#12407=CARTESIAN_POINT ( 'NONE',  ( -0.6214413264104945434, 3.346456692913386100, 2.012537465693970962 ) ) ;
#12409=ORIENTED_EDGE ( 'NONE', *, *, #12975, .T. ) ;
#12412=DIRECTION ( 'NONE',  ( -0.000000000000000000, 1.000000000000000000, -0.000000000000000000 ) ) ;
#12413=AXIS2_PLACEMENT_3D ( 'NONE', #40526, #5665, #29411 ) ;
#12414=ORIENTED_EDGE ( 'NONE', *, *, #23383, .F. ) ;
#12415=EDGE_CURVE ( 'NONE', #21582, #2475, #38063, .T. ) ;
#12418=CARTESIAN_POINT ( 'NONE',  ( 1.909347346926324462, 3.346456692913386100, -1.102362204724406602 ) ) ;
#12419=CARTESIAN_POINT ( 'NONE',  ( -1.363819533518803473, 3.267716535433071279, -1.929133858267710000 ) ) ;
#12420=FACE_OUTER_BOUND ( 'NONE', #38415, .T. ) ;
#12421=EDGE_LOOP ( 'NONE', ( #16844, #47666, #3264, #46319 ) ) ;
#12425=ORIENTED_EDGE ( 'NONE', *, *, #4619, .T. ) ;
#12426=DIRECTION ( 'NONE',  ( -3.469446951953613696E-16, 0.000000000000000000, -1.000000000000000000 ) ) ;
#12427=PLANE ( 'NONE',  #3084 ) ;
#12430=ORIENTED_EDGE ( 'NONE', *, *, #3487, .T. ) ;
#12432=VERTEX_POINT ( 'NONE', #15061 ) ;
#12433=LINE ( 'NONE', #45381, #22944 ) ;
#12434=ORIENTED_EDGE ( 'NONE', *, *, #49454, .T. ) ;
#12435=ADVANCED_FACE ( 'NONE', ( #42671 ), #30808, .F. ) ;
#12439=DIRECTION ( 'NONE',  ( 0.000000000000000000, 1.000000000000000000, 0.000000000000000000 ) ) ;
#12440=VECTOR ( 'NONE', #41740, 39.37007874015748143 ) ;
#12441=EDGE_CURVE ( 'NONE', #45936, #16745, #7319, .T. ) ;
#12442=ORIENTED_EDGE ( 'NONE', *, *, #17010, .F. ) ;
#12443=ORIENTED_EDGE ( 'NONE', *, *, #41761, .T. ) ;
#12444=VERTEX_POINT ( 'NONE', #38812 ) ;
#12445=DIRECTION ( 'NONE',  ( 1.734723475976806848E-16, -0.000000000000000000, 1.000000000000000000 ) ) ;
#12446=VERTEX_POINT ( 'NONE', #3440 ) ;
#12448=CARTESIAN_POINT ( 'NONE',  ( 2.106197740627112402, 0.000000000000000000, 0.7874015748031456541 ) ) ;
#12450=AXIS2_PLACEMENT_3D ( 'NONE', #29613, #22617, #33753 ) ;
#12452=AXIS2_PLACEMENT_3D ( 'NONE', #33974, #34978, #23095 ) ;
#12453=ORIENTED_EDGE ( 'NONE', *, *, #9049, .T. ) ;
#12455=LINE ( 'NONE', #8842, #37381 ) ;
#12456=LINE ( 'NONE', #20458, #44314 ) ;
#12457=VERTEX_POINT ( 'NONE', #20188 ) ;
#12458=CARTESIAN_POINT ( 'NONE',  ( -1.195183497228115035E-16, 3.346456692913386100, -0.3149606299212591165 ) ) ;
#12459=PLANE ( 'NONE',  #15332 ) ;
#12460=VERTEX_POINT ( 'NONE', #12711 ) ;
#12461=LINE ( 'NONE', #43944, #6003 ) ;
#12462=VERTEX_POINT ( 'NONE', #43427 ) ;
#12464=PLANE ( 'NONE',  #6451 ) ;
#12465=( LENGTH_UNIT ( ) NAMED_UNIT ( * ) SI_UNIT ( $, .METRE. ) );
#12466=DIRECTION ( 'NONE',  ( -0.000000000000000000, 1.000000000000000000, -0.000000000000000000 ) ) ;
#12467=EDGE_CURVE ( 'NONE', #13176, #18622, #835, .T. ) ;
#12468=DIRECTION ( 'NONE',  ( 1.734723475976806848E-16, -0.000000000000000000, 1.000000000000000000 ) ) ;
#12469=LINE ( 'NONE', #28210, #768 ) ;
#12470=ORIENTED_EDGE ( 'NONE', *, *, #48415, .T. ) ;
#12471=ORIENTED_EDGE ( 'NONE', *, *, #39068, .F. ) ;
#12473=ORIENTED_EDGE ( 'NONE', *, *, #12286, .T. ) ;
#12474=FACE_OUTER_BOUND ( 'NONE', #26682, .T. ) ;
#12475=EDGE_CURVE ( 'NONE', #4264, #29976, #4961, .T. ) ;
#12477=AXIS2_PLACEMENT_3D ( 'NONE', #46118, #38657, #3280 ) ;
#12478=ADVANCED_FACE ( 'NONE', ( #24333 ), #20704, .F. ) ;
#12479=LINE ( 'NONE', #46613, #32448 ) ;
#12480=DIRECTION ( 'NONE',  ( -1.000000000000000000, 0.000000000000000000, -0.000000000000000000 ) ) ;
#12481=VECTOR ( 'NONE', #11745, 39.37007874015748143 ) ;
#12482=CARTESIAN_POINT ( 'NONE',  ( -1.166969139818015755, 3.267716535433071279, 4.048737525165545662E-16 ) ) ;
#12483=ORIENTED_EDGE ( 'NONE', *, *, #14666, .F. ) ;
#12484=DIRECTION ( 'NONE',  ( 1.734723475976806848E-16, 0.000000000000000000, 1.000000000000000000 ) ) ;
#12485=ADVANCED_FACE ( 'NONE', ( #582 ), #39566, .F. ) ;
#12486=VECTOR ( 'NONE', #1156, 39.37007874015748143 ) ;
#12489=ORIENTED_EDGE ( 'NONE', *, *, #47270, .T. ) ;
#12490=AXIS2_PLACEMENT_3D ( 'NONE', #620, #43970, #8621 ) ;
#12492=DIRECTION ( 'NONE',  ( -0.000000000000000000, 1.000000000000000000, -0.000000000000000000 ) ) ;
#12493=LINE ( 'NONE', #28746, #29610 ) ;
#12494=ORIENTED_EDGE ( 'NONE', *, *, #49137, .T. ) ;
#12495=FACE_OUTER_BOUND ( 'NONE', #22618, .T. ) ;
#12497=CARTESIAN_POINT ( 'NONE',  ( 2.378961647330872786, 3.346456692913386100, 0.4330708661417287386 ) ) ;
#12498=ORIENTED_EDGE ( 'NONE', *, *, #34634, .F. ) ;
#12499=DIRECTION ( 'NONE',  ( 1.000000000000000000, 0.000000000000000000, 0.000000000000000000 ) ) ;
#12500=PLANE ( 'NONE',  #13047 ) ;
#12501=EDGE_LOOP ( 'NONE', ( #7545, #44610, #44935, #25472 ) ) ;
#12502=DIRECTION ( 'NONE',  ( 1.734723475976806848E-16, -0.000000000000000000, 1.000000000000000000 ) ) ;
#12503=EDGE_CURVE ( 'NONE', #35629, #29992, #24589, .T. ) ;
#12505=FACE_OUTER_BOUND ( 'NONE', #48165, .T. ) ;
#12506=LINE ( 'NONE', #1399, #13648 ) ;
#12510=ORIENTED_EDGE ( 'NONE', *, *, #13139, .F. ) ;
#12513=ORIENTED_EDGE ( 'NONE', *, *, #42500, .T. ) ;
#12514=LINE ( 'NONE', #36275, #1136 ) ;
#12515=DIRECTION ( 'NONE',  ( -3.469446951953613696E-16, 0.000000000000000000, -1.000000000000000000 ) ) ;
#12517=VECTOR ( 'NONE', #44734, 39.37007874015748143 ) ;
#12518=DIRECTION ( 'NONE',  ( 0.000000000000000000, -1.000000000000000000, 0.000000000000000000 ) ) ;
#12519=ORIENTED_EDGE ( 'NONE', *, *, #5102, .T. ) ;
#12521=ORIENTED_EDGE ( 'NONE', *, *, #36117, .T. ) ;
#12523=CARTESIAN_POINT ( 'NONE',  ( 4.268512490100411402E-16, 3.346456692913386100, 1.259842519685033357 ) ) ;
#12525=LINE ( 'NONE', #13555, #6738 ) ;
#12526=AXIS2_PLACEMENT_3D ( 'NONE', #42666, #34682, #18930 ) ;
#12527=FACE_BOUND ( 'NONE', #11376, .T. ) ;
#12528=ORIENTED_EDGE ( 'NONE', *, *, #13076, .F. ) ;
#12529=DIRECTION ( 'NONE',  ( 0.000000000000000000, 1.000000000000000000, 0.000000000000000000 ) ) ;
#12531=VECTOR ( 'NONE', #50496, 39.37007874015748143 ) ;
#12532=ORIENTED_EDGE ( 'NONE', *, *, #12741, .T. ) ;
#12533=DIRECTION ( 'NONE',  ( -1.000000000000000000, 0.000000000000000000, -0.000000000000000000 ) ) ;
#12535=EDGE_LOOP ( 'NONE', ( #29432, #21468, #44168, #9414 ) ) ;
#12536=EDGE_CURVE ( 'NONE', #5596, #18938, #1084, .T. ) ;
#12537=ORIENTED_EDGE ( 'NONE', *, *, #16310, .F. ) ;
#12538=DIRECTION ( 'NONE',  ( -1.000000000000000000, 0.000000000000000000, 0.000000000000000000 ) ) ;
#12540=LINE ( 'NONE', #28281, #32854 ) ;
#12542=EDGE_CURVE ( 'NONE', #31043, #2822, #1359, .T. ) ;
#12544=EDGE_CURVE ( 'NONE', #22163, #37684, #16848, .T. ) ;
#12545=EDGE_CURVE ( 'NONE', #41777, #7739, #8579, .T. ) ;
#12546=PLANE ( 'NONE',  #48635 ) ;
#12547=EDGE_CURVE ( 'NONE', #850, #10535, #8836, .T. ) ;
#12548=CARTESIAN_POINT ( 'NONE',  ( -1.536664496436148184E-16, 0.000000000000000000, -1.771653543307081025 ) ) ;
#12550=ORIENTED_EDGE ( 'NONE', *, *, #10175, .T. ) ;
#12551=PLANE ( 'NONE',  #24188 ) ;
#12552=DIRECTION ( 'NONE',  ( -1.000000000000000000, -0.000000000000000000, -0.000000000000000000 ) ) ;
#12553=CARTESIAN_POINT ( 'NONE',  ( -1.788632549858358844, 3.267716535433071279, 1.220472440944875059 ) ) ;
#12554=ORIENTED_EDGE ( 'NONE', *, *, #46467, .F. ) ;
#12555=VECTOR ( 'NONE', #15257, 39.37007874015748143 ) ;
#12556=CARTESIAN_POINT ( 'NONE',  ( -0.8942052331142552601, 3.346456692913386100, 2.007874015748021268 ) ) ;
#12558=ORIENTED_EDGE ( 'NONE', *, *, #2216, .F. ) ;
#12559=DIRECTION ( 'NONE',  ( -0.000000000000000000, 0.000000000000000000, 1.000000000000000000 ) ) ;
#12560=ADVANCED_FACE ( 'NONE', ( #24072 ), #27678, .F. ) ;
#12563=VECTOR ( 'NONE', #39381, 39.37007874015748143 ) ;
#12565=CIRCLE ( 'NONE', #47120, 2.106299212598425008 ) ;
#12567=EDGE_CURVE ( 'NONE', #31313, #32010, #23555, .T. ) ;
#12568=ORIENTED_EDGE ( 'NONE', *, *, #4616, .F. ) ;
#12569=DIRECTION ( 'NONE',  ( -0.000000000000000000, 1.000000000000000000, -0.000000000000000000 ) ) ;
#12571=CIRCLE ( 'NONE', #35634, 2.106299212598425008 ) ;
#12574=CARTESIAN_POINT ( 'NONE',  ( -1.091055626815042423, 3.267716535433071279, 1.892679809432644143E-16 ) ) ;
#12575=EDGE_CURVE ( 'NONE', #17653, #15706, #15808, .T. ) ;
#12576=VERTEX_POINT ( 'NONE', #35955 ) ;
#12578=CARTESIAN_POINT ( 'NONE',  ( 1.560669927219590303, 3.346456692913386100, -1.102362204724405714 ) ) ;
#12580=VERTEX_POINT ( 'NONE', #2110 ) ;
#12581=CARTESIAN_POINT ( 'NONE',  ( 1.833433833923351353, 3.346456692913386100, -1.161035397307311917E-15 ) ) ;
#12583=VERTEX_POINT ( 'NONE', #40847 ) ;
#12584=DIRECTION ( 'NONE',  ( -3.469446951953613696E-16, 0.000000000000000000, -1.000000000000000000 ) ) ;
#12585=ORIENTED_EDGE ( 'NONE', *, *, #39213, .F. ) ;
#12586=CARTESIAN_POINT ( 'NONE',  ( -0.8942052331142547050, 0.000000000000000000, 1.062992125984246083 ) ) ;
#12588=ORIENTED_EDGE ( 'NONE', *, *, #9203, .T. ) ;
#12589=CARTESIAN_POINT ( 'NONE',  ( 0.8182917201112819283, 3.346456692913386100, 0.5905511811023579360 ) ) ;
#12590=VERTEX_POINT ( 'NONE', #9346 ) ;
#12592=LINE ( 'NONE', #16732, #32025 ) ;
#12593=VERTEX_POINT ( 'NONE', #1601 ) ;
#12594=ORIENTED_EDGE ( 'NONE', *, *, #2268, .T. ) ;
#12596=VECTOR ( 'NONE', #16854, 39.37007874015748143 ) ;
#12597=VERTEX_POINT ( 'NONE', #1855 ) ;
#12598=VECTOR ( 'NONE', #39830, 39.37007874015748143 ) ;
#12599=LINE ( 'NONE', #27826, #8101 ) ;
#12600=VERTEX_POINT ( 'NONE', #5731 ) ;
#12601=LINE ( 'NONE', #32235, #10427 ) ;
#12602=VECTOR ( 'NONE', #18141, 39.37007874015748143 ) ;
#12603=VECTOR ( 'NONE', #33161, 39.37007874015748143 ) ;
#12604=CARTESIAN_POINT ( 'NONE',  ( 1.670330979180827180, 3.267716535433071279, 1.377952755905504256 ) ) ;
#12607=VERTEX_POINT ( 'NONE', #41608 ) ;
#12608=ORIENTED_EDGE ( 'NONE', *, *, #32146, .F. ) ;
#12609=EDGE_CURVE ( 'NONE', #17641, #35680, #44451, .T. ) ;
#12610=CARTESIAN_POINT ( 'NONE',  ( -0.5455278134075214336, 3.346456692913386100, -0.3149606299212593941 ) ) ;
#12612=VECTOR ( 'NONE', #46805, 39.37007874015748143 ) ;
#12613=ADVANCED_FACE ( 'NONE', ( #49555 ), #37746, .T. ) ;
#12614=LINE ( 'NONE', #16749, #31542 ) ;
#12615=DIRECTION ( 'NONE',  ( -1.000000000000000000, 0.000000000000000000, -0.000000000000000000 ) ) ;
#12616=DIRECTION ( 'NONE',  ( -0.000000000000000000, 1.000000000000000000, -0.000000000000000000 ) ) ;
#12617=DIRECTION ( 'NONE',  ( -3.469446951953613696E-16, 0.000000000000000000, -1.000000000000000000 ) ) ;
#12618=CARTESIAN_POINT ( 'NONE',  ( 0.4696143004045478797, 3.346456692913386100, -0.3543307086614173040 ) ) ;
#12619=EDGE_LOOP ( 'NONE', ( #4486, #19424, #33652, #32685 ) ) ;
#12621=VERTEX_POINT ( 'NONE', #33621 ) ;
#12625=PLANE ( 'NONE',  #24248 ) ;
#12626=CARTESIAN_POINT ( 'NONE',  ( 1.909347346926324684, 0.000000000000000000, 0.7874015748031456541 ) ) ;
#12627=EDGE_CURVE ( 'NONE', #15792, #17531, #28703, .T. ) ;
#12630=ORIENTED_EDGE ( 'NONE', *, *, #33603, .F. ) ;
#12632=AXIS2_PLACEMENT_3D ( 'NONE', #24274, #4654, #32030 ) ;
#12633=FACE_BOUND ( 'NONE', #4056, .T. ) ;
#12634=ADVANCED_FACE ( 'NONE', ( #18114 ), #29216, .F. ) ;
#12637=VECTOR ( 'NONE', #17965, 39.37007874015748143 ) ;
#12638=EDGE_CURVE ( 'NONE', #48286, #36377, #6309, .T. ) ;
#12639=ORIENTED_EDGE ( 'NONE', *, *, #41193, .F. ) ;
#12640=VECTOR ( 'NONE', #45213, 39.37007874015748143 ) ;
#12641=VECTOR ( 'NONE', #4672, 39.37007874015748143 ) ;
#12643=CARTESIAN_POINT ( 'NONE',  ( 2.182111253630085290, 0.000000000000000000, -0.5118110236220471121 ) ) ;
#12644=VECTOR ( 'NONE', #30845, 39.37007874015748143 ) ;
#12646=ORIENTED_EDGE ( 'NONE', *, *, #19116, .F. ) ;
#12647=VERTEX_POINT ( 'NONE', #10112 ) ;
#12649=CARTESIAN_POINT ( 'NONE',  ( 1.833433833923351353, 3.346456692913386100, 1.574803149606291974 ) ) ;
#12651=DIRECTION ( 'NONE',  ( 1.734723475976806848E-16, -0.000000000000000000, 1.000000000000000000 ) ) ;
#12653=ORIENTED_EDGE ( 'NONE', *, *, #31347, .T. ) ;
#12655=ORIENTED_EDGE ( 'NONE', *, *, #12542, .T. ) ;
#12656=ORIENTED_EDGE ( 'NONE', *, *, #45189, .F. ) ;
#12657=EDGE_LOOP ( 'NONE', ( #2093, #9977, #1952, #28859 ) ) ;
#12659=CARTESIAN_POINT ( 'NONE',  ( 1.636583440222563857, 0.000000000000000000, 1.259842519685033135 ) ) ;
#12660=PLANE ( 'NONE',  #25058 ) ;
#12662=ORIENTED_EDGE ( 'NONE', *, *, #27640, .T. ) ;
#12663=ORIENTED_EDGE ( 'NONE', *, *, #42008, .T. ) ;
#12665=ADVANCED_FACE ( 'NONE', ( #45198 ), #25854, .F. ) ;
#12666=CARTESIAN_POINT ( 'NONE',  ( -0.5455278134075214336, 3.346456692913386100, -1.574803149606293529 ) ) ;
#12667=EDGE_CURVE ( 'NONE', #34486, #23961, #45020, .T. ) ;
#12668=DIRECTION ( 'NONE',  ( 0.000000000000000000, -0.000000000000000000, 1.000000000000000000 ) ) ;
#12671=FACE_OUTER_BOUND ( 'NONE', #12028, .T. ) ;
#12672=ADVANCED_FACE ( 'NONE', ( #9605 ), #25349, .F. ) ;
#12673=AXIS2_PLACEMENT_3D ( 'NONE', #10995, #123, #15870 ) ;
#12674=FACE_OUTER_BOUND ( 'NONE', #851, .T. ) ;
#12676=CARTESIAN_POINT ( 'NONE',  ( 1.015142113812069313, 0.000000000000000000, 0.4724409448818868706 ) ) ;
#12678=DIRECTION ( 'NONE',  ( 0.000000000000000000, 0.000000000000000000, 1.000000000000000000 ) ) ;
#12679=DIRECTION ( 'NONE',  ( -0.000000000000000000, 1.000000000000000000, -0.000000000000000000 ) ) ;
#12680=VECTOR ( 'NONE', #2593, 39.37007874015748143 ) ;
#12684=ORIENTED_EDGE ( 'NONE', *, *, #24119, .F. ) ;
#12685=ORIENTED_EDGE ( 'NONE', *, *, #28011, .F. ) ;
#12687=DIRECTION ( 'NONE',  ( -3.469446951953613696E-16, 0.000000000000000000, -1.000000000000000000 ) ) ;
#12689=CARTESIAN_POINT ( 'NONE',  ( 0.000000000000000000, 3.346456692913386100, 0.000000000000000000 ) ) ;
#12690=EDGE_LOOP ( 'NONE', ( #44395, #35458, #39117, #308 ) ) ;
#12692=EDGE_CURVE ( 'NONE', #19583, #47436, #19109, .T. ) ;
#12694=LINE ( 'NONE', #12178, #50101 ) ;
#12695=VERTEX_POINT ( 'NONE', #46456 ) ;
#12696=DIRECTION ( 'NONE',  ( 1.734723475976806848E-16, -0.000000000000000000, 1.000000000000000000 ) ) ;
#12697=VERTEX_POINT ( 'NONE', #29984 ) ;
#12699=DIRECTION ( 'NONE',  ( -1.000000000000000000, 0.000000000000000000, 1.734723475976806848E-16 ) ) ;
#12700=DIRECTION ( 'NONE',  ( 1.734723475976806848E-16, -0.000000000000000000, 1.000000000000000000 ) ) ;
#12702=CIRCLE ( 'NONE', #309, 2.106299212598425008 ) ;
#12703=ORIENTED_EDGE ( 'NONE', *, *, #36607, .T. ) ;
#12711=CARTESIAN_POINT ( 'NONE',  ( -0.2727639067037607723, 3.346456692913386100, -0.1574803149606301411 ) ) ;
#12713=ADVANCED_FACE ( 'NONE', ( #22494 ), #38990, .F. ) ;
#12714=VECTOR ( 'NONE', #48841, 39.37007874015748143 ) ;
#12716=VERTEX_POINT ( 'NONE', #19358 ) ;
#12717=CARTESIAN_POINT ( 'NONE',  ( 0.7423782071083082634, 3.267716535433071279, -2.086614173228340086 ) ) ;
#12718=DIRECTION ( 'NONE',  ( -0.000000000000000000, 1.000000000000000000, -0.000000000000000000 ) ) ;
#12722=FACE_OUTER_BOUND ( 'NONE', #48120, .T. ) ;
#12723=AXIS2_PLACEMENT_3D ( 'NONE', #5387, #28359, #8747 ) ;
#12724=ORIENTED_EDGE ( 'NONE', *, *, #48040, .F. ) ;
#12727=ORIENTED_EDGE ( 'NONE', *, *, #15052, .F. ) ;
#12729=FACE_OUTER_BOUND ( 'NONE', #1447, .T. ) ;
#12731=LINE ( 'NONE', #16353, #17253 ) ;
#12732=ORIENTED_EDGE ( 'NONE', *, *, #13146, .T. ) ;
#12733=ORIENTED_EDGE ( 'NONE', *, *, #30115, .T. ) ;
#12734=EDGE_CURVE ( 'NONE', #39780, #904, #46704, .T. ) ;
#12735=CARTESIAN_POINT ( 'NONE',  ( 2.182111253630085290, 0.000000000000000000, -0.5118110236220471121 ) ) ;
#12737=PLANE ( 'NONE',  #13748 ) ;
#12738=LINE ( 'NONE', #11971, #40796 ) ;
#12741=EDGE_CURVE ( 'NONE', #5207, #5416, #35126, .T. ) ;
#12742=ADVANCED_FACE ( 'NONE', ( #38250 ), #22244, .F. ) ;
#12743=CARTESIAN_POINT ( 'NONE',  ( -1.794796351285542491, 3.346456692913386100, 1.102362204724404160 ) ) ;
#12745=PLANE ( 'NONE',  #35961 ) ;
#12746=CARTESIAN_POINT ( 'NONE',  ( 2.182111253630085290, 3.346456692913386100, -0.1968503937007886062 ) ) ;
#12747=VERTEX_POINT ( 'NONE', #34119 ) ;
#12748=VECTOR ( 'NONE', #20995, 39.37007874015748143 ) ;
#12749=DIRECTION ( 'NONE',  ( -0.000000000000000000, 1.000000000000000000, -0.000000000000000000 ) ) ;
#12750=VECTOR ( 'NONE', #7523, 39.37007874015748143 ) ;
#12751=CARTESIAN_POINT ( 'NONE',  ( 1.015142113812069313, 3.267716535433071279, -0.9842519685039348154 ) ) ;
#12754=VERTEX_POINT ( 'NONE', #46208 ) ;
#12755=DIRECTION ( 'NONE',  ( 0.000000000000000000, -1.000000000000000000, 0.000000000000000000 ) ) ;
#12756=DIRECTION ( 'NONE',  ( 1.000000000000000000, 0.000000000000000000, 0.000000000000000000 ) ) ;
#12757=EDGE_CURVE ( 'NONE', #29976, #8862, #14998, .T. ) ;
#12758=LINE ( 'NONE', #13013, #18878 ) ;
#12760=CARTESIAN_POINT ( 'NONE',  ( -0.07591351300297362326, 3.267716535433071279, -2.104930761696520491 ) ) ;
#12761=CARTESIAN_POINT ( 'NONE',  ( -1.353122744573580727, 3.267716535433071279, -1.614173228346451605 ) ) ;
#12763=VECTOR ( 'NONE', #15516, 39.37007874015748143 ) ;
#12764=ADVANCED_FACE ( 'NONE', ( #49808 ), #14493, .F. ) ;
#12765=ORIENTED_EDGE ( 'NONE', *, *, #30133, .F. ) ;
#12766=LINE ( 'NONE', #19975, #21380 ) ;
#12768=ORIENTED_EDGE ( 'NONE', *, *, #32795, .F. ) ;
#12770=CARTESIAN_POINT ( 'NONE',  ( -0.8942052331142552601, 3.346456692913386100, -0.6299212598425177889 ) ) ;
#12771=PLANE ( 'NONE',  #42018 ) ;
#12772=CARTESIAN_POINT ( 'NONE',  ( -1.985260859929297572, 3.346456692913386100, -0.3149606299212589500 ) ) ;
#12774=VERTEX_POINT ( 'NONE', #30243 ) ;
#12776=DIRECTION ( 'NONE',  ( 0.000000000000000000, 0.000000000000000000, -1.000000000000000000 ) ) ;
#12777=PLANE ( 'NONE',  #6518 ) ;
#12778=VERTEX_POINT ( 'NONE', #34872 ) ;
#12779=DIRECTION ( 'NONE',  ( -0.000000000000000000, 1.000000000000000000, -0.000000000000000000 ) ) ;
#12780=FACE_OUTER_BOUND ( 'NONE', #16962, .T. ) ;
#12784=ORIENTED_EDGE ( 'NONE', *, *, #46327, .F. ) ;
#12786=PLANE ( 'NONE',  #6487 ) ;
#12787=DIRECTION ( 'NONE',  ( -0.000000000000000000, 1.000000000000000000, -0.000000000000000000 ) ) ;
#12791=FACE_BOUND ( 'NONE', #43079, .T. ) ;
#12792=VECTOR ( 'NONE', #16807, 39.37007874015748143 ) ;
#12793=ORIENTED_EDGE ( 'NONE', *, *, #45834, .F. ) ;
#12794=EDGE_CURVE ( 'NONE', #17583, #15817, #11125, .T. ) ;
#12797=ORIENTED_EDGE ( 'NONE', *, *, #42804, .T. ) ;
#12798=ORIENTED_EDGE ( 'NONE', *, *, #22601, .F. ) ;
#12800=VECTOR ( 'NONE', #34989, 39.37007874015748143 ) ;
#12802=ORIENTED_EDGE ( 'NONE', *, *, #49462, .F. ) ;
#12803=ORIENTED_EDGE ( 'NONE', *, *, #48328, .F. ) ;
#12805=ORIENTED_EDGE ( 'NONE', *, *, #50588, .F. ) ;
#12806=VECTOR ( 'NONE', #42967, 39.37007874015748143 ) ;
#12809=CARTESIAN_POINT ( 'NONE',  ( 1.560669927219590525, 0.000000000000000000, -0.9842519685039348154 ) ) ;
#12811=CARTESIAN_POINT ( 'NONE',  ( 0.7423782071083087075, 0.000000000000000000, 0.9448818897637746295 ) ) ;
#12813=DIRECTION ( 'NONE',  ( 0.000000000000000000, 0.000000000000000000, 1.000000000000000000 ) ) ;
#12814=CARTESIAN_POINT ( 'NONE',  ( -0.8182917201112823724, 3.267716535433071279, 1.419509857074484278E-16 ) ) ;
#12815=VERTEX_POINT ( 'NONE', #18875 ) ;
#12816=FACE_OUTER_BOUND ( 'NONE', #25241, .T. ) ;
#12818=LINE ( 'NONE', #680, #89 ) ;
#12819=ORIENTED_EDGE ( 'NONE', *, *, #8818, .F. ) ;
#12822=VERTEX_POINT ( 'NONE', #28382 ) ;
#12823=CARTESIAN_POINT ( 'NONE',  ( -0.6214413264104939882, 0.000000000000000000, 1.535433070866133898 ) ) ;
#12827=VECTOR ( 'NONE', #22996, 39.37007874015748143 ) ;
#12829=LINE ( 'NONE', #40458, #10908 ) ;
#12830=VERTEX_POINT ( 'NONE', #19860 ) ;
#12831=FACE_BOUND ( 'NONE', #9078, .T. ) ;
#12832=VECTOR ( 'NONE', #26411, 39.37007874015748143 ) ;
#12833=CARTESIAN_POINT ( 'NONE',  ( 3.927031490892378253E-16, 0.000000000000000000, 1.692913385826762873 ) ) ;
#12834=CARTESIAN_POINT ( 'NONE',  ( -1.536664496436148184E-16, 3.346456692913386100, -1.456692913385822630 ) ) ;
#12835=CARTESIAN_POINT ( 'NONE',  ( 1.091055626815042645, 3.346456692913386100, -0.5118110236220471121 ) ) ;
#12836=AXIS2_PLACEMENT_3D ( 'NONE', #2944, #34196, #18700 ) ;
#12837=ADVANCED_FACE ( 'NONE', ( #23491 ), #35631, .F. ) ;
#12838=VECTOR ( 'NONE', #19799, 39.37007874015748143 ) ;
#12839=ORIENTED_EDGE ( 'NONE', *, *, #1032, .T. ) ;
#12840=ORIENTED_EDGE ( 'NONE', *, *, #32092, .F. ) ;
#12841=DIRECTION ( 'NONE',  ( 1.734723475976806848E-16, -0.000000000000000000, 1.000000000000000000 ) ) ;
#12843=DIRECTION ( 'NONE',  ( 1.000000000000000000, -0.000000000000000000, 0.000000000000000000 ) ) ;
#12844=ORIENTED_EDGE ( 'NONE', *, *, #18615, .F. ) ;
#12849=DIRECTION ( 'NONE',  ( 1.000000000000000000, 0.000000000000000000, 0.000000000000000000 ) ) ;
#12852=ORIENTED_EDGE ( 'NONE', *, *, #27819, .F. ) ;
#12853=CARTESIAN_POINT ( 'NONE',  ( 0.000000000000000000, 3.346456692913386100, 0.000000000000000000 ) ) ;
#12854=ORIENTED_EDGE ( 'NONE', *, *, #49452, .F. ) ;
#12855=CARTESIAN_POINT ( 'NONE',  ( -0.2727639067037608278, 3.267716535433071279, -0.3543307086614175816 ) ) ;
#12856=ORIENTED_EDGE ( 'NONE', *, *, #29863, .F. ) ;
#12857=VERTEX_POINT ( 'NONE', #8518 ) ;
#12858=EDGE_CURVE ( 'NONE', #10544, #14916, #24269, .T. ) ;
#12860=VECTOR ( 'NONE', #13712, 39.37007874015748143 ) ;
#12862=ORIENTED_EDGE ( 'NONE', *, *, #7469, .T. ) ;
#12864=VECTOR ( 'NONE', #27860, 39.37007874015748143 ) ;
#12865=EDGE_LOOP ( 'NONE', ( #15645, #23375, #8493, #50063 ) ) ;
#12866=DIRECTION ( 'NONE',  ( -3.469446951953613696E-16, 0.000000000000000000, -1.000000000000000000 ) ) ;
#12869=VECTOR ( 'NONE', #13489, 39.37007874015748143 ) ;
#12873=VECTOR ( 'NONE', #30170, 39.37007874015748143 ) ;
#12875=CARTESIAN_POINT ( 'NONE',  ( -1.091055626815042201, 3.346456692913386100, 0.9448818897637749625 ) ) ;
#12877=DIRECTION ( 'NONE',  ( -1.000000000000000000, -0.000000000000000000, -0.000000000000000000 ) ) ;
#12878=DIRECTION ( 'NONE',  ( 1.000000000000000000, 0.000000000000000000, 0.000000000000000000 ) ) ;
#12881=ORIENTED_EDGE ( 'NONE', *, *, #27184, .T. ) ;
#12882=LINE ( 'NONE', #30, #2336 ) ;
#12886=ORIENTED_EDGE ( 'NONE', *, *, #22380, .T. ) ;
#12887=PLANE ( 'NONE',  #48670 ) ;
#12888=CARTESIAN_POINT ( 'NONE',  ( 1.997134316236881091, 3.346456692913386100, -0.6692913385826764205 ) ) ;
#12889=LINE ( 'NONE', #9014, #3966 ) ;
#12890=DIRECTION ( 'NONE',  ( -0.000000000000000000, 0.000000000000000000, 1.000000000000000000 ) ) ;
#12891=CARTESIAN_POINT ( 'NONE',  ( 0.000000000000000000, 3.267716535433071279, 0.000000000000000000 ) ) ;
#12892=VERTEX_POINT ( 'NONE', #40014 ) ;
#12894=DIRECTION ( 'NONE',  ( -1.000000000000000000, 0.000000000000000000, 0.000000000000000000 ) ) ;
#12896=FACE_BOUND ( 'NONE', #45610, .T. ) ;
#12897=VECTOR ( 'NONE', #39973, 39.37007874015748143 ) ;
#12898=ORIENTED_EDGE ( 'NONE', *, *, #22316, .F. ) ;
#12899=CARTESIAN_POINT ( 'NONE',  ( 0.8182917201112819283, 0.000000000000000000, -1.102362204724405714 ) ) ;
#12901=ORIENTED_EDGE ( 'NONE', *, *, #4250, .F. ) ;
#12903=LINE ( 'NONE', #32272, #36312 ) ;
#12904=EDGE_CURVE ( 'NONE', #33946, #1872, #8262, .T. ) ;
#12905=AXIS2_PLACEMENT_3D ( 'NONE', #25944, #25686, #25183 ) ;
#12908=VECTOR ( 'NONE', #13101, 39.37007874015748143 ) ;
#12910=ORIENTED_EDGE ( 'NONE', *, *, #10007, .T. ) ;
#12911=EDGE_LOOP ( 'NONE', ( #16536, #13348, #202, #22857 ) ) ;
#12913=CARTESIAN_POINT ( 'NONE',  ( 0.2727639067037604392, 3.346456692913386100, -1.614173228346451605 ) ) ;
#12914=LINE ( 'NONE', #17544, #50354 ) ;
#12915=FACE_BOUND ( 'NONE', #15098, .T. ) ;
#12916=EDGE_CURVE ( 'NONE', #35907, #9339, #39755, .T. ) ;
#12918=PLANE ( 'NONE',  #48083 ) ;
#12919=VERTEX_POINT ( 'NONE', #47202 ) ;
#12920=LINE ( 'NONE', #28132, #43896 ) ;
#12921=ORIENTED_EDGE ( 'NONE', *, *, #47694, .T. ) ;
#12922=ORIENTED_EDGE ( 'NONE', *, *, #30719, .T. ) ;
#12923=ADVANCED_FACE ( 'NONE', ( #3882 ), #44130, .F. ) ;
#12926=CARTESIAN_POINT ( 'NONE',  ( 0.4696143004045476577, 3.346456692913386100, -2.047244094488182231 ) ) ;
#12927=EDGE_CURVE ( 'NONE', #25574, #17583, #4565, .T. ) ;
#12928=VECTOR ( 'NONE', #43647, 39.37007874015748143 ) ;
#12931=EDGE_CURVE ( 'NONE', #40451, #11955, #36144, .T. ) ;
#12933=VERTEX_POINT ( 'NONE', #32277 ) ;
#12934=DIRECTION ( 'NONE',  ( -1.000000000000000000, 0.000000000000000000, 1.734723475976806848E-16 ) ) ;
#12935=VECTOR ( 'NONE', #46110, 39.37007874015748143 ) ;
#12936=LINE ( 'NONE', #13192, #27917 ) ;
#12940=ADVANCED_FACE ( 'NONE', ( #47972 ), #35381, .F. ) ;
#12942=LINE ( 'NONE', #24035, #41277 ) ;
#12943=CARTESIAN_POINT ( 'NONE',  ( 0.1968503937007872462, 0.000000000000000000, -1.141732283464564013 ) ) ;
#12945=CARTESIAN_POINT ( 'NONE',  ( 1.909347346926324462, 3.346456692913386100, -1.102362204724406602 ) ) ;
#12947=ORIENTED_EDGE ( 'NONE', *, *, #19103, .F. ) ;
#12949=DIRECTION ( 'NONE',  ( -1.000000000000000000, 0.000000000000000000, 0.000000000000000000 ) ) ;
#12950=ORIENTED_EDGE ( 'NONE', *, *, #6255, .F. ) ;
#12951=ORIENTED_EDGE ( 'NONE', *, *, #48141, .T. ) ;
#12952=DIRECTION ( 'NONE',  ( -0.000000000000000000, 1.000000000000000000, -0.000000000000000000 ) ) ;
#12953=CARTESIAN_POINT ( 'NONE',  ( -1.363819533518803473, 3.244427737985139171, 2.040716226787704368 ) ) ;
#12955=ORIENTED_EDGE ( 'NONE', *, *, #43513, .F. ) ;
#12956=PLANE ( 'NONE',  #16361 ) ;
#12957=ORIENTED_EDGE ( 'NONE', *, *, #16310, .T. ) ;
#12958=VERTEX_POINT ( 'NONE', #48992 ) ;
#12960=PLANE ( 'NONE',  #9883 ) ;
#12963=ORIENTED_EDGE ( 'NONE', *, *, #20191, .F. ) ;
#12964=EDGE_CURVE ( 'NONE', #18779, #45470, #32800, .T. ) ;
#12965=ORIENTED_EDGE ( 'NONE', *, *, #9861, .T. ) ;
#12968=LINE ( 'NONE', #43928, #2427 ) ;
#12970=ORIENTED_EDGE ( 'NONE', *, *, #19003, .F. ) ;
#12971=ORIENTED_EDGE ( 'NONE', *, *, #47119, .F. ) ;
#12972=CARTESIAN_POINT ( 'NONE',  ( 1.833433833923351353, 3.346456692913386100, 0.6299212598425164567 ) ) ;
#12973=DIRECTION ( 'NONE',  ( -0.000000000000000000, 0.000000000000000000, 1.000000000000000000 ) ) ;
#12975=EDGE_CURVE ( 'NONE', #10793, #40287, #44632, .T. ) ;
#12977=LINE ( 'NONE', #48038, #13935 ) ;
#12979=LINE ( 'NONE', #21232, #24530 ) ;
#12980=ORIENTED_EDGE ( 'NONE', *, *, #21146, .T. ) ;
#12981=DIRECTION ( 'NONE',  ( -0.000000000000000000, 0.000000000000000000, 1.000000000000000000 ) ) ;
#12984=ORIENTED_EDGE ( 'NONE', *, *, #3811, .F. ) ;
#12985=ORIENTED_EDGE ( 'NONE', *, *, #41961, .F. ) ;
#12986=DIRECTION ( 'NONE',  ( 0.000000000000000000, 1.000000000000000000, 0.000000000000000000 ) ) ;
#12988=VECTOR ( 'NONE', #19325, 39.37007874015748143 ) ;
#12990=EDGE_CURVE ( 'NONE', #44874, #17837, #13674, .T. ) ;
#12991=CARTESIAN_POINT ( 'NONE',  ( 0.000000000000000000, 3.267716535433071279, -1.102362204724406602 ) ) ;
#12992=CARTESIAN_POINT ( 'NONE',  ( -1.439733046521776361, 3.346456692913386100, 1.062992125984246083 ) ) ;
#12998=ORIENTED_EDGE ( 'NONE', *, *, #48589, .F. ) ;
#12999=CARTESIAN_POINT ( 'NONE',  ( 0.000000000000000000, 0.000000000000000000, 0.000000000000000000 ) ) ;
#13001=VECTOR ( 'NONE', #46753, 39.37007874015748143 ) ;
#13002=AXIS2_PLACEMENT_3D ( 'NONE', #28680, #41087, #25077 ) ;
#13004=LINE ( 'NONE', #5245, #33509 ) ;
#13005=CARTESIAN_POINT ( 'NONE',  ( 1.560669927219590303, 3.267716535433071279, -1.880327210325009046 ) ) ;
#13006=ORIENTED_EDGE ( 'NONE', *, *, #46550, .F. ) ;
#13007=LINE ( 'NONE', #28739, #36579 ) ;
#13011=CARTESIAN_POINT ( 'NONE',  ( 0.000000000000000000, 3.267716535433071279, -0.6299212598425177889 ) ) ;
#13013=CARTESIAN_POINT ( 'NONE',  ( 0.000000000000000000, 3.267716535433071279, 1.889763779527550369 ) ) ;
#13014=ORIENTED_EDGE ( 'NONE', *, *, #2980, .F. ) ;
#13019=FACE_OUTER_BOUND ( 'NONE', #27370, .T. ) ;
#13022=VECTOR ( 'NONE', #27207, 39.37007874015748143 ) ;
#13023=CARTESIAN_POINT ( 'NONE',  ( -0.2727639067037607723, 0.000000000000000000, -1.417322834645664331 ) ) ;
#13024=DIRECTION ( 'NONE',  ( -0.000000000000000000, 1.000000000000000000, -0.000000000000000000 ) ) ;
#13027=DIRECTION ( 'NONE',  ( -3.469446951953613696E-16, 0.000000000000000000, -1.000000000000000000 ) ) ;
#13028=DIRECTION ( 'NONE',  ( -1.000000000000000000, -0.000000000000000000, -0.000000000000000000 ) ) ;
#13029=EDGE_CURVE ( 'NONE', #48909, #34275, #44888, .T. ) ;
#13031=VERTEX_POINT ( 'NONE', #24781 ) ;
#13032=CARTESIAN_POINT ( 'NONE',  ( 0.000000000000000000, 3.267716535433071279, 0.1181102362204704270 ) ) ;
#13033=CARTESIAN_POINT ( 'NONE',  ( -0.8182917201112819283, 0.000000000000000000, -1.102362204724405492 ) ) ;
#13035=VERTEX_POINT ( 'NONE', #1792 ) ;
#13036=CARTESIAN_POINT ( 'NONE',  ( -0.5455278134075216556, 0.000000000000000000, -2.401574803149598036 ) ) ;
#13041=ORIENTED_EDGE ( 'NONE', *, *, #27524, .T. ) ;
#13043=EDGE_CURVE ( 'NONE', #24046, #43573, #28897, .T. ) ;
#13044=CARTESIAN_POINT ( 'NONE',  ( 0.000000000000000000, 3.267716535433071279, -0.6692913385826764205 ) ) ;
#13045=DIRECTION ( 'NONE',  ( -0.000000000000000000, 1.000000000000000000, -0.000000000000000000 ) ) ;
#13046=VECTOR ( 'NONE', #29532, 39.37007874015748143 ) ;
#13047=AXIS2_PLACEMENT_3D ( 'NONE', #19976, #40134, #28496 ) ;
#13050=ORIENTED_EDGE ( 'NONE', *, *, #34206, .T. ) ;
#13052=FACE_BOUND ( 'NONE', #41047, .T. ) ;
#13054=CARTESIAN_POINT ( 'NONE',  ( 1.091055626815042645, 3.267716535433071279, -0.5118110236220471121 ) ) ;
#13056=AXIS2_PLACEMENT_3D ( 'NONE', #39703, #44333, #51005 ) ;
#13057=VERTEX_POINT ( 'NONE', #28559 ) ;
#13060=EDGE_CURVE ( 'NONE', #28852, #16144, #30952, .T. ) ;
#13061=ORIENTED_EDGE ( 'NONE', *, *, #9758, .T. ) ;
#13062=DIRECTION ( 'NONE',  ( 1.000000000000000000, 0.000000000000000000, 0.000000000000000000 ) ) ;
#13064=ORIENTED_EDGE ( 'NONE', *, *, #47248, .F. ) ;
#13066=CIRCLE ( 'NONE', #3985, 2.165354330708661568 ) ;
#13067=LINE ( 'NONE', #12031, #26243 ) ;
#13071=FACE_OUTER_BOUND ( 'NONE', #45244, .T. ) ;
#13072=LINE ( 'NONE', #31929, #27799 ) ;
#13073=CARTESIAN_POINT ( 'NONE',  ( -0.8182917201112819283, 0.000000000000000000, -0.3543307086614175816 ) ) ;
#13076=EDGE_CURVE ( 'NONE', #30686, #25226, #5073, .T. ) ;
#13078=EDGE_LOOP ( 'NONE', ( #34185, #10480, #45079, #17835 ) ) ;
#13079=LINE ( 'NONE', #29837, #14970 ) ;
#13080=LINE ( 'NONE', #8433, #39300 ) ;
#13081=ORIENTED_EDGE ( 'NONE', *, *, #15344, .T. ) ;
#13082=DIRECTION ( 'NONE',  ( -1.000000000000000000, 0.000000000000000000, 0.000000000000000000 ) ) ;
#13083=VECTOR ( 'NONE', #15178, 39.37007874015748143 ) ;
#13084=DIRECTION ( 'NONE',  ( -1.000000000000000000, 0.000000000000000000, -0.000000000000000000 ) ) ;
#13086=ORIENTED_EDGE ( 'NONE', *, *, #17981, .F. ) ;
#13087=VECTOR ( 'NONE', #3614, 39.37007874015748143 ) ;
#13088=LINE ( 'NONE', #8186, #14193 ) ;
#13089=ORIENTED_EDGE ( 'NONE', *, *, #19206, .F. ) ;
#13090=FACE_BOUND ( 'NONE', #6563, .T. ) ;
#13091=DIRECTION ( 'NONE',  ( 1.734723475976806848E-16, 0.000000000000000000, 1.000000000000000000 ) ) ;
#13092=VECTOR ( 'NONE', #1145, 39.37007874015748143 ) ;
#13093=CARTESIAN_POINT ( 'NONE',  ( -1.741553095960963734E-16, 3.267716535433071279, 3.021113040223572790E-32 ) ) ;
#13094=DIRECTION ( 'NONE',  ( 0.000000000000000000, -1.000000000000000000, 0.000000000000000000 ) ) ;
#13095=AXIS2_PLACEMENT_3D ( 'NONE', #40434, #31923, #28797 ) ;
#13098=CARTESIAN_POINT ( 'NONE',  ( -0.5455278134075214336, 0.000000000000000000, 2.204724409448808764 ) ) ;
#13099=ORIENTED_EDGE ( 'NONE', *, *, #15765, .F. ) ;
#13100=VECTOR ( 'NONE', #15916, 39.37007874015748143 ) ;
#13101=DIRECTION ( 'NONE',  ( 1.000000000000000000, -0.000000000000000000, 0.000000000000000000 ) ) ;
#13102=VERTEX_POINT ( 'NONE', #44306 ) ;
#13104=LINE ( 'NONE', #44324, #33888 ) ;
#13105=ORIENTED_EDGE ( 'NONE', *, *, #17426, .T. ) ;
#13106=FACE_OUTER_BOUND ( 'NONE', #35498, .T. ) ;
#13108=DIRECTION ( 'NONE',  ( 1.734723475976806848E-16, -0.000000000000000000, 1.000000000000000000 ) ) ;
#13109=ORIENTED_EDGE ( 'NONE', *, *, #21026, .T. ) ;
#13111=VERTEX_POINT ( 'NONE', #20820 ) ;
#13112=VERTEX_POINT ( 'NONE', #8185 ) ;
#13114=AXIS2_PLACEMENT_3D ( 'NONE', #16974, #32731, #48409 ) ;
#13115=ORIENTED_EDGE ( 'NONE', *, *, #5710, .F. ) ;
#13116=ORIENTED_EDGE ( 'NONE', *, *, #47431, .F. ) ;
#13119=DIRECTION ( 'NONE',  ( -1.000000000000000000, -0.000000000000000000, -0.000000000000000000 ) ) ;
#13120=ORIENTED_EDGE ( 'NONE', *, *, #46694, .T. ) ;
#13122=VECTOR ( 'NONE', #18370, 39.37007874015748143 ) ;
#13123=VECTOR ( 'NONE', #6591, 39.37007874015748143 ) ;
#13124=EDGE_CURVE ( 'NONE', #37873, #24076, #47118, .T. ) ;
#13125=DIRECTION ( 'NONE',  ( -0.000000000000000000, 1.000000000000000000, -0.000000000000000000 ) ) ;
#13128=CARTESIAN_POINT ( 'NONE',  ( 1.363819533518803251, 3.267716535433071279, -2.365849761790805487E-16 ) ) ;
#13131=DIRECTION ( 'NONE',  ( -1.000000000000000000, 0.000000000000000000, -0.000000000000000000 ) ) ;
#13132=VECTOR ( 'NONE', #22286, 39.37007874015748143 ) ;
#13133=DIRECTION ( 'NONE',  ( 0.000000000000000000, 0.000000000000000000, -1.000000000000000000 ) ) ;
#13134=EDGE_CURVE ( 'NONE', #46917, #33096, #23927, .T. ) ;
#13135=DIRECTION ( 'NONE',  ( 1.000000000000000000, -0.000000000000000000, 0.000000000000000000 ) ) ;
#13137=EDGE_LOOP ( 'NONE', ( #49535, #37804, #38985, #50264 ) ) ;
#13138=LINE ( 'NONE', #37144, #36124 ) ;
#13139=EDGE_CURVE ( 'NONE', #24845, #43525, #40194, .T. ) ;
#13140=DIRECTION ( 'NONE',  ( -1.000000000000000000, -0.000000000000000000, -0.000000000000000000 ) ) ;
#13143=EDGE_CURVE ( 'NONE', #14372, #40564, #8438, .T. ) ;
#13145=LINE ( 'NONE', #13653, #19539 ) ;
#13146=EDGE_CURVE ( 'NONE', #45868, #39288, #4824, .T. ) ;
#13149=CARTESIAN_POINT ( 'NONE',  ( 0.2727639067037610499, 0.000000000000000000, 2.047244094488179567 ) ) ;
#13150=CARTESIAN_POINT ( 'NONE',  ( 2.106197740627111514, 3.223484195733438362, -1.279361934207793094 ) ) ;
#13152=ORIENTED_EDGE ( 'NONE', *, *, #32950, .T. ) ;
#13153=DIRECTION ( 'NONE',  ( -0.000000000000000000, 1.000000000000000000, -0.000000000000000000 ) ) ;
#13154=CARTESIAN_POINT ( 'NONE',  ( 1.636583440222563857, 0.000000000000000000, -0.6299212598425181220 ) ) ;
#13156=ORIENTED_EDGE ( 'NONE', *, *, #20729, .F. ) ;
#13157=CARTESIAN_POINT ( 'NONE',  ( 2.378961647330872786, 3.267716535433070391, 0.5584465239797037350 ) ) ;
#13161=CARTESIAN_POINT ( 'NONE',  ( -0.8942052331142547050, 0.000000000000000000, 1.259842519685033357 ) ) ;
#13162=DIRECTION ( 'NONE',  ( 1.734723475976806848E-16, -0.000000000000000000, 1.000000000000000000 ) ) ;
#13163=LINE ( 'NONE', #39304, #27356 ) ;
#13165=CARTESIAN_POINT ( 'NONE',  ( -1.636583440222564301, 3.346456692913386100, -0.6299212598425177889 ) ) ;
#13167=EDGE_LOOP ( 'NONE', ( #30267, #2253, #17066, #15549 ) ) ;
#13168=EDGE_LOOP ( 'NONE', ( #1791, #36235, #26921, #27053 ) ) ;
#13171=FACE_BOUND ( 'NONE', #11889, .T. ) ;
#13172=ORIENTED_EDGE ( 'NONE', *, *, #40482, .T. ) ;
#13175=CARTESIAN_POINT ( 'NONE',  ( -1.195183497228115035E-16, 0.000000000000000000, -0.3149606299212591165 ) ) ;
#13176=VERTEX_POINT ( 'NONE', #19786 ) ;
#13178=CARTESIAN_POINT ( 'NONE',  ( 0.000000000000000000, 3.267716535433071279, 0.000000000000000000 ) ) ;
#13180=ORIENTED_EDGE ( 'NONE', *, *, #7278, .T. ) ;
#13181=VERTEX_POINT ( 'NONE', #31942 ) ;
#13182=ORIENTED_EDGE ( 'NONE', *, *, #23495, .T. ) ;
#13183=CARTESIAN_POINT ( 'NONE',  ( -0.3486774197067339376, 3.267716535433071279, 1.209717811016579078E-16 ) ) ;
#13186=LINE ( 'NONE', #5694, #13526 ) ;
#13187=EDGE_CURVE ( 'NONE', #35330, #39943, #47636, .T. ) ;
#13192=CARTESIAN_POINT ( 'NONE',  ( -0.6214413264104939882, 0.000000000000000000, 1.732283464566921172 ) ) ;
#13193=CARTESIAN_POINT ( 'NONE',  ( 0.000000000000000000, 0.000000000000000000, 0.000000000000000000 ) ) ;
#13195=CARTESIAN_POINT ( 'NONE',  ( -1.439733046521777027, 3.267716535433071279, -1.771653543307080581 ) ) ;
#13199=DIRECTION ( 'NONE',  ( -0.000000000000000000, 1.000000000000000000, -0.000000000000000000 ) ) ;
#13202=EDGE_CURVE ( 'NONE', #24291, #16391, #9968, .T. ) ;
#13204=LINE ( 'NONE', #33346, #11860 ) ;
#13205=DIRECTION ( 'NONE',  ( 1.000000000000000000, 0.000000000000000000, 0.000000000000000000 ) ) ;
#13206=AXIS2_PLACEMENT_3D ( 'NONE', #43155, #24062, #306 ) ;
#13207=ORIENTED_EDGE ( 'NONE', *, *, #47657, .F. ) ;
#13209=CARTESIAN_POINT ( 'NONE',  ( 0.000000000000000000, 3.267716535433071279, -0.5118110236220466680 ) ) ;
#13210=CARTESIAN_POINT ( 'NONE',  ( 0.1968503937007870241, 3.346456692913386100, -2.204724409448811429 ) ) ;
#13211=ORIENTED_EDGE ( 'NONE', *, *, #29110, .F. ) ;
#13213=LINE ( 'NONE', #21464, #47642 ) ;
#13216=CARTESIAN_POINT ( 'NONE',  ( -0.07591351300297284610, 3.267716535433071279, 0.9055118110236167750 ) ) ;
#13217=EDGE_CURVE ( 'NONE', #11147, #22241, #24949, .T. ) ;
#13218=CARTESIAN_POINT ( 'NONE',  ( -1.909347346926324906, 0.000000000000000000, -0.6692913385826758654 ) ) ;
#13220=VERTEX_POINT ( 'NONE', #1967 ) ;
#13223=DIRECTION ( 'NONE',  ( -0.000000000000000000, 0.000000000000000000, 1.000000000000000000 ) ) ;
#13225=EDGE_CURVE ( 'NONE', #49804, #27786, #25711, .T. ) ;
#13227=EDGE_LOOP ( 'NONE', ( #15513, #42523, #265, #38423 ) ) ;
#13228=DIRECTION ( 'NONE',  ( 1.734723475976806848E-16, -0.000000000000000000, 1.000000000000000000 ) ) ;
#13232=EDGE_LOOP ( 'NONE', ( #29248, #41686, #13432, #48802 ) ) ;
#13233=VECTOR ( 'NONE', #19442, 39.37007874015748143 ) ;
#13239=CARTESIAN_POINT ( 'NONE',  ( -0.2727639067037607723, 0.000000000000000000, -0.4724409448818883694 ) ) ;
#13240=CARTESIAN_POINT ( 'NONE',  ( 1.363819533518803251, 3.267716535433071279, -0.6692913385826764205 ) ) ;
#13241=EDGE_LOOP ( 'NONE', ( #24345, #7431, #1146, #15564 ) ) ;
#13242=ORIENTED_EDGE ( 'NONE', *, *, #14068, .F. ) ;
#13243=VECTOR ( 'NONE', #43607, 39.37007874015748143 ) ;
#13244=LINE ( 'NONE', #43690, #28728 ) ;
#13246=PLANE ( 'NONE',  #50247 ) ;
#13247=DIRECTION ( 'NONE',  ( 0.000000000000000000, -1.000000000000000000, 0.000000000000000000 ) ) ;
#13249=VERTEX_POINT ( 'NONE', #33480 ) ;
#13253=CARTESIAN_POINT ( 'NONE',  ( 0.000000000000000000, 3.267716535433071279, 0.7874015748031456541 ) ) ;
#13254=CARTESIAN_POINT ( 'NONE',  ( -0.2727639067037605503, 3.267716535433071279, 4.731699523581609125E-17 ) ) ;
#13256=EDGE_CURVE ( 'NONE', #49170, #33914, #37859, .T. ) ;
#13258=LINE ( 'NONE', #25377, #8106 ) ;
#13260=ADVANCED_FACE ( 'NONE', ( #49418 ), #9718, .F. ) ;
#13261=DIRECTION ( 'NONE',  ( 1.734723475976806848E-16, -0.000000000000000000, 1.000000000000000000 ) ) ;
#13262=CARTESIAN_POINT ( 'NONE',  ( 1.363819533518803251, 3.267716535433071279, -2.365849761790805487E-16 ) ) ;
#13265=VECTOR ( 'NONE', #13135, 39.37007874015748143 ) ;
#13268=VECTOR ( 'NONE', #42670, 39.37007874015748143 ) ;
#13269=CARTESIAN_POINT ( 'NONE',  ( -1.909347346926324462, 0.000000000000000000, 0.2755905511810996522 ) ) ;
#13270=DIRECTION ( 'NONE',  ( 1.000000000000000000, -0.000000000000000000, 0.000000000000000000 ) ) ;
#13272=CARTESIAN_POINT ( 'NONE',  ( 1.909347346926324684, 0.000000000000000000, 0.5905511811023582691 ) ) ;
#13274=VERTEX_POINT ( 'NONE', #21078 ) ;
#13275=LINE ( 'NONE', #29007, #42810 ) ;
#13278=ORIENTED_EDGE ( 'NONE', *, *, #31878, .F. ) ;
#13279=CARTESIAN_POINT ( 'NONE',  ( -2.082617625631827174, 3.267716535433071279, -0.3149606299212589500 ) ) ;
#13280=CARTESIAN_POINT ( 'NONE',  ( -1.636583440222563635, 0.000000000000000000, -4.780733988912460139E-16 ) ) ;
#13282=FACE_OUTER_BOUND ( 'NONE', #14231, .T. ) ;
#13284=CARTESIAN_POINT ( 'NONE',  ( -1.909347346926324462, 3.267716535433071279, 3.312189666507127188E-16 ) ) ;
#13285=EDGE_LOOP ( 'NONE', ( #49756, #22932, #2439, #15571 ) ) ;
#13286=VERTEX_POINT ( 'NONE', #17209 ) ;
#13288=LINE ( 'NONE', #17160, #38647 ) ;
#13289=EDGE_CURVE ( 'NONE', #7776, #22612, #44808, .T. ) ;
#13290=ORIENTED_EDGE ( 'NONE', *, *, #50604, .T. ) ;
#13291=DIRECTION ( 'NONE',  ( -0.000000000000000000, 1.000000000000000000, -0.000000000000000000 ) ) ;
#13292=CARTESIAN_POINT ( 'NONE',  ( 0.000000000000000000, 3.267716535433071279, -1.141732283464563791 ) ) ;
#13293=DIRECTION ( 'NONE',  ( -3.469446951953613696E-16, 0.000000000000000000, -1.000000000000000000 ) ) ;
#13294=B_SPLINE_CURVE_WITH_KNOTS ( 'NONE', 3,
 ( #14180, #14439, #12024, #11515 ),
 .UNSPECIFIED., .F., .F.,
 ( 4, 4 ),
 ( 0.02644966475140674358, 0.02714458517981072419 ),
 .UNSPECIFIED. ) ;
#13295=CARTESIAN_POINT ( 'NONE',  ( 0.000000000000000000, 3.346456692913386100, 0.000000000000000000 ) ) ;
#13296=ORIENTED_EDGE ( 'NONE', *, *, #47739, .T. ) ;
#13298=CARTESIAN_POINT ( 'NONE',  ( -1.636583440222563635, 3.346456692913386100, 0.3149606299212578953 ) ) ;
#13299=LINE ( 'NONE', #10181, #6854 ) ;
#13300=CARTESIAN_POINT ( 'NONE',  ( -0.3486774197067339376, 3.346456692913386100, 0.3149606299212577287 ) ) ;
#13301=VERTEX_POINT ( 'NONE', #5585 ) ;
#13302=CARTESIAN_POINT ( 'NONE',  ( 1.953585199828835606, 3.346456692913386100, -0.7874015748031474304 ) ) ;
#13303=FACE_BOUND ( 'NONE', #32336, .T. ) ;
#13304=VERTEX_POINT ( 'NONE', #21337 ) ;
#13305=DIRECTION ( 'NONE',  ( 1.000000000000000000, -0.000000000000000000, 0.000000000000000000 ) ) ;
#13307=EDGE_LOOP ( 'NONE', ( #28269, #49538, #42739, #23995 ) ) ;
#13308=CARTESIAN_POINT ( 'NONE',  ( -0.6214413264104939882, 3.267716535433071279, 0.5905511811023582691 ) ) ;
#13310=AXIS2_PLACEMENT_3D ( 'NONE', #48420, #9225, #37112 ) ;
#13311=ORIENTED_EDGE ( 'NONE', *, *, #31051, .F. ) ;
#13313=DIRECTION ( 'NONE',  ( -0.000000000000000000, 1.000000000000000000, -0.000000000000000000 ) ) ;
#13317=DIRECTION ( 'NONE',  ( -1.000000000000000000, 0.000000000000000000, -0.000000000000000000 ) ) ;
#13319=VECTOR ( 'NONE', #34032, 39.37007874015748143 ) ;
#13320=CARTESIAN_POINT ( 'NONE',  ( -0.8182917201112819283, 0.000000000000000000, -0.7874015748031467643 ) ) ;
#13321=EDGE_CURVE ( 'NONE', #12193, #30195, #33221, .T. ) ;
#13322=DIRECTION ( 'NONE',  ( -0.000000000000000000, 1.000000000000000000, -0.000000000000000000 ) ) ;
#13324=ORIENTED_EDGE ( 'NONE', *, *, #12320, .T. ) ;
#13326=CARTESIAN_POINT ( 'NONE',  ( -0.3486774197067334935, 3.267716535433071279, 0.4330708661417290162 ) ) ;
#13328=EDGE_CURVE ( 'NONE', #10750, #1759, #29327, .T. ) ;
#13329=ORIENTED_EDGE ( 'NONE', *, *, #42519, .F. ) ;
#13330=FACE_OUTER_BOUND ( 'NONE', #47917, .T. ) ;
#13331=CARTESIAN_POINT ( 'NONE',  ( 0.7423782071083084855, 3.346456692913386100, -1.574803149606293529 ) ) ;
#13332=VERTEX_POINT ( 'NONE', #21588 ) ;
#13333=CARTESIAN_POINT ( 'NONE',  ( 0.1968503937007871074, 3.267716535433071279, -6.829619984160646953E-17 ) ) ;
#13334=DIRECTION ( 'NONE',  ( -1.000000000000000000, 0.000000000000000000, -0.000000000000000000 ) ) ;
#13337=CARTESIAN_POINT ( 'NONE',  ( -0.2727639067037602172, 0.000000000000000000, 1.102362204724404160 ) ) ;
#13338=ORIENTED_EDGE ( 'NONE', *, *, #23286, .F. ) ;
#13339=FACE_BOUND ( 'NONE', #23314, .T. ) ;
#13340=FACE_OUTER_BOUND ( 'NONE', #15658, .T. ) ;
#13341=VECTOR ( 'NONE', #31603, 39.37007874015748143 ) ;
#13343=CARTESIAN_POINT ( 'NONE',  ( -0.5455278134075217666, 3.240372690294659908, -2.395036701391033862 ) ) ;
#13344=EDGE_CURVE ( 'NONE', #2567, #48435, #18976, .T. ) ;
#13345=CARTESIAN_POINT ( 'NONE',  ( 1.909347346926324684, 3.267716535433071279, -3.312189666507128175E-16 ) ) ;
#13346=AXIS2_PLACEMENT_3D ( 'NONE', #41786, #22672, #41283 ) ;
#13347=EDGE_LOOP ( 'NONE', ( #11051, #33886, #22625, #50738 ) ) ;
#13348=ORIENTED_EDGE ( 'NONE', *, *, #1617, .T. ) ;
#13349=DIRECTION ( 'NONE',  ( 1.000000000000000000, 0.000000000000000000, -3.469446951953613696E-16 ) ) ;
#13350=ORIENTED_EDGE ( 'NONE', *, *, #18421, .T. ) ;
#13351=ADVANCED_FACE ( 'NONE', ( #7610 ), #6853, .F. ) ;
#13352=AXIS2_PLACEMENT_3D ( 'NONE', #8975, #36090, #1481 ) ;
#13354=EDGE_LOOP ( 'NONE', ( #32537, #39516, #24268, #1586 ) ) ;
#13356=VECTOR ( 'NONE', #19151, 39.37007874015748143 ) ;
#13357=EDGE_LOOP ( 'NONE', ( #28551, #48967, #26198, #19905 ) ) ;
#13358=LINE ( 'NONE', #41991, #31535 ) ;
#13359=LINE ( 'NONE', #9484, #20693 ) ;
#13361=DIRECTION ( 'NONE',  ( 1.000000000000000000, 0.000000000000000000, 0.000000000000000000 ) ) ;
#13363=EDGE_LOOP ( 'NONE', ( #18816, #11466, #44015, #18736 ) ) ;
#13366=ORIENTED_EDGE ( 'NONE', *, *, #37683, .T. ) ;
#13367=CARTESIAN_POINT ( 'NONE',  ( 0.7423782071083087075, 3.267716535433071279, -2.575641807848710194E-16 ) ) ;
#13368=EDGE_LOOP ( 'NONE', ( #31237, #18701, #3301, #5286 ) ) ;
#13369=CARTESIAN_POINT ( 'NONE',  ( 0.8182917201112817063, 0.000000000000000000, -1.417322834645664331 ) ) ;
#13373=DIRECTION ( 'NONE',  ( -1.000000000000000000, 0.000000000000000000, -0.000000000000000000 ) ) ;
#13374=ORIENTED_EDGE ( 'NONE', *, *, #41782, .F. ) ;
#13375=VECTOR ( 'NONE', #13410, 39.37007874015748143 ) ;
#13376=PLANE ( 'NONE',  #39305 ) ;
#13378=ORIENTED_EDGE ( 'NONE', *, *, #32735, .F. ) ;
#13381=DIRECTION ( 'NONE',  ( -0.000000000000000000, 0.000000000000000000, 1.000000000000000000 ) ) ;
#13382=CARTESIAN_POINT ( 'NONE',  ( 0.4696143004045479352, 0.000000000000000000, 0.1574803149606283648 ) ) ;
#13383=ADVANCED_FACE ( 'NONE', ( #15104 ), #34481, .F. ) ;
#13384=VECTOR ( 'NONE', #4688, 39.37007874015748143 ) ;
#13385=DIRECTION ( 'NONE',  ( 0.000000000000000000, 0.000000000000000000, -1.000000000000000000 ) ) ;
#13386=ADVANCED_FACE ( 'NONE', ( #30860 ), #22354, .F. ) ;
#13388=CARTESIAN_POINT ( 'NONE',  ( -1.712496953225537633, 3.267716535433071279, 1.325184350462985883 ) ) ;
#13389=ADVANCED_FACE ( 'NONE', ( #10478 ), #14348, .F. ) ;
#13390=CARTESIAN_POINT ( 'NONE',  ( -0.07591351300297340121, 3.267716535433071279, -0.6692913385826758654 ) ) ;
#13392=CARTESIAN_POINT ( 'NONE',  ( 2.069629837364519886, 3.267716535433071279, -1.299212598425194320 ) ) ;
#13393=ORIENTED_EDGE ( 'NONE', *, *, #26298, .F. ) ;
#13394=DIRECTION ( 'NONE',  ( 0.000000000000000000, 1.000000000000000000, 0.000000000000000000 ) ) ;
#13395=CARTESIAN_POINT ( 'NONE',  ( 0.5455278134075217666, 0.000000000000000000, 1.889763779527550369 ) ) ;
#13396=CARTESIAN_POINT ( 'NONE',  ( 0.000000000000000000, 3.267716535433071279, 0.4330708661417290162 ) ) ;
#13397=DIRECTION ( 'NONE',  ( 0.000000000000000000, 0.000000000000000000, -1.000000000000000000 ) ) ;
#13398=EDGE_CURVE ( 'NONE', #2602, #48050, #50415, .T. ) ;
#13401=CARTESIAN_POINT ( 'NONE',  ( 0.5455278134075211005, 3.267716535433071279, -9.463399047163219482E-17 ) ) ;
#13402=FACE_BOUND ( 'NONE', #29833, .T. ) ;
#13403=VERTEX_POINT ( 'NONE', #19221 ) ;
#13405=ORIENTED_EDGE ( 'NONE', *, *, #26204, .T. ) ;
#13406=DIRECTION ( 'NONE',  ( -1.000000000000000000, 0.000000000000000000, -0.000000000000000000 ) ) ;
#13409=EDGE_CURVE ( 'NONE', #16156, #4725, #42958, .T. ) ;
#13410=DIRECTION ( 'NONE',  ( 1.734723475976806848E-16, -0.000000000000000000, 1.000000000000000000 ) ) ;
#13412=CARTESIAN_POINT ( 'NONE',  ( -1.363819533518803029, 3.267716535433071279, 1.102362204724404160 ) ) ;
#13413=VERTEX_POINT ( 'NONE', #11488 ) ;
#13415=DIRECTION ( 'NONE',  ( -0.000000000000000000, 1.000000000000000000, -0.000000000000000000 ) ) ;
#13416=AXIS2_PLACEMENT_3D ( 'NONE', #32613, #849, #48047 ) ;
#13418=FACE_BOUND ( 'NONE', #37453, .T. ) ;
#13419=VERTEX_POINT ( 'NONE', #41971 ) ;
#13423=DIRECTION ( 'NONE',  ( 1.000000000000000000, 0.000000000000000000, 0.000000000000000000 ) ) ;
#13424=DIRECTION ( 'NONE',  ( -3.469446951953613696E-16, 0.000000000000000000, -1.000000000000000000 ) ) ;
#13425=ORIENTED_EDGE ( 'NONE', *, *, #37145, .T. ) ;
#13427=CARTESIAN_POINT ( 'NONE',  ( -0.8182917201112819283, 3.346456692913386100, -2.047244094488181343 ) ) ;
#13429=CARTESIAN_POINT ( 'NONE',  ( 0.1968503937007873017, 0.000000000000000000, -0.6299212598425177889 ) ) ;
#13430=EDGE_CURVE ( 'NONE', #18373, #23227, #34983, .T. ) ;
#13431=ORIENTED_EDGE ( 'NONE', *, *, #3585, .F. ) ;
#13432=ORIENTED_EDGE ( 'NONE', *, *, #43544, .F. ) ;
#13434=EDGE_CURVE ( 'NONE', #19538, #28015, #10979, .T. ) ;
#13435=DIRECTION ( 'NONE',  ( 1.000000000000000000, 0.000000000000000000, -3.469446951953613696E-16 ) ) ;
#13437=DIRECTION ( 'NONE',  ( -1.000000000000000000, 0.000000000000000000, 1.734723475976806848E-16 ) ) ;
#13438=LINE ( 'NONE', #9565, #39528 ) ;
#13439=EDGE_LOOP ( 'NONE', ( #24708, #10887, #47350, #15561 ) ) ;
#13440=ORIENTED_EDGE ( 'NONE', *, *, #43095, .T. ) ;
#13441=CARTESIAN_POINT ( 'NONE',  ( 1.363819533518803029, 0.000000000000000000, -1.732283464566923170 ) ) ;
#13447=EDGE_CURVE ( 'NONE', #23374, #3253, #42718, .T. ) ;
#13450=EDGE_CURVE ( 'NONE', #5207, #3630, #2725, .T. ) ;
#13454=CARTESIAN_POINT ( 'NONE',  ( -1.091055626815042201, 3.346456692913386100, 0.4330708661417290162 ) ) ;
#13456=ORIENTED_EDGE ( 'NONE', *, *, #4411, .F. ) ;
#13458=ORIENTED_EDGE ( 'NONE', *, *, #38599, .F. ) ;
#13459=VECTOR ( 'NONE', #44853, 39.37007874015748143 ) ;
#13460=CARTESIAN_POINT ( 'NONE',  ( 1.909347346926324684, 3.267716535433071279, 0.4724409448818868706 ) ) ;
#13461=DIRECTION ( 'NONE',  ( 1.000000000000000000, 0.000000000000000000, -3.469446951953613696E-16 ) ) ;
#13462=EDGE_LOOP ( 'NONE', ( #9380, #1511, #45440, #2681 ) ) ;
#13464=ORIENTED_EDGE ( 'NONE', *, *, #22081, .T. ) ;
#13465=DIRECTION ( 'NONE',  ( -0.000000000000000000, 0.000000000000000000, 1.000000000000000000 ) ) ;
#13466=VERTEX_POINT ( 'NONE', #31111 ) ;
#13468=DIRECTION ( 'NONE',  ( -3.469446951953613696E-16, 0.000000000000000000, -1.000000000000000000 ) ) ;
#13473=DIRECTION ( 'NONE',  ( 1.000000000000000000, 0.000000000000000000, 0.000000000000000000 ) ) ;
#13475=ORIENTED_EDGE ( 'NONE', *, *, #36811, .F. ) ;
#13476=CARTESIAN_POINT ( 'NONE',  ( -0.07591351300297333182, 0.000000000000000000, 0.1574803149606283648 ) ) ;
#13477=DIRECTION ( 'NONE',  ( -0.000000000000000000, -1.000000000000000000, -0.000000000000000000 ) ) ;
#13479=ADVANCED_FACE ( 'NONE', ( #38357 ), #33831, .F. ) ;
#13480=VERTEX_POINT ( 'NONE', #14453 ) ;
#13481=EDGE_CURVE ( 'NONE', #26976, #2475, #17560, .T. ) ;
#13482=DIRECTION ( 'NONE',  ( 0.000000000000000000, 0.000000000000000000, 1.000000000000000000 ) ) ;
#13484=DIRECTION ( 'NONE',  ( 1.734723475976806848E-16, -0.000000000000000000, 1.000000000000000000 ) ) ;
#13485=EDGE_CURVE ( 'NONE', #42097, #38291, #29943, .T. ) ;
#13488=VECTOR ( 'NONE', #28130, 39.37007874015748143 ) ;
#13489=DIRECTION ( 'NONE',  ( -0.000000000000000000, 1.000000000000000000, -0.000000000000000000 ) ) ;
#13490=DIRECTION ( 'NONE',  ( 1.734723475976806848E-16, -0.000000000000000000, 1.000000000000000000 ) ) ;
#13491=ORIENTED_EDGE ( 'NONE', *, *, #44186, .F. ) ;
#13492=VECTOR ( 'NONE', #37598, 39.37007874015748143 ) ;
#13495=CIRCLE ( 'NONE', #5231, 2.106299212598425008 ) ;
#13497=PLANE ( 'NONE',  #38763 ) ;
#13499=CARTESIAN_POINT ( 'NONE',  ( -1.439733046521776583, 3.267716535433071279, -1.259842519685034468 ) ) ;
#13500=VERTEX_POINT ( 'NONE', #25814 ) ;
#13502=VECTOR ( 'NONE', #30594, 39.37007874015748143 ) ;
#13503=DIRECTION ( 'NONE',  ( -1.000000000000000000, 0.000000000000000000, -0.000000000000000000 ) ) ;
#13504=ORIENTED_EDGE ( 'NONE', *, *, #5334, .T. ) ;
#13508=ADVANCED_FACE ( 'NONE', ( #17311 ), #30197, .F. ) ;
#13509=ADVANCED_FACE ( 'NONE', ( #2322 ), #6453, .F. ) ;
#13511=DIRECTION ( 'NONE',  ( -3.469446951953613696E-16, 0.000000000000000000, -1.000000000000000000 ) ) ;
#13513=ORIENTED_EDGE ( 'NONE', *, *, #24415, .T. ) ;
#13514=ADVANCED_FACE ( 'NONE', ( #37956 ), #33323, .F. ) ;
#13516=EDGE_CURVE ( 'NONE', #21275, #12193, #10071, .T. ) ;
#13517=LINE ( 'NONE', #21005, #48738 ) ;
#13518=ORIENTED_EDGE ( 'NONE', *, *, #29050, .T. ) ;
#13519=LINE ( 'NONE', #21263, #35605 ) ;
#13521=DIRECTION ( 'NONE',  ( -0.000000000000000000, 1.000000000000000000, -0.000000000000000000 ) ) ;
#13522=ORIENTED_EDGE ( 'NONE', *, *, #21282, .T. ) ;
#13524=CARTESIAN_POINT ( 'NONE',  ( 2.106197740627111514, 0.000000000000000000, -1.102362204724406602 ) ) ;
#13525=VECTOR ( 'NONE', #34955, 39.37007874015748143 ) ;
#13526=VECTOR ( 'NONE', #8791, 39.37007874015748143 ) ;
#13530=CARTESIAN_POINT ( 'NONE',  ( 1.636583440222563857, 0.000000000000000000, 1.259842519685033135 ) ) ;
#13531=EDGE_LOOP ( 'NONE', ( #18080, #30126, #48378, #41374 ) ) ;
#13532=DIRECTION ( 'NONE',  ( -0.000000000000000000, 0.000000000000000000, 1.000000000000000000 ) ) ;
#13533=VECTOR ( 'NONE', #38789, 39.37007874015748143 ) ;
#13535=CARTESIAN_POINT ( 'NONE',  ( 1.287906020515829919, 3.346456692913386100, -1.666671669919371102 ) ) ;
#13536=LINE ( 'NONE', #29271, #41190 ) ;
#13537=CARTESIAN_POINT ( 'NONE',  ( 1.015142113812069535, 3.267716535433071279, -3.521981712565032882E-16 ) ) ;
#13538=DIRECTION ( 'NONE',  ( 1.734723475976806848E-16, -0.000000000000000000, 1.000000000000000000 ) ) ;
#13539=EDGE_LOOP ( 'NONE', ( #7937, #43437, #7961, #28212 ) ) ;
#13540=ORIENTED_EDGE ( 'NONE', *, *, #26473, .T. ) ;
#13541=LINE ( 'NONE', #29541, #28987 ) ;
#13542=VECTOR ( 'NONE', #41584, 39.37007874015748143 ) ;
#13543=CARTESIAN_POINT ( 'NONE',  ( -0.3486774197067334935, 0.000000000000000000, 0.4330708661417290162 ) ) ;
#13544=VERTEX_POINT ( 'NONE', #37446 ) ;
#13545=CARTESIAN_POINT ( 'NONE',  ( 1.287906020515830141, 0.000000000000000000, -0.3149606299212596716 ) ) ;
#13546=DIRECTION ( 'NONE',  ( -3.469446951953613696E-16, 0.000000000000000000, -1.000000000000000000 ) ) ;
#13548=EDGE_LOOP ( 'NONE', ( #4977, #12077, #35369, #46918 ) ) ;
#13549=ORIENTED_EDGE ( 'NONE', *, *, #2147, .T. ) ;
#13550=ADVANCED_FACE ( 'NONE', ( #18075 ), #45914, .F. ) ;
#13551=DIRECTION ( 'NONE',  ( -1.000000000000000000, 0.000000000000000000, 1.734723475976806848E-16 ) ) ;
#13552=DIRECTION ( 'NONE',  ( -1.000000000000000000, 0.000000000000000000, 0.000000000000000000 ) ) ;
#13554=VERTEX_POINT ( 'NONE', #49511 ) ;
#13555=CARTESIAN_POINT ( 'NONE',  ( 1.833433833923351353, 0.000000000000000000, 1.574803149606291974 ) ) ;
#13557=FACE_BOUND ( 'NONE', #43192, .T. ) ;
#13558=EDGE_LOOP ( 'NONE', ( #391, #13522, #32776, #4201 ) ) ;
#13560=ORIENTED_EDGE ( 'NONE', *, *, #24911, .T. ) ;
#13561=ORIENTED_EDGE ( 'NONE', *, *, #47358, .F. ) ;
#13562=LINE ( 'NONE', #21559, #11847 ) ;
#13563=ORIENTED_EDGE ( 'NONE', *, *, #42014, .F. ) ;
#13564=DIRECTION ( 'NONE',  ( -1.000000000000000000, 0.000000000000000000, 1.734723475976806848E-16 ) ) ;
#13566=VERTEX_POINT ( 'NONE', #41819 ) ;
#13568=VECTOR ( 'NONE', #6837, 39.37007874015748143 ) ;
#13569=VECTOR ( 'NONE', #28052, 39.37007874015748143 ) ;
#13570=EDGE_CURVE ( 'NONE', #28950, #5726, #18321, .T. ) ;
#13573=CARTESIAN_POINT ( 'NONE',  ( -0.2727639067037602172, 0.000000000000000000, 1.417322834645662777 ) ) ;
#13575=AXIS2_PLACEMENT_3D ( 'NONE', #32455, #44305, #13084 ) ;
#13579=DIRECTION ( 'NONE',  ( 0.000000000000000000, 0.000000000000000000, -1.000000000000000000 ) ) ;
#13581=AXIS2_PLACEMENT_3D ( 'NONE', #35100, #491, #7478 ) ;
#13584=EDGE_CURVE ( 'NONE', #20129, #9823, #9562, .T. ) ;
#13585=EDGE_CURVE ( 'NONE', #14008, #7984, #45154, .T. ) ;
#13588=CARTESIAN_POINT ( 'NONE',  ( 1.363819533518803029, 0.000000000000000000, -1.417322834645665219 ) ) ;
#13589=FACE_OUTER_BOUND ( 'NONE', #40339, .T. ) ;
#13590=ORIENTED_EDGE ( 'NONE', *, *, #29590, .T. ) ;
#13591=LINE ( 'NONE', #22100, #26319 ) ;
#13592=LINE ( 'NONE', #29591, #10171 ) ;
#13594=VERTEX_POINT ( 'NONE', #41312 ) ;
#13596=ORIENTED_EDGE ( 'NONE', *, *, #47759, .T. ) ;
#13597=FACE_BOUND ( 'NONE', #2627, .T. ) ;
#13599=PLANE ( 'NONE',  #7846 ) ;
#13600=LINE ( 'NONE', #29337, #40025 ) ;
#13601=ORIENTED_EDGE ( 'NONE', *, *, #22064, .F. ) ;
#13602=EDGE_LOOP ( 'NONE', ( #20185, #34681, #34601, #10275 ) ) ;
#13604=CARTESIAN_POINT ( 'NONE',  ( -0.2727639067037602172, 3.346456692913386100, 1.102362204724404160 ) ) ;
#13605=ORIENTED_EDGE ( 'NONE', *, *, #23574, .T. ) ;
#13606=VECTOR ( 'NONE', #44664, 39.37007874015748143 ) ;
#13607=LINE ( 'NONE', #36081, #42566 ) ;
#13608=EDGE_LOOP ( 'NONE', ( #31778, #23515, #11870, #17844 ) ) ;
#13609=AXIS2_PLACEMENT_3D ( 'NONE', #27734, #4247, #19981 ) ;
#13610=DIRECTION ( 'NONE',  ( 0.000000000000000000, -1.000000000000000000, 0.000000000000000000 ) ) ;
#13611=ORIENTED_EDGE ( 'NONE', *, *, #29777, .T. ) ;
#13612=CARTESIAN_POINT ( 'NONE',  ( 0.8182917201112824834, 3.346456692913386100, 2.047244094488179567 ) ) ;
#13616=EDGE_LOOP ( 'NONE', ( #12881, #43457, #43141, #41683 ) ) ;
#13618=CARTESIAN_POINT ( 'NONE',  ( 0.000000000000000000, 3.267716535433071279, 0.000000000000000000 ) ) ;
#13619=ORIENTED_EDGE ( 'NONE', *, *, #4896, .F. ) ;
#13620=EDGE_LOOP ( 'NONE', ( #18277, #38388, #40730, #5093 ) ) ;
#13621=EDGE_CURVE ( 'NONE', #1816, #46637, #27066, .T. ) ;
#13622=ORIENTED_EDGE ( 'NONE', *, *, #13134, .F. ) ;
#13623=ORIENTED_EDGE ( 'NONE', *, *, #44828, .F. ) ;
#13624=DIRECTION ( 'NONE',  ( 0.000000000000000000, 0.000000000000000000, -1.000000000000000000 ) ) ;
#13625=ORIENTED_EDGE ( 'NONE', *, *, #33669, .F. ) ;
#13626=CARTESIAN_POINT ( 'NONE',  ( 2.378961647330872786, 3.267716535433071279, -0.5118110236220471121 ) ) ;
#13627=ORIENTED_EDGE ( 'NONE', *, *, #40719, .F. ) ;
#13630=LINE ( 'NONE', #6395, #42869 ) ;
#13631=ORIENTED_EDGE ( 'NONE', *, *, #21032, .T. ) ;
#13632=DIRECTION ( 'NONE',  ( 1.000000000000000000, 0.000000000000000000, -3.469446951953613696E-16 ) ) ;
#13633=CARTESIAN_POINT ( 'NONE',  ( -0.6214413264104945434, 3.267716535433071279, -1.102362204724405492 ) ) ;
#13634=VECTOR ( 'NONE', #16173, 39.37007874015748143 ) ;
#13637=CARTESIAN_POINT ( 'NONE',  ( -1.166969139818016199, 3.346456692913386100, 1.850393700787392293 ) ) ;
#13640=CARTESIAN_POINT ( 'NONE',  ( 1.363819533518803029, 3.267716535433071279, -1.929133858267710666 ) ) ;
#13641=VECTOR ( 'NONE', #35174, 39.37007874015748143 ) ;
#13644=DIRECTION ( 'NONE',  ( 0.000000000000000000, -1.000000000000000000, 0.000000000000000000 ) ) ;
#13645=EDGE_LOOP ( 'NONE', ( #47319, #26225, #29942, #9730 ) ) ;
#13646=FACE_OUTER_BOUND ( 'NONE', #19555, .T. ) ;
#13647=DIRECTION ( 'NONE',  ( 0.000000000000000000, 0.000000000000000000, -1.000000000000000000 ) ) ;
#13648=VECTOR ( 'NONE', #35747, 39.37007874015748143 ) ;
#13649=ORIENTED_EDGE ( 'NONE', *, *, #4933, .T. ) ;
#13652=EDGE_CURVE ( 'NONE', #33364, #27812, #7213, .T. ) ;
#13653=CARTESIAN_POINT ( 'NONE',  ( 0.5455278134075217666, 3.346456692913386100, 1.889763779527550369 ) ) ;
#13655=DIRECTION ( 'NONE',  ( -0.000000000000000000, 1.000000000000000000, -0.000000000000000000 ) ) ;
#13657=CARTESIAN_POINT ( 'NONE',  ( 0.000000000000000000, 3.267716535433071279, 1.259842519685033357 ) ) ;
#13658=ORIENTED_EDGE ( 'NONE', *, *, #2140, .T. ) ;
#13659=DIRECTION ( 'NONE',  ( 0.000000000000000000, 0.000000000000000000, -1.000000000000000000 ) ) ;
#13662=VERTEX_POINT ( 'NONE', #34827 ) ;
#13663=DIRECTION ( 'NONE',  ( -0.000000000000000000, 1.000000000000000000, -0.000000000000000000 ) ) ;
#13664=DIRECTION ( 'NONE',  ( 1.000000000000000000, 0.000000000000000000, 0.000000000000000000 ) ) ;
#13665=ORIENTED_EDGE ( 'NONE', *, *, #50257, .F. ) ;
#13667=CARTESIAN_POINT ( 'NONE',  ( 0.8182917201112819283, 0.000000000000000000, 0.2755905511810994302 ) ) ;
#13668=CARTESIAN_POINT ( 'NONE',  ( 0.000000000000000000, 3.267716535433071279, 0.1181102362204704270 ) ) ;
#13671=ADVANCED_FACE ( 'NONE', ( #3081 ), #30957, .F. ) ;
#13672=ORIENTED_EDGE ( 'NONE', *, *, #46798, .T. ) ;
#13673=VECTOR ( 'NONE', #36617, 39.37007874015748143 ) ;
#13674=LINE ( 'NONE', #9286, #18577 ) ;
#13675=DIRECTION ( 'NONE',  ( 1.734723475976806848E-16, -0.000000000000000000, 1.000000000000000000 ) ) ;
#13676=FACE_BOUND ( 'NONE', #17994, .T. ) ;
#13678=ADVANCED_FACE ( 'NONE', ( #31209 ), #22955, .F. ) ;
#13680=DIRECTION ( 'NONE',  ( -0.000000000000000000, 1.000000000000000000, -0.000000000000000000 ) ) ;
#13682=AXIS2_PLACEMENT_3D ( 'NONE', #42610, #34874, #19360 ) ;
#13683=EDGE_CURVE ( 'NONE', #26431, #26163, #51017, .T. ) ;
#13684=EDGE_LOOP ( 'NONE', ( #36840, #39769, #12093, #7857 ) ) ;
#13690=ORIENTED_EDGE ( 'NONE', *, *, #49585, .T. ) ;
#13692=CARTESIAN_POINT ( 'NONE',  ( 1.761123562704338452, 3.346456692913386100, 1.259842519685033135 ) ) ;
#13693=DIRECTION ( 'NONE',  ( -0.000000000000000000, 0.000000000000000000, 1.000000000000000000 ) ) ;
#13694=EDGE_CURVE ( 'NONE', #9041, #30555, #16993, .T. ) ;
#13695=PLANE ( 'NONE',  #9392 ) ;
#13696=CARTESIAN_POINT ( 'NONE',  ( 1.687984952120843207, 3.346456692913386100, -1.259842519685035800 ) ) ;
#13697=VERTEX_POINT ( 'NONE', #15707 ) ;
#13698=VERTEX_POINT ( 'NONE', #26568 ) ;
#13699=DIRECTION ( 'NONE',  ( -0.000000000000000000, 1.000000000000000000, -0.000000000000000000 ) ) ;
#13701=LINE ( 'NONE', #50030, #40660 ) ;
#13702=EDGE_CURVE ( 'NONE', #7345, #36591, #42571, .T. ) ;
#13703=FACE_OUTER_BOUND ( 'NONE', #49601, .T. ) ;
#13704=CARTESIAN_POINT ( 'NONE',  ( 1.015142113812069091, 3.267716535433071279, -2.222792731763669760 ) ) ;
#13705=CARTESIAN_POINT ( 'NONE',  ( -0.5455278134075208785, 3.346456692913386100, 0.9448818897637749625 ) ) ;
#13707=VECTOR ( 'NONE', #25125, 39.37007874015748143 ) ;
#13710=VECTOR ( 'NONE', #13205, 39.37007874015748143 ) ;
#13711=LINE ( 'NONE', #9836, #1149 ) ;
#13712=DIRECTION ( 'NONE',  ( 1.000000000000000000, -0.000000000000000000, 0.000000000000000000 ) ) ;
#13713=AXIS2_PLACEMENT_3D ( 'NONE', #45595, #14387, #24987 ) ;
#13714=ORIENTED_EDGE ( 'NONE', *, *, #19059, .T. ) ;
#13715=EDGE_CURVE ( 'NONE', #31775, #39889, #22704, .T. ) ;
#13716=AXIS2_PLACEMENT_3D ( 'NONE', #40077, #40344, #4713 ) ;
#13717=VERTEX_POINT ( 'NONE', #38211 ) ;
#13719=PLANE ( 'NONE',  #36925 ) ;
#13720=AXIS2_PLACEMENT_3D ( 'NONE', #25358, #26121, #45967 ) ;
#13722=VECTOR ( 'NONE', #17229, 39.37007874015748143 ) ;
#13725=CARTESIAN_POINT ( 'NONE',  ( -0.2727639067037602727, 3.346456692913386100, 1.535433070866133898 ) ) ;
#13726=VERTEX_POINT ( 'NONE', #11582 ) ;
#13727=FACE_OUTER_BOUND ( 'NONE', #33681, .T. ) ;
#13728=CARTESIAN_POINT ( 'NONE',  ( 0.8182917201112824834, 3.346456692913386100, 1.535433070866133898 ) ) ;
#13730=ORIENTED_EDGE ( 'NONE', *, *, #2017, .F. ) ;
#13731=LINE ( 'NONE', #50060, #8205 ) ;
#13733=ORIENTED_EDGE ( 'NONE', *, *, #40138, .T. ) ;
#13734=DIRECTION ( 'NONE',  ( -0.000000000000000000, 1.000000000000000000, -0.000000000000000000 ) ) ;
#13736=CARTESIAN_POINT ( 'NONE',  ( 0.2727639067037604947, 0.000000000000000000, -1.102362204724405714 ) ) ;
#13739=DIRECTION ( 'NONE',  ( -0.000000000000000000, 1.000000000000000000, -0.000000000000000000 ) ) ;
#13740=CARTESIAN_POINT ( 'NONE',  ( -0.6214413264104939882, 3.267716535433071279, 0.9055118110236167750 ) ) ;
#13741=CARTESIAN_POINT ( 'NONE',  ( 2.629403693901861360E-16, 3.267716535433071279, -4.561288315631693258E-32 ) ) ;
#13742=AXIS2_PLACEMENT_3D ( 'NONE', #15160, #18781, #19275 ) ;
#13743=EDGE_CURVE ( 'NONE', #26074, #39122, #4345, .T. ) ;
#13744=ORIENTED_EDGE ( 'NONE', *, *, #3269, .T. ) ;
#13745=LINE ( 'NONE', #9615, #43013 ) ;
#13746=CARTESIAN_POINT ( 'NONE',  ( 0.000000000000000000, 3.267716535433071279, -0.9448818897637765168 ) ) ;
#13748=AXIS2_PLACEMENT_3D ( 'NONE', #50897, #39847, #4480 ) ;
#13751=VERTEX_POINT ( 'NONE', #28083 ) ;
#13752=LINE ( 'NONE', #29495, #12640 ) ;
#13753=CIRCLE ( 'NONE', #12084, 2.952755905511811552 ) ;
#13754=CARTESIAN_POINT ( 'NONE',  ( -4.268512490100411402E-16, 3.267716535433071279, -2.086614173228339641 ) ) ;
#13759=CARTESIAN_POINT ( 'NONE',  ( -0.8942052331142552601, 0.000000000000000000, 1.692913385826762873 ) ) ;
#13761=LINE ( 'NONE', #37008, #38980 ) ;
#13762=LINE ( 'NONE', #13254, #12748 ) ;
#13763=EDGE_CURVE ( 'NONE', #7991, #30461, #4100, .T. ) ;
#13764=DIRECTION ( 'NONE',  ( 0.000000000000000000, -0.9063077870366510469, -0.4226182617406972208 ) ) ;
#13765=PLANE ( 'NONE',  #34315 ) ;
#13767=ORIENTED_EDGE ( 'NONE', *, *, #24462, .F. ) ;
#13768=PLANE ( 'NONE',  #21719 ) ;
#13771=EDGE_CURVE ( 'NONE', #21877, #21738, #20603, .T. ) ;
#13775=DIRECTION ( 'NONE',  ( -0.000000000000000000, 1.000000000000000000, -0.000000000000000000 ) ) ;
#13776=LINE ( 'NONE', #9902, #13132 ) ;
#13777=VERTEX_POINT ( 'NONE', #4602 ) ;
#13779=AXIS2_PLACEMENT_3D ( 'NONE', #49352, #48584, #37277 ) ;
#13780=DIRECTION ( 'NONE',  ( 1.734723475976806848E-16, -0.000000000000000000, 1.000000000000000000 ) ) ;
#13782=VECTOR ( 'NONE', #2769, 39.37007874015748854 ) ;
#13783=EDGE_CURVE ( 'NONE', #1039, #20045, #20346, .T. ) ;
#13785=CARTESIAN_POINT ( 'NONE',  ( 0.5455278134075211005, 0.000000000000000000, -1.456692913385822630 ) ) ;
#13787=VERTEX_POINT ( 'NONE', #8730 ) ;
#13789=EDGE_CURVE ( 'NONE', #552, #22006, #32758, .T. ) ;
#13790=DIRECTION ( 'NONE',  ( 1.000000000000000000, 0.000000000000000000, 0.000000000000000000 ) ) ;
#13791=CARTESIAN_POINT ( 'NONE',  ( 0.4696143004045476022, 3.267716535433071279, -2.113816876263008293 ) ) ;
#13792=LINE ( 'NONE', #13537, #6206 ) ;
#13794=EDGE_LOOP ( 'NONE', ( #6380, #30007, #6182, #43761 ) ) ;
#13795=ORIENTED_EDGE ( 'NONE', *, *, #39296, .F. ) ;
#13796=CARTESIAN_POINT ( 'NONE',  ( -0.07591351300297340121, 3.267716535433071279, -1.929133858267710000 ) ) ;
#13797=DIRECTION ( 'NONE',  ( 1.000000000000000000, 0.000000000000000000, -3.469446951953613696E-16 ) ) ;
#13799=CARTESIAN_POINT ( 'NONE',  ( 1.833433833923351353, 0.000000000000000000, -1.259842519685035800 ) ) ;
#13800=DIRECTION ( 'NONE',  ( -3.469446951953613696E-16, 0.000000000000000000, -1.000000000000000000 ) ) ;
#13802=VECTOR ( 'NONE', #12103, 39.37007874015748143 ) ;
#13803=EDGE_CURVE ( 'NONE', #11723, #38637, #47928, .T. ) ;
#13805=VERTEX_POINT ( 'NONE', #16483 ) ;
#13806=CARTESIAN_POINT ( 'NONE',  ( 0.8182917201112818173, 3.267716535433071279, -1.419509857074483292E-16 ) ) ;
#13807=CARTESIAN_POINT ( 'NONE',  ( -1.439733046521776361, 3.267716535433071279, 0.1181102362204704270 ) ) ;
#13811=LINE ( 'NONE', #2188, #38873 ) ;
#13813=EDGE_LOOP ( 'NONE', ( #6310, #19737, #49868, #12844 ) ) ;
#13814=CARTESIAN_POINT ( 'NONE',  ( 0.000000000000000000, 3.346456692913386100, 0.000000000000000000 ) ) ;
#13815=VERTEX_POINT ( 'NONE', #19823 ) ;
#13818=DIRECTION ( 'NONE',  ( -3.469446951953613696E-16, 0.000000000000000000, -1.000000000000000000 ) ) ;
#13819=AXIS2_PLACEMENT_3D ( 'NONE', #47532, #11949, #24339 ) ;
#13820=VECTOR ( 'NONE', #18911, 39.37007874015748143 ) ;
#13821=ORIENTED_EDGE ( 'NONE', *, *, #45532, .T. ) ;
#13823=DIRECTION ( 'NONE',  ( -0.000000000000000000, 1.000000000000000000, -0.000000000000000000 ) ) ;
#13825=AXIS2_PLACEMENT_3D ( 'NONE', #10964, #11221, #42704 ) ;
#13826=DIRECTION ( 'NONE',  ( -1.000000000000000000, 0.000000000000000000, 0.000000000000000000 ) ) ;
#13827=FACE_OUTER_BOUND ( 'NONE', #49062, .T. ) ;
#13829=DIRECTION ( 'NONE',  ( -0.000000000000000000, 1.000000000000000000, -0.000000000000000000 ) ) ;
#13831=VERTEX_POINT ( 'NONE', #24739 ) ;
#13832=PLANE ( 'NONE',  #42308 ) ;
#13836=LINE ( 'NONE', #48898, #37238 ) ;
#13837=EDGE_CURVE ( 'NONE', #43925, #12716, #47419, .T. ) ;
#13839=ORIENTED_EDGE ( 'NONE', *, *, #1239, .T. ) ;
#13840=FACE_OUTER_BOUND ( 'NONE', #3760, .T. ) ;
#13841=EDGE_CURVE ( 'NONE', #35717, #7477, #12601, .T. ) ;
#13842=LINE ( 'NONE', #33979, #16774 ) ;
#13844=DIRECTION ( 'NONE',  ( 1.734723475976806848E-16, -0.000000000000000000, 1.000000000000000000 ) ) ;
#13846=CARTESIAN_POINT ( 'NONE',  ( 0.5455278134075217666, 3.346456692913386100, 2.095509194042718626 ) ) ;
#13847=ORIENTED_EDGE ( 'NONE', *, *, #49403, .F. ) ;
#13849=FACE_BOUND ( 'NONE', #2494, .T. ) ;
#13852=PLANE ( 'NONE',  #8702 ) ;
#13853=AXIS2_PLACEMENT_3D ( 'NONE', #48847, #13532, #5780 ) ;
#13854=VECTOR ( 'NONE', #13655, 39.37007874015748143 ) ;
#13856=ORIENTED_EDGE ( 'NONE', *, *, #20608, .F. ) ;
#13857=LINE ( 'NONE', #6104, #17206 ) ;
#13858=ORIENTED_EDGE ( 'NONE', *, *, #14474, .T. ) ;
#13859=VECTOR ( 'NONE', #29422, 39.37007874015748143 ) ;
#13861=DIRECTION ( 'NONE',  ( -0.000000000000000000, 0.000000000000000000, 1.000000000000000000 ) ) ;
#13863=LINE ( 'NONE', #18747, #23985 ) ;
#13864=EDGE_CURVE ( 'NONE', #46567, #2988, #44589, .T. ) ;
#13865=ORIENTED_EDGE ( 'NONE', *, *, #2777, .F. ) ;
#13866=DIRECTION ( 'NONE',  ( 1.734723475976806848E-16, 0.000000000000000000, 1.000000000000000000 ) ) ;
#13867=ADVANCED_FACE ( 'NONE', ( #43574 ), #15960, .F. ) ;
#13869=DIRECTION ( 'NONE',  ( 0.000000000000000000, 0.000000000000000000, 1.000000000000000000 ) ) ;
#13873=ORIENTED_EDGE ( 'NONE', *, *, #16214, .F. ) ;
#13874=EDGE_LOOP ( 'NONE', ( #47859, #22654, #11735, #4552 ) ) ;
#13876=ORIENTED_EDGE ( 'NONE', *, *, #41261, .F. ) ;
#13877=VERTEX_POINT ( 'NONE', #16225 ) ;
#13880=DIRECTION ( 'NONE',  ( 1.734723475976806848E-16, -0.000000000000000000, 1.000000000000000000 ) ) ;
#13882=VECTOR ( 'NONE', #2549, 39.37007874015748143 ) ;
#13884=VERTEX_POINT ( 'NONE', #9240 ) ;
#13887=CARTESIAN_POINT ( 'NONE',  ( 1.833433833923351353, 0.000000000000000000, -0.6299212598425181220 ) ) ;
#13890=CARTESIAN_POINT ( 'NONE',  ( 0.000000000000000000, 3.346456692913386100, 0.000000000000000000 ) ) ;
#13891=CARTESIAN_POINT ( 'NONE',  ( 0.000000000000000000, 3.346456692913386100, 0.000000000000000000 ) ) ;
#13892=CARTESIAN_POINT ( 'NONE',  ( -1.091055626815042645, 3.346456692913386100, -0.6299212598425177889 ) ) ;
#13893=VECTOR ( 'NONE', #35427, 39.37007874015748143 ) ;
#13894=CARTESIAN_POINT ( 'NONE',  ( 1.363819533518803251, 0.000000000000000000, 0.7874015748031454320 ) ) ;
#13896=ORIENTED_EDGE ( 'NONE', *, *, #29505, .F. ) ;
#13899=VECTOR ( 'NONE', #17494, 39.37007874015748143 ) ;
#13900=EDGE_CURVE ( 'NONE', #39624, #21917, #17251, .T. ) ;
#13902=ORIENTED_EDGE ( 'NONE', *, *, #4403, .T. ) ;
#13905=AXIS2_PLACEMENT_3D ( 'NONE', #19783, #23155, #3544 ) ;
#13906=ORIENTED_EDGE ( 'NONE', *, *, #17789, .F. ) ;
#13907=DIRECTION ( 'NONE',  ( 1.734723475976806848E-16, -0.000000000000000000, 1.000000000000000000 ) ) ;
#13910=CARTESIAN_POINT ( 'NONE',  ( 0.4696143004045479352, 3.346456692913386100, -0.1574803149606298636 ) ) ;
#13911=VECTOR ( 'NONE', #41008, 39.37007874015748143 ) ;
#13912=CARTESIAN_POINT ( 'NONE',  ( 0.1968503937007877735, 3.346456692913386100, 0.7480314960629874665 ) ) ;
#13913=DIRECTION ( 'NONE',  ( -1.000000000000000000, 0.000000000000000000, -0.000000000000000000 ) ) ;
#13915=DIRECTION ( 'NONE',  ( 1.000000000000000000, 0.000000000000000000, 0.000000000000000000 ) ) ;
#13916=ORIENTED_EDGE ( 'NONE', *, *, #37580, .F. ) ;
#13917=ORIENTED_EDGE ( 'NONE', *, *, #5565, .F. ) ;
#13918=DIRECTION ( 'NONE',  ( -1.000000000000000000, 0.000000000000000000, 1.734723475976806848E-16 ) ) ;
#13919=ORIENTED_EDGE ( 'NONE', *, *, #5408, .T. ) ;
#13920=DIRECTION ( 'NONE',  ( 1.000000000000000000, 0.000000000000000000, 0.000000000000000000 ) ) ;
#13922=VERTEX_POINT ( 'NONE', #5624 ) ;
#13923=DIRECTION ( 'NONE',  ( -0.000000000000000000, 0.000000000000000000, 1.000000000000000000 ) ) ;
#13926=VECTOR ( 'NONE', #39626, 39.37007874015748143 ) ;
#13927=LINE ( 'NONE', #34314, #18315 ) ;
#13930=ORIENTED_EDGE ( 'NONE', *, *, #1374, .F. ) ;
#13931=ADVANCED_FACE ( 'NONE', ( #41754 ), #17750, .F. ) ;
#13932=LINE ( 'NONE', #45899, #31472 ) ;
#13933=FACE_BOUND ( 'NONE', #34671, .T. ) ;
#13934=ORIENTED_EDGE ( 'NONE', *, *, #37123, .T. ) ;
#13935=VECTOR ( 'NONE', #44455, 39.37007874015748143 ) ;
#13938=DIRECTION ( 'NONE',  ( 1.734723475976806848E-16, 0.000000000000000000, 1.000000000000000000 ) ) ;
#13939=ORIENTED_EDGE ( 'NONE', *, *, #4963, .F. ) ;
#13941=LINE ( 'NONE', #18314, #4333 ) ;
#13943=EDGE_LOOP ( 'NONE', ( #31006, #49260, #44187, #27625 ) ) ;
#13944=ORIENTED_EDGE ( 'NONE', *, *, #47759, .F. ) ;
#13947=DIRECTION ( 'NONE',  ( -0.000000000000000000, 0.000000000000000000, 1.000000000000000000 ) ) ;
#13948=CARTESIAN_POINT ( 'NONE',  ( -1.166969139818015533, 3.346456692913386100, 1.102362204724404160 ) ) ;
#13951=ORIENTED_EDGE ( 'NONE', *, *, #18385, .F. ) ;
#13952=ORIENTED_EDGE ( 'NONE', *, *, #11187, .F. ) ;
#13953=LINE ( 'NONE', #18330, #10954 ) ;
#13954=DIRECTION ( 'NONE',  ( -0.000000000000000000, 0.000000000000000000, 1.000000000000000000 ) ) ;
#13955=LINE ( 'NONE', #33840, #43949 ) ;
#13960=DIRECTION ( 'NONE',  ( -3.469446951953613696E-16, 0.000000000000000000, -1.000000000000000000 ) ) ;
#13961=EDGE_CURVE ( 'NONE', #28095, #37439, #37385, .T. ) ;
#13962=ORIENTED_EDGE ( 'NONE', *, *, #17880, .F. ) ;
#13964=CARTESIAN_POINT ( 'NONE',  ( -1.091055626815042645, 3.346456692913386100, 1.801691980386209258 ) ) ;
#13967=EDGE_CURVE ( 'NONE', #21978, #29226, #33257, .T. ) ;
#13968=ORIENTED_EDGE ( 'NONE', *, *, #35313, .T. ) ;
#13970=CARTESIAN_POINT ( 'NONE',  ( -1.363819533518803473, 3.267716535433071279, 2.027638360164056852 ) ) ;
#13971=VERTEX_POINT ( 'NONE', #37639 ) ;
#13972=EDGE_CURVE ( 'NONE', #2567, #47393, #49205, .T. ) ;
#13973=VECTOR ( 'NONE', #38609, 39.37007874015748143 ) ;
#13976=VECTOR ( 'NONE', #27656, 39.37007874015748143 ) ;
#13978=DIRECTION ( 'NONE',  ( 0.000000000000000000, 0.000000000000000000, -1.000000000000000000 ) ) ;
#13979=LINE ( 'NONE', #26601, #18950 ) ;
#13982=VERTEX_POINT ( 'NONE', #29371 ) ;
#13984=VERTEX_POINT ( 'NONE', #30132 ) ;
#13987=DIRECTION ( 'NONE',  ( 1.734723475976806848E-16, -0.000000000000000000, 1.000000000000000000 ) ) ;
#13991=LINE ( 'NONE', #49815, #34532 ) ;
#13993=AXIS2_PLACEMENT_3D ( 'NONE', #10365, #22489, #29979 ) ;
#13994=ADVANCED_FACE ( 'NONE', ( #45096 ), #25492, .F. ) ;
#13995=CARTESIAN_POINT ( 'NONE',  ( 0.000000000000000000, 3.267716535433071279, -1.929133858267710000 ) ) ;
#13996=ORIENTED_EDGE ( 'NONE', *, *, #16264, .F. ) ;
#13998=DIRECTION ( 'NONE',  ( 1.000000000000000000, -0.000000000000000000, 0.000000000000000000 ) ) ;
#14000=VERTEX_POINT ( 'NONE', #9499 ) ;
#14001=VERTEX_POINT ( 'NONE', #2259 ) ;
#14003=EDGE_CURVE ( 'NONE', #32172, #25793, #5874, .T. ) ;
#14005=DIRECTION ( 'NONE',  ( -3.469446951953613696E-16, 0.000000000000000000, -1.000000000000000000 ) ) ;
#14007=DIRECTION ( 'NONE',  ( 1.000000000000000000, 0.000000000000000000, 0.000000000000000000 ) ) ;
#14008=VERTEX_POINT ( 'NONE', #21623 ) ;
#14009=VERTEX_POINT ( 'NONE', #25748 ) ;
#14011=VECTOR ( 'NONE', #2359, 39.37007874015748143 ) ;
#14012=EDGE_LOOP ( 'NONE', ( #38278, #47827, #22291, #16937 ) ) ;
#14015=DIRECTION ( 'NONE',  ( -1.000000000000000000, 0.000000000000000000, 1.734723475976806848E-16 ) ) ;
#14017=CARTESIAN_POINT ( 'NONE',  ( 0.000000000000000000, 3.346456692913386100, 0.000000000000000000 ) ) ;
#14018=VERTEX_POINT ( 'NONE', #49450 ) ;
#14019=CARTESIAN_POINT ( 'NONE',  ( -1.909347346926324906, 0.000000000000000000, -0.4724409448818884805 ) ) ;
#14021=DIRECTION ( 'NONE',  ( 1.000000000000000000, 0.000000000000000000, -3.469446951953613696E-16 ) ) ;
#14024=FACE_OUTER_BOUND ( 'NONE', #37359, .T. ) ;
#14025=DIRECTION ( 'NONE',  ( 1.734723475976806848E-16, 0.000000000000000000, 1.000000000000000000 ) ) ;
#14027=EDGE_CURVE ( 'NONE', #27409, #26538, #14130, .T. ) ;
#14029=EDGE_CURVE ( 'NONE', #18853, #9214, #46854, .T. ) ;
#14031=ORIENTED_EDGE ( 'NONE', *, *, #16939, .T. ) ;
#14032=DIRECTION ( 'NONE',  ( -3.469446951953613696E-16, 0.000000000000000000, -1.000000000000000000 ) ) ;
#14036=VECTOR ( 'NONE', #9756, 39.37007874015748143 ) ;
#14037=LINE ( 'NONE', #13535, #24318 ) ;
#14039=CARTESIAN_POINT ( 'NONE',  ( 1.560669927219590747, 0.000000000000000000, -0.7874015748031473194 ) ) ;
#14041=DIRECTION ( 'NONE',  ( -0.000000000000000000, 1.000000000000000000, -0.000000000000000000 ) ) ;
#14042=ORIENTED_EDGE ( 'NONE', *, *, #19491, .F. ) ;
#14043=ORIENTED_EDGE ( 'NONE', *, *, #21032, .F. ) ;
#14046=ORIENTED_EDGE ( 'NONE', *, *, #40098, .T. ) ;
#14047=LINE ( 'NONE', #49373, #37463 ) ;
#14048=DIRECTION ( 'NONE',  ( 1.000000000000000000, 0.000000000000000000, 0.000000000000000000 ) ) ;
#14050=LINE ( 'NONE', #30051, #22015 ) ;
#14051=ORIENTED_EDGE ( 'NONE', *, *, #42467, .F. ) ;
#14052=VERTEX_POINT ( 'NONE', #46105 ) ;
#14054=LINE ( 'NONE', #14305, #11775 ) ;
#14059=LINE ( 'NONE', #38327, #16146 ) ;
#14060=VERTEX_POINT ( 'NONE', #38646 ) ;
#14061=CARTESIAN_POINT ( 'NONE',  ( -0.8182917201112819283, 3.346456692913386100, -2.047244094488181343 ) ) ;
#14063=VERTEX_POINT ( 'NONE', #10763 ) ;
#14065=CARTESIAN_POINT ( 'NONE',  ( -0.8182917201112814842, 0.000000000000000000, 0.9055118110236167750 ) ) ;
#14068=EDGE_CURVE ( 'NONE', #18488, #38076, #15649, .T. ) ;
#14069=VERTEX_POINT ( 'NONE', #6888 ) ;
#14073=EDGE_CURVE ( 'NONE', #42740, #10279, #42756, .T. ) ;
#14074=CARTESIAN_POINT ( 'NONE',  ( 0.2727639067037602172, 3.346456692913386100, -2.088563196121306476 ) ) ;
#14075=FACE_OUTER_BOUND ( 'NONE', #41368, .T. ) ;
#14076=EDGE_CURVE ( 'NONE', #19538, #42180, #19011, .T. ) ;
#14077=AXIS2_PLACEMENT_3D ( 'NONE', #43642, #32568, #24548 ) ;
#14079=CARTESIAN_POINT ( 'NONE',  ( 0.8182917201112819283, 3.346456692913386100, -1.299212598425193210 ) ) ;
#14080=FACE_OUTER_BOUND ( 'NONE', #25351, .T. ) ;
#14085=FACE_OUTER_BOUND ( 'NONE', #794, .T. ) ;
#14088=CARTESIAN_POINT ( 'NONE',  ( 0.1968503937007878568, 3.346456692913386100, 1.259842519685033357 ) ) ;
#14090=ORIENTED_EDGE ( 'NONE', *, *, #41590, .T. ) ;
#14091=CARTESIAN_POINT ( 'NONE',  ( 0.000000000000000000, 3.267716535433071279, 2.362204724409437961 ) ) ;
#14094=EDGE_CURVE ( 'NONE', #26280, #50705, #14894, .T. ) ;
#14095=CARTESIAN_POINT ( 'NONE',  ( 1.015142113812069313, 0.000000000000000000, 0.9055118110236164419 ) ) ;
#14096=ORIENTED_EDGE ( 'NONE', *, *, #44892, .T. ) ;
#14097=DIRECTION ( 'NONE',  ( -3.469446951953613696E-16, 0.000000000000000000, -1.000000000000000000 ) ) ;
#14098=EDGE_LOOP ( 'NONE', ( #34932, #40524, #22103, #49023 ) ) ;
#14099=LINE ( 'NONE', #23608, #29507 ) ;
#14101=CARTESIAN_POINT ( 'NONE',  ( 0.5455278134075217666, 3.346456692913386100, 1.889763779527550369 ) ) ;
#14102=CARTESIAN_POINT ( 'NONE',  ( -0.6214413264104945434, 3.267716535433071279, -0.3543307086614175816 ) ) ;
#14103=EDGE_CURVE ( 'NONE', #8395, #43635, #42006, .T. ) ;
#14107=DIRECTION ( 'NONE',  ( 1.000000000000000000, 0.000000000000000000, 0.000000000000000000 ) ) ;
#14108=EDGE_LOOP ( 'NONE', ( #11898, #11831, #41244, #44049 ) ) ;
#14111=VECTOR ( 'NONE', #23951, 39.37007874015748143 ) ;
#14112=ORIENTED_EDGE ( 'NONE', *, *, #16728, .T. ) ;
#14113=DIRECTION ( 'NONE',  ( 0.000000000000000000, -1.000000000000000000, 0.000000000000000000 ) ) ;
#14115=DIRECTION ( 'NONE',  ( 1.000000000000000000, 0.000000000000000000, 0.000000000000000000 ) ) ;
#14117=CARTESIAN_POINT ( 'NONE',  ( 1.015142113812069757, 3.267716535433071279, -3.521981712565034361E-16 ) ) ;
#14119=VECTOR ( 'NONE', #27362, 39.37007874015748143 ) ;
#14120=ORIENTED_EDGE ( 'NONE', *, *, #35024, .T. ) ;
#14121=ADVANCED_FACE ( 'NONE', ( #19258 ), #50699, .F. ) ;
#14122=AXIS2_PLACEMENT_3D ( 'NONE', #7166, #15159, #30657 ) ;
#14123=EDGE_CURVE ( 'NONE', #23451, #4391, #34270, .T. ) ;
#14124=ADVANCED_FACE ( 'NONE', ( #23386 ), #18768, .F. ) ;
#14125=ORIENTED_EDGE ( 'NONE', *, *, #684, .T. ) ;
#14126=EDGE_LOOP ( 'NONE', ( #48947, #42024, #24131, #21284 ) ) ;
#14127=DIRECTION ( 'NONE',  ( -3.469446951953613696E-16, 0.000000000000000000, -1.000000000000000000 ) ) ;
#14128=ORIENTED_EDGE ( 'NONE', *, *, #10338, .F. ) ;
#14129=CARTESIAN_POINT ( 'NONE',  ( 1.560669927219590303, 0.000000000000000000, -1.732283464566923170 ) ) ;
#14130=LINE ( 'NONE', #3270, #31843 ) ;
#14134=CARTESIAN_POINT ( 'NONE',  ( 0.5455278134075211005, 3.346456692913386100, 0.4330708661417287386 ) ) ;
#14135=ORIENTED_EDGE ( 'NONE', *, *, #23762, .F. ) ;
#14137=CARTESIAN_POINT ( 'NONE',  ( 0.000000000000000000, 3.267716535433071279, 0.3149606299212578953 ) ) ;
#14139=DIRECTION ( 'NONE',  ( 0.000000000000000000, 0.000000000000000000, -1.000000000000000000 ) ) ;
#14140=CARTESIAN_POINT ( 'NONE',  ( -0.5455278134075208785, 3.267716535433071279, 0.4330708661417290162 ) ) ;
#14141=VECTOR ( 'NONE', #11029, 39.37007874015748143 ) ;
#14142=ORIENTED_EDGE ( 'NONE', *, *, #38920, .T. ) ;
#14143=VECTOR ( 'NONE', #7886, 39.37007874015748143 ) ;
#14144=LINE ( 'NONE', #2016, #35044 ) ;
#14148=FACE_OUTER_BOUND ( 'NONE', #37016, .T. ) ;
#14149=EDGE_CURVE ( 'NONE', #2854, #44079, #47869, .T. ) ;
#14153=ORIENTED_EDGE ( 'NONE', *, *, #43250, .T. ) ;
#14154=LINE ( 'NONE', #15166, #24797 ) ;
#14155=CARTESIAN_POINT ( 'NONE',  ( -0.2727639067037607723, 3.267716535433071279, -1.102362204724405714 ) ) ;
#14157=CARTESIAN_POINT ( 'NONE',  ( -1.909347346926324906, 3.346456692913386100, -0.7874015748031470974 ) ) ;
#14159=CARTESIAN_POINT ( 'NONE',  ( 1.091055626815043311, 0.000000000000000000, 1.377952755905504256 ) ) ;
#14160=ORIENTED_EDGE ( 'NONE', *, *, #5156, .F. ) ;
#14161=CARTESIAN_POINT ( 'NONE',  ( -0.2727639067037602727, 0.000000000000000000, 1.220472440944875281 ) ) ;
#14163=ORIENTED_EDGE ( 'NONE', *, *, #19897, .T. ) ;
#14164=DIRECTION ( 'NONE',  ( 0.000000000000000000, -1.000000000000000000, 0.000000000000000000 ) ) ;
#14165=ORIENTED_EDGE ( 'NONE', *, *, #32567, .F. ) ;
#14167=CARTESIAN_POINT ( 'NONE',  ( 0.2727639067037604947, 3.346456692913386100, -0.7874015748031473194 ) ) ;
#14169=CARTESIAN_POINT ( 'NONE',  ( 1.363819533518803029, 3.346456692913386100, -1.732283464566923170 ) ) ;
#14170=CARTESIAN_POINT ( 'NONE',  ( -0.6214413264104939882, 3.267716535433071279, 1.417322834645662777 ) ) ;
#14173=ORIENTED_EDGE ( 'NONE', *, *, #37106, .F. ) ;
#14175=FACE_BOUND ( 'NONE', #37216, .T. ) ;
#14176=EDGE_LOOP ( 'NONE', ( #49992, #45515, #36708, #49818 ) ) ;
#14177=AXIS2_PLACEMENT_3D ( 'NONE', #18151, #42140, #38035 ) ;
#14180=CARTESIAN_POINT ( 'NONE',  ( -2.443311489867025621, 3.267716535433071279, -0.03937007874015881204 ) ) ;
#14182=EDGE_LOOP ( 'NONE', ( #3870, #39293, #28227, #33384 ) ) ;
#14183=ORIENTED_EDGE ( 'NONE', *, *, #7329, .F. ) ;
#14189=ORIENTED_EDGE ( 'NONE', *, *, #45169, .F. ) ;
#14191=EDGE_LOOP ( 'NONE', ( #45991, #4394, #49761, #5973 ) ) ;
#14193=VECTOR ( 'NONE', #24189, 39.37007874015748143 ) ;
#14195=CARTESIAN_POINT ( 'NONE',  ( 0.8182917201112819283, 3.346456692913386100, -0.1574803149606301411 ) ) ;
#14196=CARTESIAN_POINT ( 'NONE',  ( 0.4696143004045476577, 0.000000000000000000, -1.732283464566922726 ) ) ;
#14201=DIRECTION ( 'NONE',  ( -1.000000000000000000, 0.000000000000000000, 1.734723475976806848E-16 ) ) ;
#14203=CARTESIAN_POINT ( 'NONE',  ( 1.287906020515829919, 3.261681340554358766, -2.079996175279934523 ) ) ;
#14204=DIRECTION ( 'NONE',  ( -0.000000000000000000, 1.000000000000000000, -0.000000000000000000 ) ) ;
#14206=CARTESIAN_POINT ( 'NONE',  ( 0.2727639067037604947, 3.267716535433071279, 0.4724409448818868706 ) ) ;
#14207=CARTESIAN_POINT ( 'NONE',  ( -2.182111253630085290, 3.226699998040846395, -1.141732283464563791 ) ) ;
#14209=CARTESIAN_POINT ( 'NONE',  ( 1.560669927219590303, 0.000000000000000000, -1.102362204724405714 ) ) ;
#14210=LINE ( 'NONE', #34098, #2171 ) ;
#14211=EDGE_CURVE ( 'NONE', #4521, #10846, #8421, .T. ) ;
#14212=EDGE_CURVE ( 'NONE', #27610, #22305, #20283, .T. ) ;
#14213=ORIENTED_EDGE ( 'NONE', *, *, #26104, .T. ) ;
#14214=ORIENTED_EDGE ( 'NONE', *, *, #49204, .F. ) ;
#14215=CIRCLE ( 'NONE', #48699, 2.165354330708661568 ) ;
#14216=CARTESIAN_POINT ( 'NONE',  ( 2.378961647330872786, 0.000000000000000000, 0.3149606299212573401 ) ) ;
#14217=ORIENTED_EDGE ( 'NONE', *, *, #43080, .F. ) ;
#14218=VECTOR ( 'NONE', #11315, 39.37007874015748143 ) ;
#14220=LINE ( 'NONE', #45688, #48448 ) ;
#14221=VECTOR ( 'NONE', #40264, 39.37007874015748143 ) ;
#14222=ORIENTED_EDGE ( 'NONE', *, *, #27408, .T. ) ;
#14223=AXIS2_PLACEMENT_3D ( 'NONE', #8997, #11649, #46731 ) ;
#14227=ORIENTED_EDGE ( 'NONE', *, *, #48899, .F. ) ;
#14230=ORIENTED_EDGE ( 'NONE', *, *, #13450, .F. ) ;
#14231=EDGE_LOOP ( 'NONE', ( #37093, #6688, #4601, #22887 ) ) ;
#14233=DIRECTION ( 'NONE',  ( -0.000000000000000000, 1.000000000000000000, -0.000000000000000000 ) ) ;
#14234=DIRECTION ( 'NONE',  ( 1.000000000000000000, 0.000000000000000000, -3.469446951953613696E-16 ) ) ;
#14235=CARTESIAN_POINT ( 'NONE',  ( 0.1968503937007872462, 0.000000000000000000, 0.1181102362204701633 ) ) ;
#14236=EDGE_LOOP ( 'NONE', ( #36347, #2522, #9541, #51032 ) ) ;
#14237=CARTESIAN_POINT ( 'NONE',  ( -1.985260859929298238, 0.000000000000000000, -1.141732283464563791 ) ) ;
#14238=CARTESIAN_POINT ( 'NONE',  ( 1.636583440222563857, 0.000000000000000000, -0.3149606299212596716 ) ) ;
#14239=DIRECTION ( 'NONE',  ( -1.000000000000000000, 0.000000000000000000, -0.000000000000000000 ) ) ;
#14240=ORIENTED_EDGE ( 'NONE', *, *, #29423, .F. ) ;
#14241=DIRECTION ( 'NONE',  ( 1.734723475976806848E-16, 0.000000000000000000, 1.000000000000000000 ) ) ;
#14243=EDGE_CURVE ( 'NONE', #41617, #25178, #27510, .T. ) ;
#14245=LINE ( 'NONE', #29996, #50460 ) ;
#14246=ORIENTED_EDGE ( 'NONE', *, *, #7668, .T. ) ;
#14247=ORIENTED_EDGE ( 'NONE', *, *, #32634, .F. ) ;
#14250=CARTESIAN_POINT ( 'NONE',  ( 1.560669927219590747, 3.267716535433071279, -5.414661521997677271E-16 ) ) ;
#14252=ADVANCED_FACE ( 'NONE', ( #39401 ), #27771, .F. ) ;
#14253=CARTESIAN_POINT ( 'NONE',  ( 1.636583440222563857, 0.000000000000000000, 0.9448818897637746295 ) ) ;
#14254=ORIENTED_EDGE ( 'NONE', *, *, #25727, .F. ) ;
#14256=EDGE_LOOP ( 'NONE', ( #20216, #9739, #32600, #2962, #11100, #6357, #44422, #26855, #28706, #31454, #22038, #11868, #31711, #34780, #46276, #8947, #37767, #20307, #30803, #38189, #47397, #4955, #47522, #46188, #23216, #44582, #4386, #47251, #35437, #31551, #44402, #44300, #9430, #42013, #15787, #38447, #21267, #37489, #10323, #17086, #32978, #50802, #223, #30263, #44851, #40058, #48363, #6205, #34810, #38426, #27635, #26778, #14939, #21908, #19723, #32427, #15771, #30072, #11766, #24259, #18873, #13672, #44331, #49574, #13504, #43104, #32597, #32425, #50573, #27543, #23130, #41592, #21672, #23695, #4154, #15922, #1431, #39201, #49937, #1545, #11068, #11863, #41826, #29620, #49274, #35233, #42266, #47472, #49879, #31331, #23076, #50119, #27948, #46258, #8964, #28258, #20528, #27225, #27348, #11009, #24275, #22482, #34834, #5144, #41455, #6777, #18798, #11805, #12191, #4510, #2408, #1990, #28683, #3674, #2449, #13631, #12839, #32757, #5097, #38365, #20271, #13919, #11001, #8297, #8367, #31846, #2631, #8678, #45628, #20536, #45247, #29969, #1717, #40238, #40119, #15674, #38013, #50363, #5127, #18128, #13560, #36131, #28657, #39263, #6548, #8602, #16584 ) ) ;
#14257=VECTOR ( 'NONE', #32417, 39.37007874015748143 ) ;
#14258=DIRECTION ( 'NONE',  ( 1.000000000000000000, 0.000000000000000000, -3.469446951953613696E-16 ) ) ;
#14259=ORIENTED_EDGE ( 'NONE', *, *, #26699, .F. ) ;
#14260=CARTESIAN_POINT ( 'NONE',  ( 1.287906020515830141, 0.000000000000000000, -0.6299212598425181220 ) ) ;
#14261=CARTESIAN_POINT ( 'NONE',  ( -0.8182917201112814842, 3.267716535433071279, 0.7874015748031456541 ) ) ;
#14263=VECTOR ( 'NONE', #41325, 39.37007874015748143 ) ;
#14266=DIRECTION ( 'NONE',  ( -1.000000000000000000, -0.000000000000000000, -0.000000000000000000 ) ) ;
#14267=DIRECTION ( 'NONE',  ( -0.000000000000000000, 0.000000000000000000, 1.000000000000000000 ) ) ;
#14268=AXIS2_PLACEMENT_3D ( 'NONE', #24433, #31932, #32707 ) ;
#14270=DIRECTION ( 'NONE',  ( -0.000000000000000000, 1.000000000000000000, -0.000000000000000000 ) ) ;
#14272=EDGE_CURVE ( 'NONE', #50405, #8785, #40435, .T. ) ;
#14274=ORIENTED_EDGE ( 'NONE', *, *, #13143, .F. ) ;
#14275=CARTESIAN_POINT ( 'NONE',  ( 0.1968503937007878568, 3.267716535433071279, 1.889763779527550369 ) ) ;
#14276=DIRECTION ( 'NONE',  ( -1.000000000000000000, 0.000000000000000000, 1.734723475976806848E-16 ) ) ;
#14279=CARTESIAN_POINT ( 'NONE',  ( 1.363819533518803251, 0.000000000000000000, 0.5905511811023579360 ) ) ;
#14282=LINE ( 'NONE', #10156, #12603 ) ;
#14287=CARTESIAN_POINT ( 'NONE',  ( -0.2727639067037607723, 3.346456692913386100, -0.4724409448818883694 ) ) ;
#14288=LINE ( 'NONE', #1910, #32638 ) ;
#14289=VECTOR ( 'NONE', #11131, 39.37007874015748143 ) ;
#14290=VERTEX_POINT ( 'NONE', #36301 ) ;
#14291=EDGE_LOOP ( 'NONE', ( #24536, #38930, #12081, #49179, #25326, #14823, #10687, #17963, #48541, #38757, #43365, #8049, #30996, #32046, #27450, #35687, #11554, #2683, #41301 ) ) ;
#14292=DIRECTION ( 'NONE',  ( -3.469446951953613696E-16, 0.000000000000000000, -1.000000000000000000 ) ) ;
#14293=PLANE ( 'NONE',  #41164 ) ;
#14295=VECTOR ( 'NONE', #16117, 39.37007874015748143 ) ;
#14297=DIRECTION ( 'NONE',  ( -3.469446951953613696E-16, 0.000000000000000000, -1.000000000000000000 ) ) ;
#14298=DIRECTION ( 'NONE',  ( 1.734723475976806848E-16, -0.000000000000000000, 1.000000000000000000 ) ) ;
#14299=VECTOR ( 'NONE', #3501, 39.37007874015748143 ) ;
#14300=VECTOR ( 'NONE', #23782, 39.37007874015748143 ) ;
#14301=ORIENTED_EDGE ( 'NONE', *, *, #43024, .T. ) ;
#14302=EDGE_LOOP ( 'NONE', ( #38263, #31079, #15296, #24386 ) ) ;
#14305=CARTESIAN_POINT ( 'NONE',  ( -1.636583440222564523, 3.267716535433071279, 2.839019714148967570E-16 ) ) ;
#14307=VERTEX_POINT ( 'NONE', #31657 ) ;
#14309=FACE_BOUND ( 'NONE', #16392, .T. ) ;
#14311=ORIENTED_EDGE ( 'NONE', *, *, #26092, .F. ) ;
#14313=CARTESIAN_POINT ( 'NONE',  ( -1.091055626815042645, 3.346456692913386100, -1.889763779527552146 ) ) ;
#14314=ORIENTED_EDGE ( 'NONE', *, *, #15975, .T. ) ;
#14315=ORIENTED_EDGE ( 'NONE', *, *, #48775, .T. ) ;
#14317=CARTESIAN_POINT ( 'NONE',  ( 1.560669927219590747, 0.000000000000000000, -0.1574803149606304187 ) ) ;
#14318=EDGE_CURVE ( 'NONE', #9214, #30067, #35784, .T. ) ;
#14320=ADVANCED_FACE ( 'NONE', ( #412 ), #31924, .F. ) ;
#14324=LINE ( 'NONE', #10199, #11494 ) ;
#14325=ORIENTED_EDGE ( 'NONE', *, *, #6255, .T. ) ;
#14326=ORIENTED_EDGE ( 'NONE', *, *, #28011, .T. ) ;
#14329=EDGE_CURVE ( 'NONE', #24374, #36538, #32697, .T. ) ;
#14330=CARTESIAN_POINT ( 'NONE',  ( 0.000000000000000000, 3.267716535433071279, 0.1574803149606286423 ) ) ;
#14331=AXIS2_PLACEMENT_3D ( 'NONE', #36804, #40675, #1427 ) ;
#14332=LINE ( 'NONE', #18209, #35223 ) ;
#14333=DIRECTION ( 'NONE',  ( -1.000000000000000000, -0.000000000000000000, -0.000000000000000000 ) ) ;
#14337=VECTOR ( 'NONE', #29131, 39.37007874015748143 ) ;
#14338=PLANE ( 'NONE',  #21560 ) ;
#14340=VECTOR ( 'NONE', #2590, 39.37007874015748143 ) ;
#14342=DIRECTION ( 'NONE',  ( 1.734723475976806848E-16, -0.000000000000000000, 1.000000000000000000 ) ) ;
#14344=EDGE_LOOP ( 'NONE', ( #44254, #23480, #9005, #43626 ) ) ;
#14345=DIRECTION ( 'NONE',  ( -0.000000000000000000, 1.000000000000000000, -0.000000000000000000 ) ) ;
#14346=EDGE_CURVE ( 'NONE', #43159, #40619, #17192, .T. ) ;
#14348=PLANE ( 'NONE',  #14477 ) ;
#14350=ORIENTED_EDGE ( 'NONE', *, *, #24049, .T. ) ;
#14353=CARTESIAN_POINT ( 'NONE',  ( 0.000000000000000000, 3.267716535433071279, 0.000000000000000000 ) ) ;
#14354=EDGE_CURVE ( 'NONE', #31439, #23113, #5818, .T. ) ;
#14356=DIRECTION ( 'NONE',  ( -3.469446951953613696E-16, 0.000000000000000000, -1.000000000000000000 ) ) ;
#14357=LINE ( 'NONE', #33744, #27623 ) ;
#14358=ORIENTED_EDGE ( 'NONE', *, *, #11180, .T. ) ;
#14359=VERTEX_POINT ( 'NONE', #6335 ) ;
#14360=DIRECTION ( 'NONE',  ( 0.000000000000000000, 0.000000000000000000, -1.000000000000000000 ) ) ;
#14361=EDGE_CURVE ( 'NONE', #42073, #25538, #45041, .T. ) ;
#14362=DIRECTION ( 'NONE',  ( -0.000000000000000000, 1.000000000000000000, -0.000000000000000000 ) ) ;
#14364=EDGE_LOOP ( 'NONE', ( #17665, #49485, #25925, #1848 ) ) ;
#14365=EDGE_CURVE ( 'NONE', #13884, #575, #29313, .T. ) ;
#14366=LINE ( 'NONE', #25473, #30596 ) ;
#14367=ORIENTED_EDGE ( 'NONE', *, *, #14506, .F. ) ;
#14368=LINE ( 'NONE', #25991, #21628 ) ;
#14369=VECTOR ( 'NONE', #50885, 39.37007874015748143 ) ;
#14370=LINE ( 'NONE', #3008, #37195 ) ;
#14372=VERTEX_POINT ( 'NONE', #49147 ) ;
#14373=CARTESIAN_POINT ( 'NONE',  ( -1.166969139818015755, 3.267716535433071279, 4.048737525165544676E-16 ) ) ;
#14374=AXIS2_PLACEMENT_3D ( 'NONE', #20730, #24356, #21501 ) ;
#14376=ORIENTED_EDGE ( 'NONE', *, *, #50908, .F. ) ;
#14377=AXIS2_PLACEMENT_3D ( 'NONE', #17412, #2175, #17671 ) ;
#14379=CONICAL_SURFACE ( 'NONE', #37495, 2.422428857167389982, 0.4363323129985800519 ) ;
#14381=ORIENTED_EDGE ( 'NONE', *, *, #25264, .T. ) ;
#14382=CARTESIAN_POINT ( 'NONE',  ( 0.000000000000000000, 0.000000000000000000, -2.106299212598425008 ) ) ;
#14383=ADVANCED_FACE ( 'NONE', ( #5306 ), #1689, .F. ) ;
#14384=VECTOR ( 'NONE', #49224, 39.37007874015748143 ) ;
#14385=VERTEX_POINT ( 'NONE', #45539 ) ;
#14387=DIRECTION ( 'NONE',  ( 1.000000000000000000, 0.000000000000000000, -3.469446951953613696E-16 ) ) ;
#14388=CARTESIAN_POINT ( 'NONE',  ( -1.636583440222564301, 0.000000000000000000, -0.3149606299212592275 ) ) ;
#14389=LINE ( 'NONE', #37646, #33549 ) ;
#14390=LINE ( 'NONE', #42012, #23696 ) ;
#14391=ORIENTED_EDGE ( 'NONE', *, *, #34, .F. ) ;
#14392=CARTESIAN_POINT ( 'NONE',  ( -1.091055626815042645, 0.000000000000000000, 2.204724409448808764 ) ) ;
#14395=LINE ( 'NONE', #44856, #18267 ) ;
#14396=ORIENTED_EDGE ( 'NONE', *, *, #10047, .T. ) ;
#14397=LINE ( 'NONE', #26518, #10839 ) ;
#14398=DIRECTION ( 'NONE',  ( 1.000000000000000000, 0.000000000000000000, 0.000000000000000000 ) ) ;
#14400=CARTESIAN_POINT ( 'NONE',  ( 0.000000000000000000, 3.267716535433071279, 0.000000000000000000 ) ) ;
#14402=CARTESIAN_POINT ( 'NONE',  ( 1.909347346926324462, 3.267716535433071279, -1.299212598425194320 ) ) ;
#14404=ORIENTED_EDGE ( 'NONE', *, *, #15757, .F. ) ;
#14405=VECTOR ( 'NONE', #48886, 39.37007874015748143 ) ;
#14407=EDGE_LOOP ( 'NONE', ( #40588, #13182, #30030, #31593 ) ) ;
#14409=ADVANCED_FACE ( 'NONE', ( #29049 ), #9949, .F. ) ;
#14410=VECTOR ( 'NONE', #40709, 39.37007874015748143 ) ;
#14411=PLANE ( 'NONE',  #2805 ) ;
#14414=EDGE_CURVE ( 'NONE', #29717, #32803, #16941, .T. ) ;
#14415=PLANE ( 'NONE',  #47306 ) ;
#14416=CARTESIAN_POINT ( 'NONE',  ( 1.636583440222563857, 3.346456692913386100, 0.9448818897637746295 ) ) ;
#14418=EDGE_CURVE ( 'NONE', #15165, #44082, #28799, .T. ) ;
#14420=VECTOR ( 'NONE', #40710, 39.37007874015748143 ) ;
#14421=ORIENTED_EDGE ( 'NONE', *, *, #48463, .F. ) ;
#14422=ORIENTED_EDGE ( 'NONE', *, *, #9644, .F. ) ;
#14423=LINE ( 'NONE', #30167, #38614 ) ;
#14425=EDGE_CURVE ( 'NONE', #33393, #8577, #9443, .T. ) ;
#14427=DIRECTION ( 'NONE',  ( 1.000000000000000000, 0.000000000000000000, -3.469446951953613696E-16 ) ) ;
#14429=LINE ( 'NONE', #14169, #9103 ) ;
#14430=CARTESIAN_POINT ( 'NONE',  ( 1.636583440222563635, 3.346456692913386100, -0.9448818897637765168 ) ) ;
#14431=CARTESIAN_POINT ( 'NONE',  ( -2.182111253630085734, 3.346456692913386100, -0.6299212598425177889 ) ) ;
#14432=VERTEX_POINT ( 'NONE', #32956 ) ;
#14433=ORIENTED_EDGE ( 'NONE', *, *, #7346, .F. ) ;
#14434=DIRECTION ( 'NONE',  ( -1.000000000000000000, 0.000000000000000000, 1.734723475976806848E-16 ) ) ;
#14435=FACE_BOUND ( 'NONE', #27714, .T. ) ;
#14436=ORIENTED_EDGE ( 'NONE', *, *, #27641, .T. ) ;
#14439=CARTESIAN_POINT ( 'NONE',  ( -2.447166048624850543, 3.259451480409341961, -0.03937007874015881204 ) ) ;
#14441=VERTEX_POINT ( 'NONE', #48884 ) ;
#14443=CARTESIAN_POINT ( 'NONE',  ( -1.636583440222564301, 3.346456692913386100, -0.9448818897637762948 ) ) ;
#14448=VERTEX_POINT ( 'NONE', #42941 ) ;
#14453=CARTESIAN_POINT ( 'NONE',  ( -0.8182917201112819283, 3.346456692913386100, -1.417322834645664331 ) ) ;
#14455=CARTESIAN_POINT ( 'NONE',  ( -1.363819533518803029, 3.346456692913386100, -0.03937007874015868020 ) ) ;
#14456=ORIENTED_EDGE ( 'NONE', *, *, #2882, .T. ) ;
#14457=EDGE_LOOP ( 'NONE', ( #46793, #48518, #24245, #1519 ) ) ;
#14458=VECTOR ( 'NONE', #47324, 39.37007874015748143 ) ;
#14460=PLANE ( 'NONE',  #712 ) ;
#14464=CARTESIAN_POINT ( 'NONE',  ( -2.182111253630085290, 3.267716535433071279, 3.785359618865288779E-16 ) ) ;
#14466=ORIENTED_EDGE ( 'NONE', *, *, #14361, .T. ) ;
#14468=DIRECTION ( 'NONE',  ( 1.000000000000000000, -0.000000000000000000, 0.000000000000000000 ) ) ;
#14470=ORIENTED_EDGE ( 'NONE', *, *, #5516, .T. ) ;
#14471=LINE ( 'NONE', #38972, #22075 ) ;
#14472=EDGE_CURVE ( 'NONE', #41084, #29009, #42194, .T. ) ;
#14474=EDGE_CURVE ( 'NONE', #16004, #14001, #14587, .T. ) ;
#14476=AXIS2_PLACEMENT_3D ( 'NONE', #10146, #33407, #41643 ) ;
#14477=AXIS2_PLACEMENT_3D ( 'NONE', #2484, #3486, #30352 ) ;
#14478=VERTEX_POINT ( 'NONE', #22579 ) ;
#14480=AXIS2_PLACEMENT_3D ( 'NONE', #9593, #45187, #16833 ) ;
#14482=EDGE_CURVE ( 'NONE', #508, #41536, #38340, .T. ) ;
#14484=CARTESIAN_POINT ( 'NONE',  ( -1.363819533518803473, 0.000000000000000000, -0.4724409448818886470 ) ) ;
#14486=VERTEX_POINT ( 'NONE', #50643 ) ;
#14488=VECTOR ( 'NONE', #7556, 39.37007874015748143 ) ;
#14489=CARTESIAN_POINT ( 'NONE',  ( 0.000000000000000000, 3.267716535433071279, 0.6299212598425164567 ) ) ;
#14490=ORIENTED_EDGE ( 'NONE', *, *, #39213, .T. ) ;
#14491=ORIENTED_EDGE ( 'NONE', *, *, #31732, .F. ) ;
#14493=PLANE ( 'NONE',  #44129 ) ;
#14494=CARTESIAN_POINT ( 'NONE',  ( 1.833433833923351353, 0.000000000000000000, 0.6299212598425164567 ) ) ;
#14495=LINE ( 'NONE', #5732, #10479 ) ;
#14496=EDGE_CURVE ( 'NONE', #28725, #18986, #46053, .T. ) ;
#14497=VERTEX_POINT ( 'NONE', #7093 ) ;
#14498=EDGE_CURVE ( 'NONE', #44517, #5052, #3469, .T. ) ;
#14501=CARTESIAN_POINT ( 'NONE',  ( -1.909347346926324462, 0.000000000000000000, -0.03937007874015881204 ) ) ;
#14502=EDGE_LOOP ( 'NONE', ( #33235, #18405, #16717, #40333 ) ) ;
#14503=ADVANCED_FACE ( 'NONE', ( #19203 ), #50397, .F. ) ;
#14505=CARTESIAN_POINT ( 'NONE',  ( -1.091055626815042201, 3.346456692913386100, 1.574803149606291974 ) ) ;
#14506=EDGE_CURVE ( 'NONE', #47754, #10447, #34214, .T. ) ;
#14507=VERTEX_POINT ( 'NONE', #30837 ) ;
#14508=ORIENTED_EDGE ( 'NONE', *, *, #20433, .T. ) ;
#14510=ADVANCED_FACE ( 'NONE', ( #26449 ), #23331, .F. ) ;
#14511=FACE_OUTER_BOUND ( 'NONE', #37314, .T. ) ;
#14512=DIRECTION ( 'NONE',  ( 1.000000000000000000, -0.000000000000000000, 0.000000000000000000 ) ) ;
#14513=PLANE ( 'NONE',  #42007 ) ;
#14515=ORIENTED_EDGE ( 'NONE', *, *, #7495, .T. ) ;
#14517=DIRECTION ( 'NONE',  ( -3.469446951953613696E-16, 0.000000000000000000, -1.000000000000000000 ) ) ;
#14518=VECTOR ( 'NONE', #8930, 39.37007874015748143 ) ;
#14519=CARTESIAN_POINT ( 'NONE',  ( 0.000000000000000000, 3.346456692913386100, 0.000000000000000000 ) ) ;
#14520=ORIENTED_EDGE ( 'NONE', *, *, #7017, .T. ) ;
#14522=CARTESIAN_POINT ( 'NONE',  ( 0.000000000000000000, 3.267716535433071279, 0.000000000000000000 ) ) ;
#14524=AXIS2_PLACEMENT_3D ( 'NONE', #36904, #48719, #5656 ) ;
#14527=CARTESIAN_POINT ( 'NONE',  ( -1.439733046521776583, 0.000000000000000000, -0.3149606299212592275 ) ) ;
#14528=VECTOR ( 'NONE', #48164, 39.37007874015748143 ) ;
#14530=CARTESIAN_POINT ( 'NONE',  ( -0.07591351300297340121, 3.267716535433071279, -1.614173228346451605 ) ) ;
#14533=DIRECTION ( 'NONE',  ( -1.000000000000000000, 0.000000000000000000, 1.734723475976806848E-16 ) ) ;
#14535=PLANE ( 'NONE',  #29828 ) ;
#14538=ORIENTED_EDGE ( 'NONE', *, *, #36203, .T. ) ;
#14539=DIRECTION ( 'NONE',  ( -1.000000000000000000, 0.000000000000000000, -0.000000000000000000 ) ) ;
#14541=EDGE_CURVE ( 'NONE', #41218, #19504, #38089, .T. ) ;
#14542=VERTEX_POINT ( 'NONE', #50152 ) ;
#14543=DIRECTION ( 'NONE',  ( -1.000000000000000000, 0.000000000000000000, -0.000000000000000000 ) ) ;
#14544=ORIENTED_EDGE ( 'NONE', *, *, #40164, .F. ) ;
#14546=EDGE_CURVE ( 'NONE', #7441, #43525, #46546, .T. ) ;
#14547=CARTESIAN_POINT ( 'NONE',  ( 1.909347346926324684, 0.000000000000000000, 0.7874015748031456541 ) ) ;
#14549=CARTESIAN_POINT ( 'NONE',  ( 0.5455278134075211005, 3.346456692913386100, -0.8267716535433055070 ) ) ;
#14553=CARTESIAN_POINT ( 'NONE',  ( 0.000000000000000000, 3.267716535433071279, 0.4330708661417287386 ) ) ;
#14554=VECTOR ( 'NONE', #37630, 39.37007874015748143 ) ;
#14556=AXIS2_PLACEMENT_3D ( 'NONE', #35214, #32118, #47551 ) ;
#14557=VERTEX_POINT ( 'NONE', #34711 ) ;
#14558=DIRECTION ( 'NONE',  ( -1.000000000000000000, 0.000000000000000000, 0.000000000000000000 ) ) ;
#14559=DIRECTION ( 'NONE',  ( -1.000000000000000000, -0.000000000000000000, -0.000000000000000000 ) ) ;
#14561=AXIS2_PLACEMENT_3D ( 'NONE', #21290, #33434, #9672 ) ;
#14563=ORIENTED_EDGE ( 'NONE', *, *, #33964, .F. ) ;
#14564=EDGE_CURVE ( 'NONE', #5216, #17026, #2464, .T. ) ;
#14565=CARTESIAN_POINT ( 'NONE',  ( 1.363819533518803251, 3.346456692913386100, 0.7874015748031454320 ) ) ;
#14566=DIRECTION ( 'NONE',  ( 1.000000000000000000, -0.000000000000000000, 0.000000000000000000 ) ) ;
#14567=AXIS2_PLACEMENT_3D ( 'NONE', #22421, #49730, #13913 ) ;
#14568=CARTESIAN_POINT ( 'NONE',  ( 2.182111253630085290, 0.000000000000000000, 0.6299212598425161236 ) ) ;
#14569=VERTEX_POINT ( 'NONE', #42449 ) ;
#14572=VECTOR ( 'NONE', #34188, 39.37007874015748143 ) ;
#14574=EDGE_CURVE ( 'NONE', #7189, #46760, #42700, .T. ) ;
#14576=CARTESIAN_POINT ( 'NONE',  ( -0.3486774197067340486, 3.346456692913386100, -1.456692913385822630 ) ) ;
#14577=ORIENTED_EDGE ( 'NONE', *, *, #5684, .F. ) ;
#14578=ORIENTED_EDGE ( 'NONE', *, *, #36631, .F. ) ;
#14580=CARTESIAN_POINT ( 'NONE',  ( 1.015142113812069091, 0.000000000000000000, -1.929133858267711110 ) ) ;
#14582=CARTESIAN_POINT ( 'NONE',  ( 1.287906020515830363, 3.267716535433071279, -4.468321617281356063E-16 ) ) ;
#14584=CARTESIAN_POINT ( 'NONE',  ( 1.091055626815042645, 0.000000000000000000, -0.6299212598425181220 ) ) ;
#14586=ORIENTED_EDGE ( 'NONE', *, *, #734, .F. ) ;
#14587=LINE ( 'NONE', #6835, #12079 ) ;
#14588=DIRECTION ( 'NONE',  ( 1.734723475976806848E-16, 0.000000000000000000, 1.000000000000000000 ) ) ;
#14590=DIRECTION ( 'NONE',  ( 1.734723475976806848E-16, -0.000000000000000000, 1.000000000000000000 ) ) ;
#14591=DIRECTION ( 'NONE',  ( 0.000000000000000000, 0.000000000000000000, -1.000000000000000000 ) ) ;
#14592=AXIS2_PLACEMENT_3D ( 'NONE', #35347, #46173, #30963 ) ;
#14594=CARTESIAN_POINT ( 'NONE',  ( -0.3486774197067342151, 3.346456692913386100, -2.204724409448810540 ) ) ;
#14595=DIRECTION ( 'NONE',  ( 1.734723475976806848E-16, -0.000000000000000000, 1.000000000000000000 ) ) ;
#14597=FACE_OUTER_BOUND ( 'NONE', #13620, .T. ) ;
#14598=DIRECTION ( 'NONE',  ( 1.734723475976806848E-16, -0.000000000000000000, 1.000000000000000000 ) ) ;
#14599=VERTEX_POINT ( 'NONE', #48065 ) ;
#14600=DIRECTION ( 'NONE',  ( 0.000000000000000000, -1.000000000000000000, 0.000000000000000000 ) ) ;
#14601=VECTOR ( 'NONE', #16868, 39.37007874015748143 ) ;
#14602=CARTESIAN_POINT ( 'NONE',  ( 1.015142113812069091, 3.346456692913386100, -1.417322834645664331 ) ) ;
#14603=CARTESIAN_POINT ( 'NONE',  ( -0.2727639067037607168, 3.267716535433071279, 4.731699523581612206E-17 ) ) ;
#14604=ADVANCED_FACE ( 'NONE', ( #31860 ), #8863, .F. ) ;
#14605=ADVANCED_FACE ( 'NONE', ( #8353 ), #40110, .F. ) ;
#14607=DIRECTION ( 'NONE',  ( -3.469446951953613696E-16, 0.000000000000000000, -1.000000000000000000 ) ) ;
#14609=FACE_BOUND ( 'NONE', #8720, .T. ) ;
#14611=DIRECTION ( 'NONE',  ( -0.000000000000000000, 1.000000000000000000, -0.000000000000000000 ) ) ;
#14613=CARTESIAN_POINT ( 'NONE',  ( 1.560669927219590747, 3.346456692913386100, -0.1574803149606304187 ) ) ;
#14614=DIRECTION ( 'NONE',  ( -0.000000000000000000, 1.000000000000000000, -0.000000000000000000 ) ) ;
#14615=ADVANCED_FACE ( 'NONE', ( #35982 ), #16359, .F. ) ;
#14616=EDGE_CURVE ( 'NONE', #4005, #46097, #36241, .T. ) ;
#14617=ORIENTED_EDGE ( 'NONE', *, *, #16338, .T. ) ;
#14619=FACE_OUTER_BOUND ( 'NONE', #50357, .T. ) ;
#14620=CARTESIAN_POINT ( 'NONE',  ( 0.1968503937007872184, 3.267716535433071279, -6.829619984160650651E-17 ) ) ;
#14621=DIRECTION ( 'NONE',  ( 1.000000000000000000, 0.000000000000000000, 0.000000000000000000 ) ) ;
#14624=ORIENTED_EDGE ( 'NONE', *, *, #34662, .F. ) ;
#14625=EDGE_CURVE ( 'NONE', #30593, #3260, #19709, .T. ) ;
#14628=VECTOR ( 'NONE', #17864, 39.37007874015748143 ) ;
#14629=VECTOR ( 'NONE', #3221, 39.37007874015748143 ) ;
#14631=VECTOR ( 'NONE', #12298, 39.37007874015748143 ) ;
#14632=VERTEX_POINT ( 'NONE', #11715 ) ;
#14633=ADVANCED_FACE ( 'NONE', ( #12474 ), #12737, .F. ) ;
#14634=DIRECTION ( 'NONE',  ( -3.469446951953613696E-16, 0.000000000000000000, -1.000000000000000000 ) ) ;
#14635=ORIENTED_EDGE ( 'NONE', *, *, #3413, .T. ) ;
#14639=ORIENTED_EDGE ( 'NONE', *, *, #20400, .F. ) ;
#14640=CARTESIAN_POINT ( 'NONE',  ( 0.1968503937007872462, 3.346456692913386100, -0.8267716535433052849 ) ) ;
#14641=VECTOR ( 'NONE', #16877, 39.37007874015748143 ) ;
#14642=LINE ( 'NONE', #34766, #19621 ) ;
#14643=ADVANCED_FACE ( 'NONE', ( #31345 ), #8606, .F. ) ;
#14645=CARTESIAN_POINT ( 'NONE',  ( -0.5455278134075214336, 3.346456692913386100, -1.771653543307081025 ) ) ;
#14649=CARTESIAN_POINT ( 'NONE',  ( 1.244991204790707684, 3.267716535433071279, -1.771653543307081691 ) ) ;
#14650=CARTESIAN_POINT ( 'NONE',  ( -0.8942052331142547050, 3.346456692913386100, 0.1181102362204705658 ) ) ;
#14651=CARTESIAN_POINT ( 'NONE',  ( 1.909347346926324684, 3.267716535433071279, 1.021348170950612033 ) ) ;
#14652=DIRECTION ( 'NONE',  ( 1.000000000000000000, 0.000000000000000000, 0.000000000000000000 ) ) ;
#14653=EDGE_LOOP ( 'NONE', ( #10990, #2213, #33941, #10970 ) ) ;
#14654=CARTESIAN_POINT ( 'NONE',  ( -1.863748091109392879, 3.346456692913386100, 1.102362204724404160 ) ) ;
#14655=LINE ( 'NONE', #46122, #9613 ) ;
#14657=DIRECTION ( 'NONE',  ( -0.000000000000000000, 1.000000000000000000, -0.000000000000000000 ) ) ;
#14658=VECTOR ( 'NONE', #33922, 39.37007874015748143 ) ;
#14659=AXIS2_PLACEMENT_3D ( 'NONE', #24048, #812, #12687 ) ;
#14661=ORIENTED_EDGE ( 'NONE', *, *, #17015, .T. ) ;
#14663=CARTESIAN_POINT ( 'NONE',  ( -0.5455278134075214336, 3.346456692913386100, -0.3149606299212593941 ) ) ;
#14664=ORIENTED_EDGE ( 'NONE', *, *, #50333, .F. ) ;
#14665=CARTESIAN_POINT ( 'NONE',  ( 0.2727639067037604392, 3.346456692913386100, -0.9842519685039348154 ) ) ;
#14666=EDGE_CURVE ( 'NONE', #47601, #35447, #20217, .T. ) ;
#14670=CARTESIAN_POINT ( 'NONE',  ( -2.102985103392958077, 3.267716535433071279, 0.1181102362204704270 ) ) ;
#14672=ORIENTED_EDGE ( 'NONE', *, *, #19890, .T. ) ;
#14673=EDGE_CURVE ( 'NONE', #37048, #32813, #20480, .T. ) ;
#14675=DIRECTION ( 'NONE',  ( -3.469446951953613696E-16, 0.000000000000000000, -1.000000000000000000 ) ) ;
#14676=EDGE_LOOP ( 'NONE', ( #38856, #3927, #7772, #50010 ) ) ;
#14678=LINE ( 'NONE', #42789, #7283 ) ;
#14679=ORIENTED_EDGE ( 'NONE', *, *, #20661, .F. ) ;
#14680=LINE ( 'NONE', #18046, #2357 ) ;
#14681=CARTESIAN_POINT ( 'NONE',  ( -1.363819533518803029, 3.346456692913386100, 1.417322834645662777 ) ) ;
#14682=ORIENTED_EDGE ( 'NONE', *, *, #6333, .F. ) ;
#14684=DIRECTION ( 'NONE',  ( 1.734723475976806848E-16, -0.000000000000000000, 1.000000000000000000 ) ) ;
#14687=ORIENTED_EDGE ( 'NONE', *, *, #41350, .F. ) ;
#14690=FACE_BOUND ( 'NONE', #31553, .T. ) ;
#14691=ORIENTED_EDGE ( 'NONE', *, *, #14472, .T. ) ;
#14692=CARTESIAN_POINT ( 'NONE',  ( -1.363819533518803473, 3.232777166330603524, 2.047244094488179567 ) ) ;
#14693=FACE_OUTER_BOUND ( 'NONE', #18711, .T. ) ;
#14695=EDGE_CURVE ( 'NONE', #15287, #24457, #346, .T. ) ;
#14696=ORIENTED_EDGE ( 'NONE', *, *, #18500, .F. ) ;
#14697=VERTEX_POINT ( 'NONE', #7844 ) ;
#14701=AXIS2_PLACEMENT_3D ( 'NONE', #28588, #24217, #31968 ) ;
#14703=EDGE_LOOP ( 'NONE', ( #21673, #2859, #33837, #13050 ) ) ;
#14704=DIRECTION ( 'NONE',  ( -3.469446951953613696E-16, 0.000000000000000000, -1.000000000000000000 ) ) ;
#14705=DIRECTION ( 'NONE',  ( -1.000000000000000000, 0.000000000000000000, -0.000000000000000000 ) ) ;
#14707=EDGE_CURVE ( 'NONE', #8950, #50349, #15837, .T. ) ;
#14709=AXIS2_PLACEMENT_3D ( 'NONE', #19567, #23706, #3079 ) ;
#14712=CARTESIAN_POINT ( 'NONE',  ( -1.363819533518803473, 3.346456692913386100, -0.7874015748031470974 ) ) ;
#14713=FACE_OUTER_BOUND ( 'NONE', #17149, .T. ) ;
#14714=CARTESIAN_POINT ( 'NONE',  ( 1.091055626815042645, 3.346456692913386100, 1.259842519685033357 ) ) ;
#14717=ADVANCED_FACE ( 'NONE', ( #20993 ), #44719, .F. ) ;
#14718=CARTESIAN_POINT ( 'NONE',  ( 1.560669927219590747, 0.000000000000000000, -0.4724409448818889246 ) ) ;
#14719=CARTESIAN_POINT ( 'NONE',  ( -2.442519317017155078, 3.215267933203563189, -0.3543307086614173040 ) ) ;
#14720=LINE ( 'NONE', #49784, #50569 ) ;
#14721=ORIENTED_EDGE ( 'NONE', *, *, #24228, .T. ) ;
#14722=PLANE ( 'NONE',  #48937 ) ;
#14723=LINE ( 'NONE', #30475, #16208 ) ;
#14725=ORIENTED_EDGE ( 'NONE', *, *, #23803, .F. ) ;
#14728=LINE ( 'NONE', #46191, #41055 ) ;
#14729=VECTOR ( 'NONE', #46519, 39.37007874015748854 ) ;
#14730=ORIENTED_EDGE ( 'NONE', *, *, #18150, .T. ) ;
#14731=EDGE_CURVE ( 'NONE', #24457, #36095, #28255, .T. ) ;
#14733=EDGE_CURVE ( 'NONE', #13031, #4521, #24867, .T. ) ;
#14734=EDGE_LOOP ( 'NONE', ( #24219, #32316, #43662, #30331 ) ) ;
#14736=VECTOR ( 'NONE', #28111, 39.37007874015748143 ) ;
#14737=EDGE_LOOP ( 'NONE', ( #43271, #46879, #49735, #4580 ) ) ;
#14738=VECTOR ( 'NONE', #1605, 39.37007874015748143 ) ;
#14739=AXIS2_PLACEMENT_3D ( 'NONE', #44751, #45504, #32919 ) ;
#14741=FACE_OUTER_BOUND ( 'NONE', #50918, .T. ) ;
#14742=ADVANCED_FACE ( 'NONE', ( #1877 ), #25372, .F. ) ;
#14744=ORIENTED_EDGE ( 'NONE', *, *, #38437, .F. ) ;
#14749=DIRECTION ( 'NONE',  ( 0.000000000000000000, 0.000000000000000000, -1.000000000000000000 ) ) ;
#14750=CARTESIAN_POINT ( 'NONE',  ( 0.8182917201112824834, 3.346456692913386100, 2.004783788421103718 ) ) ;
#14752=VECTOR ( 'NONE', #13082, 39.37007874015748143 ) ;
#14754=DIRECTION ( 'NONE',  ( 1.734723475976806848E-16, -0.000000000000000000, 1.000000000000000000 ) ) ;
#14755=CARTESIAN_POINT ( 'NONE',  ( 0.2727639067037604947, 0.000000000000000000, -1.102362204724405714 ) ) ;
#14758=ORIENTED_EDGE ( 'NONE', *, *, #27839, .F. ) ;
#14760=ORIENTED_EDGE ( 'NONE', *, *, #18500, .T. ) ;
#14761=EDGE_LOOP ( 'NONE', ( #23533, #1999, #27525, #12803 ) ) ;
#14763=EDGE_CURVE ( 'NONE', #24410, #12066, #9116, .T. ) ;
#14767=LINE ( 'NONE', #11394, #802 ) ;
#14769=EDGE_LOOP ( 'NONE', ( #2155, #33112, #45761, #33848 ) ) ;
#14770=EDGE_CURVE ( 'NONE', #21615, #7243, #40871, .T. ) ;
#14771=LINE ( 'NONE', #9696, #10615 ) ;
#14773=VERTEX_POINT ( 'NONE', #5756 ) ;
#14775=LINE ( 'NONE', #10649, #37488 ) ;
#14776=VECTOR ( 'NONE', #3969, 39.37007874015748143 ) ;
#14777=VECTOR ( 'NONE', #35740, 39.37007874015748143 ) ;
#14778=LINE ( 'NONE', #23026, #23355 ) ;
#14780=DIRECTION ( 'NONE',  ( -1.000000000000000000, 0.000000000000000000, -0.000000000000000000 ) ) ;
#14781=ORIENTED_EDGE ( 'NONE', *, *, #5811, .F. ) ;
#14782=DIRECTION ( 'NONE',  ( 1.734723475976806848E-16, 0.000000000000000000, 1.000000000000000000 ) ) ;
#14783=FACE_OUTER_BOUND ( 'NONE', #9713, .T. ) ;
#14784=EDGE_CURVE ( 'NONE', #20320, #18496, #33136, .T. ) ;
#14785=VECTOR ( 'NONE', #38604, 39.37007874015748143 ) ;
#14786=DIRECTION ( 'NONE',  ( 1.734723475976806848E-16, -0.000000000000000000, 1.000000000000000000 ) ) ;
#14787=ORIENTED_EDGE ( 'NONE', *, *, #26645, .T. ) ;
#14788=CARTESIAN_POINT ( 'NONE',  ( -0.8182917201112819283, 3.346456692913386100, -2.047244094488181343 ) ) ;
#14789=EDGE_CURVE ( 'NONE', #27908, #7564, #13761, .T. ) ;
#14790=LINE ( 'NONE', #34663, #35260 ) ;
#14791=LINE ( 'NONE', #42147, #6582 ) ;
#14794=DIRECTION ( 'NONE',  ( 0.000000000000000000, 0.000000000000000000, -1.000000000000000000 ) ) ;
#14795=EDGE_CURVE ( 'NONE', #30476, #15256, #29504, .T. ) ;
#14796=EDGE_CURVE ( 'NONE', #12747, #12590, #21503, .T. ) ;
#14799=ORIENTED_EDGE ( 'NONE', *, *, #37536, .T. ) ;
#14800=CARTESIAN_POINT ( 'NONE',  ( 2.106197740627112402, 0.000000000000000000, 0.7874015748031456541 ) ) ;
#14802=DIRECTION ( 'NONE',  ( -1.000000000000000000, 0.000000000000000000, -0.000000000000000000 ) ) ;
#14803=LINE ( 'NONE', #34923, #10364 ) ;
#14805=ORIENTED_EDGE ( 'NONE', *, *, #25225, .F. ) ;
#14808=LINE ( 'NONE', #14553, #48781 ) ;
#14809=LINE ( 'NONE', #18426, #42000 ) ;
#14811=CARTESIAN_POINT ( 'NONE',  ( -2.182111253630085290, 0.000000000000000000, -0.5118110236220464460 ) ) ;
#14813=FACE_OUTER_BOUND ( 'NONE', #25410, .T. ) ;
#14814=VECTOR ( 'NONE', #32044, 39.37007874015748143 ) ;
#14816=ORIENTED_EDGE ( 'NONE', *, *, #50750, .T. ) ;
#14817=CARTESIAN_POINT ( 'NONE',  ( 1.909347346926324462, 0.000000000000000000, -0.7874015748031473194 ) ) ;
#14818=LINE ( 'NONE', #22559, #42293 ) ;
#14820=ORIENTED_EDGE ( 'NONE', *, *, #527, .T. ) ;
#14821=( LENGTH_UNIT ( ) NAMED_UNIT ( * ) SI_UNIT ( $, .METRE. ) );
#14822=FACE_BOUND ( 'NONE', #41696, .T. ) ;
#14823=ORIENTED_EDGE ( 'NONE', *, *, #20683, .T. ) ;
#14825=ORIENTED_EDGE ( 'NONE', *, *, #21126, .T. ) ;
#14826=ORIENTED_EDGE ( 'NONE', *, *, #2114, .F. ) ;
#14828=LINE ( 'NONE', #2952, #18827 ) ;
#14831=EDGE_CURVE ( 'NONE', #13249, #20960, #45474, .T. ) ;
#14832=DIRECTION ( 'NONE',  ( -0.000000000000000000, 1.000000000000000000, -0.000000000000000000 ) ) ;
#14834=ORIENTED_EDGE ( 'NONE', *, *, #10399, .F. ) ;
#14835=ADVANCED_FACE ( 'NONE', ( #24614 ), #40372, .F. ) ;
#14837=ORIENTED_EDGE ( 'NONE', *, *, #23910, .T. ) ;
#14838=DIRECTION ( 'NONE',  ( 1.734723475976806848E-16, -0.000000000000000000, 1.000000000000000000 ) ) ;
#14839=EDGE_CURVE ( 'NONE', #10544, #27409, #11148, .T. ) ;
#14841=VECTOR ( 'NONE', #44270, 39.37007874015748143 ) ;
#14842=FACE_OUTER_BOUND ( 'NONE', #21013, .T. ) ;
#14843=DIRECTION ( 'NONE',  ( -1.000000000000000000, 0.000000000000000000, 1.734723475976806848E-16 ) ) ;
#14845=EDGE_LOOP ( 'NONE', ( #32338, #6709, #5389, #4754 ) ) ;
#14846=LINE ( 'NONE', #22342, #13502 ) ;
#14848=CARTESIAN_POINT ( 'NONE',  ( -0.8182917201112819283, 0.000000000000000000, -1.732283464566922726 ) ) ;
#14849=VECTOR ( 'NONE', #42315, 39.37007874015748143 ) ;
#14850=VERTEX_POINT ( 'NONE', #15274 ) ;
#14851=DIRECTION ( 'NONE',  ( -0.000000000000000000, 1.000000000000000000, -0.000000000000000000 ) ) ;
#14855=LINE ( 'NONE', #15355, #21217 ) ;
#14858=CARTESIAN_POINT ( 'NONE',  ( -0.8182917201112814842, 3.267716535433071279, 1.102362204724404160 ) ) ;
#14859=CARTESIAN_POINT ( 'NONE',  ( -0.2727639067037608278, 0.000000000000000000, -1.614173228346451605 ) ) ;
#14860=EDGE_CURVE ( 'NONE', #9111, #48211, #38279, .T. ) ;
#14861=ORIENTED_EDGE ( 'NONE', *, *, #18290, .T. ) ;
#14863=AXIS2_PLACEMENT_3D ( 'NONE', #3430, #22541, #15301 ) ;
#14865=FACE_BOUND ( 'NONE', #33242, .T. ) ;
#14868=ORIENTED_EDGE ( 'NONE', *, *, #37414, .T. ) ;
#14870=CARTESIAN_POINT ( 'NONE',  ( -1.909347346926324906, 0.000000000000000000, 1.417322834645662333 ) ) ;
#14871=LINE ( 'NONE', #26733, #29589 ) ;
#14872=CARTESIAN_POINT ( 'NONE',  ( -1.091055626815042645, 3.267716535433071279, -7.512581982576723358E-16 ) ) ;
#14873=DIRECTION ( 'NONE',  ( -1.000000000000000000, 0.000000000000000000, 1.734723475976806848E-16 ) ) ;
#14874=CARTESIAN_POINT ( 'NONE',  ( 0.8182917201112819283, 0.000000000000000000, -1.299212598425193210 ) ) ;
#14875=LINE ( 'NONE', #12010, #37203 ) ;
#14876=ORIENTED_EDGE ( 'NONE', *, *, #47497, .F. ) ;
#14877=EDGE_LOOP ( 'NONE', ( #42436, #6671, #34879, #40150 ) ) ;
#14878=DIRECTION ( 'NONE',  ( 1.000000000000000000, 0.000000000000000000, -3.469446951953613696E-16 ) ) ;
#14879=LINE ( 'NONE', #26742, #19035 ) ;
#14884=ORIENTED_EDGE ( 'NONE', *, *, #28652, .T. ) ;
#14885=AXIS2_PLACEMENT_3D ( 'NONE', #36048, #35789, #23652 ) ;
#14886=VECTOR ( 'NONE', #17101, 39.37007874015748143 ) ;
#14887=VERTEX_POINT ( 'NONE', #41886 ) ;
#14889=CARTESIAN_POINT ( 'NONE',  ( -1.439733046521776583, 0.000000000000000000, -0.9448818897637762948 ) ) ;
#14890=EDGE_CURVE ( 'NONE', #37147, #26914, #22018, .T. ) ;
#14892=AXIS2_PLACEMENT_3D ( 'NONE', #14935, #13923, #22431 ) ;
#14893=LINE ( 'NONE', #3520, #46006 ) ;
#14894=LINE ( 'NONE', #10514, #8761 ) ;
#14897=DIRECTION ( 'NONE',  ( 1.734723475976806848E-16, -0.000000000000000000, 1.000000000000000000 ) ) ;
#14901=ORIENTED_EDGE ( 'NONE', *, *, #10282, .T. ) ;
#14902=DIRECTION ( 'NONE',  ( 1.000000000000000000, 0.000000000000000000, 0.000000000000000000 ) ) ;
#14904=DIRECTION ( 'NONE',  ( -0.000000000000000000, 1.000000000000000000, -0.000000000000000000 ) ) ;
#14905=LINE ( 'NONE', #35036, #14141 ) ;
#14906=ORIENTED_EDGE ( 'NONE', *, *, #38281, .F. ) ;
#14907=DIRECTION ( 'NONE',  ( 1.734723475976806848E-16, -0.000000000000000000, 1.000000000000000000 ) ) ;
#14908=EDGE_CURVE ( 'NONE', #15326, #18533, #42260, .T. ) ;
#14909=CARTESIAN_POINT ( 'NONE',  ( 0.000000000000000000, 3.267716535433071279, -0.03937007874015881204 ) ) ;
#14912=CARTESIAN_POINT ( 'NONE',  ( -1.091055626815042645, 3.346456692913386100, -7.512581982576723358E-16 ) ) ;
#14913=EDGE_CURVE ( 'NONE', #27463, #8395, #30523, .T. ) ;
#14915=LINE ( 'NONE', #30919, #19957 ) ;
#14916=VERTEX_POINT ( 'NONE', #6528 ) ;
#14920=FACE_OUTER_BOUND ( 'NONE', #26394, .T. ) ;
#14922=LINE ( 'NONE', #11301, #9445 ) ;
#14923=CARTESIAN_POINT ( 'NONE',  ( 0.000000000000000000, 3.267716535433071279, -0.9842519685039348154 ) ) ;
#14925=DIRECTION ( 'NONE',  ( 0.000000000000000000, 0.000000000000000000, -1.000000000000000000 ) ) ;
#14926=ORIENTED_EDGE ( 'NONE', *, *, #36351, .F. ) ;
#14927=ORIENTED_EDGE ( 'NONE', *, *, #3465, .F. ) ;
#14928=CARTESIAN_POINT ( 'NONE',  ( -0.07591351300297277671, 3.346456692913386100, 1.102362204724404160 ) ) ;
#14930=CARTESIAN_POINT ( 'NONE',  ( -1.439733046521776583, 3.346456692913386100, -0.6299212598425177889 ) ) ;
#14931=VECTOR ( 'NONE', #3759, 39.37007874015748143 ) ;
#14932=DIRECTION ( 'NONE',  ( -1.000000000000000000, 0.000000000000000000, 0.000000000000000000 ) ) ;
#14934=VERTEX_POINT ( 'NONE', #49579 ) ;
#14935=CARTESIAN_POINT ( 'NONE',  ( -0.8182917201112814842, 0.000000000000000000, 1.102362204724404160 ) ) ;
#14937=DIRECTION ( 'NONE',  ( -0.000000000000000000, 1.000000000000000000, -0.000000000000000000 ) ) ;
#14939=ORIENTED_EDGE ( 'NONE', *, *, #38469, .T. ) ;
#14941=FACE_BOUND ( 'NONE', #1842, .T. ) ;
#14943=PLANE ( 'NONE',  #40244 ) ;
#14944=ORIENTED_EDGE ( 'NONE', *, *, #37836, .F. ) ;
#14945=VERTEX_POINT ( 'NONE', #50331 ) ;
#14946=CARTESIAN_POINT ( 'NONE',  ( 1.363819533518803695, 3.267716535433071279, 1.605145679676862835 ) ) ;
#14948=DIRECTION ( 'NONE',  ( -0.000000000000000000, 0.000000000000000000, 1.000000000000000000 ) ) ;
#14949=ORIENTED_EDGE ( 'NONE', *, *, #18580, .T. ) ;
#14950=VECTOR ( 'NONE', #39708, 39.37007874015748143 ) ;
#14951=CARTESIAN_POINT ( 'NONE',  ( -1.091055626815042423, 3.267716535433071279, 1.892679809432644143E-16 ) ) ;
#14952=VERTEX_POINT ( 'NONE', #30013 ) ;
#14954=EDGE_CURVE ( 'NONE', #7296, #21655, #30770, .T. ) ;
#14955=VECTOR ( 'NONE', #50653, 39.37007874015748143 ) ;
#14956=LINE ( 'NONE', #30707, #22554 ) ;
#14957=MECHANICAL_DESIGN_GEOMETRIC_PRESENTATION_REPRESENTATION('',(#8357),#16619);
#14958=EDGE_CURVE ( 'NONE', #40779, #18488, #7281, .T. ) ;
#14959=ADVANCED_FACE ( 'NONE', ( #45984 ), #38772, .F. ) ;
#14960=DIRECTION ( 'NONE',  ( -1.000000000000000000, 0.000000000000000000, 1.734723475976806848E-16 ) ) ;
#14962=ORIENTED_EDGE ( 'NONE', *, *, #42264, .T. ) ;
#14963=VECTOR ( 'NONE', #27997, 39.37007874015748143 ) ;
#14964=LINE ( 'NONE', #23452, #11271 ) ;
#14965=LINE ( 'NONE', #19577, #31115 ) ;
#14967=AXIS2_PLACEMENT_3D ( 'NONE', #28383, #37432, #48482 ) ;
#14968=LINE ( 'NONE', #26828, #34245 ) ;
#14970=VECTOR ( 'NONE', #45302, 39.37007874015748143 ) ;
#14971=CARTESIAN_POINT ( 'NONE',  ( -2.417802884545332542, 3.267716535433071279, -0.3543307086614173040 ) ) ;
#14972=EDGE_CURVE ( 'NONE', #39122, #9992, #18390, .T. ) ;
#14973=LINE ( 'NONE', #6215, #14340 ) ;
#14974=ORIENTED_EDGE ( 'NONE', *, *, #44435, .T. ) ;
#14975=FACE_OUTER_BOUND ( 'NONE', #14182, .T. ) ;
#14976=CARTESIAN_POINT ( 'NONE',  ( 1.015142113812069313, 3.267716535433071279, 0.9055118110236164419 ) ) ;
#14977=EDGE_CURVE ( 'NONE', #5175, #29752, #10648, .T. ) ;
#14979=ORIENTED_EDGE ( 'NONE', *, *, #16636, .T. ) ;
#14981=CARTESIAN_POINT ( 'NONE',  ( 0.7423782071083085965, 0.000000000000000000, -0.1968503937007880511 ) ) ;
#14983=EDGE_CURVE ( 'NONE', #17597, #4354, #12614, .T. ) ;
#14984=ORIENTED_EDGE ( 'NONE', *, *, #46387, .T. ) ;
#14988=VECTOR ( 'NONE', #43709, 39.37007874015748143 ) ;
#14989=LINE ( 'NONE', #6231, #38374 ) ;
#14990=CARTESIAN_POINT ( 'NONE',  ( 0.1968503937007873017, 3.267716535433071279, 0.6299212598425161236 ) ) ;
#14992=ORIENTED_EDGE ( 'NONE', *, *, #5162, .T. ) ;
#14995=ORIENTED_EDGE ( 'NONE', *, *, #29777, .F. ) ;
#14996=EDGE_LOOP ( 'NONE', ( #8829, #26218, #44949, #45114 ) ) ;
#14997=ADVANCED_FACE ( 'NONE', ( #40750 ), #44096, .F. ) ;
#14998=LINE ( 'NONE', #42851, #12827 ) ;
#14999=VECTOR ( 'NONE', #39448, 39.37007874015748143 ) ;
#15000=PLANE ( 'NONE',  #6714 ) ;
#15002=EDGE_CURVE ( 'NONE', #4018, #24951, #24491, .T. ) ;
#15003=VECTOR ( 'NONE', #50590, 39.37007874015748143 ) ;
#15006=DIRECTION ( 'NONE',  ( -0.000000000000000000, 1.000000000000000000, -0.000000000000000000 ) ) ;
#15007=ORIENTED_EDGE ( 'NONE', *, *, #36607, .F. ) ;
#15008=DIRECTION ( 'NONE',  ( -3.469446951953613696E-16, 0.000000000000000000, -1.000000000000000000 ) ) ;
#15009=ORIENTED_EDGE ( 'NONE', *, *, #1463, .F. ) ;
#15011=CARTESIAN_POINT ( 'NONE',  ( 0.2727639067037610499, 3.346456692913386100, 1.417322834645662777 ) ) ;
#15013=DIRECTION ( 'NONE',  ( -0.000000000000000000, 1.000000000000000000, -0.000000000000000000 ) ) ;
#15015=ADVANCED_FACE ( 'NONE', ( #40241 ), #48443, .F. ) ;
#15016=EDGE_CURVE ( 'NONE', #50839, #45040, #24745, .T. ) ;
#15017=CARTESIAN_POINT ( 'NONE',  ( 0.5455278134075212115, 0.000000000000000000, -1.259842519685035134 ) ) ;
#15018=ORIENTED_EDGE ( 'NONE', *, *, #9998, .F. ) ;
#15019=ORIENTED_EDGE ( 'NONE', *, *, #1770, .F. ) ;
#15020=DIRECTION ( 'NONE',  ( -1.000000000000000000, -0.000000000000000000, -0.000000000000000000 ) ) ;
#15022=ORIENTED_EDGE ( 'NONE', *, *, #1666, .T. ) ;
#15024=PLANE ( 'NONE',  #45735 ) ;
#15028=CIRCLE ( 'NONE', #42221, 2.106299212598425008 ) ;
#15030=ORIENTED_EDGE ( 'NONE', *, *, #3676, .T. ) ;
#15032=CARTESIAN_POINT ( 'NONE',  ( 0.8182917201112819283, 3.267716535433071279, 0.9055118110236164419 ) ) ;
#15033=CIRCLE ( 'NONE', #40575, 2.106299212598425008 ) ;
#15034=CARTESIAN_POINT ( 'NONE',  ( -1.091055626815042201, 3.346456692913386100, 1.259842519685033357 ) ) ;
#15036=VECTOR ( 'NONE', #48908, 39.37007874015748143 ) ;
#15037=FACE_OUTER_BOUND ( 'NONE', #1275, .T. ) ;
#15038=CARTESIAN_POINT ( 'NONE',  ( -1.091055626815042645, 3.346456692913386100, 1.801691980386209258 ) ) ;
#15039=CARTESIAN_POINT ( 'NONE',  ( 1.287906020515830141, 3.267716535433071279, 0.6299212598425161236 ) ) ;
#15040=EDGE_LOOP ( 'NONE', ( #39590, #21110, #47273, #11480 ) ) ;
#15041=EDGE_CURVE ( 'NONE', #49607, #38635, #28862, .T. ) ;
#15042=CARTESIAN_POINT ( 'NONE',  ( 0.4696143004045479352, 3.346456692913386100, 0.4724409448818868706 ) ) ;
#15045=VERTEX_POINT ( 'NONE', #36367 ) ;
#15046=PLANE ( 'NONE',  #47595 ) ;
#15047=EDGE_CURVE ( 'NONE', #7771, #7991, #21131, .T. ) ;
#15048=ORIENTED_EDGE ( 'NONE', *, *, #11561, .T. ) ;
#15049=LINE ( 'NONE', #50605, #44133 ) ;
#15050=CARTESIAN_POINT ( 'NONE',  ( -0.3486774197067334380, 3.267716535433071279, 0.6299212598425164567 ) ) ;
#15051=LINE ( 'NONE', #32594, #28524 ) ;
#15052=EDGE_CURVE ( 'NONE', #36717, #16462, #44349, .T. ) ;
#15058=CARTESIAN_POINT ( 'NONE',  ( -0.4513972801127658641, 3.267716535433071279, -2.401574803149598036 ) ) ;
#15059=ORIENTED_EDGE ( 'NONE', *, *, #36250, .T. ) ;
#15061=CARTESIAN_POINT ( 'NONE',  ( 1.560669927219590303, 3.346456692913386100, -1.614173228346452715 ) ) ;
#15062=DIRECTION ( 'NONE',  ( 0.000000000000000000, -1.000000000000000000, 0.000000000000000000 ) ) ;
#15063=ORIENTED_EDGE ( 'NONE', *, *, #4398, .F. ) ;
#15064=VERTEX_POINT ( 'NONE', #19382 ) ;
#15066=PLANE ( 'NONE',  #10131 ) ;
#15068=EDGE_CURVE ( 'NONE', #34446, #35684, #5119, .T. ) ;
#15069=ORIENTED_EDGE ( 'NONE', *, *, #23770, .F. ) ;
#15071=VECTOR ( 'NONE', #48673, 39.37007874015748143 ) ;
#15072=DIRECTION ( 'NONE',  ( -0.000000000000000000, 1.000000000000000000, -0.000000000000000000 ) ) ;
#15074=DIRECTION ( 'NONE',  ( -1.000000000000000000, 0.000000000000000000, 0.000000000000000000 ) ) ;
#15077=VERTEX_POINT ( 'NONE', #1247 ) ;
#15078=DIRECTION ( 'NONE',  ( 1.734723475976806848E-16, -0.000000000000000000, 1.000000000000000000 ) ) ;
#15080=AXIS2_PLACEMENT_3D ( 'NONE', #17125, #17888, #45221 ) ;
#15081=ADVANCED_FACE ( 'NONE', ( #17005 ), #32765, .F. ) ;
#15082=VECTOR ( 'NONE', #30203, 39.37007874015748143 ) ;
#15084=CARTESIAN_POINT ( 'NONE',  ( 0.1968503937007872462, 3.346456692913386100, 0.4330708661417287386 ) ) ;
#15085=EDGE_CURVE ( 'NONE', #30042, #22568, #9250, .T. ) ;
#15086=ADVANCED_FACE ( 'NONE', ( #50829 ), #23516, .F. ) ;
#15088=ORIENTED_EDGE ( 'NONE', *, *, #32795, .T. ) ;
#15090=EDGE_LOOP ( 'NONE', ( #36436, #32057, #12442, #49883 ) ) ;
#15091=CARTESIAN_POINT ( 'NONE',  ( -1.091055626815042201, 3.346456692913386100, 0.7480314960629874665 ) ) ;
#15095=EDGE_LOOP ( 'NONE', ( #6462, #48137, #48386, #21977, #27658 ) ) ;
#15096=CARTESIAN_POINT ( 'NONE',  ( -0.5455278134075217666, 3.267716535433071279, 9.463399047163231808E-17 ) ) ;
#15098=EDGE_LOOP ( 'NONE', ( #10497, #32034, #41101, #7932 ) ) ;
#15099=CARTESIAN_POINT ( 'NONE',  ( -0.07591351300297284610, 0.000000000000000000, 1.220472440944875281 ) ) ;
#15101=LINE ( 'NONE', #8113, #14785 ) ;
#15102=CARTESIAN_POINT ( 'NONE',  ( 0.4696143004045478797, 0.000000000000000000, -0.03937007874015908959 ) ) ;
#15103=PLANE ( 'NONE',  #45593 ) ;
#15104=FACE_OUTER_BOUND ( 'NONE', #4789, .T. ) ;
#15105=VECTOR ( 'NONE', #47530, 39.37007874015748143 ) ;
#15106=ORIENTED_EDGE ( 'NONE', *, *, #25453, .F. ) ;
#15107=LINE ( 'NONE', #34235, #13973 ) ;
#15108=EDGE_LOOP ( 'NONE', ( #43546, #1220, #31061, #29800 ) ) ;
#15109=CARTESIAN_POINT ( 'NONE',  ( 1.833433833923351353, 3.267716535433071279, 0.1181102362204701633 ) ) ;
#15113=CARTESIAN_POINT ( 'NONE',  ( 1.363819533518803251, 3.267716535433071279, -2.365849761790805487E-16 ) ) ;
#15114=EDGE_CURVE ( 'NONE', #25737, #40030, #1503, .T. ) ;
#15115=EDGE_CURVE ( 'NONE', #1147, #1290, #31280, .T. ) ;
#15116=VERTEX_POINT ( 'NONE', #41507 ) ;
#15117=VERTEX_POINT ( 'NONE', #41263 ) ;
#15118=CARTESIAN_POINT ( 'NONE',  ( -2.182111253630085290, 3.346456692913386100, -0.5118110236220464460 ) ) ;
#15120=CARTESIAN_POINT ( 'NONE',  ( 0.000000000000000000, 3.346456692913386100, 0.000000000000000000 ) ) ;
#15122=DIRECTION ( 'NONE',  ( 0.000000000000000000, 0.000000000000000000, -1.000000000000000000 ) ) ;
#15123=DIRECTION ( 'NONE',  ( 0.000000000000000000, -1.000000000000000000, 0.000000000000000000 ) ) ;
#15124=EDGE_CURVE ( 'NONE', #47754, #30246, #6139, .T. ) ;
#15126=VERTEX_POINT ( 'NONE', #9506 ) ;
#15127=ORIENTED_EDGE ( 'NONE', *, *, #17932, .T. ) ;
#15128=CARTESIAN_POINT ( 'NONE',  ( 0.7423782071083092626, 0.000000000000000000, 1.574803149606291974 ) ) ;
#15129=CARTESIAN_POINT ( 'NONE',  ( -0.8182917201112814842, 3.346456692913386100, 1.732283464566921172 ) ) ;
#15132=EDGE_LOOP ( 'NONE', ( #15856, #29459, #30793, #4086 ) ) ;
#15133=VERTEX_POINT ( 'NONE', #5631 ) ;
#15135=EDGE_CURVE ( 'NONE', #16989, #19095, #25254, .T. ) ;
#15136=ORIENTED_EDGE ( 'NONE', *, *, #35823, .F. ) ;
#15138=LINE ( 'NONE', #42003, #20289 ) ;
#15140=VECTOR ( 'NONE', #36728, 39.37007874015748143 ) ;
#15143=FACE_OUTER_BOUND ( 'NONE', #35708, .T. ) ;
#15145=ADVANCED_FACE ( 'NONE', ( #1750 ), #10264, .F. ) ;
#15148=AXIS2_PLACEMENT_3D ( 'NONE', #6271, #14015, #29761 ) ;
#15150=CARTESIAN_POINT ( 'NONE',  ( -4.268512490100411402E-16, 0.000000000000000000, -2.401574803149598480 ) ) ;
#15152=AXIS2_PLACEMENT_3D ( 'NONE', #16041, #28157, #32058 ) ;
#15154=DIRECTION ( 'NONE',  ( -1.000000000000000000, 0.000000000000000000, -0.000000000000000000 ) ) ;
#15156=CARTESIAN_POINT ( 'NONE',  ( 1.833433833923351353, 3.346456692913386100, 0.1181102362204701633 ) ) ;
#15158=VERTEX_POINT ( 'NONE', #6399 ) ;
#15159=DIRECTION ( 'NONE',  ( -1.000000000000000000, 0.000000000000000000, 1.734723475976806848E-16 ) ) ;
#15160=CARTESIAN_POINT ( 'NONE',  ( -0.5455278134075214336, 0.000000000000000000, -1.574803149606293529 ) ) ;
#15163=CARTESIAN_POINT ( 'NONE',  ( 0.000000000000000000, 0.000000000000000000, 0.000000000000000000 ) ) ;
#15165=VERTEX_POINT ( 'NONE', #22146 ) ;
#15166=CARTESIAN_POINT ( 'NONE',  ( -0.6214413264104945434, 0.000000000000000000, -0.9842519685039342603 ) ) ;
#15168=DIRECTION ( 'NONE',  ( -1.000000000000000000, -0.000000000000000000, -0.000000000000000000 ) ) ;
#15169=DIRECTION ( 'NONE',  ( -1.000000000000000000, -0.000000000000000000, -0.000000000000000000 ) ) ;
#15170=LINE ( 'NONE', #12835, #45716 ) ;
#15171=EDGE_LOOP ( 'NONE', ( #24340, #7613, #14217, #36446 ) ) ;
#15174=ORIENTED_EDGE ( 'NONE', *, *, #24575, .F. ) ;
#15176=AXIS2_PLACEMENT_3D ( 'NONE', #16426, #12034, #47619 ) ;
#15177=EDGE_CURVE ( 'NONE', #20686, #15727, #45354, .T. ) ;
#15178=DIRECTION ( 'NONE',  ( -0.000000000000000000, 1.000000000000000000, -0.000000000000000000 ) ) ;
#15181=VECTOR ( 'NONE', #41223, 39.37007874015748143 ) ;
#15182=PLANE ( 'NONE',  #36799 ) ;
#15183=EDGE_LOOP ( 'NONE', ( #25334, #48440, #7080, #43407 ) ) ;
#15184=EDGE_CURVE ( 'NONE', #24477, #7825, #37903, .T. ) ;
#15186=VECTOR ( 'NONE', #43589, 39.37007874015748143 ) ;
#15188=CARTESIAN_POINT ( 'NONE',  ( 0.000000000000000000, 3.267716535433071279, -0.1968503937007886062 ) ) ;
#15189=VECTOR ( 'NONE', #44364, 39.37007874015748143 ) ;
#15193=FACE_BOUND ( 'NONE', #6475, .T. ) ;
#15195=PLANE ( 'NONE',  #37748 ) ;
#15196=EDGE_CURVE ( 'NONE', #15817, #8923, #30139, .T. ) ;
#15198=ORIENTED_EDGE ( 'NONE', *, *, #33400, .F. ) ;
#15201=EDGE_CURVE ( 'NONE', #13274, #22175, #17759, .T. ) ;
#15202=ORIENTED_EDGE ( 'NONE', *, *, #14958, .F. ) ;
#15203=DIRECTION ( 'NONE',  ( -0.000000000000000000, 1.000000000000000000, -0.000000000000000000 ) ) ;
#15204=ORIENTED_EDGE ( 'NONE', *, *, #9528, .T. ) ;
#15211=PLANE ( 'NONE',  #14592 ) ;
#15212=LINE ( 'NONE', #4107, #10512 ) ;
#15213=VECTOR ( 'NONE', #26389, 39.37007874015748143 ) ;
#15215=VECTOR ( 'NONE', #29335, 39.37007874015748143 ) ;
#15216=EDGE_CURVE ( 'NONE', #1801, #12300, #2266, .T. ) ;
#15224=VERTEX_POINT ( 'NONE', #10520 ) ;
#15227=ORIENTED_EDGE ( 'NONE', *, *, #41545, .T. ) ;
#15228=ORIENTED_EDGE ( 'NONE', *, *, #31435, .T. ) ;
#15230=LINE ( 'NONE', #30979, #10532 ) ;
#15231=ORIENTED_EDGE ( 'NONE', *, *, #41481, .T. ) ;
#15235=CARTESIAN_POINT ( 'NONE',  ( -2.182111253630085290, 3.346456692913386100, 0.6299212598425164567 ) ) ;
#15236=ORIENTED_EDGE ( 'NONE', *, *, #22020, .F. ) ;
#15238=CARTESIAN_POINT ( 'NONE',  ( -0.2727639067037602172, 3.346456692913386100, 2.047244094488179567 ) ) ;
#15239=CARTESIAN_POINT ( 'NONE',  ( 1.287906020515830141, 3.267716535433071279, -4.468321617281355077E-16 ) ) ;
#15240=EDGE_CURVE ( 'NONE', #19363, #43652, #44852, .T. ) ;
#15241=EDGE_CURVE ( 'NONE', #22479, #35392, #38897, .T. ) ;
#15242=VERTEX_POINT ( 'NONE', #46863 ) ;
#15243=FACE_OUTER_BOUND ( 'NONE', #29667, .T. ) ;
#15244=AXIS2_PLACEMENT_3D ( 'NONE', #44158, #27898, #11650 ) ;
#15245=ORIENTED_EDGE ( 'NONE', *, *, #24712, .T. ) ;
#15247=VECTOR ( 'NONE', #5439, 39.37007874015748143 ) ;
#15249=CARTESIAN_POINT ( 'NONE',  ( -1.863748091109392213, 3.267716535433071279, -1.102362204724405492 ) ) ;
#15251=VECTOR ( 'NONE', #22609, 39.37007874015748143 ) ;
#15253=LINE ( 'NONE', #11130, #31991 ) ;
#15254=EDGE_CURVE ( 'NONE', #3461, #15126, #3788, .T. ) ;
#15255=LINE ( 'NONE', #42613, #20887 ) ;
#15256=VERTEX_POINT ( 'NONE', #31408 ) ;
#15257=DIRECTION ( 'NONE',  ( -1.000000000000000000, 0.000000000000000000, 0.000000000000000000 ) ) ;
#15258=CIRCLE ( 'NONE', #47353, 2.165354330708661568 ) ;
#15260=ORIENTED_EDGE ( 'NONE', *, *, #24324, .F. ) ;
#15262=ORIENTED_EDGE ( 'NONE', *, *, #21437, .F. ) ;
#15263=CARTESIAN_POINT ( 'NONE',  ( 0.000000000000000000, 3.267716535433071279, 0.000000000000000000 ) ) ;
#15264=PLANE ( 'NONE',  #26638 ) ;
#15265=SHAPE_REPRESENTATION ( 'Back Cover', ( #26741 ), #3635 ) ;
#15267=CARTESIAN_POINT ( 'NONE',  ( 0.000000000000000000, 3.267716535433071279, -0.3149606299212593941 ) ) ;
#15268=CARTESIAN_POINT ( 'NONE',  ( -0.2727639067037607723, 3.346456692913386100, -0.7874015748031470974 ) ) ;
#15270=ORIENTED_EDGE ( 'NONE', *, *, #29122, .F. ) ;
#15272=CARTESIAN_POINT ( 'NONE',  ( 0.000000000000000000, 3.267716535433071279, 0.1181102362204698858 ) ) ;
#15273=VERTEX_POINT ( 'NONE', #42763 ) ;
#15274=CARTESIAN_POINT ( 'NONE',  ( -0.6214413264104945434, 3.267716535433071279, -0.6692913385826760875 ) ) ;
#15275=EDGE_CURVE ( 'NONE', #20943, #21582, #42255, .T. ) ;
#15276=CARTESIAN_POINT ( 'NONE',  ( -1.636583440222564301, 3.346456692913386100, -0.3149606299212592275 ) ) ;
#15277=CARTESIAN_POINT ( 'NONE',  ( 0.5455278134075216556, 3.267716535433071279, 2.034427629037600660 ) ) ;
#15279=CARTESIAN_POINT ( 'NONE',  ( 1.015142113812069091, 3.267716535433071279, -2.222792731763669760 ) ) ;
#15281=VECTOR ( 'NONE', #46865, 39.37007874015748143 ) ;
#15282=FACE_OUTER_BOUND ( 'NONE', #36550, .T. ) ;
#15283=DIRECTION ( 'NONE',  ( -1.000000000000000000, 0.000000000000000000, 0.000000000000000000 ) ) ;
#15284=VECTOR ( 'NONE', #28642, 39.37007874015748143 ) ;
#15285=EDGE_CURVE ( 'NONE', #383, #17591, #50706, .T. ) ;
#15286=AXIS2_PLACEMENT_3D ( 'NONE', #6489, #3110, #26848 ) ;
#15287=VERTEX_POINT ( 'NONE', #47108 ) ;
#15288=PLANE ( 'NONE',  #49596 ) ;
#15289=FACE_OUTER_BOUND ( 'NONE', #434, .T. ) ;
#15290=LINE ( 'NONE', #35166, #3247 ) ;
#15291=VECTOR ( 'NONE', #27615, 39.37007874015748143 ) ;
#15293=AXIS2_PLACEMENT_3D ( 'NONE', #10420, #26169, #45503 ) ;
#15294=ORIENTED_EDGE ( 'NONE', *, *, #35249, .F. ) ;
#15296=ORIENTED_EDGE ( 'NONE', *, *, #11, .F. ) ;
#15297=LINE ( 'NONE', #39040, #5625 ) ;
#15300=DIRECTION ( 'NONE',  ( -1.000000000000000000, -0.000000000000000000, -0.000000000000000000 ) ) ;
#15301=DIRECTION ( 'NONE',  ( 1.734723475976806848E-16, 0.000000000000000000, 1.000000000000000000 ) ) ;
#15302=CARTESIAN_POINT ( 'NONE',  ( -0.8182917201112819283, 3.267716535433071279, -2.047244094488181343 ) ) ;
#15303=EDGE_CURVE ( 'NONE', #7498, #19545, #23657, .T. ) ;
#15304=ORIENTED_EDGE ( 'NONE', *, *, #35534, .F. ) ;
#15306=VERTEX_POINT ( 'NONE', #11531 ) ;
#15308=DIRECTION ( 'NONE',  ( -1.000000000000000000, 0.000000000000000000, -0.000000000000000000 ) ) ;
#15309=ORIENTED_EDGE ( 'NONE', *, *, #5065, .T. ) ;
#15310=ORIENTED_EDGE ( 'NONE', *, *, #41453, .T. ) ;
#15311=DIRECTION ( 'NONE',  ( -0.000000000000000000, 1.000000000000000000, -0.000000000000000000 ) ) ;
#15316=CARTESIAN_POINT ( 'NONE',  ( -0.8942052331142552601, 3.267716535433071279, -0.6299212598425177889 ) ) ;
#15318=DIRECTION ( 'NONE',  ( 1.000000000000000000, -0.000000000000000000, 0.000000000000000000 ) ) ;
#15319=EDGE_LOOP ( 'NONE', ( #15310, #46189, #17852, #16222 ) ) ;
#15320=CARTESIAN_POINT ( 'NONE',  ( 2.106197740627111958, 3.267716535433071279, -7.307341331430321661E-16 ) ) ;
#15321=DIRECTION ( 'NONE',  ( 1.000000000000000000, 0.000000000000000000, 0.000000000000000000 ) ) ;
#15323=VERTEX_POINT ( 'NONE', #3029 ) ;
#15325=LINE ( 'NONE', #26687, #34859 ) ;
#15326=VERTEX_POINT ( 'NONE', #14649 ) ;
#15327=ORIENTED_EDGE ( 'NONE', *, *, #41409, .T. ) ;
#15328=CARTESIAN_POINT ( 'NONE',  ( 1.015142113812069313, 3.267716535433071279, 1.102362204724403938 ) ) ;
#15331=DIRECTION ( 'NONE',  ( -3.469446951953613696E-16, 0.000000000000000000, -1.000000000000000000 ) ) ;
#15332=AXIS2_PLACEMENT_3D ( 'NONE', #28200, #9357, #40352 ) ;
#15333=EDGE_CURVE ( 'NONE', #13884, #18498, #3531, .T. ) ;
#15335=LINE ( 'NONE', #30834, #39492 ) ;
#15337=ORIENTED_EDGE ( 'NONE', *, *, #27647, .T. ) ;
#15339=ORIENTED_EDGE ( 'NONE', *, *, #28389, .T. ) ;
#15340=DIRECTION ( 'NONE',  ( -0.000000000000000000, 1.000000000000000000, -0.000000000000000000 ) ) ;
#15341=EDGE_CURVE ( 'NONE', #31898, #34706, #15412, .T. ) ;
#15343=ADVANCED_FACE ( 'NONE', ( #34276 ), #23397, .F. ) ;
#15344=EDGE_CURVE ( 'NONE', #17266, #2383, #49966, .T. ) ;
#15345=CARTESIAN_POINT ( 'NONE',  ( 1.636583440222563857, 0.000000000000000000, 0.4330708661417290162 ) ) ;
#15347=CARTESIAN_POINT ( 'NONE',  ( 0.5455278134075217666, 3.346456692913386100, 1.574803149606291974 ) ) ;
#15348=ORIENTED_EDGE ( 'NONE', *, *, #10596, .F. ) ;
#15349=LINE ( 'NONE', #3217, #20901 ) ;
#15350=EDGE_CURVE ( 'NONE', #22912, #19510, #30396, .T. ) ;
#15351=CARTESIAN_POINT ( 'NONE',  ( -2.182111253630085290, 3.346456692913386100, -0.3149606299212589500 ) ) ;
#15352=EDGE_CURVE ( 'NONE', #12933, #15273, #10770, .T. ) ;
#15355=CARTESIAN_POINT ( 'NONE',  ( 0.8182917201112821504, 3.267716535433071279, -1.419509857074483539E-16 ) ) ;
#15357=VECTOR ( 'NONE', #8611, 39.37007874015748143 ) ;
#15358=DIRECTION ( 'NONE',  ( 1.734723475976806848E-16, 0.000000000000000000, 1.000000000000000000 ) ) ;
#15359=LINE ( 'NONE', #19471, #43245 ) ;
#15363=VERTEX_POINT ( 'NONE', #30648 ) ;
#15364=FACE_OUTER_BOUND ( 'NONE', #14734, .T. ) ;
#15365=ORIENTED_EDGE ( 'NONE', *, *, #11516, .T. ) ;
#15369=LINE ( 'NONE', #42219, #36709 ) ;
#15370=CARTESIAN_POINT ( 'NONE',  ( -1.363819533518803029, 3.346456692913386100, 0.1574803149606287811 ) ) ;
#15372=EDGE_CURVE ( 'NONE', #43170, #49343, #19017, .T. ) ;
#15373=AXIS2_PLACEMENT_3D ( 'NONE', #22871, #15123, #30876 ) ;
#15374=ORIENTED_EDGE ( 'NONE', *, *, #41773, .T. ) ;
#15375=ORIENTED_EDGE ( 'NONE', *, *, #8889, .T. ) ;
#15377=EDGE_CURVE ( 'NONE', #35545, #10279, #23329, .T. ) ;
#15378=CARTESIAN_POINT ( 'NONE',  ( 2.083268748869757658, 3.346456692913386100, 0.5905511811023582691 ) ) ;
#15380=DIRECTION ( 'NONE',  ( 1.734723475976806848E-16, -0.000000000000000000, 1.000000000000000000 ) ) ;
#15385=LINE ( 'NONE', #42983, #44715 ) ;
#15386=CARTESIAN_POINT ( 'NONE',  ( -0.2727639067037607723, 3.346456692913386100, 0.1574803149606283648 ) ) ;
#15388=CARTESIAN_POINT ( 'NONE',  ( -0.5455278134075214336, 3.267716535433071279, -1.456692913385822630 ) ) ;
#15390=VERTEX_POINT ( 'NONE', #8936 ) ;
#15392=VECTOR ( 'NONE', #6906, 39.37007874015748143 ) ;
#15395=LINE ( 'NONE', #19253, #12076 ) ;
#15396=ORIENTED_EDGE ( 'NONE', *, *, #10049, .F. ) ;
#15398=VECTOR ( 'NONE', #14838, 39.37007874015748143 ) ;
#15400=CARTESIAN_POINT ( 'NONE',  ( 1.015142113812069313, 3.346456692913386100, -0.7874015748031473194 ) ) ;
#15401=DIRECTION ( 'NONE',  ( -1.000000000000000000, 0.000000000000000000, 1.734723475976806848E-16 ) ) ;
#15402=CARTESIAN_POINT ( 'NONE',  ( -1.636583440222564301, 0.000000000000000000, -0.8267716535433052849 ) ) ;
#15405=ADVANCED_FACE ( 'NONE', ( #155 ), #16171, .F. ) ;
#15409=CARTESIAN_POINT ( 'NONE',  ( 0.000000000000000000, 0.000000000000000000, -2.165354330708661568 ) ) ;
#15411=VERTEX_POINT ( 'NONE', #40444 ) ;
#15412=LINE ( 'NONE', #7656, #1887 ) ;
#15416=EDGE_LOOP ( 'NONE', ( #36043, #28591, #47098, #5262 ) ) ;
#15417=CARTESIAN_POINT ( 'NONE',  ( -1.536664496436148184E-16, 0.000000000000000000, 0.1181102362204701633 ) ) ;
#15420=CARTESIAN_POINT ( 'NONE',  ( -1.363819533518803029, 0.000000000000000000, 0.4724409448818871482 ) ) ;
#15424=ORIENTED_EDGE ( 'NONE', *, *, #39447, .T. ) ;
#15427=EDGE_CURVE ( 'NONE', #17840, #2919, #36310, .T. ) ;
#15429=DIRECTION ( 'NONE',  ( 1.000000000000000000, 0.000000000000000000, 0.000000000000000000 ) ) ;
#15432=EDGE_CURVE ( 'NONE', #22927, #13982, #16689, .T. ) ;
#15433=VECTOR ( 'NONE', #21325, 39.37007874015748143 ) ;
#15434=ORIENTED_EDGE ( 'NONE', *, *, #10366, .F. ) ;
#15435=VERTEX_POINT ( 'NONE', #1192 ) ;
#15437=CARTESIAN_POINT ( 'NONE',  ( -0.8942052331142547050, 0.000000000000000000, 0.9448818897637749625 ) ) ;
#15439=ORIENTED_EDGE ( 'NONE', *, *, #6521, .F. ) ;
#15440=LINE ( 'NONE', #43550, #15542 ) ;
#15441=CARTESIAN_POINT ( 'NONE',  ( -1.636583440222564301, 0.000000000000000000, 1.574803149606291530 ) ) ;
#15442=ORIENTED_EDGE ( 'NONE', *, *, #72, .T. ) ;
#15443=DIRECTION ( 'NONE',  ( -3.469446951953613696E-16, 0.000000000000000000, -1.000000000000000000 ) ) ;
#15445=FACE_OUTER_BOUND ( 'NONE', #13347, .T. ) ;
#15446=ORIENTED_EDGE ( 'NONE', *, *, #11761, .F. ) ;
#15448=LINE ( 'NONE', #47405, #28173 ) ;
#15451=FACE_OUTER_BOUND ( 'NONE', #17706, .T. ) ;
#15452=ORIENTED_EDGE ( 'NONE', *, *, #42857, .T. ) ;
#15453=VERTEX_POINT ( 'NONE', #12301 ) ;
#15454=CARTESIAN_POINT ( 'NONE',  ( -1.166969139818015977, 0.000000000000000000, -1.732283464566922726 ) ) ;
#15458=FACE_OUTER_BOUND ( 'NONE', #15943, .T. ) ;
#15459=ORIENTED_EDGE ( 'NONE', *, *, #41091, .F. ) ;
#15461=FACE_OUTER_BOUND ( 'NONE', #31434, .T. ) ;
#15462=AXIS2_PLACEMENT_3D ( 'NONE', #36472, #33377, #45205 ) ;
#15463=VECTOR ( 'NONE', #23730, 39.37007874015748143 ) ;
#15464=DIRECTION ( 'NONE',  ( 1.000000000000000000, 0.000000000000000000, -3.469446951953613696E-16 ) ) ;
#15467=EDGE_CURVE ( 'NONE', #12919, #36525, #4553, .T. ) ;
#15470=ADVANCED_FACE ( 'NONE', ( #12041 ), #12551, .F. ) ;
#15472=VECTOR ( 'NONE', #50502, 39.37007874015748143 ) ;
#15474=ADVANCED_FACE ( 'NONE', ( #12816 ), #418, .F. ) ;
#15478=CARTESIAN_POINT ( 'NONE',  ( -1.091055626815042645, 0.000000000000000000, -0.6299212598425177889 ) ) ;
#15479=ORIENTED_EDGE ( 'NONE', *, *, #14243, .T. ) ;
#15481=AXIS2_PLACEMENT_3D ( 'NONE', #50649, #10965, #3981 ) ;
#15482=EDGE_LOOP ( 'NONE', ( #264, #44647, #13917, #41430 ) ) ;
#15483=ORIENTED_EDGE ( 'NONE', *, *, #28866, .T. ) ;
#15484=CARTESIAN_POINT ( 'NONE',  ( -0.3486774197067339376, 3.346456692913386100, 2.204724409448808764 ) ) ;
#15485=CARTESIAN_POINT ( 'NONE',  ( 0.5455278134075211005, 3.267716535433071279, -0.1968503937007880511 ) ) ;
#15486=EDGE_CURVE ( 'NONE', #10410, #16704, #8427, .T. ) ;
#15487=EDGE_LOOP ( 'NONE', ( #30754, #25053, #28007, #6346 ) ) ;
#15488=CARTESIAN_POINT ( 'NONE',  ( -0.5455278134075211005, 3.267716535433071279, 9.463399047163219482E-17 ) ) ;
#15490=ORIENTED_EDGE ( 'NONE', *, *, #3458, .T. ) ;
#15491=DIRECTION ( 'NONE',  ( 1.734723475976806848E-16, 0.000000000000000000, 1.000000000000000000 ) ) ;
#15492=ORIENTED_EDGE ( 'NONE', *, *, #29759, .T. ) ;
#15493=PLANE ( 'NONE',  #24397 ) ;
#15494=DIRECTION ( 'NONE',  ( -0.000000000000000000, 1.000000000000000000, -0.000000000000000000 ) ) ;
#15497=VERTEX_POINT ( 'NONE', #47876 ) ;
#15498=CARTESIAN_POINT ( 'NONE',  ( 2.182111253630085290, 3.346456692913386100, -0.5118110236220471121 ) ) ;
#15499=VERTEX_POINT ( 'NONE', #28290 ) ;
#15503=LINE ( 'NONE', #10868, #47421 ) ;
#15505=VERTEX_POINT ( 'NONE', #20555 ) ;
#15506=AXIS2_PLACEMENT_3D ( 'NONE', #48784, #13465, #5719 ) ;
#15507=DIRECTION ( 'NONE',  ( -0.000000000000000000, -1.000000000000000000, -0.000000000000000000 ) ) ;
#15508=DIRECTION ( 'NONE',  ( -0.000000000000000000, 0.000000000000000000, 1.000000000000000000 ) ) ;
#15509=ORIENTED_EDGE ( 'NONE', *, *, #20955, .T. ) ;
#15511=DIRECTION ( 'NONE',  ( -0.000000000000000000, 1.000000000000000000, -0.000000000000000000 ) ) ;
#15513=ORIENTED_EDGE ( 'NONE', *, *, #16762, .T. ) ;
#15515=EDGE_LOOP ( 'NONE', ( #38532, #29207, #8780, #41100 ) ) ;
#15516=DIRECTION ( 'NONE',  ( 1.734723475976806848E-16, -0.000000000000000000, 1.000000000000000000 ) ) ;
#15517=PLANE ( 'NONE',  #37386 ) ;
#15518=DIRECTION ( 'NONE',  ( -1.000000000000000000, 0.000000000000000000, 1.734723475976806848E-16 ) ) ;
#15519=LINE ( 'NONE', #43120, #27990 ) ;
#15520=ORIENTED_EDGE ( 'NONE', *, *, #22543, .F. ) ;
#15522=EDGE_CURVE ( 'NONE', #41844, #9230, #934, .T. ) ;
#15525=CARTESIAN_POINT ( 'NONE',  ( 0.4696143004045484903, 0.000000000000000000, 1.102362204724404160 ) ) ;
#15526=ORIENTED_EDGE ( 'NONE', *, *, #6783, .T. ) ;
#15527=DIRECTION ( 'NONE',  ( 1.000000000000000000, 0.000000000000000000, 0.000000000000000000 ) ) ;
#15528=LINE ( 'NONE', #47995, #22660 ) ;
#15531=AXIS2_PLACEMENT_3D ( 'NONE', #33551, #13918, #40065 ) ;
#15533=FACE_OUTER_BOUND ( 'NONE', #23358, .T. ) ;
#15534=DIRECTION ( 'NONE',  ( -0.000000000000000000, 0.000000000000000000, 1.000000000000000000 ) ) ;
#15535=CARTESIAN_POINT ( 'NONE',  ( 0.000000000000000000, 0.000000000000000000, -2.874015748031496731 ) ) ;
#15536=EDGE_LOOP ( 'NONE', ( #5578, #29290, #33422, #19462 ) ) ;
#15539=VECTOR ( 'NONE', #36480, 39.37007874015748143 ) ;
#15541=ORIENTED_EDGE ( 'NONE', *, *, #12415, .T. ) ;
#15542=VECTOR ( 'NONE', #16903, 39.37007874015748143 ) ;
#15543=CARTESIAN_POINT ( 'NONE',  ( 0.000000000000000000, 3.267716535433071279, -2.047244094488181343 ) ) ;
#15544=PLANE ( 'NONE',  #31915 ) ;
#15545=EDGE_CURVE ( 'NONE', #24313, #45537, #5317, .T. ) ;
#15546=ORIENTED_EDGE ( 'NONE', *, *, #3295, .T. ) ;
#15547=VECTOR ( 'NONE', #43821, 39.37007874015748143 ) ;
#15548=ADVANCED_FACE ( 'NONE', ( #30088 ), #49656, .F. ) ;
#15549=ORIENTED_EDGE ( 'NONE', *, *, #48840, .F. ) ;
#15552=VECTOR ( 'NONE', #4302, 39.37007874015748143 ) ;
#15555=DIRECTION ( 'NONE',  ( -0.000000000000000000, 1.000000000000000000, -0.000000000000000000 ) ) ;
#15560=EDGE_LOOP ( 'NONE', ( #84, #32477, #32390, #37298 ) ) ;
#15561=ORIENTED_EDGE ( 'NONE', *, *, #44271, .F. ) ;
#15562=LINE ( 'NONE', #47260, #35627 ) ;
#15564=ORIENTED_EDGE ( 'NONE', *, *, #17698, .F. ) ;
#15566=PLANE ( 'NONE',  #7472 ) ;
#15567=DIRECTION ( 'NONE',  ( -0.000000000000000000, 0.000000000000000000, 1.000000000000000000 ) ) ;
#15568=CARTESIAN_POINT ( 'NONE',  ( -2.182111253630085290, 3.346456692913386100, 0.3149606299212578953 ) ) ;
#15569=ADVANCED_FACE ( 'NONE', ( #1954 ), #44795, .F. ) ;
#15570=EDGE_LOOP ( 'NONE', ( #21627, #19285, #20650, #24517 ) ) ;
#15571=ORIENTED_EDGE ( 'NONE', *, *, #16053, .T. ) ;
#15572=CARTESIAN_POINT ( 'NONE',  ( -0.2727639067037608278, 3.267716535433071279, -1.614173228346451605 ) ) ;
#15573=DIRECTION ( 'NONE',  ( -1.000000000000000000, 0.000000000000000000, 1.734723475976806848E-16 ) ) ;
#15575=DIRECTION ( 'NONE',  ( -0.000000000000000000, 1.000000000000000000, -0.000000000000000000 ) ) ;
#15576=ORIENTED_EDGE ( 'NONE', *, *, #14076, .T. ) ;
#15577=PLANE ( 'NONE',  #2645 ) ;
#15578=CARTESIAN_POINT ( 'NONE',  ( 2.182111253630085290, 3.346456692913386100, 0.3149606299212573401 ) ) ;
#15580=DIRECTION ( 'NONE',  ( 0.000000000000000000, 0.000000000000000000, -1.000000000000000000 ) ) ;
#15583=CARTESIAN_POINT ( 'NONE',  ( 1.363819533518803251, 3.346456692913386100, -0.1574803149606304187 ) ) ;
#15585=AXIS2_PLACEMENT_3D ( 'NONE', #21566, #37326, #17690 ) ;
#15589=FACE_OUTER_BOUND ( 'NONE', #13241, .T. ) ;
#15590=ORIENTED_EDGE ( 'NONE', *, *, #47528, .F. ) ;
#15591=VERTEX_POINT ( 'NONE', #37850 ) ;
#15592=VECTOR ( 'NONE', #24886, 39.37007874015748143 ) ;
#15593=ORIENTED_EDGE ( 'NONE', *, *, #36468, .F. ) ;
#15594=CARTESIAN_POINT ( 'NONE',  ( 2.182111253630085290, 0.000000000000000000, 0.6299212598425161236 ) ) ;
#15595=DIRECTION ( 'NONE',  ( -3.469446951953613696E-16, 0.000000000000000000, -1.000000000000000000 ) ) ;
#15596=ADVANCED_FACE ( 'NONE', ( #36822 ), #17199, .F. ) ;
#15597=ADVANCED_FACE ( 'NONE', ( #29581 ), #13832, .F. ) ;
#15599=PLANE ( 'NONE',  #50869 ) ;
#15600=EDGE_LOOP ( 'NONE', ( #20903, #10561, #26975, #12192 ) ) ;
#15602=CARTESIAN_POINT ( 'NONE',  ( -0.5455278134075208785, 3.346456692913386100, 0.4330708661417290162 ) ) ;
#15603=EDGE_LOOP ( 'NONE', ( #49381, #7488, #38351, #6171 ) ) ;
#15607=VECTOR ( 'NONE', #19674, 39.37007874015748143 ) ;
#15608=ORIENTED_EDGE ( 'NONE', *, *, #3776, .T. ) ;
#15611=CARTESIAN_POINT ( 'NONE',  ( -2.142325647309101022, 3.267716535433071279, -0.3149606299212589500 ) ) ;
#15612=VERTEX_POINT ( 'NONE', #13326 ) ;
#15613=DIRECTION ( 'NONE',  ( -1.000000000000000000, 0.000000000000000000, 0.000000000000000000 ) ) ;
#15615=CARTESIAN_POINT ( 'NONE',  ( -1.195183497228115035E-16, 3.346456692913386100, -0.6299212598425177889 ) ) ;
#15617=DIRECTION ( 'NONE',  ( -3.469446951953613696E-16, 0.000000000000000000, -1.000000000000000000 ) ) ;
#15618=DIRECTION ( 'NONE',  ( 1.734723475976806848E-16, -0.000000000000000000, 1.000000000000000000 ) ) ;
#15619=ADVANCED_FACE ( 'NONE', ( #6076 ), #33210, .F. ) ;
#15623=LINE ( 'NONE', #18742, #44643 ) ;
#15625=EDGE_LOOP ( 'NONE', ( #43506, #10109, #33643, #24566 ) ) ;
#15626=CARTESIAN_POINT ( 'NONE',  ( -1.363819533518803473, 0.000000000000000000, -0.1574803149606300023 ) ) ;
#15627=CARTESIAN_POINT ( 'NONE',  ( -0.2727639067037602727, 0.000000000000000000, 0.9055118110236167750 ) ) ;
#15628=VECTOR ( 'NONE', #24896, 39.37007874015748143 ) ;
#15631=CARTESIAN_POINT ( 'NONE',  ( 1.287906020515829919, 3.267716535433071279, -2.076684646723067296 ) ) ;
#15634=LINE ( 'NONE', #31385, #1873 ) ;
#15635=FACE_OUTER_BOUND ( 'NONE', #8386, .T. ) ;
#15636=ORIENTED_EDGE ( 'NONE', *, *, #22411, .F. ) ;
#15638=CARTESIAN_POINT ( 'NONE',  ( -0.07591351300297305427, 3.267716535433071279, 2.633779063002558971E-17 ) ) ;
#15639=EDGE_LOOP ( 'NONE', ( #49313, #50860, #5237, #41916 ) ) ;
#15640=ORIENTED_EDGE ( 'NONE', *, *, #38495, .F. ) ;
#15641=CARTESIAN_POINT ( 'NONE',  ( 1.015142113812069979, 0.000000000000000000, 1.732283464566921172 ) ) ;
#15644=ORIENTED_EDGE ( 'NONE', *, *, #32460, .F. ) ;
#15645=ORIENTED_EDGE ( 'NONE', *, *, #37118, .T. ) ;
#15646=CARTESIAN_POINT ( 'NONE',  ( -1.091055626815042201, 0.000000000000000000, 1.574803149606291974 ) ) ;
#15647=ORIENTED_EDGE ( 'NONE', *, *, #20496, .T. ) ;
#15648=DIRECTION ( 'NONE',  ( -0.000000000000000000, 1.000000000000000000, -0.000000000000000000 ) ) ;
#15649=LINE ( 'NONE', #26756, #17834 ) ;
#15651=EDGE_CURVE ( 'NONE', #26854, #31614, #2214, .T. ) ;
#15652=VECTOR ( 'NONE', #13125, 39.37007874015748143 ) ;
#15653=FACE_OUTER_BOUND ( 'NONE', #4825, .T. ) ;
#15655=EDGE_CURVE ( 'NONE', #48919, #44707, #49408, .T. ) ;
#15656=DIRECTION ( 'NONE',  ( 1.000000000000000000, 0.000000000000000000, 0.000000000000000000 ) ) ;
#15658=EDGE_LOOP ( 'NONE', ( #31121, #21864, #4202, #36364 ) ) ;
#15659=CARTESIAN_POINT ( 'NONE',  ( -1.166969139818015755, 0.000000000000000000, -0.03937007874015868020 ) ) ;
#15660=VECTOR ( 'NONE', #29467, 39.37007874015748143 ) ;
#15662=DIRECTION ( 'NONE',  ( -3.469446951953613696E-16, 0.000000000000000000, -1.000000000000000000 ) ) ;
#15664=DIRECTION ( 'NONE',  ( -3.469446951953613696E-16, 0.000000000000000000, -1.000000000000000000 ) ) ;
#15666=LINE ( 'NONE', #425, #21317 ) ;
#15673=CARTESIAN_POINT ( 'NONE',  ( -0.3486774197067334935, 3.267716535433071279, 1.692913385826762873 ) ) ;
#15674=ORIENTED_EDGE ( 'NONE', *, *, #50503, .T. ) ;
#15675=EDGE_CURVE ( 'NONE', #32615, #10700, #2972, .T. ) ;
#15676=ORIENTED_EDGE ( 'NONE', *, *, #14733, .F. ) ;
#15678=DIRECTION ( 'NONE',  ( 1.000000000000000000, 0.000000000000000000, 0.000000000000000000 ) ) ;
#15679=ORIENTED_EDGE ( 'NONE', *, *, #38686, .T. ) ;
#15681=FACE_OUTER_BOUND ( 'NONE', #47960, .T. ) ;
#15682=ORIENTED_EDGE ( 'NONE', *, *, #25840, .F. ) ;
#15683=EDGE_CURVE ( 'NONE', #19556, #35330, #42457, .T. ) ;
#15684=VECTOR ( 'NONE', #7904, 39.37007874015748143 ) ;
#15685=CARTESIAN_POINT ( 'NONE',  ( 0.4696143004045479352, 0.000000000000000000, -0.1574803149606298636 ) ) ;
#15688=VERTEX_POINT ( 'NONE', #35225 ) ;
#15689=CARTESIAN_POINT ( 'NONE',  ( 0.2727639067037604392, 3.267716535433071279, 0.5905511811023579360 ) ) ;
#15692=ORIENTED_EDGE ( 'NONE', *, *, #16544, .F. ) ;
#15693=ORIENTED_EDGE ( 'NONE', *, *, #35532, .T. ) ;
#15695=ORIENTED_EDGE ( 'NONE', *, *, #44122, .T. ) ;
#15696=VECTOR ( 'NONE', #6175, 39.37007874015748143 ) ;
#15697=PLANE ( 'NONE',  #5633 ) ;
#15699=ORIENTED_EDGE ( 'NONE', *, *, #22505, .T. ) ;
#15700=ADVANCED_FACE ( 'NONE', ( #30341 ), #26958, .F. ) ;
#15701=LINE ( 'NONE', #2824, #28241 ) ;
#15702=DIRECTION ( 'NONE',  ( 1.000000000000000000, 0.000000000000000000, -3.469446951953613696E-16 ) ) ;
#15703=ORIENTED_EDGE ( 'NONE', *, *, #47431, .T. ) ;
#15706=VERTEX_POINT ( 'NONE', #46556 ) ;
#15707=CARTESIAN_POINT ( 'NONE',  ( -0.2727639067037602727, 3.346456692913386100, 1.220472440944875281 ) ) ;
#15708=DIRECTION ( 'NONE',  ( 0.000000000000000000, -1.000000000000000000, 0.000000000000000000 ) ) ;
#15709=CARTESIAN_POINT ( 'NONE',  ( -0.8182917201112819283, 3.267716535433071279, -1.732283464566922726 ) ) ;
#15710=EDGE_CURVE ( 'NONE', #27748, #13176, #6844, .T. ) ;
#15711=EDGE_CURVE ( 'NONE', #13982, #36614, #9371, .T. ) ;
#15712=VERTEX_POINT ( 'NONE', #10967 ) ;
#15713=VERTEX_POINT ( 'NONE', #50905 ) ;
#15714=CARTESIAN_POINT ( 'NONE',  ( 0.8182917201112824834, 0.000000000000000000, 2.047244094488179567 ) ) ;
#15715=LINE ( 'NONE', #38715, #46729 ) ;
#15717=DIRECTION ( 'NONE',  ( 1.000000000000000000, -0.000000000000000000, 0.000000000000000000 ) ) ;
#15718=DIRECTION ( 'NONE',  ( -0.000000000000000000, 1.000000000000000000, -0.000000000000000000 ) ) ;
#15719=CARTESIAN_POINT ( 'NONE',  ( 1.091055626815043311, 3.346456692913386100, 1.574803149606291974 ) ) ;
#15721=VECTOR ( 'NONE', #27792, 39.37007874015748143 ) ;
#15723=ORIENTED_EDGE ( 'NONE', *, *, #22928, .F. ) ;
#15724=LINE ( 'NONE', #38966, #44065 ) ;
#15725=ORIENTED_EDGE ( 'NONE', *, *, #31699, .T. ) ;
#15726=DIRECTION ( 'NONE',  ( -1.000000000000000000, 0.000000000000000000, 1.734723475976806848E-16 ) ) ;
#15727=VERTEX_POINT ( 'NONE', #14594 ) ;
#15730=ORIENTED_EDGE ( 'NONE', *, *, #3396, .T. ) ;
#15732=VERTEX_POINT ( 'NONE', #46060 ) ;
#15733=LINE ( 'NONE', #27347, #5638 ) ;
#15734=ORIENTED_EDGE ( 'NONE', *, *, #10579, .F. ) ;
#15735=FACE_OUTER_BOUND ( 'NONE', #26421, .T. ) ;
#15737=EDGE_CURVE ( 'NONE', #3517, #11390, #18965, .T. ) ;
#15738=ORIENTED_EDGE ( 'NONE', *, *, #19461, .F. ) ;
#15739=EDGE_CURVE ( 'NONE', #33931, #18423, #15349, .T. ) ;
#15741=ORIENTED_EDGE ( 'NONE', *, *, #31782, .T. ) ;
#15742=ORIENTED_EDGE ( 'NONE', *, *, #11557, .F. ) ;
#15744=CARTESIAN_POINT ( 'NONE',  ( -1.363819533518803473, 0.000000000000000000, -0.9842519685039344823 ) ) ;
#15745=DIRECTION ( 'NONE',  ( -3.469446951953613696E-16, 0.000000000000000000, -1.000000000000000000 ) ) ;
#15747=VECTOR ( 'NONE', #24748, 39.37007874015748143 ) ;
#15751=DIRECTION ( 'NONE',  ( 0.000000000000000000, -1.000000000000000000, 0.000000000000000000 ) ) ;
#15752=EDGE_LOOP ( 'NONE', ( #13081, #39307, #50289, #10900 ) ) ;
#15753=CARTESIAN_POINT ( 'NONE',  ( 0.000000000000000000, 3.346456692913386100, 0.000000000000000000 ) ) ;
#15755=VERTEX_POINT ( 'NONE', #31351 ) ;
#15757=EDGE_CURVE ( 'NONE', #2547, #8994, #7101, .T. ) ;
#15759=ORIENTED_EDGE ( 'NONE', *, *, #7600, .T. ) ;
#15761=CARTESIAN_POINT ( 'NONE',  ( 1.818390528211208945, 3.267716535433071279, 1.062992125984245639 ) ) ;
#15762=EDGE_CURVE ( 'NONE', #27808, #12583, #47046, .T. ) ;
#15765=EDGE_CURVE ( 'NONE', #351, #35551, #14846, .T. ) ;
#15766=EDGE_LOOP ( 'NONE', ( #35418, #18180, #31543, #47560, #50732 ) ) ;
#15767=ORIENTED_EDGE ( 'NONE', *, *, #22505, .F. ) ;
#15768=CARTESIAN_POINT ( 'NONE',  ( 1.091055626815042645, 3.346456692913386100, 0.7480314960629872445 ) ) ;
#15770=DIRECTION ( 'NONE',  ( -1.000000000000000000, 0.000000000000000000, 0.000000000000000000 ) ) ;
#15771=ORIENTED_EDGE ( 'NONE', *, *, #7528, .T. ) ;
#15772=CARTESIAN_POINT ( 'NONE',  ( 0.1968503937007873017, 3.267716535433071279, -0.3149606299212591165 ) ) ;
#15775=LINE ( 'NONE', #31534, #16163 ) ;
#15777=ORIENTED_EDGE ( 'NONE', *, *, #14211, .T. ) ;
#15778=LINE ( 'NONE', #29710, #24257 ) ;
#15779=CARTESIAN_POINT ( 'NONE',  ( -1.985260859929297572, 3.346456692913386100, -0.3149606299212589500 ) ) ;
#15780=EDGE_LOOP ( 'NONE', ( #9800, #3908, #8516, #43812 ) ) ;
#15781=VECTOR ( 'NONE', #48642, 39.37007874015748143 ) ;
#15783=CARTESIAN_POINT ( 'NONE',  ( 2.106197740627112402, 0.000000000000000000, 1.102362204724403938 ) ) ;
#15784=VECTOR ( 'NONE', #28784, 39.37007874015748143 ) ;
#15786=DIRECTION ( 'NONE',  ( -0.000000000000000000, 1.000000000000000000, -0.000000000000000000 ) ) ;
#15787=ORIENTED_EDGE ( 'NONE', *, *, #17363, .T. ) ;
#15788=AXIS2_PLACEMENT_3D ( 'NONE', #17920, #40652, #21286 ) ;
#15789=VERTEX_POINT ( 'NONE', #8105 ) ;
#15790=DIRECTION ( 'NONE',  ( 0.000000000000000000, 0.000000000000000000, -1.000000000000000000 ) ) ;
#15791=VECTOR ( 'NONE', #30943, 39.37007874015748143 ) ;
#15792=VERTEX_POINT ( 'NONE', #4230 ) ;
#15794=EDGE_LOOP ( 'NONE', ( #40090, #39766, #14311, #49133 ) ) ;
#15796=CARTESIAN_POINT ( 'NONE',  ( 0.7423782071083087075, 3.346456692913386100, -1.259842519685035134 ) ) ;
#15797=DIRECTION ( 'NONE',  ( 0.000000000000000000, 0.000000000000000000, 1.000000000000000000 ) ) ;
#15798=ORIENTED_EDGE ( 'NONE', *, *, #22713, .F. ) ;
#15800=ORIENTED_EDGE ( 'NONE', *, *, #9243, .F. ) ;
#15801=ORIENTED_EDGE ( 'NONE', *, *, #43267, .T. ) ;
#15803=CARTESIAN_POINT ( 'NONE',  ( -1.166969139818016199, 0.000000000000000000, 1.535433070866133232 ) ) ;
#15805=ORIENTED_EDGE ( 'NONE', *, *, #39347, .T. ) ;
#15806=EDGE_LOOP ( 'NONE', ( #12950, #11329, #35898, #17308 ) ) ;
#15807=DIRECTION ( 'NONE',  ( -0.000000000000000000, 1.000000000000000000, -0.000000000000000000 ) ) ;
#15808=LINE ( 'NONE', #8325, #3718 ) ;
#15809=LINE ( 'NONE', #15568, #40964 ) ;
#15810=ADVANCED_FACE ( 'NONE', ( #20225 ), #36501, .F. ) ;
#15811=ORIENTED_EDGE ( 'NONE', *, *, #37187, .T. ) ;
#15812=ORIENTED_EDGE ( 'NONE', *, *, #27716, .F. ) ;
#15815=DIRECTION ( 'NONE',  ( -0.000000000000000000, 1.000000000000000000, -0.000000000000000000 ) ) ;
#15816=EDGE_CURVE ( 'NONE', #10053, #7713, #23361, .T. ) ;
#15817=VERTEX_POINT ( 'NONE', #39600 ) ;
#15818=LINE ( 'NONE', #7826, #45477 ) ;
#15819=FACE_OUTER_BOUND ( 'NONE', #1422, .T. ) ;
#15820=ORIENTED_EDGE ( 'NONE', *, *, #8440, .T. ) ;
#15821=DIRECTION ( 'NONE',  ( -0.000000000000000000, 1.000000000000000000, -0.000000000000000000 ) ) ;
#15822=ORIENTED_EDGE ( 'NONE', *, *, #11138, .F. ) ;
#15828=ADVANCED_FACE ( 'NONE', ( #24367 ), #40380, .F. ) ;
#15829=CARTESIAN_POINT ( 'NONE',  ( 0.8182917201112819283, 3.346456692913386100, 0.2755905511810994302 ) ) ;
#15833=VECTOR ( 'NONE', #2811, 39.37007874015748143 ) ;
#15835=AXIS2_PLACEMENT_3D ( 'NONE', #16152, #27499, #35770 ) ;
#15836=ORIENTED_EDGE ( 'NONE', *, *, #15114, .F. ) ;
#15837=LINE ( 'NONE', #11970, #42590 ) ;
#15839=DIRECTION ( 'NONE',  ( -3.469446951953613696E-16, 0.000000000000000000, -1.000000000000000000 ) ) ;
#15843=EDGE_CURVE ( 'NONE', #43721, #41731, #31866, .T. ) ;
#15844=DIRECTION ( 'NONE',  ( 0.000000000000000000, 0.000000000000000000, -1.000000000000000000 ) ) ;
#15846=CARTESIAN_POINT ( 'NONE',  ( 0.000000000000000000, 3.267716535433071279, 1.692913385826762873 ) ) ;
#15847=CARTESIAN_POINT ( 'NONE',  ( -1.091055626815042201, 3.267716535433071279, 1.377952755905504256 ) ) ;
#15849=EDGE_LOOP ( 'NONE', ( #31977, #9898, #43007, #42963 ) ) ;
#15850=CARTESIAN_POINT ( 'NONE',  ( 1.091055626815042423, 3.346456692913386100, -2.086614173228339641 ) ) ;
#15851=DIRECTION ( 'NONE',  ( -0.000000000000000000, 1.000000000000000000, -0.000000000000000000 ) ) ;
#15853=CARTESIAN_POINT ( 'NONE',  ( -1.536664496436148184E-16, 3.346456692913386100, -0.8267716535433052849 ) ) ;
#15854=VERTEX_POINT ( 'NONE', #12235 ) ;
#15855=CARTESIAN_POINT ( 'NONE',  ( -1.712496953225537188, 0.000000000000000000, -0.1574803149606297248 ) ) ;
#15856=ORIENTED_EDGE ( 'NONE', *, *, #40681, .T. ) ;
#15858=AXIS2_PLACEMENT_3D ( 'NONE', #13178, #24788, #32546 ) ;
#15859=DIRECTION ( 'NONE',  ( -3.469446951953613696E-16, 0.000000000000000000, -1.000000000000000000 ) ) ;
#15860=LINE ( 'NONE', #36011, #48572 ) ;
#15861=LINE ( 'NONE', #50421, #12806 ) ;
#15862=CIRCLE ( 'NONE', #50453, 2.165354330708661568 ) ;
#15863=ORIENTED_EDGE ( 'NONE', *, *, #32373, .F. ) ;
#15865=CARTESIAN_POINT ( 'NONE',  ( 1.560669927219590525, 3.346456692913386100, -0.03937007874015908959 ) ) ;
#15866=CARTESIAN_POINT ( 'NONE',  ( 0.8182917201112822614, 3.267716535433071279, -1.419509857074483785E-16 ) ) ;
#15868=ORIENTED_EDGE ( 'NONE', *, *, #13434, .F. ) ;
#15870=DIRECTION ( 'NONE',  ( -3.469446951953613696E-16, 0.000000000000000000, -1.000000000000000000 ) ) ;
#15872=DIRECTION ( 'NONE',  ( -3.469446951953613696E-16, 0.000000000000000000, -1.000000000000000000 ) ) ;
#15873=ADVANCED_FACE ( 'NONE', ( #23593 ), #8615, .F. ) ;
#15874=VECTOR ( 'NONE', #26880, 39.37007874015748143 ) ;
#15876=AXIS2_PLACEMENT_3D ( 'NONE', #25059, #28924, #44660 ) ;
#15878=ORIENTED_EDGE ( 'NONE', *, *, #11893, .T. ) ;
#15880=ORIENTED_EDGE ( 'NONE', *, *, #15184, .F. ) ;
#15882=FACE_OUTER_BOUND ( 'NONE', #4940, .T. ) ;
#15883=EDGE_CURVE ( 'NONE', #35559, #47517, #4747, .T. ) ;
#15884=DIRECTION ( 'NONE',  ( -0.000000000000000000, 0.000000000000000000, 1.000000000000000000 ) ) ;
#15887=ORIENTED_EDGE ( 'NONE', *, *, #44796, .T. ) ;
#15889=CARTESIAN_POINT ( 'NONE',  ( 0.000000000000000000, 3.267716535433071279, 0.3149606299212577287 ) ) ;
#15891=VERTEX_POINT ( 'NONE', #47302 ) ;
#15892=VERTEX_POINT ( 'NONE', #32124 ) ;
#15893=DIRECTION ( 'NONE',  ( -0.000000000000000000, 1.000000000000000000, -0.000000000000000000 ) ) ;
#15894=ORIENTED_EDGE ( 'NONE', *, *, #14784, .F. ) ;
#15896=EDGE_CURVE ( 'NONE', #19400, #15497, #43135, .T. ) ;
#15897=CARTESIAN_POINT ( 'NONE',  ( 1.833433833923350909, 3.346456692913386100, 1.152076279655074087 ) ) ;
#15902=VECTOR ( 'NONE', #42174, 39.37007874015748143 ) ;
#15903=CARTESIAN_POINT ( 'NONE',  ( -1.636583440222564301, 3.346456692913386100, -0.6299212598425177889 ) ) ;
#15904=DIRECTION ( 'NONE',  ( 1.000000000000000000, 0.000000000000000000, 0.000000000000000000 ) ) ;
#15907=DIRECTION ( 'NONE',  ( 1.000000000000000000, 0.000000000000000000, -3.469446951953613696E-16 ) ) ;
#15908=EDGE_CURVE ( 'NONE', #31838, #8862, #32640, .T. ) ;
#15909=FACE_OUTER_BOUND ( 'NONE', #39208, .T. ) ;
#15910=VECTOR ( 'NONE', #18324, 39.37007874015748143 ) ;
#15911=VECTOR ( 'NONE', #42077, 39.37007874015748143 ) ;
#15912=EDGE_LOOP ( 'NONE', ( #5691, #12947, #43049, #24065 ) ) ;
#15915=ORIENTED_EDGE ( 'NONE', *, *, #29590, .F. ) ;
#15916=DIRECTION ( 'NONE',  ( -3.469446951953613696E-16, 0.000000000000000000, -1.000000000000000000 ) ) ;
#15919=VECTOR ( 'NONE', #19521, 39.37007874015748143 ) ;
#15922=ORIENTED_EDGE ( 'NONE', *, *, #18628, .T. ) ;
#15923=LINE ( 'NONE', #47382, #32216 ) ;
#15924=EDGE_CURVE ( 'NONE', #36052, #32045, #17637, .T. ) ;
#15925=LINE ( 'NONE', #4066, #29181 ) ;
#15927=DIRECTION ( 'NONE',  ( 1.000000000000000000, 0.000000000000000000, -3.469446951953613696E-16 ) ) ;
#15928=ORIENTED_EDGE ( 'NONE', *, *, #6860, .T. ) ;
#15930=ORIENTED_EDGE ( 'NONE', *, *, #27422, .F. ) ;
#15934=DIRECTION ( 'NONE',  ( -0.000000000000000000, 0.000000000000000000, 1.000000000000000000 ) ) ;
#15937=LINE ( 'NONE', #31698, #18979 ) ;
#15939=CARTESIAN_POINT ( 'NONE',  ( 2.106197740627111514, 3.346456692913386100, -1.102362204724406602 ) ) ;
#15941=VECTOR ( 'NONE', #13680, 39.37007874015748143 ) ;
#15942=CARTESIAN_POINT ( 'NONE',  ( 1.520337605863835151, 3.240842057052200964, -1.929133858267710666 ) ) ;
#15943=EDGE_LOOP ( 'NONE', ( #14350, #22266, #5007, #18645 ) ) ;
#15944=ORIENTED_EDGE ( 'NONE', *, *, #8855, .F. ) ;
#15945=DIRECTION ( 'NONE',  ( -1.000000000000000000, 0.000000000000000000, -0.000000000000000000 ) ) ;
#15948=VECTOR ( 'NONE', #4011, 39.37007874015748143 ) ;
#15950=CARTESIAN_POINT ( 'NONE',  ( 1.560669927219590303, 3.267716535433071279, -1.880327210325009046 ) ) ;
#15953=ADVANCED_FACE ( 'NONE', ( #6276 ), #13768, .F. ) ;
#15957=ORIENTED_EDGE ( 'NONE', *, *, #14318, .F. ) ;
#15959=ORIENTED_EDGE ( 'NONE', *, *, #1372, .F. ) ;
#15960=PLANE ( 'NONE',  #45849 ) ;
#15961=CARTESIAN_POINT ( 'NONE',  ( -1.636583440222563635, 3.267716535433071279, 0.7480314960629874665 ) ) ;
#15962=EDGE_CURVE ( 'NONE', #46993, #33556, #29513, .T. ) ;
#15965=ORIENTED_EDGE ( 'NONE', *, *, #37937, .F. ) ;
#15966=LINE ( 'NONE', #43326, #8796 ) ;
#15968=FACE_OUTER_BOUND ( 'NONE', #29193, .T. ) ;
#15969=DIRECTION ( 'NONE',  ( 1.000000000000000000, -0.000000000000000000, 0.000000000000000000 ) ) ;
#15972=EDGE_CURVE ( 'NONE', #32098, #43573, #22027, .T. ) ;
#15974=ORIENTED_EDGE ( 'NONE', *, *, #16125, .F. ) ;
#15975=EDGE_CURVE ( 'NONE', #27834, #38248, #9895, .T. ) ;
#15978=AXIS2_PLACEMENT_3D ( 'NONE', #45036, #37829, #18193 ) ;
#15979=VERTEX_POINT ( 'NONE', #17894 ) ;
#15984=ORIENTED_EDGE ( 'NONE', *, *, #27488, .F. ) ;
#15987=AXIS2_PLACEMENT_3D ( 'NONE', #43132, #549, #43391 ) ;
#15988=DIRECTION ( 'NONE',  ( 1.000000000000000000, 0.000000000000000000, 0.000000000000000000 ) ) ;
#15990=ORIENTED_EDGE ( 'NONE', *, *, #48206, .F. ) ;
#15991=VECTOR ( 'NONE', #16300, 39.37007874015748143 ) ;
#15993=ORIENTED_EDGE ( 'NONE', *, *, #43708, .F. ) ;
#15994=DIRECTION ( 'NONE',  ( -0.000000000000000000, 1.000000000000000000, -0.000000000000000000 ) ) ;
#15997=LINE ( 'NONE', #4131, #40916 ) ;
#15999=EDGE_CURVE ( 'NONE', #6103, #36932, #21509, .T. ) ;
#16001=CARTESIAN_POINT ( 'NONE',  ( 2.182111253630085290, 3.346456692913386100, -0.3149606299212596716 ) ) ;
#16002=EDGE_CURVE ( 'NONE', #5956, #14009, #37524, .T. ) ;
#16004=VERTEX_POINT ( 'NONE', #49344 ) ;
#16005=DIRECTION ( 'NONE',  ( -0.000000000000000000, 1.000000000000000000, -0.000000000000000000 ) ) ;
#16006=LINE ( 'NONE', #31764, #10029 ) ;
#16007=CARTESIAN_POINT ( 'NONE',  ( 0.5455278134075217666, 3.267716535433071279, 2.204724409448808764 ) ) ;
#16008=ORIENTED_EDGE ( 'NONE', *, *, #30209, .T. ) ;
#16009=CARTESIAN_POINT ( 'NONE',  ( -0.8182917201112819283, 0.000000000000000000, -1.299212598425193210 ) ) ;
#16011=ORIENTED_EDGE ( 'NONE', *, *, #29953, .F. ) ;
#16012=CARTESIAN_POINT ( 'NONE',  ( 0.4696143004045479352, 3.267716535433071279, 0.4724409448818868706 ) ) ;
#16014=VECTOR ( 'NONE', #22019, 39.37007874015748143 ) ;
#16017=ORIENTED_EDGE ( 'NONE', *, *, #42499, .T. ) ;
#16019=AXIS2_PLACEMENT_3D ( 'NONE', #21147, #48215, #20883 ) ;
#16020=ORIENTED_EDGE ( 'NONE', *, *, #43768, .T. ) ;
#16023=PLANE ( 'NONE',  #6859 ) ;
#16025=CARTESIAN_POINT ( 'NONE',  ( 0.4696143004045478797, 3.346456692913386100, -0.03937007874015908959 ) ) ;
#16026=ORIENTED_EDGE ( 'NONE', *, *, #39666, .T. ) ;
#16027=ORIENTED_EDGE ( 'NONE', *, *, #41186, .F. ) ;
#16028=AXIS2_PLACEMENT_3D ( 'NONE', #11232, #29650, #30602 ) ;
#16034=DIRECTION ( 'NONE',  ( -3.469446951953613696E-16, 0.000000000000000000, -1.000000000000000000 ) ) ;
#16035=EDGE_CURVE ( 'NONE', #27306, #38137, #29250, .T. ) ;
#16037=CARTESIAN_POINT ( 'NONE',  ( -0.3486774197067338266, 3.267716535433071279, 1.209717811016578585E-16 ) ) ;
#16038=EDGE_CURVE ( 'NONE', #45493, #13751, #13007, .T. ) ;
#16039=LINE ( 'NONE', #19386, #33547 ) ;
#16041=CARTESIAN_POINT ( 'NONE',  ( -0.8182917201112819283, 0.000000000000000000, 0.1574803149606285035 ) ) ;
#16042=LINE ( 'NONE', #16817, #16992 ) ;
#16043=ORIENTED_EDGE ( 'NONE', *, *, #32959, .T. ) ;
#16044=ORIENTED_EDGE ( 'NONE', *, *, #46632, .T. ) ;
#16045=LINE ( 'NONE', #20160, #47943 ) ;
#16046=CARTESIAN_POINT ( 'NONE',  ( -1.909347346926324906, 3.267716535433071279, -0.4724409448818884805 ) ) ;
#16047=DIRECTION ( 'NONE',  ( -3.469446951953613696E-16, 0.000000000000000000, -1.000000000000000000 ) ) ;
#16050=VERTEX_POINT ( 'NONE', #9124 ) ;
#16052=FACE_OUTER_BOUND ( 'NONE', #47264, .T. ) ;
#16053=EDGE_CURVE ( 'NONE', #42475, #40629, #24878, .T. ) ;
#16054=VERTEX_POINT ( 'NONE', #36757 ) ;
#16055=DIRECTION ( 'NONE',  ( -1.000000000000000000, -0.000000000000000000, -0.000000000000000000 ) ) ;
#16056=VECTOR ( 'NONE', #47833, 39.37007874015748143 ) ;
#16058=CARTESIAN_POINT ( 'NONE',  ( -0.2727639067037607723, 0.000000000000000000, -0.1574803149606301411 ) ) ;
#16059=EDGE_CURVE ( 'NONE', #28931, #3036, #32900, .T. ) ;
#16060=LINE ( 'NONE', #27161, #36277 ) ;
#16061=CARTESIAN_POINT ( 'NONE',  ( 0.1968503937007878568, 3.346456692913386100, 1.889763779527550369 ) ) ;
#16062=EDGE_CURVE ( 'NONE', #2854, #10877, #25129, .T. ) ;
#16063=ORIENTED_EDGE ( 'NONE', *, *, #39951, .T. ) ;
#16064=ORIENTED_EDGE ( 'NONE', *, *, #31922, .T. ) ;
#16065=ORIENTED_EDGE ( 'NONE', *, *, #22656, .T. ) ;
#16066=DIRECTION ( 'NONE',  ( -0.000000000000000000, 1.000000000000000000, -0.000000000000000000 ) ) ;
#16067=AXIS2_PLACEMENT_3D ( 'NONE', #15263, #34885, #50568 ) ;
#16069=ADVANCED_FACE ( 'NONE', ( #45736 ), #22783, .F. ) ;
#16070=ORIENTED_EDGE ( 'NONE', *, *, #691, .F. ) ;
#16071=ORIENTED_EDGE ( 'NONE', *, *, #2845, .F. ) ;
#16073=DIRECTION ( 'NONE',  ( 1.000000000000000000, -0.000000000000000000, 0.000000000000000000 ) ) ;
#16077=PLANE ( 'NONE',  #43576 ) ;
#16079=CARTESIAN_POINT ( 'NONE',  ( 1.636583440222563635, 3.346456692913386100, -1.259842519685035800 ) ) ;
#16080=ORIENTED_EDGE ( 'NONE', *, *, #16782, .T. ) ;
#16083=CARTESIAN_POINT ( 'NONE',  ( -0.5455278134075214336, 0.000000000000000000, -1.456692913385822630 ) ) ;
#16084=VERTEX_POINT ( 'NONE', #11155 ) ;
#16085=CARTESIAN_POINT ( 'NONE',  ( 0.7423782071083085965, 3.346456692913386100, -0.8267716535433055070 ) ) ;
#16086=ORIENTED_EDGE ( 'NONE', *, *, #16320, .T. ) ;
#16088=CARTESIAN_POINT ( 'NONE',  ( 1.139183960333101098, 3.267716535433071279, -1.771653543307081691 ) ) ;
#16089=SHAPE_REPRESENTATION_RELATIONSHIP ( 'NONE' , 'NONE' ,  #15265, #18129 ) ;
#16090=CARTESIAN_POINT ( 'NONE',  ( 0.1968503937007878568, 0.000000000000000000, 1.259842519685033357 ) ) ;
#16092=CARTESIAN_POINT ( 'NONE',  ( 1.636583440222563857, 3.267716535433071279, -2.839019714148966584E-16 ) ) ;
#16093=EDGE_LOOP ( 'NONE', ( #8073, #35046, #44492, #23777 ) ) ;
#16094=ORIENTED_EDGE ( 'NONE', *, *, #27462, .F. ) ;
#16095=AXIS2_PLACEMENT_3D ( 'NONE', #18017, #45605, #22648 ) ;
#16098=EDGE_LOOP ( 'NONE', ( #5861, #28246, #12985, #19751 ) ) ;
#16100=CARTESIAN_POINT ( 'NONE',  ( -1.091055626815042645, 3.346456692913386100, -0.1968503937007881899 ) ) ;
#16102=EDGE_CURVE ( 'NONE', #3556, #49445, #50098, .T. ) ;
#16105=AXIS2_PLACEMENT_3D ( 'NONE', #11496, #31119, #7618 ) ;
#16106=ORIENTED_EDGE ( 'NONE', *, *, #44701, .F. ) ;
#16107=EDGE_CURVE ( 'NONE', #2753, #25164, #39030, .T. ) ;
#16110=EDGE_CURVE ( 'NONE', #10637, #48582, #38533, .T. ) ;
#16111=ORIENTED_EDGE ( 'NONE', *, *, #41006, .F. ) ;
#16112=PLANE ( 'NONE',  #12490 ) ;
#16113=FACE_OUTER_BOUND ( 'NONE', #4210, .T. ) ;
#16116=CARTESIAN_POINT ( 'NONE',  ( 0.8182917201112824834, 0.000000000000000000, 2.047244094488179567 ) ) ;
#16117=DIRECTION ( 'NONE',  ( 1.000000000000000000, 0.000000000000000000, 0.000000000000000000 ) ) ;
#16119=ORIENTED_EDGE ( 'NONE', *, *, #50720, .T. ) ;
#16120=CARTESIAN_POINT ( 'NONE',  ( 1.091055626815042423, 3.346456692913386100, -1.889763779527552368 ) ) ;
#16121=CARTESIAN_POINT ( 'NONE',  ( -0.5455278134075214336, 0.000000000000000000, -1.259842519685035134 ) ) ;
#16122=EDGE_LOOP ( 'NONE', ( #2291, #9685, #42177, #35618 ) ) ;
#16124=CARTESIAN_POINT ( 'NONE',  ( 0.1968503937007878568, 0.000000000000000000, 0.9448818897637749625 ) ) ;
#16125=EDGE_CURVE ( 'NONE', #18551, #47200, #27146, .T. ) ;
#16126=CARTESIAN_POINT ( 'NONE',  ( 1.636583440222563857, 3.267716535433071279, -2.839019714148966584E-16 ) ) ;
#16127=LINE ( 'NONE', #21025, #7046 ) ;
#16128=ORIENTED_EDGE ( 'NONE', *, *, #11323, .T. ) ;
#16129=ORIENTED_EDGE ( 'NONE', *, *, #35985, .F. ) ;
#16130=PLANE ( 'NONE',  #3420 ) ;
#16133=VECTOR ( 'NONE', #46318, 39.37007874015748143 ) ;
#16134=ADVANCED_FACE ( 'NONE', ( #15282 ), #42886, .F. ) ;
#16137=DIRECTION ( 'NONE',  ( -3.469446951953613696E-16, 0.000000000000000000, -1.000000000000000000 ) ) ;
#16138=DIRECTION ( 'NONE',  ( 1.734723475976806848E-16, -0.000000000000000000, 1.000000000000000000 ) ) ;
#16142=VERTEX_POINT ( 'NONE', #10659 ) ;
#16143=VERTEX_POINT ( 'NONE', #14530 ) ;
#16144=VERTEX_POINT ( 'NONE', #6778 ) ;
#16146=VECTOR ( 'NONE', #6055, 39.37007874015748143 ) ;
#16148=LINE ( 'NONE', #31908, #47079 ) ;
#16149=FACE_BOUND ( 'NONE', #41005, .T. ) ;
#16150=AXIS2_PLACEMENT_3D ( 'NONE', #34805, #34311, #46391 ) ;
#16151=ORIENTED_EDGE ( 'NONE', *, *, #50160, .F. ) ;
#16152=CARTESIAN_POINT ( 'NONE',  ( -2.182111253630085290, 0.000000000000000000, 0.1181102362204704270 ) ) ;
#16154=ORIENTED_EDGE ( 'NONE', *, *, #36448, .F. ) ;
#16156=VERTEX_POINT ( 'NONE', #7534 ) ;
#16157=EDGE_LOOP ( 'NONE', ( #16734, #7165, #35816, #1470 ) ) ;
#16160=FACE_OUTER_BOUND ( 'NONE', #6013, .T. ) ;
#16162=LINE ( 'NONE', #32435, #39091 ) ;
#16163=VECTOR ( 'NONE', #32056, 39.37007874015748143 ) ;
#16164=DIRECTION ( 'NONE',  ( -3.469446951953613696E-16, 0.000000000000000000, -1.000000000000000000 ) ) ;
#16166=CARTESIAN_POINT ( 'NONE',  ( -0.8942052331142552601, 0.000000000000000000, -7.512581982576723358E-16 ) ) ;
#16167=DIRECTION ( 'NONE',  ( 1.000000000000000000, -0.000000000000000000, 0.000000000000000000 ) ) ;
#16168=VECTOR ( 'NONE', #9641, 39.37007874015748143 ) ;
#16170=ADVANCED_FACE ( 'NONE', ( #23274 ), #3661, .F. ) ;
#16171=PLANE ( 'NONE',  #16748 ) ;
#16172=VECTOR ( 'NONE', #48690, 39.37007874015748143 ) ;
#16173=DIRECTION ( 'NONE',  ( -3.469446951953613696E-16, 0.000000000000000000, -1.000000000000000000 ) ) ;
#16176=EDGE_CURVE ( 'NONE', #41557, #37198, #18402, .T. ) ;
#16178=CARTESIAN_POINT ( 'NONE',  ( 1.363819533518803251, 0.000000000000000000, 0.1574803149606283648 ) ) ;
#16179=EDGE_CURVE ( 'NONE', #3361, #44517, #26395, .T. ) ;
#16181=ORIENTED_EDGE ( 'NONE', *, *, #10579, .T. ) ;
#16182=FACE_OUTER_BOUND ( 'NONE', #12366, .T. ) ;
#16183=VECTOR ( 'NONE', #29995, 39.37007874015748143 ) ;
#16184=EDGE_CURVE ( 'NONE', #30042, #49974, #18660, .T. ) ;
#16185=LINE ( 'NONE', #17455, #17615 ) ;
#16189=ORIENTED_EDGE ( 'NONE', *, *, #28916, .T. ) ;
#16191=LINE ( 'NONE', #38673, #1992 ) ;
#16192=CARTESIAN_POINT ( 'NONE',  ( 0.5455278134075216556, 0.000000000000000000, 2.007874015748021268 ) ) ;
#16193=EDGE_CURVE ( 'NONE', #17447, #48287, #22278, .T. ) ;
#16194=PLANE ( 'NONE',  #30928 ) ;
#16196=ORIENTED_EDGE ( 'NONE', *, *, #12340, .T. ) ;
#16197=CARTESIAN_POINT ( 'NONE',  ( 0.000000000000000000, 3.267716535433071279, 1.535433070866133232 ) ) ;
#16200=DIRECTION ( 'NONE',  ( -1.000000000000000000, 0.000000000000000000, 1.734723475976806848E-16 ) ) ;
#16205=CARTESIAN_POINT ( 'NONE',  ( 0.000000000000000000, 3.346456692913386100, 0.000000000000000000 ) ) ;
#16206=VECTOR ( 'NONE', #26275, 39.37007874015748143 ) ;
#16207=FACE_OUTER_BOUND ( 'NONE', #44739, .T. ) ;
#16208=VECTOR ( 'NONE', #38228, 39.37007874015748143 ) ;
#16209=EDGE_LOOP ( 'NONE', ( #45195, #19747, #11897, #32402 ) ) ;
#16210=VECTOR ( 'NONE', #28472, 39.37007874015748143 ) ;
#16214=EDGE_CURVE ( 'NONE', #18782, #49800, #3407, .T. ) ;
#16219=CARTESIAN_POINT ( 'NONE',  ( 1.287906020515829919, 3.267716535433071279, -1.259842519685035134 ) ) ;
#16222=ORIENTED_EDGE ( 'NONE', *, *, #40079, .F. ) ;
#16225=CARTESIAN_POINT ( 'NONE',  ( 2.106197740627111958, 3.346456692913386100, 0.5905511811023582691 ) ) ;
#16228=ORIENTED_EDGE ( 'NONE', *, *, #1438, .T. ) ;
#16229=EDGE_LOOP ( 'NONE', ( #28738, #5462, #25113, #31691 ) ) ;
#16230=DIRECTION ( 'NONE',  ( 1.734723475976806848E-16, -0.000000000000000000, 1.000000000000000000 ) ) ;
#16233=LINE ( 'NONE', #16751, #35076 ) ;
#16237=ORIENTED_EDGE ( 'NONE', *, *, #14365, .F. ) ;
#16240=DIRECTION ( 'NONE',  ( -3.469446951953613696E-16, 0.000000000000000000, -1.000000000000000000 ) ) ;
#16243=VECTOR ( 'NONE', #12355, 39.37007874015748143 ) ;
#16244=PLANE ( 'NONE',  #2039 ) ;
#16246=CARTESIAN_POINT ( 'NONE',  ( -1.091055626815042645, 0.000000000000000000, -1.456692913385822186 ) ) ;
#16247=DIRECTION ( 'NONE',  ( -0.000000000000000000, 0.000000000000000000, 1.000000000000000000 ) ) ;
#16248=LINE ( 'NONE', #8502, #39137 ) ;
#16251=CARTESIAN_POINT ( 'NONE',  ( 1.287906020515830141, 3.346456692913386100, -0.6299212598425181220 ) ) ;
#16252=ORIENTED_EDGE ( 'NONE', *, *, #28848, .F. ) ;
#16253=CARTESIAN_POINT ( 'NONE',  ( 0.5455278134075208785, 3.346456692913386100, -1.574803149606293529 ) ) ;
#16255=DIRECTION ( 'NONE',  ( 1.734723475976806848E-16, -0.000000000000000000, 1.000000000000000000 ) ) ;
#16256=DIRECTION ( 'NONE',  ( 0.000000000000000000, 0.000000000000000000, -1.000000000000000000 ) ) ;
#16257=EDGE_CURVE ( 'NONE', #24019, #8765, #43649, .T. ) ;
#16259=ORIENTED_EDGE ( 'NONE', *, *, #47366, .F. ) ;
#16262=DIRECTION ( 'NONE',  ( 1.000000000000000000, -0.000000000000000000, 0.000000000000000000 ) ) ;
#16263=FACE_BOUND ( 'NONE', #37251, .T. ) ;
#16264=EDGE_CURVE ( 'NONE', #34259, #35717, #287, .T. ) ;
#16265=DIRECTION ( 'NONE',  ( -1.000000000000000000, 0.000000000000000000, -0.000000000000000000 ) ) ;
#16267=VECTOR ( 'NONE', #10182, 39.37007874015748143 ) ;
#16268=EDGE_CURVE ( 'NONE', #1395, #20168, #7787, .T. ) ;
#16269=AXIS2_PLACEMENT_3D ( 'NONE', #4370, #16247, #28367 ) ;
#16270=VERTEX_POINT ( 'NONE', #32312 ) ;
#16273=ADVANCED_FACE ( 'NONE', ( #8293 ), #39789, .F. ) ;
#16277=ORIENTED_EDGE ( 'NONE', *, *, #10668, .T. ) ;
#16279=CARTESIAN_POINT ( 'NONE',  ( -1.166969139818016199, 3.267716535433071279, -1.614173228346451605 ) ) ;
#16281=DIRECTION ( 'NONE',  ( 1.734723475976806848E-16, 0.000000000000000000, 1.000000000000000000 ) ) ;
#16282=LINE ( 'NONE', #23772, #14814 ) ;
#16283=VERTEX_POINT ( 'NONE', #27906 ) ;
#16284=EDGE_LOOP ( 'NONE', ( #2067, #32269, #47045, #38098, #48559 ) ) ;
#16287=CARTESIAN_POINT ( 'NONE',  ( 1.091055626815042423, 3.346456692913386100, -1.771653543307081691 ) ) ;
#16288=VECTOR ( 'NONE', #5314, 39.37007874015748143 ) ;
#16289=ORIENTED_EDGE ( 'NONE', *, *, #26443, .F. ) ;
#16290=DIRECTION ( 'NONE',  ( 1.000000000000000000, -0.000000000000000000, 0.000000000000000000 ) ) ;
#16291=DIRECTION ( 'NONE',  ( -0.000000000000000000, 1.000000000000000000, -0.000000000000000000 ) ) ;
#16292=ADVANCED_FACE ( 'NONE', ( #12166 ), #20157, .F. ) ;
#16294=EDGE_CURVE ( 'NONE', #45764, #39732, #43903, .T. ) ;
#16296=DIRECTION ( 'NONE',  ( -3.469446951953613696E-16, 0.000000000000000000, -1.000000000000000000 ) ) ;
#16300=DIRECTION ( 'NONE',  ( 1.000000000000000000, 0.000000000000000000, 0.000000000000000000 ) ) ;
#16301=CARTESIAN_POINT ( 'NONE',  ( 0.4696143004045478797, 3.346456692913386100, -1.614173228346451605 ) ) ;
#16302=ORIENTED_EDGE ( 'NONE', *, *, #12858, .T. ) ;
#16303=EDGE_LOOP ( 'NONE', ( #16761, #13876, #19762, #44928 ) ) ;
#16304=CARTESIAN_POINT ( 'NONE',  ( -0.5455278134075214336, 3.346456692913386100, -1.574803149606293529 ) ) ;
#16306=DIRECTION ( 'NONE',  ( 1.000000000000000000, 0.000000000000000000, 0.000000000000000000 ) ) ;
#16307=VECTOR ( 'NONE', #26971, 39.37007874015748143 ) ;
#16310=EDGE_CURVE ( 'NONE', #41937, #11420, #4684, .T. ) ;
#16312=LINE ( 'NONE', #27661, #26240 ) ;
#16319=DIRECTION ( 'NONE',  ( 1.000000000000000000, 0.000000000000000000, -3.469446951953613696E-16 ) ) ;
#16320=EDGE_CURVE ( 'NONE', #25880, #49218, #31797, .T. ) ;
#16321=VECTOR ( 'NONE', #39196, 39.37007874015748143 ) ;
#16323=VERTEX_POINT ( 'NONE', #35162 ) ;
#16325=DIRECTION ( 'NONE',  ( 1.000000000000000000, 0.000000000000000000, -3.469446951953613696E-16 ) ) ;
#16327=ORIENTED_EDGE ( 'NONE', *, *, #35937, .F. ) ;
#16328=DIRECTION ( 'NONE',  ( -3.469446951953613696E-16, 0.000000000000000000, -1.000000000000000000 ) ) ;
#16331=VECTOR ( 'NONE', #999, 39.37007874015748143 ) ;
#16333=EDGE_LOOP ( 'NONE', ( #3188, #36838 ) ) ;
#16337=FACE_OUTER_BOUND ( 'NONE', #29547, .T. ) ;
#16338=EDGE_CURVE ( 'NONE', #33355, #3033, #15778, .T. ) ;
#16339=EDGE_LOOP ( 'NONE', ( #46037, #14868, #31450, #15127 ) ) ;
#16340=DIRECTION ( 'NONE',  ( 1.734723475976806848E-16, -0.000000000000000000, 1.000000000000000000 ) ) ;
#16342=CARTESIAN_POINT ( 'NONE',  ( 1.015142113812069313, 3.346456692913386100, -1.299212598425193210 ) ) ;
#16343=ORIENTED_EDGE ( 'NONE', *, *, #13961, .F. ) ;
#16344=CARTESIAN_POINT ( 'NONE',  ( 0.000000000000000000, 3.346456692913386100, -2.874015748031496731 ) ) ;
#16345=VERTEX_POINT ( 'NONE', #13454 ) ;
#16348=CARTESIAN_POINT ( 'NONE',  ( -0.07591351300297277671, 3.346456692913386100, 0.7874015748031456541 ) ) ;
#16350=VECTOR ( 'NONE', #24458, 39.37007874015748143 ) ;
#16352=EDGE_CURVE ( 'NONE', #18551, #42223, #16816, .T. ) ;
#16353=CARTESIAN_POINT ( 'NONE',  ( -2.182111253630085734, 3.267716535433071279, 3.785359618865289765E-16 ) ) ;
#16355=ORIENTED_EDGE ( 'NONE', *, *, #23742, .T. ) ;
#16356=VECTOR ( 'NONE', #6325, 39.37007874015748143 ) ;
#16358=EDGE_LOOP ( 'NONE', ( #44657, #6266, #37960, #30732 ) ) ;
#16359=PLANE ( 'NONE',  #14556 ) ;
#16360=CARTESIAN_POINT ( 'NONE',  ( 1.015142113812069313, 3.267716535433071279, -0.7874015748031473194 ) ) ;
#16361=AXIS2_PLACEMENT_3D ( 'NONE', #40329, #32588, #4947 ) ;
#16362=EDGE_CURVE ( 'NONE', #11338, #4264, #9065, .T. ) ;
#16364=AXIS2_PLACEMENT_3D ( 'NONE', #14129, #1741, #26004 ) ;
#16365=CARTESIAN_POINT ( 'NONE',  ( 0.2727639067037604947, 0.000000000000000000, -0.4724409448818886470 ) ) ;
#16366=CARTESIAN_POINT ( 'NONE',  ( 1.287906020515829475, 3.267716535433071279, -4.468321617281353104E-16 ) ) ;
#16367=CARTESIAN_POINT ( 'NONE',  ( -0.6214413264104939882, 0.000000000000000000, 1.102362204724404160 ) ) ;
#16368=VERTEX_POINT ( 'NONE', #17329 ) ;
#16370=DIRECTION ( 'NONE',  ( -1.000000000000000000, 0.000000000000000000, 1.734723475976806848E-16 ) ) ;
#16371=ADVANCED_FACE ( 'NONE', ( #36693 ), #49285, .F. ) ;
#16373=CARTESIAN_POINT ( 'NONE',  ( -1.636583440222564301, 3.346456692913386100, -1.417869535855831975 ) ) ;
#16375=LINE ( 'NONE', #4751, #21608 ) ;
#16376=DIRECTION ( 'NONE',  ( -1.000000000000000000, 0.000000000000000000, -0.000000000000000000 ) ) ;
#16377=CARTESIAN_POINT ( 'NONE',  ( -1.636583440222563635, 3.346456692913386100, 0.3149606299212578953 ) ) ;
#16378=VERTEX_POINT ( 'NONE', #40820 ) ;
#16379=CARTESIAN_POINT ( 'NONE',  ( 0.000000000000000000, 3.267716535433071279, -0.5118110236220471121 ) ) ;
#16382=ORIENTED_EDGE ( 'NONE', *, *, #37460, .T. ) ;
#16383=CARTESIAN_POINT ( 'NONE',  ( 0.000000000000000000, 3.267716535433071279, -0.8267716535433052849 ) ) ;
#16384=CARTESIAN_POINT ( 'NONE',  ( -1.909347346926324906, 3.346456692913386100, -0.4724409448818884805 ) ) ;
#16386=CARTESIAN_POINT ( 'NONE',  ( -1.716666360678977155, 3.267716535433071279, 1.220472440944875059 ) ) ;
#16387=CARTESIAN_POINT ( 'NONE',  ( 0.2727639067037609943, 0.000000000000000000, 0.9055118110236167750 ) ) ;
#16390=AXIS2_PLACEMENT_3D ( 'NONE', #24651, #40408, #5025 ) ;
#16391=VERTEX_POINT ( 'NONE', #24816 ) ;
#16392=EDGE_LOOP ( 'NONE', ( #14682, #41420, #47982, #11803 ) ) ;
#16393=DIRECTION ( 'NONE',  ( -0.000000000000000000, 1.000000000000000000, -0.000000000000000000 ) ) ;
#16396=CARTESIAN_POINT ( 'NONE',  ( -1.363819533518803473, 3.267716535433071279, -1.605145679676863057 ) ) ;
#16400=VECTOR ( 'NONE', #34691, 39.37007874015748143 ) ;
#16401=VECTOR ( 'NONE', #42042, 39.37007874015748143 ) ;
#16402=EDGE_LOOP ( 'NONE', ( #17167, #15375, #35247, #11964, #6934, #315, #46269, #9492, #12453, #40912, #31142, #5707, #39452, #45201, #46520, #50799, #28617, #12072, #29309, #49661, #33003, #21847, #25346, #44842, #37880, #17581, #26833, #43698, #41104, #9854, #1876, #26768, #46205, #9908, #29092, #37258, #15811, #2239, #11685, #4845, #30724, #19092, #16475, #49666, #37664, #8726, #32647, #24278, #27200, #3858, #5869, #12045, #39295, #21809, #34397, #12063, #43042, #27572, #22569, #36803, #15801, #16026, #47801, #17901, #8561, #9847, #29476, #31420, #41530, #6633, #34757, #28810, #37625, #25019, #2744, #17238, #17960, #10078, #3107, #13934, #35284, #38043, #36552, #38270 ) ) ;
#16403=ORIENTED_EDGE ( 'NONE', *, *, #28410, .F. ) ;
#16405=CARTESIAN_POINT ( 'NONE',  ( -2.182111253630085290, 0.000000000000000000, 0.3149606299212578953 ) ) ;
#16407=CARTESIAN_POINT ( 'NONE',  ( -0.2727639067037607723, 3.346456692913386100, 2.362204724409437961 ) ) ;
#16408=VECTOR ( 'NONE', #32048, 39.37007874015748143 ) ;
#16410=EDGE_CURVE ( 'NONE', #18300, #19616, #13204, .T. ) ;
#16411=FACE_BOUND ( 'NONE', #2692, .T. ) ;
#16412=ORIENTED_EDGE ( 'NONE', *, *, #8488, .T. ) ;
#16414=CARTESIAN_POINT ( 'NONE',  ( 0.1968503937007874127, 3.267716535433071279, -6.829619984160656814E-17 ) ) ;
#16417=VECTOR ( 'NONE', #32646, 39.37007874015748143 ) ;
#16419=ORIENTED_EDGE ( 'NONE', *, *, #15739, .T. ) ;
#16422=ORIENTED_EDGE ( 'NONE', *, *, #47662, .F. ) ;
#16425=CARTESIAN_POINT ( 'NONE',  ( -0.6214413264104945434, 0.000000000000000000, -0.03937007874015895081 ) ) ;
#16426=CARTESIAN_POINT ( 'NONE',  ( -1.439733046521776139, 0.000000000000000000, -4.780733988912460139E-16 ) ) ;
#16427=EDGE_CURVE ( 'NONE', #8967, #17096, #40562, .T. ) ;
#16429=CARTESIAN_POINT ( 'NONE',  ( 0.000000000000000000, 3.267716535433071279, -0.5118110236220467790 ) ) ;
#16430=DIRECTION ( 'NONE',  ( 1.000000000000000000, 0.000000000000000000, 0.000000000000000000 ) ) ;
#16431=LINE ( 'NONE', #16947, #17150 ) ;
#16432=ORIENTED_EDGE ( 'NONE', *, *, #26136, .T. ) ;
#16434=ADVANCED_FACE ( 'NONE', ( #21201 ), #33599, .F. ) ;
#16435=PLANE ( 'NONE',  #14476 ) ;
#16436=CARTESIAN_POINT ( 'NONE',  ( 1.091055626815042645, 0.000000000000000000, 0.3149606299212578953 ) ) ;
#16437=AXIS2_PLACEMENT_3D ( 'NONE', #11465, #35464, #38586 ) ;
#16441=ORIENTED_EDGE ( 'NONE', *, *, #7195, .T. ) ;
#16442=DIRECTION ( 'NONE',  ( -3.469446951953613696E-16, 0.000000000000000000, -1.000000000000000000 ) ) ;
#16443=PLANE ( 'NONE',  #39868 ) ;
#16447=LINE ( 'NONE', #32199, #175 ) ;
#16448=VECTOR ( 'NONE', #16901, 39.37007874015748143 ) ;
#16449=EDGE_LOOP ( 'NONE', ( #50615, #17356, #6350, #17578 ) ) ;
#16452=DIRECTION ( 'NONE',  ( -3.469446951953613696E-16, 0.000000000000000000, -1.000000000000000000 ) ) ;
#16453=CARTESIAN_POINT ( 'NONE',  ( -0.6214413264104940993, 3.267716535433071279, 2.156057715732899547E-16 ) ) ;
#16454=ORIENTED_EDGE ( 'NONE', *, *, #42419, .T. ) ;
#16455=VERTEX_POINT ( 'NONE', #48771 ) ;
#16456=CARTESIAN_POINT ( 'NONE',  ( -0.5455278134075214336, 3.346456692913386100, -8.878505979408855953E-16 ) ) ;
#16457=VERTEX_POINT ( 'NONE', #44924 ) ;
#16458=FACE_OUTER_BOUND ( 'NONE', #3041, .T. ) ;
#16459=ORIENTED_EDGE ( 'NONE', *, *, #23041, .F. ) ;
#16460=CARTESIAN_POINT ( 'NONE',  ( -0.6214413264104939882, 3.346456692913386100, 0.2755905511810998187 ) ) ;
#16461=VECTOR ( 'NONE', #7251, 39.37007874015748143 ) ;
#16462=VERTEX_POINT ( 'NONE', #1828 ) ;
#16465=EDGE_CURVE ( 'NONE', #30930, #24374, #13711, .T. ) ;
#16466=VERTEX_POINT ( 'NONE', #34845 ) ;
#16467=EDGE_CURVE ( 'NONE', #13984, #1578, #10599, .T. ) ;
#16469=ORIENTED_EDGE ( 'NONE', *, *, #36220, .F. ) ;
#16470=EDGE_CURVE ( 'NONE', #34365, #46240, #26340, .T. ) ;
#16472=AXIS2_PLACEMENT_3D ( 'NONE', #11896, #30516, #30763 ) ;
#16474=EDGE_CURVE ( 'NONE', #20192, #1675, #6976, .T. ) ;
#16475=ORIENTED_EDGE ( 'NONE', *, *, #44784, .F. ) ;
#16476=VERTEX_POINT ( 'NONE', #42087 ) ;
#16479=VERTEX_POINT ( 'NONE', #41838 ) ;
#16480=AXIS2_PLACEMENT_3D ( 'NONE', #39298, #27927, #3935 ) ;
#16481=DIRECTION ( 'NONE',  ( -1.000000000000000000, 0.000000000000000000, 1.734723475976806848E-16 ) ) ;
#16482=EDGE_LOOP ( 'NONE', ( #2615, #2429, #6945, #27593 ) ) ;
#16483=CARTESIAN_POINT ( 'NONE',  ( -1.909347346926324462, 3.267716535433071279, 0.1574803149606286423 ) ) ;
#16484=FACE_OUTER_BOUND ( 'NONE', #33200, .T. ) ;
#16485=EDGE_CURVE ( 'NONE', #38922, #3379, #6473, .T. ) ;
#16489=PLANE ( 'NONE',  #45884 ) ;
#16490=CARTESIAN_POINT ( 'NONE',  ( 0.000000000000000000, 3.267716535433071279, 0.4724409448818868706 ) ) ;
#16491=DIRECTION ( 'NONE',  ( -0.000000000000000000, 1.000000000000000000, -0.000000000000000000 ) ) ;
#16493=ADVANCED_FACE ( 'NONE', ( #46683 ), #14722, .F. ) ;
#16494=DIRECTION ( 'NONE',  ( -0.000000000000000000, 0.000000000000000000, 1.000000000000000000 ) ) ;
#16497=LINE ( 'NONE', #23721, #6193 ) ;
#16498=AXIS2_PLACEMENT_3D ( 'NONE', #42678, #6814, #50376 ) ;
#16505=EDGE_CURVE ( 'NONE', #17713, #33393, #37723, .T. ) ;
#16506=DIRECTION ( 'NONE',  ( 1.734723475976806848E-16, 0.000000000000000000, 1.000000000000000000 ) ) ;
#16508=LINE ( 'NONE', #7733, #17977 ) ;
#16509=VECTOR ( 'NONE', #43950, 39.37007874015748143 ) ;
#16510=CARTESIAN_POINT ( 'NONE',  ( 1.253212129322610613, 3.267716535433071279, 1.692913385826762873 ) ) ;
#16511=CARTESIAN_POINT ( 'NONE',  ( 1.363819533518803695, 0.000000000000000000, 1.732283464566921172 ) ) ;
#16514=FACE_BOUND ( 'NONE', #35819, .T. ) ;
#16515=ORIENTED_EDGE ( 'NONE', *, *, #15350, .F. ) ;
#16518=ORIENTED_EDGE ( 'NONE', *, *, #14574, .F. ) ;
#16519=DIRECTION ( 'NONE',  ( 1.734723475976806848E-16, 0.000000000000000000, 1.000000000000000000 ) ) ;
#16521=CARTESIAN_POINT ( 'NONE',  ( 0.7423782071083085965, 3.267716535433071279, -0.1968503937007880511 ) ) ;
#16523=ORIENTED_EDGE ( 'NONE', *, *, #837, .F. ) ;
#16524=EDGE_CURVE ( 'NONE', #3576, #44829, #45677, .T. ) ;
#16525=DIRECTION ( 'NONE',  ( -1.000000000000000000, 0.000000000000000000, 0.000000000000000000 ) ) ;
#16527=FACE_BOUND ( 'NONE', #49319, .T. ) ;
#16528=ADVANCED_FACE ( 'NONE', ( #14975 ), #10343, .F. ) ;
#16529=DIRECTION ( 'NONE',  ( 1.734723475976806848E-16, 0.000000000000000000, 1.000000000000000000 ) ) ;
#16531=EDGE_CURVE ( 'NONE', #24393, #22479, #38227, .T. ) ;
#16533=EDGE_LOOP ( 'NONE', ( #5206, #42918, #27089 ) ) ;
#16536=ORIENTED_EDGE ( 'NONE', *, *, #37123, .F. ) ;
#16537=ORIENTED_EDGE ( 'NONE', *, *, #44483, .T. ) ;
#16540=LINE ( 'NONE', #36676, #27592 ) ;
#16541=AXIS2_PLACEMENT_3D ( 'NONE', #12811, #12036, #16164 ) ;
#16542=CARTESIAN_POINT ( 'NONE',  ( -1.985260859929297794, 3.267716535433071279, 6.887757239314512246E-16 ) ) ;
#16544=EDGE_CURVE ( 'NONE', #1746, #46902, #49787, .T. ) ;
#16545=CARTESIAN_POINT ( 'NONE',  ( -1.363819533518803473, 3.346456692913386100, -1.299212598425192544 ) ) ;
#16547=ORIENTED_EDGE ( 'NONE', *, *, #11561, .F. ) ;
#16552=EDGE_CURVE ( 'NONE', #38226, #6075, #2850, .T. ) ;
#16553=VECTOR ( 'NONE', #42978, 39.37007874015748143 ) ;
#16554=LINE ( 'NONE', #4673, #10316 ) ;
#16555=DIRECTION ( 'NONE',  ( -3.469446951953613696E-16, 0.000000000000000000, -1.000000000000000000 ) ) ;
#16556=FACE_OUTER_BOUND ( 'NONE', #27202, .T. ) ;
#16558=DIRECTION ( 'NONE',  ( 0.000000000000000000, 0.000000000000000000, -1.000000000000000000 ) ) ;
#16560=ORIENTED_EDGE ( 'NONE', *, *, #6740, .F. ) ;
#16561=CARTESIAN_POINT ( 'NONE',  ( 2.182111253630085290, 0.000000000000000000, -0.3149606299212596716 ) ) ;
#16562=CARTESIAN_POINT ( 'NONE',  ( -0.3486774197067334935, 0.000000000000000000, 1.377952755905504256 ) ) ;
#16564=EDGE_CURVE ( 'NONE', #2069, #23689, #22971, .T. ) ;
#16565=ORIENTED_EDGE ( 'NONE', *, *, #36010, .F. ) ;
#16566=CARTESIAN_POINT ( 'NONE',  ( -0.2727639067037607723, 0.000000000000000000, -0.4724409448818883694 ) ) ;
#16567=CARTESIAN_POINT ( 'NONE',  ( -1.909347346926324906, 0.000000000000000000, -0.7874015748031470974 ) ) ;
#16568=DIRECTION ( 'NONE',  ( -0.000000000000000000, 0.000000000000000000, 1.000000000000000000 ) ) ;
#16574=LINE ( 'NONE', #4696, #27862 ) ;
#16576=EDGE_CURVE ( 'NONE', #26914, #18530, #7983, .T. ) ;
#16578=CARTESIAN_POINT ( 'NONE',  ( -1.363819533518803029, 3.267716535433071279, 2.365849761790804994E-16 ) ) ;
#16580=DIRECTION ( 'NONE',  ( -3.469446951953613696E-16, 0.000000000000000000, -1.000000000000000000 ) ) ;
#16581=VECTOR ( 'NONE', #5730, 39.37007874015748143 ) ;
#16582=ORIENTED_EDGE ( 'NONE', *, *, #32208, .T. ) ;
#16583=ORIENTED_EDGE ( 'NONE', *, *, #13585, .F. ) ;
#16584=ORIENTED_EDGE ( 'NONE', *, *, #43858, .T. ) ;
#16585=DIRECTION ( 'NONE',  ( -0.000000000000000000, 0.000000000000000000, 1.000000000000000000 ) ) ;
#16587=ORIENTED_EDGE ( 'NONE', *, *, #8882, .T. ) ;
#16588=LINE ( 'NONE', #4712, #46179 ) ;
#16589=DIRECTION ( 'NONE',  ( 0.000000000000000000, 0.000000000000000000, -1.000000000000000000 ) ) ;
#16590=VECTOR ( 'NONE', #43615, 39.37007874015748143 ) ;
#16592=EDGE_CURVE ( 'NONE', #30490, #6449, #4118, .T. ) ;
#16593=VECTOR ( 'NONE', #48955, 39.37007874015748143 ) ;
#16595=CARTESIAN_POINT ( 'NONE',  ( 0.1968503937007873017, 3.346456692913386100, -0.3149606299212591165 ) ) ;
#16596=CARTESIAN_POINT ( 'NONE',  ( -0.8182917201112819283, 3.267716535433071279, 1.850393700787391849 ) ) ;
#16598=ADVANCED_FACE ( 'NONE', ( #39479 ), #19842, .F. ) ;
#16599=ORIENTED_EDGE ( 'NONE', *, *, #12095, .F. ) ;
#16601=DIRECTION ( 'NONE',  ( 1.734723475976806848E-16, -0.000000000000000000, 1.000000000000000000 ) ) ;
#16602=ORIENTED_EDGE ( 'NONE', *, *, #15924, .F. ) ;
#16604=ORIENTED_EDGE ( 'NONE', *, *, #22184, .F. ) ;
#16605=VERTEX_POINT ( 'NONE', #35610 ) ;
#16611=ORIENTED_EDGE ( 'NONE', *, *, #42269, .F. ) ;
#16613=LINE ( 'NONE', #13759, #36636 ) ;
#16615=EDGE_LOOP ( 'NONE', ( #50416, #42086, #181, #37813 ) ) ;
#16616=CARTESIAN_POINT ( 'NONE',  ( 1.833433833923351353, 0.000000000000000000, 0.4330708661417290162 ) ) ;
#16618=VECTOR ( 'NONE', #41454, 39.37007874015748143 ) ;
#16619=( GEOMETRIC_REPRESENTATION_CONTEXT ( 3 ) GLOBAL_UNCERTAINTY_ASSIGNED_CONTEXT ( ( #24162 ) ) GLOBAL_UNIT_ASSIGNED_CONTEXT ( ( #23563, #19689, #46530 ) ) REPRESENTATION_CONTEXT ( 'NONE', 'WORKASPACE' ) );
#16620=EDGE_CURVE ( 'NONE', #1302, #30490, #47949, .T. ) ;
#16624=LINE ( 'NONE', #32376, #30307 ) ;
#16627=VECTOR ( 'NONE', #42555, 39.37007874015748143 ) ;
#16632=ADVANCED_FACE ( 'NONE', ( #12365 ), #19338, .F. ) ;
#16633=DIRECTION ( 'NONE',  ( 1.734723475976806848E-16, -0.000000000000000000, 1.000000000000000000 ) ) ;
#16634=LINE ( 'NONE', #24114, #9816 ) ;
#16636=EDGE_CURVE ( 'NONE', #5850, #3960, #43336, .T. ) ;
#16637=LINE ( 'NONE', #48079, #26754 ) ;
#16638=CARTESIAN_POINT ( 'NONE',  ( 1.363819533518803251, 0.000000000000000000, -0.1574803149606304187 ) ) ;
#16642=CARTESIAN_POINT ( 'NONE',  ( 1.560669927219590747, 0.000000000000000000, 0.4724409448818871482 ) ) ;
#16643=CARTESIAN_POINT ( 'NONE',  ( -0.2727639067037608278, 3.267716535433071279, 0.2755905511810995412 ) ) ;
#16644=EDGE_LOOP ( 'NONE', ( #24353, #37226, #34620, #35102, #40173 ) ) ;
#16645=PLANE ( 'NONE',  #20428 ) ;
#16646=DIRECTION ( 'NONE',  ( -1.000000000000000000, 0.000000000000000000, 0.000000000000000000 ) ) ;
#16648=DIRECTION ( 'NONE',  ( -0.000000000000000000, 1.000000000000000000, -0.000000000000000000 ) ) ;
#16651=ORIENTED_EDGE ( 'NONE', *, *, #29468, .T. ) ;
#16653=DIRECTION ( 'NONE',  ( -1.000000000000000000, -0.000000000000000000, -0.000000000000000000 ) ) ;
#16655=FACE_OUTER_BOUND ( 'NONE', #35772, .T. ) ;
#16656=FACE_OUTER_BOUND ( 'NONE', #5341, .T. ) ;
#16658=VECTOR ( 'NONE', #9897, 39.37007874015748143 ) ;
#16659=EDGE_CURVE ( 'NONE', #50326, #46463, #32253, .T. ) ;
#16660=DIRECTION ( 'NONE',  ( 0.000000000000000000, 0.000000000000000000, -1.000000000000000000 ) ) ;
#16661=ORIENTED_EDGE ( 'NONE', *, *, #12734, .F. ) ;
#16662=VECTOR ( 'NONE', #17610, 39.37007874015748143 ) ;
#16663=ORIENTED_EDGE ( 'NONE', *, *, #7847, .F. ) ;
#16665=LINE ( 'NONE', #44269, #236 ) ;
#16667=EDGE_CURVE ( 'NONE', #5831, #32813, #31233, .T. ) ;
#16668=EDGE_CURVE ( 'NONE', #19099, #25200, #31740, .T. ) ;
#16669=DIRECTION ( 'NONE',  ( -3.469446951953613696E-16, 0.000000000000000000, -1.000000000000000000 ) ) ;
#16670=AXIS2_PLACEMENT_3D ( 'NONE', #38059, #22805, #2675 ) ;
#16671=FACE_BOUND ( 'NONE', #6621, .T. ) ;
#16672=ORIENTED_EDGE ( 'NONE', *, *, #2407, .T. ) ;
#16673=LINE ( 'NONE', #16414, #5122 ) ;
#16674=ORIENTED_EDGE ( 'NONE', *, *, #15085, .T. ) ;
#16677=VECTOR ( 'NONE', #23408, 39.37007874015748143 ) ;
#16680=FACE_OUTER_BOUND ( 'NONE', #27073, .T. ) ;
#16681=ORIENTED_EDGE ( 'NONE', *, *, #45364, .T. ) ;
#16682=DIRECTION ( 'NONE',  ( -1.000000000000000000, 0.000000000000000000, 1.734723475976806848E-16 ) ) ;
#16686=CARTESIAN_POINT ( 'NONE',  ( 0.1968503937007873017, 0.000000000000000000, -0.3149606299212591165 ) ) ;
#16687=DIRECTION ( 'NONE',  ( -1.000000000000000000, -0.000000000000000000, -0.000000000000000000 ) ) ;
#16688=ORIENTED_EDGE ( 'NONE', *, *, #31051, .T. ) ;
#16689=LINE ( 'NONE', #39663, #48017 ) ;
#16690=DIRECTION ( 'NONE',  ( 0.000000000000000000, 1.000000000000000000, 0.000000000000000000 ) ) ;
#16691=FACE_OUTER_BOUND ( 'NONE', #17293, .T. ) ;
#16692=VERTEX_POINT ( 'NONE', #43591 ) ;
#16693=VECTOR ( 'NONE', #21943, 39.37007874015748143 ) ;
#16694=DIRECTION ( 'NONE',  ( -0.000000000000000000, 0.000000000000000000, 1.000000000000000000 ) ) ;
#16695=EDGE_CURVE ( 'NONE', #44838, #14018, #12114, .T. ) ;
#16696=LINE ( 'NONE', #41966, #27723 ) ;
#16698=LINE ( 'NONE', #32453, #48499 ) ;
#16700=DIRECTION ( 'NONE',  ( -1.000000000000000000, 0.000000000000000000, 0.000000000000000000 ) ) ;
#16704=VERTEX_POINT ( 'NONE', #43845 ) ;
#16706=LINE ( 'NONE', #694, #17512 ) ;
#16708=FACE_BOUND ( 'NONE', #41332, .T. ) ;
#16709=CARTESIAN_POINT ( 'NONE',  ( 1.363819533518803029, 3.267716535433071279, -1.605145679676863724 ) ) ;
#16710=EDGE_CURVE ( 'NONE', #31458, #1749, #47692, .T. ) ;
#16711=AXIS2_PLACEMENT_3D ( 'NONE', #29781, #25906, #17319 ) ;
#16713=CARTESIAN_POINT ( 'NONE',  ( 0.7423782071083087075, 3.267716535433071279, -6.146657985744592735E-16 ) ) ;
#16715=EDGE_LOOP ( 'NONE', ( #4791, #28026, #46931, #30637 ) ) ;
#16716=DIRECTION ( 'NONE',  ( 1.000000000000000000, -0.000000000000000000, 0.000000000000000000 ) ) ;
#16717=ORIENTED_EDGE ( 'NONE', *, *, #96, .F. ) ;
#16718=ADVANCED_FACE ( 'NONE', ( #51037 ), #16244, .F. ) ;
#16719=LINE ( 'NONE', #32211, #41757 ) ;
#16720=ORIENTED_EDGE ( 'NONE', *, *, #13837, .T. ) ;
#16721=CARTESIAN_POINT ( 'NONE',  ( 0.4696143004045478242, 3.267716535433071279, -1.629301903132387013E-16 ) ) ;
#16722=EDGE_CURVE ( 'NONE', #39361, #41791, #31703, .T. ) ;
#16725=ADVANCED_FACE ( 'NONE', ( #47180 ), #32513, .F. ) ;
#16727=VERTEX_POINT ( 'NONE', #44108 ) ;
#16728=EDGE_CURVE ( 'NONE', #39348, #30279, #17018, .T. ) ;
#16731=EDGE_CURVE ( 'NONE', #1644, #37208, #24503, .T. ) ;
#16732=CARTESIAN_POINT ( 'NONE',  ( 0.2727639067037607168, 3.267716535433071279, -4.731699523581612206E-17 ) ) ;
#16734=ORIENTED_EDGE ( 'NONE', *, *, #33166, .T. ) ;
#16735=CARTESIAN_POINT ( 'NONE',  ( -1.909347346926324906, 3.346456692913386100, -0.6692913385826758654 ) ) ;
#16736=VECTOR ( 'NONE', #13045, 39.37007874015748143 ) ;
#16739=EDGE_LOOP ( 'NONE', ( #3649, #22014, #21220, #31254 ) ) ;
#16741=VECTOR ( 'NONE', #41632, 39.37007874015748143 ) ;
#16742=AXIS2_PLACEMENT_3D ( 'NONE', #1504, #5376, #48444 ) ;
#16743=CARTESIAN_POINT ( 'NONE',  ( 0.7423782071083087075, 0.000000000000000000, -0.3149606299212593941 ) ) ;
#16744=CARTESIAN_POINT ( 'NONE',  ( -0.07591351300297333182, 0.000000000000000000, -0.4724409448818883694 ) ) ;
#16745=VERTEX_POINT ( 'NONE', #40506 ) ;
#16746=CARTESIAN_POINT ( 'NONE',  ( -0.3486774197067339376, 3.346456692913386100, 2.204724409448808764 ) ) ;
#16747=DIRECTION ( 'NONE',  ( -0.000000000000000000, 1.000000000000000000, -0.000000000000000000 ) ) ;
#16748=AXIS2_PLACEMENT_3D ( 'NONE', #44544, #24691, #39921 ) ;
#16749=CARTESIAN_POINT ( 'NONE',  ( -2.182111253630085734, 3.346456692913386100, -0.6299212598425177889 ) ) ;
#16751=CARTESIAN_POINT ( 'NONE',  ( 0.000000000000000000, 3.267716535433071279, -2.244094488188969283 ) ) ;
#16755=CARTESIAN_POINT ( 'NONE',  ( 0.5455278134075212115, 0.000000000000000000, -0.3149606299212593941 ) ) ;
#16757=EDGE_CURVE ( 'NONE', #34628, #48087, #5894, .T. ) ;
#16758=ORIENTED_EDGE ( 'NONE', *, *, #29349, .T. ) ;
#16759=DIRECTION ( 'NONE',  ( 1.734723475976806848E-16, 0.000000000000000000, 1.000000000000000000 ) ) ;
#16760=EDGE_CURVE ( 'NONE', #50682, #35324, #44608, .T. ) ;
#16761=ORIENTED_EDGE ( 'NONE', *, *, #16722, .T. ) ;
#16762=EDGE_CURVE ( 'NONE', #47284, #27651, #33538, .T. ) ;
#16763=CARTESIAN_POINT ( 'NONE',  ( -0.6214413264104939882, 3.346456692913386100, 1.732283464566921172 ) ) ;
#16764=DIRECTION ( 'NONE',  ( 0.000000000000000000, 0.000000000000000000, -1.000000000000000000 ) ) ;
#16765=DIRECTION ( 'NONE',  ( 0.000000000000000000, 0.000000000000000000, -1.000000000000000000 ) ) ;
#16766=LINE ( 'NONE', #44373, #21940 ) ;
#16769=CARTESIAN_POINT ( 'NONE',  ( -0.07591351300297340121, 0.000000000000000000, -1.614173228346451605 ) ) ;
#16770=VECTOR ( 'NONE', #21174, 39.37007874015748143 ) ;
#16771=FACE_BOUND ( 'NONE', #13285, .T. ) ;
#16772=VERTEX_POINT ( 'NONE', #21140 ) ;
#16773=DIRECTION ( 'NONE',  ( -1.000000000000000000, -0.000000000000000000, -0.000000000000000000 ) ) ;
#16774=VECTOR ( 'NONE', #21587, 39.37007874015748143 ) ;
#16775=ORIENTED_EDGE ( 'NONE', *, *, #44892, .F. ) ;
#16776=VECTOR ( 'NONE', #39258, 39.37007874015748143 ) ;
#16777=LINE ( 'NONE', #41041, #9548 ) ;
#16780=AXIS2_PLACEMENT_3D ( 'NONE', #42948, #50652, #39093 ) ;
#16782=EDGE_CURVE ( 'NONE', #13301, #20798, #28619, .T. ) ;
#16787=PLANE ( 'NONE',  #14967 ) ;
#16788=FACE_BOUND ( 'NONE', #7599, .T. ) ;
#16790=CARTESIAN_POINT ( 'NONE',  ( -0.5455278134075214336, 0.000000000000000000, -0.9448818897637762948 ) ) ;
#16791=EDGE_LOOP ( 'NONE', ( #23300, #5776, #35720, #13622 ) ) ;
#16792=DIRECTION ( 'NONE',  ( -3.469446951953613696E-16, 0.000000000000000000, -1.000000000000000000 ) ) ;
#16796=CARTESIAN_POINT ( 'NONE',  ( 0.000000000000000000, 3.267716535433071279, 0.5905511811023582691 ) ) ;
#16798=DIRECTION ( 'NONE',  ( 1.000000000000000000, 0.000000000000000000, -3.469446951953613696E-16 ) ) ;
#16801=ORIENTED_EDGE ( 'NONE', *, *, #32804, .F. ) ;
#16804=DIRECTION ( 'NONE',  ( 1.734723475976806848E-16, -0.000000000000000000, 1.000000000000000000 ) ) ;
#16807=DIRECTION ( 'NONE',  ( -1.000000000000000000, 0.000000000000000000, 0.000000000000000000 ) ) ;
#16808=VECTOR ( 'NONE', #5280, 39.37007874015748143 ) ;
#16812=FACE_OUTER_BOUND ( 'NONE', #8830, .T. ) ;
#16814=AXIS2_PLACEMENT_3D ( 'NONE', #38968, #27594, #3602 ) ;
#16816=LINE ( 'NONE', #20675, #22603 ) ;
#16817=CARTESIAN_POINT ( 'NONE',  ( -1.909347346926324906, 3.346456692913386100, 1.417322834645662333 ) ) ;
#16818=EDGE_CURVE ( 'NONE', #16904, #16878, #29390, .T. ) ;
#16819=ORIENTED_EDGE ( 'NONE', *, *, #7952, .F. ) ;
#16820=ADVANCED_FACE ( 'NONE', ( #9009, #32777 ), #9776, .T. ) ;
#16822=VERTEX_POINT ( 'NONE', #33028 ) ;
#16824=DIRECTION ( 'NONE',  ( -1.000000000000000000, 0.000000000000000000, 1.734723475976806848E-16 ) ) ;
#16825=LINE ( 'NONE', #32581, #13976 ) ;
#16827=ORIENTED_EDGE ( 'NONE', *, *, #31487, .F. ) ;
#16828=EDGE_CURVE ( 'NONE', #43386, #43398, #5131, .T. ) ;
#16829=ORIENTED_EDGE ( 'NONE', *, *, #13202, .F. ) ;
#16830=PLANE ( 'NONE',  #27068 ) ;
#16831=ORIENTED_EDGE ( 'NONE', *, *, #49999, .T. ) ;
#16832=VERTEX_POINT ( 'NONE', #41022 ) ;
#16833=DIRECTION ( 'NONE',  ( 1.734723475976806848E-16, 0.000000000000000000, 1.000000000000000000 ) ) ;
#16834=LINE ( 'NONE', #37224, #30521 ) ;
#16839=ORIENTED_EDGE ( 'NONE', *, *, #43029, .T. ) ;
#16840=EDGE_LOOP ( 'NONE', ( #29298, #49543, #18667, #37077 ) ) ;
#16842=VECTOR ( 'NONE', #43517, 39.37007874015748143 ) ;
#16843=ORIENTED_EDGE ( 'NONE', *, *, #20707, .F. ) ;
#16844=ORIENTED_EDGE ( 'NONE', *, *, #34860, .T. ) ;
#16848=LINE ( 'NONE', #44194, #22775 ) ;
#16850=AXIS2_PLACEMENT_3D ( 'NONE', #39885, #4516, #20255 ) ;
#16852=ORIENTED_EDGE ( 'NONE', *, *, #50110, .T. ) ;
#16853=PLANE ( 'NONE',  #27098 ) ;
#16854=DIRECTION ( 'NONE',  ( -0.000000000000000000, 1.000000000000000000, -0.000000000000000000 ) ) ;
#16855=EDGE_CURVE ( 'NONE', #10381, #1302, #49997, .T. ) ;
#16856=LINE ( 'NONE', #13741, #45110 ) ;
#16857=ORIENTED_EDGE ( 'NONE', *, *, #605, .F. ) ;
#16859=DIRECTION ( 'NONE',  ( -3.469446951953613696E-16, 0.000000000000000000, -1.000000000000000000 ) ) ;
#16860=VECTOR ( 'NONE', #8240, 39.37007874015748143 ) ;
#16861=DIRECTION ( 'NONE',  ( 1.734723475976806848E-16, 0.000000000000000000, 1.000000000000000000 ) ) ;
#16863=ORIENTED_EDGE ( 'NONE', *, *, #15962, .T. ) ;
#16865=DIRECTION ( 'NONE',  ( 1.000000000000000000, 0.000000000000000000, 0.000000000000000000 ) ) ;
#16866=EDGE_CURVE ( 'NONE', #49288, #41994, #44863, .T. ) ;
#16867=PLANE ( 'NONE',  #9917 ) ;
#16868=DIRECTION ( 'NONE',  ( -3.469446951953613696E-16, 0.000000000000000000, -1.000000000000000000 ) ) ;
#16869=FACE_OUTER_BOUND ( 'NONE', #13462, .T. ) ;
#16871=ORIENTED_EDGE ( 'NONE', *, *, #27918, .T. ) ;
#16872=CARTESIAN_POINT ( 'NONE',  ( -1.091055626815042201, 0.000000000000000000, 0.6299212598425164567 ) ) ;
#16874=DIRECTION ( 'NONE',  ( 0.000000000000000000, -1.000000000000000000, 0.000000000000000000 ) ) ;
#16877=DIRECTION ( 'NONE',  ( -3.469446951953613696E-16, 0.000000000000000000, -1.000000000000000000 ) ) ;
#16878=VERTEX_POINT ( 'NONE', #47056 ) ;
#16880=CARTESIAN_POINT ( 'NONE',  ( 0.000000000000000000, 3.267716535433071279, 1.377952755905504256 ) ) ;
#16881=AXIS2_PLACEMENT_3D ( 'NONE', #6264, #14258, #45472 ) ;
#16882=DIRECTION ( 'NONE',  ( -3.469446951953613696E-16, 0.000000000000000000, -1.000000000000000000 ) ) ;
#16884=EDGE_CURVE ( 'NONE', #33629, #29961, #2848, .T. ) ;
#16886=EDGE_LOOP ( 'NONE', ( #12588, #47788, #14826, #22259 ) ) ;
#16887=DIRECTION ( 'NONE',  ( 1.734723475976806848E-16, -0.000000000000000000, 1.000000000000000000 ) ) ;
#16890=ORIENTED_EDGE ( 'NONE', *, *, #20272, .F. ) ;
#16891=CARTESIAN_POINT ( 'NONE',  ( -1.363819533518803029, 3.267716535433071279, 0.7874015748031456541 ) ) ;
#16892=EDGE_CURVE ( 'NONE', #31439, #17089, #26964, .T. ) ;
#16893=DIRECTION ( 'NONE',  ( -1.000000000000000000, 0.000000000000000000, -0.000000000000000000 ) ) ;
#16895=ORIENTED_EDGE ( 'NONE', *, *, #20368, .T. ) ;
#16897=CARTESIAN_POINT ( 'NONE',  ( 2.182111253630085290, 0.000000000000000000, 0.1181102362204698858 ) ) ;
#16898=VERTEX_POINT ( 'NONE', #49470 ) ;
#16900=DIRECTION ( 'NONE',  ( 1.000000000000000000, 0.000000000000000000, 0.000000000000000000 ) ) ;
#16901=DIRECTION ( 'NONE',  ( -3.469446951953613696E-16, 0.000000000000000000, -1.000000000000000000 ) ) ;
#16902=PLANE ( 'NONE',  #33460 ) ;
#16903=DIRECTION ( 'NONE',  ( 1.000000000000000000, -0.000000000000000000, 0.000000000000000000 ) ) ;
#16904=VERTEX_POINT ( 'NONE', #19470 ) ;
#16905=ORIENTED_EDGE ( 'NONE', *, *, #22087, .T. ) ;
#16907=CARTESIAN_POINT ( 'NONE',  ( -1.091055626815042645, 0.000000000000000000, 2.007874015748021268 ) ) ;
#16910=FACE_OUTER_BOUND ( 'NONE', #23700, .T. ) ;
#16911=CARTESIAN_POINT ( 'NONE',  ( -0.5455278134075214336, 3.346456692913386100, 2.204724409448808764 ) ) ;
#16912=LINE ( 'NONE', #4777, #12486 ) ;
#16916=DIRECTION ( 'NONE',  ( 1.000000000000000000, -0.000000000000000000, 0.000000000000000000 ) ) ;
#16917=ADVANCED_FACE ( 'NONE', ( #7361 ), #23600, .F. ) ;
#16920=LINE ( 'NONE', #48620, #22402 ) ;
#16921=FACE_BOUND ( 'NONE', #24720, .T. ) ;
#16922=VECTOR ( 'NONE', #30269, 39.37007874015748143 ) ;
#16924=VECTOR ( 'NONE', #1201, 39.37007874015748143 ) ;
#16925=LINE ( 'NONE', #40929, #169 ) ;
#16926=AXIS2_PLACEMENT_3D ( 'NONE', #47173, #7720, #7229 ) ;
#16927=ORIENTED_EDGE ( 'NONE', *, *, #16102, .F. ) ;
#16930=EDGE_CURVE ( 'NONE', #35430, #34365, #50661, .T. ) ;
#16932=EDGE_CURVE ( 'NONE', #35391, #5168, #39355, .T. ) ;
#16934=ORIENTED_EDGE ( 'NONE', *, *, #4587, .F. ) ;
#16935=EDGE_LOOP ( 'NONE', ( #2885, #36332, #14696, #40585 ) ) ;
#16937=ORIENTED_EDGE ( 'NONE', *, *, #28417, .F. ) ;
#16938=VECTOR ( 'NONE', #17914, 39.37007874015748143 ) ;
#16939=EDGE_CURVE ( 'NONE', #37379, #7713, #3993, .T. ) ;
#16941=LINE ( 'NONE', #9184, #17870 ) ;
#16947=CARTESIAN_POINT ( 'NONE',  ( -1.363819533518803473, 3.346456692913386100, 1.850393700787392293 ) ) ;
#16948=VERTEX_POINT ( 'NONE', #42956 ) ;
#16949=CARTESIAN_POINT ( 'NONE',  ( 1.091055626815042645, 0.000000000000000000, -0.9448818897637765168 ) ) ;
#16950=DIRECTION ( 'NONE',  ( -0.000000000000000000, 1.000000000000000000, -0.000000000000000000 ) ) ;
#16952=VERTEX_POINT ( 'NONE', #18029 ) ;
#16953=CARTESIAN_POINT ( 'NONE',  ( 0.2727639067037609943, 0.000000000000000000, 1.850393700787392293 ) ) ;
#16954=CARTESIAN_POINT ( 'NONE',  ( -1.091055626815042201, 0.000000000000000000, 0.6299212598425164567 ) ) ;
#16955=ORIENTED_EDGE ( 'NONE', *, *, #26597, .F. ) ;
#16956=DIRECTION ( 'NONE',  ( 1.000000000000000000, 0.000000000000000000, 0.000000000000000000 ) ) ;
#16958=EDGE_CURVE ( 'NONE', #13751, #14372, #31362, .T. ) ;
#16959=DIRECTION ( 'NONE',  ( 0.000000000000000000, 0.000000000000000000, -1.000000000000000000 ) ) ;
#16960=VECTOR ( 'NONE', #26766, 39.37007874015748143 ) ;
#16961=VECTOR ( 'NONE', #13844, 39.37007874015748143 ) ;
#16962=EDGE_LOOP ( 'NONE', ( #26984, #5696, #36821, #47285 ) ) ;
#16963=DIRECTION ( 'NONE',  ( -0.000000000000000000, 1.000000000000000000, -0.000000000000000000 ) ) ;
#16965=FACE_BOUND ( 'NONE', #3660, .T. ) ;
#16967=CARTESIAN_POINT ( 'NONE',  ( -0.5455278134075214336, 0.000000000000000000, 2.204724409448808764 ) ) ;
#16968=CARTESIAN_POINT ( 'NONE',  ( -0.2727639067037607723, 3.346456692913386100, -0.7874015748031470974 ) ) ;
#16969=CARTESIAN_POINT ( 'NONE',  ( -1.712496953225537188, 3.267716535433071279, 0.2755905511810996522 ) ) ;
#16970=CIRCLE ( 'NONE', #6233, 2.165354330708661568 ) ;
#16971=AXIS2_PLACEMENT_3D ( 'NONE', #19548, #16200, #35820 ) ;
#16973=ORIENTED_EDGE ( 'NONE', *, *, #37872, .T. ) ;
#16974=CARTESIAN_POINT ( 'NONE',  ( 1.909347346926324462, 0.000000000000000000, -1.102362204724406602 ) ) ;
#16975=ORIENTED_EDGE ( 'NONE', *, *, #14123, .F. ) ;
#16976=DIRECTION ( 'NONE',  ( -1.000000000000000000, -0.000000000000000000, -0.000000000000000000 ) ) ;
#16977=VERTEX_POINT ( 'NONE', #7608 ) ;
#16980=DIRECTION ( 'NONE',  ( -0.000000000000000000, 1.000000000000000000, -0.000000000000000000 ) ) ;
#16982=ORIENTED_EDGE ( 'NONE', *, *, #40231, .T. ) ;
#16983=DIRECTION ( 'NONE',  ( -0.000000000000000000, 0.000000000000000000, 1.000000000000000000 ) ) ;
#16984=EDGE_LOOP ( 'NONE', ( #17302, #21538, #27626, #45488, #10422 ) ) ;
#16986=EDGE_CURVE ( 'NONE', #45623, #21877, #25919, .T. ) ;
#16987=EDGE_CURVE ( 'NONE', #46194, #8104, #10976, .T. ) ;
#16988=ORIENTED_EDGE ( 'NONE', *, *, #16467, .F. ) ;
#16989=VERTEX_POINT ( 'NONE', #11728 ) ;
#16990=CARTESIAN_POINT ( 'NONE',  ( -2.182111253630085290, 3.346456692913386100, -0.3149606299212589500 ) ) ;
#16991=ADVANCED_FACE ( 'NONE', ( #39103 ), #50914, .F. ) ;
#16992=VECTOR ( 'NONE', #31539, 39.37007874015748143 ) ;
#16993=CIRCLE ( 'NONE', #27650, 2.165354330708661568 ) ;
#16994=ORIENTED_EDGE ( 'NONE', *, *, #27711, .T. ) ;
#16998=DIRECTION ( 'NONE',  ( -0.000000000000000000, 1.000000000000000000, -0.000000000000000000 ) ) ;
#16999=VECTOR ( 'NONE', #13998, 39.37007874015748143 ) ;
#17000=LINE ( 'NONE', #29373, #3307 ) ;
#17001=ORIENTED_EDGE ( 'NONE', *, *, #33219, .F. ) ;
#17003=DIRECTION ( 'NONE',  ( 1.734723475976806848E-16, -0.000000000000000000, 1.000000000000000000 ) ) ;
#17004=DIRECTION ( 'NONE',  ( 1.734723475976806848E-16, -0.000000000000000000, 1.000000000000000000 ) ) ;
#17005=FACE_OUTER_BOUND ( 'NONE', #9614, .T. ) ;
#17007=ADVANCED_FACE ( 'NONE', ( #22854 ), #38605, .F. ) ;
#17008=CARTESIAN_POINT ( 'NONE',  ( 1.287906020515830141, 3.346456692913386100, 0.4330708661417287386 ) ) ;
#17010=EDGE_CURVE ( 'NONE', #8152, #37129, #41519, .T. ) ;
#17012=ORIENTED_EDGE ( 'NONE', *, *, #34914, .T. ) ;
#17014=DIRECTION ( 'NONE',  ( -1.000000000000000000, 0.000000000000000000, 0.000000000000000000 ) ) ;
#17015=EDGE_CURVE ( 'NONE', #39871, #48261, #31609, .T. ) ;
#17018=LINE ( 'NONE', #1765, #49785 ) ;
#17021=LINE ( 'NONE', #45119, #21216 ) ;
#17022=CARTESIAN_POINT ( 'NONE',  ( 0.4696143004045484348, 3.346456692913386100, 1.850393700787392293 ) ) ;
#17023=DIRECTION ( 'NONE',  ( -0.000000000000000000, 0.000000000000000000, 1.000000000000000000 ) ) ;
#17024=DIRECTION ( 'NONE',  ( 0.000000000000000000, -1.000000000000000000, 0.000000000000000000 ) ) ;
#17025=DIRECTION ( 'NONE',  ( -3.469446951953613696E-16, 0.000000000000000000, -1.000000000000000000 ) ) ;
#17026=VERTEX_POINT ( 'NONE', #8626 ) ;
#17027=VECTOR ( 'NONE', #23027, 39.37007874015748143 ) ;
#17028=LINE ( 'NONE', #13401, #29891 ) ;
#17029=VECTOR ( 'NONE', #25488, 39.37007874015748143 ) ;
#17032=ORIENTED_EDGE ( 'NONE', *, *, #49067, .F. ) ;
#17034=VECTOR ( 'NONE', #33177, 39.37007874015748143 ) ;
#17036=PLANE ( 'NONE',  #10395 ) ;
#17038=AXIS2_PLACEMENT_3D ( 'NONE', #2959, #7087, #18954 ) ;
#17039=FACE_OUTER_BOUND ( 'NONE', #18748, .T. ) ;
#17040=VECTOR ( 'NONE', #47778, 39.37007874015748143 ) ;
#17041=LINE ( 'NONE', #9029, #3261 ) ;
#17045=LINE ( 'NONE', #5919, #39691 ) ;
#17046=CARTESIAN_POINT ( 'NONE',  ( -0.7053729475263578186, 3.346456692913386100, -2.047244094488181343 ) ) ;
#17048=CARTESIAN_POINT ( 'NONE',  ( -1.636583440222564301, 3.267716535433071279, -0.9448818897637762948 ) ) ;
#17049=LINE ( 'NONE', #44394, #35737 ) ;
#17050=ORIENTED_EDGE ( 'NONE', *, *, #26066, .F. ) ;
#17052=ADVANCED_FACE ( 'NONE', ( #8878 ), #24634, .F. ) ;
#17054=ADVANCED_FACE ( 'NONE', ( #47824 ), #106, .F. ) ;
#17055=CARTESIAN_POINT ( 'NONE',  ( -2.165354330708661568, 3.267716535433071279, -6.146657985744592735E-16 ) ) ;
#17056=ORIENTED_EDGE ( 'NONE', *, *, #7473, .F. ) ;
#17057=VERTEX_POINT ( 'NONE', #15850 ) ;
#17058=EDGE_CURVE ( 'NONE', #15499, #38331, #1126, .T. ) ;
#17060=LINE ( 'NONE', #8788, #40810 ) ;
#17061=LINE ( 'NONE', #12926, #50500 ) ;
#17062=VECTOR ( 'NONE', #14398, 39.37007874015748143 ) ;
#17063=CARTESIAN_POINT ( 'NONE',  ( 0.2727639067037604392, 0.000000000000000000, -0.6692913385826760875 ) ) ;
#17065=ORIENTED_EDGE ( 'NONE', *, *, #42795, .F. ) ;
#17066=ORIENTED_EDGE ( 'NONE', *, *, #22432, .F. ) ;
#17067=CARTESIAN_POINT ( 'NONE',  ( 1.833433833923351353, 0.000000000000000000, 0.7480314960629872445 ) ) ;
#17068=VECTOR ( 'NONE', #16230, 39.37007874015748143 ) ;
#17069=CARTESIAN_POINT ( 'NONE',  ( 4.268512490100411402E-16, 0.000000000000000000, 1.889763779527550369 ) ) ;
#17072=ADVANCED_FACE ( 'NONE', ( #12495 ), #35999, .F. ) ;
#17074=AXIS2_PLACEMENT_3D ( 'NONE', #8090, #23324, #601 ) ;
#17075=DIRECTION ( 'NONE',  ( -3.469446951953613696E-16, 0.000000000000000000, -1.000000000000000000 ) ) ;
#17077=EDGE_LOOP ( 'NONE', ( #49548, #5534, #21988, #3515 ) ) ;
#17079=FACE_OUTER_BOUND ( 'NONE', #18248, .T. ) ;
#17081=ORIENTED_EDGE ( 'NONE', *, *, #29852, .F. ) ;
#17084=LINE ( 'NONE', #13210, #20393 ) ;
#17086=ORIENTED_EDGE ( 'NONE', *, *, #36115, .T. ) ;
#17088=ORIENTED_EDGE ( 'NONE', *, *, #43513, .T. ) ;
#17089=VERTEX_POINT ( 'NONE', #12760 ) ;
#17091=CARTESIAN_POINT ( 'NONE',  ( 0.000000000000000000, 0.000000000000000000, 0.000000000000000000 ) ) ;
#17092=VECTOR ( 'NONE', #44611, 39.37007874015748143 ) ;
#17094=EDGE_LOOP ( 'NONE', ( #35842, #14962, #40726, #14635 ) ) ;
#17096=VERTEX_POINT ( 'NONE', #5008 ) ;
#17098=CARTESIAN_POINT ( 'NONE',  ( -0.8182917201112814842, 0.000000000000000000, 1.417322834645662777 ) ) ;
#17099=EDGE_LOOP ( 'NONE', ( #3381, #32596, #47249, #7209 ) ) ;
#17100=VERTEX_POINT ( 'NONE', #11987 ) ;
#17101=DIRECTION ( 'NONE',  ( -0.000000000000000000, 1.000000000000000000, -0.000000000000000000 ) ) ;
#17105=CARTESIAN_POINT ( 'NONE',  ( 1.253212129322610613, 3.346456692913386100, 1.692913385826762873 ) ) ;
#17106=CARTESIAN_POINT ( 'NONE',  ( 0.000000000000000000, 3.346456692913386100, 0.000000000000000000 ) ) ;
#17107=LINE ( 'NONE', #37243, #40206 ) ;
#17108=EDGE_LOOP ( 'NONE', ( #27254, #28187, #9087, #47038 ) ) ;
#17112=EDGE_CURVE ( 'NONE', #40318, #18552, #39610, .T. ) ;
#17113=LINE ( 'NONE', #16344, #27396 ) ;
#17115=VERTEX_POINT ( 'NONE', #24375 ) ;
#17119=CARTESIAN_POINT ( 'NONE',  ( -0.07591351300297277671, 3.267716535433071279, 0.7874015748031456541 ) ) ;
#17121=ORIENTED_EDGE ( 'NONE', *, *, #33628, .F. ) ;
#17123=CARTESIAN_POINT ( 'NONE',  ( 0.000000000000000000, 3.267716535433071279, 0.4330708661417287386 ) ) ;
#17125=CARTESIAN_POINT ( 'NONE',  ( -1.712496953225537633, 0.000000000000000000, -0.4724409448818884805 ) ) ;
#17127=EDGE_CURVE ( 'NONE', #24669, #47091, #16637, .T. ) ;
#17130=LINE ( 'NONE', #33140, #20897 ) ;
#17131=LINE ( 'NONE', #45479, #50743 ) ;
#17133=ORIENTED_EDGE ( 'NONE', *, *, #3540, .F. ) ;
#17136=VECTOR ( 'NONE', #5418, 39.37007874015748143 ) ;
#17137=CARTESIAN_POINT ( 'NONE',  ( 0.7423782071083085965, 3.267716535433071279, 0.1181102362204701633 ) ) ;
#17138=ORIENTED_EDGE ( 'NONE', *, *, #41933, .T. ) ;
#17139=DIRECTION ( 'NONE',  ( 1.000000000000000000, 0.000000000000000000, 0.000000000000000000 ) ) ;
#17140=FACE_OUTER_BOUND ( 'NONE', #36616, .T. ) ;
#17141=CARTESIAN_POINT ( 'NONE',  ( -1.439733046521776583, 3.346456692913386100, -0.3149606299212592275 ) ) ;
#17142=ORIENTED_EDGE ( 'NONE', *, *, #33913, .T. ) ;
#17144=VECTOR ( 'NONE', #35082, 39.37007874015748143 ) ;
#17145=DIRECTION ( 'NONE',  ( -0.000000000000000000, 1.000000000000000000, -0.000000000000000000 ) ) ;
#17146=ORIENTED_EDGE ( 'NONE', *, *, #32092, .T. ) ;
#17149=EDGE_LOOP ( 'NONE', ( #28333, #9496, #7490, #12685 ) ) ;
#17150=VECTOR ( 'NONE', #932, 39.37007874015748143 ) ;
#17151=DIRECTION ( 'NONE',  ( 1.734723475976806848E-16, 0.000000000000000000, 1.000000000000000000 ) ) ;
#17152=EDGE_CURVE ( 'NONE', #17158, #46657, #18886, .T. ) ;
#17153=DIRECTION ( 'NONE',  ( -0.000000000000000000, 1.000000000000000000, -0.000000000000000000 ) ) ;
#17155=LINE ( 'NONE', #12772, #25993 ) ;
#17157=ORIENTED_EDGE ( 'NONE', *, *, #26709, .F. ) ;
#17158=VERTEX_POINT ( 'NONE', #50321 ) ;
#17159=LINE ( 'NONE', #13032, #22409 ) ;
#17160=CARTESIAN_POINT ( 'NONE',  ( 0.1968503937007877458, 3.267716535433071279, -6.829619984160669139E-17 ) ) ;
#17161=ORIENTED_EDGE ( 'NONE', *, *, #5348, .T. ) ;
#17163=CARTESIAN_POINT ( 'NONE',  ( 1.091055626815042645, 0.000000000000000000, 0.7480314960629872445 ) ) ;
#17164=DIRECTION ( 'NONE',  ( 1.000000000000000000, 0.000000000000000000, 0.000000000000000000 ) ) ;
#17167=ORIENTED_EDGE ( 'NONE', *, *, #30158, .T. ) ;
#17168=DIRECTION ( 'NONE',  ( -0.000000000000000000, 1.000000000000000000, -0.000000000000000000 ) ) ;
#17169=DIRECTION ( 'NONE',  ( -1.000000000000000000, 0.000000000000000000, -0.000000000000000000 ) ) ;
#17170=CIRCLE ( 'NONE', #28722, 2.165354330708661568 ) ;
#17171=VECTOR ( 'NONE', #43594, 39.37007874015748143 ) ;
#17172=DIRECTION ( 'NONE',  ( 1.734723475976806848E-16, -0.000000000000000000, 1.000000000000000000 ) ) ;
#17173=ORIENTED_EDGE ( 'NONE', *, *, #22064, .T. ) ;
#17174=CARTESIAN_POINT ( 'NONE',  ( 0.2727639067037604947, 3.346456692913386100, -0.1574803149606298636 ) ) ;
#17175=FACE_BOUND ( 'NONE', #11851, .T. ) ;
#17177=DIRECTION ( 'NONE',  ( -3.469446951953613696E-16, 0.000000000000000000, -1.000000000000000000 ) ) ;
#17178=ORIENTED_EDGE ( 'NONE', *, *, #28615, .T. ) ;
#17179=VECTOR ( 'NONE', #46536, 39.37007874015748143 ) ;
#17180=ORIENTED_EDGE ( 'NONE', *, *, #1514, .T. ) ;
#17183=AXIS2_PLACEMENT_3D ( 'NONE', #24055, #15790, #300 ) ;
#17184=EDGE_CURVE ( 'NONE', #33705, #45841, #35023, .T. ) ;
#17186=FACE_OUTER_BOUND ( 'NONE', #13368, .T. ) ;
#17188=VECTOR ( 'NONE', #22640, 39.37007874015748143 ) ;
#17192=LINE ( 'NONE', #29825, #29405 ) ;
#17193=DIRECTION ( 'NONE',  ( -0.000000000000000000, 1.000000000000000000, -0.000000000000000000 ) ) ;
#17195=LINE ( 'NONE', #32960, #23946 ) ;
#17196=CARTESIAN_POINT ( 'NONE',  ( -1.363819533518803029, 0.000000000000000000, 0.5905511811023582691 ) ) ;
#17197=DIRECTION ( 'NONE',  ( 1.734723475976806848E-16, -0.000000000000000000, 1.000000000000000000 ) ) ;
#17199=PLANE ( 'NONE',  #29115 ) ;
#17200=DIRECTION ( 'NONE',  ( 1.734723475976806848E-16, -0.000000000000000000, 1.000000000000000000 ) ) ;
#17201=VERTEX_POINT ( 'NONE', #46223 ) ;
#17202=CARTESIAN_POINT ( 'NONE',  ( -1.909347346926324462, 3.346456692913386100, -0.03937007874015881204 ) ) ;
#17203=DIRECTION ( 'NONE',  ( -3.469446951953613696E-16, 0.000000000000000000, -1.000000000000000000 ) ) ;
#17204=ORIENTED_EDGE ( 'NONE', *, *, #40791, .T. ) ;
#17205=FACE_OUTER_BOUND ( 'NONE', #43324, .T. ) ;
#17206=VECTOR ( 'NONE', #29081, 39.37007874015748143 ) ;
#17207=EDGE_CURVE ( 'NONE', #47496, #45614, #3138, .T. ) ;
#17209=CARTESIAN_POINT ( 'NONE',  ( -1.439733046521776583, 3.267716535433071279, -0.6299212598425177889 ) ) ;
#17211=VECTOR ( 'NONE', #48306, 39.37007874015748143 ) ;
#17214=FACE_BOUND ( 'NONE', #33809, .T. ) ;
#17215=EDGE_CURVE ( 'NONE', #29095, #42180, #23505, .T. ) ;
#17216=DIRECTION ( 'NONE',  ( -0.000000000000000000, 0.000000000000000000, 1.000000000000000000 ) ) ;
#17217=VECTOR ( 'NONE', #36028, 39.37007874015748143 ) ;
#17219=PLANE ( 'NONE',  #19361 ) ;
#17220=CARTESIAN_POINT ( 'NONE',  ( -1.439733046521776139, 3.267716535433071279, 1.259842519685033357 ) ) ;
#17222=VECTOR ( 'NONE', #45162, 39.37007874015748143 ) ;
#17223=EDGE_LOOP ( 'NONE', ( #47337, #47055, #18987, #33982 ) ) ;
#17225=DIRECTION ( 'NONE',  ( -3.469446951953613696E-16, 0.000000000000000000, -1.000000000000000000 ) ) ;
#17226=ORIENTED_EDGE ( 'NONE', *, *, #49108, .F. ) ;
#17227=EDGE_CURVE ( 'NONE', #3253, #3427, #46719, .T. ) ;
#17228=AXIS2_PLACEMENT_3D ( 'NONE', #14400, #33535, #37402 ) ;
#17229=DIRECTION ( 'NONE',  ( -0.000000000000000000, 1.000000000000000000, -0.000000000000000000 ) ) ;
#17230=ORIENTED_EDGE ( 'NONE', *, *, #34511, .T. ) ;
#17234=LINE ( 'NONE', #12586, #19984 ) ;
#17235=CARTESIAN_POINT ( 'NONE',  ( -2.454875160333845674, 3.346456692913386100, -0.1574803149606298636 ) ) ;
#17236=ORIENTED_EDGE ( 'NONE', *, *, #9074, .T. ) ;
#17237=DIRECTION ( 'NONE',  ( 0.000000000000000000, -1.000000000000000000, 0.000000000000000000 ) ) ;
#17238=ORIENTED_EDGE ( 'NONE', *, *, #20358, .T. ) ;
#17239=VERTEX_POINT ( 'NONE', #11139 ) ;
#17240=EDGE_CURVE ( 'NONE', #50120, #22538, #13, .T. ) ;
#17241=VECTOR ( 'NONE', #36719, 39.37007874015748143 ) ;
#17242=ORIENTED_EDGE ( 'NONE', *, *, #44663, .F. ) ;
#17243=VERTEX_POINT ( 'NONE', #43373 ) ;
#17244=EDGE_CURVE ( 'NONE', #38459, #24866, #42369, .T. ) ;
#17245=LINE ( 'NONE', #33004, #34351 ) ;
#17248=ORIENTED_EDGE ( 'NONE', *, *, #20561, .F. ) ;
#17249=DIRECTION ( 'NONE',  ( 1.734723475976806848E-16, -0.000000000000000000, 1.000000000000000000 ) ) ;
#17251=LINE ( 'NONE', #29879, #18647 ) ;
#17252=AXIS2_PLACEMENT_3D ( 'NONE', #26115, #25604, #2374 ) ;
#17253=VECTOR ( 'NONE', #47800, 39.37007874015748143 ) ;
#17254=DIRECTION ( 'NONE',  ( 0.000000000000000000, 0.000000000000000000, -1.000000000000000000 ) ) ;
#17255=AXIS2_PLACEMENT_3D ( 'NONE', #10155, #6291, #48340 ) ;
#17256=ORIENTED_EDGE ( 'NONE', *, *, #44616, .F. ) ;
#17257=LINE ( 'NONE', #18260, #37674 ) ;
#17260=CARTESIAN_POINT ( 'NONE',  ( -2.454875160333845674, 3.346456692913386100, -0.1574803149606298636 ) ) ;
#17261=DIRECTION ( 'NONE',  ( 0.000000000000000000, 0.000000000000000000, -1.000000000000000000 ) ) ;
#17262=VECTOR ( 'NONE', #362, 39.37007874015748143 ) ;
#17263=CARTESIAN_POINT ( 'NONE',  ( 1.091055626815042645, 0.000000000000000000, -0.6299212598425181220 ) ) ;
#17264=LINE ( 'NONE', #41511, #6666 ) ;
#17265=DIRECTION ( 'NONE',  ( 0.000000000000000000, 0.000000000000000000, -1.000000000000000000 ) ) ;
#17266=VERTEX_POINT ( 'NONE', #47214 ) ;
#17267=LINE ( 'NONE', #25259, #26249 ) ;
#17268=EDGE_CURVE ( 'NONE', #23466, #20757, #26867, .T. ) ;
#17272=VERTEX_POINT ( 'NONE', #7271 ) ;
#17273=CARTESIAN_POINT ( 'NONE',  ( 1.287906020515829919, 0.000000000000000000, -1.456692913385822630 ) ) ;
#17274=EDGE_CURVE ( 'NONE', #39828, #42444, #15258, .T. ) ;
#17275=CARTESIAN_POINT ( 'NONE',  ( -1.636583440222563635, 0.000000000000000000, 0.3149606299212578953 ) ) ;
#17276=CARTESIAN_POINT ( 'NONE',  ( -0.8942052331142552601, 3.267716535433071279, 1.692913385826762873 ) ) ;
#17278=CARTESIAN_POINT ( 'NONE',  ( 0.5455278134075212115, 3.346456692913386100, 0.9448818897637746295 ) ) ;
#17280=VECTOR ( 'NONE', #19352, 39.37007874015748143 ) ;
#17282=EDGE_CURVE ( 'NONE', #25584, #20592, #4661, .T. ) ;
#17284=DIRECTION ( 'NONE',  ( -0.000000000000000000, 1.000000000000000000, -0.000000000000000000 ) ) ;
#17288=CIRCLE ( 'NONE', #2474, 2.106299212598425008 ) ;
#17290=CARTESIAN_POINT ( 'NONE',  ( 1.363819533518803695, 0.000000000000000000, 1.732283464566921172 ) ) ;
#17292=DIRECTION ( 'NONE',  ( 1.000000000000000000, 0.000000000000000000, 0.000000000000000000 ) ) ;
#17293=EDGE_LOOP ( 'NONE', ( #42365, #26648, #5573, #424 ) ) ;
#17296=CARTESIAN_POINT ( 'NONE',  ( -0.2727639067037604392, 3.267716535433071279, 4.731699523581607276E-17 ) ) ;
#17297=FACE_BOUND ( 'NONE', #27346, .T. ) ;
#17300=FACE_OUTER_BOUND ( 'NONE', #50741, .T. ) ;
#17301=LINE ( 'NONE', #24786, #39013 ) ;
#17302=ORIENTED_EDGE ( 'NONE', *, *, #837, .T. ) ;
#17305=DIRECTION ( 'NONE',  ( -3.469446951953613696E-16, 0.000000000000000000, -1.000000000000000000 ) ) ;
#17307=LINE ( 'NONE', #13429, #39397 ) ;
#17308=ORIENTED_EDGE ( 'NONE', *, *, #10169, .F. ) ;
#17309=ORIENTED_EDGE ( 'NONE', *, *, #50032, .F. ) ;
#17310=ORIENTED_EDGE ( 'NONE', *, *, #36215, .F. ) ;
#17311=FACE_OUTER_BOUND ( 'NONE', #13232, .T. ) ;
#17313=VECTOR ( 'NONE', #4784, 39.37007874015748143 ) ;
#17315=LINE ( 'NONE', #1042, #18466 ) ;
#17316=FACE_OUTER_BOUND ( 'NONE', #29016, .T. ) ;
#17318=ORIENTED_EDGE ( 'NONE', *, *, #3418, .T. ) ;
#17319=DIRECTION ( 'NONE',  ( 1.734723475976806848E-16, 0.000000000000000000, 1.000000000000000000 ) ) ;
#17321=DIRECTION ( 'NONE',  ( 0.000000000000000000, 1.000000000000000000, 0.000000000000000000 ) ) ;
#17322=PLANE ( 'NONE',  #3717 ) ;
#17323=DIRECTION ( 'NONE',  ( 1.734723475976806848E-16, 0.000000000000000000, 1.000000000000000000 ) ) ;
#17327=FACE_OUTER_BOUND ( 'NONE', #13874, .T. ) ;
#17328=VERTEX_POINT ( 'NONE', #16279 ) ;
#17329=CARTESIAN_POINT ( 'NONE',  ( -1.166969139818015533, 3.267716535433071279, 0.7874015748031456541 ) ) ;
#17331=VECTOR ( 'NONE', #32593, 39.37007874015748143 ) ;
#17333=ORIENTED_EDGE ( 'NONE', *, *, #6892, .T. ) ;
#17334=EDGE_LOOP ( 'NONE', ( #41031, #9965, #10794, #27529 ) ) ;
#17335=LINE ( 'NONE', #48011, #29862 ) ;
#17336=DIRECTION ( 'NONE',  ( -3.469446951953613696E-16, 0.000000000000000000, -1.000000000000000000 ) ) ;
#17338=VERTEX_POINT ( 'NONE', #20920 ) ;
#17340=ORIENTED_EDGE ( 'NONE', *, *, #25389, .F. ) ;
#17342=VERTEX_POINT ( 'NONE', #9045 ) ;
#17343=DIRECTION ( 'NONE',  ( 1.000000000000000000, 0.000000000000000000, 0.000000000000000000 ) ) ;
#17344=CARTESIAN_POINT ( 'NONE',  ( -0.2727639067037607723, 0.000000000000000000, -0.1574803149606301411 ) ) ;
#17345=ORIENTED_EDGE ( 'NONE', *, *, #8749, .T. ) ;
#17346=ORIENTED_EDGE ( 'NONE', *, *, #42275, .F. ) ;
#17347=EDGE_LOOP ( 'NONE', ( #16419, #2076, #33497, #38526 ) ) ;
#17348=DIRECTION ( 'NONE',  ( -0.000000000000000000, 1.000000000000000000, -0.000000000000000000 ) ) ;
#17349=ORIENTED_EDGE ( 'NONE', *, *, #37730, .T. ) ;
#17351=FACE_OUTER_BOUND ( 'NONE', #11865, .T. ) ;
#17356=ORIENTED_EDGE ( 'NONE', *, *, #16892, .F. ) ;
#17357=EDGE_CURVE ( 'NONE', #20926, #20810, #787, .T. ) ;
#17358=AXIS2_PLACEMENT_3D ( 'NONE', #6586, #45531, #50145 ) ;
#17360=DIRECTION ( 'NONE',  ( 1.734723475976806848E-16, -0.000000000000000000, 1.000000000000000000 ) ) ;
#17361=DIRECTION ( 'NONE',  ( -3.469446951953613696E-16, 0.000000000000000000, -1.000000000000000000 ) ) ;
#17363=EDGE_CURVE ( 'NONE', #45537, #12259, #9302, .T. ) ;
#17365=DIRECTION ( 'NONE',  ( -3.469446951953613696E-16, 0.000000000000000000, -1.000000000000000000 ) ) ;
#17366=EDGE_CURVE ( 'NONE', #3716, #49734, #43629, .T. ) ;
#17367=CARTESIAN_POINT ( 'NONE',  ( 0.000000000000000000, 3.267716535433071279, -0.1968503937007879123 ) ) ;
#17368=ORIENTED_EDGE ( 'NONE', *, *, #22933, .F. ) ;
#17369=ORIENTED_EDGE ( 'NONE', *, *, #34875, .F. ) ;
#17371=DIRECTION ( 'NONE',  ( 0.000000000000000000, -1.000000000000000000, 0.000000000000000000 ) ) ;
#17373=VERTEX_POINT ( 'NONE', #20402 ) ;
#17374=ORIENTED_EDGE ( 'NONE', *, *, #44666, .T. ) ;
#17375=CARTESIAN_POINT ( 'NONE',  ( -1.486187880958816931, 3.346456692913386100, 1.574803149606291530 ) ) ;
#17378=DIRECTION ( 'NONE',  ( -1.000000000000000000, -0.000000000000000000, -0.000000000000000000 ) ) ;
#17379=DIRECTION ( 'NONE',  ( 1.734723475976806848E-16, 0.000000000000000000, 1.000000000000000000 ) ) ;
#17380=CARTESIAN_POINT ( 'NONE',  ( -2.160501893660597084, 3.267716535433071279, -1.141732283464563791 ) ) ;
#17382=ORIENTED_EDGE ( 'NONE', *, *, #3043, .F. ) ;
#17385=VECTOR ( 'NONE', #26830, 39.37007874015748143 ) ;
#17386=EDGE_LOOP ( 'NONE', ( #40906, #1433, #15767, #43734 ) ) ;
#17387=CARTESIAN_POINT ( 'NONE',  ( -1.198202975868768005, 3.346456692913386100, 1.732283464566920950 ) ) ;
#17388=VECTOR ( 'NONE', #49981, 39.37007874015748143 ) ;
#17390=DIRECTION ( 'NONE',  ( -1.000000000000000000, 0.000000000000000000, -0.000000000000000000 ) ) ;
#17391=ORIENTED_EDGE ( 'NONE', *, *, #51011, .F. ) ;
#17392=DIRECTION ( 'NONE',  ( -3.469446951953613696E-16, 0.000000000000000000, -1.000000000000000000 ) ) ;
#17395=EDGE_CURVE ( 'NONE', #34717, #22865, #16540, .T. ) ;
#17396=ORIENTED_EDGE ( 'NONE', *, *, #8007, .F. ) ;
#17401=DIRECTION ( 'NONE',  ( 1.734723475976806848E-16, -0.000000000000000000, 1.000000000000000000 ) ) ;
#17402=EDGE_CURVE ( 'NONE', #41605, #10030, #17060, .T. ) ;
#17403=CARTESIAN_POINT ( 'NONE',  ( 0.000000000000000000, 3.267716535433071279, 0.000000000000000000 ) ) ;
#17404=LINE ( 'NONE', #33167, #12314 ) ;
#17406=CARTESIAN_POINT ( 'NONE',  ( -0.5455278134075214336, 3.346456692913386100, -2.034427629037601104 ) ) ;
#17410=CARTESIAN_POINT ( 'NONE',  ( 1.091055626815042645, 3.267716535433071279, -1.892679809432644882E-16 ) ) ;
#17412=CARTESIAN_POINT ( 'NONE',  ( -1.091055626815042645, 0.000000000000000000, 1.889763779527550147 ) ) ;
#17413=LINE ( 'NONE', #49619, #40099 ) ;
#17415=LINE ( 'NONE', #14750, #36379 ) ;
#17416=VERTEX_POINT ( 'NONE', #32817 ) ;
#17418=EDGE_CURVE ( 'NONE', #46251, #37360, #48501, .T. ) ;
#17419=DIRECTION ( 'NONE',  ( 1.000000000000000000, 0.000000000000000000, -3.469446951953613696E-16 ) ) ;
#17421=CARTESIAN_POINT ( 'NONE',  ( 4.268512490100411402E-16, 0.000000000000000000, 1.574803149606291974 ) ) ;
#17422=ORIENTED_EDGE ( 'NONE', *, *, #12150, .T. ) ;
#17423=CARTESIAN_POINT ( 'NONE',  ( 1.091055626815043311, 3.346456692913386100, 1.889763779527550369 ) ) ;
#17424=FACE_BOUND ( 'NONE', #7589, .T. ) ;
#17425=ORIENTED_EDGE ( 'NONE', *, *, #12667, .F. ) ;
#17426=EDGE_CURVE ( 'NONE', #25538, #4899, #8275, .T. ) ;
#17428=VERTEX_POINT ( 'NONE', #24020 ) ;
#17429=ORIENTED_EDGE ( 'NONE', *, *, #27252, .F. ) ;
#17430=CIRCLE ( 'NONE', #19863, 2.106299212598425008 ) ;
#17431=DIRECTION ( 'NONE',  ( 0.000000000000000000, 1.000000000000000000, 0.000000000000000000 ) ) ;
#17433=AXIS2_PLACEMENT_3D ( 'NONE', #9991, #6375, #13869 ) ;
#17435=CARTESIAN_POINT ( 'NONE',  ( 1.015142113812069979, 3.267716535433071279, 1.912654141836395372 ) ) ;
#17436=CARTESIAN_POINT ( 'NONE',  ( 1.287906020515830141, 0.000000000000000000, -0.3149606299212596716 ) ) ;
#17437=ORIENTED_EDGE ( 'NONE', *, *, #18207, .T. ) ;
#17439=DIRECTION ( 'NONE',  ( 1.000000000000000000, 0.000000000000000000, 0.000000000000000000 ) ) ;
#17440=EDGE_CURVE ( 'NONE', #12193, #22497, #47387, .T. ) ;
#17441=CARTESIAN_POINT ( 'NONE',  ( 1.909347346926324684, 0.000000000000000000, 0.5905511811023582691 ) ) ;
#17442=PLANE ( 'NONE',  #26707 ) ;
#17446=DIRECTION ( 'NONE',  ( -0.000000000000000000, 1.000000000000000000, -0.000000000000000000 ) ) ;
#17447=VERTEX_POINT ( 'NONE', #15673 ) ;
#17451=LINE ( 'NONE', #13588, #1772 ) ;
#17453=VERTEX_POINT ( 'NONE', #35051 ) ;
#17454=CARTESIAN_POINT ( 'NONE',  ( -0.8182917201112819283, 0.000000000000000000, 1.850393700787391849 ) ) ;
#17455=CARTESIAN_POINT ( 'NONE',  ( -0.6214413264104945434, 0.000000000000000000, -0.6692913385826760875 ) ) ;
#17456=DIRECTION ( 'NONE',  ( -1.000000000000000000, 0.000000000000000000, 0.000000000000000000 ) ) ;
#17457=EDGE_CURVE ( 'NONE', #3179, #7335, #3294, .T. ) ;
#17458=ORIENTED_EDGE ( 'NONE', *, *, #49140, .F. ) ;
#17459=PLANE ( 'NONE',  #32112 ) ;
#17460=EDGE_LOOP ( 'NONE', ( #12684, #46220, #12594, #50697 ) ) ;
#17461=FACE_BOUND ( 'NONE', #25950, .T. ) ;
#17464=AXIS2_PLACEMENT_3D ( 'NONE', #19964, #27461, #39346 ) ;
#17465=VECTOR ( 'NONE', #27753, 39.37007874015748143 ) ;
#17466=DIRECTION ( 'NONE',  ( 0.000000000000000000, 0.000000000000000000, -1.000000000000000000 ) ) ;
#17467=CARTESIAN_POINT ( 'NONE',  ( -1.091055626815042645, 3.346456692913386100, 1.889763779527550147 ) ) ;
#17469=EDGE_CURVE ( 'NONE', #50140, #35927, #39684, .T. ) ;
#17472=ORIENTED_EDGE ( 'NONE', *, *, #48467, .F. ) ;
#17473=LINE ( 'NONE', #13604, #42758 ) ;
#17474=EDGE_LOOP ( 'NONE', ( #20238, #48538, #11711, #5563 ) ) ;
#17475=VECTOR ( 'NONE', #22186, 39.37007874015748143 ) ;
#17477=ORIENTED_EDGE ( 'NONE', *, *, #556, .F. ) ;
#17478=CARTESIAN_POINT ( 'NONE',  ( -1.712496953225537633, 3.346456692913386100, -1.102362204724405492 ) ) ;
#17480=EDGE_CURVE ( 'NONE', #9409, #35448, #47128, .T. ) ;
#17481=ORIENTED_EDGE ( 'NONE', *, *, #29987, .T. ) ;
#17482=CARTESIAN_POINT ( 'NONE',  ( -0.2727639067037602172, 3.346456692913386100, 1.732283464566921172 ) ) ;
#17483=CARTESIAN_POINT ( 'NONE',  ( 0.8182917201112819283, 3.346456692913386100, 0.1574803149606286423 ) ) ;
#17484=ORIENTED_EDGE ( 'NONE', *, *, #19814, .F. ) ;
#17485=ADVANCED_FACE ( 'NONE', ( #31178 ), #11798, .F. ) ;
#17486=CARTESIAN_POINT ( 'NONE',  ( -2.417802884545332542, 3.267716535433071279, -0.3543307086614173040 ) ) ;
#17487=ORIENTED_EDGE ( 'NONE', *, *, #5455, .T. ) ;
#17489=EDGE_CURVE ( 'NONE', #25903, #14916, #38676, .T. ) ;
#17491=ORIENTED_EDGE ( 'NONE', *, *, #13715, .T. ) ;
#17493=VERTEX_POINT ( 'NONE', #23165 ) ;
#17494=DIRECTION ( 'NONE',  ( -0.000000000000000000, 1.000000000000000000, -0.000000000000000000 ) ) ;
#17495=EDGE_CURVE ( 'NONE', #27834, #3496, #2077, .T. ) ;
#17499=DIRECTION ( 'NONE',  ( -3.469446951953613696E-16, 0.000000000000000000, -1.000000000000000000 ) ) ;
#17501=VECTOR ( 'NONE', #37170, 39.37007874015748143 ) ;
#17502=DIRECTION ( 'NONE',  ( -1.000000000000000000, -0.000000000000000000, -0.000000000000000000 ) ) ;
#17505=CARTESIAN_POINT ( 'NONE',  ( 1.363819533518803695, 3.346456692913386100, 1.535433070866133898 ) ) ;
#17507=EDGE_CURVE ( 'NONE', #13815, #29456, #38921, .T. ) ;
#17508=CIRCLE ( 'NONE', #38125, 2.106299212598425008 ) ;
#17509=LINE ( 'NONE', #28865, #4564 ) ;
#17510=EDGE_CURVE ( 'NONE', #48815, #26618, #7929, .T. ) ;
#17512=VECTOR ( 'NONE', #44308, 39.37007874015748143 ) ;
#17514=ORIENTED_EDGE ( 'NONE', *, *, #35535, .F. ) ;
#17519=ORIENTED_EDGE ( 'NONE', *, *, #35514, .T. ) ;
#17520=LINE ( 'NONE', #48713, #40472 ) ;
#17521=ADVANCED_FACE ( 'NONE', ( #27541 ), #19284, .F. ) ;
#17522=DIRECTION ( 'NONE',  ( -1.000000000000000000, 0.000000000000000000, 1.734723475976806848E-16 ) ) ;
#17523=DIRECTION ( 'NONE',  ( -1.000000000000000000, 0.000000000000000000, 0.000000000000000000 ) ) ;
#17525=CARTESIAN_POINT ( 'NONE',  ( 1.091055626815042867, 3.267716535433071279, -1.892679809432645129E-16 ) ) ;
#17527=ADVANCED_FACE ( 'NONE', ( #35306 ), #16194, .F. ) ;
#17528=DIRECTION ( 'NONE',  ( -0.000000000000000000, 1.000000000000000000, -0.000000000000000000 ) ) ;
#17531=VERTEX_POINT ( 'NONE', #23935 ) ;
#17532=LINE ( 'NONE', #12899, #41943 ) ;
#17534=CARTESIAN_POINT ( 'NONE',  ( 0.000000000000000000, 3.346456692913386100, 0.000000000000000000 ) ) ;
#17535=CARTESIAN_POINT ( 'NONE',  ( -0.8182917201112819283, 0.000000000000000000, -0.4724409448818886470 ) ) ;
#17536=CIRCLE ( 'NONE', #32359, 2.165354330708661568 ) ;
#17538=VECTOR ( 'NONE', #4847, 39.37007874015748143 ) ;
#17539=CARTESIAN_POINT ( 'NONE',  ( -0.5455278134075214336, 0.000000000000000000, -1.889763779527552146 ) ) ;
#17541=EDGE_LOOP ( 'NONE', ( #14884, #40062, #40803, #32483 ) ) ;
#17544=CARTESIAN_POINT ( 'NONE',  ( -0.07591351300297340121, 0.000000000000000000, -1.929133858267710000 ) ) ;
#17545=FACE_BOUND ( 'NONE', #16482, .T. ) ;
#17549=CARTESIAN_POINT ( 'NONE',  ( -0.5455278134075214336, 3.346456692913386100, 0.3149606299212577287 ) ) ;
#17550=DIRECTION ( 'NONE',  ( 1.734723475976806848E-16, 0.000000000000000000, 1.000000000000000000 ) ) ;
#17552=ORIENTED_EDGE ( 'NONE', *, *, #7895, .F. ) ;
#17554=LINE ( 'NONE', #37950, #24125 ) ;
#17555=FACE_OUTER_BOUND ( 'NONE', #10948, .T. ) ;
#17556=ORIENTED_EDGE ( 'NONE', *, *, #34204, .T. ) ;
#17559=VERTEX_POINT ( 'NONE', #50985 ) ;
#17560=LINE ( 'NONE', #25303, #18608 ) ;
#17563=EDGE_CURVE ( 'NONE', #42223, #32548, #15170, .T. ) ;
#17565=PLANE ( 'NONE',  #18165 ) ;
#17568=ORIENTED_EDGE ( 'NONE', *, *, #27968, .T. ) ;
#17569=DIRECTION ( 'NONE',  ( 1.000000000000000000, -0.000000000000000000, 0.000000000000000000 ) ) ;
#17570=CARTESIAN_POINT ( 'NONE',  ( -1.166969139818015533, 0.000000000000000000, 0.4724409448818871482 ) ) ;
#17571=CARTESIAN_POINT ( 'NONE',  ( -0.2727639067037607723, 0.000000000000000000, -1.732283464566922726 ) ) ;
#17572=EDGE_CURVE ( 'NONE', #45000, #45220, #9212, .T. ) ;
#17573=DIRECTION ( 'NONE',  ( -3.469446951953613696E-16, 0.000000000000000000, -1.000000000000000000 ) ) ;
#17574=CARTESIAN_POINT ( 'NONE',  ( 1.015142113812069091, 3.226129038349118794, -2.244094488188969283 ) ) ;
#17575=LINE ( 'NONE', #33340, #43278 ) ;
#17577=VECTOR ( 'NONE', #12787, 39.37007874015748143 ) ;
#17578=ORIENTED_EDGE ( 'NONE', *, *, #47002, .T. ) ;
#17579=DIRECTION ( 'NONE',  ( -1.000000000000000000, -0.000000000000000000, -0.000000000000000000 ) ) ;
#17580=CARTESIAN_POINT ( 'NONE',  ( 1.636583440222563857, 3.346456692913386100, -1.161035397307311917E-15 ) ) ;
#17581=ORIENTED_EDGE ( 'NONE', *, *, #25489, .T. ) ;
#17583=VERTEX_POINT ( 'NONE', #1209 ) ;
#17584=EDGE_CURVE ( 'NONE', #606, #30894, #24455, .T. ) ;
#17585=VECTOR ( 'NONE', #15717, 39.37007874015748143 ) ;
#17586=DIRECTION ( 'NONE',  ( -1.000000000000000000, 0.000000000000000000, -0.000000000000000000 ) ) ;
#17589=EDGE_CURVE ( 'NONE', #21352, #34259, #33233, .T. ) ;
#17590=EDGE_CURVE ( 'NONE', #47487, #19912, #48157, .T. ) ;
#17591=VERTEX_POINT ( 'NONE', #16713 ) ;
#17593=ORIENTED_EDGE ( 'NONE', *, *, #2591, .F. ) ;
#17594=DIRECTION ( 'NONE',  ( 1.734723475976806848E-16, -0.000000000000000000, 1.000000000000000000 ) ) ;
#17595=CARTESIAN_POINT ( 'NONE',  ( -1.636583440222563857, 3.267716535433071279, 2.839019714148966584E-16 ) ) ;
#17597=VERTEX_POINT ( 'NONE', #43795 ) ;
#17599=LINE ( 'NONE', #8832, #17241 ) ;
#17600=ORIENTED_EDGE ( 'NONE', *, *, #2821, .T. ) ;
#17601=ORIENTED_EDGE ( 'NONE', *, *, #32856, .T. ) ;
#17602=CARTESIAN_POINT ( 'NONE',  ( 0.000000000000000000, 3.267716535433071279, -1.771653543307081025 ) ) ;
#17604=CARTESIAN_POINT ( 'NONE',  ( 0.000000000000000000, 3.267716535433071279, 1.220472440944875281 ) ) ;
#17605=VERTEX_POINT ( 'NONE', #24960 ) ;
#17606=CARTESIAN_POINT ( 'NONE',  ( 0.7423782071083092626, 3.346456692913386100, 2.204724409448808764 ) ) ;
#17607=CARTESIAN_POINT ( 'NONE',  ( -1.985260859929297572, 3.267716535433071279, -6.146657985744592735E-16 ) ) ;
#17608=CARTESIAN_POINT ( 'NONE',  ( 0.8182917201112824834, 3.346456692913386100, 1.417322834645662777 ) ) ;
#17610=DIRECTION ( 'NONE',  ( 1.000000000000000000, -0.000000000000000000, 0.000000000000000000 ) ) ;
#17611=AXIS2_PLACEMENT_3D ( 'NONE', #14755, #30502, #10873 ) ;
#17612=CARTESIAN_POINT ( 'NONE',  ( 1.091055626815043311, 0.000000000000000000, 1.889763779527550369 ) ) ;
#17613=PLANE ( 'NONE',  #8474 ) ;
#17615=VECTOR ( 'NONE', #41970, 39.37007874015748143 ) ;
#17616=VERTEX_POINT ( 'NONE', #17220 ) ;
#17618=VECTOR ( 'NONE', #4603, 39.37007874015748143 ) ;
#17619=VECTOR ( 'NONE', #9763, 39.37007874015748143 ) ;
#17620=CARTESIAN_POINT ( 'NONE',  ( 1.091055626815042645, 3.346456692913386100, -0.3149606299212596716 ) ) ;
#17621=EDGE_CURVE ( 'NONE', #50730, #19682, #40973, .T. ) ;
#17622=EDGE_CURVE ( 'NONE', #21285, #25659, #40463, .T. ) ;
#17623=LINE ( 'NONE', #36484, #47531 ) ;
#17624=CARTESIAN_POINT ( 'NONE',  ( 1.091055626815042423, 3.346456692913386100, -1.574803149606294417 ) ) ;
#17625=ORIENTED_EDGE ( 'NONE', *, *, #47329, .F. ) ;
#17627=EDGE_CURVE ( 'NONE', #10406, #27808, #8700, .T. ) ;
#17630=ORIENTED_EDGE ( 'NONE', *, *, #7047, .F. ) ;
#17631=CARTESIAN_POINT ( 'NONE',  ( -1.363819533518803473, 3.346456692913386100, -0.1574803149606300023 ) ) ;
#17633=DIRECTION ( 'NONE',  ( -0.000000000000000000, 1.000000000000000000, -0.000000000000000000 ) ) ;
#17634=CARTESIAN_POINT ( 'NONE',  ( 1.761123562704336232, 3.346456692913386100, -1.259842519685035800 ) ) ;
#17635=DIRECTION ( 'NONE',  ( 0.000000000000000000, 0.000000000000000000, -1.000000000000000000 ) ) ;
#17636=VERTEX_POINT ( 'NONE', #8448 ) ;
#17637=LINE ( 'NONE', #41642, #42341 ) ;
#17638=LINE ( 'NONE', #2404, #21079 ) ;
#17641=VERTEX_POINT ( 'NONE', #24713 ) ;
#17644=CARTESIAN_POINT ( 'NONE',  ( -1.166969139818016199, 3.346456692913386100, -1.614173228346451605 ) ) ;
#17645=LINE ( 'NONE', #3666, #12284 ) ;
#17646=ORIENTED_EDGE ( 'NONE', *, *, #9407, .F. ) ;
#17647=PLANE ( 'NONE',  #5227 ) ;
#17649=CARTESIAN_POINT ( 'NONE',  ( 1.761123562704338452, 3.346456692913386100, 1.259842519685033135 ) ) ;
#17651=VECTOR ( 'NONE', #10075, 39.37007874015748143 ) ;
#17652=EDGE_CURVE ( 'NONE', #5216, #6745, #20223, .T. ) ;
#17653=VERTEX_POINT ( 'NONE', #4575 ) ;
#17657=ORIENTED_EDGE ( 'NONE', *, *, #37818, .F. ) ;
#17658=LINE ( 'NONE', #47832, #10531 ) ;
#17659=CIRCLE ( 'NONE', #21787, 2.165354330708661568 ) ;
#17660=AXIS2_PLACEMENT_3D ( 'NONE', #20672, #29187, #36434 ) ;
#17661=PLANE ( 'NONE',  #44904 ) ;
#17662=FACE_OUTER_BOUND ( 'NONE', #42171, .T. ) ;
#17665=ORIENTED_EDGE ( 'NONE', *, *, #7847, .T. ) ;
#17666=VERTEX_POINT ( 'NONE', #1716 ) ;
#17669=DIRECTION ( 'NONE',  ( 1.000000000000000000, 0.000000000000000000, -3.469446951953613696E-16 ) ) ;
#17670=ORIENTED_EDGE ( 'NONE', *, *, #21027, .T. ) ;
#17671=DIRECTION ( 'NONE',  ( 1.000000000000000000, 0.000000000000000000, 0.000000000000000000 ) ) ;
#17672=LINE ( 'NONE', #6307, #25983 ) ;
#17673=DIRECTION ( 'NONE',  ( -0.000000000000000000, 1.000000000000000000, -0.000000000000000000 ) ) ;
#17676=CARTESIAN_POINT ( 'NONE',  ( -1.363819533518803473, 3.346456692913386100, -0.7874015748031470974 ) ) ;
#17677=CARTESIAN_POINT ( 'NONE',  ( -1.166969139818016199, 0.000000000000000000, -0.6692913385826760875 ) ) ;
#17678=DIRECTION ( 'NONE',  ( -0.000000000000000000, 1.000000000000000000, -0.000000000000000000 ) ) ;
#17680=CARTESIAN_POINT ( 'NONE',  ( -1.091055626815042201, 3.346456692913386100, 1.377952755905504256 ) ) ;
#17681=DIRECTION ( 'NONE',  ( -1.000000000000000000, 0.000000000000000000, 1.734723475976806848E-16 ) ) ;
#17682=ORIENTED_EDGE ( 'NONE', *, *, #46072, .F. ) ;
#17683=CARTESIAN_POINT ( 'NONE',  ( 1.363819533518803251, 0.000000000000000000, -0.7874015748031473194 ) ) ;
#17684=VERTEX_POINT ( 'NONE', #16969 ) ;
#17686=LINE ( 'NONE', #33453, #3156 ) ;
#17687=CARTESIAN_POINT ( 'NONE',  ( 1.560669927219590303, 3.267716535433071279, -1.501022570047217508 ) ) ;
#17688=EDGE_LOOP ( 'NONE', ( #43012, #45194, #31496, #11669 ) ) ;
#17690=DIRECTION ( 'NONE',  ( -1.000000000000000000, 0.000000000000000000, -0.000000000000000000 ) ) ;
#17692=VECTOR ( 'NONE', #12216, 39.37007874015748143 ) ;
#17693=EDGE_CURVE ( 'NONE', #18779, #49170, #28827, .T. ) ;
#17694=VECTOR ( 'NONE', #608, 39.37007874015748143 ) ;
#17695=EDGE_CURVE ( 'NONE', #40865, #24856, #44816, .T. ) ;
#17696=VECTOR ( 'NONE', #23411, 39.37007874015748143 ) ;
#17697=CARTESIAN_POINT ( 'NONE',  ( -1.536664496436148184E-16, 0.000000000000000000, 0.4330708661417287386 ) ) ;
#17698=EDGE_CURVE ( 'NONE', #41767, #19583, #701, .T. ) ;
#17699=CARTESIAN_POINT ( 'NONE',  ( -1.909347346926324462, 3.346456692913386100, -0.1574803149606297248 ) ) ;
#17701=CIRCLE ( 'NONE', #35016, 2.165354330708661568 ) ;
#17703=PLANE ( 'NONE',  #3893 ) ;
#17704=DIRECTION ( 'NONE',  ( -3.469446951953613696E-16, 0.000000000000000000, -1.000000000000000000 ) ) ;
#17706=EDGE_LOOP ( 'NONE', ( #40966, #979, #30375, #44671 ) ) ;
#17709=EDGE_LOOP ( 'NONE', ( #35840, #47136, #36664, #20364 ) ) ;
#17710=LINE ( 'NONE', #16953, #21573 ) ;
#17711=EDGE_CURVE ( 'NONE', #50549, #11356, #47897, .T. ) ;
#17712=CARTESIAN_POINT ( 'NONE',  ( -0.3486774197067339376, 3.346456692913386100, -1.574803149606293529 ) ) ;
#17713=VERTEX_POINT ( 'NONE', #49926 ) ;
#17714=LINE ( 'NONE', #10474, #25470 ) ;
#17715=CARTESIAN_POINT ( 'NONE',  ( 0.5455278134075208785, 3.346456692913386100, -1.574803149606293529 ) ) ;
#17717=ORIENTED_EDGE ( 'NONE', *, *, #6892, .F. ) ;
#17718=DIRECTION ( 'NONE',  ( 1.000000000000000000, 0.000000000000000000, 0.000000000000000000 ) ) ;
#17719=ORIENTED_EDGE ( 'NONE', *, *, #47823, .T. ) ;
#17720=FACE_BOUND ( 'NONE', #9581, .T. ) ;
#17723=CARTESIAN_POINT ( 'NONE',  ( 1.287906020515830585, 3.346456692913386100, 1.740706023381843659 ) ) ;
#17725=ORIENTED_EDGE ( 'NONE', *, *, #49867, .T. ) ;
#17726=EDGE_LOOP ( 'NONE', ( #31883, #31739, #22790, #1194 ) ) ;
#17729=ORIENTED_EDGE ( 'NONE', *, *, #6485, .F. ) ;
#17731=DIRECTION ( 'NONE',  ( 0.000000000000000000, 0.000000000000000000, 1.000000000000000000 ) ) ;
#17732=ORIENTED_EDGE ( 'NONE', *, *, #49031, .T. ) ;
#17733=VECTOR ( 'NONE', #16646, 39.37007874015748143 ) ;
#17734=LINE ( 'NONE', #18994, #41326 ) ;
#17735=ORIENTED_EDGE ( 'NONE', *, *, #47037, .F. ) ;
#17736=LINE ( 'NONE', #9483, #10944 ) ;
#17737=CARTESIAN_POINT ( 'NONE',  ( 1.636583440222563635, 3.346456692913386100, -1.259842519685035800 ) ) ;
#17739=ORIENTED_EDGE ( 'NONE', *, *, #5455, .F. ) ;
#17741=VERTEX_POINT ( 'NONE', #18486 ) ;
#17745=CARTESIAN_POINT ( 'NONE',  ( -1.091055626815042201, 3.346456692913386100, 0.3149606299212580063 ) ) ;
#17746=EDGE_CURVE ( 'NONE', #31458, #37657, #10230, .T. ) ;
#17747=ADVANCED_FACE ( 'NONE', ( #26472 ), #9726, .F. ) ;
#17748=ORIENTED_EDGE ( 'NONE', *, *, #37396, .F. ) ;
#17750=PLANE ( 'NONE',  #13713 ) ;
#17751=EDGE_CURVE ( 'NONE', #12958, #27093, #2735, .T. ) ;
#17752=EDGE_CURVE ( 'NONE', #18200, #36096, #41980, .T. ) ;
#17753=CARTESIAN_POINT ( 'NONE',  ( -1.091055626815042201, 3.267716535433071279, 1.259842519685033357 ) ) ;
#17757=VECTOR ( 'NONE', #4361, 39.37007874015748143 ) ;
#17758=ORIENTED_EDGE ( 'NONE', *, *, #24167, .T. ) ;
#17759=LINE ( 'NONE', #17505, #43097 ) ;
#17760=DIRECTION ( 'NONE',  ( 1.000000000000000000, -0.000000000000000000, 0.000000000000000000 ) ) ;
#17761=DIRECTION ( 'NONE',  ( 1.000000000000000000, 0.000000000000000000, 0.000000000000000000 ) ) ;
#17762=VECTOR ( 'NONE', #15300, 39.37007874015748143 ) ;
#17767=LINE ( 'NONE', #25763, #16206 ) ;
#17769=CARTESIAN_POINT ( 'NONE',  ( 0.4696143004045478797, 3.267716535433071279, -1.614173228346451605 ) ) ;
#17773=DIRECTION ( 'NONE',  ( -0.000000000000000000, 1.000000000000000000, -0.000000000000000000 ) ) ;
#17774=EDGE_CURVE ( 'NONE', #49369, #11755, #48913, .T. ) ;
#17775=EDGE_LOOP ( 'NONE', ( #9274, #3668, #5963, #43502 ) ) ;
#17776=DIRECTION ( 'NONE',  ( -0.000000000000000000, 1.000000000000000000, -0.000000000000000000 ) ) ;
#17779=DIRECTION ( 'NONE',  ( -0.000000000000000000, 1.000000000000000000, -0.000000000000000000 ) ) ;
#17780=DIRECTION ( 'NONE',  ( -0.000000000000000000, 0.000000000000000000, 1.000000000000000000 ) ) ;
#17781=VERTEX_POINT ( 'NONE', #22361 ) ;
#17782=EDGE_CURVE ( 'NONE', #28960, #18289, #6364, .T. ) ;
#17783=CARTESIAN_POINT ( 'NONE',  ( 0.000000000000000000, 3.267716535433071279, -2.244094488188968395 ) ) ;
#17784=ORIENTED_EDGE ( 'NONE', *, *, #47553, .T. ) ;
#17786=ORIENTED_EDGE ( 'NONE', *, *, #17698, .T. ) ;
#17788=DIRECTION ( 'NONE',  ( 1.000000000000000000, 0.000000000000000000, 0.000000000000000000 ) ) ;
#17789=EDGE_CURVE ( 'NONE', #13301, #31303, #14357, .T. ) ;
#17795=ORIENTED_EDGE ( 'NONE', *, *, #44380, .T. ) ;
#17798=LINE ( 'NONE', #40531, #43804 ) ;
#17799=FACE_BOUND ( 'NONE', #37113, .T. ) ;
#17800=ORIENTED_EDGE ( 'NONE', *, *, #3252, .T. ) ;
#17801=AXIS2_PLACEMENT_3D ( 'NONE', #32409, #48355, #24395 ) ;
#17803=CARTESIAN_POINT ( 'NONE',  ( 0.000000000000000000, 3.267716535433071279, -1.456692913385823296 ) ) ;
#17804=VECTOR ( 'NONE', #2629, 39.37007874015748143 ) ;
#17806=ORIENTED_EDGE ( 'NONE', *, *, #49711, .F. ) ;
#17808=VECTOR ( 'NONE', #7188, 39.37007874015748143 ) ;
#17809=DIRECTION ( 'NONE',  ( 0.000000000000000000, 0.000000000000000000, 1.000000000000000000 ) ) ;
#17810=VERTEX_POINT ( 'NONE', #14102 ) ;
#17811=EDGE_LOOP ( 'NONE', ( #11204, #41531, #5421, #40415 ) ) ;
#17812=VERTEX_POINT ( 'NONE', #6099 ) ;
#17814=EDGE_CURVE ( 'NONE', #49632, #23850, #6617, .T. ) ;
#17815=DIRECTION ( 'NONE',  ( -0.000000000000000000, 0.000000000000000000, 1.000000000000000000 ) ) ;
#17816=EDGE_CURVE ( 'NONE', #14372, #23850, #10487, .T. ) ;
#17817=DIRECTION ( 'NONE',  ( -1.000000000000000000, -0.000000000000000000, -0.000000000000000000 ) ) ;
#17818=EDGE_CURVE ( 'NONE', #18090, #6701, #45822, .T. ) ;
#17819=LINE ( 'NONE', #3845, #41246 ) ;
#17820=ORIENTED_EDGE ( 'NONE', *, *, #14346, .F. ) ;
#17823=FACE_OUTER_BOUND ( 'NONE', #8528, .T. ) ;
#17824=CARTESIAN_POINT ( 'NONE',  ( 0.000000000000000000, 3.267716535433071279, -1.456692913385822630 ) ) ;
#17825=LINE ( 'NONE', #2081, #42445 ) ;
#17826=CARTESIAN_POINT ( 'NONE',  ( 0.000000000000000000, 3.267716535433071279, 0.000000000000000000 ) ) ;
#17827=CARTESIAN_POINT ( 'NONE',  ( 2.372989701366758020, 3.242957824277338030, 0.6299212598425161236 ) ) ;
#17828=CIRCLE ( 'NONE', #46647, 2.874015748031496731 ) ;
#17829=CARTESIAN_POINT ( 'NONE',  ( -0.8182917201112819283, 3.346456692913386100, -1.102362204724405492 ) ) ;
#17830=ORIENTED_EDGE ( 'NONE', *, *, #15675, .F. ) ;
#17833=DIRECTION ( 'NONE',  ( 1.000000000000000000, 0.000000000000000000, 0.000000000000000000 ) ) ;
#17834=VECTOR ( 'NONE', #26505, 39.37007874015748143 ) ;
#17835=ORIENTED_EDGE ( 'NONE', *, *, #10826, .F. ) ;
#17836=VECTOR ( 'NONE', #35189, 39.37007874015748143 ) ;
#17837=VERTEX_POINT ( 'NONE', #41728 ) ;
#17838=CARTESIAN_POINT ( 'NONE',  ( 0.9671406142315196464, 3.267716535433070391, -2.244094488188969283 ) ) ;
#17839=VECTOR ( 'NONE', #8924, 39.37007874015748143 ) ;
#17840=VERTEX_POINT ( 'NONE', #18739 ) ;
#17841=EDGE_CURVE ( 'NONE', #6632, #37350, #13600, .T. ) ;
#17844=ORIENTED_EDGE ( 'NONE', *, *, #42017, .F. ) ;
#17845=PLANE ( 'NONE',  #3977 ) ;
#17849=CARTESIAN_POINT ( 'NONE',  ( 0.000000000000000000, 3.267716535433071279, -1.456692913385822186 ) ) ;
#17850=ADVANCED_FACE ( 'NONE', ( #41225 ), #13852, .F. ) ;
#17852=ORIENTED_EDGE ( 'NONE', *, *, #29005, .F. ) ;
#17856=ADVANCED_FACE ( 'NONE', ( #17974 ), #22109, .F. ) ;
#17857=CARTESIAN_POINT ( 'NONE',  ( -2.443311489867025621, 3.267716535433071279, -0.03937007874015881204 ) ) ;
#17858=CARTESIAN_POINT ( 'NONE',  ( -1.091055626815042201, 0.000000000000000000, 0.6299212598425164567 ) ) ;
#17859=CARTESIAN_POINT ( 'NONE',  ( -0.8182917201112819283, 3.267716535433071279, -2.244094488188968395 ) ) ;
#17861=ORIENTED_EDGE ( 'NONE', *, *, #47739, .F. ) ;
#17862=LINE ( 'NONE', #37241, #23833 ) ;
#17864=DIRECTION ( 'NONE',  ( -0.000000000000000000, 1.000000000000000000, -0.000000000000000000 ) ) ;
#17867=DIRECTION ( 'NONE',  ( 0.000000000000000000, 0.000000000000000000, -1.000000000000000000 ) ) ;
#17868=DIRECTION ( 'NONE',  ( -0.000000000000000000, 1.000000000000000000, -0.000000000000000000 ) ) ;
#17869=AXIS2_PLACEMENT_3D ( 'NONE', #38958, #19324, #43066 ) ;
#17870=VECTOR ( 'NONE', #49398, 39.37007874015748143 ) ;
#17871=CARTESIAN_POINT ( 'NONE',  ( 0.000000000000000000, 3.267716535433071279, 1.535433070866133898 ) ) ;
#17873=ORIENTED_EDGE ( 'NONE', *, *, #26502, .F. ) ;
#17875=EDGE_CURVE ( 'NONE', #4281, #44874, #27481, .T. ) ;
#17876=CARTESIAN_POINT ( 'NONE',  ( -0.8182917201112819283, 3.346456692913386100, -0.7874015748031467643 ) ) ;
#17878=CARTESIAN_POINT ( 'NONE',  ( -1.091055626815042645, 0.000000000000000000, -0.5118110236220467790 ) ) ;
#17880=EDGE_CURVE ( 'NONE', #16054, #14478, #15861, .T. ) ;
#17882=VERTEX_POINT ( 'NONE', #4002 ) ;
#17883=ORIENTED_EDGE ( 'NONE', *, *, #25382, .F. ) ;
#17888=DIRECTION ( 'NONE',  ( 1.000000000000000000, 0.000000000000000000, -3.469446951953613696E-16 ) ) ;
#17891=LINE ( 'NONE', #40877, #18641 ) ;
#17893=ORIENTED_EDGE ( 'NONE', *, *, #30052, .T. ) ;
#17894=CARTESIAN_POINT ( 'NONE',  ( -2.121605289024800722, 3.267716535433071279, 0.4330708661417290162 ) ) ;
#17896=CARTESIAN_POINT ( 'NONE',  ( 0.4696143004045479352, 0.000000000000000000, -0.7874015748031473194 ) ) ;
#17898=CARTESIAN_POINT ( 'NONE',  ( -0.7053729475263578186, 3.346456692913386100, -2.047244094488181343 ) ) ;
#17899=FACE_OUTER_BOUND ( 'NONE', #41816, .T. ) ;
#17900=PLANE ( 'NONE',  #27922 ) ;
#17901=ORIENTED_EDGE ( 'NONE', *, *, #12189, .T. ) ;
#17903=EDGE_CURVE ( 'NONE', #47182, #12647, #50669, .T. ) ;
#17904=CARTESIAN_POINT ( 'NONE',  ( 0.000000000000000000, 3.267716535433071279, -0.9448818897637765168 ) ) ;
#17905=VECTOR ( 'NONE', #27776, 39.37007874015748143 ) ;
#17906=VERTEX_POINT ( 'NONE', #11998 ) ;
#17911=EDGE_CURVE ( 'NONE', #34814, #19095, #35496, .T. ) ;
#17914=DIRECTION ( 'NONE',  ( -0.000000000000000000, 1.000000000000000000, -0.000000000000000000 ) ) ;
#17915=ADVANCED_FACE ( 'NONE', ( #46573 ), #11244, .F. ) ;
#17916=ADVANCED_FACE ( 'NONE', ( #10987 ), #50923, .F. ) ;
#17917=DIRECTION ( 'NONE',  ( -0.000000000000000000, 1.000000000000000000, -0.000000000000000000 ) ) ;
#17918=ORIENTED_EDGE ( 'NONE', *, *, #24324, .T. ) ;
#17919=ORIENTED_EDGE ( 'NONE', *, *, #33964, .T. ) ;
#17920=CARTESIAN_POINT ( 'NONE',  ( 0.1968503937007878568, 0.000000000000000000, 1.259842519685033357 ) ) ;
#17922=ORIENTED_EDGE ( 'NONE', *, *, #6588, .F. ) ;
#17923=CARTESIAN_POINT ( 'NONE',  ( 0.5455278134075212115, 3.346456692913386100, 0.3149606299212576177 ) ) ;
#17925=LINE ( 'NONE', #18689, #33560 ) ;
#17928=VERTEX_POINT ( 'NONE', #26973 ) ;
#17929=CARTESIAN_POINT ( 'NONE',  ( 0.000000000000000000, 3.267716535433071279, -0.03937007874015881204 ) ) ;
#17930=CARTESIAN_POINT ( 'NONE',  ( -1.195183497228115035E-16, 3.346456692913386100, -0.9448818897637765168 ) ) ;
#17931=LINE ( 'NONE', #36795, #43667 ) ;
#17932=EDGE_CURVE ( 'NONE', #42532, #31299, #39112, .T. ) ;
#17934=LINE ( 'NONE', #10695, #37264 ) ;
#17935=FACE_BOUND ( 'NONE', #24476, .T. ) ;
#17940=EDGE_CURVE ( 'NONE', #33992, #44975, #19481, .T. ) ;
#17941=DIRECTION ( 'NONE',  ( -1.000000000000000000, 0.000000000000000000, -0.000000000000000000 ) ) ;
#17943=VECTOR ( 'NONE', #3699, 39.37007874015748143 ) ;
#17944=VECTOR ( 'NONE', #6222, 39.37007874015748143 ) ;
#17945=VERTEX_POINT ( 'NONE', #31624 ) ;
#17947=EDGE_CURVE ( 'NONE', #48074, #14448, #27228, .T. ) ;
#17948=CARTESIAN_POINT ( 'NONE',  ( -0.2727639067037608278, 3.346456692913386100, -0.3543307086614175816 ) ) ;
#17950=EDGE_CURVE ( 'NONE', #37274, #23861, #38613, .T. ) ;
#17951=DIRECTION ( 'NONE',  ( 0.000000000000000000, 0.000000000000000000, -1.000000000000000000 ) ) ;
#17952=DIRECTION ( 'NONE',  ( -3.469446951953613696E-16, 0.000000000000000000, -1.000000000000000000 ) ) ;
#17953=CARTESIAN_POINT ( 'NONE',  ( -2.182111253630085734, 3.240462944951739033, -1.127888942729357469 ) ) ;
#17956=VERTEX_POINT ( 'NONE', #18985 ) ;
#17958=AXIS2_PLACEMENT_3D ( 'NONE', #22089, #5572, #33968 ) ;
#17959=CARTESIAN_POINT ( 'NONE',  ( 1.091055626815043311, 3.267716535433071279, 1.870389530743258755 ) ) ;
#17960=ORIENTED_EDGE ( 'NONE', *, *, #24940, .T. ) ;
#17963=ORIENTED_EDGE ( 'NONE', *, *, #22650, .T. ) ;
#17964=DIRECTION ( 'NONE',  ( -1.000000000000000000, 0.000000000000000000, 0.000000000000000000 ) ) ;
#17965=DIRECTION ( 'NONE',  ( 1.734723475976806848E-16, -0.000000000000000000, 1.000000000000000000 ) ) ;
#17966=CARTESIAN_POINT ( 'NONE',  ( 0.000000000000000000, 3.267716535433071279, -0.3149606299212592275 ) ) ;
#17971=LINE ( 'NONE', #33739, #30324 ) ;
#17972=CARTESIAN_POINT ( 'NONE',  ( 0.2727639067037604947, 3.267716535433071279, -1.102362204724405714 ) ) ;
#17973=CARTESIAN_POINT ( 'NONE',  ( -0.5455278134075216556, 3.254044873612428557, -2.388497533030866204 ) ) ;
#17974=FACE_OUTER_BOUND ( 'NONE', #24675, .T. ) ;
#17975=EDGE_CURVE ( 'NONE', #32481, #39570, #31372, .T. ) ;
#17976=VECTOR ( 'NONE', #37031, 39.37007874015748143 ) ;
#17977=VECTOR ( 'NONE', #31744, 39.37007874015748143 ) ;
#17980=ORIENTED_EDGE ( 'NONE', *, *, #18396, .T. ) ;
#17981=EDGE_CURVE ( 'NONE', #23434, #3623, #43223, .T. ) ;
#17982=DIRECTION ( 'NONE',  ( 0.000000000000000000, 1.000000000000000000, 0.000000000000000000 ) ) ;
#17983=VECTOR ( 'NONE', #11073, 39.37007874015748143 ) ;
#17984=CARTESIAN_POINT ( 'NONE',  ( -0.07591351300297340121, 3.346456692913386100, -0.6692913385826758654 ) ) ;
#17985=ORIENTED_EDGE ( 'NONE', *, *, #50061, .F. ) ;
#17986=DIRECTION ( 'NONE',  ( 0.000000000000000000, 1.000000000000000000, 0.000000000000000000 ) ) ;
#17988=VERTEX_POINT ( 'NONE', #34739 ) ;
#17989=CARTESIAN_POINT ( 'NONE',  ( 0.000000000000000000, 3.346456692913386100, 0.000000000000000000 ) ) ;
#17992=ORIENTED_EDGE ( 'NONE', *, *, #29661, .T. ) ;
#17993=CARTESIAN_POINT ( 'NONE',  ( 0.000000000000000000, 3.267716535433071279, -1.929133858267711110 ) ) ;
#17994=EDGE_LOOP ( 'NONE', ( #28270, #7947, #12337 ) ) ;
#17995=ORIENTED_EDGE ( 'NONE', *, *, #46072, .T. ) ;
#17997=VECTOR ( 'NONE', #46981, 39.37007874015748143 ) ;
#17998=EDGE_CURVE ( 'NONE', #58, #24845, #8384, .T. ) ;
#17999=ORIENTED_EDGE ( 'NONE', *, *, #50553, .T. ) ;
#18000=ORIENTED_EDGE ( 'NONE', *, *, #7697, .F. ) ;
#18001=PLANE ( 'NONE',  #49952 ) ;
#18002=ADVANCED_FACE ( 'NONE', ( #25152 ), #44750, .F. ) ;
#18003=ORIENTED_EDGE ( 'NONE', *, *, #13143, .T. ) ;
#18005=EDGE_CURVE ( 'NONE', #16878, #8594, #20246, .T. ) ;
#18006=DIRECTION ( 'NONE',  ( -0.000000000000000000, 1.000000000000000000, -0.000000000000000000 ) ) ;
#18007=VECTOR ( 'NONE', #8565, 39.37007874015748143 ) ;
#18008=DIRECTION ( 'NONE',  ( 1.734723475976806848E-16, 0.000000000000000000, 1.000000000000000000 ) ) ;
#18011=DIRECTION ( 'NONE',  ( -3.469446951953613696E-16, 0.000000000000000000, -1.000000000000000000 ) ) ;
#18012=LINE ( 'NONE', #33776, #36165 ) ;
#18013=EDGE_LOOP ( 'NONE', ( #35320, #50864, #3704, #5927 ) ) ;
#18014=DIRECTION ( 'NONE',  ( 1.000000000000000000, 0.000000000000000000, 0.000000000000000000 ) ) ;
#18015=CARTESIAN_POINT ( 'NONE',  ( -1.909347346926324906, 3.346456692913386100, -0.7874015748031470974 ) ) ;
#18016=AXIS2_PLACEMENT_3D ( 'NONE', #3202, #18951, #26941 ) ;
#18017=CARTESIAN_POINT ( 'NONE',  ( 3.927031490892378253E-16, 0.000000000000000000, 1.692913385826762873 ) ) ;
#18018=DIRECTION ( 'NONE',  ( 0.000000000000000000, 0.000000000000000000, -1.000000000000000000 ) ) ;
#18019=VECTOR ( 'NONE', #5034, 39.37007874015748143 ) ;
#18020=CIRCLE ( 'NONE', #12269, 2.106299212598425008 ) ;
#18021=ORIENTED_EDGE ( 'NONE', *, *, #30878, .T. ) ;
#18022=CARTESIAN_POINT ( 'NONE',  ( -1.712496953225537633, 3.346456692913386100, 1.325184350462985883 ) ) ;
#18023=CARTESIAN_POINT ( 'NONE',  ( -0.8182917201112819283, 3.346456692913386100, -0.4724409448818886470 ) ) ;
#18024=EDGE_LOOP ( 'NONE', ( #29486, #14787, #11260, #9128 ) ) ;
#18025=CARTESIAN_POINT ( 'NONE',  ( -0.8182917201112819283, 0.000000000000000000, 2.047244094488179567 ) ) ;
#18026=CARTESIAN_POINT ( 'NONE',  ( 0.000000000000000000, 3.267716535433071279, -1.889763779527552812 ) ) ;
#18027=VECTOR ( 'NONE', #22892, 39.37007874015748143 ) ;
#18029=CARTESIAN_POINT ( 'NONE',  ( 1.909347346926324684, 3.346456692913386100, -0.4724409448818889246 ) ) ;
#18030=VECTOR ( 'NONE', #21844, 39.37007874015748143 ) ;
#18031=EDGE_LOOP ( 'NONE', ( #18939, #47139, #17437, #32135 ) ) ;
#18032=CARTESIAN_POINT ( 'NONE',  ( -1.363819533518803473, 3.267716535433071279, -1.417322834645664109 ) ) ;
#18034=DIRECTION ( 'NONE',  ( -1.000000000000000000, 0.000000000000000000, -0.000000000000000000 ) ) ;
#18039=LINE ( 'NONE', #49483, #2612 ) ;
#18041=ORIENTED_EDGE ( 'NONE', *, *, #10175, .F. ) ;
#18046=CARTESIAN_POINT ( 'NONE',  ( 1.091055626815042645, 0.000000000000000000, 1.259842519685033357 ) ) ;
#18047=DIRECTION ( 'NONE',  ( -1.000000000000000000, 0.000000000000000000, 1.734723475976806848E-16 ) ) ;
#18050=EDGE_CURVE ( 'NONE', #24025, #8409, #17155, .T. ) ;
#18051=DIRECTION ( 'NONE',  ( -0.000000000000000000, 0.000000000000000000, 1.000000000000000000 ) ) ;
#18052=VECTOR ( 'NONE', #44565, 39.37007874015748143 ) ;
#18053=DIRECTION ( 'NONE',  ( 1.734723475976806848E-16, -0.000000000000000000, 1.000000000000000000 ) ) ;
#18057=ORIENTED_EDGE ( 'NONE', *, *, #12638, .F. ) ;
#18059=FACE_BOUND ( 'NONE', #47165, .T. ) ;
#18061=VECTOR ( 'NONE', #42676, 39.37007874015748143 ) ;
#18064=EDGE_CURVE ( 'NONE', #38331, #43301, #16127, .T. ) ;
#18065=DIRECTION ( 'NONE',  ( 1.000000000000000000, 0.000000000000000000, 0.000000000000000000 ) ) ;
#18066=ORIENTED_EDGE ( 'NONE', *, *, #34152, .T. ) ;
#18067=EDGE_LOOP ( 'NONE', ( #34061, #19807, #38442, #19568 ) ) ;
#18068=AXIS2_PLACEMENT_3D ( 'NONE', #24803, #33331, #9056 ) ;
#18070=CARTESIAN_POINT ( 'NONE',  ( 1.015142113812069313, 3.346456692913386100, -1.102362204724405714 ) ) ;
#18071=EDGE_CURVE ( 'NONE', #27247, #6147, #36775, .T. ) ;
#18072=ORIENTED_EDGE ( 'NONE', *, *, #24860, .T. ) ;
#18074=ORIENTED_EDGE ( 'NONE', *, *, #40138, .F. ) ;
#18075=FACE_OUTER_BOUND ( 'NONE', #5712, .T. ) ;
#18078=DIRECTION ( 'NONE',  ( 0.000000000000000000, 0.000000000000000000, 1.000000000000000000 ) ) ;
#18079=ORIENTED_EDGE ( 'NONE', *, *, #21728, .F. ) ;
#18080=ORIENTED_EDGE ( 'NONE', *, *, #34386, .T. ) ;
#18081=FACE_OUTER_BOUND ( 'NONE', #726, .T. ) ;
#18082=DIRECTION ( 'NONE',  ( -0.000000000000000000, 1.000000000000000000, -0.000000000000000000 ) ) ;
#18083=CARTESIAN_POINT ( 'NONE',  ( -1.439733046521776583, 0.000000000000000000, 1.574803149606291530 ) ) ;
#18084=EDGE_CURVE ( 'NONE', #19616, #46654, #12506, .T. ) ;
#18088=AXIS2_PLACEMENT_3D ( 'NONE', #5469, #24837, #20961 ) ;
#18089=DIRECTION ( 'NONE',  ( -1.000000000000000000, -0.000000000000000000, -0.000000000000000000 ) ) ;
#18090=VERTEX_POINT ( 'NONE', #20513 ) ;
#18092=CARTESIAN_POINT ( 'NONE',  ( 1.363819533518803251, 3.267716535433071279, 0.4724409448818871482 ) ) ;
#18094=ORIENTED_EDGE ( 'NONE', *, *, #9436, .T. ) ;
#18097=ORIENTED_EDGE ( 'NONE', *, *, #11110, .T. ) ;
#18098=AXIS2_PLACEMENT_3D ( 'NONE', #11993, #3997, #47060 ) ;
#18101=CARTESIAN_POINT ( 'NONE',  ( 0.000000000000000000, 3.267716535433071279, -1.732283464566922726 ) ) ;
#18102=ORIENTED_EDGE ( 'NONE', *, *, #35142, .F. ) ;
#18103=EDGE_CURVE ( 'NONE', #4317, #183, #20761, .T. ) ;
#18104=LINE ( 'NONE', #10856, #19394 ) ;
#18105=LINE ( 'NONE', #10613, #42056 ) ;
#18106=ADVANCED_FACE ( 'NONE', ( #48347 ), #16902, .F. ) ;
#18107=EDGE_CURVE ( 'NONE', #9230, #20129, #24365, .T. ) ;
#18108=ORIENTED_EDGE ( 'NONE', *, *, #18350, .T. ) ;
#18110=DIRECTION ( 'NONE',  ( -0.000000000000000000, 1.000000000000000000, -0.000000000000000000 ) ) ;
#18112=ORIENTED_EDGE ( 'NONE', *, *, #24402, .F. ) ;
#18114=FACE_OUTER_BOUND ( 'NONE', #13307, .T. ) ;
#18115=PLANE ( 'NONE',  #28476 ) ;
#18117=DIRECTION ( 'NONE',  ( 0.000000000000000000, 1.000000000000000000, 0.000000000000000000 ) ) ;
#18120=VECTOR ( 'NONE', #34316, 39.37007874015748143 ) ;
#18121=LINE ( 'NONE', #49318, #36890 ) ;
#18122=ORIENTED_EDGE ( 'NONE', *, *, #18220, .T. ) ;
#18125=DIRECTION ( 'NONE',  ( 1.000000000000000000, 0.000000000000000000, -3.469446951953613696E-16 ) ) ;
#18126=EDGE_CURVE ( 'NONE', #2091, #40341, #48600, .T. ) ;
#18127=EDGE_LOOP ( 'NONE', ( #24839, #25265, #42234, #3605 ) ) ;
#18128=ORIENTED_EDGE ( 'NONE', *, *, #47329, .T. ) ;
#18129=ADVANCED_BREP_SHAPE_REPRESENTATION ( '', ( #6895, #26741 ), #3635 ) ;
#18130=VECTOR ( 'NONE', #36680, 39.37007874015748143 ) ;
#18131=LINE ( 'NONE', #41121, #6045 ) ;
#18132=EDGE_CURVE ( 'NONE', #44656, #34116, #35897, .T. ) ;
#18133=DIRECTION ( 'NONE',  ( -0.000000000000000000, 1.000000000000000000, -0.000000000000000000 ) ) ;
#18135=VERTEX_POINT ( 'NONE', #25914 ) ;
#18136=ORIENTED_EDGE ( 'NONE', *, *, #31435, .F. ) ;
#18140=EDGE_LOOP ( 'NONE', ( #2134, #44690, #43338, #42243 ) ) ;
#18141=DIRECTION ( 'NONE',  ( -0.000000000000000000, 1.000000000000000000, -0.000000000000000000 ) ) ;
#18142=ADVANCED_FACE ( 'NONE', ( #37292 ), #41663, .F. ) ;
#18144=DIRECTION ( 'NONE',  ( -1.000000000000000000, 0.000000000000000000, 1.734723475976806848E-16 ) ) ;
#18147=ORIENTED_EDGE ( 'NONE', *, *, #17215, .T. ) ;
#18148=CARTESIAN_POINT ( 'NONE',  ( -1.536664496436148184E-16, 0.000000000000000000, 0.4330708661417287386 ) ) ;
#18149=CARTESIAN_POINT ( 'NONE',  ( 0.2727639067037604947, 3.267716535433071279, -0.4724409448818886470 ) ) ;
#18150=EDGE_CURVE ( 'NONE', #37382, #12364, #37801, .T. ) ;
#18151=CARTESIAN_POINT ( 'NONE',  ( -0.5455278134075208785, 0.000000000000000000, 1.574803149606291974 ) ) ;
#18152=EDGE_CURVE ( 'NONE', #8911, #11424, #13792, .T. ) ;
#18153=EDGE_LOOP ( 'NONE', ( #37516, #34000, #15262, #26696 ) ) ;
#18154=PLANE ( 'NONE',  #31475 ) ;
#18155=CARTESIAN_POINT ( 'NONE',  ( -0.2727639067037602727, 3.346456692913386100, 1.850393700787392293 ) ) ;
#18159=ORIENTED_EDGE ( 'NONE', *, *, #43319, .F. ) ;
#18160=DIRECTION ( 'NONE',  ( 0.000000000000000000, 0.000000000000000000, -1.000000000000000000 ) ) ;
#18165=AXIS2_PLACEMENT_3D ( 'NONE', #6460, #36939, #9307 ) ;
#18167=DIRECTION ( 'NONE',  ( 1.000000000000000000, 0.000000000000000000, 0.000000000000000000 ) ) ;
#18170=EDGE_CURVE ( 'NONE', #15256, #24477, #25400, .T. ) ;
#18172=ORIENTED_EDGE ( 'NONE', *, *, #8211, .F. ) ;
#18176=CARTESIAN_POINT ( 'NONE',  ( 0.000000000000000000, 3.267716535433071279, 0.9055118110236167750 ) ) ;
#18177=LINE ( 'NONE', #10431, #25212 ) ;
#18180=ORIENTED_EDGE ( 'NONE', *, *, #43294, .T. ) ;
#18182=PLANE ( 'NONE',  #49297 ) ;
#18183=CARTESIAN_POINT ( 'NONE',  ( -0.3486774197067339376, 3.346456692913386100, -1.574803149606293529 ) ) ;
#18185=ORIENTED_EDGE ( 'NONE', *, *, #24776, .F. ) ;
#18186=DIRECTION ( 'NONE',  ( -0.000000000000000000, 1.000000000000000000, -0.000000000000000000 ) ) ;
#18187=CARTESIAN_POINT ( 'NONE',  ( 0.000000000000000000, 3.346456692913386100, 0.000000000000000000 ) ) ;
#18188=ORIENTED_EDGE ( 'NONE', *, *, #20201, .T. ) ;
#18189=DIRECTION ( 'NONE',  ( 1.000000000000000000, 0.000000000000000000, 0.000000000000000000 ) ) ;
#18190=EDGE_LOOP ( 'NONE', ( #20022, #19965, #45725, #31707 ) ) ;
#18191=EDGE_LOOP ( 'NONE', ( #17204, #17230, #17922, #45592 ) ) ;
#18192=CARTESIAN_POINT ( 'NONE',  ( 1.363819533518803251, 0.000000000000000000, 1.417322834645662777 ) ) ;
#18193=DIRECTION ( 'NONE',  ( -3.469446951953613696E-16, 0.000000000000000000, -1.000000000000000000 ) ) ;
#18197=DIRECTION ( 'NONE',  ( -0.000000000000000000, 1.000000000000000000, -0.000000000000000000 ) ) ;
#18198=DIRECTION ( 'NONE',  ( 1.734723475976806848E-16, -0.000000000000000000, 1.000000000000000000 ) ) ;
#18199=EDGE_LOOP ( 'NONE', ( #12558, #6958, #26034, #12425 ) ) ;
#18200=VERTEX_POINT ( 'NONE', #21281 ) ;
#18202=EDGE_CURVE ( 'NONE', #48375, #47259, #14288, .T. ) ;
#18206=EDGE_CURVE ( 'NONE', #2602, #47863, #5530, .T. ) ;
#18207=EDGE_CURVE ( 'NONE', #31796, #36931, #18420, .T. ) ;
#18208=PLANE ( 'NONE',  #35478 ) ;
#18209=CARTESIAN_POINT ( 'NONE',  ( -0.07591351300297277671, 0.000000000000000000, 1.102362204724404160 ) ) ;
#18210=DIRECTION ( 'NONE',  ( 0.000000000000000000, -1.000000000000000000, 0.000000000000000000 ) ) ;
#18211=ORIENTED_EDGE ( 'NONE', *, *, #2786, .F. ) ;
#18214=LINE ( 'NONE', #42203, #28127 ) ;
#18216=PLANE ( 'NONE',  #12452 ) ;
#18219=CARTESIAN_POINT ( 'NONE',  ( -0.5455278134075214336, 3.346456692913386100, 0.3149606299212577287 ) ) ;
#18220=EDGE_CURVE ( 'NONE', #47654, #183, #37035, .T. ) ;
#18221=DIRECTION ( 'NONE',  ( 0.000000000000000000, 0.000000000000000000, -1.000000000000000000 ) ) ;
#18222=CARTESIAN_POINT ( 'NONE',  ( -0.07591351300297273508, 3.267716535433071279, 2.633779063002547569E-17 ) ) ;
#18225=VERTEX_POINT ( 'NONE', #45759 ) ;
#18226=FACE_BOUND ( 'NONE', #5976, .T. ) ;
#18229=PLANE ( 'NONE',  #3723 ) ;
#18231=EDGE_CURVE ( 'NONE', #49634, #46386, #21792, .T. ) ;
#18232=EDGE_LOOP ( 'NONE', ( #50695, #8971, #33091, #48334 ) ) ;
#18234=ADVANCED_FACE ( 'NONE', ( #29787 ), #33426, .F. ) ;
#18235=CARTESIAN_POINT ( 'NONE',  ( 1.363819533518803029, 3.346456692913386100, -1.417322834645665219 ) ) ;
#18236=CARTESIAN_POINT ( 'NONE',  ( 0.8182917201112817063, 3.346456692913386100, -2.047244094488181343 ) ) ;
#18237=ORIENTED_EDGE ( 'NONE', *, *, #22125, .F. ) ;
#18238=VECTOR ( 'NONE', #36688, 39.37007874015748143 ) ;
#18240=AXIS2_PLACEMENT_3D ( 'NONE', #22243, #45700, #10369 ) ;
#18241=ORIENTED_EDGE ( 'NONE', *, *, #34924, .F. ) ;
#18242=DIRECTION ( 'NONE',  ( -0.000000000000000000, 1.000000000000000000, -0.000000000000000000 ) ) ;
#18245=DIRECTION ( 'NONE',  ( -1.000000000000000000, -0.000000000000000000, -0.000000000000000000 ) ) ;
#18247=VECTOR ( 'NONE', #3120, 39.37007874015748143 ) ;
#18248=EDGE_LOOP ( 'NONE', ( #8340, #5114, #48159, #20290 ) ) ;
#18249=VECTOR ( 'NONE', #1961, 39.37007874015748143 ) ;
#18250=EDGE_LOOP ( 'NONE', ( #42312, #35729, #21420, #11172 ) ) ;
#18252=LINE ( 'NONE', #25238, #10425 ) ;
#18253=ORIENTED_EDGE ( 'NONE', *, *, #19501, .F. ) ;
#18255=CARTESIAN_POINT ( 'NONE',  ( -0.2727639067037608278, 3.267716535433071279, 4.731699523581614055E-17 ) ) ;
#18257=ADVANCED_FACE ( 'NONE', ( #45251 ), #2165, .F. ) ;
#18258=CARTESIAN_POINT ( 'NONE',  ( 1.833433833923351353, 0.000000000000000000, 1.377952755905504256 ) ) ;
#18259=ADVANCED_FACE ( 'NONE', ( #6798 ), #46999, .F. ) ;
#18260=CARTESIAN_POINT ( 'NONE',  ( 1.560669927219590747, 3.346456692913386100, 1.417322834645662777 ) ) ;
#18264=CARTESIAN_POINT ( 'NONE',  ( 0.2727639067037604392, 3.346456692913386100, -0.03937007874015908959 ) ) ;
#18265=LINE ( 'NONE', #2775, #16960 ) ;
#18267=VECTOR ( 'NONE', #25001, 39.37007874015748143 ) ;
#18268=EDGE_CURVE ( 'NONE', #26586, #5952, #35934, .T. ) ;
#18270=VECTOR ( 'NONE', #47085, 39.37007874015748143 ) ;
#18272=DIRECTION ( 'NONE',  ( 0.000000000000000000, 0.000000000000000000, 1.000000000000000000 ) ) ;
#18275=DIRECTION ( 'NONE',  ( 1.000000000000000000, -0.000000000000000000, 0.000000000000000000 ) ) ;
#18276=AXIS2_PLACEMENT_3D ( 'NONE', #36017, #43226, #35500 ) ;
#18277=ORIENTED_EDGE ( 'NONE', *, *, #22716, .F. ) ;
#18278=VECTOR ( 'NONE', #37692, 39.37007874015748143 ) ;
#18281=ORIENTED_EDGE ( 'NONE', *, *, #22824, .F. ) ;
#18282=DIRECTION ( 'NONE',  ( -3.469446951953613696E-16, 0.000000000000000000, -1.000000000000000000 ) ) ;
#18284=VECTOR ( 'NONE', #23596, 39.37007874015748143 ) ;
#18287=LINE ( 'NONE', #21653, #33371 ) ;
#18288=PLANE ( 'NONE',  #27737 ) ;
#18289=VERTEX_POINT ( 'NONE', #31559 ) ;
#18290=EDGE_CURVE ( 'NONE', #8765, #39693, #7308, .T. ) ;
#18291=PLANE ( 'NONE',  #10026 ) ;
#18292=ORIENTED_EDGE ( 'NONE', *, *, #19547, .T. ) ;
#18294=CARTESIAN_POINT ( 'NONE',  ( -2.182111253630085290, 3.346456692913386100, 0.7480314960629874665 ) ) ;
#18295=EDGE_CURVE ( 'NONE', #28575, #7183, #3177, .T. ) ;
#18298=CARTESIAN_POINT ( 'NONE',  ( -0.6214413264104945434, 3.346456692913386100, -1.102362204724405492 ) ) ;
#18299=EDGE_CURVE ( 'NONE', #10637, #12169, #38800, .T. ) ;
#18300=VERTEX_POINT ( 'NONE', #10924 ) ;
#18304=EDGE_LOOP ( 'NONE', ( #38406, #12341, #23945, #20917 ) ) ;
#18305=ORIENTED_EDGE ( 'NONE', *, *, #17746, .F. ) ;
#18306=PLANE ( 'NONE',  #32325 ) ;
#18307=FACE_BOUND ( 'NONE', #42762, .T. ) ;
#18309=VECTOR ( 'NONE', #20714, 39.37007874015748143 ) ;
#18310=DIRECTION ( 'NONE',  ( 1.000000000000000000, 0.000000000000000000, 0.000000000000000000 ) ) ;
#18311=DIRECTION ( 'NONE',  ( -3.469446951953613696E-16, 0.000000000000000000, -1.000000000000000000 ) ) ;
#18312=ORIENTED_EDGE ( 'NONE', *, *, #23286, .T. ) ;
#18313=ORIENTED_EDGE ( 'NONE', *, *, #13900, .T. ) ;
#18314=CARTESIAN_POINT ( 'NONE',  ( -0.2727639067037607723, 0.000000000000000000, 0.1574803149606283648 ) ) ;
#18315=VECTOR ( 'NONE', #14684, 39.37007874015748143 ) ;
#18317=ORIENTED_EDGE ( 'NONE', *, *, #49296, .F. ) ;
#18318=ORIENTED_EDGE ( 'NONE', *, *, #45585, .T. ) ;
#18319=VECTOR ( 'NONE', #33702, 39.37007874015748143 ) ;
#18320=VERTEX_POINT ( 'NONE', #15302 ) ;
#18321=LINE ( 'NONE', #49007, #48265 ) ;
#18323=AXIS2_PLACEMENT_3D ( 'NONE', #29194, #48776, #17586 ) ;
#18324=DIRECTION ( 'NONE',  ( 1.734723475976806848E-16, -0.000000000000000000, 1.000000000000000000 ) ) ;
#18326=DIRECTION ( 'NONE',  ( 1.734723475976806848E-16, -0.000000000000000000, 1.000000000000000000 ) ) ;
#18329=EDGE_CURVE ( 'NONE', #22912, #17453, #49085, .T. ) ;
#18330=CARTESIAN_POINT ( 'NONE',  ( -0.2727639067037607723, 3.346456692913386100, -0.1574803149606301411 ) ) ;
#18331=DIRECTION ( 'NONE',  ( -0.000000000000000000, 1.000000000000000000, -0.000000000000000000 ) ) ;
#18333=FACE_OUTER_BOUND ( 'NONE', #42241, .T. ) ;
#18336=FACE_OUTER_BOUND ( 'NONE', #3701, .T. ) ;
#18338=CARTESIAN_POINT ( 'NONE',  ( 0.8182917201112817063, 3.346456692913386100, -1.929133858267711110 ) ) ;
#18339=ORIENTED_EDGE ( 'NONE', *, *, #22832, .T. ) ;
#18341=CARTESIAN_POINT ( 'NONE',  ( 2.106197740627112402, 3.267716535433071279, 0.7874015748031456541 ) ) ;
#18342=ORIENTED_EDGE ( 'NONE', *, *, #441, .F. ) ;
#18343=ORIENTED_EDGE ( 'NONE', *, *, #33563, .T. ) ;
#18344=VECTOR ( 'NONE', #48238, 39.37007874015748143 ) ;
#18346=EDGE_CURVE ( 'NONE', #7396, #18861, #14803, .T. ) ;
#18347=ORIENTED_EDGE ( 'NONE', *, *, #2189, .T. ) ;
#18348=VECTOR ( 'NONE', #43235, 39.37007874015748143 ) ;
#18349=EDGE_CURVE ( 'NONE', #7558, #40640, #18675, .T. ) ;
#18350=EDGE_CURVE ( 'NONE', #49658, #22538, #30548, .T. ) ;
#18352=DIRECTION ( 'NONE',  ( 1.734723475976806848E-16, -0.000000000000000000, 1.000000000000000000 ) ) ;
#18353=VECTOR ( 'NONE', #46138, 39.37007874015748143 ) ;
#18355=VECTOR ( 'NONE', #50579, 39.37007874015748143 ) ;
#18356=VECTOR ( 'NONE', #9142, 39.37007874015748143 ) ;
#18357=DIRECTION ( 'NONE',  ( -0.000000000000000000, 1.000000000000000000, -0.000000000000000000 ) ) ;
#18358=CARTESIAN_POINT ( 'NONE',  ( 0.000000000000000000, 3.346456692913386100, 0.000000000000000000 ) ) ;
#18361=ORIENTED_EDGE ( 'NONE', *, *, #9388, .T. ) ;
#18362=LINE ( 'NONE', #14489, #30433 ) ;
#18365=CARTESIAN_POINT ( 'NONE',  ( 0.000000000000000000, 3.267716535433071279, -0.3543307086614173040 ) ) ;
#18366=CARTESIAN_POINT ( 'NONE',  ( -0.6214413264104945434, 0.000000000000000000, -1.299212598425193210 ) ) ;
#18368=CARTESIAN_POINT ( 'NONE',  ( -0.07591351300297333182, 3.346456692913386100, 0.4724409448818869817 ) ) ;
#18370=DIRECTION ( 'NONE',  ( -1.000000000000000000, -0.000000000000000000, -0.000000000000000000 ) ) ;
#18371=CARTESIAN_POINT ( 'NONE',  ( 0.1968503937007873017, 3.267716535433071279, -0.9448818897637765168 ) ) ;
#18372=CARTESIAN_POINT ( 'NONE',  ( 1.287906020515829919, 3.346456692913386100, -1.889763779527552368 ) ) ;
#18373=VERTEX_POINT ( 'NONE', #7806 ) ;
#18374=CARTESIAN_POINT ( 'NONE',  ( 1.636583440222563857, 0.000000000000000000, -0.5118110236220471121 ) ) ;
#18375=CARTESIAN_POINT ( 'NONE',  ( -1.363819533518803473, 3.346456692913386100, -1.614173228346451605 ) ) ;
#18377=ORIENTED_EDGE ( 'NONE', *, *, #30158, .F. ) ;
#18379=CARTESIAN_POINT ( 'NONE',  ( 0.8182917201112817063, 3.267716535433071279, -1.614173228346451605 ) ) ;
#18380=LINE ( 'NONE', #15267, #12120 ) ;
#18381=FACE_OUTER_BOUND ( 'NONE', #20063, .T. ) ;
#18384=AXIS2_PLACEMENT_3D ( 'NONE', #45454, #29484, #2116 ) ;
#18385=EDGE_CURVE ( 'NONE', #26820, #42568, #50607, .T. ) ;
#18386=LINE ( 'NONE', #41198, #41981 ) ;
#18387=ADVANCED_FACE ( 'NONE', ( #27162 ), #39299, .F. ) ;
#18389=EDGE_LOOP ( 'NONE', ( #40990, #26095, #1579, #47021, #10880 ) ) ;
#18390=LINE ( 'NONE', #34150, #43060 ) ;
#18391=CARTESIAN_POINT ( 'NONE',  ( 1.670330979180827180, 3.346456692913386100, 1.377952755905504256 ) ) ;
#18392=EDGE_CURVE ( 'NONE', #27908, #10859, #22542, .T. ) ;
#18396=EDGE_CURVE ( 'NONE', #33096, #10269, #15051, .T. ) ;
#18398=CARTESIAN_POINT ( 'NONE',  ( -1.712496953225537188, 3.346456692913386100, 0.9055118110236167750 ) ) ;
#18401=ORIENTED_EDGE ( 'NONE', *, *, #33761, .F. ) ;
#18402=LINE ( 'NONE', #42642, #23395 ) ;
#18403=LINE ( 'NONE', #26396, #21929 ) ;
#18404=FACE_OUTER_BOUND ( 'NONE', #8917, .T. ) ;
#18405=ORIENTED_EDGE ( 'NONE', *, *, #35719, .F. ) ;
#18406=DIRECTION ( 'NONE',  ( 1.000000000000000000, 0.000000000000000000, 0.000000000000000000 ) ) ;
#18408=ADVANCED_FACE ( 'NONE', ( #47512 ), #20692, .F. ) ;
#18409=DIRECTION ( 'NONE',  ( 0.000000000000000000, 0.000000000000000000, -1.000000000000000000 ) ) ;
#18410=VERTEX_POINT ( 'NONE', #49240 ) ;
#18411=CARTESIAN_POINT ( 'NONE',  ( -0.07591351300297283222, 3.267716535433071279, 2.633779063002550959E-17 ) ) ;
#18412=EDGE_CURVE ( 'NONE', #48423, #29935, #44184, .T. ) ;
#18413=ORIENTED_EDGE ( 'NONE', *, *, #23808, .T. ) ;
#18420=LINE ( 'NONE', #49860, #35121 ) ;
#18421=EDGE_CURVE ( 'NONE', #15390, #12933, #32078, .T. ) ;
#18423=VERTEX_POINT ( 'NONE', #16061 ) ;
#18424=ORIENTED_EDGE ( 'NONE', *, *, #44416, .T. ) ;
#18426=CARTESIAN_POINT ( 'NONE',  ( -0.07591351300297363713, 3.346456692913386100, -2.164023224473873963 ) ) ;
#18430=DIRECTION ( 'NONE',  ( 0.000000000000000000, -1.000000000000000000, 0.000000000000000000 ) ) ;
#18431=LINE ( 'NONE', #29797, #14572 ) ;
#18432=ADVANCED_FACE ( 'NONE', ( #47768 ), #31821, .F. ) ;
#18433=VECTOR ( 'NONE', #46913, 39.37007874015748143 ) ;
#18434=VECTOR ( 'NONE', #27642, 39.37007874015748143 ) ;
#18435=ORIENTED_EDGE ( 'NONE', *, *, #38998, .F. ) ;
#18436=ORIENTED_EDGE ( 'NONE', *, *, #23738, .T. ) ;
#18437=CARTESIAN_POINT ( 'NONE',  ( 0.000000000000000000, 3.267716535433071279, 1.062992125984246083 ) ) ;
#18438=FACE_OUTER_BOUND ( 'NONE', #47762, .T. ) ;
#18439=DIRECTION ( 'NONE',  ( 0.000000000000000000, 0.000000000000000000, -1.000000000000000000 ) ) ;
#18440=ORIENTED_EDGE ( 'NONE', *, *, #23852, .F. ) ;
#18442=FACE_BOUND ( 'NONE', #34039, .T. ) ;
#18443=VECTOR ( 'NONE', #2148, 39.37007874015748143 ) ;
#18444=ORIENTED_EDGE ( 'NONE', *, *, #22011, .T. ) ;
#18446=CARTESIAN_POINT ( 'NONE',  ( -1.636583440222564301, 3.346456692913386100, -0.9448818897637762948 ) ) ;
#18447=ORIENTED_EDGE ( 'NONE', *, *, #22337, .F. ) ;
#18450=CARTESIAN_POINT ( 'NONE',  ( 0.000000000000000000, 3.267716535433071279, 0.000000000000000000 ) ) ;
#18451=CARTESIAN_POINT ( 'NONE',  ( -2.182111253630085290, 0.000000000000000000, -0.1968503937007880511 ) ) ;
#18455=ORIENTED_EDGE ( 'NONE', *, *, #37357, .F. ) ;
#18456=ORIENTED_EDGE ( 'NONE', *, *, #33378, .F. ) ;
#18457=DIRECTION ( 'NONE',  ( -3.469446951953613696E-16, 0.000000000000000000, -1.000000000000000000 ) ) ;
#18458=LINE ( 'NONE', #7094, #26743 ) ;
#18459=EDGE_CURVE ( 'NONE', #12011, #2745, #43924, .T. ) ;
#18460=CARTESIAN_POINT ( 'NONE',  ( -1.363819533518803473, 3.346456692913386100, 1.732283464566920950 ) ) ;
#18464=CARTESIAN_POINT ( 'NONE',  ( 1.560669927219590303, 0.000000000000000000, -1.299212598425193210 ) ) ;
#18466=VECTOR ( 'NONE', #48757, 39.37007874015748143 ) ;
#18469=DIRECTION ( 'NONE',  ( 1.000000000000000000, 0.000000000000000000, 0.000000000000000000 ) ) ;
#18470=AXIS2_PLACEMENT_3D ( 'NONE', #28749, #5775, #16893 ) ;
#18473=CARTESIAN_POINT ( 'NONE',  ( 0.5455278134075216556, 3.267716535433071279, 1.062992125984246083 ) ) ;
#18474=DIRECTION ( 'NONE',  ( 1.000000000000000000, -0.000000000000000000, 0.000000000000000000 ) ) ;
#18475=ORIENTED_EDGE ( 'NONE', *, *, #13328, .F. ) ;
#18476=DIRECTION ( 'NONE',  ( -0.000000000000000000, 1.000000000000000000, -0.000000000000000000 ) ) ;
#18477=CARTESIAN_POINT ( 'NONE',  ( 2.378961647330872786, 3.267716535433071279, -8.253681236146643855E-16 ) ) ;
#18478=CARTESIAN_POINT ( 'NONE',  ( 0.000000000000000000, 3.267716535433071279, 1.574803149606291974 ) ) ;
#18479=VECTOR ( 'NONE', #46430, 39.37007874015748143 ) ;
#18481=DIRECTION ( 'NONE',  ( -0.000000000000000000, 1.000000000000000000, -0.000000000000000000 ) ) ;
#18483=FACE_BOUND ( 'NONE', #18680, .T. ) ;
#18485=LINE ( 'NONE', #34240, #15251 ) ;
#18486=CARTESIAN_POINT ( 'NONE',  ( -0.3486774197067334380, 3.346456692913386100, 1.889763779527550369 ) ) ;
#18487=EDGE_CURVE ( 'NONE', #36908, #31407, #28434, .T. ) ;
#18488=VERTEX_POINT ( 'NONE', #27928 ) ;
#18489=VERTEX_POINT ( 'NONE', #48984 ) ;
#18490=FACE_OUTER_BOUND ( 'NONE', #37320, .T. ) ;
#18494=EDGE_CURVE ( 'NONE', #46941, #6476, #33555, .T. ) ;
#18496=VERTEX_POINT ( 'NONE', #40336 ) ;
#18498=VERTEX_POINT ( 'NONE', #29408 ) ;
#18499=PLANE ( 'NONE',  #29067 ) ;
#18500=EDGE_CURVE ( 'NONE', #4594, #40457, #45131, .T. ) ;
#18503=ORIENTED_EDGE ( 'NONE', *, *, #40980, .F. ) ;
#18505=CARTESIAN_POINT ( 'NONE',  ( 4.268512490100411402E-16, 3.346456692913386100, 0.9448818897637749625 ) ) ;
#18506=VECTOR ( 'NONE', #25624, 39.37007874015748143 ) ;
#18507=ORIENTED_EDGE ( 'NONE', *, *, #41769, .F. ) ;
#18508=ORIENTED_EDGE ( 'NONE', *, *, #20237, .F. ) ;
#18509=VECTOR ( 'NONE', #37411, 39.37007874015748143 ) ;
#18510=EDGE_CURVE ( 'NONE', #58, #7441, #5911, .T. ) ;
#18512=ORIENTED_EDGE ( 'NONE', *, *, #49302, .F. ) ;
#18513=ORIENTED_EDGE ( 'NONE', *, *, #20126, .T. ) ;
#18514=LINE ( 'NONE', #34763, #22806 ) ;
#18515=VECTOR ( 'NONE', #35865, 39.37007874015748143 ) ;
#18516=ORIENTED_EDGE ( 'NONE', *, *, #34545, .F. ) ;
#18519=ADVANCED_FACE ( 'NONE', ( #35944 ), #8312, .F. ) ;
#18521=EDGE_CURVE ( 'NONE', #12259, #3361, #41697, .T. ) ;
#18523=DIRECTION ( 'NONE',  ( 1.000000000000000000, 0.000000000000000000, -3.469446951953613696E-16 ) ) ;
#18524=EDGE_CURVE ( 'NONE', #19657, #39052, #28180, .T. ) ;
#18527=PLANE ( 'NONE',  #50501 ) ;
#18528=FACE_OUTER_BOUND ( 'NONE', #41909, .T. ) ;
#18530=VERTEX_POINT ( 'NONE', #32333 ) ;
#18531=CARTESIAN_POINT ( 'NONE',  ( 0.000000000000000000, 3.267716535433071279, -0.5118110236220467790 ) ) ;
#18532=LINE ( 'NONE', #37910, #44239 ) ;
#18533=VERTEX_POINT ( 'NONE', #26297 ) ;
#18534=CARTESIAN_POINT ( 'NONE',  ( -0.8942052331142547050, 0.000000000000000000, 0.6299212598425164567 ) ) ;
#18535=CARTESIAN_POINT ( 'NONE',  ( 1.363819533518803251, 3.267716535433071279, -0.3543307086614178592 ) ) ;
#18540=ORIENTED_EDGE ( 'NONE', *, *, #30443, .T. ) ;
#18542=AXIS2_PLACEMENT_3D ( 'NONE', #17403, #49104, #5528 ) ;
#18543=DIRECTION ( 'NONE',  ( 1.000000000000000000, 0.000000000000000000, 0.000000000000000000 ) ) ;
#18544=LINE ( 'NONE', #19034, #28684 ) ;
#18546=CARTESIAN_POINT ( 'NONE',  ( 0.8182917201112819283, 3.346456692913386100, -0.4724409448818889246 ) ) ;
#18548=EDGE_CURVE ( 'NONE', #21385, #2753, #25216, .T. ) ;
#18549=DIRECTION ( 'NONE',  ( -0.000000000000000000, 1.000000000000000000, -0.000000000000000000 ) ) ;
#18551=VERTEX_POINT ( 'NONE', #29916 ) ;
#18552=VERTEX_POINT ( 'NONE', #6933 ) ;
#18556=DIRECTION ( 'NONE',  ( -0.000000000000000000, 1.000000000000000000, -0.000000000000000000 ) ) ;
#18557=CARTESIAN_POINT ( 'NONE',  ( 0.000000000000000000, 3.267716535433071279, -2.086614173228339641 ) ) ;
#18558=ORIENTED_EDGE ( 'NONE', *, *, #10806, .F. ) ;
#18559=CARTESIAN_POINT ( 'NONE',  ( 0.1968503937007872462, 3.346456692913386100, -1.141732283464564013 ) ) ;
#18562=ADVANCED_FACE ( 'NONE', ( #42043 ), #22679, .F. ) ;
#18563=ADVANCED_FACE ( 'NONE', ( #10296 ), #34054, .F. ) ;
#18564=PLANE ( 'NONE',  #24722 ) ;
#18565=ORIENTED_EDGE ( 'NONE', *, *, #21356, .T. ) ;
#18566=VERTEX_POINT ( 'NONE', #10044 ) ;
#18567=DIRECTION ( 'NONE',  ( -1.000000000000000000, 0.000000000000000000, 0.000000000000000000 ) ) ;
#18568=FACE_BOUND ( 'NONE', #16791, .T. ) ;
#18569=ORIENTED_EDGE ( 'NONE', *, *, #50407, .F. ) ;
#18570=CARTESIAN_POINT ( 'NONE',  ( -1.363819533518803473, 0.000000000000000000, -1.299212598425192544 ) ) ;
#18571=LINE ( 'NONE', #47347, #34967 ) ;
#18572=VERTEX_POINT ( 'NONE', #18298 ) ;
#18573=VERTEX_POINT ( 'NONE', #38187 ) ;
#18574=DIRECTION ( 'NONE',  ( 1.734723475976806848E-16, -0.000000000000000000, 1.000000000000000000 ) ) ;
#18576=LINE ( 'NONE', #34334, #27846 ) ;
#18577=VECTOR ( 'NONE', #21421, 39.37007874015748143 ) ;
#18578=VECTOR ( 'NONE', #23461, 39.37007874015748143 ) ;
#18579=ORIENTED_EDGE ( 'NONE', *, *, #18843, .F. ) ;
#18580=EDGE_CURVE ( 'NONE', #32558, #26618, #49740, .T. ) ;
#18581=AXIS2_PLACEMENT_3D ( 'NONE', #14547, #27160, #42903 ) ;
#18583=CARTESIAN_POINT ( 'NONE',  ( -0.8942052331142559263, 3.267716535433071279, 3.102397620449225439E-16 ) ) ;
#18586=FACE_OUTER_BOUND ( 'NONE', #43725, .T. ) ;
#18587=EDGE_CURVE ( 'NONE', #22163, #15713, #2297, .T. ) ;
#18588=ORIENTED_EDGE ( 'NONE', *, *, #19319, .F. ) ;
#18591=CARTESIAN_POINT ( 'NONE',  ( -0.8942052331142552601, 0.000000000000000000, 2.007874015748021268 ) ) ;
#18592=CARTESIAN_POINT ( 'NONE',  ( 0.5455278134075212115, 0.000000000000000000, -0.9448818897637765168 ) ) ;
#18594=LINE ( 'NONE', #14714, #5193 ) ;
#18597=CARTESIAN_POINT ( 'NONE',  ( -1.636583440222563635, 3.267716535433071279, -4.780733988912460139E-16 ) ) ;
#18598=CARTESIAN_POINT ( 'NONE',  ( -0.8182917201112814842, 3.346456692913386100, 0.7874015748031456541 ) ) ;
#18599=ORIENTED_EDGE ( 'NONE', *, *, #47124, .T. ) ;
#18601=DIRECTION ( 'NONE',  ( -0.000000000000000000, 1.000000000000000000, -0.000000000000000000 ) ) ;
#18602=EDGE_LOOP ( 'NONE', ( #28156, #43686, #38204, #2864 ) ) ;
#18608=VECTOR ( 'NONE', #48752, 39.37007874015748143 ) ;
#18609=ORIENTED_EDGE ( 'NONE', *, *, #2825, .F. ) ;
#18610=CARTESIAN_POINT ( 'NONE',  ( -1.195183497228115035E-16, 3.267716535433071279, -1.259842519685035134 ) ) ;
#18611=VECTOR ( 'NONE', #14297, 39.37007874015748143 ) ;
#18612=ORIENTED_EDGE ( 'NONE', *, *, #462, .T. ) ;
#18613=CARTESIAN_POINT ( 'NONE',  ( 1.091055626815042423, 3.346456692913386100, -1.771653543307081691 ) ) ;
#18614=DIRECTION ( 'NONE',  ( -0.000000000000000000, 1.000000000000000000, -0.000000000000000000 ) ) ;
#18615=EDGE_CURVE ( 'NONE', #42119, #24025, #22931, .T. ) ;
#18616=AXIS2_PLACEMENT_3D ( 'NONE', #18187, #33445, #10186 ) ;
#18618=EDGE_CURVE ( 'NONE', #41248, #20003, #26544, .T. ) ;
#18619=AXIS2_PLACEMENT_3D ( 'NONE', #1074, #36458, #13664 ) ;
#18620=DIRECTION ( 'NONE',  ( -3.469446951953613696E-16, 0.000000000000000000, -1.000000000000000000 ) ) ;
#18621=EDGE_CURVE ( 'NONE', #31414, #32045, #10554, .T. ) ;
#18622=VERTEX_POINT ( 'NONE', #18807 ) ;
#18623=ORIENTED_EDGE ( 'NONE', *, *, #25806, .F. ) ;
#18624=CARTESIAN_POINT ( 'NONE',  ( -0.8942052331142552601, 3.346456692913386100, 2.204724409448808764 ) ) ;
#18625=DIRECTION ( 'NONE',  ( -0.000000000000000000, 1.000000000000000000, -0.000000000000000000 ) ) ;
#18626=LINE ( 'NONE', #34376, #40508 ) ;
#18628=EDGE_CURVE ( 'NONE', #7592, #50730, #22429, .T. ) ;
#18629=ORIENTED_EDGE ( 'NONE', *, *, #31062, .T. ) ;
#18631=CARTESIAN_POINT ( 'NONE',  ( 0.5455278134075216556, 3.346456692913386100, 1.377952755905504256 ) ) ;
#18633=VERTEX_POINT ( 'NONE', #30678 ) ;
#18635=ORIENTED_EDGE ( 'NONE', *, *, #2947, .F. ) ;
#18636=ORIENTED_EDGE ( 'NONE', *, *, #43710, .T. ) ;
#18640=ADVANCED_FACE ( 'NONE', ( #6173 ), #6429, .F. ) ;
#18641=VECTOR ( 'NONE', #9637, 39.37007874015748143 ) ;
#18644=ORIENTED_EDGE ( 'NONE', *, *, #8929, .T. ) ;
#18645=ORIENTED_EDGE ( 'NONE', *, *, #5183, .F. ) ;
#18647=VECTOR ( 'NONE', #21375, 39.37007874015748143 ) ;
#18648=EDGE_CURVE ( 'NONE', #2383, #50578, #49491, .T. ) ;
#18650=ORIENTED_EDGE ( 'NONE', *, *, #4988, .T. ) ;
#18652=LINE ( 'NONE', #34402, #29249 ) ;
#18653=AXIS2_PLACEMENT_3D ( 'NONE', #19490, #34999, #3246 ) ;
#18654=VECTOR ( 'NONE', #11952, 39.37007874015748143 ) ;
#18656=CARTESIAN_POINT ( 'NONE',  ( 2.651794250122221246E-16, 0.000000000000000000, 2.165354330708661568 ) ) ;
#18657=CARTESIAN_POINT ( 'NONE',  ( 0.2727639067037604947, 0.000000000000000000, -0.1574803149606298636 ) ) ;
#18658=VECTOR ( 'NONE', #16138, 39.37007874015748143 ) ;
#18659=ORIENTED_EDGE ( 'NONE', *, *, #30199, .T. ) ;
#18660=LINE ( 'NONE', #50340, #33344 ) ;
#18661=CARTESIAN_POINT ( 'NONE',  ( -1.636583440222564301, 3.267716535433071279, -1.771653543307080581 ) ) ;
#18662=CARTESIAN_POINT ( 'NONE',  ( 0.000000000000000000, 3.346456692913386100, 0.000000000000000000 ) ) ;
#18663=EDGE_LOOP ( 'NONE', ( #31526, #2365, #43844, #30128 ) ) ;
#18664=DIRECTION ( 'NONE',  ( 0.000000000000000000, -1.000000000000000000, 0.000000000000000000 ) ) ;
#18667=ORIENTED_EDGE ( 'NONE', *, *, #8952, .F. ) ;
#18669=ORIENTED_EDGE ( 'NONE', *, *, #2015, .F. ) ;
#18670=DIRECTION ( 'NONE',  ( -0.000000000000000000, 1.000000000000000000, -0.000000000000000000 ) ) ;
#18671=EDGE_LOOP ( 'NONE', ( #3885, #12400, #46218, #12656 ) ) ;
#18675=LINE ( 'NONE', #31306, #7888 ) ;
#18678=ADVANCED_FACE ( 'NONE', ( #37931 ), #8454, .F. ) ;
#18680=EDGE_LOOP ( 'NONE', ( #38747, #44780, #10352, #12910 ) ) ;
#18681=DIRECTION ( 'NONE',  ( 0.000000000000000000, -1.000000000000000000, 0.000000000000000000 ) ) ;
#18682=VECTOR ( 'NONE', #5619, 39.37007874015748143 ) ;
#18684=EDGE_CURVE ( 'NONE', #22386, #20489, #27805, .T. ) ;
#18685=VECTOR ( 'NONE', #47804, 39.37007874015748143 ) ;
#18686=ORIENTED_EDGE ( 'NONE', *, *, #17244, .F. ) ;
#18688=CARTESIAN_POINT ( 'NONE',  ( -1.091055626815042645, 0.000000000000000000, 1.889763779527550147 ) ) ;
#18689=CARTESIAN_POINT ( 'NONE',  ( 1.363819533518803251, 0.000000000000000000, -0.03937007874015908959 ) ) ;
#18690=ADVANCED_FACE ( 'NONE', ( #186 ), #50485, .F. ) ;
#18691=ORIENTED_EDGE ( 'NONE', *, *, #18862, .F. ) ;
#18692=EDGE_LOOP ( 'NONE', ( #2247, #19850, #17820, #23635 ) ) ;
#18693=DIRECTION ( 'NONE',  ( 1.734723475976806848E-16, -0.000000000000000000, 1.000000000000000000 ) ) ;
#18695=AXIS2_PLACEMENT_3D ( 'NONE', #8667, #47612, #8161 ) ;
#18696=CARTESIAN_POINT ( 'NONE',  ( -0.3486774197067334935, 3.267716535433071279, 1.377952755905504256 ) ) ;
#18700=DIRECTION ( 'NONE',  ( 0.000000000000000000, -0.000000000000000000, 1.000000000000000000 ) ) ;
#18701=ORIENTED_EDGE ( 'NONE', *, *, #42239, .T. ) ;
#18702=LINE ( 'NONE', #14061, #42226 ) ;
#18704=VERTEX_POINT ( 'NONE', #7436 ) ;
#18705=CARTESIAN_POINT ( 'NONE',  ( 1.636583440222563857, 3.346456692913386100, 1.259842519685033135 ) ) ;
#18708=EDGE_CURVE ( 'NONE', #29664, #1395, #39949, .T. ) ;
#18710=DIRECTION ( 'NONE',  ( 1.000000000000000000, -0.000000000000000000, 0.000000000000000000 ) ) ;
#18711=EDGE_LOOP ( 'NONE', ( #21724, #28904, #24726, #9958 ) ) ;
#18713=ADVANCED_FACE ( 'NONE', ( #43037 ), #15182, .F. ) ;
#18714=ORIENTED_EDGE ( 'NONE', *, *, #37536, .F. ) ;
#18715=CARTESIAN_POINT ( 'NONE',  ( 1.091055626815042645, 0.000000000000000000, -8.878505979408855953E-16 ) ) ;
#18716=CARTESIAN_POINT ( 'NONE',  ( -0.5455278134075208785, 3.346456692913386100, 0.9448818897637749625 ) ) ;
#18722=ORIENTED_EDGE ( 'NONE', *, *, #41371, .T. ) ;
#18723=CARTESIAN_POINT ( 'NONE',  ( 0.8182917201112819283, 3.346456692913386100, 1.102362204724403938 ) ) ;
#18725=DIRECTION ( 'NONE',  ( 1.000000000000000000, -0.000000000000000000, 0.000000000000000000 ) ) ;
#18727=PLANE ( 'NONE',  #43840 ) ;
#18728=PLANE ( 'NONE',  #38509 ) ;
#18731=VECTOR ( 'NONE', #43187, 39.37007874015748143 ) ;
#18732=CARTESIAN_POINT ( 'NONE',  ( -0.3486774197067339376, 3.346456692913386100, -0.3149606299212593941 ) ) ;
#18733=DIRECTION ( 'NONE',  ( 1.000000000000000000, -0.000000000000000000, 0.000000000000000000 ) ) ;
#18736=ORIENTED_EDGE ( 'NONE', *, *, #46265, .T. ) ;
#18737=FACE_BOUND ( 'NONE', #27934, .T. ) ;
#18739=CARTESIAN_POINT ( 'NONE',  ( -0.6214413264104939882, 3.346456692913386100, 1.417322834645662777 ) ) ;
#18740=ORIENTED_EDGE ( 'NONE', *, *, #5388, .T. ) ;
#18741=EDGE_LOOP ( 'NONE', ( #10157, #9786, #39623, #39344 ) ) ;
#18742=CARTESIAN_POINT ( 'NONE',  ( -1.091055626815042645, 3.346456692913386100, 2.007874015748021268 ) ) ;
#18744=FACE_OUTER_BOUND ( 'NONE', #46901, .T. ) ;
#18746=ADVANCED_FACE ( 'NONE', ( #47396 ), #23944, .F. ) ;
#18747=CARTESIAN_POINT ( 'NONE',  ( -1.195183497228115035E-16, 0.000000000000000000, -1.259842519685035134 ) ) ;
#18748=EDGE_LOOP ( 'NONE', ( #39819, #2758, #50621, #25625 ) ) ;
#18752=VECTOR ( 'NONE', #35451, 39.37007874015748143 ) ;
#18753=AXIS2_PLACEMENT_3D ( 'NONE', #34105, #10603, #38731 ) ;
#18755=CARTESIAN_POINT ( 'NONE',  ( -0.3486774197067340486, 3.267716535433071279, -1.771653543307081025 ) ) ;
#18757=ORIENTED_EDGE ( 'NONE', *, *, #24034, .T. ) ;
#18758=CARTESIAN_POINT ( 'NONE',  ( 3.927031490892378253E-16, 3.346456692913386100, 0.7480314960629874665 ) ) ;
#18759=EDGE_LOOP ( 'NONE', ( #25921, #24159, #26114, #6655 ) ) ;
#18766=VECTOR ( 'NONE', #16167, 39.37007874015748143 ) ;
#18767=CARTESIAN_POINT ( 'NONE',  ( -1.985260859929297794, 0.000000000000000000, -0.1968503937007880511 ) ) ;
#18768=PLANE ( 'NONE',  #20292 ) ;
#18770=DIRECTION ( 'NONE',  ( -1.000000000000000000, -0.000000000000000000, -0.000000000000000000 ) ) ;
#18771=LINE ( 'NONE', #30645, #12935 ) ;
#18773=EDGE_LOOP ( 'NONE', ( #24110, #32220, #14578, #16927 ) ) ;
#18774=CARTESIAN_POINT ( 'NONE',  ( 0.2727639067037604947, 0.000000000000000000, -0.7874015748031473194 ) ) ;
#18779=VERTEX_POINT ( 'NONE', #42793 ) ;
#18780=CARTESIAN_POINT ( 'NONE',  ( -1.636583440222563635, 3.346456692913386100, 0.7480314960629874665 ) ) ;
#18781=DIRECTION ( 'NONE',  ( -1.000000000000000000, 0.000000000000000000, 1.734723475976806848E-16 ) ) ;
#18782=VERTEX_POINT ( 'NONE', #27295 ) ;
#18784=VECTOR ( 'NONE', #17401, 39.37007874015748143 ) ;
#18785=VECTOR ( 'NONE', #28421, 39.37007874015748143 ) ;
#18787=ADVANCED_FACE ( 'NONE', ( #23422 ), #39178, .F. ) ;
#18788=VECTOR ( 'NONE', #15507, 39.37007874015748143 ) ;
#18789=PLANE ( 'NONE',  #2657 ) ;
#18790=ORIENTED_EDGE ( 'NONE', *, *, #22691, .F. ) ;
#18792=ADVANCED_FACE ( 'NONE', ( #15681 ), #47135, .F. ) ;
#18793=LINE ( 'NONE', #21910, #36605 ) ;
#18794=AXIS2_PLACEMENT_3D ( 'NONE', #7116, #6614, #22358 ) ;
#18795=CARTESIAN_POINT ( 'NONE',  ( -1.909347346926324462, 0.000000000000000000, 1.102362204724404160 ) ) ;
#18796=DIRECTION ( 'NONE',  ( -1.000000000000000000, 0.000000000000000000, 1.734723475976806848E-16 ) ) ;
#18797=LINE ( 'NONE', #21914, #43390 ) ;
#18798=ORIENTED_EDGE ( 'NONE', *, *, #25701, .T. ) ;
#18801=ORIENTED_EDGE ( 'NONE', *, *, #21356, .F. ) ;
#18802=ORIENTED_EDGE ( 'NONE', *, *, #27556, .T. ) ;
#18803=DIRECTION ( 'NONE',  ( -3.469446951953613696E-16, 0.000000000000000000, -1.000000000000000000 ) ) ;
#18804=ORIENTED_EDGE ( 'NONE', *, *, #8208, .T. ) ;
#18805=CARTESIAN_POINT ( 'NONE',  ( -1.712496953225537633, 3.346456692913386100, 1.325184350462985883 ) ) ;
#18807=CARTESIAN_POINT ( 'NONE',  ( -0.3486774197067339376, 3.267716535433071279, 2.204724409448808764 ) ) ;
#18808=VERTEX_POINT ( 'NONE', #40468 ) ;
#18809=EDGE_CURVE ( 'NONE', #4725, #31145, #40982, .T. ) ;
#18810=CARTESIAN_POINT ( 'NONE',  ( -1.712496953225537188, 0.000000000000000000, 0.1574803149606286423 ) ) ;
#18811=DIRECTION ( 'NONE',  ( 0.000000000000000000, 0.000000000000000000, -1.000000000000000000 ) ) ;
#18813=EDGE_CURVE ( 'NONE', #9339, #31055, #9736, .T. ) ;
#18814=CARTESIAN_POINT ( 'NONE',  ( 0.1968503937007877735, 0.000000000000000000, 1.692913385826762873 ) ) ;
#18816=ORIENTED_EDGE ( 'NONE', *, *, #34919, .T. ) ;
#18818=FACE_BOUND ( 'NONE', #20398, .T. ) ;
#18819=VERTEX_POINT ( 'NONE', #28834 ) ;
#18821=VECTOR ( 'NONE', #30426, 39.37007874015748143 ) ;
#18822=EDGE_LOOP ( 'NONE', ( #47096, #55, #32226, #17121 ) ) ;
#18824=LINE ( 'NONE', #34575, #5957 ) ;
#18826=ORIENTED_EDGE ( 'NONE', *, *, #12441, .T. ) ;
#18827=VECTOR ( 'NONE', #10951, 39.37007874015748143 ) ;
#18830=DIRECTION ( 'NONE',  ( 1.000000000000000000, 0.000000000000000000, -3.469446951953613696E-16 ) ) ;
#18832=VECTOR ( 'NONE', #2097, 39.37007874015748143 ) ;
#18833=EDGE_CURVE ( 'NONE', #46201, #33355, #29347, .T. ) ;
#18834=PLANE ( 'NONE',  #1649 ) ;
#18835=VECTOR ( 'NONE', #13880, 39.37007874015748143 ) ;
#18836=ORIENTED_EDGE ( 'NONE', *, *, #22347, .F. ) ;
#18837=ORIENTED_EDGE ( 'NONE', *, *, #4846, .F. ) ;
#18839=LINE ( 'NONE', #45666, #22198 ) ;
#18840=CARTESIAN_POINT ( 'NONE',  ( 1.287906020515829919, 3.346456692913386100, -1.574803149606294417 ) ) ;
#18841=CIRCLE ( 'NONE', #17228, 2.106299212598425008 ) ;
#18843=EDGE_CURVE ( 'NONE', #30490, #27988, #44568, .T. ) ;
#18844=CARTESIAN_POINT ( 'NONE',  ( 0.2727639067037609943, 3.267716535433071279, 1.535433070866133898 ) ) ;
#18845=ADVANCED_FACE ( 'NONE', ( #45075 ), #32987, .F. ) ;
#18846=DIRECTION ( 'NONE',  ( 0.000000000000000000, 1.000000000000000000, 0.000000000000000000 ) ) ;
#18847=EDGE_CURVE ( 'NONE', #129, #28656, #44061, .T. ) ;
#18850=CARTESIAN_POINT ( 'NONE',  ( 0.4696143004045484903, 0.000000000000000000, 2.362204724409437961 ) ) ;
#18853=VERTEX_POINT ( 'NONE', #708 ) ;
#18854=DIRECTION ( 'NONE',  ( 1.000000000000000000, 0.000000000000000000, -3.469446951953613696E-16 ) ) ;
#18857=ORIENTED_EDGE ( 'NONE', *, *, #8840, .T. ) ;
#18861=VERTEX_POINT ( 'NONE', #29083 ) ;
#18862=EDGE_CURVE ( 'NONE', #42794, #38226, #36849, .T. ) ;
#18866=PLANE ( 'NONE',  #47751 ) ;
#18867=EDGE_CURVE ( 'NONE', #37726, #47811, #44821, .T. ) ;
#18868=EDGE_CURVE ( 'NONE', #19280, #29009, #16719, .T. ) ;
#18872=EDGE_CURVE ( 'NONE', #22659, #5755, #1469, .T. ) ;
#18873=ORIENTED_EDGE ( 'NONE', *, *, #38599, .T. ) ;
#18874=ORIENTED_EDGE ( 'NONE', *, *, #51011, .T. ) ;
#18875=CARTESIAN_POINT ( 'NONE',  ( -1.166969139818015977, 3.267716535433071279, -1.732283464566922726 ) ) ;
#18876=CARTESIAN_POINT ( 'NONE',  ( -2.182111253630085290, 3.267716535433071279, -6.146657985744592735E-16 ) ) ;
#18878=VECTOR ( 'NONE', #13270, 39.37007874015748143 ) ;
#18879=ORIENTED_EDGE ( 'NONE', *, *, #25687, .T. ) ;
#18880=PLANE ( 'NONE',  #43501 ) ;
#18882=ORIENTED_EDGE ( 'NONE', *, *, #32079, .F. ) ;
#18884=VERTEX_POINT ( 'NONE', #8708 ) ;
#18886=LINE ( 'NONE', #38760, #11099 ) ;
#18889=AXIS2_PLACEMENT_3D ( 'NONE', #2932, #30301, #30046 ) ;
#18890=DIRECTION ( 'NONE',  ( 1.734723475976806848E-16, -0.000000000000000000, 1.000000000000000000 ) ) ;
#18891=DIRECTION ( 'NONE',  ( -0.000000000000000000, 1.000000000000000000, -0.000000000000000000 ) ) ;
#18892=ORIENTED_EDGE ( 'NONE', *, *, #44581, .T. ) ;
#18893=ORIENTED_EDGE ( 'NONE', *, *, #8400, .F. ) ;
#18895=LINE ( 'NONE', #42378, #36672 ) ;
#18898=CARTESIAN_POINT ( 'NONE',  ( 0.4696143004045479352, 3.346456692913386100, -0.1574803149606298636 ) ) ;
#18899=VECTOR ( 'NONE', #44469, 39.37007874015748143 ) ;
#18901=AXIS2_PLACEMENT_3D ( 'NONE', #7365, #3489, #34735 ) ;
#18902=CARTESIAN_POINT ( 'NONE',  ( -0.8942052331142552601, 0.000000000000000000, -0.3149606299212593941 ) ) ;
#18903=EDGE_CURVE ( 'NONE', #48838, #49994, #13607, .T. ) ;
#18904=CARTESIAN_POINT ( 'NONE',  ( 2.182111253630085290, 3.346456692913386100, 0.1181102362204698858 ) ) ;
#18905=DIRECTION ( 'NONE',  ( -0.000000000000000000, 1.000000000000000000, -0.000000000000000000 ) ) ;
#18906=EDGE_LOOP ( 'NONE', ( #42752, #3437, #5049, #20181, #47201 ) ) ;
#18907=DIRECTION ( 'NONE',  ( 1.000000000000000000, 0.000000000000000000, 0.000000000000000000 ) ) ;
#18909=ORIENTED_EDGE ( 'NONE', *, *, #25513, .F. ) ;
#18910=DIRECTION ( 'NONE',  ( -0.000000000000000000, 0.000000000000000000, 1.000000000000000000 ) ) ;
#18911=DIRECTION ( 'NONE',  ( -3.469446951953613696E-16, 0.000000000000000000, -1.000000000000000000 ) ) ;
#18912=DIRECTION ( 'NONE',  ( 0.000000000000000000, -1.000000000000000000, 0.000000000000000000 ) ) ;
#18913=ORIENTED_EDGE ( 'NONE', *, *, #34945, .F. ) ;
#18915=ORIENTED_EDGE ( 'NONE', *, *, #5901, .F. ) ;
#18916=CARTESIAN_POINT ( 'NONE',  ( -4.268512490100411402E-16, 3.346456692913386100, -2.086614173228339641 ) ) ;
#18917=ADVANCED_FACE ( 'NONE', ( #16458 ), #36335, .F. ) ;
#18918=EDGE_LOOP ( 'NONE', ( #38171, #50953, #44272, #27010 ) ) ;
#18919=CARTESIAN_POINT ( 'NONE',  ( -1.439733046521777249, 3.267716535433071279, 4.995077429881869829E-16 ) ) ;
#18920=ORIENTED_EDGE ( 'NONE', *, *, #26204, .F. ) ;
#18922=ADVANCED_FACE ( 'NONE', ( #34251 ), #10998, .F. ) ;
#18923=CARTESIAN_POINT ( 'NONE',  ( 1.015142113812069091, 0.000000000000000000, -2.047244094488181343 ) ) ;
#18924=CARTESIAN_POINT ( 'NONE',  ( -1.195183497228115035E-16, 3.346456692913386100, -0.9448818897637765168 ) ) ;
#18925=VECTOR ( 'NONE', #4526, 39.37007874015748143 ) ;
#18926=EDGE_CURVE ( 'NONE', #37379, #38729, #1982, .T. ) ;
#18927=ORIENTED_EDGE ( 'NONE', *, *, #30003, .F. ) ;
#18928=ORIENTED_EDGE ( 'NONE', *, *, #15711, .F. ) ;
#18929=ORIENTED_EDGE ( 'NONE', *, *, #15052, .T. ) ;
#18930=DIRECTION ( 'NONE',  ( 0.000000000000000000, 0.000000000000000000, 1.000000000000000000 ) ) ;
#18932=ADVANCED_FACE ( 'NONE', ( #33496 ), #42229, .F. ) ;
#18933=VERTEX_POINT ( 'NONE', #18236 ) ;
#18934=CARTESIAN_POINT ( 'NONE',  ( -1.166969139818015977, 3.346456692913386100, -1.753476375576570323 ) ) ;
#18935=CARTESIAN_POINT ( 'NONE',  ( 1.560669927219590525, 3.267716535433071279, 0.5905511811023579360 ) ) ;
#18936=CARTESIAN_POINT ( 'NONE',  ( -0.6214413264104945434, 3.267716535433071279, -1.299212598425193210 ) ) ;
#18937=CIRCLE ( 'NONE', #25533, 2.106299212598425008 ) ;
#18938=VERTEX_POINT ( 'NONE', #42485 ) ;
#18939=ORIENTED_EDGE ( 'NONE', *, *, #40897, .T. ) ;
#18941=DIRECTION ( 'NONE',  ( -1.000000000000000000, 0.000000000000000000, 1.734723475976806848E-16 ) ) ;
#18942=CARTESIAN_POINT ( 'NONE',  ( -1.363819533518803029, 0.000000000000000000, 1.220472440944875281 ) ) ;
#18944=DIRECTION ( 'NONE',  ( 1.734723475976806848E-16, 0.000000000000000000, 1.000000000000000000 ) ) ;
#18945=DIRECTION ( 'NONE',  ( -1.000000000000000000, 0.000000000000000000, -0.000000000000000000 ) ) ;
#18946=ORIENTED_EDGE ( 'NONE', *, *, #46054, .T. ) ;
#18947=DIRECTION ( 'NONE',  ( -1.000000000000000000, -0.000000000000000000, -0.000000000000000000 ) ) ;
#18949=VERTEX_POINT ( 'NONE', #41988 ) ;
#18950=VECTOR ( 'NONE', #26354, 39.37007874015748143 ) ;
#18951=DIRECTION ( 'NONE',  ( -0.000000000000000000, 0.000000000000000000, 1.000000000000000000 ) ) ;
#18954=DIRECTION ( 'NONE',  ( 0.000000000000000000, 0.000000000000000000, -1.000000000000000000 ) ) ;
#18955=PLANE ( 'NONE',  #4893 ) ;
#18957=VERTEX_POINT ( 'NONE', #46336 ) ;
#18961=LINE ( 'NONE', #42453, #41828 ) ;
#18963=ORIENTED_EDGE ( 'NONE', *, *, #30796, .T. ) ;
#18965=LINE ( 'NONE', #10720, #39882 ) ;
#18966=CARTESIAN_POINT ( 'NONE',  ( -2.009899395340762673, 3.346456692913386100, 0.6299212598425164567 ) ) ;
#18969=ORIENTED_EDGE ( 'NONE', *, *, #4912, .T. ) ;
#18970=LINE ( 'NONE', #34227, #47908 ) ;
#18972=CARTESIAN_POINT ( 'NONE',  ( -0.2727639067037607723, 0.000000000000000000, 0.4724409448818869817 ) ) ;
#18973=CARTESIAN_POINT ( 'NONE',  ( -1.091055626815042201, 3.346456692913386100, 0.3149606299212580063 ) ) ;
#18974=DIRECTION ( 'NONE',  ( -1.000000000000000000, 0.000000000000000000, 1.734723475976806848E-16 ) ) ;
#18975=DIRECTION ( 'NONE',  ( 1.734723475976806848E-16, 0.000000000000000000, 1.000000000000000000 ) ) ;
#18976=LINE ( 'NONE', #18222, #21932 ) ;
#18978=CARTESIAN_POINT ( 'NONE',  ( 0.000000000000000000, 3.267716535433071279, 0.1574803149606285035 ) ) ;
#18979=VECTOR ( 'NONE', #7439, 39.37007874015748143 ) ;
#18980=VERTEX_POINT ( 'NONE', #26480 ) ;
#18981=FACE_BOUND ( 'NONE', #14108, .T. ) ;
#18982=CARTESIAN_POINT ( 'NONE',  ( 0.5455278134075212115, 3.346456692913386100, 0.6299212598425161236 ) ) ;
#18984=EDGE_CURVE ( 'NONE', #17666, #15979, #50757, .T. ) ;
#18985=CARTESIAN_POINT ( 'NONE',  ( -1.794796351285542491, 3.267716535433071279, 1.102362204724404160 ) ) ;
#18986=VERTEX_POINT ( 'NONE', #17984 ) ;
#18987=ORIENTED_EDGE ( 'NONE', *, *, #41484, .F. ) ;
#18990=EDGE_CURVE ( 'NONE', #11767, #1340, #21604, .T. ) ;
#18991=DIRECTION ( 'NONE',  ( -0.000000000000000000, 1.000000000000000000, -0.000000000000000000 ) ) ;
#18993=PLANE ( 'NONE',  #40106 ) ;
#18994=CARTESIAN_POINT ( 'NONE',  ( -1.439733046521776139, 3.267716535433071279, 4.995077429881866871E-16 ) ) ;
#18995=EDGE_LOOP ( 'NONE', ( #7843, #35883, #50972, #30299 ) ) ;
#18998=CARTESIAN_POINT ( 'NONE',  ( -1.909347346926324906, 0.000000000000000000, -0.4724409448818884805 ) ) ;
#18999=EDGE_LOOP ( 'NONE', ( #26418, #25852, #45353, #16111 ) ) ;
#19000=LINE ( 'NONE', #34756, #11713 ) ;
#19002=ORIENTED_EDGE ( 'NONE', *, *, #48548, .F. ) ;
#19003=EDGE_CURVE ( 'NONE', #34452, #4494, #25985, .T. ) ;
#19004=VECTOR ( 'NONE', #16291, 39.37007874015748143 ) ;
#19005=VECTOR ( 'NONE', #27425, 39.37007874015748143 ) ;
#19006=ORIENTED_EDGE ( 'NONE', *, *, #30468, .T. ) ;
#19008=DIRECTION ( 'NONE',  ( 1.000000000000000000, -0.000000000000000000, 0.000000000000000000 ) ) ;
#19009=VECTOR ( 'NONE', #15443, 39.37007874015748143 ) ;
#19010=DIRECTION ( 'NONE',  ( -3.469446951953613696E-16, 0.000000000000000000, -1.000000000000000000 ) ) ;
#19011=LINE ( 'NONE', #42507, #9580 ) ;
#19012=LINE ( 'NONE', #50701, #44500 ) ;
#19013=LINE ( 'NONE', #23143, #3859 ) ;
#19015=ORIENTED_EDGE ( 'NONE', *, *, #37789, .T. ) ;
#19016=ADVANCED_FACE ( 'NONE', ( #30112 ), #37364, .F. ) ;
#19017=LINE ( 'NONE', #34775, #36546 ) ;
#19018=DIRECTION ( 'NONE',  ( 1.000000000000000000, 0.000000000000000000, 0.000000000000000000 ) ) ;
#19019=CARTESIAN_POINT ( 'NONE',  ( 1.560669927219590747, 0.000000000000000000, 0.1574803149606283648 ) ) ;
#19022=VERTEX_POINT ( 'NONE', #2238 ) ;
#19023=CARTESIAN_POINT ( 'NONE',  ( 0.000000000000000000, 3.267716535433071279, 1.417322834645662777 ) ) ;
#19025=DIRECTION ( 'NONE',  ( 0.000000000000000000, 0.000000000000000000, -1.000000000000000000 ) ) ;
#19029=DIRECTION ( 'NONE',  ( -0.000000000000000000, 1.000000000000000000, -0.000000000000000000 ) ) ;
#19032=LINE ( 'NONE', #34295, #47818 ) ;
#19033=CARTESIAN_POINT ( 'NONE',  ( -0.5455278134075214336, 3.267716535433071279, -2.034427629037601104 ) ) ;
#19034=CARTESIAN_POINT ( 'NONE',  ( -0.2727639067037608278, 3.346456692913386100, 0.2755905511810995412 ) ) ;
#19035=VECTOR ( 'NONE', #30121, 39.37007874015748143 ) ;
#19036=DIRECTION ( 'NONE',  ( 1.000000000000000000, 0.000000000000000000, 0.000000000000000000 ) ) ;
#19039=ORIENTED_EDGE ( 'NONE', *, *, #7322, .F. ) ;
#19042=LINE ( 'NONE', #23171, #35329 ) ;
#19044=ADVANCED_FACE ( 'NONE', ( #38870 ), #43231, .F. ) ;
#19045=LINE ( 'NONE', #23684, #13092 ) ;
#19049=DIRECTION ( 'NONE',  ( 1.000000000000000000, 0.000000000000000000, 0.000000000000000000 ) ) ;
#19050=VECTOR ( 'NONE', #14907, 39.37007874015748143 ) ;
#19051=ADVANCED_FACE ( 'NONE', ( #35254 ), #18993, .F. ) ;
#19053=CARTESIAN_POINT ( 'NONE',  ( 1.443330927545150910, 3.346456692913386100, -1.614173228346452715 ) ) ;
#19055=ORIENTED_EDGE ( 'NONE', *, *, #28206, .F. ) ;
#19056=LINE ( 'NONE', #11070, #19110 ) ;
#19057=FACE_BOUND ( 'NONE', #49118, .T. ) ;
#19058=ORIENTED_EDGE ( 'NONE', *, *, #2141, .T. ) ;
#19059=EDGE_CURVE ( 'NONE', #17713, #33946, #11751, .T. ) ;
#19060=CARTESIAN_POINT ( 'NONE',  ( -0.2727639067037602172, 0.000000000000000000, 2.047244094488179567 ) ) ;
#19062=ORIENTED_EDGE ( 'NONE', *, *, #42861, .F. ) ;
#19063=CARTESIAN_POINT ( 'NONE',  ( 0.000000000000000000, 3.267716535433071279, 0.000000000000000000 ) ) ;
#19066=ORIENTED_EDGE ( 'NONE', *, *, #1075, .F. ) ;
#19068=VERTEX_POINT ( 'NONE', #46584 ) ;
#19070=AXIS2_PLACEMENT_3D ( 'NONE', #28808, #49409, #6345 ) ;
#19072=VECTOR ( 'NONE', #133, 39.37007874015748143 ) ;
#19074=ORIENTED_EDGE ( 'NONE', *, *, #10764, .T. ) ;
#19075=ORIENTED_EDGE ( 'NONE', *, *, #43693, .F. ) ;
#19076=VECTOR ( 'NONE', #31122, 39.37007874015748143 ) ;
#19079=DIRECTION ( 'NONE',  ( 1.000000000000000000, -0.000000000000000000, 0.000000000000000000 ) ) ;
#19080=AXIS2_PLACEMENT_3D ( 'NONE', #13295, #32156, #16660 ) ;
#19083=EDGE_CURVE ( 'NONE', #45220, #29397, #27492, .T. ) ;
#19084=AXIS2_PLACEMENT_3D ( 'NONE', #24629, #24884, #21010 ) ;
#19086=EDGE_CURVE ( 'NONE', #50405, #3086, #3248, .T. ) ;
#19087=LINE ( 'NONE', #42828, #30892 ) ;
#19088=ORIENTED_EDGE ( 'NONE', *, *, #32088, .T. ) ;
#19090=LINE ( 'NONE', #34846, #24431 ) ;
#19091=ORIENTED_EDGE ( 'NONE', *, *, #3125, .T. ) ;
#19092=ORIENTED_EDGE ( 'NONE', *, *, #36179, .T. ) ;
#19093=LINE ( 'NONE', #26838, #2762 ) ;
#19095=VERTEX_POINT ( 'NONE', #19744 ) ;
#19097=ORIENTED_EDGE ( 'NONE', *, *, #23006, .T. ) ;
#19098=LINE ( 'NONE', #30484, #45186 ) ;
#19099=VERTEX_POINT ( 'NONE', #23119 ) ;
#19100=VECTOR ( 'NONE', #14786, 39.37007874015748143 ) ;
#19101=DIRECTION ( 'NONE',  ( -0.000000000000000000, 1.000000000000000000, -0.000000000000000000 ) ) ;
#19102=DIRECTION ( 'NONE',  ( -1.000000000000000000, 0.000000000000000000, -0.000000000000000000 ) ) ;
#19103=EDGE_CURVE ( 'NONE', #38248, #2104, #47333, .T. ) ;
#19104=ORIENTED_EDGE ( 'NONE', *, *, #2335, .F. ) ;
#19105=VECTOR ( 'NONE', #25027, 39.37007874015748143 ) ;
#19106=CARTESIAN_POINT ( 'NONE',  ( -0.2727639067037608278, 3.346456692913386100, -1.929133858267710000 ) ) ;
#19107=EDGE_LOOP ( 'NONE', ( #41533, #7353, #7799, #14214 ) ) ;
#19109=LINE ( 'NONE', #18366, #7034 ) ;
#19110=VECTOR ( 'NONE', #30182, 39.37007874015748143 ) ;
#19114=AXIS2_PLACEMENT_3D ( 'NONE', #23529, #292, #23281 ) ;
#19116=EDGE_CURVE ( 'NONE', #28931, #19562, #39376, .T. ) ;
#19117=CARTESIAN_POINT ( 'NONE',  ( -2.454875160333845674, 3.232777166330581320, 0.1574803149606286423 ) ) ;
#19118=DIRECTION ( 'NONE',  ( -0.000000000000000000, 1.000000000000000000, -0.000000000000000000 ) ) ;
#19119=EDGE_CURVE ( 'NONE', #9992, #34145, #39630, .T. ) ;
#19121=CARTESIAN_POINT ( 'NONE',  ( 0.000000000000000000, 3.267716535433071279, -0.6692913385826760875 ) ) ;
#19122=EDGE_CURVE ( 'NONE', #2745, #9737, #46830, .T. ) ;
#19124=EDGE_LOOP ( 'NONE', ( #15509, #13744, #34803, #8824 ) ) ;
#19127=ADVANCED_FACE ( 'NONE', ( #47588 ), #11253, .F. ) ;
#19131=CARTESIAN_POINT ( 'NONE',  ( 0.7423782071083090406, 3.267716535433071279, -2.575641807848711180E-16 ) ) ;
#19135=LINE ( 'NONE', #12158, #48163 ) ;
#19139=EDGE_CURVE ( 'NONE', #47679, #12647, #37645, .T. ) ;
#19142=DIRECTION ( 'NONE',  ( 1.000000000000000000, 0.000000000000000000, 0.000000000000000000 ) ) ;
#19143=DIRECTION ( 'NONE',  ( 1.734723475976806848E-16, -0.000000000000000000, 1.000000000000000000 ) ) ;
#19144=AXIS2_PLACEMENT_3D ( 'NONE', #36598, #28579, #12849 ) ;
#19145=LINE ( 'NONE', #23272, #41910 ) ;
#19146=ORIENTED_EDGE ( 'NONE', *, *, #37927, .F. ) ;
#19147=EDGE_CURVE ( 'NONE', #41494, #1578, #27236, .T. ) ;
#19148=DIRECTION ( 'NONE',  ( 0.000000000000000000, -1.000000000000000000, 0.000000000000000000 ) ) ;
#19151=DIRECTION ( 'NONE',  ( -0.000000000000000000, 1.000000000000000000, -0.000000000000000000 ) ) ;
#19152=CARTESIAN_POINT ( 'NONE',  ( -0.8942052331142547050, 3.267716535433071279, 1.259842519685033357 ) ) ;
#19154=VERTEX_POINT ( 'NONE', #37045 ) ;
#19156=DIRECTION ( 'NONE',  ( -0.000000000000000000, 1.000000000000000000, -0.000000000000000000 ) ) ;
#19157=VERTEX_POINT ( 'NONE', #28771 ) ;
#19159=EDGE_LOOP ( 'NONE', ( #51036, #49225, #41907, #29222 ) ) ;
#19160=DIRECTION ( 'NONE',  ( 1.000000000000000000, 0.000000000000000000, -3.469446951953613696E-16 ) ) ;
#19162=DIRECTION ( 'NONE',  ( -1.000000000000000000, 0.000000000000000000, 0.000000000000000000 ) ) ;
#19165=ORIENTED_EDGE ( 'NONE', *, *, #40433, .F. ) ;
#19168=PLANE ( 'NONE',  #16670 ) ;
#19170=ORIENTED_EDGE ( 'NONE', *, *, #35313, .F. ) ;
#19173=DIRECTION ( 'NONE',  ( -1.000000000000000000, 0.000000000000000000, 1.734723475976806848E-16 ) ) ;
#19174=CARTESIAN_POINT ( 'NONE',  ( 0.4696143004045484903, 3.267716535433071279, 1.417322834645662777 ) ) ;
#19176=ORIENTED_EDGE ( 'NONE', *, *, #45402, .T. ) ;
#19177=EDGE_CURVE ( 'NONE', #12919, #34200, #29023, .T. ) ;
#19178=CARTESIAN_POINT ( 'NONE',  ( -0.07591351300297277671, 0.000000000000000000, 2.047244094488179567 ) ) ;
#19185=VECTOR ( 'NONE', #17360, 39.37007874015748143 ) ;
#19186=DIRECTION ( 'NONE',  ( 1.734723475976806848E-16, -0.000000000000000000, 1.000000000000000000 ) ) ;
#19187=VERTEX_POINT ( 'NONE', #33178 ) ;
#19189=ORIENTED_EDGE ( 'NONE', *, *, #35472, .T. ) ;
#19190=VECTOR ( 'NONE', #27189, 39.37007874015748143 ) ;
#19192=DIRECTION ( 'NONE',  ( -0.000000000000000000, 0.000000000000000000, 1.000000000000000000 ) ) ;
#19193=DIRECTION ( 'NONE',  ( -3.469446951953613696E-16, 0.000000000000000000, -1.000000000000000000 ) ) ;
#19194=AXIS2_PLACEMENT_3D ( 'NONE', #14392, #26012, #10015 ) ;
#19197=LINE ( 'NONE', #2702, #10439 ) ;
#19200=VECTOR ( 'NONE', #11477, 39.37007874015748143 ) ;
#19202=ORIENTED_EDGE ( 'NONE', *, *, #17366, .T. ) ;
#19203=FACE_OUTER_BOUND ( 'NONE', #42357, .T. ) ;
#19205=EDGE_CURVE ( 'NONE', #9948, #3567, #48611, .T. ) ;
#19206=EDGE_CURVE ( 'NONE', #23218, #2123, #4518, .T. ) ;
#19207=CARTESIAN_POINT ( 'NONE',  ( -1.166969139818015977, 0.000000000000000000, -1.417322834645664109 ) ) ;
#19208=CARTESIAN_POINT ( 'NONE',  ( -1.363819533518803473, 3.267716535433071279, -1.299212598425192544 ) ) ;
#19209=LINE ( 'NONE', #34969, #45971 ) ;
#19212=ADVANCED_FACE ( 'NONE', ( #48860 ), #8392, .F. ) ;
#19213=DIRECTION ( 'NONE',  ( 1.000000000000000000, 0.000000000000000000, 0.000000000000000000 ) ) ;
#19214=ORIENTED_EDGE ( 'NONE', *, *, #12150, .F. ) ;
#19215=DIRECTION ( 'NONE',  ( 1.000000000000000000, 0.000000000000000000, -3.469446951953613696E-16 ) ) ;
#19217=DIRECTION ( 'NONE',  ( 1.000000000000000000, 0.000000000000000000, 0.000000000000000000 ) ) ;
#19219=CARTESIAN_POINT ( 'NONE',  ( -0.07591351300297288773, 3.267716535433071279, 2.633779063002553116E-17 ) ) ;
#19220=CARTESIAN_POINT ( 'NONE',  ( 1.091055626815042645, 0.000000000000000000, -0.8267716535433055070 ) ) ;
#19221=CARTESIAN_POINT ( 'NONE',  ( -0.8942052331142552601, 3.346456692913386100, -0.3149606299212593941 ) ) ;
#19223=ORIENTED_EDGE ( 'NONE', *, *, #31093, .F. ) ;
#19224=AXIS2_PLACEMENT_3D ( 'NONE', #16638, #28492, #40391 ) ;
#19228=AXIS2_PLACEMENT_3D ( 'NONE', #36419, #28661, #9046 ) ;
#19229=VECTOR ( 'NONE', #30714, 39.37007874015748143 ) ;
#19230=CARTESIAN_POINT ( 'NONE',  ( -1.363819533518803029, 3.346456692913386100, 1.220472440944875281 ) ) ;
#19231=DIRECTION ( 'NONE',  ( 1.000000000000000000, 0.000000000000000000, 0.000000000000000000 ) ) ;
#19232=VERTEX_POINT ( 'NONE', #44262 ) ;
#19233=ORIENTED_EDGE ( 'NONE', *, *, #5033, .F. ) ;
#19234=LINE ( 'NONE', #15118, #45442 ) ;
#19235=LINE ( 'NONE', #22614, #21335 ) ;
#19236=DIRECTION ( 'NONE',  ( -0.000000000000000000, 1.000000000000000000, -0.000000000000000000 ) ) ;
#19237=DIRECTION ( 'NONE',  ( -1.000000000000000000, 0.000000000000000000, -0.000000000000000000 ) ) ;
#19238=DIRECTION ( 'NONE',  ( -3.469446951953613696E-16, 0.000000000000000000, -1.000000000000000000 ) ) ;
#19241=CARTESIAN_POINT ( 'NONE',  ( -1.536664496436148184E-16, 0.000000000000000000, -1.771653543307081025 ) ) ;
#19242=DIRECTION ( 'NONE',  ( -0.000000000000000000, 1.000000000000000000, -0.000000000000000000 ) ) ;
#19243=DIRECTION ( 'NONE',  ( -3.469446951953613696E-16, 0.000000000000000000, -1.000000000000000000 ) ) ;
#19245=ORIENTED_EDGE ( 'NONE', *, *, #8530, .F. ) ;
#19246=EDGE_CURVE ( 'NONE', #35070, #26916, #21037, .T. ) ;
#19248=EDGE_LOOP ( 'NONE', ( #39109, #18347, #40464, #48185 ) ) ;
#19250=ADVANCED_FACE ( 'NONE', ( #20257 ), #8901, .F. ) ;
#19251=ORIENTED_EDGE ( 'NONE', *, *, #2747, .T. ) ;
#19253=CARTESIAN_POINT ( 'NONE',  ( -1.909347346926324906, 3.346456692913386100, -0.9842519685039344823 ) ) ;
#19254=ORIENTED_EDGE ( 'NONE', *, *, #46423, .T. ) ;
#19256=VECTOR ( 'NONE', #33282, 39.37007874015748143 ) ;
#19257=DIRECTION ( 'NONE',  ( -1.000000000000000000, 0.000000000000000000, -0.000000000000000000 ) ) ;
#19258=FACE_OUTER_BOUND ( 'NONE', #20446, .T. ) ;
#19259=DIRECTION ( 'NONE',  ( 0.000000000000000000, -1.000000000000000000, 0.000000000000000000 ) ) ;
#19260=VECTOR ( 'NONE', #42974, 39.37007874015748143 ) ;
#19265=PLANE ( 'NONE',  #47576 ) ;
#19266=VECTOR ( 'NONE', #34599, 39.37007874015748143 ) ;
#19267=ORIENTED_EDGE ( 'NONE', *, *, #46727, .F. ) ;
#19268=CARTESIAN_POINT ( 'NONE',  ( -2.287922694693813913E-16, 3.267716535433071279, 3.968913209705475983E-32 ) ) ;
#19273=EDGE_LOOP ( 'NONE', ( #19923, #12653, #34484, #5476 ) ) ;
#19274=FACE_OUTER_BOUND ( 'NONE', #42282, .T. ) ;
#19275=DIRECTION ( 'NONE',  ( 1.734723475976806848E-16, 0.000000000000000000, 1.000000000000000000 ) ) ;
#19276=ORIENTED_EDGE ( 'NONE', *, *, #48659, .F. ) ;
#19277=FACE_OUTER_BOUND ( 'NONE', #37949, .T. ) ;
#19279=DIRECTION ( 'NONE',  ( 1.000000000000000000, 0.000000000000000000, 0.000000000000000000 ) ) ;
#19280=VERTEX_POINT ( 'NONE', #47844 ) ;
#19284=PLANE ( 'NONE',  #39142 ) ;
#19285=ORIENTED_EDGE ( 'NONE', *, *, #28160, .T. ) ;
#19286=AXIS2_PLACEMENT_3D ( 'NONE', #14065, #29813, #26191 ) ;
#19290=DIRECTION ( 'NONE',  ( -3.469446951953613696E-16, 0.000000000000000000, -1.000000000000000000 ) ) ;
#19295=AXIS2_PLACEMENT_3D ( 'NONE', #22051, #33932, #30049 ) ;
#19296=AXIS2_PLACEMENT_3D ( 'NONE', #35157, #23519, #4420 ) ;
#19297=CARTESIAN_POINT ( 'NONE',  ( 1.091055626815042645, 3.267716535433071279, 0.1181102362204704270 ) ) ;
#19298=VERTEX_POINT ( 'NONE', #20523 ) ;
#19299=PLANE ( 'NONE',  #10064 ) ;
#19301=AXIS2_PLACEMENT_3D ( 'NONE', #16116, #47313, #19971 ) ;
#19302=ORIENTED_EDGE ( 'NONE', *, *, #42774, .T. ) ;
#19303=ADVANCED_FACE ( 'NONE', ( #6566 ), #49121, .F. ) ;
#19304=EDGE_LOOP ( 'NONE', ( #42808, #6244, #33768, #8564 ) ) ;
#19305=CARTESIAN_POINT ( 'NONE',  ( -1.363819533518803473, 0.000000000000000000, 1.850393700787392293 ) ) ;
#19306=ORIENTED_EDGE ( 'NONE', *, *, #44124, .T. ) ;
#19307=EDGE_CURVE ( 'NONE', #36491, #49628, #2435, .T. ) ;
#19309=EDGE_CURVE ( 'NONE', #3695, #32172, #49620, .T. ) ;
#19311=ORIENTED_EDGE ( 'NONE', *, *, #1210, .F. ) ;
#19312=CARTESIAN_POINT ( 'NONE',  ( 0.000000000000000000, 3.267716535433071279, -1.417322834645665219 ) ) ;
#19313=DIRECTION ( 'NONE',  ( 1.000000000000000000, -0.000000000000000000, 0.000000000000000000 ) ) ;
#19314=VERTEX_POINT ( 'NONE', #42169 ) ;
#19315=CARTESIAN_POINT ( 'NONE',  ( 2.106197740627112402, 3.267716535433071279, 0.02067487291359298637 ) ) ;
#19316=ORIENTED_EDGE ( 'NONE', *, *, #16505, .F. ) ;
#19318=DIRECTION ( 'NONE',  ( -0.000000000000000000, 0.000000000000000000, 1.000000000000000000 ) ) ;
#19319=EDGE_CURVE ( 'NONE', #1960, #25880, #14050, .T. ) ;
#19321=ORIENTED_EDGE ( 'NONE', *, *, #7668, .F. ) ;
#19322=EDGE_LOOP ( 'NONE', ( #23431, #8213, #8819, #17391 ) ) ;
#19324=DIRECTION ( 'NONE',  ( 0.000000000000000000, 0.000000000000000000, -1.000000000000000000 ) ) ;
#19325=DIRECTION ( 'NONE',  ( 1.000000000000000000, -0.000000000000000000, 0.000000000000000000 ) ) ;
#19327=DIRECTION ( 'NONE',  ( 1.000000000000000000, 0.000000000000000000, 0.000000000000000000 ) ) ;
#19328=EDGE_CURVE ( 'NONE', #9804, #47774, #17925, .T. ) ;
#19329=VECTOR ( 'NONE', #39779, 39.37007874015748143 ) ;
#19331=VECTOR ( 'NONE', #17024, 39.37007874015748143 ) ;
#19335=CARTESIAN_POINT ( 'NONE',  ( -0.8182917201112819283, 0.000000000000000000, 0.1574803149606285035 ) ) ;
#19336=VECTOR ( 'NONE', #40804, 39.37007874015748143 ) ;
#19337=ORIENTED_EDGE ( 'NONE', *, *, #6158, .F. ) ;
#19338=PLANE ( 'NONE',  #13581 ) ;
#19340=EDGE_CURVE ( 'NONE', #13566, #50909, #33688, .T. ) ;
#19342=PLANE ( 'NONE',  #6077 ) ;
#19346=VERTEX_POINT ( 'NONE', #22053 ) ;
#19347=FACE_OUTER_BOUND ( 'NONE', #16093, .T. ) ;
#19350=CARTESIAN_POINT ( 'NONE',  ( -0.2727639067037608278, 3.346456692913386100, 2.165354330708650465 ) ) ;
#19351=ORIENTED_EDGE ( 'NONE', *, *, #6982, .F. ) ;
#19352=DIRECTION ( 'NONE',  ( -0.000000000000000000, 1.000000000000000000, -0.000000000000000000 ) ) ;
#19353=VECTOR ( 'NONE', #33335, 39.37007874015748143 ) ;
#19354=VERTEX_POINT ( 'NONE', #25409 ) ;
#19355=VERTEX_POINT ( 'NONE', #38318 ) ;
#19356=VECTOR ( 'NONE', #10932, 39.37007874015748143 ) ;
#19357=VECTOR ( 'NONE', #31734, 39.37007874015748143 ) ;
#19358=CARTESIAN_POINT ( 'NONE',  ( 1.287906020515830141, 3.267716535433071279, 0.4330708661417287386 ) ) ;
#19359=LINE ( 'NONE', #24270, #10836 ) ;
#19360=DIRECTION ( 'NONE',  ( -1.000000000000000000, 0.000000000000000000, -0.000000000000000000 ) ) ;
#19361=AXIS2_PLACEMENT_3D ( 'NONE', #32981, #17466, #9466 ) ;
#19363=VERTEX_POINT ( 'NONE', #6807 ) ;
#19365=DIRECTION ( 'NONE',  ( -0.000000000000000000, 1.000000000000000000, -0.000000000000000000 ) ) ;
#19366=EDGE_CURVE ( 'NONE', #18533, #13717, #34438, .T. ) ;
#19367=VERTEX_POINT ( 'NONE', #2680 ) ;
#19369=VECTOR ( 'NONE', #50177, 39.37007874015748143 ) ;
#19375=DIRECTION ( 'NONE',  ( -1.000000000000000000, -0.000000000000000000, -0.000000000000000000 ) ) ;
#19377=CARTESIAN_POINT ( 'NONE',  ( -0.07591351300297284610, 3.267716535433071279, 1.535433070866133898 ) ) ;
#19380=CARTESIAN_POINT ( 'NONE',  ( -1.166969139818016199, 3.346456692913386100, -1.929133858267710000 ) ) ;
#19381=ORIENTED_EDGE ( 'NONE', *, *, #3385, .T. ) ;
#19382=CARTESIAN_POINT ( 'NONE',  ( -1.901721518280075296, 3.267716535433071279, 0.9055118110236167750 ) ) ;
#19383=CARTESIAN_POINT ( 'NONE',  ( 0.000000000000000000, 3.267716535433071279, -1.417322834645664109 ) ) ;
#19384=EDGE_CURVE ( 'NONE', #39693, #39803, #5795, .T. ) ;
#19385=CARTESIAN_POINT ( 'NONE',  ( 0.000000000000000000, 3.267716535433071279, 1.889763779527550369 ) ) ;
#19386=CARTESIAN_POINT ( 'NONE',  ( 1.636583440222563857, 0.000000000000000000, 0.7480314960629872445 ) ) ;
#19388=ORIENTED_EDGE ( 'NONE', *, *, #10469, .F. ) ;
#19389=VECTOR ( 'NONE', #26268, 39.37007874015748143 ) ;
#19394=VECTOR ( 'NONE', #18357, 39.37007874015748143 ) ;
#19397=DIRECTION ( 'NONE',  ( 1.734723475976806848E-16, 0.000000000000000000, 1.000000000000000000 ) ) ;
#19399=VECTOR ( 'NONE', #2448, 39.37007874015748143 ) ;
#19400=VERTEX_POINT ( 'NONE', #29284 ) ;
#19401=VECTOR ( 'NONE', #38684, 39.37007874015748143 ) ;
#19402=EDGE_CURVE ( 'NONE', #7644, #35147, #33934, .T. ) ;
#19403=EDGE_LOOP ( 'NONE', ( #37260, #21867, #16422, #25324 ) ) ;
#19404=CARTESIAN_POINT ( 'NONE',  ( -1.091055626815042645, 3.346456692913386100, -7.512581982576723358E-16 ) ) ;
#19405=EDGE_LOOP ( 'NONE', ( #25369, #15022, #15880, #44109 ) ) ;
#19412=ORIENTED_EDGE ( 'NONE', *, *, #12916, .F. ) ;
#19413=ORIENTED_EDGE ( 'NONE', *, *, #49137, .F. ) ;
#19414=ORIENTED_EDGE ( 'NONE', *, *, #22416, .F. ) ;
#19415=DIRECTION ( 'NONE',  ( 1.734723475976806848E-16, 0.000000000000000000, 1.000000000000000000 ) ) ;
#19416=CARTESIAN_POINT ( 'NONE',  ( -0.8942052331142552601, 0.000000000000000000, -0.6299212598425177889 ) ) ;
#19418=ORIENTED_EDGE ( 'NONE', *, *, #46128, .F. ) ;
#19420=LINE ( 'NONE', #3693, #30220 ) ;
#19421=LINE ( 'NONE', #34688, #22822 ) ;
#19422=EDGE_CURVE ( 'NONE', #32147, #20825, #2177, .T. ) ;
#19423=ORIENTED_EDGE ( 'NONE', *, *, #5451, .T. ) ;
#19424=ORIENTED_EDGE ( 'NONE', *, *, #3547, .T. ) ;
#19427=LINE ( 'NONE', #24079, #48374 ) ;
#19428=EDGE_CURVE ( 'NONE', #23628, #32481, #18431, .T. ) ;
#19432=CARTESIAN_POINT ( 'NONE',  ( -1.091055626815042645, 3.256072117181358472, 2.192599532798640283 ) ) ;
#19433=VECTOR ( 'NONE', #34408, 39.37007874015748143 ) ;
#19435=AXIS2_PLACEMENT_3D ( 'NONE', #1558, #45657, #1809 ) ;
#19436=DIRECTION ( 'NONE',  ( 0.000000000000000000, 0.000000000000000000, -1.000000000000000000 ) ) ;
#19441=VECTOR ( 'NONE', #4380, 39.37007874015748143 ) ;
#19442=DIRECTION ( 'NONE',  ( -0.000000000000000000, 1.000000000000000000, -0.000000000000000000 ) ) ;
#19443=VECTOR ( 'NONE', #15072, 39.37007874015748143 ) ;
#19445=EDGE_CURVE ( 'NONE', #35668, #31067, #46025, .T. ) ;
#19447=ORIENTED_EDGE ( 'NONE', *, *, #19307, .F. ) ;
#19448=ORIENTED_EDGE ( 'NONE', *, *, #2853, .T. ) ;
#19449=VECTOR ( 'NONE', #21354, 39.37007874015748143 ) ;
#19452=VERTEX_POINT ( 'NONE', #42917 ) ;
#19454=DIRECTION ( 'NONE',  ( -0.000000000000000000, 1.000000000000000000, -0.000000000000000000 ) ) ;
#19456=CARTESIAN_POINT ( 'NONE',  ( -2.165354330708661568, 3.346456692913386100, -6.146657985744592735E-16 ) ) ;
#19457=LINE ( 'NONE', #46058, #27816 ) ;
#19458=ORIENTED_EDGE ( 'NONE', *, *, #11162, .T. ) ;
#19461=EDGE_CURVE ( 'NONE', #11818, #2547, #31317, .T. ) ;
#19462=ORIENTED_EDGE ( 'NONE', *, *, #44012, .T. ) ;
#19464=EDGE_CURVE ( 'NONE', #3461, #3180, #46692, .T. ) ;
#19465=CARTESIAN_POINT ( 'NONE',  ( 1.833433833923351353, 3.267716535433071279, -1.259842519685035800 ) ) ;
#19466=CARTESIAN_POINT ( 'NONE',  ( 0.2727639067037604392, 3.267716535433071279, -0.9842519685039348154 ) ) ;
#19469=VECTOR ( 'NONE', #19143, 39.37007874015748143 ) ;
#19470=CARTESIAN_POINT ( 'NONE',  ( -0.2727639067037607723, 3.267716535433071279, -1.417322834645664331 ) ) ;
#19471=CARTESIAN_POINT ( 'NONE',  ( -2.162130742952123263, 3.346456692913386100, 0.1181102362204704270 ) ) ;
#19473=VECTOR ( 'NONE', #34353, 39.37007874015748143 ) ;
#19476=PLANE ( 'NONE',  #42010 ) ;
#19477=ORIENTED_EDGE ( 'NONE', *, *, #4587, .T. ) ;
#19478=DIRECTION ( 'NONE',  ( 1.734723475976806848E-16, 0.000000000000000000, 1.000000000000000000 ) ) ;
#19479=VECTOR ( 'NONE', #34686, 39.37007874015748143 ) ;
#19480=DIRECTION ( 'NONE',  ( 1.000000000000000000, -0.000000000000000000, 0.000000000000000000 ) ) ;
#19481=LINE ( 'NONE', #35244, #4576 ) ;
#19482=CIRCLE ( 'NONE', #41755, 2.165354330708661568 ) ;
#19483=AXIS2_PLACEMENT_3D ( 'NONE', #37104, #48666, #962 ) ;
#19485=EDGE_LOOP ( 'NONE', ( #43588, #47346, #11802, #7044 ) ) ;
#19486=CARTESIAN_POINT ( 'NONE',  ( 0.1968503937007874405, 3.267716535433071279, 0.000000000000000000 ) ) ;
#19488=VERTEX_POINT ( 'NONE', #30809 ) ;
#19490=CARTESIAN_POINT ( 'NONE',  ( -0.5455278134075214336, 0.000000000000000000, 2.007874015748021268 ) ) ;
#19491=EDGE_CURVE ( 'NONE', #28656, #29807, #23304, .T. ) ;
#19492=DIRECTION ( 'NONE',  ( -1.000000000000000000, 0.000000000000000000, -0.000000000000000000 ) ) ;
#19493=CARTESIAN_POINT ( 'NONE',  ( 1.015142113812069979, 3.267716535433071279, 1.417322834645662777 ) ) ;
#19494=EDGE_LOOP ( 'NONE', ( #40256, #22363, #14944, #36696 ) ) ;
#19497=EDGE_CURVE ( 'NONE', #13500, #7335, #43428, .T. ) ;
#19498=EDGE_CURVE ( 'NONE', #38358, #41084, #19421, .T. ) ;
#19499=LINE ( 'NONE', #8149, #28984 ) ;
#19500=ORIENTED_EDGE ( 'NONE', *, *, #35245, .T. ) ;
#19501=EDGE_CURVE ( 'NONE', #27924, #12064, #15809, .T. ) ;
#19504=VERTEX_POINT ( 'NONE', #39567 ) ;
#19505=CARTESIAN_POINT ( 'NONE',  ( -3.414809992080329023E-17, 3.267716535433071279, -0.1968503937007874405 ) ) ;
#19506=VECTOR ( 'NONE', #39413, 39.37007874015748143 ) ;
#19507=ORIENTED_EDGE ( 'NONE', *, *, #42291, .T. ) ;
#19508=VERTEX_POINT ( 'NONE', #7568 ) ;
#19509=DIRECTION ( 'NONE',  ( -0.000000000000000000, 1.000000000000000000, -0.000000000000000000 ) ) ;
#19510=VERTEX_POINT ( 'NONE', #23556 ) ;
#19512=DIRECTION ( 'NONE',  ( -0.000000000000000000, 1.000000000000000000, -0.000000000000000000 ) ) ;
#19514=DIRECTION ( 'NONE',  ( 0.000000000000000000, 0.000000000000000000, -1.000000000000000000 ) ) ;
#19516=CARTESIAN_POINT ( 'NONE',  ( -1.198202975868768005, 3.267716535433071279, 1.732283464566920950 ) ) ;
#19517=VECTOR ( 'NONE', #24139, 39.37007874015748143 ) ;
#19518=LINE ( 'NONE', #50963, #28618 ) ;
#19519=CARTESIAN_POINT ( 'NONE',  ( 1.363819533518803251, 0.000000000000000000, 1.417322834645662777 ) ) ;
#19520=ORIENTED_EDGE ( 'NONE', *, *, #13771, .T. ) ;
#19521=DIRECTION ( 'NONE',  ( 1.000000000000000000, -0.000000000000000000, 0.000000000000000000 ) ) ;
#19523=CARTESIAN_POINT ( 'NONE',  ( 0.000000000000000000, 3.267716535433071279, 2.047244094488179567 ) ) ;
#19524=ORIENTED_EDGE ( 'NONE', *, *, #4519, .F. ) ;
#19526=ADVANCED_FACE ( 'NONE', ( #14813 ), #46523, .F. ) ;
#19527=DIRECTION ( 'NONE',  ( 1.000000000000000000, 0.000000000000000000, -3.469446951953613696E-16 ) ) ;
#19528=EDGE_LOOP ( 'NONE', ( #14046, #40050, #41308, #13962 ) ) ;
#19529=CARTESIAN_POINT ( 'NONE',  ( 0.2727639067037602172, 3.267716535433071279, -1.929133858267710000 ) ) ;
#19530=FACE_OUTER_BOUND ( 'NONE', #45533, .T. ) ;
#19532=FACE_OUTER_BOUND ( 'NONE', #33171, .T. ) ;
#19538=VERTEX_POINT ( 'NONE', #50370 ) ;
#19539=VECTOR ( 'NONE', #29130, 39.37007874015748143 ) ;
#19540=VECTOR ( 'NONE', #18474, 39.37007874015748143 ) ;
#19541=AXIS2_PLACEMENT_3D ( 'NONE', #34715, #30841, #46552 ) ;
#19545=VERTEX_POINT ( 'NONE', #3948 ) ;
#19546=DIRECTION ( 'NONE',  ( -0.000000000000000000, 1.000000000000000000, -0.000000000000000000 ) ) ;
#19547=EDGE_CURVE ( 'NONE', #17945, #4326, #19680, .T. ) ;
#19548=CARTESIAN_POINT ( 'NONE',  ( -1.636583440222563635, 0.000000000000000000, 0.3149606299212578953 ) ) ;
#19550=FACE_OUTER_BOUND ( 'NONE', #9719, .T. ) ;
#19552=EDGE_LOOP ( 'NONE', ( #47274, #33574, #11698, #32176 ) ) ;
#19553=CARTESIAN_POINT ( 'NONE',  ( -0.8942052331142547050, 3.346456692913386100, 1.377952755905504256 ) ) ;
#19555=EDGE_LOOP ( 'NONE', ( #21533, #1332, #10348, #12321 ) ) ;
#19556=VERTEX_POINT ( 'NONE', #19174 ) ;
#19559=ORIENTED_EDGE ( 'NONE', *, *, #3877, .F. ) ;
#19561=PLANE ( 'NONE',  #13056 ) ;
#19562=VERTEX_POINT ( 'NONE', #26674 ) ;
#19566=VERTEX_POINT ( 'NONE', #22812 ) ;
#19567=CARTESIAN_POINT ( 'NONE',  ( -1.091055626815042645, 0.000000000000000000, -0.8267716535433052849 ) ) ;
#19568=ORIENTED_EDGE ( 'NONE', *, *, #815, .F. ) ;
#19571=VECTOR ( 'NONE', #3741, 39.37007874015748143 ) ;
#19574=EDGE_LOOP ( 'NONE', ( #5002, #16017, #31114, #49856 ) ) ;
#19576=DIRECTION ( 'NONE',  ( -1.000000000000000000, 0.000000000000000000, 1.734723475976806848E-16 ) ) ;
#19577=CARTESIAN_POINT ( 'NONE',  ( 1.091055626815042423, 3.346456692913386100, -1.259842519685035134 ) ) ;
#19579=VECTOR ( 'NONE', #2, 39.37007874015748143 ) ;
#19581=CARTESIAN_POINT ( 'NONE',  ( 1.909347346926324684, 0.000000000000000000, -0.3543307086614178592 ) ) ;
#19583=VERTEX_POINT ( 'NONE', #18936 ) ;
#19584=CARTESIAN_POINT ( 'NONE',  ( 0.5455278134075216556, 3.267716535433071279, 1.692913385826762873 ) ) ;
#19585=AXIS2_PLACEMENT_3D ( 'NONE', #38946, #14948, #7453 ) ;
#19586=ADVANCED_FACE ( 'NONE', ( #26925 ), #42672, .F. ) ;
#19589=EDGE_CURVE ( 'NONE', #39559, #46927, #28704, .T. ) ;
#19590=VECTOR ( 'NONE', #3473, 39.37007874015748143 ) ;
#19591=EDGE_LOOP ( 'NONE', ( #41178, #32573, #42674, #2348 ) ) ;
#19595=VERTEX_POINT ( 'NONE', #39818 ) ;
#19596=EDGE_CURVE ( 'NONE', #456, #26189, #32091, .T. ) ;
#19597=CARTESIAN_POINT ( 'NONE',  ( 0.1968503937007870241, 0.000000000000000000, -1.889763779527552146 ) ) ;
#19600=DIRECTION ( 'NONE',  ( -1.000000000000000000, 0.000000000000000000, 1.734723475976806848E-16 ) ) ;
#19601=ORIENTED_EDGE ( 'NONE', *, *, #47470, .T. ) ;
#19602=PLANE ( 'NONE',  #26054 ) ;
#19603=CARTESIAN_POINT ( 'NONE',  ( 0.000000000000000000, 3.267716535433071279, -1.732283464566923170 ) ) ;
#19605=VECTOR ( 'NONE', #47648, 39.37007874015748143 ) ;
#19607=ORIENTED_EDGE ( 'NONE', *, *, #23745, .F. ) ;
#19610=ORIENTED_EDGE ( 'NONE', *, *, #29369, .T. ) ;
#19611=ADVANCED_FACE ( 'NONE', ( #4454 ), #4962, .F. ) ;
#19612=CARTESIAN_POINT ( 'NONE',  ( 0.000000000000000000, 3.346456692913386100, 0.000000000000000000 ) ) ;
#19613=CARTESIAN_POINT ( 'NONE',  ( -1.712496953225537633, 3.346456692913386100, 1.417322834645662333 ) ) ;
#19614=CARTESIAN_POINT ( 'NONE',  ( -0.3486774197067339376, 3.346456692913386100, 2.204724409448808764 ) ) ;
#19615=VECTOR ( 'NONE', #25940, 39.37007874015748143 ) ;
#19616=VERTEX_POINT ( 'NONE', #20189 ) ;
#19617=VECTOR ( 'NONE', #50542, 39.37007874015748143 ) ;
#19618=LINE ( 'NONE', #30750, #19579 ) ;
#19620=ORIENTED_EDGE ( 'NONE', *, *, #4908, .F. ) ;
#19621=VECTOR ( 'NONE', #26755, 39.37007874015748143 ) ;
#19623=ORIENTED_EDGE ( 'NONE', *, *, #29759, .F. ) ;
#19624=ORIENTED_EDGE ( 'NONE', *, *, #29656, .F. ) ;
#19625=AXIS2_PLACEMENT_3D ( 'NONE', #42884, #30777, #31287 ) ;
#19626=EDGE_CURVE ( 'NONE', #37726, #11359, #8327, .T. ) ;
#19630=CARTESIAN_POINT ( 'NONE',  ( 0.8182917201112819283, 0.000000000000000000, -0.3543307086614175816 ) ) ;
#19631=DIRECTION ( 'NONE',  ( 0.000000000000000000, 0.000000000000000000, 1.000000000000000000 ) ) ;
#19633=ORIENTED_EDGE ( 'NONE', *, *, #26298, .T. ) ;
#19634=CARTESIAN_POINT ( 'NONE',  ( -1.536664496436148184E-16, 3.267716535433071279, -0.8267716535433052849 ) ) ;
#19635=PLANE ( 'NONE',  #40800 ) ;
#19636=ORIENTED_EDGE ( 'NONE', *, *, #19946, .F. ) ;
#19637=DIRECTION ( 'NONE',  ( -0.000000000000000000, 1.000000000000000000, -0.000000000000000000 ) ) ;
#19638=CARTESIAN_POINT ( 'NONE',  ( 0.000000000000000000, 3.267716535433071279, 1.732283464566921172 ) ) ;
#19640=VECTOR ( 'NONE', #182, 39.37007874015748143 ) ;
#19641=DIRECTION ( 'NONE',  ( 0.000000000000000000, -1.000000000000000000, 0.000000000000000000 ) ) ;
#19642=PLANE ( 'NONE',  #8757 ) ;
#19644=ORIENTED_EDGE ( 'NONE', *, *, #11674, .T. ) ;
#19648=AXIS2_PLACEMENT_3D ( 'NONE', #40775, #1270, #48219 ) ;
#19649=EDGE_LOOP ( 'NONE', ( #4946, #15693, #29560, #17786 ) ) ;
#19650=EDGE_CURVE ( 'NONE', #6147, #33328, #24842, .T. ) ;
#19654=FACE_OUTER_BOUND ( 'NONE', #27164, .T. ) ;
#19657=VERTEX_POINT ( 'NONE', #20706 ) ;
#19660=ORIENTED_EDGE ( 'NONE', *, *, #28837, .T. ) ;
#19663=AXIS2_PLACEMENT_3D ( 'NONE', #28814, #48647, #24442 ) ;
#19664=DIRECTION ( 'NONE',  ( -1.000000000000000000, -0.000000000000000000, -0.000000000000000000 ) ) ;
#19669=EDGE_CURVE ( 'NONE', #10859, #34607, #4714, .T. ) ;
#19670=ORIENTED_EDGE ( 'NONE', *, *, #20108, .F. ) ;
#19671=EDGE_LOOP ( 'NONE', ( #27535, #19015, #38058, #32747 ) ) ;
#19673=LINE ( 'NONE', #9281, #19105 ) ;
#19674=DIRECTION ( 'NONE',  ( -1.000000000000000000, 0.000000000000000000, 0.000000000000000000 ) ) ;
#19676=EDGE_LOOP ( 'NONE', ( #13440, #33132, #46346, #44578 ) ) ;
#19678=DIRECTION ( 'NONE',  ( -1.000000000000000000, 0.000000000000000000, 1.734723475976806848E-16 ) ) ;
#19680=LINE ( 'NONE', #27427, #48317 ) ;
#19681=ORIENTED_EDGE ( 'NONE', *, *, #5565, .T. ) ;
#19682=VERTEX_POINT ( 'NONE', #28191 ) ;
#19683=CARTESIAN_POINT ( 'NONE',  ( 1.015142113812069091, 3.267716535433071279, -1.417322834645664331 ) ) ;
#19685=VECTOR ( 'NONE', #16653, 39.37007874015748143 ) ;
#19687=CARTESIAN_POINT ( 'NONE',  ( 0.2727639067037604947, 0.000000000000000000, -0.4724409448818886470 ) ) ;
#19689=( NAMED_UNIT ( * ) PLANE_ANGLE_UNIT ( ) SI_UNIT ( $, .RADIAN. ) );
#19690=LINE ( 'NONE', #35454, #40101 ) ;
#19691=VERTEX_POINT ( 'NONE', #25097 ) ;
#19694=VERTEX_POINT ( 'NONE', #36212 ) ;
#19695=CARTESIAN_POINT ( 'NONE',  ( 0.8182917201112819283, 3.346456692913386100, -0.1574803149606301411 ) ) ;
#19698=VECTOR ( 'NONE', #21806, 39.37007874015748143 ) ;
#19699=VECTOR ( 'NONE', #33390, 39.37007874015748143 ) ;
#19701=LINE ( 'NONE', #27701, #22852 ) ;
#19702=AXIS2_PLACEMENT_3D ( 'NONE', #6767, #49830, #26632 ) ;
#19703=CARTESIAN_POINT ( 'NONE',  ( 0.7423782071083087075, 3.346456692913386100, -0.3149606299212593941 ) ) ;
#19705=ORIENTED_EDGE ( 'NONE', *, *, #47490, .F. ) ;
#19706=EDGE_CURVE ( 'NONE', #6435, #20003, #20968, .T. ) ;
#19707=AXIS2_PLACEMENT_3D ( 'NONE', #22033, #29258, #2413 ) ;
#19709=LINE ( 'NONE', #35721, #46684 ) ;
#19710=CARTESIAN_POINT ( 'NONE',  ( 0.1968503937007872462, 3.346456692913386100, -1.771653543307081025 ) ) ;
#19712=LINE ( 'NONE', #43196, #21964 ) ;
#19713=DIRECTION ( 'NONE',  ( 1.734723475976806848E-16, -0.000000000000000000, 1.000000000000000000 ) ) ;
#19714=ORIENTED_EDGE ( 'NONE', *, *, #50437, .T. ) ;
#19715=CARTESIAN_POINT ( 'NONE',  ( 0.7423782071083087075, 0.000000000000000000, 0.9448818897637746295 ) ) ;
#19716=CARTESIAN_POINT ( 'NONE',  ( -0.3486774197067339376, 0.000000000000000000, 2.204724409448808764 ) ) ;
#19722=VECTOR ( 'NONE', #18620, 39.37007874015748143 ) ;
#19723=ORIENTED_EDGE ( 'NONE', *, *, #41500, .T. ) ;
#19724=CARTESIAN_POINT ( 'NONE',  ( 1.363819533518803473, 3.267716535433071279, -2.365849761790805980E-16 ) ) ;
#19725=FACE_OUTER_BOUND ( 'NONE', #43447, .T. ) ;
#19726=EDGE_CURVE ( 'NONE', #5813, #49431, #14495, .T. ) ;
#19727=LINE ( 'NONE', #43977, #43168 ) ;
#19728=ORIENTED_EDGE ( 'NONE', *, *, #2705, .T. ) ;
#19729=LINE ( 'NONE', #15855, #34574 ) ;
#19730=ORIENTED_EDGE ( 'NONE', *, *, #2340, .F. ) ;
#19731=DIRECTION ( 'NONE',  ( -1.000000000000000000, 0.000000000000000000, 1.734723475976806848E-16 ) ) ;
#19732=AXIS2_PLACEMENT_3D ( 'NONE', #14253, #30261, #37256 ) ;
#19733=DIRECTION ( 'NONE',  ( 1.000000000000000000, 0.000000000000000000, 0.000000000000000000 ) ) ;
#19735=DIRECTION ( 'NONE',  ( -0.000000000000000000, 0.000000000000000000, 1.000000000000000000 ) ) ;
#19737=ORIENTED_EDGE ( 'NONE', *, *, #48073, .F. ) ;
#19742=LINE ( 'NONE', #30370, #30986 ) ;
#19743=VECTOR ( 'NONE', #42539, 39.37007874015748143 ) ;
#19744=CARTESIAN_POINT ( 'NONE',  ( 0.1968503937007878568, 3.267716535433071279, 2.156388021673882438 ) ) ;
#19746=EDGE_LOOP ( 'NONE', ( #35291, #26851, #32639, #35826 ) ) ;
#19747=ORIENTED_EDGE ( 'NONE', *, *, #14329, .T. ) ;
#19749=EDGE_CURVE ( 'NONE', #31800, #8483, #6243, .T. ) ;
#19750=DIRECTION ( 'NONE',  ( 1.734723475976806848E-16, -0.000000000000000000, 1.000000000000000000 ) ) ;
#19751=ORIENTED_EDGE ( 'NONE', *, *, #2882, .F. ) ;
#19752=CIRCLE ( 'NONE', #2311, 2.106299212598425008 ) ;
#19754=VERTEX_POINT ( 'NONE', #1602 ) ;
#19755=ORIENTED_EDGE ( 'NONE', *, *, #33370, .T. ) ;
#19756=DIRECTION ( 'NONE',  ( 0.000000000000000000, 0.000000000000000000, -1.000000000000000000 ) ) ;
#19758=EDGE_CURVE ( 'NONE', #50824, #40528, #10623, .T. ) ;
#19761=EDGE_LOOP ( 'NONE', ( #21113, #19448, #49463, #8129 ) ) ;
#19762=ORIENTED_EDGE ( 'NONE', *, *, #31034, .F. ) ;
#19763=CARTESIAN_POINT ( 'NONE',  ( 1.636583440222563635, 3.346456692913386100, -1.141732283464564013 ) ) ;
#19764=VERTEX_POINT ( 'NONE', #37747 ) ;
#19767=DIRECTION ( 'NONE',  ( -0.000000000000000000, 0.000000000000000000, 1.000000000000000000 ) ) ;
#19768=LINE ( 'NONE', #12809, #7758 ) ;
#19769=VECTOR ( 'NONE', #33260, 39.37007874015748143 ) ;
#19770=DIRECTION ( 'NONE',  ( 1.734723475976806848E-16, -0.000000000000000000, 1.000000000000000000 ) ) ;
#19773=ORIENTED_EDGE ( 'NONE', *, *, #42528, .T. ) ;
#19775=AXIS2_PLACEMENT_3D ( 'NONE', #30488, #21982, #10857 ) ;
#19777=DIRECTION ( 'NONE',  ( 1.000000000000000000, 0.000000000000000000, -3.469446951953613696E-16 ) ) ;
#19780=CARTESIAN_POINT ( 'NONE',  ( 0.4696143004045479352, 3.267716535433071279, 0.7874015748031454320 ) ) ;
#19783=CARTESIAN_POINT ( 'NONE',  ( 0.5455278134075212115, 0.000000000000000000, -1.259842519685035134 ) ) ;
#19786=CARTESIAN_POINT ( 'NONE',  ( -0.5455278134075214336, 3.267716535433071279, 2.204724409448808764 ) ) ;
#19789=LINE ( 'NONE', #39934, #15721 ) ;
#19790=DIRECTION ( 'NONE',  ( -0.000000000000000000, 1.000000000000000000, -0.000000000000000000 ) ) ;
#19791=DIRECTION ( 'NONE',  ( 1.000000000000000000, -0.000000000000000000, 0.000000000000000000 ) ) ;
#19792=DIRECTION ( 'NONE',  ( 0.000000000000000000, 1.000000000000000000, 0.000000000000000000 ) ) ;
#19794=ORIENTED_EDGE ( 'NONE', *, *, #33712, .F. ) ;
#19796=LINE ( 'NONE', #23682, #32017 ) ;
#19798=DIRECTION ( 'NONE',  ( 0.000000000000000000, -1.000000000000000000, 0.000000000000000000 ) ) ;
#19799=DIRECTION ( 'NONE',  ( -0.000000000000000000, 1.000000000000000000, -0.000000000000000000 ) ) ;
#19800=VERTEX_POINT ( 'NONE', #29217 ) ;
#19802=DIRECTION ( 'NONE',  ( -0.000000000000000000, 0.000000000000000000, 1.000000000000000000 ) ) ;
#19803=VECTOR ( 'NONE', #14005, 39.37007874015748143 ) ;
#19804=ORIENTED_EDGE ( 'NONE', *, *, #18005, .F. ) ;
#19805=LINE ( 'NONE', #15188, #14218 ) ;
#19807=ORIENTED_EDGE ( 'NONE', *, *, #15275, .T. ) ;
#19808=ORIENTED_EDGE ( 'NONE', *, *, #21473, .T. ) ;
#19809=CARTESIAN_POINT ( 'NONE',  ( 0.5455278134075211005, 3.267716535433071279, -9.463399047163218249E-17 ) ) ;
#19810=VERTEX_POINT ( 'NONE', #18368 ) ;
#19812=CARTESIAN_POINT ( 'NONE',  ( -1.091055626815042201, 0.000000000000000000, 1.259842519685033357 ) ) ;
#19813=EDGE_CURVE ( 'NONE', #31004, #9761, #10113, .T. ) ;
#19814=EDGE_CURVE ( 'NONE', #37232, #15390, #49810, .T. ) ;
#19815=ORIENTED_EDGE ( 'NONE', *, *, #14796, .F. ) ;
#19818=ADVANCED_FACE ( 'NONE', ( #49052 ), #29731, .F. ) ;
#19819=CARTESIAN_POINT ( 'NONE',  ( 0.000000000000000000, 3.267716535433071279, -2.401574803149598036 ) ) ;
#19820=ORIENTED_EDGE ( 'NONE', *, *, #6024, .T. ) ;
#19821=CARTESIAN_POINT ( 'NONE',  ( -0.3486774197067340486, 3.267716535433071279, 0.1181102362204703021 ) ) ;
#19822=EDGE_LOOP ( 'NONE', ( #2656, #10805, #1936, #12608 ) ) ;
#19823=CARTESIAN_POINT ( 'NONE',  ( 1.636583440222563857, 3.267716535433071279, -0.8267716535433055070 ) ) ;
#19825=DIRECTION ( 'NONE',  ( 1.000000000000000000, 0.000000000000000000, -3.469446951953613696E-16 ) ) ;
#19826=VERTEX_POINT ( 'NONE', #17859 ) ;
#19828=LINE ( 'NONE', #51023, #45084 ) ;
#19829=DIRECTION ( 'NONE',  ( 0.000000000000000000, 0.000000000000000000, -1.000000000000000000 ) ) ;
#19830=CARTESIAN_POINT ( 'NONE',  ( -0.8182917201112819283, 3.346456692913386100, -1.102362204724405492 ) ) ;
#19831=ADVANCED_FACE ( 'NONE', ( #45449 ), #25855, .F. ) ;
#19833=LINE ( 'NONE', #40247, #34713 ) ;
#19835=ADVANCED_FACE ( 'NONE', ( #9860 ), #18115, .F. ) ;
#19836=VECTOR ( 'NONE', #3692, 39.37007874015748143 ) ;
#19837=LINE ( 'NONE', #40500, #3719 ) ;
#19838=ORIENTED_EDGE ( 'NONE', *, *, #25037, .F. ) ;
#19842=PLANE ( 'NONE',  #16814 ) ;
#19845=VERTEX_POINT ( 'NONE', #2621 ) ;
#19846=FACE_OUTER_BOUND ( 'NONE', #21550, .T. ) ;
#19848=ORIENTED_EDGE ( 'NONE', *, *, #18521, .F. ) ;
#19849=DIRECTION ( 'NONE',  ( -3.469446951953613696E-16, 0.000000000000000000, -1.000000000000000000 ) ) ;
#19850=ORIENTED_EDGE ( 'NONE', *, *, #3046, .F. ) ;
#19851=LINE ( 'NONE', #35111, #733 ) ;
#19858=EDGE_LOOP ( 'NONE', ( #45662, #43688, #47050, #48639 ) ) ;
#19860=CARTESIAN_POINT ( 'NONE',  ( 1.560669927219590303, 3.346456692913386100, -1.299212598425193210 ) ) ;
#19862=CARTESIAN_POINT ( 'NONE',  ( -0.8182917201112819283, 3.267716535433071279, -0.1574803149606301411 ) ) ;
#19863=AXIS2_PLACEMENT_3D ( 'NONE', #36612, #4595, #47668 ) ;
#19864=VECTOR ( 'NONE', #37080, 39.37007874015748143 ) ;
#19865=ORIENTED_EDGE ( 'NONE', *, *, #46384, .F. ) ;
#19867=PLANE ( 'NONE',  #49266 ) ;
#19868=DIRECTION ( 'NONE',  ( 0.000000000000000000, 0.000000000000000000, 1.000000000000000000 ) ) ;
#19869=ORIENTED_EDGE ( 'NONE', *, *, #44663, .T. ) ;
#19870=LINE ( 'NONE', #33575, #40609 ) ;
#19871=ADVANCED_FACE ( 'NONE', ( #42356 ), #34377, .F. ) ;
#19873=ORIENTED_EDGE ( 'NONE', *, *, #4455, .F. ) ;
#19874=ORIENTED_EDGE ( 'NONE', *, *, #49825, .T. ) ;
#19879=DIRECTION ( 'NONE',  ( -1.000000000000000000, 0.000000000000000000, 0.000000000000000000 ) ) ;
#19880=AXIS2_PLACEMENT_3D ( 'NONE', #44301, #8177, #47630 ) ;
#19881=DIRECTION ( 'NONE',  ( -0.000000000000000000, 0.000000000000000000, 1.000000000000000000 ) ) ;
#19882=CARTESIAN_POINT ( 'NONE',  ( -2.258024766633058622, 3.267716535433071279, 7.834097144030835427E-16 ) ) ;
#19883=LINE ( 'NONE', #271, #18130 ) ;
#19884=VERTEX_POINT ( 'NONE', #19614 ) ;
#19885=VERTEX_POINT ( 'NONE', #23241 ) ;
#19886=CARTESIAN_POINT ( 'NONE',  ( 2.378961647330872786, 0.000000000000000000, -0.3149606299212596716 ) ) ;
#19887=ORIENTED_EDGE ( 'NONE', *, *, #22215, .F. ) ;
#19888=LINE ( 'NONE', #20151, #30916 ) ;
#19889=CARTESIAN_POINT ( 'NONE',  ( -0.2727639067037602727, 0.000000000000000000, 1.535433070866133898 ) ) ;
#19890=EDGE_CURVE ( 'NONE', #14486, #27199, #31504, .T. ) ;
#19891=LINE ( 'NONE', #31027, #34138 ) ;
#19897=EDGE_CURVE ( 'NONE', #514, #39701, #15503, .T. ) ;
#19899=VECTOR ( 'NONE', #43203, 39.37007874015748143 ) ;
#19900=ORIENTED_EDGE ( 'NONE', *, *, #49175, .F. ) ;
#19901=CARTESIAN_POINT ( 'NONE',  ( -1.166969139818015977, 3.267716535433071279, -0.4724409448818886470 ) ) ;
#19904=DIRECTION ( 'NONE',  ( -1.000000000000000000, 0.000000000000000000, 1.734723475976806848E-16 ) ) ;
#19905=ORIENTED_EDGE ( 'NONE', *, *, #47048, .T. ) ;
#19906=VECTOR ( 'NONE', #34244, 39.37007874015748143 ) ;
#19907=ORIENTED_EDGE ( 'NONE', *, *, #20637, .T. ) ;
#19908=LINE ( 'NONE', #39802, #13893 ) ;
#19909=AXIS2_PLACEMENT_3D ( 'NONE', #12853, #48422, #32482 ) ;
#19911=FACE_OUTER_BOUND ( 'NONE', #20527, .T. ) ;
#19912=VERTEX_POINT ( 'NONE', #47204 ) ;
#19913=AXIS2_PLACEMENT_3D ( 'NONE', #26151, #25894, #49597 ) ;
#19914=LINE ( 'NONE', #16578, #2911 ) ;
#19915=CARTESIAN_POINT ( 'NONE',  ( 0.8182917201112817063, 3.346456692913386100, -1.417322834645664331 ) ) ;
#19916=CARTESIAN_POINT ( 'NONE',  ( 0.2727639067037610499, 3.346456692913386100, 1.102362204724404160 ) ) ;
#19919=EDGE_LOOP ( 'NONE', ( #16537, #26664, #16661, #7831 ) ) ;
#19921=CARTESIAN_POINT ( 'NONE',  ( -1.334208625815133553, 3.267716535433071279, 2.047244094488179567 ) ) ;
#19923=ORIENTED_EDGE ( 'NONE', *, *, #19749, .T. ) ;
#19924=DIRECTION ( 'NONE',  ( -3.469446951953613696E-16, 0.000000000000000000, -1.000000000000000000 ) ) ;
#19925=CARTESIAN_POINT ( 'NONE',  ( 0.4696143004045479352, 0.000000000000000000, -0.4724409448818886470 ) ) ;
#19928=EDGE_LOOP ( 'NONE', ( #22129, #38232, #17682, #36627 ) ) ;
#19929=CARTESIAN_POINT ( 'NONE',  ( -1.536664496436148184E-16, 3.346456692913386100, 0.4330708661417287386 ) ) ;
#19930=CARTESIAN_POINT ( 'NONE',  ( -1.166969139818015533, 3.346456692913386100, 0.4724409448818871482 ) ) ;
#19932=ORIENTED_EDGE ( 'NONE', *, *, #32079, .T. ) ;
#19934=CARTESIAN_POINT ( 'NONE',  ( -1.363819533518803029, 0.000000000000000000, 1.102362204724404160 ) ) ;
#19937=EDGE_CURVE ( 'NONE', #43573, #4193, #34622, .T. ) ;
#19938=DIRECTION ( 'NONE',  ( 0.000000000000000000, -1.000000000000000000, 0.000000000000000000 ) ) ;
#19939=ORIENTED_EDGE ( 'NONE', *, *, #34707, .T. ) ;
#19944=DIRECTION ( 'NONE',  ( 1.734723475976806848E-16, -0.000000000000000000, 1.000000000000000000 ) ) ;
#19945=VECTOR ( 'NONE', #3892, 39.37007874015748143 ) ;
#19946=EDGE_CURVE ( 'NONE', #30890, #30042, #38992, .T. ) ;
#19948=ADVANCED_FACE ( 'NONE', ( #7749 ), #3628, .F. ) ;
#19949=CARTESIAN_POINT ( 'NONE',  ( 1.558105373646058389, 3.346456692913386100, -1.417322834645665441 ) ) ;
#19950=EDGE_LOOP ( 'NONE', ( #39441, #6431, #42001, #13714 ) ) ;
#19952=AXIS2_PLACEMENT_3D ( 'NONE', #13667, #41043, #21666 ) ;
#19953=VECTOR ( 'NONE', #2949, 39.37007874015748143 ) ;
#19954=ORIENTED_EDGE ( 'NONE', *, *, #32175, .T. ) ;
#19955=DIRECTION ( 'NONE',  ( 1.734723475976806848E-16, 0.000000000000000000, 1.000000000000000000 ) ) ;
#19957=VECTOR ( 'NONE', #35298, 39.37007874015748143 ) ;
#19958=ADVANCED_FACE ( 'NONE', ( #3121 ), #39244, .F. ) ;
#19961=ORIENTED_EDGE ( 'NONE', *, *, #2597, .F. ) ;
#19963=EDGE_CURVE ( 'NONE', #39256, #19298, #22496, .T. ) ;
#19964=CARTESIAN_POINT ( 'NONE',  ( -0.07591351300297333182, 0.000000000000000000, 2.362204724409437961 ) ) ;
#19965=ORIENTED_EDGE ( 'NONE', *, *, #37937, .T. ) ;
#19967=DIRECTION ( 'NONE',  ( -0.000000000000000000, 1.000000000000000000, -0.000000000000000000 ) ) ;
#19970=ORIENTED_EDGE ( 'NONE', *, *, #3561, .F. ) ;
#19971=DIRECTION ( 'NONE',  ( 1.000000000000000000, 0.000000000000000000, 0.000000000000000000 ) ) ;
#19972=LINE ( 'NONE', #9135, #34100 ) ;
#19974=VERTEX_POINT ( 'NONE', #51053 ) ;
#19975=CARTESIAN_POINT ( 'NONE',  ( 1.091055626815042645, 0.000000000000000000, 0.1181102362204704270 ) ) ;
#19976=CARTESIAN_POINT ( 'NONE',  ( -1.195183497228115035E-16, 0.000000000000000000, -0.9448818897637765168 ) ) ;
#19977=ORIENTED_EDGE ( 'NONE', *, *, #36542, .F. ) ;
#19978=DIRECTION ( 'NONE',  ( -0.000000000000000000, 1.000000000000000000, -0.000000000000000000 ) ) ;
#19981=DIRECTION ( 'NONE',  ( 1.734723475976806848E-16, 0.000000000000000000, 1.000000000000000000 ) ) ;
#19984=VECTOR ( 'NONE', #16980, 39.37007874015748143 ) ;
#19986=VERTEX_POINT ( 'NONE', #31000 ) ;
#19987=CARTESIAN_POINT ( 'NONE',  ( 1.015142113812069313, 3.267716535433071279, -3.521981712565032882E-16 ) ) ;
#19990=AXIS2_PLACEMENT_3D ( 'NONE', #2630, #25612, #1612 ) ;
#19991=CARTESIAN_POINT ( 'NONE',  ( 1.363819533518803251, 0.000000000000000000, 0.7874015748031454320 ) ) ;
#19992=DIRECTION ( 'NONE',  ( 1.734723475976806848E-16, 0.000000000000000000, 1.000000000000000000 ) ) ;
#19993=DIRECTION ( 'NONE',  ( -3.469446951953613696E-16, 0.000000000000000000, -1.000000000000000000 ) ) ;
#19995=VECTOR ( 'NONE', #29441, 39.37007874015748143 ) ;
#19996=EDGE_LOOP ( 'NONE', ( #1687, #43370, #41335, #16008 ) ) ;
#19997=VERTEX_POINT ( 'NONE', #16007 ) ;
#20000=LINE ( 'NONE', #24148, #17313 ) ;
#20001=PLANE ( 'NONE',  #2608 ) ;
#20002=FACE_BOUND ( 'NONE', #11363, .T. ) ;
#20003=VERTEX_POINT ( 'NONE', #28384 ) ;
#20004=CARTESIAN_POINT ( 'NONE',  ( 0.000000000000000000, 3.267716535433071279, 0.4330708661417290162 ) ) ;
#20005=ORIENTED_EDGE ( 'NONE', *, *, #45974, .T. ) ;
#20006=ORIENTED_EDGE ( 'NONE', *, *, #10533, .T. ) ;
#20008=ADVANCED_FACE ( 'NONE', ( #4139 ), #20121, .F. ) ;
#20011=ORIENTED_EDGE ( 'NONE', *, *, #17818, .F. ) ;
#20012=CARTESIAN_POINT ( 'NONE',  ( 0.000000000000000000, 3.267716535433071279, 1.377952755905504256 ) ) ;
#20013=ADVANCED_FACE ( 'NONE', ( #8520 ), #252, .F. ) ;
#20014=ORIENTED_EDGE ( 'NONE', *, *, #37763, .T. ) ;
#20018=CARTESIAN_POINT ( 'NONE',  ( -0.8182917201112814842, 3.346456692913386100, 0.9055118110236167750 ) ) ;
#20019=CIRCLE ( 'NONE', #48852, 2.165354330708661568 ) ;
#20021=CARTESIAN_POINT ( 'NONE',  ( 0.000000000000000000, 3.267716535433071279, 0.9055118110236164419 ) ) ;
#20022=ORIENTED_EDGE ( 'NONE', *, *, #20316, .T. ) ;
#20023=DIRECTION ( 'NONE',  ( 1.734723475976806848E-16, -0.000000000000000000, 1.000000000000000000 ) ) ;
#20024=PLANE ( 'NONE',  #39195 ) ;
#20025=DIRECTION ( 'NONE',  ( -1.000000000000000000, 0.000000000000000000, 0.000000000000000000 ) ) ;
#20026=AXIS2_PLACEMENT_3D ( 'NONE', #50570, #19881, #7517 ) ;
#20028=AXIS2_PLACEMENT_3D ( 'NONE', #18083, #46175, #26576 ) ;
#20032=ORIENTED_EDGE ( 'NONE', *, *, #43294, .F. ) ;
#20033=FACE_OUTER_BOUND ( 'NONE', #42586, .T. ) ;
#20036=CARTESIAN_POINT ( 'NONE',  ( 1.833433833923351353, 3.346456692913386100, 1.259842519685033135 ) ) ;
#20037=VECTOR ( 'NONE', #20023, 39.37007874015748143 ) ;
#20039=ORIENTED_EDGE ( 'NONE', *, *, #42981, .F. ) ;
#20041=EDGE_CURVE ( 'NONE', #33786, #43157, #44132, .T. ) ;
#20042=CARTESIAN_POINT ( 'NONE',  ( 2.021817418930639931, 3.346456692913386100, 0.5905511811023582691 ) ) ;
#20043=CARTESIAN_POINT ( 'NONE',  ( -0.3486774197067339376, 3.267716535433071279, -1.574803149606293529 ) ) ;
#20045=VERTEX_POINT ( 'NONE', #19862 ) ;
#20046=EDGE_CURVE ( 'NONE', #25164, #25916, #16970, .T. ) ;
#20048=ORIENTED_EDGE ( 'NONE', *, *, #29758, .F. ) ;
#20049=LINE ( 'NONE', #28314, #20470 ) ;
#20052=DIRECTION ( 'NONE',  ( -1.000000000000000000, 0.000000000000000000, 1.734723475976806848E-16 ) ) ;
#20053=EDGE_LOOP ( 'NONE', ( #41286, #24145, #47027, #42706 ) ) ;
#20054=EDGE_CURVE ( 'NONE', #850, #5596, #44390, .T. ) ;
#20055=FACE_OUTER_BOUND ( 'NONE', #35895, .T. ) ;
#20057=CARTESIAN_POINT ( 'NONE',  ( -0.5455278134075208785, 3.267716535433071279, 0.6299212598425164567 ) ) ;
#20058=VECTOR ( 'NONE', #13424, 39.37007874015748143 ) ;
#20059=PLANE ( 'NONE',  #39682 ) ;
#20061=CARTESIAN_POINT ( 'NONE',  ( -1.909347346926324906, 0.000000000000000000, 1.417322834645662333 ) ) ;
#20063=EDGE_LOOP ( 'NONE', ( #50837, #36993, #23936, #3433 ) ) ;
#20065=VECTOR ( 'NONE', #20079, 39.37007874015748143 ) ;
#20067=VECTOR ( 'NONE', #26511, 39.37007874015748143 ) ;
#20068=CARTESIAN_POINT ( 'NONE',  ( -0.07591351300297333182, 3.346456692913386100, 0.1574803149606283648 ) ) ;
#20069=VERTEX_POINT ( 'NONE', #8264 ) ;
#20071=ADVANCED_FACE ( 'NONE', ( #4903, #48483, #13171, #35889, #4652, #39757, #36402, #12390, #16263, #32024, #28125, #16788, #778, #518, #47715, #16527, #32279, #24527, #20647, #1028, #32541, #48232, #12915, #9034, #40532, #5155, #20907, #9289, #21934, #21171, #9546, #13676, #33057, #40789, #37693, #36920, #17799, #48735, #41050, #1794, #1544, #13418, #5415, #2306, #17297, #33566, #29157, #5673, #17545, #25035, #22187, #44634, #13933, #18307, #45644, #41549, #49251, #34063, #37433, #18059, #14175, #2563, #49500, #45141, #33309, #26052, #5920, #45393, #29679, #10055, #44890, #25797, #41805, #33819, #6181, #25540, #37942, #29928, #48994, #29420, #9803, #10308, #25293, #6438, #21423, #41300, #37177, #21676, #49752, #14435, #2054, #34322, #6691, #23893, #26804, #656, #30183, #43497, #45900, #8151, #22439, #38197, #50254, #14941, #38695, #30688, #24150, #50009, #4529, #4270, #42299, #46401, #18818, #16149, #7201, #46653, #46155, #39639, #36032, #39895, #20002, #14690, #2817, #18568, #20269, #30944, #34567, #3315, #35768, #27755, #31909, #11071, #10563, #34813, #42054, #42556, #43749, #395, #50497, #47600, #19057, #12278, #28014, #30441, #8404, #15193, #26307, #10809, #26553, #6944, #12018, #22688, #22940, #38446, #3068, #29292, #44274, #36288, #24409, #4786, #5803, #44773, #8654, #40668, #20533, #12791, #24668, #47856, #45030, #16411, #36798, #41184, #17424, #13303, #5293, #21552, #9168, #40926, #37056, #16671, #9681, #16921, #40422, #48870, #28785, #25417, #8913, #28265, #40162, #5040, #1677, #28523, #36545, #909, #20786, #33189, #32944, #17175, #1421, #21046, #37313, #9426, #32420, #1164, #48111, #32683, #48621, #44524, #32163, #24918, #29034, #48365, #12527, #25172, #13052, #5550, #21302, #13557, #44010, #14309, #46283, #30063, #2691, #41934, #18442, #1932, #22320, #50135, #26433, #38072, #33943, #17935, #30316, #34447, #49384, #45522, #26684, #14822 ), #21811, .T. ) ;
#20073=VECTOR ( 'NONE', #29765, 39.37007874015748143 ) ;
#20074=DIRECTION ( 'NONE',  ( -3.469446951953613696E-16, 0.000000000000000000, -1.000000000000000000 ) ) ;
#20077=EDGE_LOOP ( 'NONE', ( #34291, #16094, #21458 ) ) ;
#20079=DIRECTION ( 'NONE',  ( 1.734723475976806848E-16, -0.000000000000000000, 1.000000000000000000 ) ) ;
#20080=PLANE ( 'NONE',  #9060 ) ;
#20083=DIRECTION ( 'NONE',  ( -3.469446951953613696E-16, 0.000000000000000000, -1.000000000000000000 ) ) ;
#20084=PLANE ( 'NONE',  #41840 ) ;
#20085=CARTESIAN_POINT ( 'NONE',  ( -1.636583440222563635, 0.000000000000000000, 0.1181102362204704270 ) ) ;
#20087=CARTESIAN_POINT ( 'NONE',  ( -1.439733046521777027, 3.267716535433071279, 1.377952755905504256 ) ) ;
#20088=LINE ( 'NONE', #35857, #13265 ) ;
#20090=VERTEX_POINT ( 'NONE', #37821 ) ;
#20091=ADVANCED_FACE ( 'NONE', ( #49131 ), #22821, .F. ) ;
#20092=CARTESIAN_POINT ( 'NONE',  ( -2.121605289024800722, 3.346456692913386100, 0.4330708661417290162 ) ) ;
#20094=ORIENTED_EDGE ( 'NONE', *, *, #38998, .T. ) ;
#20095=CARTESIAN_POINT ( 'NONE',  ( -0.8942052331142549271, 3.267716535433071279, 3.102397620449222481E-16 ) ) ;
#20100=VECTOR ( 'NONE', #33433, 39.37007874015748143 ) ;
#20102=VECTOR ( 'NONE', #39476, 39.37007874015748143 ) ;
#20103=DIRECTION ( 'NONE',  ( 1.000000000000000000, 0.000000000000000000, 0.000000000000000000 ) ) ;
#20107=EDGE_CURVE ( 'NONE', #38209, #19566, #30570, .T. ) ;
#20108=EDGE_CURVE ( 'NONE', #39410, #23414, #10697, .T. ) ;
#20110=DIRECTION ( 'NONE',  ( -1.000000000000000000, 0.000000000000000000, 0.000000000000000000 ) ) ;
#20114=FACE_OUTER_BOUND ( 'NONE', #28776, .T. ) ;
#20117=ORIENTED_EDGE ( 'NONE', *, *, #11761, .T. ) ;
#20118=ORIENTED_EDGE ( 'NONE', *, *, #36759, .T. ) ;
#20120=LINE ( 'NONE', #42852, #926 ) ;
#20121=PLANE ( 'NONE',  #3763 ) ;
#20123=EDGE_CURVE ( 'NONE', #50597, #35404, #10443, .T. ) ;
#20126=EDGE_CURVE ( 'NONE', #8254, #5726, #9552, .T. ) ;
#20127=CARTESIAN_POINT ( 'NONE',  ( 0.2727639067037609943, 0.000000000000000000, 1.850393700787392293 ) ) ;
#20128=CARTESIAN_POINT ( 'NONE',  ( -1.439733046521776583, 3.346456692913386100, 1.537421584259135443 ) ) ;
#20129=VERTEX_POINT ( 'NONE', #9937 ) ;
#20131=CARTESIAN_POINT ( 'NONE',  ( -0.5455278134075214336, 0.000000000000000000, 2.007874015748021268 ) ) ;
#20132=EDGE_CURVE ( 'NONE', #19764, #4018, #14059, .T. ) ;
#20134=VECTOR ( 'NONE', #14611, 39.37007874015748143 ) ;
#20136=SHAPE_DEFINITION_REPRESENTATION ( #46625, #15265 ) ;
#20137=AXIS2_PLACEMENT_3D ( 'NONE', #2286, #33544, #22420 ) ;
#20138=ORIENTED_EDGE ( 'NONE', *, *, #43309, .F. ) ;
#20140=VECTOR ( 'NONE', #4823, 39.37007874015748143 ) ;
#20141=PLANE ( 'NONE',  #28294 ) ;
#20142=DIRECTION ( 'NONE',  ( -1.000000000000000000, -0.000000000000000000, -0.000000000000000000 ) ) ;
#20143=DIRECTION ( 'NONE',  ( 1.000000000000000000, -0.000000000000000000, 0.000000000000000000 ) ) ;
#20144=ORIENTED_EDGE ( 'NONE', *, *, #34418, .F. ) ;
#20146=AXIS2_PLACEMENT_3D ( 'NONE', #364, #32387, #40390 ) ;
#20148=CARTESIAN_POINT ( 'NONE',  ( -1.712496953225537633, 0.000000000000000000, -1.102362204724405492 ) ) ;
#20150=VERTEX_POINT ( 'NONE', #2190 ) ;
#20151=CARTESIAN_POINT ( 'NONE',  ( -1.909347346926325129, 3.346456692913386100, -0.8893194486674343979 ) ) ;
#20152=LINE ( 'NONE', #27899, #29733 ) ;
#20154=CARTESIAN_POINT ( 'NONE',  ( -1.636583440222564301, 0.000000000000000000, -1.141732283464563791 ) ) ;
#20155=CARTESIAN_POINT ( 'NONE',  ( 0.7423782071083085965, 0.000000000000000000, -1.456692913385822630 ) ) ;
#20156=ORIENTED_EDGE ( 'NONE', *, *, #6922, .T. ) ;
#20157=PLANE ( 'NONE',  #15152 ) ;
#20158=ORIENTED_EDGE ( 'NONE', *, *, #20841, .T. ) ;
#20159=EDGE_LOOP ( 'NONE', ( #11248, #1998, #10312, #8160 ) ) ;
#20160=CARTESIAN_POINT ( 'NONE',  ( -1.985260859929297572, 3.346456692913386100, 0.3149606299212578953 ) ) ;
#20162=CARTESIAN_POINT ( 'NONE',  ( -0.8942052331142548161, 3.267716535433071279, 3.102397620449221988E-16 ) ) ;
#20163=EDGE_CURVE ( 'NONE', #16898, #12857, #41681, .T. ) ;
#20165=EDGE_CURVE ( 'NONE', #21513, #2854, #6319, .T. ) ;
#20166=CIRCLE ( 'NONE', #25981, 2.165354330708661568 ) ;
#20167=EDGE_CURVE ( 'NONE', #10246, #31232, #31840, .T. ) ;
#20168=VERTEX_POINT ( 'NONE', #8336 ) ;
#20169=VECTOR ( 'NONE', #49783, 39.37007874015748143 ) ;
#20170=DIRECTION ( 'NONE',  ( -1.000000000000000000, 0.000000000000000000, -0.000000000000000000 ) ) ;
#20171=VERTEX_POINT ( 'NONE', #43177 ) ;
#20173=ADVANCED_FACE ( 'NONE', ( #3957 ), #31075, .F. ) ;
#20174=VECTOR ( 'NONE', #25720, 39.37007874015748143 ) ;
#20175=VERTEX_POINT ( 'NONE', #39069 ) ;
#20176=LINE ( 'NONE', #24574, #36750 ) ;
#20177=DIRECTION ( 'NONE',  ( -0.000000000000000000, 1.000000000000000000, -0.000000000000000000 ) ) ;
#20179=EDGE_LOOP ( 'NONE', ( #3650, #8895, #41863, #43078 ) ) ;
#20181=ORIENTED_EDGE ( 'NONE', *, *, #46423, .F. ) ;
#20183=VECTOR ( 'NONE', #12149, 39.37007874015748143 ) ;
#20184=PLANE ( 'NONE',  #37889 ) ;
#20185=ORIENTED_EDGE ( 'NONE', *, *, #2198, .T. ) ;
#20188=CARTESIAN_POINT ( 'NONE',  ( 1.287906020515830585, 3.267716535433071279, 1.574803149606291974 ) ) ;
#20189=CARTESIAN_POINT ( 'NONE',  ( -1.363819533518803473, 3.346456692913386100, -1.732283464566922726 ) ) ;
#20191=EDGE_CURVE ( 'NONE', #43265, #29231, #19690, .T. ) ;
#20192=VERTEX_POINT ( 'NONE', #34948 ) ;
#20193=EDGE_CURVE ( 'NONE', #3832, #12397, #26906, .T. ) ;
#20195=DIRECTION ( 'NONE',  ( 1.734723475976806848E-16, -0.000000000000000000, 1.000000000000000000 ) ) ;
#20200=ORIENTED_EDGE ( 'NONE', *, *, #30975, .T. ) ;
#20201=EDGE_CURVE ( 'NONE', #49607, #28604, #3703, .T. ) ;
#20202=CARTESIAN_POINT ( 'NONE',  ( 1.833433833923351353, 3.346456692913386100, -0.6299212598425181220 ) ) ;
#20203=ORIENTED_EDGE ( 'NONE', *, *, #43277, .F. ) ;
#20205=CARTESIAN_POINT ( 'NONE',  ( 1.287906020515829919, 0.000000000000000000, -1.574803149606294417 ) ) ;
#20207=ADVANCED_FACE ( 'NONE', ( #15819 ), #47280, .F. ) ;
#20208=CARTESIAN_POINT ( 'NONE',  ( -1.091055626815042201, 0.000000000000000000, 1.259842519685033357 ) ) ;
#20209=DIRECTION ( 'NONE',  ( 1.734723475976806848E-16, -0.000000000000000000, 1.000000000000000000 ) ) ;
#20211=ORIENTED_EDGE ( 'NONE', *, *, #28042, .T. ) ;
#20212=ORIENTED_EDGE ( 'NONE', *, *, #3669, .F. ) ;
#20213=VECTOR ( 'NONE', #14904, 39.37007874015748143 ) ;
#20214=VECTOR ( 'NONE', #44046, 39.37007874015748143 ) ;
#20216=ORIENTED_EDGE ( 'NONE', *, *, #17911, .T. ) ;
#20217=LINE ( 'NONE', #4220, #21155 ) ;
#20218=CARTESIAN_POINT ( 'NONE',  ( 0.1968503937007873017, 3.346456692913386100, -0.9448818897637765168 ) ) ;
#20219=VECTOR ( 'NONE', #822, 39.37007874015748143 ) ;
#20220=DIRECTION ( 'NONE',  ( -1.000000000000000000, 0.000000000000000000, 1.734723475976806848E-16 ) ) ;
#20223=CIRCLE ( 'NONE', #42493, 2.106299212598425008 ) ;
#20225=FACE_OUTER_BOUND ( 'NONE', #7220, .T. ) ;
#20226=DIRECTION ( 'NONE',  ( 1.734723475976806848E-16, 0.000000000000000000, 1.000000000000000000 ) ) ;
#20231=CARTESIAN_POINT ( 'NONE',  ( -0.6214413264104945434, 3.267716535433071279, 2.156057715732901026E-16 ) ) ;
#20233=CARTESIAN_POINT ( 'NONE',  ( -0.8942052331142547050, 3.346456692913386100, 1.259842519685033357 ) ) ;
#20234=DIRECTION ( 'NONE',  ( -3.469446951953613696E-16, 0.000000000000000000, -1.000000000000000000 ) ) ;
#20237=EDGE_CURVE ( 'NONE', #47091, #48366, #30822, .T. ) ;
#20238=ORIENTED_EDGE ( 'NONE', *, *, #36893, .F. ) ;
#20239=FACE_BOUND ( 'NONE', #15416, .T. ) ;
#20240=LINE ( 'NONE', #49606, #6008 ) ;
#20245=CARTESIAN_POINT ( 'NONE',  ( 1.287906020515829919, 3.267716535433071279, -1.889763779527552368 ) ) ;
#20246=LINE ( 'NONE', #31891, #11976 ) ;
#20247=ADVANCED_FACE ( 'NONE', ( #12210 ), #42926, .F. ) ;
#20248=EDGE_LOOP ( 'NONE', ( #8162, #827, #33319, #46083 ) ) ;
#20252=CARTESIAN_POINT ( 'NONE',  ( 1.287906020515830141, 3.346456692913386100, 0.3149606299212578953 ) ) ;
#20253=AXIS2_PLACEMENT_3D ( 'NONE', #45407, #13947, #26068 ) ;
#20254=ORIENTED_EDGE ( 'NONE', *, *, #20431, .T. ) ;
#20255=DIRECTION ( 'NONE',  ( 1.000000000000000000, 0.000000000000000000, 0.000000000000000000 ) ) ;
#20256=CARTESIAN_POINT ( 'NONE',  ( -1.363819533518803473, 0.000000000000000000, -1.102362204724405270 ) ) ;
#20257=FACE_OUTER_BOUND ( 'NONE', #37614, .T. ) ;
#20258=AXIS2_PLACEMENT_3D ( 'NONE', #9026, #36912, #28636 ) ;
#20259=CARTESIAN_POINT ( 'NONE',  ( 0.000000000000000000, 3.267716535433071279, 0.000000000000000000 ) ) ;
#20260=VERTEX_POINT ( 'NONE', #15578 ) ;
#20262=ADVANCED_FACE ( 'NONE', ( #50381 ), #23826, .F. ) ;
#20264=LINE ( 'NONE', #32159, #34502 ) ;
#20265=CARTESIAN_POINT ( 'NONE',  ( -1.732283464566932052, 3.267716535433071279, -1.299212598425193210 ) ) ;
#20266=AXIS2_PLACEMENT_3D ( 'NONE', #24271, #12137, #36146 ) ;
#20267=CARTESIAN_POINT ( 'NONE',  ( -0.8182917201112814842, 3.346456692913386100, 0.4724409448818872592 ) ) ;
#20269=FACE_BOUND ( 'NONE', #47857, .T. ) ;
#20270=VECTOR ( 'NONE', #35433, 39.37007874015748143 ) ;
#20271=ORIENTED_EDGE ( 'NONE', *, *, #29869, .T. ) ;
#20272=EDGE_CURVE ( 'NONE', #48050, #20926, #38574, .T. ) ;
#20277=ORIENTED_EDGE ( 'NONE', *, *, #42920, .F. ) ;
#20279=CARTESIAN_POINT ( 'NONE',  ( -0.07591351300297359550, 3.346456692913386100, -2.047244094488181343 ) ) ;
#20281=LINE ( 'NONE', #148, #29567 ) ;
#20282=ADVANCED_FACE ( 'NONE', ( #47023 ), #11199, .F. ) ;
#20283=LINE ( 'NONE', #24422, #23604 ) ;
#20284=LINE ( 'NONE', #27772, #16842 ) ;
#20286=CARTESIAN_POINT ( 'NONE',  ( 0.4696143004045484348, 3.267716535433071279, -1.629301903132388985E-16 ) ) ;
#20287=FACE_OUTER_BOUND ( 'NONE', #42350, .T. ) ;
#20288=CARTESIAN_POINT ( 'NONE',  ( 0.2727639067037602172, 0.000000000000000000, -2.244094488188969727 ) ) ;
#20289=VECTOR ( 'NONE', #42753, 39.37007874015748143 ) ;
#20290=ORIENTED_EDGE ( 'NONE', *, *, #49428, .F. ) ;
#20291=CARTESIAN_POINT ( 'NONE',  ( -1.985260859929297572, 0.000000000000000000, 0.9448818897637749625 ) ) ;
#20292=AXIS2_PLACEMENT_3D ( 'NONE', #22391, #31148, #38144 ) ;
#20293=CARTESIAN_POINT ( 'NONE',  ( 0.1968503937007870241, 3.346456692913386100, -2.204724409448811429 ) ) ;
#20294=VECTOR ( 'NONE', #44759, 39.37007874015748143 ) ;
#20296=ORIENTED_EDGE ( 'NONE', *, *, #15240, .T. ) ;
#20297=PLANE ( 'NONE',  #27299 ) ;
#20298=LINE ( 'NONE', #8684, #49988 ) ;
#20299=VERTEX_POINT ( 'NONE', #38822 ) ;
#20302=FACE_OUTER_BOUND ( 'NONE', #15319, .T. ) ;
#20304=AXIS2_PLACEMENT_3D ( 'NONE', #46643, #12068, #11311 ) ;
#20305=EDGE_CURVE ( 'NONE', #24856, #28374, #27437, .T. ) ;
#20307=ORIENTED_EDGE ( 'NONE', *, *, #15432, .T. ) ;
#20309=EDGE_LOOP ( 'NONE', ( #29912, #25378, #1934, #15798 ) ) ;
#20310=DIRECTION ( 'NONE',  ( -0.000000000000000000, 1.000000000000000000, -0.000000000000000000 ) ) ;
#20312=DIRECTION ( 'NONE',  ( 1.000000000000000000, -0.000000000000000000, 0.000000000000000000 ) ) ;
#20314=CARTESIAN_POINT ( 'NONE',  ( -1.636583440222563635, 3.267716535433071279, 2.839019714148966584E-16 ) ) ;
#20315=ADVANCED_FACE ( 'NONE', ( #9099 ), #4722, .F. ) ;
#20316=EDGE_CURVE ( 'NONE', #49974, #47433, #24082, .T. ) ;
#20320=VERTEX_POINT ( 'NONE', #8846 ) ;
#20322=ORIENTED_EDGE ( 'NONE', *, *, #26416, .T. ) ;
#20327=CARTESIAN_POINT ( 'NONE',  ( -1.602125192864240821, 3.267716535433071279, -1.456692913385822186 ) ) ;
#20328=VECTOR ( 'NONE', #31988, 39.37007874015748143 ) ;
#20331=EDGE_CURVE ( 'NONE', #20408, #22204, #24853, .T. ) ;
#20332=LINE ( 'NONE', #19809, #12531 ) ;
#20334=CARTESIAN_POINT ( 'NONE',  ( 0.2727639067037604392, 3.346456692913386100, -0.3543307086614173040 ) ) ;
#20338=VERTEX_POINT ( 'NONE', #16342 ) ;
#20340=AXIS2_PLACEMENT_3D ( 'NONE', #41672, #2936, #33435 ) ;
#20341=DIRECTION ( 'NONE',  ( -0.000000000000000000, 1.000000000000000000, -0.000000000000000000 ) ) ;
#20342=ORIENTED_EDGE ( 'NONE', *, *, #43309, .T. ) ;
#20344=EDGE_CURVE ( 'NONE', #11074, #5663, #36223, .T. ) ;
#20345=ORIENTED_EDGE ( 'NONE', *, *, #21026, .F. ) ;
#20346=LINE ( 'NONE', #5109, #23567 ) ;
#20347=CARTESIAN_POINT ( 'NONE',  ( 0.2727639067037604947, 3.346456692913386100, 0.7874015748031454320 ) ) ;
#20350=EDGE_LOOP ( 'NONE', ( #33957, #47205 ) ) ;
#20355=CARTESIAN_POINT ( 'NONE',  ( -1.363819533518803473, 3.267716535433071279, 2.365849761790805980E-16 ) ) ;
#20358=EDGE_CURVE ( 'NONE', #45000, #33320, #32874, .T. ) ;
#20364=ORIENTED_EDGE ( 'NONE', *, *, #45524, .T. ) ;
#20365=AXIS2_PLACEMENT_3D ( 'NONE', #17196, #25191, #37075 ) ;
#20366=DIRECTION ( 'NONE',  ( 1.734723475976806848E-16, -0.000000000000000000, 1.000000000000000000 ) ) ;
#20367=ORIENTED_EDGE ( 'NONE', *, *, #1683, .F. ) ;
#20368=EDGE_CURVE ( 'NONE', #38168, #44408, #4464, .T. ) ;
#20369=DIRECTION ( 'NONE',  ( -0.000000000000000000, 1.000000000000000000, -0.000000000000000000 ) ) ;
#20370=LINE ( 'NONE', #11604, #31983 ) ;
#20372=LINE ( 'NONE', #20629, #37611 ) ;
#20373=ORIENTED_EDGE ( 'NONE', *, *, #32691, .F. ) ;
#20374=ADVANCED_FACE ( 'NONE', ( #20978 ), #12459, .F. ) ;
#20377=FACE_BOUND ( 'NONE', #21107, .T. ) ;
#20379=DIRECTION ( 'NONE',  ( -1.000000000000000000, -0.000000000000000000, -0.000000000000000000 ) ) ;
#20380=AXIS2_PLACEMENT_3D ( 'NONE', #13887, #18523, #29636 ) ;
#20382=CARTESIAN_POINT ( 'NONE',  ( -0.07591351300297333182, 3.267716535433071279, 2.362204724409437961 ) ) ;
#20386=ORIENTED_EDGE ( 'NONE', *, *, #6783, .F. ) ;
#20387=CARTESIAN_POINT ( 'NONE',  ( 1.015142113812069313, 0.000000000000000000, -1.102362204724405714 ) ) ;
#20388=CARTESIAN_POINT ( 'NONE',  ( 1.287906020515830363, 3.267716535433071279, -4.468321617281356063E-16 ) ) ;
#20391=CARTESIAN_POINT ( 'NONE',  ( -0.8182917201112814842, 0.000000000000000000, 0.4724409448818872592 ) ) ;
#20392=VECTOR ( 'NONE', #33940, 39.37007874015748143 ) ;
#20393=VECTOR ( 'NONE', #5958, 39.37007874015748143 ) ;
#20394=EDGE_CURVE ( 'NONE', #41467, #39512, #36989, .T. ) ;
#20395=ORIENTED_EDGE ( 'NONE', *, *, #27830, .F. ) ;
#20396=DIRECTION ( 'NONE',  ( -1.000000000000000000, 0.000000000000000000, 0.000000000000000000 ) ) ;
#20398=EDGE_LOOP ( 'NONE', ( #21465, #37372, #26837, #21136 ) ) ;
#20399=PRODUCT_CONTEXT ( 'NONE', #40795, 'mechanical' ) ;
#20400=EDGE_CURVE ( 'NONE', #45906, #22792, #36476, .T. ) ;
#20401=VERTEX_POINT ( 'NONE', #48804 ) ;
#20402=CARTESIAN_POINT ( 'NONE',  ( 0.7423782071083084855, 3.346456692913386100, -1.971134437475891454 ) ) ;
#20403=DIRECTION ( 'NONE',  ( -1.000000000000000000, 0.000000000000000000, 1.734723475976806848E-16 ) ) ;
#20404=EDGE_CURVE ( 'NONE', #1425, #18884, #40088, .T. ) ;
#20405=ADVANCED_FACE ( 'NONE', ( #12722 ), #32351, .F. ) ;
#20406=PLANE ( 'NONE',  #6352 ) ;
#20408=VERTEX_POINT ( 'NONE', #44204 ) ;
#20411=PLANE ( 'NONE',  #35376 ) ;
#20420=ORIENTED_EDGE ( 'NONE', *, *, #369, .F. ) ;
#20423=EDGE_CURVE ( 'NONE', #50372, #34255, #49321, .T. ) ;
#20424=ORIENTED_EDGE ( 'NONE', *, *, #40647, .F. ) ;
#20425=DIRECTION ( 'NONE',  ( -1.000000000000000000, 0.000000000000000000, 1.734723475976806848E-16 ) ) ;
#20426=CARTESIAN_POINT ( 'NONE',  ( 0.000000000000000000, 3.267716535433071279, 0.2755905511810994302 ) ) ;
#20428=AXIS2_PLACEMENT_3D ( 'NONE', #32394, #29783, #41659 ) ;
#20430=AXIS2_PLACEMENT_3D ( 'NONE', #34298, #30418, #42277 ) ;
#20431=EDGE_CURVE ( 'NONE', #46441, #919, #5740, .T. ) ;
#20433=EDGE_CURVE ( 'NONE', #26916, #2822, #37502, .T. ) ;
#20437=ORIENTED_EDGE ( 'NONE', *, *, #30970, .F. ) ;
#20438=CARTESIAN_POINT ( 'NONE',  ( 0.000000000000000000, 3.267716535433071279, 0.000000000000000000 ) ) ;
#20439=ORIENTED_EDGE ( 'NONE', *, *, #49081, .T. ) ;
#20443=DIRECTION ( 'NONE',  ( 0.000000000000000000, 0.000000000000000000, -1.000000000000000000 ) ) ;
#20444=VECTOR ( 'NONE', #39457, 39.37007874015748143 ) ;
#20445=ORIENTED_EDGE ( 'NONE', *, *, #49691, .F. ) ;
#20446=EDGE_LOOP ( 'NONE', ( #32002, #19254, #6189, #31594 ) ) ;
#20447=ORIENTED_EDGE ( 'NONE', *, *, #17152, .F. ) ;
#20448=DIRECTION ( 'NONE',  ( -1.000000000000000000, -0.000000000000000000, -0.000000000000000000 ) ) ;
#20450=ORIENTED_EDGE ( 'NONE', *, *, #20656, .T. ) ;
#20451=LINE ( 'NONE', #32089, #7506 ) ;
#20452=DIRECTION ( 'NONE',  ( 1.000000000000000000, -0.000000000000000000, 0.000000000000000000 ) ) ;
#20453=CARTESIAN_POINT ( 'NONE',  ( 0.6363476328836782381, 3.346456692913386100, 2.007874015748021268 ) ) ;
#20455=EDGE_LOOP ( 'NONE', ( #39134, #44887, #32234, #38601 ) ) ;
#20456=DIRECTION ( 'NONE',  ( -0.000000000000000000, 1.000000000000000000, -0.000000000000000000 ) ) ;
#20457=DIRECTION ( 'NONE',  ( -0.000000000000000000, 1.000000000000000000, -0.000000000000000000 ) ) ;
#20458=CARTESIAN_POINT ( 'NONE',  ( -0.2727639067037602172, 0.000000000000000000, 1.732283464566921172 ) ) ;
#20463=LINE ( 'NONE', #12212, #12598 ) ;
#20467=DIRECTION ( 'NONE',  ( 0.000000000000000000, 0.000000000000000000, 1.000000000000000000 ) ) ;
#20468=DIRECTION ( 'NONE',  ( 1.734723475976806848E-16, 0.000000000000000000, 1.000000000000000000 ) ) ;
#20469=EDGE_CURVE ( 'NONE', #7160, #42304, #1863, .T. ) ;
#20470=VECTOR ( 'NONE', #16716, 39.37007874015748143 ) ;
#20471=EDGE_CURVE ( 'NONE', #30246, #50120, #37247, .T. ) ;
#20472=DIRECTION ( 'NONE',  ( 1.734723475976806848E-16, -0.000000000000000000, 1.000000000000000000 ) ) ;
#20474=ORIENTED_EDGE ( 'NONE', *, *, #18867, .F. ) ;
#20476=EDGE_CURVE ( 'NONE', #25478, #9639, #21488, .T. ) ;
#20477=DIRECTION ( 'NONE',  ( 1.000000000000000000, 0.000000000000000000, 0.000000000000000000 ) ) ;
#20478=VECTOR ( 'NONE', #40224, 39.37007874015748143 ) ;
#20479=ORIENTED_EDGE ( 'NONE', *, *, #2140, .F. ) ;
#20480=LINE ( 'NONE', #16616, #16210 ) ;
#20481=CARTESIAN_POINT ( 'NONE',  ( 2.378961647330872786, 0.000000000000000000, -0.1968503937007886062 ) ) ;
#20482=ADVANCED_FACE ( 'NONE', ( #41365 ), #5989, .F. ) ;
#20483=AXIS2_PLACEMENT_3D ( 'NONE', #1416, #29028, #8398 ) ;
#20484=VECTOR ( 'NONE', #50599, 39.37007874015748143 ) ;
#20485=VECTOR ( 'NONE', #33769, 39.37007874015748143 ) ;
#20486=DIRECTION ( 'NONE',  ( -0.000000000000000000, 1.000000000000000000, -0.000000000000000000 ) ) ;
#20487=CARTESIAN_POINT ( 'NONE',  ( 0.2727639067037604947, 3.346456692913386100, 0.4724409448818868706 ) ) ;
#20488=DIRECTION ( 'NONE',  ( -0.000000000000000000, 1.000000000000000000, -0.000000000000000000 ) ) ;
#20489=VERTEX_POINT ( 'NONE', #41619 ) ;
#20491=ADVANCED_FACE ( 'NONE', ( #33381 ), #49060, .F. ) ;
#20492=VECTOR ( 'NONE', #8181, 39.37007874015748143 ) ;
#20494=ORIENTED_EDGE ( 'NONE', *, *, #42509, .F. ) ;
#20495=LINE ( 'NONE', #3989, #23212 ) ;
#20496=EDGE_CURVE ( 'NONE', #46412, #3654, #10121, .T. ) ;
#20502=EDGE_CURVE ( 'NONE', #30196, #39803, #34129, .T. ) ;
#20505=ORIENTED_EDGE ( 'NONE', *, *, #34511, .F. ) ;
#20506=LINE ( 'NONE', #24379, #50178 ) ;
#20507=FACE_OUTER_BOUND ( 'NONE', #9674, .T. ) ;
#20508=ORIENTED_EDGE ( 'NONE', *, *, #47497, .T. ) ;
#20509=EDGE_CURVE ( 'NONE', #11981, #18410, #45458, .T. ) ;
#20511=CARTESIAN_POINT ( 'NONE',  ( 1.015142113812069091, 3.346456692913386100, -2.047244094488181343 ) ) ;
#20512=LINE ( 'NONE', #24127, #5754 ) ;
#20513=CARTESIAN_POINT ( 'NONE',  ( 1.833433833923351353, 3.267716535433071279, -0.9448818897637765168 ) ) ;
#20514=VECTOR ( 'NONE', #10234, 39.37007874015748143 ) ;
#20516=ORIENTED_EDGE ( 'NONE', *, *, #44645, .F. ) ;
#20518=FACE_OUTER_BOUND ( 'NONE', #39141, .T. ) ;
#20519=DIRECTION ( 'NONE',  ( -0.000000000000000000, 1.000000000000000000, -0.000000000000000000 ) ) ;
#20521=FACE_OUTER_BOUND ( 'NONE', #33526, .T. ) ;
#20522=DIRECTION ( 'NONE',  ( -3.469446951953613696E-16, 0.000000000000000000, -1.000000000000000000 ) ) ;
#20523=CARTESIAN_POINT ( 'NONE',  ( -1.909347346926324462, 3.267716535433071279, 0.4724409448818871482 ) ) ;
#20526=VECTOR ( 'NONE', #23173, 39.37007874015748143 ) ;
#20527=EDGE_LOOP ( 'NONE', ( #2509, #42270, #15174, #3881 ) ) ;
#20528=ORIENTED_EDGE ( 'NONE', *, *, #16828, .T. ) ;
#20529=CARTESIAN_POINT ( 'NONE',  ( 0.5455278134075211005, 3.346456692913386100, -0.8267716535433055070 ) ) ;
#20532=FACE_OUTER_BOUND ( 'NONE', #49905, .T. ) ;
#20533=FACE_BOUND ( 'NONE', #8457, .T. ) ;
#20534=ORIENTED_EDGE ( 'NONE', *, *, #24129, .F. ) ;
#20535=LINE ( 'NONE', #36548, #21634 ) ;
#20536=ORIENTED_EDGE ( 'NONE', *, *, #49576, .T. ) ;
#20537=ORIENTED_EDGE ( 'NONE', *, *, #29753, .T. ) ;
#20539=DIRECTION ( 'NONE',  ( -0.000000000000000000, 1.000000000000000000, -0.000000000000000000 ) ) ;
#20540=ORIENTED_EDGE ( 'NONE', *, *, #45204, .F. ) ;
#20543=ORIENTED_EDGE ( 'NONE', *, *, #6588, .T. ) ;
#20544=EDGE_CURVE ( 'NONE', #11143, #15306, #33884, .T. ) ;
#20547=CARTESIAN_POINT ( 'NONE',  ( 0.000000000000000000, 3.267716535433071279, 1.259842519685033357 ) ) ;
#20549=DIRECTION ( 'NONE',  ( -1.000000000000000000, 0.000000000000000000, 0.000000000000000000 ) ) ;
#20550=VECTOR ( 'NONE', #38060, 39.37007874015748143 ) ;
#20551=FACE_OUTER_BOUND ( 'NONE', #18304, .T. ) ;
#20552=CARTESIAN_POINT ( 'NONE',  ( -0.6214413264104939882, 3.267716535433071279, 0.4724409448818872592 ) ) ;
#20555=CARTESIAN_POINT ( 'NONE',  ( -0.2727639067037608278, 3.346456692913386100, -0.9842519685039344823 ) ) ;
#20558=VECTOR ( 'NONE', #20726, 39.37007874015748143 ) ;
#20559=ORIENTED_EDGE ( 'NONE', *, *, #31812, .F. ) ;
#20561=EDGE_CURVE ( 'NONE', #17428, #728, #1524, .T. ) ;
#20562=DIRECTION ( 'NONE',  ( -0.000000000000000000, 1.000000000000000000, -0.000000000000000000 ) ) ;
#20564=FACE_OUTER_BOUND ( 'NONE', #22185, .T. ) ;
#20565=CARTESIAN_POINT ( 'NONE',  ( 0.000000000000000000, 3.267716535433071279, -0.6692913385826760875 ) ) ;
#20566=VECTOR ( 'NONE', #20755, 39.37007874015748143 ) ;
#20567=CARTESIAN_POINT ( 'NONE',  ( 0.1968503937007877735, 3.267716535433071279, -6.829619984160670372E-17 ) ) ;
#20571=CARTESIAN_POINT ( 'NONE',  ( 0.000000000000000000, 3.267716535433071279, -2.443628662382284489 ) ) ;
#20572=VECTOR ( 'NONE', #7181, 39.37007874015748143 ) ;
#20573=EDGE_LOOP ( 'NONE', ( #23284, #49991, #29950, #6259 ) ) ;
#20574=FACE_BOUND ( 'NONE', #44047, .T. ) ;
#20575=FACE_OUTER_BOUND ( 'NONE', #33151, .T. ) ;
#20576=LINE ( 'NONE', #28567, #25099 ) ;
#20579=ORIENTED_EDGE ( 'NONE', *, *, #39029, .T. ) ;
#20580=VERTEX_POINT ( 'NONE', #28369 ) ;
#20581=CARTESIAN_POINT ( 'NONE',  ( 1.287906020515830141, 0.000000000000000000, 1.259842519685033357 ) ) ;
#20584=ORIENTED_EDGE ( 'NONE', *, *, #8959, .F. ) ;
#20585=LINE ( 'NONE', #39953, #7479 ) ;
#20587=VERTEX_POINT ( 'NONE', #36645 ) ;
#20588=LINE ( 'NONE', #968, #26591 ) ;
#20590=EDGE_LOOP ( 'NONE', ( #28326, #25739, #6122, #37279 ) ) ;
#20592=VERTEX_POINT ( 'NONE', #9785 ) ;
#20594=LINE ( 'NONE', #19812, #41897 ) ;
#20596=ORIENTED_EDGE ( 'NONE', *, *, #45356, .F. ) ;
#20598=EDGE_CURVE ( 'NONE', #3086, #44277, #20372, .T. ) ;
#20599=ORIENTED_EDGE ( 'NONE', *, *, #20994, .F. ) ;
#20600=VECTOR ( 'NONE', #26661, 39.37007874015748143 ) ;
#20601=CARTESIAN_POINT ( 'NONE',  ( 1.091055626815042867, 3.267716535433071279, -1.892679809432644882E-16 ) ) ;
#20602=ORIENTED_EDGE ( 'NONE', *, *, #9181, .F. ) ;
#20603=LINE ( 'NONE', #24227, #12897 ) ;
#20606=EDGE_CURVE ( 'NONE', #24946, #18566, #16766, .T. ) ;
#20608=EDGE_CURVE ( 'NONE', #39964, #43653, #21123, .T. ) ;
#20610=ORIENTED_EDGE ( 'NONE', *, *, #39354, .F. ) ;
#20612=FACE_OUTER_BOUND ( 'NONE', #42597, .T. ) ;
#20613=DIRECTION ( 'NONE',  ( -3.469446951953613696E-16, 0.000000000000000000, -1.000000000000000000 ) ) ;
#20614=CARTESIAN_POINT ( 'NONE',  ( 0.5455278134075216556, 3.346456692913386100, 1.377952755905504256 ) ) ;
#20615=DIRECTION ( 'NONE',  ( -0.000000000000000000, 1.000000000000000000, -0.000000000000000000 ) ) ;
#20616=CARTESIAN_POINT ( 'NONE',  ( -0.8942052331142547050, 0.000000000000000000, 1.574803149606291974 ) ) ;
#20622=DIRECTION ( 'NONE',  ( 1.000000000000000000, -0.000000000000000000, 0.000000000000000000 ) ) ;
#20623=EDGE_CURVE ( 'NONE', #17342, #44964, #33286, .T. ) ;
#20624=ORIENTED_EDGE ( 'NONE', *, *, #47141, .T. ) ;
#20626=CARTESIAN_POINT ( 'NONE',  ( 0.000000000000000000, 3.346456692913386100, 0.000000000000000000 ) ) ;
#20629=CARTESIAN_POINT ( 'NONE',  ( 0.000000000000000000, 3.267716535433071279, -1.574803149606293529 ) ) ;
#20630=ORIENTED_EDGE ( 'NONE', *, *, #18867, .T. ) ;
#20631=EDGE_CURVE ( 'NONE', #6824, #30018, #49927, .T. ) ;
#20632=LINE ( 'NONE', #14161, #18353 ) ;
#20633=FACE_BOUND ( 'NONE', #29973, .T. ) ;
#20634=EDGE_LOOP ( 'NONE', ( #10489, #9042, #50986, #16775 ) ) ;
#20636=AXIS2_PLACEMENT_3D ( 'NONE', #44625, #32535, #25026 ) ;
#20637=EDGE_CURVE ( 'NONE', #17906, #47500, #44873, .T. ) ;
#20638=ORIENTED_EDGE ( 'NONE', *, *, #40897, .F. ) ;
#20639=CARTESIAN_POINT ( 'NONE',  ( -0.8182917201112819283, 0.000000000000000000, -0.6692913385826760875 ) ) ;
#20640=LINE ( 'NONE', #1018, #48641 ) ;
#20644=ADVANCED_FACE ( 'NONE', ( #9016 ), #48975, .F. ) ;
#20645=DIRECTION ( 'NONE',  ( 0.000000000000000000, -1.000000000000000000, 0.000000000000000000 ) ) ;
#20646=CARTESIAN_POINT ( 'NONE',  ( 1.091055626815042423, 3.346456692913386100, -1.574803149606294417 ) ) ;
#20647=FACE_BOUND ( 'NONE', #29836, .T. ) ;
#20648=CARTESIAN_POINT ( 'NONE',  ( 0.4696143004045484348, 3.346456692913386100, 0.9055118110236167750 ) ) ;
#20650=ORIENTED_EDGE ( 'NONE', *, *, #8332, .F. ) ;
#20653=EDGE_LOOP ( 'NONE', ( #40123, #37628, #35953, #44188 ) ) ;
#20656=EDGE_CURVE ( 'NONE', #14441, #43305, #5138, .T. ) ;
#20657=AXIS2_PLACEMENT_3D ( 'NONE', #35914, #20670, #1310 ) ;
#20658=DIRECTION ( 'NONE',  ( 1.734723475976806848E-16, 0.000000000000000000, 1.000000000000000000 ) ) ;
#20660=FACE_OUTER_BOUND ( 'NONE', #22708, .T. ) ;
#20661=EDGE_CURVE ( 'NONE', #48582, #17616, #8754, .T. ) ;
#20665=FACE_OUTER_BOUND ( 'NONE', #28358, .T. ) ;
#20666=PLANE ( 'NONE',  #18068 ) ;
#20668=AXIS2_PLACEMENT_3D ( 'NONE', #34748, #27238, #46832 ) ;
#20669=CARTESIAN_POINT ( 'NONE',  ( 1.287906020515829919, 3.249608194809333384, -2.086614173228340086 ) ) ;
#20670=DIRECTION ( 'NONE',  ( -1.000000000000000000, 0.000000000000000000, 1.734723475976806848E-16 ) ) ;
#20671=CARTESIAN_POINT ( 'NONE',  ( 1.909347346926324684, 0.000000000000000000, 0.4724409448818868706 ) ) ;
#20672=CARTESIAN_POINT ( 'NONE',  ( -1.363819533518803473, 0.000000000000000000, 1.535433070866133232 ) ) ;
#20673=CARTESIAN_POINT ( 'NONE',  ( -0.2727639067037610499, 3.346456692913386100, -2.047244094488181343 ) ) ;
#20674=ORIENTED_EDGE ( 'NONE', *, *, #28016, .T. ) ;
#20675=CARTESIAN_POINT ( 'NONE',  ( 1.287906020515830141, 0.000000000000000000, -0.5118110236220471121 ) ) ;
#20676=LINE ( 'NONE', #32575, #47444 ) ;
#20679=PLANE ( 'NONE',  #18323 ) ;
#20680=LINE ( 'NONE', #11916, #47555 ) ;
#20682=EDGE_LOOP ( 'NONE', ( #5338, #36659, #19062 ) ) ;
#20683=EDGE_CURVE ( 'NONE', #49793, #10381, #30439, .T. ) ;
#20686=VERTEX_POINT ( 'NONE', #4886 ) ;
#20687=ADVANCED_FACE ( 'NONE', ( #37412 ), #18288, .F. ) ;
#20688=ORIENTED_EDGE ( 'NONE', *, *, #18618, .T. ) ;
#20689=VECTOR ( 'NONE', #32768, 39.37007874015748143 ) ;
#20690=DIRECTION ( 'NONE',  ( -0.000000000000000000, 0.000000000000000000, 1.000000000000000000 ) ) ;
#20691=DIRECTION ( 'NONE',  ( 1.000000000000000000, 0.000000000000000000, 0.000000000000000000 ) ) ;
#20692=PLANE ( 'NONE',  #18619 ) ;
#20693=VECTOR ( 'NONE', #25229, 39.37007874015748143 ) ;
#20694=EDGE_CURVE ( 'NONE', #40166, #43305, #18797, .T. ) ;
#20695=EDGE_CURVE ( 'NONE', #36994, #21756, #2036, .T. ) ;
#20696=ORIENTED_EDGE ( 'NONE', *, *, #47787, .T. ) ;
#20697=ORIENTED_EDGE ( 'NONE', *, *, #39185, .F. ) ;
#20700=EDGE_LOOP ( 'NONE', ( #44944, #48515, #5680, #12387 ) ) ;
#20702=ADVANCED_FACE ( 'NONE', ( #22169 ), #10543, .F. ) ;
#20703=DIRECTION ( 'NONE',  ( 1.000000000000000000, 0.000000000000000000, -3.469446951953613696E-16 ) ) ;
#20704=PLANE ( 'NONE',  #4638 ) ;
#20705=AXIS2_PLACEMENT_3D ( 'NONE', #21038, #12518, #9159 ) ;
#20706=CARTESIAN_POINT ( 'NONE',  ( 1.833433833923351353, 3.346456692913386100, -1.259842519685035800 ) ) ;
#20707=EDGE_CURVE ( 'NONE', #45906, #4245, #41783, .T. ) ;
#20708=AXIS2_PLACEMENT_3D ( 'NONE', #9195, #21841, #37593 ) ;
#20709=ORIENTED_EDGE ( 'NONE', *, *, #10988, .F. ) ;
#20711=LINE ( 'NONE', #32608, #43086 ) ;
#20712=DIRECTION ( 'NONE',  ( -1.000000000000000000, 0.000000000000000000, 0.000000000000000000 ) ) ;
#20714=DIRECTION ( 'NONE',  ( -0.000000000000000000, 1.000000000000000000, -0.000000000000000000 ) ) ;
#20717=EDGE_LOOP ( 'NONE', ( #22782, #17806, #20445, #43484 ) ) ;
#20719=CARTESIAN_POINT ( 'NONE',  ( 1.287906020515830141, 3.267716535433071279, 0.7480314960629872445 ) ) ;
#20722=ADVANCED_FACE ( 'NONE', ( #6420 ), #42279, .F. ) ;
#20723=CARTESIAN_POINT ( 'NONE',  ( 1.363819533518803251, 0.000000000000000000, -0.4724409448818889246 ) ) ;
#20724=CARTESIAN_POINT ( 'NONE',  ( 0.1968503937007878568, 0.000000000000000000, 2.204724409448808764 ) ) ;
#20726=DIRECTION ( 'NONE',  ( 1.734723475976806848E-16, -0.000000000000000000, 1.000000000000000000 ) ) ;
#20727=EDGE_LOOP ( 'NONE', ( #34329, #37618, #7324, #18879 ) ) ;
#20729=EDGE_CURVE ( 'NONE', #35776, #41844, #45376, .T. ) ;
#20730=CARTESIAN_POINT ( 'NONE',  ( -0.8182917201112819283, 0.000000000000000000, -2.047244094488181343 ) ) ;
#20732=ORIENTED_EDGE ( 'NONE', *, *, #43415, .T. ) ;
#20736=VECTOR ( 'NONE', #19243, 39.37007874015748143 ) ;
#20739=VECTOR ( 'NONE', #6301, 39.37007874015748143 ) ;
#20740=DIRECTION ( 'NONE',  ( -3.469446951953613696E-16, 0.000000000000000000, -1.000000000000000000 ) ) ;
#20741=VERTEX_POINT ( 'NONE', #45879 ) ;
#20745=ORIENTED_EDGE ( 'NONE', *, *, #32740, .F. ) ;
#20746=AXIS2_PLACEMENT_3D ( 'NONE', #26896, #18910, #38784 ) ;
#20747=CARTESIAN_POINT ( 'NONE',  ( 1.091055626815042645, 3.346456692913386100, 0.6299212598425161236 ) ) ;
#20749=CARTESIAN_POINT ( 'NONE',  ( -1.909347346926324462, 3.346456692913386100, 1.102362204724404160 ) ) ;
#20750=VERTEX_POINT ( 'NONE', #14416 ) ;
#20752=LINE ( 'NONE', #8627, #48893 ) ;
#20755=DIRECTION ( 'NONE',  ( -3.469446951953613696E-16, 0.000000000000000000, -1.000000000000000000 ) ) ;
#20756=DIRECTION ( 'NONE',  ( -0.000000000000000000, 1.000000000000000000, -0.000000000000000000 ) ) ;
#20757=VERTEX_POINT ( 'NONE', #18546 ) ;
#20758=LINE ( 'NONE', #32914, #33646 ) ;
#20759=CARTESIAN_POINT ( 'NONE',  ( 0.000000000000000000, 3.267716535433071279, -1.299212598425193210 ) ) ;
#20760=CARTESIAN_POINT ( 'NONE',  ( -0.5455278134075211005, 3.267716535433071279, 9.463399047163219482E-17 ) ) ;
#20761=LINE ( 'NONE', #36521, #47389 ) ;
#20762=EDGE_CURVE ( 'NONE', #1205, #48217, #21654, .T. ) ;
#20765=EDGE_CURVE ( 'NONE', #50597, #2602, #33799, .T. ) ;
#20766=CARTESIAN_POINT ( 'NONE',  ( 0.8182917201112817063, 3.267716535433071279, -1.929133858267711110 ) ) ;
#20767=EDGE_LOOP ( 'NONE', ( #19074, #41760, #33213, #32983 ) ) ;
#20769=DIRECTION ( 'NONE',  ( -3.469446951953613696E-16, 0.000000000000000000, -1.000000000000000000 ) ) ;
#20770=FACE_OUTER_BOUND ( 'NONE', #48586, .T. ) ;
#20771=ORIENTED_EDGE ( 'NONE', *, *, #50395, .F. ) ;
#20772=LINE ( 'NONE', #13036, #34102 ) ;
#20773=CARTESIAN_POINT ( 'NONE',  ( 4.268512490100411402E-16, 3.346456692913386100, 2.204724409448808764 ) ) ;
#20774=DIRECTION ( 'NONE',  ( -0.000000000000000000, 1.000000000000000000, -0.000000000000000000 ) ) ;
#20776=LINE ( 'NONE', #14494, #5053 ) ;
#20777=ORIENTED_EDGE ( 'NONE', *, *, #16668, .F. ) ;
#20778=AXIS2_PLACEMENT_3D ( 'NONE', #22001, #45714, #14241 ) ;
#20783=ORIENTED_EDGE ( 'NONE', *, *, #3391, .T. ) ;
#20784=DIRECTION ( 'NONE',  ( -0.000000000000000000, 1.000000000000000000, -0.000000000000000000 ) ) ;
#20785=VECTOR ( 'NONE', #18681, 39.37007874015748143 ) ;
#20786=FACE_BOUND ( 'NONE', #12196, .T. ) ;
#20787=ORIENTED_EDGE ( 'NONE', *, *, #27004, .F. ) ;
#20788=CARTESIAN_POINT ( 'NONE',  ( 0.7423782071083092626, 0.000000000000000000, 2.204724409448808764 ) ) ;
#20790=AXIS2_PLACEMENT_3D ( 'NONE', #34512, #50194, #3010 ) ;
#20791=ORIENTED_EDGE ( 'NONE', *, *, #41315, .F. ) ;
#20793=EDGE_CURVE ( 'NONE', #13815, #38409, #25777, .T. ) ;
#20794=CARTESIAN_POINT ( 'NONE',  ( -1.091055626815042645, 3.267716535433071279, -2.086614173228339641 ) ) ;
#20796=ADVANCED_FACE ( 'NONE', ( #49986 ), #41281, .F. ) ;
#20798=VERTEX_POINT ( 'NONE', #14670 ) ;
#20799=CARTESIAN_POINT ( 'NONE',  ( -0.8182917201112819283, 3.346456692913386100, -0.7874015748031467643 ) ) ;
#20800=EDGE_CURVE ( 'NONE', #4205, #28641, #30421, .T. ) ;
#20801=ORIENTED_EDGE ( 'NONE', *, *, #46451, .T. ) ;
#20802=EDGE_CURVE ( 'NONE', #36182, #22163, #26533, .T. ) ;
#20803=CARTESIAN_POINT ( 'NONE',  ( 0.1968503937007872462, 0.000000000000000000, -1.456692913385822630 ) ) ;
#20805=PLANE ( 'NONE',  #15176 ) ;
#20806=FACE_OUTER_BOUND ( 'NONE', #31466, .T. ) ;
#20809=CARTESIAN_POINT ( 'NONE',  ( -0.9302092402134520821, 3.346456692913386100, -1.889763779527552146 ) ) ;
#20810=VERTEX_POINT ( 'NONE', #5903 ) ;
#20811=CARTESIAN_POINT ( 'NONE',  ( -2.182111253630085734, 0.000000000000000000, -0.6299212598425177889 ) ) ;
#20812=CARTESIAN_POINT ( 'NONE',  ( -0.5455278134075214336, 3.346456692913386100, 2.034427629037600660 ) ) ;
#20813=ORIENTED_EDGE ( 'NONE', *, *, #12975, .F. ) ;
#20815=DIRECTION ( 'NONE',  ( 0.000000000000000000, 0.000000000000000000, -1.000000000000000000 ) ) ;
#20816=FACE_OUTER_BOUND ( 'NONE', #24823, .T. ) ;
#20820=CARTESIAN_POINT ( 'NONE',  ( 2.378961647330872786, 3.346456692913386100, 0.1181102362204698858 ) ) ;
#20821=CIRCLE ( 'NONE', #19144, 2.106299212598425008 ) ;
#20822=EDGE_LOOP ( 'NONE', ( #44179, #3197, #10602, #32414 ) ) ;
#20824=LINE ( 'NONE', #36324, #41437 ) ;
#20825=VERTEX_POINT ( 'NONE', #44020 ) ;
#20826=FACE_BOUND ( 'NONE', #39558, .T. ) ;
#20827=DIRECTION ( 'NONE',  ( 1.734723475976806848E-16, 0.000000000000000000, 1.000000000000000000 ) ) ;
#20828=VECTOR ( 'NONE', #25626, 39.37007874015748143 ) ;
#20829=VECTOR ( 'NONE', #28406, 39.37007874015748143 ) ;
#20831=DIRECTION ( 'NONE',  ( 1.000000000000000000, 0.000000000000000000, 0.000000000000000000 ) ) ;
#20833=ADVANCED_FACE ( 'NONE', ( #36041 ), #5050, .F. ) ;
#20835=VERTEX_POINT ( 'NONE', #28025 ) ;
#20837=PLANE ( 'NONE',  #37857 ) ;
#20840=VERTEX_POINT ( 'NONE', #24418 ) ;
#20841=EDGE_CURVE ( 'NONE', #29961, #33629, #13753, .T. ) ;
#20844=FACE_OUTER_BOUND ( 'NONE', #3281, .T. ) ;
#20845=CARTESIAN_POINT ( 'NONE',  ( 0.5455278134075212115, 3.346456692913386100, 0.9448818897637746295 ) ) ;
#20848=VERTEX_POINT ( 'NONE', #24161 ) ;
#20849=EDGE_CURVE ( 'NONE', #16745, #27664, #48122, .T. ) ;
#20852=ORIENTED_EDGE ( 'NONE', *, *, #22253, .F. ) ;
#20853=CARTESIAN_POINT ( 'NONE',  ( 0.000000000000000000, 3.267716535433071279, -0.3543307086614175816 ) ) ;
#20855=ADVANCED_FACE ( 'NONE', ( #47351 ), #664, .F. ) ;
#20858=EDGE_LOOP ( 'NONE', ( #27122, #5768, #6847, #31816 ) ) ;
#20860=VECTOR ( 'NONE', #25815, 39.37007874015748143 ) ;
#20863=DIRECTION ( 'NONE',  ( -1.000000000000000000, -0.000000000000000000, -0.000000000000000000 ) ) ;
#20865=CARTESIAN_POINT ( 'NONE',  ( -1.166969139818016199, 3.346456692913386100, -0.3543307086614174151 ) ) ;
#20866=CARTESIAN_POINT ( 'NONE',  ( 1.091055626815042645, 3.267716535433071279, 0.4330708661417287386 ) ) ;
#20869=PLANE ( 'NONE',  #16742 ) ;
#20870=CARTESIAN_POINT ( 'NONE',  ( 0.8182917201112819283, 3.267716535433071279, -0.4724409448818889246 ) ) ;
#20877=ORIENTED_EDGE ( 'NONE', *, *, #7042, .T. ) ;
#20879=ORIENTED_EDGE ( 'NONE', *, *, #20765, .F. ) ;
#20880=CARTESIAN_POINT ( 'NONE',  ( 1.636583440222563635, 3.346456692913386100, -1.141732283464564013 ) ) ;
#20881=FACE_OUTER_BOUND ( 'NONE', #336, .T. ) ;
#20883=DIRECTION ( 'NONE',  ( 0.000000000000000000, 0.000000000000000000, 1.000000000000000000 ) ) ;
#20885=ORIENTED_EDGE ( 'NONE', *, *, #45500, .T. ) ;
#20887=VECTOR ( 'NONE', #15006, 39.37007874015748143 ) ;
#20889=FACE_BOUND ( 'NONE', #14845, .T. ) ;
#20890=ADVANCED_FACE ( 'NONE', ( #16680 ), #11768, .F. ) ;
#20892=LINE ( 'NONE', #44378, #36188 ) ;
#20893=VECTOR ( 'NONE', #43466, 39.37007874015748143 ) ;
#20895=EDGE_CURVE ( 'NONE', #21029, #24, #44284, .T. ) ;
#20896=VECTOR ( 'NONE', #50428, 39.37007874015748143 ) ;
#20897=VECTOR ( 'NONE', #4994, 39.37007874015748143 ) ;
#20898=DIRECTION ( 'NONE',  ( -3.469446951953613696E-16, 0.000000000000000000, -1.000000000000000000 ) ) ;
#20899=CARTESIAN_POINT ( 'NONE',  ( 0.5455278134075217666, 3.346456692913386100, 1.259842519685033357 ) ) ;
#20900=EDGE_CURVE ( 'NONE', #8317, #7323, #39396, .T. ) ;
#20901=VECTOR ( 'NONE', #38349, 39.37007874015748143 ) ;
#20903=ORIENTED_EDGE ( 'NONE', *, *, #34991, .T. ) ;
#20904=EDGE_LOOP ( 'NONE', ( #15009, #14758, #12528 ) ) ;
#20907=FACE_BOUND ( 'NONE', #48868, .T. ) ;
#20909=CARTESIAN_POINT ( 'NONE',  ( -2.182111253630085734, 3.267716535433071279, -0.6299212598425177889 ) ) ;
#20911=LINE ( 'NONE', #25296, #6113 ) ;
#20912=ORIENTED_EDGE ( 'NONE', *, *, #12097, .T. ) ;
#20913=DIRECTION ( 'NONE',  ( 1.000000000000000000, -0.000000000000000000, 0.000000000000000000 ) ) ;
#20917=ORIENTED_EDGE ( 'NONE', *, *, #19119, .T. ) ;
#20919=ORIENTED_EDGE ( 'NONE', *, *, #24815, .F. ) ;
#20920=CARTESIAN_POINT ( 'NONE',  ( 0.5455278134075211005, 3.346456692913386100, 0.1181102362204701633 ) ) ;
#20921=DIRECTION ( 'NONE',  ( 0.000000000000000000, 1.000000000000000000, 0.000000000000000000 ) ) ;
#20922=DIRECTION ( 'NONE',  ( 1.000000000000000000, 0.000000000000000000, 0.000000000000000000 ) ) ;
#20923=LINE ( 'NONE', #535, #50206 ) ;
#20926=VERTEX_POINT ( 'NONE', #4033 ) ;
#20928=CARTESIAN_POINT ( 'NONE',  ( -1.909347346926324462, 0.000000000000000000, -0.1574803149606297248 ) ) ;
#20934=VECTOR ( 'NONE', #24889, 39.37007874015748143 ) ;
#20935=PLANE ( 'NONE',  #37969 ) ;
#20936=AXIS2_PLACEMENT_3D ( 'NONE', #7723, #22969, #11846 ) ;
#20939=VECTOR ( 'NONE', #36183, 39.37007874015748143 ) ;
#20940=ORIENTED_EDGE ( 'NONE', *, *, #29651, .F. ) ;
#20942=CARTESIAN_POINT ( 'NONE',  ( 0.000000000000000000, 3.346456692913386100, 0.000000000000000000 ) ) ;
#20943=VERTEX_POINT ( 'NONE', #32430 ) ;
#20946=PLANE ( 'NONE',  #610 ) ;
#20950=ORIENTED_EDGE ( 'NONE', *, *, #21722, .T. ) ;
#20951=ORIENTED_EDGE ( 'NONE', *, *, #441, .T. ) ;
#20952=EDGE_CURVE ( 'NONE', #16283, #5399, #28534, .T. ) ;
#20954=CARTESIAN_POINT ( 'NONE',  ( 0.8182917201112817063, 3.346456692913386100, -2.047244094488181343 ) ) ;
#20955=EDGE_CURVE ( 'NONE', #31614, #18410, #35525, .T. ) ;
#20957=EDGE_CURVE ( 'NONE', #40341, #46985, #34732, .T. ) ;
#20959=VERTEX_POINT ( 'NONE', #27505 ) ;
#20960=VERTEX_POINT ( 'NONE', #17435 ) ;
#20961=DIRECTION ( 'NONE',  ( 0.000000000000000000, 0.000000000000000000, 1.000000000000000000 ) ) ;
#20962=CIRCLE ( 'NONE', #28360, 2.106299212598425008 ) ;
#20963=EDGE_LOOP ( 'NONE', ( #13561, #10356, #50609, #33815 ) ) ;
#20964=ORIENTED_EDGE ( 'NONE', *, *, #11546, .T. ) ;
#20966=DIRECTION ( 'NONE',  ( -0.000000000000000000, 1.000000000000000000, -0.000000000000000000 ) ) ;
#20967=DIRECTION ( 'NONE',  ( 1.734723475976806848E-16, 0.000000000000000000, 1.000000000000000000 ) ) ;
#20968=LINE ( 'NONE', #48545, #475 ) ;
#20971=ORIENTED_EDGE ( 'NONE', *, *, #30457, .F. ) ;
#20973=CARTESIAN_POINT ( 'NONE',  ( -1.909347346926324906, 0.000000000000000000, 1.417322834645662333 ) ) ;
#20974=DIRECTION ( 'NONE',  ( 0.000000000000000000, 0.000000000000000000, -1.000000000000000000 ) ) ;
#20977=LINE ( 'NONE', #40351, #18309 ) ;
#20978=FACE_OUTER_BOUND ( 'NONE', #25644, .T. ) ;
#20980=FACE_OUTER_BOUND ( 'NONE', #30138, .T. ) ;
#20983=LINE ( 'NONE', #24087, #22149 ) ;
#20984=CARTESIAN_POINT ( 'NONE',  ( 0.000000000000000000, 0.000000000000000000, 0.000000000000000000 ) ) ;
#20986=ADVANCED_FACE ( 'NONE', ( #5561 ), #5301, .F. ) ;
#20987=LINE ( 'NONE', #21495, #35195 ) ;
#20989=ORIENTED_EDGE ( 'NONE', *, *, #1841, .T. ) ;
#20992=ORIENTED_EDGE ( 'NONE', *, *, #15710, .F. ) ;
#20993=FACE_OUTER_BOUND ( 'NONE', #35725, .T. ) ;
#20994=EDGE_CURVE ( 'NONE', #23689, #17781, #2200, .T. ) ;
#20995=DIRECTION ( 'NONE',  ( 1.734723475976806848E-16, -0.000000000000000000, 1.000000000000000000 ) ) ;
#20997=FACE_OUTER_BOUND ( 'NONE', #48807, .T. ) ;
#20998=FACE_OUTER_BOUND ( 'NONE', #45888, .T. ) ;
#21000=VECTOR ( 'NONE', #8607, 39.37007874015748143 ) ;
#21001=DIRECTION ( 'NONE',  ( -3.469446951953613696E-16, 0.000000000000000000, -1.000000000000000000 ) ) ;
#21003=ADVANCED_FACE ( 'NONE', ( #17186 ), #29818, .F. ) ;
#21005=CARTESIAN_POINT ( 'NONE',  ( 1.560669927219590525, 0.000000000000000000, 0.9055118110236164419 ) ) ;
#21008=VECTOR ( 'NONE', #41215, 39.37007874015748143 ) ;
#21010=DIRECTION ( 'NONE',  ( 1.734723475976806848E-16, 0.000000000000000000, 1.000000000000000000 ) ) ;
#21013=EDGE_LOOP ( 'NONE', ( #1067, #23202, #42375, #31001 ) ) ;
#21015=CARTESIAN_POINT ( 'NONE',  ( 1.833433833923351353, 3.346456692913386100, 0.7480314960629872445 ) ) ;
#21017=EDGE_LOOP ( 'NONE', ( #31310, #36921, #22510, #11437 ) ) ;
#21018=DIRECTION ( 'NONE',  ( -3.469446951953613696E-16, 0.000000000000000000, -1.000000000000000000 ) ) ;
#21019=PLANE ( 'NONE',  #50464 ) ;
#21020=ORIENTED_EDGE ( 'NONE', *, *, #40902, .F. ) ;
#21021=CARTESIAN_POINT ( 'NONE',  ( -0.2727639067037610499, 0.000000000000000000, -2.047244094488181343 ) ) ;
#21022=ADVANCED_FACE ( 'NONE', ( #44781 ), #9946, .F. ) ;
#21024=DIRECTION ( 'NONE',  ( -0.000000000000000000, 1.000000000000000000, -0.000000000000000000 ) ) ;
#21025=CARTESIAN_POINT ( 'NONE',  ( -1.091055626815042201, 3.346456692913386100, 1.062992125984246083 ) ) ;
#21026=EDGE_CURVE ( 'NONE', #10852, #11355, #21564, .T. ) ;
#21027=EDGE_CURVE ( 'NONE', #11581, #39976, #40142, .T. ) ;
#21028=CARTESIAN_POINT ( 'NONE',  ( 0.2727639067037604392, 0.000000000000000000, -1.299212598425193210 ) ) ;
#21029=VERTEX_POINT ( 'NONE', #1173 ) ;
#21031=CARTESIAN_POINT ( 'NONE',  ( -2.454875160333845674, 0.000000000000000000, -0.3543307086614173040 ) ) ;
#21032=EDGE_CURVE ( 'NONE', #14557, #6504, #19482, .T. ) ;
#21033=FACE_OUTER_BOUND ( 'NONE', #26572, .T. ) ;
#21036=CARTESIAN_POINT ( 'NONE',  ( 1.015142113812069313, 0.000000000000000000, 0.2755905511810994302 ) ) ;
#21037=LINE ( 'NONE', #36786, #10444 ) ;
#21038=CARTESIAN_POINT ( 'NONE',  ( 0.000000000000000000, 3.346456692913386100, 0.000000000000000000 ) ) ;
#21041=LINE ( 'NONE', #16405, #27873 ) ;
#21043=CARTESIAN_POINT ( 'NONE',  ( -2.443991082961025185, 3.256070107886888554, 0.1574803149606286423 ) ) ;
#21045=DIRECTION ( 'NONE',  ( -3.469446951953613696E-16, 0.000000000000000000, -1.000000000000000000 ) ) ;
#21046=FACE_BOUND ( 'NONE', #19591, .T. ) ;
#21047=VECTOR ( 'NONE', #43893, 39.37007874015748143 ) ;
#21050=DIRECTION ( 'NONE',  ( 0.000000000000000000, 0.000000000000000000, 1.000000000000000000 ) ) ;
#21051=VECTOR ( 'NONE', #45167, 39.37007874015748143 ) ;
#21052=EDGE_LOOP ( 'NONE', ( #12263, #46516, #27671, #33673 ) ) ;
#21055=VECTOR ( 'NONE', #17153, 39.37007874015748143 ) ;
#21057=ORIENTED_EDGE ( 'NONE', *, *, #38469, .F. ) ;
#21058=CARTESIAN_POINT ( 'NONE',  ( 0.000000000000000000, 3.267716535433071279, 0.000000000000000000 ) ) ;
#21059=EDGE_LOOP ( 'NONE', ( #10783, #4667, #21780, #7204 ) ) ;
#21060=DIRECTION ( 'NONE',  ( 1.000000000000000000, 0.000000000000000000, 0.000000000000000000 ) ) ;
#21062=EDGE_CURVE ( 'NONE', #31055, #22725, #37325, .T. ) ;
#21063=CARTESIAN_POINT ( 'NONE',  ( -0.2727639067037602172, 0.000000000000000000, 1.417322834645662777 ) ) ;
#21065=EDGE_CURVE ( 'NONE', #23763, #29175, #48878, .T. ) ;
#21066=DIRECTION ( 'NONE',  ( 1.000000000000000000, 0.000000000000000000, 0.000000000000000000 ) ) ;
#21067=LINE ( 'NONE', #29578, #15433 ) ;
#21068=CARTESIAN_POINT ( 'NONE',  ( -0.07591351300297288773, 3.267716535433071279, 2.633779063002553116E-17 ) ) ;
#21071=LINE ( 'NONE', #36825, #8356 ) ;
#21073=CARTESIAN_POINT ( 'NONE',  ( -0.8182917201112819283, 0.000000000000000000, -0.4724409448818886470 ) ) ;
#21075=ORIENTED_EDGE ( 'NONE', *, *, #13256, .T. ) ;
#21077=CARTESIAN_POINT ( 'NONE',  ( 1.363819533518803251, 3.267716535433071279, -2.365849761790805487E-16 ) ) ;
#21078=CARTESIAN_POINT ( 'NONE',  ( 1.560669927219591191, 3.346456692913386100, 1.535433070866133898 ) ) ;
#21079=VECTOR ( 'NONE', #12552, 39.37007874015748143 ) ;
#21080=AXIS2_PLACEMENT_3D ( 'NONE', #10324, #13435, #29434 ) ;
#21081=VERTEX_POINT ( 'NONE', #33457 ) ;
#21082=CARTESIAN_POINT ( 'NONE',  ( -2.258024766633058622, 0.000000000000000000, 0.1574803149606286423 ) ) ;
#21084=ORIENTED_EDGE ( 'NONE', *, *, #45981, .T. ) ;
#21085=FACE_BOUND ( 'NONE', #33578, .T. ) ;
#21086=VECTOR ( 'NONE', #17594, 39.37007874015748143 ) ;
#21087=DIRECTION ( 'NONE',  ( -1.000000000000000000, 0.000000000000000000, 1.734723475976806848E-16 ) ) ;
#21089=CARTESIAN_POINT ( 'NONE',  ( -1.636583440222563635, 3.267716535433071279, 1.062992125984246083 ) ) ;
#21093=EDGE_CURVE ( 'NONE', #7484, #10001, #49395, .T. ) ;
#21094=VECTOR ( 'NONE', #41914, 39.37007874015748143 ) ;
#21096=ORIENTED_EDGE ( 'NONE', *, *, #48301, .F. ) ;
#21097=CARTESIAN_POINT ( 'NONE',  ( -0.8182917201112814842, 3.267716535433071279, 1.732283464566921172 ) ) ;
#21098=ADVANCED_FACE ( 'NONE', ( #30579 ), #38830, .F. ) ;
#21099=ORIENTED_EDGE ( 'NONE', *, *, #36428, .F. ) ;
#21101=ORIENTED_EDGE ( 'NONE', *, *, #48750, .F. ) ;
#21104=DIRECTION ( 'NONE',  ( -3.469446951953613696E-16, 0.000000000000000000, -1.000000000000000000 ) ) ;
#21106=CARTESIAN_POINT ( 'NONE',  ( 0.000000000000000000, 3.267716535433071279, -1.929133858267710000 ) ) ;
#21107=EDGE_LOOP ( 'NONE', ( #7760, #9295, #34785, #2428 ) ) ;
#21108=LINE ( 'NONE', #36346, #39725 ) ;
#21110=ORIENTED_EDGE ( 'NONE', *, *, #33318, .T. ) ;
#21111=AXIS2_PLACEMENT_3D ( 'NONE', #35473, #47557, #23848 ) ;
#21113=ORIENTED_EDGE ( 'NONE', *, *, #16467, .T. ) ;
#21115=PLANE ( 'NONE',  #4966 ) ;
#21118=LINE ( 'NONE', #28854, #27880 ) ;
#21119=AXIS2_PLACEMENT_3D ( 'NONE', #11252, #42734, #34499 ) ;
#21123=CIRCLE ( 'NONE', #14524, 2.165354330708661568 ) ;
#21124=LINE ( 'NONE', #36875, #9913 ) ;
#21125=ORIENTED_EDGE ( 'NONE', *, *, #16636, .F. ) ;
#21126=EDGE_CURVE ( 'NONE', #3114, #2304, #19197, .T. ) ;
#21127=VECTOR ( 'NONE', #5852, 39.37007874015748143 ) ;
#21129=CARTESIAN_POINT ( 'NONE',  ( -0.6214413264104945434, 3.346456692913386100, -2.074263738136479240 ) ) ;
#21130=ORIENTED_EDGE ( 'NONE', *, *, #23584, .F. ) ;
#21131=LINE ( 'NONE', #35405, #46367 ) ;
#21133=LINE ( 'NONE', #9253, #26010 ) ;
#21134=CARTESIAN_POINT ( 'NONE',  ( 0.000000000000000000, 3.346456692913386100, 0.000000000000000000 ) ) ;
#21136=ORIENTED_EDGE ( 'NONE', *, *, #5343, .F. ) ;
#21138=DIRECTION ( 'NONE',  ( 0.000000000000000000, -1.000000000000000000, 0.000000000000000000 ) ) ;
#21140=CARTESIAN_POINT ( 'NONE',  ( -1.536664496436148184E-16, 3.267716535433071279, 0.1181102362204701633 ) ) ;
#21141=EDGE_CURVE ( 'NONE', #14945, #767, #37860, .T. ) ;
#21142=ORIENTED_EDGE ( 'NONE', *, *, #39435, .F. ) ;
#21143=DIRECTION ( 'NONE',  ( 1.000000000000000000, 0.000000000000000000, 0.000000000000000000 ) ) ;
#21145=CARTESIAN_POINT ( 'NONE',  ( 1.091055626815043311, 3.267716535433071279, 1.889763779527550369 ) ) ;
#21146=EDGE_CURVE ( 'NONE', #11424, #1319, #49643, .T. ) ;
#21147=CARTESIAN_POINT ( 'NONE',  ( 0.000000000000000000, 3.267716535433071279, 0.000000000000000000 ) ) ;
#21148=DIRECTION ( 'NONE',  ( 1.000000000000000000, -0.000000000000000000, 0.000000000000000000 ) ) ;
#21149=EDGE_LOOP ( 'NONE', ( #41159, #1157, #1167, #33746 ) ) ;
#21150=AXIS2_PLACEMENT_3D ( 'NONE', #10656, #6775, #38029 ) ;
#21151=ADVANCED_FACE ( 'NONE', ( #26944 ), #34958, .F. ) ;
#21154=CARTESIAN_POINT ( 'NONE',  ( 1.015142113812069313, 3.346456692913386100, -0.9842519685039348154 ) ) ;
#21155=VECTOR ( 'NONE', #47039, 39.37007874015748143 ) ;
#21157=ORIENTED_EDGE ( 'NONE', *, *, #39764, .T. ) ;
#21159=VECTOR ( 'NONE', #48289, 39.37007874015748143 ) ;
#21170=DIRECTION ( 'NONE',  ( -3.469446951953613696E-16, 0.000000000000000000, -1.000000000000000000 ) ) ;
#21171=FACE_BOUND ( 'NONE', #4330, .T. ) ;
#21172=VERTEX_POINT ( 'NONE', #15084 ) ;
#21173=CARTESIAN_POINT ( 'NONE',  ( 0.8182917201112819283, 3.267716535433071279, -1.419509857074483292E-16 ) ) ;
#21174=DIRECTION ( 'NONE',  ( 1.000000000000000000, -0.000000000000000000, 0.000000000000000000 ) ) ;
#21176=DIRECTION ( 'NONE',  ( 1.000000000000000000, -0.000000000000000000, 0.000000000000000000 ) ) ;
#21178=EDGE_LOOP ( 'NONE', ( #33633, #34285, #39060, #1414 ) ) ;
#21180=EDGE_LOOP ( 'NONE', ( #13847, #34323, #3549, #7802 ) ) ;
#21181=CARTESIAN_POINT ( 'NONE',  ( -1.363819533518803251, 3.267716535433071279, 2.365849761790805487E-16 ) ) ;
#21184=LINE ( 'NONE', #16545, #2801 ) ;
#21185=DIRECTION ( 'NONE',  ( -1.000000000000000000, 0.000000000000000000, 0.000000000000000000 ) ) ;
#21186=ORIENTED_EDGE ( 'NONE', *, *, #15816, .T. ) ;
#21190=VECTOR ( 'NONE', #9502, 39.37007874015748143 ) ;
#21191=PLANE ( 'NONE',  #22991 ) ;
#21193=CARTESIAN_POINT ( 'NONE',  ( -1.536664496436148184E-16, 3.346456692913386100, -0.5118110236220465570 ) ) ;
#21194=DIRECTION ( 'NONE',  ( -0.000000000000000000, 1.000000000000000000, -0.000000000000000000 ) ) ;
#21196=CARTESIAN_POINT ( 'NONE',  ( -1.985260859929297572, 3.267716535433071279, -0.3149606299212589500 ) ) ;
#21197=LINE ( 'NONE', #6470, #25130 ) ;
#21198=VECTOR ( 'NONE', #18133, 39.37007874015748143 ) ;
#21199=CARTESIAN_POINT ( 'NONE',  ( -1.909347346926324462, 0.000000000000000000, -0.3543307086614171930 ) ) ;
#21201=FACE_OUTER_BOUND ( 'NONE', #569, .T. ) ;
#21205=LINE ( 'NONE', #40321, #29041 ) ;
#21209=EDGE_CURVE ( 'NONE', #35032, #25253, #50146, .T. ) ;
#21211=DIRECTION ( 'NONE',  ( 1.000000000000000000, 0.000000000000000000, -3.469446951953613696E-16 ) ) ;
#21214=FACE_OUTER_BOUND ( 'NONE', #12160, .T. ) ;
#21215=DIRECTION ( 'NONE',  ( -0.000000000000000000, 1.000000000000000000, -0.000000000000000000 ) ) ;
#21216=VECTOR ( 'NONE', #28875, 39.37007874015748143 ) ;
#21217=VECTOR ( 'NONE', #14598, 39.37007874015748143 ) ;
#21219=EDGE_LOOP ( 'NONE', ( #12409, #43612, #51040, #11638 ) ) ;
#21220=ORIENTED_EDGE ( 'NONE', *, *, #5243, .F. ) ;
#21223=EDGE_LOOP ( 'NONE', ( #30329, #17556, #31566, #44019 ) ) ;
#21224=ORIENTED_EDGE ( 'NONE', *, *, #21500, .T. ) ;
#21225=DIRECTION ( 'NONE',  ( -3.469446951953613696E-16, 0.000000000000000000, -1.000000000000000000 ) ) ;
#21226=DIRECTION ( 'NONE',  ( -1.000000000000000000, 0.000000000000000000, 1.734723475976806848E-16 ) ) ;
#21229=ORIENTED_EDGE ( 'NONE', *, *, #12198, .T. ) ;
#21230=CARTESIAN_POINT ( 'NONE',  ( 1.560669927219590747, 0.000000000000000000, -0.4724409448818889246 ) ) ;
#21231=CARTESIAN_POINT ( 'NONE',  ( -0.2727639067037608278, 0.000000000000000000, -1.614173228346451605 ) ) ;
#21232=CARTESIAN_POINT ( 'NONE',  ( 0.000000000000000000, 3.267716535433071279, 0.7480314960629872445 ) ) ;
#21233=ORIENTED_EDGE ( 'NONE', *, *, #44421, .T. ) ;
#21234=DIRECTION ( 'NONE',  ( -1.000000000000000000, 0.000000000000000000, 1.734723475976806848E-16 ) ) ;
#21236=DIRECTION ( 'NONE',  ( 0.000000000000000000, -1.000000000000000000, 0.000000000000000000 ) ) ;
#21239=VECTOR ( 'NONE', #48069, 39.37007874015748143 ) ;
#21240=CARTESIAN_POINT ( 'NONE',  ( 0.000000000000000000, 3.267716535433071279, 1.220472440944875281 ) ) ;
#21241=CARTESIAN_POINT ( 'NONE',  ( 0.7423782071083091516, 3.346456692913386100, 2.034117492951036166 ) ) ;
#21242=DIRECTION ( 'NONE',  ( 0.000000000000000000, 0.000000000000000000, -1.000000000000000000 ) ) ;
#21243=ORIENTED_EDGE ( 'NONE', *, *, #47470, .F. ) ;
#21244=EDGE_LOOP ( 'NONE', ( #23552, #28701, #40132, #27312 ) ) ;
#21246=DIRECTION ( 'NONE',  ( 0.000000000000000000, -1.000000000000000000, 0.000000000000000000 ) ) ;
#21247=ORIENTED_EDGE ( 'NONE', *, *, #26546, .T. ) ;
#21248=DIRECTION ( 'NONE',  ( -3.469446951953613696E-16, 0.000000000000000000, -1.000000000000000000 ) ) ;
#21249=CARTESIAN_POINT ( 'NONE',  ( 2.182111253630085290, 3.346456692913386100, -1.161035397307311917E-15 ) ) ;
#21250=EDGE_CURVE ( 'NONE', #41945, #13922, #26442, .T. ) ;
#21251=EDGE_CURVE ( 'NONE', #39570, #10700, #341, .T. ) ;
#21252=VECTOR ( 'NONE', #9912, 39.37007874015748143 ) ;
#21253=VECTOR ( 'NONE', #43341, 39.37007874015748143 ) ;
#21255=CARTESIAN_POINT ( 'NONE',  ( 1.287906020515829919, 3.346456692913386100, -1.740706023381844547 ) ) ;
#21256=CARTESIAN_POINT ( 'NONE',  ( 1.287906020515830141, 3.267716535433071279, -0.1968503937007883287 ) ) ;
#21257=DIRECTION ( 'NONE',  ( 1.000000000000000000, 0.000000000000000000, 0.000000000000000000 ) ) ;
#21258=ORIENTED_EDGE ( 'NONE', *, *, #8526, .F. ) ;
#21261=CARTESIAN_POINT ( 'NONE',  ( -0.07591351300297340121, 3.346456692913386100, -1.299212598425193210 ) ) ;
#21263=CARTESIAN_POINT ( 'NONE',  ( 1.833433833923351353, 0.000000000000000000, 1.259842519685033135 ) ) ;
#21266=CARTESIAN_POINT ( 'NONE',  ( 0.000000000000000000, 3.267716535433071279, 0.3149606299212578953 ) ) ;
#21267=ORIENTED_EDGE ( 'NONE', *, *, #33374, .T. ) ;
#21268=FACE_OUTER_BOUND ( 'NONE', #16715, .T. ) ;
#21269=VECTOR ( 'NONE', #5562, 39.37007874015748143 ) ;
#21271=EDGE_CURVE ( 'NONE', #22242, #40968, #19701, .T. ) ;
#21272=ORIENTED_EDGE ( 'NONE', *, *, #49451, .T. ) ;
#21275=VERTEX_POINT ( 'NONE', #35463 ) ;
#21278=CARTESIAN_POINT ( 'NONE',  ( 0.000000000000000000, 3.267716535433071279, -0.8267716535433052849 ) ) ;
#21279=CARTESIAN_POINT ( 'NONE',  ( -2.182111253630085734, 0.000000000000000000, -0.9448818897637762948 ) ) ;
#21281=CARTESIAN_POINT ( 'NONE',  ( -1.439733046521777027, 3.346456692913386100, -1.771653543307080581 ) ) ;
#21282=EDGE_CURVE ( 'NONE', #23253, #29154, #8599, .T. ) ;
#21284=ORIENTED_EDGE ( 'NONE', *, *, #27108, .T. ) ;
#21285=VERTEX_POINT ( 'NONE', #15829 ) ;
#21286=DIRECTION ( 'NONE',  ( -3.469446951953613696E-16, 0.000000000000000000, -1.000000000000000000 ) ) ;
#21287=FACE_OUTER_BOUND ( 'NONE', #20053, .T. ) ;
#21289=FACE_OUTER_BOUND ( 'NONE', #22410, .T. ) ;
#21290=CARTESIAN_POINT ( 'NONE',  ( 0.000000000000000000, 0.000000000000000000, 0.000000000000000000 ) ) ;
#21292=EDGE_CURVE ( 'NONE', #17810, #18573, #31591, .T. ) ;
#21294=ORIENTED_EDGE ( 'NONE', *, *, #39827, .F. ) ;
#21295=EDGE_LOOP ( 'NONE', ( #44518, #23902, #49508, #22050 ) ) ;
#21296=CARTESIAN_POINT ( 'NONE',  ( 0.8182917201112824834, 3.346456692913386100, 2.047244094488179567 ) ) ;
#21297=DIRECTION ( 'NONE',  ( 0.000000000000000000, 0.000000000000000000, -1.000000000000000000 ) ) ;
#21299=LINE ( 'NONE', #49128, #32171 ) ;
#21300=ORIENTED_EDGE ( 'NONE', *, *, #45464, .F. ) ;
#21301=LINE ( 'NONE', #33187, #44638 ) ;
#21302=FACE_BOUND ( 'NONE', #34294, .T. ) ;
#21306=ORIENTED_EDGE ( 'NONE', *, *, #9329, .T. ) ;
#21307=VECTOR ( 'NONE', #338, 39.37007874015748143 ) ;
#21308=ORIENTED_EDGE ( 'NONE', *, *, #13409, .T. ) ;
#21311=AXIS2_PLACEMENT_3D ( 'NONE', #25843, #39489, #31752 ) ;
#21312=ORIENTED_EDGE ( 'NONE', *, *, #33444, .T. ) ;
#21313=CARTESIAN_POINT ( 'NONE',  ( -0.8182917201112819283, 0.000000000000000000, -1.732283464566922726 ) ) ;
#21314=VECTOR ( 'NONE', #33008, 39.37007874015748143 ) ;
#21315=LINE ( 'NONE', #31974, #2329 ) ;
#21316=ORIENTED_EDGE ( 'NONE', *, *, #5616, .F. ) ;
#21317=VECTOR ( 'NONE', #42773, 39.37007874015748143 ) ;
#21319=DIRECTION ( 'NONE',  ( -3.469446951953613696E-16, 0.000000000000000000, -1.000000000000000000 ) ) ;
#21324=EDGE_CURVE ( 'NONE', #47130, #10670, #12220, .T. ) ;
#21325=DIRECTION ( 'NONE',  ( -1.000000000000000000, -0.000000000000000000, -0.000000000000000000 ) ) ;
#21329=LINE ( 'NONE', #9961, #19864 ) ;
#21330=ORIENTED_EDGE ( 'NONE', *, *, #39827, .T. ) ;
#21331=CARTESIAN_POINT ( 'NONE',  ( -1.363819533518803473, 3.267716535433071279, -0.6692913385826760875 ) ) ;
#21332=LINE ( 'NONE', #41458, #27798 ) ;
#21334=LINE ( 'NONE', #9199, #41950 ) ;
#21335=VECTOR ( 'NONE', #22114, 39.37007874015748143 ) ;
#21336=LINE ( 'NONE', #25454, #21008 ) ;
#21337=CARTESIAN_POINT ( 'NONE',  ( 1.909347346926324684, 3.346456692913386100, 0.7874015748031456541 ) ) ;
#21338=ORIENTED_EDGE ( 'NONE', *, *, #30133, .T. ) ;
#21341=FACE_BOUND ( 'NONE', #40213, .T. ) ;
#21342=LINE ( 'NONE', #12833, #8617 ) ;
#21344=VECTOR ( 'NONE', #45960, 39.37007874015748143 ) ;
#21346=CARTESIAN_POINT ( 'NONE',  ( 0.4696143004045484348, 0.000000000000000000, 2.165354330708650910 ) ) ;
#21347=CARTESIAN_POINT ( 'NONE',  ( 0.8182917201112819283, 3.346456692913386100, 0.4724409448818868706 ) ) ;
#21349=ORIENTED_EDGE ( 'NONE', *, *, #1144, .T. ) ;
#21350=ORIENTED_EDGE ( 'NONE', *, *, #15196, .F. ) ;
#21351=DIRECTION ( 'NONE',  ( 0.000000000000000000, 0.000000000000000000, 1.000000000000000000 ) ) ;
#21352=VERTEX_POINT ( 'NONE', #50890 ) ;
#21354=DIRECTION ( 'NONE',  ( 1.000000000000000000, 0.000000000000000000, 0.000000000000000000 ) ) ;
#21356=EDGE_CURVE ( 'NONE', #26492, #37481, #47033, .T. ) ;
#21357=DIRECTION ( 'NONE',  ( -0.000000000000000000, 0.000000000000000000, 1.000000000000000000 ) ) ;
#21358=ADVANCED_FACE ( 'NONE', ( #11961 ), #31853, .F. ) ;
#21360=CARTESIAN_POINT ( 'NONE',  ( 1.015142113812069979, 0.000000000000000000, 1.417322834645662777 ) ) ;
#21361=EDGE_CURVE ( 'NONE', #44686, #33629, #43694, .T. ) ;
#21362=DIRECTION ( 'NONE',  ( -1.000000000000000000, 0.000000000000000000, 0.000000000000000000 ) ) ;
#21363=ORIENTED_EDGE ( 'NONE', *, *, #7955, .T. ) ;
#21366=ORIENTED_EDGE ( 'NONE', *, *, #14414, .T. ) ;
#21367=ORIENTED_EDGE ( 'NONE', *, *, #44581, .F. ) ;
#21369=ORIENTED_EDGE ( 'NONE', *, *, #46822, .F. ) ;
#21373=LINE ( 'NONE', #45851, #35309 ) ;
#21374=ORIENTED_EDGE ( 'NONE', *, *, #18150, .F. ) ;
#21375=DIRECTION ( 'NONE',  ( -1.000000000000000000, 0.000000000000000000, 0.000000000000000000 ) ) ;
#21377=VECTOR ( 'NONE', #27198, 39.37007874015748143 ) ;
#21378=FACE_OUTER_BOUND ( 'NONE', #6168, .T. ) ;
#21379=ADVANCED_FACE ( 'NONE', ( #40863 ), #9366, .F. ) ;
#21380=VECTOR ( 'NONE', #43982, 39.37007874015748143 ) ;
#21381=EDGE_LOOP ( 'NONE', ( #2761, #43179, #4711, #46213 ) ) ;
#21382=CARTESIAN_POINT ( 'NONE',  ( -1.363819533518803029, 0.000000000000000000, 0.5905511811023582691 ) ) ;
#21383=CARTESIAN_POINT ( 'NONE',  ( 1.015142113812069979, 3.267716535433071279, 1.732283464566921172 ) ) ;
#21385=VERTEX_POINT ( 'NONE', #33388 ) ;
#21387=DIRECTION ( 'NONE',  ( -1.000000000000000000, 0.000000000000000000, 1.734723475976806848E-16 ) ) ;
#21389=CARTESIAN_POINT ( 'NONE',  ( 1.636583440222563635, 3.346456692913386100, -1.456692913385823296 ) ) ;
#21391=PLANE ( 'NONE',  #48196 ) ;
#21392=EDGE_LOOP ( 'NONE', ( #12793, #28850, #43395, #6388 ) ) ;
#21393=CARTESIAN_POINT ( 'NONE',  ( 1.015142113812069313, 3.267716535433071279, 0.7874015748031454320 ) ) ;
#21394=CARTESIAN_POINT ( 'NONE',  ( -0.07591351300297284610, 3.346456692913386100, 1.220472440944875281 ) ) ;
#21396=CARTESIAN_POINT ( 'NONE',  ( 2.094031212354920957, 3.223341107052878574, -1.299212598425194320 ) ) ;
#21398=CARTESIAN_POINT ( 'NONE',  ( 1.287906020515830141, 0.000000000000000000, 0.7480314960629872445 ) ) ;
#21401=DIRECTION ( 'NONE',  ( -0.000000000000000000, 1.000000000000000000, -0.000000000000000000 ) ) ;
#21402=DIRECTION ( 'NONE',  ( -0.000000000000000000, 1.000000000000000000, -0.000000000000000000 ) ) ;
#21403=VECTOR ( 'NONE', #26046, 39.37007874015748143 ) ;
#21404=ORIENTED_EDGE ( 'NONE', *, *, #40207, .F. ) ;
#21405=DIRECTION ( 'NONE',  ( -3.469446951953613696E-16, 0.000000000000000000, -1.000000000000000000 ) ) ;
#21409=DIRECTION ( 'NONE',  ( 1.000000000000000000, 0.000000000000000000, 0.000000000000000000 ) ) ;
#21410=EDGE_LOOP ( 'NONE', ( #17318, #39879, #43966, #43891 ) ) ;
#21411=VECTOR ( 'NONE', #11142, 39.37007874015748143 ) ;
#21413=PLANE ( 'NONE',  #31367 ) ;
#21414=EDGE_CURVE ( 'NONE', #43528, #9319, #44468, .T. ) ;
#21415=CARTESIAN_POINT ( 'NONE',  ( 0.000000000000000000, 3.267716535433071279, -0.7874015748031473194 ) ) ;
#21417=EDGE_CURVE ( 'NONE', #4560, #40528, #1400, .T. ) ;
#21418=DIRECTION ( 'NONE',  ( -1.000000000000000000, 0.000000000000000000, 1.734723475976806848E-16 ) ) ;
#21419=ORIENTED_EDGE ( 'NONE', *, *, #12097, .F. ) ;
#21420=ORIENTED_EDGE ( 'NONE', *, *, #45563, .F. ) ;
#21421=DIRECTION ( 'NONE',  ( -0.000000000000000000, 1.000000000000000000, -0.000000000000000000 ) ) ;
#21423=FACE_BOUND ( 'NONE', #35307, .T. ) ;
#21424=ORIENTED_EDGE ( 'NONE', *, *, #30715, .F. ) ;
#21425=CARTESIAN_POINT ( 'NONE',  ( -1.091055626815042423, 3.267716535433071279, 1.892679809432644143E-16 ) ) ;
#21429=CARTESIAN_POINT ( 'NONE',  ( 0.8182917201112819283, 3.346456692913386100, -1.299212598425193210 ) ) ;
#21433=EDGE_CURVE ( 'NONE', #9566, #41713, #41372, .T. ) ;
#21434=VERTEX_POINT ( 'NONE', #17119 ) ;
#21437=EDGE_CURVE ( 'NONE', #16692, #42434, #20987, .T. ) ;
#21438=VECTOR ( 'NONE', #33695, 39.37007874015748143 ) ;
#21440=FACE_OUTER_BOUND ( 'NONE', #15570, .T. ) ;
#21441=EDGE_CURVE ( 'NONE', #36917, #1405, #5234, .T. ) ;
#21444=CARTESIAN_POINT ( 'NONE',  ( 0.000000000000000000, 3.267716535433071279, 1.102362204724404160 ) ) ;
#21445=LINE ( 'NONE', #40038, #27104 ) ;
#21447=CARTESIAN_POINT ( 'NONE',  ( 1.253212129322610613, 3.346456692913386100, 1.692913385826762873 ) ) ;
#21448=CARTESIAN_POINT ( 'NONE',  ( 0.5455278134075217666, 3.346456692913386100, 1.889763779527550369 ) ) ;
#21449=LINE ( 'NONE', #26334, #9174 ) ;
#21451=VECTOR ( 'NONE', #5363, 39.37007874015748143 ) ;
#21452=FACE_OUTER_BOUND ( 'NONE', #8270, .T. ) ;
#21453=CARTESIAN_POINT ( 'NONE',  ( -1.091055626815042645, 3.346456692913386100, -0.5118110236220467790 ) ) ;
#21454=EDGE_LOOP ( 'NONE', ( #47902, #13839, #6850, #42456 ) ) ;
#21455=DIRECTION ( 'NONE',  ( 0.000000000000000000, 0.000000000000000000, -1.000000000000000000 ) ) ;
#21456=DIRECTION ( 'NONE',  ( 0.000000000000000000, -1.000000000000000000, 0.000000000000000000 ) ) ;
#21457=VECTOR ( 'NONE', #36971, 39.37007874015748143 ) ;
#21458=ORIENTED_EDGE ( 'NONE', *, *, #14564, .F. ) ;
#21459=VERTEX_POINT ( 'NONE', #32618 ) ;
#21461=LINE ( 'NONE', #44930, #42651 ) ;
#21463=VERTEX_POINT ( 'NONE', #13754 ) ;
#21464=CARTESIAN_POINT ( 'NONE',  ( 0.000000000000000000, 3.267716535433071279, -0.9842519685039344823 ) ) ;
#21465=ORIENTED_EDGE ( 'NONE', *, *, #30272, .F. ) ;
#21466=CARTESIAN_POINT ( 'NONE',  ( 1.091055626815042645, 0.000000000000000000, 0.6299212598425161236 ) ) ;
#21467=DIRECTION ( 'NONE',  ( -3.469446951953613696E-16, 0.000000000000000000, -1.000000000000000000 ) ) ;
#21468=ORIENTED_EDGE ( 'NONE', *, *, #30297, .T. ) ;
#21472=CARTESIAN_POINT ( 'NONE',  ( 0.7423782071083087075, 3.267716535433071279, -2.575641807848710194E-16 ) ) ;
#21473=EDGE_CURVE ( 'NONE', #16692, #4787, #17623, .T. ) ;
#21476=DIRECTION ( 'NONE',  ( -1.000000000000000000, 0.000000000000000000, 0.000000000000000000 ) ) ;
#21477=CARTESIAN_POINT ( 'NONE',  ( 1.560669927219590747, 0.000000000000000000, 0.7874015748031454320 ) ) ;
#21480=VECTOR ( 'NONE', #19770, 39.37007874015748143 ) ;
#21482=VECTOR ( 'NONE', #15311, 39.37007874015748143 ) ;
#21485=DIRECTION ( 'NONE',  ( 1.734723475976806848E-16, -0.000000000000000000, 1.000000000000000000 ) ) ;
#21486=ORIENTED_EDGE ( 'NONE', *, *, #34309, .F. ) ;
#21488=LINE ( 'NONE', #6511, #7120 ) ;
#21490=ORIENTED_EDGE ( 'NONE', *, *, #10614, .F. ) ;
#21492=VECTOR ( 'NONE', #10556, 39.37007874015748143 ) ;
#21495=CARTESIAN_POINT ( 'NONE',  ( -0.3486774197067334380, 0.000000000000000000, 1.574803149606291974 ) ) ;
#21496=LINE ( 'NONE', #22264, #30479 ) ;
#21500=EDGE_CURVE ( 'NONE', #17906, #9076, #29235, .T. ) ;
#21501=DIRECTION ( 'NONE',  ( 1.000000000000000000, 0.000000000000000000, 0.000000000000000000 ) ) ;
#21503=LINE ( 'NONE', #13253, #34862 ) ;
#21506=DIRECTION ( 'NONE',  ( 1.000000000000000000, -0.000000000000000000, 0.000000000000000000 ) ) ;
#21508=ORIENTED_EDGE ( 'NONE', *, *, #15344, .F. ) ;
#21509=LINE ( 'NONE', #37270, #40702 ) ;
#21510=LINE ( 'NONE', #49088, #26047 ) ;
#21511=CARTESIAN_POINT ( 'NONE',  ( 0.000000000000000000, 3.346456692913386100, 0.000000000000000000 ) ) ;
#21512=VECTOR ( 'NONE', #37907, 39.37007874015748143 ) ;
#21513=VERTEX_POINT ( 'NONE', #36740 ) ;
#21514=LINE ( 'NONE', #48331, #27331 ) ;
#21518=ORIENTED_EDGE ( 'NONE', *, *, #2686, .T. ) ;
#21519=DIRECTION ( 'NONE',  ( -3.469446951953613696E-16, 0.000000000000000000, -1.000000000000000000 ) ) ;
#21520=LINE ( 'NONE', #40393, #47271 ) ;
#21521=ORIENTED_EDGE ( 'NONE', *, *, #39418, .F. ) ;
#21525=DIRECTION ( 'NONE',  ( -0.000000000000000000, 1.000000000000000000, -0.000000000000000000 ) ) ;
#21529=CARTESIAN_POINT ( 'NONE',  ( -1.091055626815042201, 0.000000000000000000, 0.7480314960629874665 ) ) ;
#21530=CARTESIAN_POINT ( 'NONE',  ( 0.000000000000000000, 3.267716535433071279, -0.1574803149606304187 ) ) ;
#21531=CARTESIAN_POINT ( 'NONE',  ( 0.000000000000000000, 3.267716535433071279, -1.141732283464564013 ) ) ;
#21532=EDGE_CURVE ( 'NONE', #27988, #37613, #5997, .T. ) ;
#21533=ORIENTED_EDGE ( 'NONE', *, *, #35445, .T. ) ;
#21534=EDGE_LOOP ( 'NONE', ( #36743, #28414, #5597, #5449 ) ) ;
#21535=FACE_OUTER_BOUND ( 'NONE', #28839, .T. ) ;
#21536=CARTESIAN_POINT ( 'NONE',  ( -1.593029370565769431, 3.346456692913386100, 1.377952755905504256 ) ) ;
#21537=EDGE_CURVE ( 'NONE', #19452, #29807, #37510, .T. ) ;
#21538=ORIENTED_EDGE ( 'NONE', *, *, #3585, .T. ) ;
#21540=DIRECTION ( 'NONE',  ( 1.000000000000000000, -0.000000000000000000, 0.000000000000000000 ) ) ;
#21545=EDGE_CURVE ( 'NONE', #9586, #47188, #50082, .T. ) ;
#21547=FACE_OUTER_BOUND ( 'NONE', #39433, .T. ) ;
#21548=CARTESIAN_POINT ( 'NONE',  ( 1.015142113812069091, 3.346456692913386100, -1.417322834645664331 ) ) ;
#21549=EDGE_CURVE ( 'NONE', #4697, #32558, #22508, .T. ) ;
#21550=EDGE_LOOP ( 'NONE', ( #886, #19874, #35197, #16106 ) ) ;
#21552=FACE_BOUND ( 'NONE', #36185, .T. ) ;
#21554=CARTESIAN_POINT ( 'NONE',  ( -2.454875160333845674, 0.000000000000000000, -0.1574803149606298636 ) ) ;
#21556=ORIENTED_EDGE ( 'NONE', *, *, #40550, .F. ) ;
#21557=VECTOR ( 'NONE', #977, 39.37007874015748143 ) ;
#21559=CARTESIAN_POINT ( 'NONE',  ( -1.363819533518803029, 3.346456692913386100, 0.2755905511810996522 ) ) ;
#21560=AXIS2_PLACEMENT_3D ( 'NONE', #49657, #7102, #19213 ) ;
#21563=ORIENTED_EDGE ( 'NONE', *, *, #48755, .F. ) ;
#21564=LINE ( 'NONE', #9435, #6314 ) ;
#21566=CARTESIAN_POINT ( 'NONE',  ( 0.8182917201112819283, 0.000000000000000000, 0.5905511811023579360 ) ) ;
#21567=ORIENTED_EDGE ( 'NONE', *, *, #1102, .F. ) ;
#21571=DIRECTION ( 'NONE',  ( 0.000000000000000000, 0.000000000000000000, -1.000000000000000000 ) ) ;
#21572=CARTESIAN_POINT ( 'NONE',  ( -1.024442997624132911E-17, 3.267716535433071279, 1.777125317778635541E-33 ) ) ;
#21573=VECTOR ( 'NONE', #1704, 39.37007874015748143 ) ;
#21575=PLANE ( 'NONE',  #45372 ) ;
#21578=ORIENTED_EDGE ( 'NONE', *, *, #19422, .F. ) ;
#21579=CARTESIAN_POINT ( 'NONE',  ( -1.091055626815042423, 3.267716535433071279, 1.892679809432644143E-16 ) ) ;
#21580=EDGE_CURVE ( 'NONE', #24780, #36033, #6257, .T. ) ;
#21582=VERTEX_POINT ( 'NONE', #34394 ) ;
#21583=FACE_OUTER_BOUND ( 'NONE', #8052, .T. ) ;
#21584=DIRECTION ( 'NONE',  ( 0.000000000000000000, -1.000000000000000000, 0.000000000000000000 ) ) ;
#21587=DIRECTION ( 'NONE',  ( 0.000000000000000000, -1.000000000000000000, 0.000000000000000000 ) ) ;
#21588=CARTESIAN_POINT ( 'NONE',  ( 2.378961647330872786, 3.346456692913386100, -0.1968503937007886062 ) ) ;
#21589=EDGE_LOOP ( 'NONE', ( #25340, #18740, #41502, #33428 ) ) ;
#21590=CARTESIAN_POINT ( 'NONE',  ( 0.4696143004045476022, 3.346456692913386100, -2.244094488188969727 ) ) ;
#21592=FACE_BOUND ( 'NONE', #9814, .T. ) ;
#21593=CARTESIAN_POINT ( 'NONE',  ( -1.712496953225537188, 0.000000000000000000, 1.102362204724404160 ) ) ;
#21595=VECTOR ( 'NONE', #50878, 39.37007874015748143 ) ;
#21596=DIRECTION ( 'NONE',  ( -0.000000000000000000, 1.000000000000000000, -0.000000000000000000 ) ) ;
#21598=VECTOR ( 'NONE', #27420, 39.37007874015748143 ) ;
#21599=ORIENTED_EDGE ( 'NONE', *, *, #8818, .T. ) ;
#21601=CARTESIAN_POINT ( 'NONE',  ( -0.5455278134075208785, 0.000000000000000000, 1.062992125984246083 ) ) ;
#21602=ORIENTED_EDGE ( 'NONE', *, *, #45638, .F. ) ;
#21603=VECTOR ( 'NONE', #24974, 39.37007874015748143 ) ;
#21604=LINE ( 'NONE', #37617, #41730 ) ;
#21605=VERTEX_POINT ( 'NONE', #23016 ) ;
#21606=ADVANCED_FACE ( 'NONE', ( #50324 ), #22010, .F. ) ;
#21608=VECTOR ( 'NONE', #35994, 39.37007874015748143 ) ;
#21610=LINE ( 'NONE', #22375, #5147 ) ;
#21611=EDGE_CURVE ( 'NONE', #20741, #606, #18380, .T. ) ;
#21615=VERTEX_POINT ( 'NONE', #45467 ) ;
#21619=EDGE_LOOP ( 'NONE', ( #2596, #8196, #2978, #48770 ) ) ;
#21623=CARTESIAN_POINT ( 'NONE',  ( -1.712496953225537633, 3.346456692913386100, -0.7874015748031470974 ) ) ;
#21624=AXIS2_PLACEMENT_3D ( 'NONE', #3075, #51010, #26315 ) ;
#21626=FACE_OUTER_BOUND ( 'NONE', #21244, .T. ) ;
#21627=ORIENTED_EDGE ( 'NONE', *, *, #12536, .T. ) ;
#21628=VECTOR ( 'NONE', #42490, 39.37007874015748143 ) ;
#21630=DIRECTION ( 'NONE',  ( 0.000000000000000000, -1.000000000000000000, 0.000000000000000000 ) ) ;
#21631=ORIENTED_EDGE ( 'NONE', *, *, #18459, .T. ) ;
#21633=CARTESIAN_POINT ( 'NONE',  ( 0.7423782071083084855, 0.000000000000000000, -1.574803149606293529 ) ) ;
#21634=VECTOR ( 'NONE', #13305, 39.37007874015748143 ) ;
#21635=PLANE ( 'NONE',  #2094 ) ;
#21638=VECTOR ( 'NONE', #36442, 39.37007874015748143 ) ;
#21640=DIRECTION ( 'NONE',  ( 0.000000000000000000, 0.000000000000000000, 1.000000000000000000 ) ) ;
#21641=VERTEX_POINT ( 'NONE', #26378 ) ;
#21643=EDGE_CURVE ( 'NONE', #337, #23167, #30004, .T. ) ;
#21644=LINE ( 'NONE', #18026, #21828 ) ;
#21645=ORIENTED_EDGE ( 'NONE', *, *, #21663, .F. ) ;
#21646=DIRECTION ( 'NONE',  ( -1.000000000000000000, 0.000000000000000000, 0.000000000000000000 ) ) ;
#21647=EDGE_CURVE ( 'NONE', #46376, #35776, #26870, .T. ) ;
#21651=DIRECTION ( 'NONE',  ( -1.000000000000000000, -0.000000000000000000, -0.000000000000000000 ) ) ;
#21653=CARTESIAN_POINT ( 'NONE',  ( -1.195183497228115035E-16, 3.346456692913386100, 0.6299212598425161236 ) ) ;
#21654=LINE ( 'NONE', #34549, #8768 ) ;
#21655=VERTEX_POINT ( 'NONE', #10385 ) ;
#21657=ORIENTED_EDGE ( 'NONE', *, *, #12931, .F. ) ;
#21658=FACE_OUTER_BOUND ( 'NONE', #18602, .T. ) ;
#21659=ORIENTED_EDGE ( 'NONE', *, *, #6593, .F. ) ;
#21662=EDGE_LOOP ( 'NONE', ( #31294, #36790, #35377, #37954 ) ) ;
#21663=EDGE_CURVE ( 'NONE', #17447, #24413, #45977, .T. ) ;
#21664=CARTESIAN_POINT ( 'NONE',  ( -1.353122744573580727, 3.346456692913386100, -1.614173228346451605 ) ) ;
#21666=DIRECTION ( 'NONE',  ( -1.000000000000000000, 0.000000000000000000, -0.000000000000000000 ) ) ;
#21669=AXIS2_PLACEMENT_3D ( 'NONE', #23950, #39955, #39697 ) ;
#21670=CARTESIAN_POINT ( 'NONE',  ( 0.5455278134075211005, 3.267716535433071279, -0.8267716535433055070 ) ) ;
#21671=EDGE_CURVE ( 'NONE', #9761, #4026, #11393, .T. ) ;
#21672=ORIENTED_EDGE ( 'NONE', *, *, #7095, .T. ) ;
#21673=ORIENTED_EDGE ( 'NONE', *, *, #25489, .F. ) ;
#21676=FACE_BOUND ( 'NONE', #32855, .T. ) ;
#21678=VECTOR ( 'NONE', #2011, 39.37007874015748143 ) ;
#21680=DIRECTION ( 'NONE',  ( -1.000000000000000000, 0.000000000000000000, 1.734723475976806848E-16 ) ) ;
#21681=ORIENTED_EDGE ( 'NONE', *, *, #48681, .T. ) ;
#21682=EDGE_LOOP ( 'NONE', ( #34350, #44220, #5858, #11030 ) ) ;
#21683=ADVANCED_FACE ( 'NONE', ( #4152 ), #20406, .F. ) ;
#21684=LINE ( 'NONE', #6188, #3492 ) ;
#21688=EDGE_LOOP ( 'NONE', ( #22382, #35940, #22282, #20885 ) ) ;
#21689=ORIENTED_EDGE ( 'NONE', *, *, #18833, .F. ) ;
#21691=DIRECTION ( 'NONE',  ( 1.000000000000000000, -0.000000000000000000, 0.000000000000000000 ) ) ;
#21693=ADVANCED_FACE ( 'NONE', ( #39519 ), #11895, .F. ) ;
#21694=CARTESIAN_POINT ( 'NONE',  ( -1.712496953225537188, 0.000000000000000000, 0.7874015748031456541 ) ) ;
#21697=LINE ( 'NONE', #25563, #41470 ) ;
#21698=LINE ( 'NONE', #25821, #32895 ) ;
#21699=CARTESIAN_POINT ( 'NONE',  ( -1.166969139818015755, 0.000000000000000000, 0.5905511811023582691 ) ) ;
#21700=CARTESIAN_POINT ( 'NONE',  ( 1.091055626815042645, 3.346456692913386100, -0.3149606299212596716 ) ) ;
#21702=CARTESIAN_POINT ( 'NONE',  ( -1.091055626815042645, 0.000000000000000000, -1.889763779527552146 ) ) ;
#21703=EDGE_CURVE ( 'NONE', #29397, #32424, #42872, .T. ) ;
#21704=CARTESIAN_POINT ( 'NONE',  ( 0.000000000000000000, 3.267716535433071279, -0.4724409448818886470 ) ) ;
#21705=EDGE_CURVE ( 'NONE', #50730, #19354, #31523, .T. ) ;
#21706=PLANE ( 'NONE',  #30001 ) ;
#21707=EDGE_CURVE ( 'NONE', #34031, #12607, #50822, .T. ) ;
#21709=EDGE_LOOP ( 'NONE', ( #48048, #45891, #38793, #42193 ) ) ;
#21712=ORIENTED_EDGE ( 'NONE', *, *, #34639, .F. ) ;
#21713=VECTOR ( 'NONE', #10884, 39.37007874015748143 ) ;
#21714=ORIENTED_EDGE ( 'NONE', *, *, #37067, .T. ) ;
#21715=VECTOR ( 'NONE', #22214, 39.37007874015748143 ) ;
#21716=CARTESIAN_POINT ( 'NONE',  ( -1.363819533518803473, 3.267716535433071279, -0.7874015748031470974 ) ) ;
#21718=ADVANCED_FACE ( 'NONE', ( #35396 ), #35144, .F. ) ;
#21719=AXIS2_PLACEMENT_3D ( 'NONE', #18148, #37017, #25890 ) ;
#21721=CARTESIAN_POINT ( 'NONE',  ( -0.8182917201112817063, 3.267716535433071279, 1.419509857074483046E-16 ) ) ;
#21722=EDGE_CURVE ( 'NONE', #4354, #4010, #47479, .T. ) ;
#21724=ORIENTED_EDGE ( 'NONE', *, *, #24485, .T. ) ;
#21725=DIRECTION ( 'NONE',  ( 1.734723475976806848E-16, 0.000000000000000000, 1.000000000000000000 ) ) ;
#21726=EDGE_CURVE ( 'NONE', #1147, #20835, #46967, .T. ) ;
#21727=LINE ( 'NONE', #48281, #37944 ) ;
#21728=EDGE_CURVE ( 'NONE', #9285, #17328, #31014, .T. ) ;
#21729=ORIENTED_EDGE ( 'NONE', *, *, #16552, .F. ) ;
#21731=DIRECTION ( 'NONE',  ( 1.000000000000000000, 0.000000000000000000, 0.000000000000000000 ) ) ;
#21733=EDGE_LOOP ( 'NONE', ( #31243, #13930, #12430, #16469 ) ) ;
#21735=DIRECTION ( 'NONE',  ( -0.000000000000000000, 1.000000000000000000, -0.000000000000000000 ) ) ;
#21736=DIRECTION ( 'NONE',  ( 0.000000000000000000, 0.000000000000000000, 1.000000000000000000 ) ) ;
#21737=DIRECTION ( 'NONE',  ( 1.734723475976806848E-16, -0.000000000000000000, 1.000000000000000000 ) ) ;
#21738=VERTEX_POINT ( 'NONE', #7769 ) ;
#21739=LINE ( 'NONE', #14237, #8989 ) ;
#21741=DIRECTION ( 'NONE',  ( -0.000000000000000000, 1.000000000000000000, -0.000000000000000000 ) ) ;
#21744=VECTOR ( 'NONE', #23245, 39.37007874015748143 ) ;
#21745=CARTESIAN_POINT ( 'NONE',  ( 0.000000000000000000, 3.267716535433071279, -0.9842519685039342603 ) ) ;
#21748=VECTOR ( 'NONE', #38971, 39.37007874015748143 ) ;
#21752=DIRECTION ( 'NONE',  ( 1.734723475976806848E-16, -0.000000000000000000, 1.000000000000000000 ) ) ;
#21754=LINE ( 'NONE', #45724, #46867 ) ;
#21755=ORIENTED_EDGE ( 'NONE', *, *, #47608, .F. ) ;
#21756=VERTEX_POINT ( 'NONE', #534 ) ;
#21759=VERTEX_POINT ( 'NONE', #32042 ) ;
#21760=DIRECTION ( 'NONE',  ( 1.000000000000000000, 0.000000000000000000, 0.000000000000000000 ) ) ;
#21762=ADVANCED_FACE ( 'NONE', ( #3901 ), #43119, .F. ) ;
#21764=ADVANCED_FACE ( 'NONE', ( #47216 ), #47732, .F. ) ;
#21765=CARTESIAN_POINT ( 'NONE',  ( -1.166969139818015977, 3.346456692913386100, -0.7874015748031470974 ) ) ;
#21766=CARTESIAN_POINT ( 'NONE',  ( 1.636583440222563857, 3.346456692913386100, 0.4330708661417290162 ) ) ;
#21768=EDGE_CURVE ( 'NONE', #15363, #48074, #21184, .T. ) ;
#21769=DIRECTION ( 'NONE',  ( -3.469446951953613696E-16, 0.000000000000000000, -1.000000000000000000 ) ) ;
#21770=CARTESIAN_POINT ( 'NONE',  ( 1.636583440222563857, 3.346456692913386100, -1.161035397307311917E-15 ) ) ;
#21771=PLANE ( 'NONE',  #30654 ) ;
#21773=LINE ( 'NONE', #37276, #32295 ) ;
#21774=DIRECTION ( 'NONE',  ( 1.000000000000000000, 0.000000000000000000, 0.000000000000000000 ) ) ;
#21777=DIRECTION ( 'NONE',  ( -3.469446951953613696E-16, 0.000000000000000000, -1.000000000000000000 ) ) ;
#21779=VECTOR ( 'NONE', #17817, 39.37007874015748143 ) ;
#21780=ORIENTED_EDGE ( 'NONE', *, *, #24049, .F. ) ;
#21781=VECTOR ( 'NONE', #40869, 39.37007874015748143 ) ;
#21782=DIRECTION ( 'NONE',  ( 1.000000000000000000, -0.000000000000000000, 0.000000000000000000 ) ) ;
#21786=CARTESIAN_POINT ( 'NONE',  ( 1.909347346926324684, 3.346456692913386100, 0.2755905511810994302 ) ) ;
#21787=AXIS2_PLACEMENT_3D ( 'NONE', #5793, #31611, #39357 ) ;
#21789=DIRECTION ( 'NONE',  ( -0.000000000000000000, 0.000000000000000000, 1.000000000000000000 ) ) ;
#21790=EDGE_CURVE ( 'NONE', #5106, #28960, #44148, .T. ) ;
#21791=CARTESIAN_POINT ( 'NONE',  ( 0.7423782071083088185, 3.267716535433071279, -2.575641807848710687E-16 ) ) ;
#21792=LINE ( 'NONE', #29272, #43325 ) ;
#21793=PLANE ( 'NONE',  #14739 ) ;
#21794=ORIENTED_EDGE ( 'NONE', *, *, #6288, .T. ) ;
#21795=ORIENTED_EDGE ( 'NONE', *, *, #17693, .F. ) ;
#21797=VECTOR ( 'NONE', #11849, 39.37007874015748143 ) ;
#21798=DIRECTION ( 'NONE',  ( -3.469446951953613696E-16, 0.000000000000000000, -1.000000000000000000 ) ) ;
#21801=LINE ( 'NONE', #18176, #30036 ) ;
#21802=DIRECTION ( 'NONE',  ( -0.000000000000000000, 1.000000000000000000, -0.000000000000000000 ) ) ;
#21803=DIRECTION ( 'NONE',  ( 1.000000000000000000, -0.000000000000000000, 0.000000000000000000 ) ) ;
#21806=DIRECTION ( 'NONE',  ( -1.000000000000000000, 0.000000000000000000, 0.000000000000000000 ) ) ;
#21807=CARTESIAN_POINT ( 'NONE',  ( -1.363819533518803473, 0.000000000000000000, -1.299212598425192544 ) ) ;
#21809=ORIENTED_EDGE ( 'NONE', *, *, #5098, .T. ) ;
#21810=DIRECTION ( 'NONE',  ( 1.734723475976806848E-16, -0.000000000000000000, 1.000000000000000000 ) ) ;
#21811=PLANE ( 'NONE',  #12836 ) ;
#21812=ORIENTED_EDGE ( 'NONE', *, *, #39965, .F. ) ;
#21813=CARTESIAN_POINT ( 'NONE',  ( 2.106197740627111514, 3.346456692913386100, -1.299212598425194320 ) ) ;
#21814=ORIENTED_EDGE ( 'NONE', *, *, #39366, .F. ) ;
#21815=EDGE_LOOP ( 'NONE', ( #25614, #31630, #34928, #17050 ) ) ;
#21816=CARTESIAN_POINT ( 'NONE',  ( 0.000000000000000000, 3.267716535433071279, -1.299212598425193210 ) ) ;
#21817=FACE_OUTER_BOUND ( 'NONE', #18190, .T. ) ;
#21820=DIRECTION ( 'NONE',  ( 0.000000000000000000, -1.000000000000000000, 0.000000000000000000 ) ) ;
#21821=ORIENTED_EDGE ( 'NONE', *, *, #19328, .T. ) ;
#21826=CARTESIAN_POINT ( 'NONE',  ( -0.07591351300297340121, 0.000000000000000000, 2.165354330708650465 ) ) ;
#21827=VECTOR ( 'NONE', #31682, 39.37007874015748143 ) ;
#21828=VECTOR ( 'NONE', #49222, 39.37007874015748143 ) ;
#21830=EDGE_CURVE ( 'NONE', #9429, #35180, #20962, .T. ) ;
#21831=CARTESIAN_POINT ( 'NONE',  ( 0.2727639067037602172, 0.000000000000000000, -2.047244094488182231 ) ) ;
#21832=LINE ( 'NONE', #37588, #27000 ) ;
#21833=VECTOR ( 'NONE', #30760, 39.37007874015748143 ) ;
#21835=ADVANCED_FACE ( 'NONE', ( #44406 ), #40806, .F. ) ;
#21837=EDGE_CURVE ( 'NONE', #49411, #38085, #13186, .T. ) ;
#21838=DIRECTION ( 'NONE',  ( -0.000000000000000000, 1.000000000000000000, -0.000000000000000000 ) ) ;
#21839=EDGE_CURVE ( 'NONE', #37269, #12892, #1299, .T. ) ;
#21840=ORIENTED_EDGE ( 'NONE', *, *, #8722, .F. ) ;
#21841=DIRECTION ( 'NONE',  ( -0.000000000000000000, 0.000000000000000000, 1.000000000000000000 ) ) ;
#21843=ORIENTED_EDGE ( 'NONE', *, *, #47181, .F. ) ;
#21844=DIRECTION ( 'NONE',  ( -0.000000000000000000, 1.000000000000000000, -0.000000000000000000 ) ) ;
#21847=ORIENTED_EDGE ( 'NONE', *, *, #45306, .T. ) ;
#21848=LINE ( 'NONE', #49420, #771 ) ;
#21850=FACE_BOUND ( 'NONE', #13363, .T. ) ;
#21851=CARTESIAN_POINT ( 'NONE',  ( 0.000000000000000000, 3.267716535433071279, 0.9055118110236164419 ) ) ;
#21852=DIRECTION ( 'NONE',  ( 1.734723475976806848E-16, -0.000000000000000000, 1.000000000000000000 ) ) ;
#21853=ADVANCED_FACE ( 'NONE', ( #20660 ), #13695, .F. ) ;
#21855=DIRECTION ( 'NONE',  ( -0.000000000000000000, 1.000000000000000000, -0.000000000000000000 ) ) ;
#21858=VECTOR ( 'NONE', #5437, 39.37007874015748143 ) ;
#21859=FACE_OUTER_BOUND ( 'NONE', #31031, .T. ) ;
#21860=ORIENTED_EDGE ( 'NONE', *, *, #36729, .F. ) ;
#21862=VECTOR ( 'NONE', #4159, 39.37007874015748143 ) ;
#21864=ORIENTED_EDGE ( 'NONE', *, *, #44999, .F. ) ;
#21866=LINE ( 'NONE', #38128, #23137 ) ;
#21867=ORIENTED_EDGE ( 'NONE', *, *, #23770, .T. ) ;
#21870=VECTOR ( 'NONE', #28311, 39.37007874015748143 ) ;
#21871=ORIENTED_EDGE ( 'NONE', *, *, #6109, .F. ) ;
#21873=ORIENTED_EDGE ( 'NONE', *, *, #48881, .F. ) ;
#21875=ADVANCED_FACE ( 'NONE', ( #24798 ), #40549, .F. ) ;
#21876=ORIENTED_EDGE ( 'NONE', *, *, #21324, .F. ) ;
#21877=VERTEX_POINT ( 'NONE', #37451 ) ;
#21878=CARTESIAN_POINT ( 'NONE',  ( 1.091055626815042645, 3.346456692913386100, -8.878505979408855953E-16 ) ) ;
#21879=ORIENTED_EDGE ( 'NONE', *, *, #20957, .T. ) ;
#21880=FACE_OUTER_BOUND ( 'NONE', #37082, .T. ) ;
#21883=ORIENTED_EDGE ( 'NONE', *, *, #20695, .T. ) ;
#21884=DIRECTION ( 'NONE',  ( -1.000000000000000000, 0.000000000000000000, 1.734723475976806848E-16 ) ) ;
#21885=LINE ( 'NONE', #49210, #24630 ) ;
#21886=VECTOR ( 'NONE', #12616, 39.37007874015748143 ) ;
#21888=EDGE_CURVE ( 'NONE', #43399, #9369, #17315, .T. ) ;
#21889=DIRECTION ( 'NONE',  ( 1.734723475976806848E-16, -0.000000000000000000, 1.000000000000000000 ) ) ;
#21890=DIRECTION ( 'NONE',  ( 1.000000000000000000, 0.000000000000000000, 0.000000000000000000 ) ) ;
#21891=VECTOR ( 'NONE', #3370, 39.37007874015748143 ) ;
#21892=FACE_OUTER_BOUND ( 'NONE', #41983, .T. ) ;
#21893=AXIS2_PLACEMENT_3D ( 'NONE', #1590, #13978, #25085 ) ;
#21895=EDGE_CURVE ( 'NONE', #4115, #32803, #32298, .T. ) ;
#21896=ORIENTED_EDGE ( 'NONE', *, *, #30115, .F. ) ;
#21903=ADVANCED_FACE ( 'NONE', ( #1812 ), #12660, .F. ) ;
#21904=DIRECTION ( 'NONE',  ( -1.000000000000000000, -0.000000000000000000, -0.000000000000000000 ) ) ;
#21905=VECTOR ( 'NONE', #32204, 39.37007874015748143 ) ;
#21906=ORIENTED_EDGE ( 'NONE', *, *, #29410, .F. ) ;
#21907=CARTESIAN_POINT ( 'NONE',  ( 0.000000000000000000, 0.000000000000000000, 0.000000000000000000 ) ) ;
#21908=ORIENTED_EDGE ( 'NONE', *, *, #14908, .T. ) ;
#21909=CARTESIAN_POINT ( 'NONE',  ( 1.636583440222563857, 0.000000000000000000, 1.377952755905504256 ) ) ;
#21910=CARTESIAN_POINT ( 'NONE',  ( -1.536664496436148184E-16, 3.346456692913386100, -0.5118110236220465570 ) ) ;
#21911=CARTESIAN_POINT ( 'NONE',  ( 3.519654186525858491E-16, 0.000000000000000000, 2.874015748031496731 ) ) ;
#21912=LINE ( 'NONE', #44872, #42406 ) ;
#21914=CARTESIAN_POINT ( 'NONE',  ( 1.363819533518803695, 3.346456692913386100, 1.732283464566921172 ) ) ;
#21916=LINE ( 'NONE', #29910, #47155 ) ;
#21917=VERTEX_POINT ( 'NONE', #10326 ) ;
#21919=LINE ( 'NONE', #37678, #18821 ) ;
#21920=VERTEX_POINT ( 'NONE', #14195 ) ;
#21922=LINE ( 'NONE', #2295, #34533 ) ;
#21924=ORIENTED_EDGE ( 'NONE', *, *, #34992, .F. ) ;
#21925=CARTESIAN_POINT ( 'NONE',  ( 1.287906020515830141, 3.267716535433071279, 0.1181102362204704270 ) ) ;
#21926=EDGE_CURVE ( 'NONE', #50326, #19099, #30899, .T. ) ;
#21927=CARTESIAN_POINT ( 'NONE',  ( 0.2727639067037602172, 3.267716535433071279, -2.047244094488182231 ) ) ;
#21928=CARTESIAN_POINT ( 'NONE',  ( 1.363819533518803251, 0.000000000000000000, -0.9842519685039348154 ) ) ;
#21929=VECTOR ( 'NONE', #42387, 39.37007874015748143 ) ;
#21930=ORIENTED_EDGE ( 'NONE', *, *, #6795, .F. ) ;
#21932=VECTOR ( 'NONE', #50169, 39.37007874015748143 ) ;
#21933=LINE ( 'NONE', #3067, #17475 ) ;
#21934=FACE_BOUND ( 'NONE', #1589, .T. ) ;
#21935=ORIENTED_EDGE ( 'NONE', *, *, #18346, .T. ) ;
#21937=VECTOR ( 'NONE', #43740, 39.37007874015748143 ) ;
#21938=CARTESIAN_POINT ( 'NONE',  ( 0.000000000000000000, 3.267716535433071279, 0.7874015748031454320 ) ) ;
#21939=DIRECTION ( 'NONE',  ( 1.734723475976806848E-16, -0.000000000000000000, 1.000000000000000000 ) ) ;
#21940=VECTOR ( 'NONE', #25272, 39.37007874015748143 ) ;
#21943=DIRECTION ( 'NONE',  ( 1.734723475976806848E-16, -0.000000000000000000, 1.000000000000000000 ) ) ;
#21944=AXIS2_PLACEMENT_3D ( 'NONE', #39808, #16319, #572 ) ;
#21946=ADVANCED_FACE ( 'NONE', ( #50959 ), #7402, .F. ) ;
#21947=ORIENTED_EDGE ( 'NONE', *, *, #23193, .F. ) ;
#21948=ORIENTED_EDGE ( 'NONE', *, *, #15352, .T. ) ;
#21949=VERTEX_POINT ( 'NONE', #41823 ) ;
#21951=DIRECTION ( 'NONE',  ( -3.469446951953613696E-16, 0.000000000000000000, -1.000000000000000000 ) ) ;
#21952=FACE_OUTER_BOUND ( 'NONE', #39367, .T. ) ;
#21955=EDGE_LOOP ( 'NONE', ( #43206, #40976, #2554, #41669 ) ) ;
#21956=ORIENTED_EDGE ( 'NONE', *, *, #30052, .F. ) ;
#21958=CARTESIAN_POINT ( 'NONE',  ( 0.4696143004045479352, 3.346456692913386100, 0.1574803149606283648 ) ) ;
#21959=DIRECTION ( 'NONE',  ( -0.000000000000000000, 1.000000000000000000, -0.000000000000000000 ) ) ;
#21960=CARTESIAN_POINT ( 'NONE',  ( 1.287906020515829919, 3.249608194809333384, -2.086614173228340086 ) ) ;
#21963=CARTESIAN_POINT ( 'NONE',  ( 2.367016559580884305, 3.255337473942148119, 0.6299212598425161236 ) ) ;
#21964=VECTOR ( 'NONE', #15839, 39.37007874015748143 ) ;
#21966=PLANE ( 'NONE',  #38266 ) ;
#21968=CIRCLE ( 'NONE', #39264, 2.165354330708661568 ) ;
#21973=VECTOR ( 'NONE', #43677, 39.37007874015748143 ) ;
#21977=ORIENTED_EDGE ( 'NONE', *, *, #44980, .F. ) ;
#21978=VERTEX_POINT ( 'NONE', #2073 ) ;
#21979=DIRECTION ( 'NONE',  ( 1.000000000000000000, -0.000000000000000000, 0.000000000000000000 ) ) ;
#21980=EDGE_LOOP ( 'NONE', ( #9980, #26106, #40288, #32422 ) ) ;
#21981=DIRECTION ( 'NONE',  ( -3.469446951953613696E-16, 0.000000000000000000, -1.000000000000000000 ) ) ;
#21982=DIRECTION ( 'NONE',  ( 0.000000000000000000, 0.000000000000000000, -1.000000000000000000 ) ) ;
#21985=ORIENTED_EDGE ( 'NONE', *, *, #20046, .T. ) ;
#21986=LINE ( 'NONE', #33869, #46069 ) ;
#21988=ORIENTED_EDGE ( 'NONE', *, *, #24280, .F. ) ;
#21989=LINE ( 'NONE', #9604, #48704 ) ;
#21991=DIRECTION ( 'NONE',  ( -0.000000000000000000, 1.000000000000000000, -0.000000000000000000 ) ) ;
#21993=ORIENTED_EDGE ( 'NONE', *, *, #35590, .T. ) ;
#21994=EDGE_CURVE ( 'NONE', #7323, #5416, #43002, .T. ) ;
#21995=CARTESIAN_POINT ( 'NONE',  ( 1.909347346926324684, 3.346456692913386100, 0.2755905511810994302 ) ) ;
#21997=DIRECTION ( 'NONE',  ( 1.734723475976806848E-16, -0.000000000000000000, 1.000000000000000000 ) ) ;
#21998=EDGE_CURVE ( 'NONE', #48458, #14599, #3636, .T. ) ;
#21999=AXIS2_PLACEMENT_3D ( 'NONE', #3283, #19025, #35290 ) ;
#22000=EDGE_LOOP ( 'NONE', ( #42374, #47758, #17795, #40398 ) ) ;
#22001=CARTESIAN_POINT ( 'NONE',  ( -2.182111253630085290, 0.000000000000000000, -6.146657985744592735E-16 ) ) ;
#22003=AXIS2_PLACEMENT_3D ( 'NONE', #25250, #30135, #33775 ) ;
#22005=CARTESIAN_POINT ( 'NONE',  ( -0.07591351300297277671, 0.000000000000000000, 1.732283464566921172 ) ) ;
#22006=VERTEX_POINT ( 'NONE', #11773 ) ;
#22007=ORIENTED_EDGE ( 'NONE', *, *, #11116, .T. ) ;
#22008=LINE ( 'NONE', #22262, #27444 ) ;
#22009=VECTOR ( 'NONE', #41123, 39.37007874015748143 ) ;
#22010=PLANE ( 'NONE',  #24475 ) ;
#22011=EDGE_CURVE ( 'NONE', #49275, #6745, #7902, .T. ) ;
#22014=ORIENTED_EDGE ( 'NONE', *, *, #41634, .F. ) ;
#22015=VECTOR ( 'NONE', #45262, 39.37007874015748143 ) ;
#22016=FACE_OUTER_BOUND ( 'NONE', #40072, .T. ) ;
#22017=ORIENTED_EDGE ( 'NONE', *, *, #14908, .F. ) ;
#22018=LINE ( 'NONE', #7022, #16741 ) ;
#22019=DIRECTION ( 'NONE',  ( 1.734723475976806848E-16, -0.000000000000000000, 1.000000000000000000 ) ) ;
#22020=EDGE_CURVE ( 'NONE', #26854, #11981, #29946, .T. ) ;
#22021=ADVANCED_FACE ( 'NONE', ( #23388 ), #46855, .F. ) ;
#22022=LINE ( 'NONE', #18902, #40694 ) ;
#22024=CARTESIAN_POINT ( 'NONE',  ( -0.3486774197067339376, 0.000000000000000000, -0.9448818897637762948 ) ) ;
#22027=LINE ( 'NONE', #33147, #28304 ) ;
#22028=CARTESIAN_POINT ( 'NONE',  ( -1.636583440222564301, 3.346456692913386100, 1.574803149606291530 ) ) ;
#22029=LINE ( 'NONE', #30781, #11705 ) ;
#22031=DIRECTION ( 'NONE',  ( -0.000000000000000000, 0.000000000000000000, 1.000000000000000000 ) ) ;
#22033=CARTESIAN_POINT ( 'NONE',  ( -0.6214413264104945434, 0.000000000000000000, 0.1574803149606285035 ) ) ;
#22034=ORIENTED_EDGE ( 'NONE', *, *, #16179, .T. ) ;
#22035=AXIS2_PLACEMENT_3D ( 'NONE', #34477, #46562, #3990 ) ;
#22038=ORIENTED_EDGE ( 'NONE', *, *, #38588, .T. ) ;
#22039=DIRECTION ( 'NONE',  ( 1.734723475976806848E-16, -0.000000000000000000, 1.000000000000000000 ) ) ;
#22042=LINE ( 'NONE', #2923, #14658 ) ;
#22044=CARTESIAN_POINT ( 'NONE',  ( 0.2727639067037602172, 3.346456692913386100, -2.047244094488182231 ) ) ;
#22045=DIRECTION ( 'NONE',  ( 0.000000000000000000, 0.000000000000000000, -1.000000000000000000 ) ) ;
#22047=ORIENTED_EDGE ( 'NONE', *, *, #29656, .T. ) ;
#22049=CARTESIAN_POINT ( 'NONE',  ( 1.015142113812069313, 0.000000000000000000, 0.1574803149606286423 ) ) ;
#22050=ORIENTED_EDGE ( 'NONE', *, *, #14029, .T. ) ;
#22051=CARTESIAN_POINT ( 'NONE',  ( -0.8182917201112814842, 0.000000000000000000, 0.2755905511810998187 ) ) ;
#22052=CARTESIAN_POINT ( 'NONE',  ( 0.000000000000000000, 3.267716535433071279, -1.456692913385822186 ) ) ;
#22053=CARTESIAN_POINT ( 'NONE',  ( 1.909347346926324462, 3.267716535433071279, -0.7874015748031473194 ) ) ;
#22054=VECTOR ( 'NONE', #39723, 39.37007874015748143 ) ;
#22055=ORIENTED_EDGE ( 'NONE', *, *, #29269, .T. ) ;
#22060=LINE ( 'NONE', #46031, #20392 ) ;
#22061=ADVANCED_FACE ( 'NONE', ( #36302 ), #929, .F. ) ;
#22064=EDGE_CURVE ( 'NONE', #36994, #41352, #19768, .T. ) ;
#22065=CARTESIAN_POINT ( 'NONE',  ( 1.091055626815042645, 3.267716535433071279, -1.892679809432644882E-16 ) ) ;
#22067=DIRECTION ( 'NONE',  ( -0.000000000000000000, 1.000000000000000000, -0.000000000000000000 ) ) ;
#22068=ORIENTED_EDGE ( 'NONE', *, *, #29050, .F. ) ;
#22073=CARTESIAN_POINT ( 'NONE',  ( 1.091055626815042645, 3.346456692913386100, -0.9448818897637765168 ) ) ;
#22075=VECTOR ( 'NONE', #38484, 39.37007874015748143 ) ;
#22076=VERTEX_POINT ( 'NONE', #24423 ) ;
#22078=LINE ( 'NONE', #10454, #35373 ) ;
#22079=ORIENTED_EDGE ( 'NONE', *, *, #39152, .T. ) ;
#22080=VECTOR ( 'NONE', #50752, 39.37007874015748143 ) ;
#22081=EDGE_CURVE ( 'NONE', #3016, #16822, #28800, .T. ) ;
#22083=DIRECTION ( 'NONE',  ( -3.469446951953613696E-16, 0.000000000000000000, -1.000000000000000000 ) ) ;
#22086=CARTESIAN_POINT ( 'NONE',  ( 0.5786196242795136335, 3.346456692913386100, -2.086614173228340086 ) ) ;
#22087=EDGE_CURVE ( 'NONE', #22241, #33634, #16162, .T. ) ;
#22088=LINE ( 'NONE', #2210, #50028 ) ;
#22089=CARTESIAN_POINT ( 'NONE',  ( 1.363819533518803695, 0.000000000000000000, 1.732283464566921172 ) ) ;
#22095=DIRECTION ( 'NONE',  ( 1.734723475976806848E-16, 0.000000000000000000, 1.000000000000000000 ) ) ;
#22096=ORIENTED_EDGE ( 'NONE', *, *, #4929, .F. ) ;
#22097=CARTESIAN_POINT ( 'NONE',  ( -1.091055626815042423, 3.267716535433071279, 1.892679809432644143E-16 ) ) ;
#22099=ORIENTED_EDGE ( 'NONE', *, *, #5327, .T. ) ;
#22100=CARTESIAN_POINT ( 'NONE',  ( 0.000000000000000000, 3.267716535433071279, -1.614173228346451605 ) ) ;
#22101=DIRECTION ( 'NONE',  ( -0.000000000000000000, 0.000000000000000000, 1.000000000000000000 ) ) ;
#22103=ORIENTED_EDGE ( 'NONE', *, *, #40679, .F. ) ;
#22104=DIRECTION ( 'NONE',  ( 1.000000000000000000, 0.000000000000000000, 0.000000000000000000 ) ) ;
#22105=ORIENTED_EDGE ( 'NONE', *, *, #4605, .F. ) ;
#22106=FACE_BOUND ( 'NONE', #1985, .T. ) ;
#22107=LINE ( 'NONE', #21593, #29214 ) ;
#22108=CARTESIAN_POINT ( 'NONE',  ( -0.5455278134075214336, 3.346456692913386100, -0.6299212598425175669 ) ) ;
#22109=PLANE ( 'NONE',  #16105 ) ;
#22111=AXIS2_PLACEMENT_3D ( 'NONE', #20626, #1005, #16764 ) ;
#22114=DIRECTION ( 'NONE',  ( -1.000000000000000000, 0.000000000000000000, 0.000000000000000000 ) ) ;
#22115=AXIS2_PLACEMENT_3D ( 'NONE', #4470, #12986, #597 ) ;
#22116=DIRECTION ( 'NONE',  ( 0.000000000000000000, 1.000000000000000000, 0.000000000000000000 ) ) ;
#22119=VECTOR ( 'NONE', #25333, 39.37007874015748143 ) ;
#22120=ORIENTED_EDGE ( 'NONE', *, *, #41023, .F. ) ;
#22121=CARTESIAN_POINT ( 'NONE',  ( -1.363819533518803473, 0.000000000000000000, 1.732283464566920950 ) ) ;
#22123=B_SPLINE_CURVE_WITH_KNOTS ( 'NONE', 3,
 ( #13970, #48523, #12953, #1323 ),
 .UNSPECIFIED., .F., .F.,
 ( 4, 4 ),
 ( 0.02786225668000808300, 0.02887988550437843929 ),
 .UNSPECIFIED. ) ;
#22125=EDGE_CURVE ( 'NONE', #48282, #1443, #5057, .T. ) ;
#22126=ORIENTED_EDGE ( 'NONE', *, *, #20955, .F. ) ;
#22127=ADVANCED_FACE ( 'NONE', ( #4547 ), #20805, .F. ) ;
#22128=CARTESIAN_POINT ( 'NONE',  ( -0.3486774197067343262, 0.000000000000000000, -2.401574803149598036 ) ) ;
#22129=ORIENTED_EDGE ( 'NONE', *, *, #46607, .T. ) ;
#22132=EDGE_CURVE ( 'NONE', #1749, #10246, #20284, .T. ) ;
#22133=ORIENTED_EDGE ( 'NONE', *, *, #48624, .F. ) ;
#22134=ORIENTED_EDGE ( 'NONE', *, *, #12292, .T. ) ;
#22135=LINE ( 'NONE', #44840, #32705 ) ;
#22137=LINE ( 'NONE', #41496, #28734 ) ;
#22140=AXIS2_PLACEMENT_3D ( 'NONE', #45127, #26039, #33291 ) ;
#22141=LINE ( 'NONE', #9500, #33843 ) ;
#22143=PLANE ( 'NONE',  #20380 ) ;
#22144=ORIENTED_EDGE ( 'NONE', *, *, #50183, .T. ) ;
#22145=EDGE_CURVE ( 'NONE', #43925, #39410, #35785, .T. ) ;
#22146=CARTESIAN_POINT ( 'NONE',  ( 0.2727639067037602172, 3.346456692913386100, -2.088563196121306476 ) ) ;
#22147=LINE ( 'NONE', #30397, #45597 ) ;
#22149=VECTOR ( 'NONE', #8596, 39.37007874015748143 ) ;
#22152=VECTOR ( 'NONE', #4019, 39.37007874015748143 ) ;
#22156=DIRECTION ( 'NONE',  ( 0.000000000000000000, 1.000000000000000000, 0.000000000000000000 ) ) ;
#22157=EDGE_LOOP ( 'NONE', ( #30303, #18241, #4540, #33602 ) ) ;
#22158=CARTESIAN_POINT ( 'NONE',  ( -1.091055626815042645, 3.346456692913386100, 1.870389530743259199 ) ) ;
#22159=CARTESIAN_POINT ( 'NONE',  ( 0.5455278134075211005, 0.000000000000000000, -0.8267716535433055070 ) ) ;
#22160=VECTOR ( 'NONE', #34520, 39.37007874015748143 ) ;
#22161=ORIENTED_EDGE ( 'NONE', *, *, #29311, .T. ) ;
#22163=VERTEX_POINT ( 'NONE', #673 ) ;
#22165=LINE ( 'NONE', #22667, #46469 ) ;
#22166=CARTESIAN_POINT ( 'NONE',  ( 0.7423782071083087075, 3.346456692913386100, -0.6299212598425181220 ) ) ;
#22167=VECTOR ( 'NONE', #50209, 39.37007874015748143 ) ;
#22168=CARTESIAN_POINT ( 'NONE',  ( -0.5455278134075208785, 0.000000000000000000, 0.7480314960629874665 ) ) ;
#22169=FACE_OUTER_BOUND ( 'NONE', #31129, .T. ) ;
#22174=DIRECTION ( 'NONE',  ( -1.000000000000000000, 0.000000000000000000, -0.000000000000000000 ) ) ;
#22175=VERTEX_POINT ( 'NONE', #45540 ) ;
#22176=DIRECTION ( 'NONE',  ( 0.000000000000000000, 1.000000000000000000, 0.000000000000000000 ) ) ;
#22177=DIRECTION ( 'NONE',  ( 1.000000000000000000, 0.000000000000000000, 0.000000000000000000 ) ) ;
#22178=ORIENTED_EDGE ( 'NONE', *, *, #29233, .F. ) ;
#22180=AXIS2_PLACEMENT_3D ( 'NONE', #9669, #25405, #5791 ) ;
#22181=CARTESIAN_POINT ( 'NONE',  ( -0.8182917201112819283, 3.346456692913386100, 0.1574803149606285035 ) ) ;
#22183=VERTEX_POINT ( 'NONE', #40684 ) ;
#22184=EDGE_CURVE ( 'NONE', #15712, #14697, #40941, .T. ) ;
#22185=EDGE_LOOP ( 'NONE', ( #38566, #14760, #44317, #15682 ) ) ;
#22186=DIRECTION ( 'NONE',  ( 1.000000000000000000, -0.000000000000000000, 0.000000000000000000 ) ) ;
#22187=FACE_BOUND ( 'NONE', #26188, .T. ) ;
#22188=EDGE_LOOP ( 'NONE', ( #31856, #45679, #49946, #48604 ) ) ;
#22189=EDGE_CURVE ( 'NONE', #15045, #31017, #1177, .T. ) ;
#22191=VECTOR ( 'NONE', #18710, 39.37007874015748143 ) ;
#22192=FACE_OUTER_BOUND ( 'NONE', #28077, .T. ) ;
#22193=LINE ( 'NONE', #6695, #49733 ) ;
#22194=ADVANCED_FACE ( 'NONE', ( #41445 ), #17442, .F. ) ;
#22195=EDGE_CURVE ( 'NONE', #33217, #48211, #36814, .T. ) ;
#22197=ORIENTED_EDGE ( 'NONE', *, *, #30753, .T. ) ;
#22198=VECTOR ( 'NONE', #18082, 39.37007874015748143 ) ;
#22200=LINE ( 'NONE', #46162, #43510 ) ;
#22202=ORIENTED_EDGE ( 'NONE', *, *, #32000, .F. ) ;
#22203=VECTOR ( 'NONE', #29000, 39.37007874015748143 ) ;
#22204=VERTEX_POINT ( 'NONE', #2465 ) ;
#22205=CARTESIAN_POINT ( 'NONE',  ( 0.2727639067037604392, 0.000000000000000000, -1.614173228346451605 ) ) ;
#22206=DIRECTION ( 'NONE',  ( -0.000000000000000000, 1.000000000000000000, -0.000000000000000000 ) ) ;
#22208=DIRECTION ( 'NONE',  ( -0.000000000000000000, 1.000000000000000000, -0.000000000000000000 ) ) ;
#22210=ORIENTED_EDGE ( 'NONE', *, *, #23574, .F. ) ;
#22212=DIRECTION ( 'NONE',  ( 1.000000000000000000, 0.000000000000000000, 0.000000000000000000 ) ) ;
#22214=DIRECTION ( 'NONE',  ( -0.000000000000000000, 1.000000000000000000, -0.000000000000000000 ) ) ;
#22215=EDGE_CURVE ( 'NONE', #15891, #33992, #1437, .T. ) ;
#22217=LINE ( 'NONE', #34090, #38037 ) ;
#22218=CARTESIAN_POINT ( 'NONE',  ( 2.017116292511733189, 3.346456692913386100, -0.7874015748031473194 ) ) ;
#22222=CARTESIAN_POINT ( 'NONE',  ( -0.6214413264104939882, 3.267716535433071279, 1.102362204724404160 ) ) ;
#22223=ORIENTED_EDGE ( 'NONE', *, *, #49898, .F. ) ;
#22224=DIRECTION ( 'NONE',  ( -1.000000000000000000, 0.000000000000000000, -0.000000000000000000 ) ) ;
#22225=DIRECTION ( 'NONE',  ( 1.000000000000000000, 0.000000000000000000, -3.469446951953613696E-16 ) ) ;
#22226=ORIENTED_EDGE ( 'NONE', *, *, #49522, .F. ) ;
#22228=ORIENTED_EDGE ( 'NONE', *, *, #39366, .T. ) ;
#22229=VECTOR ( 'NONE', #1043, 39.37007874015748143 ) ;
#22230=DIRECTION ( 'NONE',  ( 1.000000000000000000, 0.000000000000000000, 0.000000000000000000 ) ) ;
#22232=VECTOR ( 'NONE', #41401, 39.37007874015748143 ) ;
#22233=ORIENTED_EDGE ( 'NONE', *, *, #24518, .F. ) ;
#22234=LINE ( 'NONE', #26594, #8099 ) ;
#22235=ORIENTED_EDGE ( 'NONE', *, *, #26380, .T. ) ;
#22236=LINE ( 'NONE', #22737, #5417 ) ;
#22240=DIRECTION ( 'NONE',  ( -0.000000000000000000, 1.000000000000000000, -0.000000000000000000 ) ) ;
#22241=VERTEX_POINT ( 'NONE', #25693 ) ;
#22242=VERTEX_POINT ( 'NONE', #29314 ) ;
#22243=CARTESIAN_POINT ( 'NONE',  ( 1.287906020515830141, 0.000000000000000000, 0.3149606299212578953 ) ) ;
#22244=PLANE ( 'NONE',  #9508 ) ;
#22248=ORIENTED_EDGE ( 'NONE', *, *, #42636, .T. ) ;
#22249=CARTESIAN_POINT ( 'NONE',  ( -0.8942052331142552601, 3.346456692913386100, -2.086614173228339641 ) ) ;
#22250=CARTESIAN_POINT ( 'NONE',  ( -1.091055626815042201, 0.000000000000000000, 0.4330708661417290162 ) ) ;
#22253=EDGE_CURVE ( 'NONE', #25178, #33862, #37330, .T. ) ;
#22256=DIRECTION ( 'NONE',  ( 0.000000000000000000, -1.000000000000000000, 0.000000000000000000 ) ) ;
#22258=ORIENTED_EDGE ( 'NONE', *, *, #17789, .T. ) ;
#22259=ORIENTED_EDGE ( 'NONE', *, *, #36722, .F. ) ;
#22261=AXIS2_PLACEMENT_3D ( 'NONE', #33772, #25494, #18008 ) ;
#22262=CARTESIAN_POINT ( 'NONE',  ( 0.7423782071083087075, 3.346456692913386100, 0.3149606299212576177 ) ) ;
#22264=CARTESIAN_POINT ( 'NONE',  ( 1.091055626815042645, 3.346456692913386100, -0.9448818897637765168 ) ) ;
#22265=ORIENTED_EDGE ( 'NONE', *, *, #24140, .T. ) ;
#22266=ORIENTED_EDGE ( 'NONE', *, *, #47984, .T. ) ;
#22267=DIRECTION ( 'NONE',  ( -1.000000000000000000, 0.000000000000000000, 0.000000000000000000 ) ) ;
#22268=CARTESIAN_POINT ( 'NONE',  ( 1.091055626815042645, 3.346456692913386100, 0.1181102362204704270 ) ) ;
#22269=VECTOR ( 'NONE', #41597, 39.37007874015748143 ) ;
#22271=CARTESIAN_POINT ( 'NONE',  ( 0.000000000000000000, 3.267716535433071279, -1.299212598425193210 ) ) ;
#22272=DIRECTION ( 'NONE',  ( 1.000000000000000000, 0.000000000000000000, 0.000000000000000000 ) ) ;
#22273=ADVANCED_FACE ( 'NONE', ( #14075 ), #24932, .F. ) ;
#22275=PLANE ( 'NONE',  #39259 ) ;
#22276=PLANE ( 'NONE',  #19625 ) ;
#22277=ORIENTED_EDGE ( 'NONE', *, *, #18231, .F. ) ;
#22278=LINE ( 'NONE', #38780, #25881 ) ;
#22280=CARTESIAN_POINT ( 'NONE',  ( 0.2727639067037604947, 3.346456692913386100, 0.7874015748031454320 ) ) ;
#22281=EDGE_CURVE ( 'NONE', #183, #30123, #45042, .T. ) ;
#22282=ORIENTED_EDGE ( 'NONE', *, *, #49775, .T. ) ;
#22284=EDGE_CURVE ( 'NONE', #41046, #23218, #5819, .T. ) ;
#22286=DIRECTION ( 'NONE',  ( -1.000000000000000000, -0.000000000000000000, -0.000000000000000000 ) ) ;
#22287=ORIENTED_EDGE ( 'NONE', *, *, #1666, .F. ) ;
#22288=EDGE_CURVE ( 'NONE', #50330, #27595, #33463, .T. ) ;
#22290=ADVANCED_FACE ( 'NONE', ( #13827 ), #25952, .F. ) ;
#22291=ORIENTED_EDGE ( 'NONE', *, *, #25800, .F. ) ;
#22292=LINE ( 'NONE', #42655, #31284 ) ;
#22295=EDGE_CURVE ( 'NONE', #12211, #42980, #23087, .T. ) ;
#22296=AXIS2_PLACEMENT_3D ( 'NONE', #39147, #47872, #50961 ) ;
#22297=CARTESIAN_POINT ( 'NONE',  ( -0.3486774197067342151, 3.267716535433071279, -2.204724409448810540 ) ) ;
#22300=VECTOR ( 'NONE', #2635, 39.37007874015748143 ) ;
#22301=ORIENTED_EDGE ( 'NONE', *, *, #47137, .T. ) ;
#22304=LINE ( 'NONE', #37553, #20550 ) ;
#22305=VERTEX_POINT ( 'NONE', #50898 ) ;
#22310=EDGE_CURVE ( 'NONE', #3065, #50816, #35216, .T. ) ;
#22311=ORIENTED_EDGE ( 'NONE', *, *, #34231, .T. ) ;
#22314=LINE ( 'NONE', #34692, #2726 ) ;
#22315=PLANE ( 'NONE',  #37108 ) ;
#22316=EDGE_CURVE ( 'NONE', #27306, #44282, #7350, .T. ) ;
#22317=ORIENTED_EDGE ( 'NONE', *, *, #19445, .F. ) ;
#22319=CARTESIAN_POINT ( 'NONE',  ( 1.091055626815043311, 3.346456692913386100, 1.377952755905504256 ) ) ;
#22320=FACE_BOUND ( 'NONE', #9904, .T. ) ;
#22321=ORIENTED_EDGE ( 'NONE', *, *, #38667, .T. ) ;
#22322=EDGE_CURVE ( 'NONE', #12349, #3787, #39085, .T. ) ;
#22324=EDGE_LOOP ( 'NONE', ( #50639, #44191, #34117, #86 ) ) ;
#22325=VERTEX_POINT ( 'NONE', #42701 ) ;
#22327=FACE_OUTER_BOUND ( 'NONE', #36967, .T. ) ;
#22331=DIRECTION ( 'NONE',  ( -1.000000000000000000, 0.000000000000000000, 1.734723475976806848E-16 ) ) ;
#22333=ORIENTED_EDGE ( 'NONE', *, *, #33464, .F. ) ;
#22334=DIRECTION ( 'NONE',  ( 1.000000000000000000, 0.000000000000000000, 0.000000000000000000 ) ) ;
#22335=CARTESIAN_POINT ( 'NONE',  ( 0.7423782071083091516, 0.000000000000000000, 1.377952755905504256 ) ) ;
#22336=VECTOR ( 'NONE', #37719, 39.37007874015748143 ) ;
#22337=EDGE_CURVE ( 'NONE', #12815, #46776, #26949, .T. ) ;
#22338=LINE ( 'NONE', #38095, #5820 ) ;
#22339=PLANE ( 'NONE',  #31098 ) ;
#22340=CARTESIAN_POINT ( 'NONE',  ( -1.166969139818016199, 3.267716535433071279, -1.299212598425192544 ) ) ;
#22342=CARTESIAN_POINT ( 'NONE',  ( 2.059322335531026837, 3.346456692913386100, -0.6692913385826764205 ) ) ;
#22343=VECTOR ( 'NONE', #44066, 39.37007874015748143 ) ;
#22344=LINE ( 'NONE', #38101, #19899 ) ;
#22345=ORIENTED_EDGE ( 'NONE', *, *, #28596, .F. ) ;
#22347=EDGE_CURVE ( 'NONE', #21029, #14001, #38836, .T. ) ;
#22348=DIRECTION ( 'NONE',  ( 1.000000000000000000, -0.000000000000000000, 0.000000000000000000 ) ) ;
#22350=CARTESIAN_POINT ( 'NONE',  ( -2.182111253630085734, 3.267716535433071279, -0.8267716535433052849 ) ) ;
#22354=PLANE ( 'NONE',  #49074 ) ;
#22356=DIRECTION ( 'NONE',  ( -1.000000000000000000, 0.000000000000000000, 0.000000000000000000 ) ) ;
#22358=DIRECTION ( 'NONE',  ( 0.000000000000000000, -0.000000000000000000, 1.000000000000000000 ) ) ;
#22361=CARTESIAN_POINT ( 'NONE',  ( -0.6214413264104945434, 3.346456692913386100, -2.244094488188968395 ) ) ;
#22363=ORIENTED_EDGE ( 'NONE', *, *, #13841, .F. ) ;
#22364=CARTESIAN_POINT ( 'NONE',  ( 0.000000000000000000, 3.267716535433071279, -0.9448818897637765168 ) ) ;
#22365=DIRECTION ( 'NONE',  ( -3.469446951953613696E-16, 0.000000000000000000, -1.000000000000000000 ) ) ;
#22367=ADVANCED_FACE ( 'NONE', ( #42195 ), #41953, .F. ) ;
#22368=DIRECTION ( 'NONE',  ( 0.000000000000000000, 0.000000000000000000, -1.000000000000000000 ) ) ;
#22369=AXIS2_PLACEMENT_3D ( 'NONE', #20616, #4362, #12617 ) ;
#22370=DIRECTION ( 'NONE',  ( -1.000000000000000000, -0.000000000000000000, -0.000000000000000000 ) ) ;
#22372=AXIS2_PLACEMENT_3D ( 'NONE', #25853, #9858, #6241 ) ;
#22374=ORIENTED_EDGE ( 'NONE', *, *, #17947, .F. ) ;
#22375=CARTESIAN_POINT ( 'NONE',  ( 0.9834642517162937025, 3.346456692913386100, -1.929133858267711110 ) ) ;
#22376=EDGE_CURVE ( 'NONE', #33634, #8308, #31092, .T. ) ;
#22380=EDGE_CURVE ( 'NONE', #34607, #25178, #18458, .T. ) ;
#22382=ORIENTED_EDGE ( 'NONE', *, *, #13289, .T. ) ;
#22383=VECTOR ( 'NONE', #32674, 39.37007874015748143 ) ;
#22385=AXIS2_PLACEMENT_3D ( 'NONE', #45608, #17265, #48449 ) ;
#22386=VERTEX_POINT ( 'NONE', #2966 ) ;
#22387=ORIENTED_EDGE ( 'NONE', *, *, #46001, .T. ) ;
#22388=CARTESIAN_POINT ( 'NONE',  ( 0.000000000000000000, 3.267716535433071279, 1.732283464566921172 ) ) ;
#22389=VERTEX_POINT ( 'NONE', #18716 ) ;
#22390=LINE ( 'NONE', #34015, #42742 ) ;
#22391=CARTESIAN_POINT ( 'NONE',  ( 2.182111253630085290, 0.000000000000000000, -1.161035397307311917E-15 ) ) ;
#22392=CARTESIAN_POINT ( 'NONE',  ( 0.000000000000000000, 3.267716535433071279, -0.6299212598425177889 ) ) ;
#22393=LINE ( 'NONE', #21382, #46682 ) ;
#22397=DIRECTION ( 'NONE',  ( 1.000000000000000000, 0.000000000000000000, 0.000000000000000000 ) ) ;
#22399=DIRECTION ( 'NONE',  ( 1.000000000000000000, 0.000000000000000000, -3.469446951953613696E-16 ) ) ;
#22401=ORIENTED_EDGE ( 'NONE', *, *, #47374, .F. ) ;
#22402=VECTOR ( 'NONE', #37055, 39.37007874015748143 ) ;
#22403=FACE_OUTER_BOUND ( 'NONE', #51021, .T. ) ;
#22404=CARTESIAN_POINT ( 'NONE',  ( -0.5455278134075216556, 0.000000000000000000, -2.204724409448810540 ) ) ;
#22405=ORIENTED_EDGE ( 'NONE', *, *, #24494, .F. ) ;
#22406=CARTESIAN_POINT ( 'NONE',  ( 0.000000000000000000, 3.267716535433071279, -0.5118110236220464460 ) ) ;
#22407=DIRECTION ( 'NONE',  ( -3.469446951953613696E-16, 0.000000000000000000, -1.000000000000000000 ) ) ;
#22409=VECTOR ( 'NONE', #37296, 39.37007874015748143 ) ;
#22410=EDGE_LOOP ( 'NONE', ( #39465, #5489, #50632, #12062 ) ) ;
#22411=EDGE_CURVE ( 'NONE', #1486, #36726, #46304, .T. ) ;
#22413=DIRECTION ( 'NONE',  ( -1.000000000000000000, 0.000000000000000000, 0.000000000000000000 ) ) ;
#22414=ORIENTED_EDGE ( 'NONE', *, *, #41233, .F. ) ;
#22415=CARTESIAN_POINT ( 'NONE',  ( 1.560669927219590525, 0.000000000000000000, 0.2755905511810996522 ) ) ;
#22416=EDGE_CURVE ( 'NONE', #43660, #13332, #4221, .T. ) ;
#22418=AXIS2_PLACEMENT_3D ( 'NONE', #33909, #18664, #18406 ) ;
#22419=DIRECTION ( 'NONE',  ( 0.000000000000000000, 0.000000000000000000, -1.000000000000000000 ) ) ;
#22420=DIRECTION ( 'NONE',  ( 1.734723475976806848E-16, 0.000000000000000000, 1.000000000000000000 ) ) ;
#22421=CARTESIAN_POINT ( 'NONE',  ( -0.2727639067037608278, 0.000000000000000000, 2.165354330708650465 ) ) ;
#22423=CARTESIAN_POINT ( 'NONE',  ( 1.091055626815042645, 3.346456692913386100, -0.1968503937007883287 ) ) ;
#22424=ORIENTED_EDGE ( 'NONE', *, *, #24917, .T. ) ;
#22425=EDGE_LOOP ( 'NONE', ( #9978, #8337, #41600, #47179 ) ) ;
#22428=CARTESIAN_POINT ( 'NONE',  ( -0.8942052331142552601, 3.346456692913386100, -0.9448818897637760728 ) ) ;
#22429=LINE ( 'NONE', #18557, #44176 ) ;
#22431=DIRECTION ( 'NONE',  ( 1.000000000000000000, 0.000000000000000000, 0.000000000000000000 ) ) ;
#22432=EDGE_CURVE ( 'NONE', #784, #50140, #36493, .T. ) ;
#22433=CARTESIAN_POINT ( 'NONE',  ( 0.000000000000000000, 3.267716535433071279, 2.047244094488179567 ) ) ;
#22434=CARTESIAN_POINT ( 'NONE',  ( -0.8182917201112819283, 0.000000000000000000, -0.4724409448818886470 ) ) ;
#22435=ORIENTED_EDGE ( 'NONE', *, *, #30819, .T. ) ;
#22438=LINE ( 'NONE', #10054, #9218 ) ;
#22439=FACE_BOUND ( 'NONE', #13645, .T. ) ;
#22440=ORIENTED_EDGE ( 'NONE', *, *, #10574, .F. ) ;
#22441=VECTOR ( 'NONE', #10943, 39.37007874015748143 ) ;
#22442=CARTESIAN_POINT ( 'NONE',  ( -0.8182917201112819283, 3.346456692913386100, -1.732283464566922726 ) ) ;
#22444=ORIENTED_EDGE ( 'NONE', *, *, #2947, .T. ) ;
#22446=LINE ( 'NONE', #19312, #36483 ) ;
#22447=VECTOR ( 'NONE', #18053, 39.37007874015748143 ) ;
#22448=LINE ( 'NONE', #35078, #24579 ) ;
#22450=ORIENTED_EDGE ( 'NONE', *, *, #3745, .F. ) ;
#22451=VECTOR ( 'NONE', #32165, 39.37007874015748143 ) ;
#22452=ORIENTED_EDGE ( 'NONE', *, *, #19758, .F. ) ;
#22454=VECTOR ( 'NONE', #40197, 39.37007874015748143 ) ;
#22455=FACE_OUTER_BOUND ( 'NONE', #31789, .T. ) ;
#22456=CARTESIAN_POINT ( 'NONE',  ( -0.2727639067037607723, 3.267716535433071279, 0.4724409448818869817 ) ) ;
#22457=EDGE_LOOP ( 'NONE', ( #4695, #20494, #16975, #47129, #6060 ) ) ;
#22458=ORIENTED_EDGE ( 'NONE', *, *, #3746, .T. ) ;
#22459=LINE ( 'NONE', #14712, #1030 ) ;
#22461=LINE ( 'NONE', #26077, #43092 ) ;
#22462=DIRECTION ( 'NONE',  ( 1.000000000000000000, 0.000000000000000000, 0.000000000000000000 ) ) ;
#22466=ADVANCED_FACE ( 'NONE', ( #47040 ), #1112, .F. ) ;
#22468=DIRECTION ( 'NONE',  ( -3.469446951953613696E-16, 0.000000000000000000, -1.000000000000000000 ) ) ;
#22471=ORIENTED_EDGE ( 'NONE', *, *, #22310, .T. ) ;
#22475=VECTOR ( 'NONE', #12395, 39.37007874015748143 ) ;
#22478=VECTOR ( 'NONE', #6372, 39.37007874015748143 ) ;
#22479=VERTEX_POINT ( 'NONE', #16100 ) ;
#22480=CARTESIAN_POINT ( 'NONE',  ( 0.000000000000000000, 3.267716535433071279, -0.4724409448818883694 ) ) ;
#22481=AXIS2_PLACEMENT_3D ( 'NONE', #28967, #40353, #16861 ) ;
#22482=ORIENTED_EDGE ( 'NONE', *, *, #46574, .T. ) ;
#22483=AXIS2_PLACEMENT_3D ( 'NONE', #12999, #16874, #21760 ) ;
#22486=PLANE ( 'NONE',  #19775 ) ;
#22488=VERTEX_POINT ( 'NONE', #16360 ) ;
#22489=DIRECTION ( 'NONE',  ( -1.000000000000000000, 0.000000000000000000, 1.734723475976806848E-16 ) ) ;
#22490=ORIENTED_EDGE ( 'NONE', *, *, #33087, .T. ) ;
#22493=DIRECTION ( 'NONE',  ( -0.000000000000000000, 1.000000000000000000, -0.000000000000000000 ) ) ;
#22494=FACE_OUTER_BOUND ( 'NONE', #40808, .T. ) ;
#22496=LINE ( 'NONE', #50552, #44137 ) ;
#22497=VERTEX_POINT ( 'NONE', #19710 ) ;
#22499=DIRECTION ( 'NONE',  ( 1.000000000000000000, 0.000000000000000000, -3.469446951953613696E-16 ) ) ;
#22500=LINE ( 'NONE', #38256, #42649 ) ;
#22501=EDGE_LOOP ( 'NONE', ( #47670, #41935, #1130, #25118 ) ) ;
#22505=EDGE_CURVE ( 'NONE', #50243, #1125, #24099, .T. ) ;
#22506=CARTESIAN_POINT ( 'NONE',  ( 0.1968503937007873017, 0.000000000000000000, -0.6299212598425177889 ) ) ;
#22508=LINE ( 'NONE', #7013, #21198 ) ;
#22509=DIRECTION ( 'NONE',  ( -1.000000000000000000, 0.000000000000000000, 0.000000000000000000 ) ) ;
#22510=ORIENTED_EDGE ( 'NONE', *, *, #2884, .T. ) ;
#22511=ORIENTED_EDGE ( 'NONE', *, *, #39726, .T. ) ;
#22516=DIRECTION ( 'NONE',  ( 0.000000000000000000, -1.000000000000000000, 0.000000000000000000 ) ) ;
#22521=FACE_OUTER_BOUND ( 'NONE', #25562, .T. ) ;
#22522=VECTOR ( 'NONE', #11779, 39.37007874015748143 ) ;
#22523=VERTEX_POINT ( 'NONE', #36242 ) ;
#22526=CARTESIAN_POINT ( 'NONE',  ( 0.2727639067037604947, 0.000000000000000000, -1.417322834645664331 ) ) ;
#22528=ORIENTED_EDGE ( 'NONE', *, *, #18615, .T. ) ;
#22529=CARTESIAN_POINT ( 'NONE',  ( 1.560669927219590747, 3.346456692913386100, 1.414498409778230492 ) ) ;
#22534=EDGE_CURVE ( 'NONE', #39686, #17583, #12738, .T. ) ;
#22535=PLANE ( 'NONE',  #322 ) ;
#22538=VERTEX_POINT ( 'NONE', #20218 ) ;
#22539=FACE_OUTER_BOUND ( 'NONE', #47447, .T. ) ;
#22541=DIRECTION ( 'NONE',  ( -1.000000000000000000, 0.000000000000000000, 1.734723475976806848E-16 ) ) ;
#22542=LINE ( 'NONE', #42411, #33491 ) ;
#22543=EDGE_CURVE ( 'NONE', #38185, #43953, #35983, .T. ) ;
#22544=VECTOR ( 'NONE', #33376, 39.37007874015748143 ) ;
#22545=ORIENTED_EDGE ( 'NONE', *, *, #34380, .F. ) ;
#22546=VERTEX_POINT ( 'NONE', #40111 ) ;
#22548=CARTESIAN_POINT ( 'NONE',  ( 1.287906020515829919, 3.267716535433071279, -1.456692913385822630 ) ) ;
#22549=ORIENTED_EDGE ( 'NONE', *, *, #1274, .T. ) ;
#22550=VECTOR ( 'NONE', #37858, 39.37007874015748143 ) ;
#22552=DIRECTION ( 'NONE',  ( -1.000000000000000000, -0.000000000000000000, -0.000000000000000000 ) ) ;
#22553=CARTESIAN_POINT ( 'NONE',  ( 0.000000000000000000, 3.267716535433071279, -1.417322834645664331 ) ) ;
#22554=VECTOR ( 'NONE', #50763, 39.37007874015748143 ) ;
#22557=ORIENTED_EDGE ( 'NONE', *, *, #20471, .F. ) ;
#22559=CARTESIAN_POINT ( 'NONE',  ( -0.5455278134075208785, 3.346456692913386100, 1.692913385826762873 ) ) ;
#22561=CARTESIAN_POINT ( 'NONE',  ( 3.927031490892378253E-16, 3.346456692913386100, 1.062992125984246083 ) ) ;
#22562=ORIENTED_EDGE ( 'NONE', *, *, #46128, .T. ) ;
#22566=EDGE_LOOP ( 'NONE', ( #47927, #32798, #50048, #29141 ) ) ;
#22567=CARTESIAN_POINT ( 'NONE',  ( 1.560669927219590525, 3.267716535433071279, 1.220472440944875281 ) ) ;
#22568=VERTEX_POINT ( 'NONE', #37009 ) ;
#22569=ORIENTED_EDGE ( 'NONE', *, *, #46758, .F. ) ;
#22573=DIRECTION ( 'NONE',  ( -3.469446951953613696E-16, 0.000000000000000000, -1.000000000000000000 ) ) ;
#22575=LINE ( 'NONE', #30328, #32933 ) ;
#22579=CARTESIAN_POINT ( 'NONE',  ( 0.1968503937007878568, 3.267716535433071279, 0.9448818897637749625 ) ) ;
#22590=LINE ( 'NONE', #10968, #3410 ) ;
#22591=AXIS2_PLACEMENT_3D ( 'NONE', #10153, #50107, #42150 ) ;
#22592=EDGE_CURVE ( 'NONE', #16822, #24184, #25885, .T. ) ;
#22593=CIRCLE ( 'NONE', #323, 2.165354330708661568 ) ;
#22598=DIRECTION ( 'NONE',  ( 1.000000000000000000, -0.000000000000000000, 0.000000000000000000 ) ) ;
#22599=ADVANCED_FACE ( 'NONE', ( #25122 ), #44477, .F. ) ;
#22601=EDGE_CURVE ( 'NONE', #25893, #47284, #5242, .T. ) ;
#22603=VECTOR ( 'NONE', #36437, 39.37007874015748143 ) ;
#22604=EDGE_CURVE ( 'NONE', #42532, #49343, #40873, .T. ) ;
#22606=CARTESIAN_POINT ( 'NONE',  ( -0.8942052331142547050, 3.346456692913386100, 0.6299212598425164567 ) ) ;
#22607=ORIENTED_EDGE ( 'NONE', *, *, #36811, .T. ) ;
#22608=FACE_BOUND ( 'NONE', #15849, .T. ) ;
#22609=DIRECTION ( 'NONE',  ( 1.000000000000000000, -0.000000000000000000, 0.000000000000000000 ) ) ;
#22611=VERTEX_POINT ( 'NONE', #49078 ) ;
#22612=VERTEX_POINT ( 'NONE', #9635 ) ;
#22613=CARTESIAN_POINT ( 'NONE',  ( -0.5455278134075214336, 0.000000000000000000, -0.3149606299212593941 ) ) ;
#22614=CARTESIAN_POINT ( 'NONE',  ( 0.000000000000000000, 3.267716535433071279, 1.062992125984246083 ) ) ;
#22616=CARTESIAN_POINT ( 'NONE',  ( 0.000000000000000000, 3.267716535433071279, 0.000000000000000000 ) ) ;
#22617=DIRECTION ( 'NONE',  ( 1.000000000000000000, 0.000000000000000000, -3.469446951953613696E-16 ) ) ;
#22618=EDGE_LOOP ( 'NONE', ( #48921, #50284, #6219, #24942 ) ) ;
#22619=VERTEX_POINT ( 'NONE', #2393 ) ;
#22620=CARTESIAN_POINT ( 'NONE',  ( -0.3486774197067340486, 3.346456692913386100, -0.5118110236220467790 ) ) ;
#22621=EDGE_CURVE ( 'NONE', #27965, #43528, #32629, .T. ) ;
#22623=CARTESIAN_POINT ( 'NONE',  ( -1.985260859929297794, 3.267716535433071279, 6.887757239314512246E-16 ) ) ;
#22624=CIRCLE ( 'NONE', #29210, 2.443628662382284489 ) ;
#22625=ORIENTED_EDGE ( 'NONE', *, *, #25261, .F. ) ;
#22626=CARTESIAN_POINT ( 'NONE',  ( 1.091055626815042645, 3.346456692913386100, -0.6299212598425181220 ) ) ;
#22628=ORIENTED_EDGE ( 'NONE', *, *, #24644, .F. ) ;
#22631=EDGE_CURVE ( 'NONE', #15706, #2298, #40621, .T. ) ;
#22632=CIRCLE ( 'NONE', #16019, 2.106299212598425008 ) ;
#22634=EDGE_CURVE ( 'NONE', #370, #16904, #13762, .T. ) ;
#22638=DIRECTION ( 'NONE',  ( 1.000000000000000000, 0.000000000000000000, 0.000000000000000000 ) ) ;
#22639=VECTOR ( 'NONE', #35734, 39.37007874015748143 ) ;
#22640=DIRECTION ( 'NONE',  ( -0.000000000000000000, 1.000000000000000000, -0.000000000000000000 ) ) ;
#22641=CARTESIAN_POINT ( 'NONE',  ( 0.4696143004045483793, 3.267716535433071279, -1.629301903132388985E-16 ) ) ;
#22646=DIRECTION ( 'NONE',  ( -0.000000000000000000, 1.000000000000000000, -0.000000000000000000 ) ) ;
#22647=CARTESIAN_POINT ( 'NONE',  ( 0.000000000000000000, 3.346456692913386100, 0.000000000000000000 ) ) ;
#22648=DIRECTION ( 'NONE',  ( -1.000000000000000000, 0.000000000000000000, -0.000000000000000000 ) ) ;
#22649=DIRECTION ( 'NONE',  ( -0.000000000000000000, 0.000000000000000000, 1.000000000000000000 ) ) ;
#22650=EDGE_CURVE ( 'NONE', #1302, #42304, #22624, .T. ) ;
#22651=VERTEX_POINT ( 'NONE', #5503 ) ;
#22652=DIRECTION ( 'NONE',  ( 1.000000000000000000, -0.000000000000000000, 0.000000000000000000 ) ) ;
#22654=ORIENTED_EDGE ( 'NONE', *, *, #8592, .T. ) ;
#22655=DIRECTION ( 'NONE',  ( -0.000000000000000000, 1.000000000000000000, -0.000000000000000000 ) ) ;
#22656=EDGE_CURVE ( 'NONE', #37684, #26933, #48575, .T. ) ;
#22658=EDGE_CURVE ( 'NONE', #11104, #33373, #41131, .T. ) ;
#22659=VERTEX_POINT ( 'NONE', #1628 ) ;
#22660=VECTOR ( 'NONE', #32306, 39.37007874015748143 ) ;
#22663=CARTESIAN_POINT ( 'NONE',  ( 2.378961647330872786, 0.000000000000000000, 0.1181102362204698858 ) ) ;
#22666=VECTOR ( 'NONE', #14356, 39.37007874015748143 ) ;
#22667=CARTESIAN_POINT ( 'NONE',  ( -0.8182917201112819283, 3.346456692913386100, -0.3543307086614175816 ) ) ;
#22668=DIRECTION ( 'NONE',  ( 1.000000000000000000, 0.000000000000000000, 0.000000000000000000 ) ) ;
#22669=DIRECTION ( 'NONE',  ( -3.469446951953613696E-16, 0.000000000000000000, -1.000000000000000000 ) ) ;
#22670=CARTESIAN_POINT ( 'NONE',  ( 0.000000000000000000, 3.267716535433071279, 0.2755905511810996522 ) ) ;
#22671=ORIENTED_EDGE ( 'NONE', *, *, #27134, .T. ) ;
#22672=DIRECTION ( 'NONE',  ( 1.000000000000000000, 0.000000000000000000, -3.469446951953613696E-16 ) ) ;
#22675=ORIENTED_EDGE ( 'NONE', *, *, #37032, .T. ) ;
#22677=VERTEX_POINT ( 'NONE', #2136 ) ;
#22679=PLANE ( 'NONE',  #40060 ) ;
#22680=EDGE_LOOP ( 'NONE', ( #43288, #46995, #27109, #3312 ) ) ;
#22683=CARTESIAN_POINT ( 'NONE',  ( -1.712496953225537188, 0.000000000000000000, 0.5905511811023582691 ) ) ;
#22687=CARTESIAN_POINT ( 'NONE',  ( -1.636583440222564301, 3.267716535433071279, -0.6299212598425177889 ) ) ;
#22688=FACE_BOUND ( 'NONE', #1722, .T. ) ;
#22689=ORIENTED_EDGE ( 'NONE', *, *, #15047, .F. ) ;
#22690=CARTESIAN_POINT ( 'NONE',  ( -1.636583440222564301, 3.346456692913386100, -1.259842519685034468 ) ) ;
#22691=EDGE_CURVE ( 'NONE', #48087, #44092, #29757, .T. ) ;
#22692=VERTEX_POINT ( 'NONE', #38773 ) ;
#22693=VERTEX_POINT ( 'NONE', #34151 ) ;
#22694=LINE ( 'NONE', #20853, #41456 ) ;
#22696=VECTOR ( 'NONE', #10773, 39.37007874015748143 ) ;
#22698=AXIS2_PLACEMENT_3D ( 'NONE', #39502, #8000, #40275 ) ;
#22703=VERTEX_POINT ( 'NONE', #18898 ) ;
#22704=LINE ( 'NONE', #50512, #38403 ) ;
#22706=CARTESIAN_POINT ( 'NONE',  ( 1.363819533518803695, 3.267716535433071279, 1.535433070866133898 ) ) ;
#22708=EDGE_LOOP ( 'NONE', ( #44970, #3368, #42148, #43346 ) ) ;
#22709=VECTOR ( 'NONE', #23111, 39.37007874015748143 ) ;
#22710=LINE ( 'NONE', #46919, #4633 ) ;
#22711=DIRECTION ( 'NONE',  ( -3.469446951953613696E-16, 0.000000000000000000, -1.000000000000000000 ) ) ;
#22712=LINE ( 'NONE', #17824, #15911 ) ;
#22713=EDGE_CURVE ( 'NONE', #11113, #11168, #14775, .T. ) ;
#22714=PLANE ( 'NONE',  #11966 ) ;
#22715=DIRECTION ( 'NONE',  ( -0.000000000000000000, 1.000000000000000000, -0.000000000000000000 ) ) ;
#22716=EDGE_CURVE ( 'NONE', #10279, #40291, #34899, .T. ) ;
#22717=DIRECTION ( 'NONE',  ( 0.000000000000000000, 0.000000000000000000, 1.000000000000000000 ) ) ;
#22719=EDGE_CURVE ( 'NONE', #388, #43639, #10893, .T. ) ;
#22721=CARTESIAN_POINT ( 'NONE',  ( -1.363819533518803029, 0.000000000000000000, 0.9055118110236167750 ) ) ;
#22722=DIRECTION ( 'NONE',  ( -3.469446951953613696E-16, 0.000000000000000000, -1.000000000000000000 ) ) ;
#22725=VERTEX_POINT ( 'NONE', #42381 ) ;
#22726=ORIENTED_EDGE ( 'NONE', *, *, #29518, .T. ) ;
#22729=VERTEX_POINT ( 'NONE', #49835 ) ;
#22734=DIRECTION ( 'NONE',  ( 1.000000000000000000, -0.000000000000000000, 0.000000000000000000 ) ) ;
#22735=VECTOR ( 'NONE', #40525, 39.37007874015748143 ) ;
#22737=CARTESIAN_POINT ( 'NONE',  ( 2.182111253630085290, 0.000000000000000000, -0.1968503937007886062 ) ) ;
#22738=DIRECTION ( 'NONE',  ( -1.000000000000000000, 0.000000000000000000, 1.734723475976806848E-16 ) ) ;
#22739=ORIENTED_EDGE ( 'NONE', *, *, #43445, .T. ) ;
#22740=VECTOR ( 'NONE', #2806, 39.37007874015748143 ) ;
#22742=FACE_OUTER_BOUND ( 'NONE', #12, .T. ) ;
#22743=ORIENTED_EDGE ( 'NONE', *, *, #16710, .F. ) ;
#22744=EDGE_LOOP ( 'NONE', ( #24387, #4913, #43335, #14112 ) ) ;
#22748=DIRECTION ( 'NONE',  ( -0.000000000000000000, 0.000000000000000000, 1.000000000000000000 ) ) ;
#22751=LINE ( 'NONE', #27117, #27471 ) ;
#22752=CARTESIAN_POINT ( 'NONE',  ( 0.000000000000000000, 3.267716535433071279, 1.377952755905504256 ) ) ;
#22757=EDGE_CURVE ( 'NONE', #42801, #19974, #10276, .T. ) ;
#22759=ORIENTED_EDGE ( 'NONE', *, *, #35593, .T. ) ;
#22760=EDGE_CURVE ( 'NONE', #27748, #9948, #27139, .T. ) ;
#22762=CARTESIAN_POINT ( 'NONE',  ( -2.182111253630085290, 0.000000000000000000, 0.1181102362204704270 ) ) ;
#22765=DIRECTION ( 'NONE',  ( -3.469446951953613696E-16, 0.000000000000000000, -1.000000000000000000 ) ) ;
#22767=ORIENTED_EDGE ( 'NONE', *, *, #43321, .T. ) ;
#22769=CARTESIAN_POINT ( 'NONE',  ( -0.8182917201112819283, 3.346456692913386100, -0.4724409448818886470 ) ) ;
#22770=VECTOR ( 'NONE', #40744, 39.37007874015748143 ) ;
#22772=VERTEX_POINT ( 'NONE', #31024 ) ;
#22773=DIRECTION ( 'NONE',  ( 0.000000000000000000, 0.000000000000000000, 1.000000000000000000 ) ) ;
#22775=VECTOR ( 'NONE', #43166, 39.37007874015748143 ) ;
#22777=VECTOR ( 'NONE', #35199, 39.37007874015748143 ) ;
#22778=LINE ( 'NONE', #34652, #36568 ) ;
#22779=FACE_OUTER_BOUND ( 'NONE', #12421, .T. ) ;
#22780=FACE_OUTER_BOUND ( 'NONE', #19928, .T. ) ;
#22782=ORIENTED_EDGE ( 'NONE', *, *, #23742, .F. ) ;
#22783=PLANE ( 'NONE',  #34107 ) ;
#22785=LINE ( 'NONE', #49594, #26515 ) ;
#22786=EDGE_LOOP ( 'NONE', ( #8870, #32577, #49493, #30885 ) ) ;
#22789=DIRECTION ( 'NONE',  ( 0.000000000000000000, 0.000000000000000000, 1.000000000000000000 ) ) ;
#22790=ORIENTED_EDGE ( 'NONE', *, *, #11853, .F. ) ;
#22792=VERTEX_POINT ( 'NONE', #14261 ) ;
#22794=ORIENTED_EDGE ( 'NONE', *, *, #20598, .T. ) ;
#22795=DIRECTION ( 'NONE',  ( -3.469446951953613696E-16, 0.000000000000000000, -1.000000000000000000 ) ) ;
#22796=ADVANCED_FACE ( 'NONE', ( #50090 ), #15024, .F. ) ;
#22799=DIRECTION ( 'NONE',  ( -3.469446951953613696E-16, 0.000000000000000000, -1.000000000000000000 ) ) ;
#22802=ORIENTED_EDGE ( 'NONE', *, *, #17440, .F. ) ;
#22804=ORIENTED_EDGE ( 'NONE', *, *, #9634, .F. ) ;
#22805=DIRECTION ( 'NONE',  ( 1.000000000000000000, 0.000000000000000000, -3.469446951953613696E-16 ) ) ;
#22806=VECTOR ( 'NONE', #34266, 39.37007874015748143 ) ;
#22809=ORIENTED_EDGE ( 'NONE', *, *, #15333, .T. ) ;
#22810=CARTESIAN_POINT ( 'NONE',  ( 0.5455278134075208785, 0.000000000000000000, -1.889763779527552812 ) ) ;
#22811=LINE ( 'NONE', #31064, #49122 ) ;
#22812=CARTESIAN_POINT ( 'NONE',  ( 2.378961647330872786, 3.267716535433071279, 0.3149606299212573401 ) ) ;
#22815=CARTESIAN_POINT ( 'NONE',  ( 0.1968503937007875237, 3.267716535433071279, -6.829619984160660511E-17 ) ) ;
#22816=CARTESIAN_POINT ( 'NONE',  ( 1.015142113812069979, 3.267716535433071279, 1.220472440944875281 ) ) ;
#22821=PLANE ( 'NONE',  #29339 ) ;
#22822=VECTOR ( 'NONE', #11944, 39.37007874015748143 ) ;
#22823=ORIENTED_EDGE ( 'NONE', *, *, #33072, .F. ) ;
#22824=EDGE_CURVE ( 'NONE', #20090, #12774, #6772, .T. ) ;
#22825=CARTESIAN_POINT ( 'NONE',  ( 1.909347346926324684, 3.346456692913386100, -0.6692913385826764205 ) ) ;
#22826=ORIENTED_EDGE ( 'NONE', *, *, #25620, .T. ) ;
#22827=ORIENTED_EDGE ( 'NONE', *, *, #41773, .F. ) ;
#22828=PLANE ( 'NONE',  #8948 ) ;
#22830=ADVANCED_FACE ( 'NONE', ( #11401 ), #7526, .F. ) ;
#22831=FACE_OUTER_BOUND ( 'NONE', #34014, .T. ) ;
#22832=EDGE_CURVE ( 'NONE', #14060, #9230, #2644, .T. ) ;
#22834=EDGE_CURVE ( 'NONE', #14569, #17840, #18652, .T. ) ;
#22835=FACE_OUTER_BOUND ( 'NONE', #24908, .T. ) ;
#22836=ORIENTED_EDGE ( 'NONE', *, *, #49301, .F. ) ;
#22837=ORIENTED_EDGE ( 'NONE', *, *, #23986, .T. ) ;
#22842=CARTESIAN_POINT ( 'NONE',  ( -0.7053729475263631477, 3.346456692913386100, 2.047244094488179567 ) ) ;
#22844=ORIENTED_EDGE ( 'NONE', *, *, #33276, .T. ) ;
#22846=ADVANCED_FACE ( 'NONE', ( #12671 ), #39270, .F. ) ;
#22847=CARTESIAN_POINT ( 'NONE',  ( 1.015142113812069313, 0.000000000000000000, -0.7874015748031473194 ) ) ;
#22848=ORIENTED_EDGE ( 'NONE', *, *, #457, .T. ) ;
#22849=CARTESIAN_POINT ( 'NONE',  ( 0.000000000000000000, 3.267716535433071279, 2.204724409448808764 ) ) ;
#22850=DIRECTION ( 'NONE',  ( 1.000000000000000000, 0.000000000000000000, -3.469446951953613696E-16 ) ) ;
#22852=VECTOR ( 'NONE', #20472, 39.37007874015748143 ) ;
#22853=EDGE_CURVE ( 'NONE', #12600, #29231, #16554, .T. ) ;
#22854=FACE_OUTER_BOUND ( 'NONE', #1718, .T. ) ;
#22855=LINE ( 'NONE', #39356, #36565 ) ;
#22857=ORIENTED_EDGE ( 'NONE', *, *, #30811, .F. ) ;
#22858=LINE ( 'NONE', #18978, #30450 ) ;
#22860=FACE_BOUND ( 'NONE', #37484, .T. ) ;
#22861=EDGE_CURVE ( 'NONE', #31043, #9429, #36173, .T. ) ;
#22865=VERTEX_POINT ( 'NONE', #24033 ) ;
#22867=LINE ( 'NONE', #18235, #23781 ) ;
#22868=EDGE_CURVE ( 'NONE', #11359, #10643, #2062, .T. ) ;
#22869=CARTESIAN_POINT ( 'NONE',  ( 0.000000000000000000, 3.267716535433071279, 0.4330708661417290162 ) ) ;
#22870=CARTESIAN_POINT ( 'NONE',  ( 1.636583440222563857, 0.000000000000000000, -0.1968503937007886062 ) ) ;
#22871=CARTESIAN_POINT ( 'NONE',  ( 0.000000000000000000, 3.346456692913386100, 0.000000000000000000 ) ) ;
#22873=CARTESIAN_POINT ( 'NONE',  ( -0.8942052331142552601, 3.267716535433071279, -1.141732283464563569 ) ) ;
#22874=ORIENTED_EDGE ( 'NONE', *, *, #3519, .F. ) ;
#22875=CARTESIAN_POINT ( 'NONE',  ( -1.166969139818016199, 3.267716535433071279, -0.3543307086614174151 ) ) ;
#22879=PLANE ( 'NONE',  #28128 ) ;
#22880=VECTOR ( 'NONE', #30084, 39.37007874015748143 ) ;
#22882=PLANE ( 'NONE',  #15835 ) ;
#22883=VERTEX_POINT ( 'NONE', #279 ) ;
#22885=ADVANCED_FACE ( 'NONE', ( #28408 ), #8030, .F. ) ;
#22887=ORIENTED_EDGE ( 'NONE', *, *, #16524, .F. ) ;
#22889=LINE ( 'NONE', #46351, #49115 ) ;
#22890=EDGE_CURVE ( 'NONE', #47335, #48366, #50830, .T. ) ;
#22892=DIRECTION ( 'NONE',  ( -0.000000000000000000, 1.000000000000000000, -0.000000000000000000 ) ) ;
#22893=CARTESIAN_POINT ( 'NONE',  ( 1.636583440222563635, 3.346456692913386100, -1.259842519685035800 ) ) ;
#22894=LINE ( 'NONE', #11527, #27213 ) ;
#22896=DIRECTION ( 'NONE',  ( 0.000000000000000000, 1.000000000000000000, 0.000000000000000000 ) ) ;
#22897=VERTEX_POINT ( 'NONE', #15772 ) ;
#22898=CARTESIAN_POINT ( 'NONE',  ( 0.2727639067037610499, 3.346456692913386100, 1.102362204724404160 ) ) ;
#22899=LINE ( 'NONE', #4482, #10215 ) ;
#22900=PLANE ( 'NONE',  #429 ) ;
#22901=CARTESIAN_POINT ( 'NONE',  ( -1.363819533518803473, 0.000000000000000000, -0.1574803149606300023 ) ) ;
#22903=DIRECTION ( 'NONE',  ( 1.000000000000000000, 0.000000000000000000, 0.000000000000000000 ) ) ;
#22904=DIRECTION ( 'NONE',  ( -0.000000000000000000, 1.000000000000000000, -0.000000000000000000 ) ) ;
#22905=ORIENTED_EDGE ( 'NONE', *, *, #18295, .T. ) ;
#22907=AXIS2_PLACEMENT_3D ( 'NONE', #21021, #36772, #45004 ) ;
#22908=AXIS2_PLACEMENT_3D ( 'NONE', #32781, #48462, #9782 ) ;
#22909=EDGE_CURVE ( 'NONE', #2752, #34446, #15528, .T. ) ;
#22910=CARTESIAN_POINT ( 'NONE',  ( -1.091055626815042645, 3.267716535433071279, -1.141732283464563569 ) ) ;
#22912=VERTEX_POINT ( 'NONE', #39781 ) ;
#22913=LINE ( 'NONE', #14665, #49478 ) ;
#22914=EDGE_CURVE ( 'NONE', #39080, #20810, #27638, .T. ) ;
#22915=DIRECTION ( 'NONE',  ( -0.000000000000000000, 1.000000000000000000, -0.000000000000000000 ) ) ;
#22916=CARTESIAN_POINT ( 'NONE',  ( -2.182111253630085290, 3.346456692913386100, 0.6299212598425164567 ) ) ;
#22917=ADVANCED_FACE ( 'NONE', ( #4415 ), #43641, .F. ) ;
#22919=DIRECTION ( 'NONE',  ( -0.000000000000000000, 1.000000000000000000, -0.000000000000000000 ) ) ;
#22921=EDGE_CURVE ( 'NONE', #3036, #36717, #23779, .T. ) ;
#22922=AXIS2_PLACEMENT_3D ( 'NONE', #725, #15702, #47413 ) ;
#22925=ORIENTED_EDGE ( 'NONE', *, *, #42528, .F. ) ;
#22926=CARTESIAN_POINT ( 'NONE',  ( -0.07591351300297333182, 3.267716535433071279, 0.1574803149606283648 ) ) ;
#22927=VERTEX_POINT ( 'NONE', #8287 ) ;
#22928=EDGE_CURVE ( 'NONE', #50789, #43058, #19888, .T. ) ;
#22929=CARTESIAN_POINT ( 'NONE',  ( 0.000000000000000000, 3.346456692913386100, 0.000000000000000000 ) ) ;
#22931=LINE ( 'NONE', #26796, #38414 ) ;
#22932=ORIENTED_EDGE ( 'NONE', *, *, #11004, .T. ) ;
#22933=EDGE_CURVE ( 'NONE', #14052, #2108, #35406, .T. ) ;
#22936=CARTESIAN_POINT ( 'NONE',  ( 0.2727639067037610499, 3.346456692913386100, 2.362204724409437961 ) ) ;
#22937=ORIENTED_EDGE ( 'NONE', *, *, #36369, .T. ) ;
#22940=FACE_BOUND ( 'NONE', #43565, .T. ) ;
#22941=ORIENTED_EDGE ( 'NONE', *, *, #20544, .T. ) ;
#22942=EDGE_CURVE ( 'NONE', #5467, #9285, #40040, .T. ) ;
#22944=VECTOR ( 'NONE', #10041, 39.37007874015748143 ) ;
#22946=ORIENTED_EDGE ( 'NONE', *, *, #31777, .T. ) ;
#22948=FACE_OUTER_BOUND ( 'NONE', #43542, .T. ) ;
#22951=VERTEX_POINT ( 'NONE', #29702 ) ;
#22952=AXIS2_PLACEMENT_3D ( 'NONE', #18192, #49637, #49390 ) ;
#22953=LINE ( 'NONE', #14951, #20444 ) ;
#22954=ORIENTED_EDGE ( 'NONE', *, *, #7689, .T. ) ;
#22955=PLANE ( 'NONE',  #33481 ) ;
#22956=FACE_OUTER_BOUND ( 'NONE', #47724, .T. ) ;
#22960=ORIENTED_EDGE ( 'NONE', *, *, #26497, .T. ) ;
#22961=EDGE_LOOP ( 'NONE', ( #4135, #40199, #16237, #8517 ) ) ;
#22963=LINE ( 'NONE', #43582, #39362 ) ;
#22964=DIRECTION ( 'NONE',  ( -0.000000000000000000, 1.000000000000000000, -0.000000000000000000 ) ) ;
#22966=CARTESIAN_POINT ( 'NONE',  ( 2.106197740627112402, 3.267716535433071279, 1.102362204724403938 ) ) ;
#22967=VECTOR ( 'NONE', #29886, 39.37007874015748143 ) ;
#22968=CARTESIAN_POINT ( 'NONE',  ( 0.1968503937007873017, 3.346456692913386100, -0.9448818897637765168 ) ) ;
#22969=DIRECTION ( 'NONE',  ( 0.000000000000000000, 1.000000000000000000, 0.000000000000000000 ) ) ;
#22971=LINE ( 'NONE', #7233, #19266 ) ;
#22974=ORIENTED_EDGE ( 'NONE', *, *, #19384, .T. ) ;
#22978=EDGE_CURVE ( 'NONE', #10179, #10605, #5702, .T. ) ;
#22979=VECTOR ( 'NONE', #24963, 39.37007874015748143 ) ;
#22980=ORIENTED_EDGE ( 'NONE', *, *, #48148, .T. ) ;
#22981=EDGE_CURVE ( 'NONE', #6479, #48094, #45419, .T. ) ;
#22982=EDGE_CURVE ( 'NONE', #28186, #25938, #17825, .T. ) ;
#22985=DIRECTION ( 'NONE',  ( -0.000000000000000000, 1.000000000000000000, -0.000000000000000000 ) ) ;
#22991=AXIS2_PLACEMENT_3D ( 'NONE', #17570, #44154, #5177 ) ;
#22992=ORIENTED_EDGE ( 'NONE', *, *, #11063, .T. ) ;
#22994=ORIENTED_EDGE ( 'NONE', *, *, #33311, .F. ) ;
#22996=DIRECTION ( 'NONE',  ( -0.000000000000000000, 1.000000000000000000, -0.000000000000000000 ) ) ;
#22999=EDGE_CURVE ( 'NONE', #32548, #8583, #9571, .T. ) ;
#23001=ORIENTED_EDGE ( 'NONE', *, *, #36053, .T. ) ;
#23002=EDGE_CURVE ( 'NONE', #42568, #21081, #28670, .T. ) ;
#23003=CARTESIAN_POINT ( 'NONE',  ( -2.182111253630085290, 0.000000000000000000, 0.1181102362204704270 ) ) ;
#23006=EDGE_CURVE ( 'NONE', #4010, #26232, #396, .T. ) ;
#23007=LINE ( 'NONE', #38756, #28164 ) ;
#23008=ADVANCED_FACE ( 'NONE', ( #25312 ), #17322, .F. ) ;
#23009=EDGE_LOOP ( 'NONE', ( #29025, #38320, #24012, #29868 ) ) ;
#23010=ORIENTED_EDGE ( 'NONE', *, *, #15135, .F. ) ;
#23012=VERTEX_POINT ( 'NONE', #20669 ) ;
#23013=DIRECTION ( 'NONE',  ( -0.000000000000000000, 1.000000000000000000, -0.000000000000000000 ) ) ;
#23014=CARTESIAN_POINT ( 'NONE',  ( 0.8182917201112819283, 0.000000000000000000, -0.3543307086614175816 ) ) ;
#23016=CARTESIAN_POINT ( 'NONE',  ( 0.5786196242795136335, 3.346456692913386100, -2.086614173228340086 ) ) ;
#23017=PLANE ( 'NONE',  #2437 ) ;
#23018=EDGE_LOOP ( 'NONE', ( #11624, #39138, #24298, #18801 ) ) ;
#23019=EDGE_LOOP ( 'NONE', ( #39650, #5460, #20138, #18837 ) ) ;
#23020=CARTESIAN_POINT ( 'NONE',  ( 1.363819533518803251, 3.346456692913386100, -0.6692913385826764205 ) ) ;
#23021=ORIENTED_EDGE ( 'NONE', *, *, #35117, .F. ) ;
#23022=DIRECTION ( 'NONE',  ( -1.000000000000000000, 0.000000000000000000, 0.000000000000000000 ) ) ;
#23025=AXIS2_PLACEMENT_3D ( 'NONE', #33483, #9205, #45560 ) ;
#23026=CARTESIAN_POINT ( 'NONE',  ( -1.363819533518803473, 3.346456692913386100, -0.4724409448818886470 ) ) ;
#23027=DIRECTION ( 'NONE',  ( 1.000000000000000000, 0.000000000000000000, 0.000000000000000000 ) ) ;
#23029=ORIENTED_EDGE ( 'NONE', *, *, #29099, .T. ) ;
#23030=DIRECTION ( 'NONE',  ( -0.000000000000000000, 1.000000000000000000, -0.000000000000000000 ) ) ;
#23033=ORIENTED_EDGE ( 'NONE', *, *, #47137, .F. ) ;
#23036=DIRECTION ( 'NONE',  ( 0.000000000000000000, 1.000000000000000000, 0.000000000000000000 ) ) ;
#23037=VERTEX_POINT ( 'NONE', #29446 ) ;
#23039=PLANE ( 'NONE',  #43204 ) ;
#23040=ADVANCED_FACE ( 'NONE', ( #13703 ), #33593, .F. ) ;
#23041=EDGE_CURVE ( 'NONE', #47517, #37178, #1819, .T. ) ;
#23043=CARTESIAN_POINT ( 'NONE',  ( 0.2727639067037604392, 0.000000000000000000, -0.9842519685039348154 ) ) ;
#23044=ORIENTED_EDGE ( 'NONE', *, *, #4158, .T. ) ;
#23045=LINE ( 'NONE', #47250, #10568 ) ;
#23047=ORIENTED_EDGE ( 'NONE', *, *, #7495, .F. ) ;
#23050=DIRECTION ( 'NONE',  ( 0.000000000000000000, -1.000000000000000000, 0.000000000000000000 ) ) ;
#23051=VECTOR ( 'NONE', #28520, 39.37007874015748143 ) ;
#23052=EDGE_LOOP ( 'NONE', ( #44363, #29724, #6638, #45286 ) ) ;
#23053=ORIENTED_EDGE ( 'NONE', *, *, #35855, .T. ) ;
#23054=ORIENTED_EDGE ( 'NONE', *, *, #38188, .T. ) ;
#23055=CARTESIAN_POINT ( 'NONE',  ( 1.139183960333101098, 3.346456692913386100, -1.771653543307081691 ) ) ;
#23056=DIRECTION ( 'NONE',  ( -1.000000000000000000, 0.000000000000000000, -0.000000000000000000 ) ) ;
#23057=ORIENTED_EDGE ( 'NONE', *, *, #49068, .T. ) ;
#23058=EDGE_LOOP ( 'NONE', ( #27289, #41974, #36293, #12854 ) ) ;
#23060=CARTESIAN_POINT ( 'NONE',  ( -0.8182917201112819283, 3.346456692913386100, -0.9842519685039342603 ) ) ;
#23062=AXIS2_PLACEMENT_3D ( 'NONE', #28663, #48504, #5173 ) ;
#23063=ORIENTED_EDGE ( 'NONE', *, *, #24368, .F. ) ;
#23065=ORIENTED_EDGE ( 'NONE', *, *, #4640, .T. ) ;
#23066=ADVANCED_FACE ( 'NONE', ( #49280 ), #28927, .F. ) ;
#23067=PLANE ( 'NONE',  #732 ) ;
#23068=CARTESIAN_POINT ( 'NONE',  ( 2.106197740627111514, 3.267716535433070391, -1.239052911296964155 ) ) ;
#23069=CARTESIAN_POINT ( 'NONE',  ( -2.182111253630085290, 3.346456692913386100, 0.6299212598425164567 ) ) ;
#23070=ORIENTED_EDGE ( 'NONE', *, *, #50857, .F. ) ;
#23072=DIRECTION ( 'NONE',  ( 1.000000000000000000, 0.000000000000000000, 0.000000000000000000 ) ) ;
#23073=ORIENTED_EDGE ( 'NONE', *, *, #11737, .F. ) ;
#23074=EDGE_CURVE ( 'NONE', #39080, #50597, #40815, .T. ) ;
#23076=ORIENTED_EDGE ( 'NONE', *, *, #50588, .T. ) ;
#23084=ORIENTED_EDGE ( 'NONE', *, *, #12964, .T. ) ;
#23086=DIRECTION ( 'NONE',  ( -3.469446951953613696E-16, 0.000000000000000000, -1.000000000000000000 ) ) ;
#23087=LINE ( 'NONE', #11219, #9439 ) ;
#23088=CARTESIAN_POINT ( 'NONE',  ( -0.8182917201112819283, 0.000000000000000000, 2.047244094488179567 ) ) ;
#23089=LINE ( 'NONE', #50903, #19590 ) ;
#23090=ORIENTED_EDGE ( 'NONE', *, *, #40231, .F. ) ;
#23091=DIRECTION ( 'NONE',  ( -3.469446951953613696E-16, 0.000000000000000000, -1.000000000000000000 ) ) ;
#23092=CARTESIAN_POINT ( 'NONE',  ( -2.182111253630085290, 0.000000000000000000, -6.146657985744592735E-16 ) ) ;
#23095=DIRECTION ( 'NONE',  ( 1.000000000000000000, 0.000000000000000000, 0.000000000000000000 ) ) ;
#23096=VECTOR ( 'NONE', #34702, 39.37007874015748143 ) ;
#23097=FACE_OUTER_BOUND ( 'NONE', #43706, .T. ) ;
#23098=CARTESIAN_POINT ( 'NONE',  ( -1.636583440222563635, 0.000000000000000000, 0.6299212598425164567 ) ) ;
#23099=DIRECTION ( 'NONE',  ( -3.469446951953613696E-16, 0.000000000000000000, -1.000000000000000000 ) ) ;
#23101=DIRECTION ( 'NONE',  ( 0.000000000000000000, 0.000000000000000000, -1.000000000000000000 ) ) ;
#23102=EDGE_CURVE ( 'NONE', #46376, #34365, #32566, .T. ) ;
#23104=ORIENTED_EDGE ( 'NONE', *, *, #14425, .F. ) ;
#23105=LINE ( 'NONE', #10982, #9028 ) ;
#23107=ORIENTED_EDGE ( 'NONE', *, *, #9468, .F. ) ;
#23108=CARTESIAN_POINT ( 'NONE',  ( -2.182111253630085734, 0.000000000000000000, -0.6299212598425177889 ) ) ;
#23110=DIRECTION ( 'NONE',  ( -0.000000000000000000, 1.000000000000000000, -0.000000000000000000 ) ) ;
#23111=DIRECTION ( 'NONE',  ( -0.000000000000000000, 1.000000000000000000, -0.000000000000000000 ) ) ;
#23113=VERTEX_POINT ( 'NONE', #45669 ) ;
#23114=ORIENTED_EDGE ( 'NONE', *, *, #44134, .F. ) ;
#23115=DIRECTION ( 'NONE',  ( -1.000000000000000000, -0.000000000000000000, -0.000000000000000000 ) ) ;
#23118=DIRECTION ( 'NONE',  ( 0.000000000000000000, 0.000000000000000000, -1.000000000000000000 ) ) ;
#23119=CARTESIAN_POINT ( 'NONE',  ( -1.636583440222564301, 3.346456692913386100, -0.8267716535433052849 ) ) ;
#23122=EDGE_CURVE ( 'NONE', #45841, #23012, #31972, .T. ) ;
#23123=CARTESIAN_POINT ( 'NONE',  ( 0.5455278134075216556, 3.267716535433071279, 1.377952755905504256 ) ) ;
#23124=LINE ( 'NONE', #34256, #43901 ) ;
#23125=FACE_OUTER_BOUND ( 'NONE', #16157, .T. ) ;
#23126=ORIENTED_EDGE ( 'NONE', *, *, #1820, .F. ) ;
#23127=EDGE_CURVE ( 'NONE', #20592, #50824, #20166, .T. ) ;
#23129=ORIENTED_EDGE ( 'NONE', *, *, #48372, .F. ) ;
#23130=ORIENTED_EDGE ( 'NONE', *, *, #48040, .T. ) ;
#23131=AXIS2_PLACEMENT_3D ( 'NONE', #2537, #50474, #18282 ) ;
#23135=ORIENTED_EDGE ( 'NONE', *, *, #10755, .T. ) ;
#23136=CARTESIAN_POINT ( 'NONE',  ( 1.909347346926324684, 3.346456692913386100, -0.6692913385826764205 ) ) ;
#23137=VECTOR ( 'NONE', #22370, 39.37007874015748143 ) ;
#23140=DIRECTION ( 'NONE',  ( -3.469446951953613696E-16, 0.000000000000000000, -1.000000000000000000 ) ) ;
#23142=DIRECTION ( 'NONE',  ( -0.000000000000000000, 0.000000000000000000, 1.000000000000000000 ) ) ;
#23143=CARTESIAN_POINT ( 'NONE',  ( 0.000000000000000000, 3.267716535433071279, 0.6299212598425164567 ) ) ;
#23144=FACE_OUTER_BOUND ( 'NONE', #45386, .T. ) ;
#23147=CARTESIAN_POINT ( 'NONE',  ( 0.4696143004045478797, 3.267716535433071279, -1.629301903132387260E-16 ) ) ;
#23148=CARTESIAN_POINT ( 'NONE',  ( -0.6214413264104939882, 0.000000000000000000, 1.417322834645662777 ) ) ;
#23151=ORIENTED_EDGE ( 'NONE', *, *, #14977, .F. ) ;
#23152=PLANE ( 'NONE',  #14122 ) ;
#23153=CARTESIAN_POINT ( 'NONE',  ( 1.560669927219590525, 0.000000000000000000, -0.3543307086614178592 ) ) ;
#23155=DIRECTION ( 'NONE',  ( -1.000000000000000000, 0.000000000000000000, 1.734723475976806848E-16 ) ) ;
#23156=PLANE ( 'NONE',  #25101 ) ;
#23162=AXIS2_PLACEMENT_3D ( 'NONE', #6970, #46924, #46677 ) ;
#23163=VECTOR ( 'NONE', #21476, 39.37007874015748143 ) ;
#23165=CARTESIAN_POINT ( 'NONE',  ( 1.363819533518803251, 3.267716535433071279, 0.9055118110236164419 ) ) ;
#23167=VERTEX_POINT ( 'NONE', #2586 ) ;
#23169=EDGE_LOOP ( 'NONE', ( #34598, #37596, #19388, #19412 ) ) ;
#23171=CARTESIAN_POINT ( 'NONE',  ( 0.000000000000000000, 3.267716535433071279, -0.6692913385826764205 ) ) ;
#23172=ORIENTED_EDGE ( 'NONE', *, *, #19083, .T. ) ;
#23173=DIRECTION ( 'NONE',  ( -3.469446951953613696E-16, 0.000000000000000000, -1.000000000000000000 ) ) ;
#23174=VECTOR ( 'NONE', #16262, 39.37007874015748143 ) ;
#23178=VECTOR ( 'NONE', #15664, 39.37007874015748143 ) ;
#23179=ORIENTED_EDGE ( 'NONE', *, *, #41357, .T. ) ;
#23181=VERTEX_POINT ( 'NONE', #34089 ) ;
#23183=LINE ( 'NONE', #43560, #15791 ) ;
#23185=DIRECTION ( 'NONE',  ( -0.000000000000000000, 1.000000000000000000, -0.000000000000000000 ) ) ;
#23187=VERTEX_POINT ( 'NONE', #50522 ) ;
#23188=ORIENTED_EDGE ( 'NONE', *, *, #41443, .T. ) ;
#23189=CARTESIAN_POINT ( 'NONE',  ( -0.3486774197067340486, 3.267716535433071279, -1.141732283464563791 ) ) ;
#23191=EDGE_LOOP ( 'NONE', ( #13041, #18659, #9039, #1095 ) ) ;
#23192=DIRECTION ( 'NONE',  ( 0.000000000000000000, -1.000000000000000000, 0.000000000000000000 ) ) ;
#23193=EDGE_CURVE ( 'NONE', #21920, #32010, #14968, .T. ) ;
#23194=ORIENTED_EDGE ( 'NONE', *, *, #8905, .F. ) ;
#23195=CARTESIAN_POINT ( 'NONE',  ( 0.000000000000000000, 3.346456692913386100, 0.000000000000000000 ) ) ;
#23196=VECTOR ( 'NONE', #36885, 39.37007874015748143 ) ;
#23198=VECTOR ( 'NONE', #24408, 39.37007874015748143 ) ;
#23200=CARTESIAN_POINT ( 'NONE',  ( -1.166969139818015755, 3.346456692913386100, 0.9055118110236167750 ) ) ;
#23201=ORIENTED_EDGE ( 'NONE', *, *, #1881, .F. ) ;
#23202=ORIENTED_EDGE ( 'NONE', *, *, #12545, .T. ) ;
#23204=DIRECTION ( 'NONE',  ( 0.000000000000000000, 0.000000000000000000, -1.000000000000000000 ) ) ;
#23207=EDGE_CURVE ( 'NONE', #11574, #41494, #10837, .T. ) ;
#23209=FACE_OUTER_BOUND ( 'NONE', #25706, .T. ) ;
#23211=CARTESIAN_POINT ( 'NONE',  ( 0.8182917201112824834, 0.000000000000000000, 1.732283464566921172 ) ) ;
#23212=VECTOR ( 'NONE', #11982, 39.37007874015748143 ) ;
#23216=ORIENTED_EDGE ( 'NONE', *, *, #32381, .T. ) ;
#23218=VERTEX_POINT ( 'NONE', #46424 ) ;
#23219=ORIENTED_EDGE ( 'NONE', *, *, #37018, .T. ) ;
#23220=ADVANCED_FACE ( 'NONE', ( #34345 ), #22714, .F. ) ;
#23221=CARTESIAN_POINT ( 'NONE',  ( -1.985260859929297794, 3.346456692913386100, 0.1181102362204704270 ) ) ;
#23227=VERTEX_POINT ( 'NONE', #23975 ) ;
#23229=ORIENTED_EDGE ( 'NONE', *, *, #21643, .T. ) ;
#23230=VECTOR ( 'NONE', #5000, 39.37007874015748143 ) ;
#23235=VECTOR ( 'NONE', #11566, 39.37007874015748143 ) ;
#23236=CARTESIAN_POINT ( 'NONE',  ( -1.439733046521776139, 3.346456692913386100, -4.780733988912460139E-16 ) ) ;
#23237=ORIENTED_EDGE ( 'NONE', *, *, #37539, .T. ) ;
#23238=ORIENTED_EDGE ( 'NONE', *, *, #16107, .F. ) ;
#23239=DIRECTION ( 'NONE',  ( -0.000000000000000000, 1.000000000000000000, -0.000000000000000000 ) ) ;
#23240=DIRECTION ( 'NONE',  ( -1.000000000000000000, -0.000000000000000000, -0.000000000000000000 ) ) ;
#23241=CARTESIAN_POINT ( 'NONE',  ( 0.5455278134075212115, 3.346456692913386100, -0.9448818897637765168 ) ) ;
#23242=AXIS2_PLACEMENT_3D ( 'NONE', #49169, #9970, #22104 ) ;
#23243=EDGE_LOOP ( 'NONE', ( #26844, #20630, #44011, #29739 ) ) ;
#23244=DIRECTION ( 'NONE',  ( 1.734723475976806848E-16, -0.000000000000000000, 1.000000000000000000 ) ) ;
#23245=DIRECTION ( 'NONE',  ( -0.000000000000000000, 1.000000000000000000, -0.000000000000000000 ) ) ;
#23248=LINE ( 'NONE', #43369, #30692 ) ;
#23252=EDGE_CURVE ( 'NONE', #15892, #36336, #745, .T. ) ;
#23253=VERTEX_POINT ( 'NONE', #220 ) ;
#23255=LINE ( 'NONE', #31271, #35710 ) ;
#23256=ADVANCED_FACE ( 'NONE', ( #23209 ), #11344, .F. ) ;
#23258=DIRECTION ( 'NONE',  ( -3.469446951953613696E-16, 0.000000000000000000, -1.000000000000000000 ) ) ;
#23259=DIRECTION ( 'NONE',  ( -0.000000000000000000, 1.000000000000000000, -0.000000000000000000 ) ) ;
#23263=LINE ( 'NONE', #276, #19329 ) ;
#23264=ORIENTED_EDGE ( 'NONE', *, *, #5359, .F. ) ;
#23265=DIRECTION ( 'NONE',  ( 1.734723475976806848E-16, -0.000000000000000000, 1.000000000000000000 ) ) ;
#23266=DIRECTION ( 'NONE',  ( -1.000000000000000000, 0.000000000000000000, -0.000000000000000000 ) ) ;
#23267=VECTOR ( 'NONE', #27059, 39.37007874015748143 ) ;
#23270=CARTESIAN_POINT ( 'NONE',  ( -1.091055626815042645, 0.000000000000000000, -1.889763779527552146 ) ) ;
#23271=AXIS2_PLACEMENT_3D ( 'NONE', #37621, #9740, #45579 ) ;
#23272=CARTESIAN_POINT ( 'NONE',  ( 0.7423782071083092626, 0.000000000000000000, 1.259842519685033357 ) ) ;
#23273=ORIENTED_EDGE ( 'NONE', *, *, #46352, .F. ) ;
#23274=FACE_OUTER_BOUND ( 'NONE', #44713, .T. ) ;
#23275=CARTESIAN_POINT ( 'NONE',  ( 4.268512490100411402E-16, 3.346456692913386100, 1.889763779527550369 ) ) ;
#23276=VECTOR ( 'NONE', #36034, 39.37007874015748143 ) ;
#23277=EDGE_CURVE ( 'NONE', #32481, #32615, #12358, .T. ) ;
#23280=VECTOR ( 'NONE', #43724, 39.37007874015748143 ) ;
#23281=DIRECTION ( 'NONE',  ( -1.000000000000000000, 0.000000000000000000, -0.000000000000000000 ) ) ;
#23282=LINE ( 'NONE', #50841, #31951 ) ;
#23283=CARTESIAN_POINT ( 'NONE',  ( 0.7423782071083085965, 0.000000000000000000, -1.141732283464564013 ) ) ;
#23284=ORIENTED_EDGE ( 'NONE', *, *, #31867, .T. ) ;
#23286=EDGE_CURVE ( 'NONE', #45509, #11074, #27079, .T. ) ;
#23289=ORIENTED_EDGE ( 'NONE', *, *, #50334, .F. ) ;
#23295=ORIENTED_EDGE ( 'NONE', *, *, #28596, .T. ) ;
#23298=DIRECTION ( 'NONE',  ( -0.000000000000000000, 0.000000000000000000, 1.000000000000000000 ) ) ;
#23300=ORIENTED_EDGE ( 'NONE', *, *, #38034, .F. ) ;
#23301=ORIENTED_EDGE ( 'NONE', *, *, #16257, .T. ) ;
#23302=DIRECTION ( 'NONE',  ( -1.000000000000000000, 0.000000000000000000, 1.734723475976806848E-16 ) ) ;
#23303=CARTESIAN_POINT ( 'NONE',  ( -1.091055626815042645, 3.232777166330607521, 2.204724409448808764 ) ) ;
#23304=LINE ( 'NONE', #35695, #24479 ) ;
#23307=CARTESIAN_POINT ( 'NONE',  ( 0.5455278134075212115, 3.267716535433071279, -6.146657985744592735E-16 ) ) ;
#23310=ORIENTED_EDGE ( 'NONE', *, *, #14616, .F. ) ;
#23311=CARTESIAN_POINT ( 'NONE',  ( 1.909347346926324684, 0.000000000000000000, -0.1574803149606304187 ) ) ;
#23313=CARTESIAN_POINT ( 'NONE',  ( -1.091055626815042201, 3.267716535433071279, 1.892679809432643896E-16 ) ) ;
#23314=EDGE_LOOP ( 'NONE', ( #44399, #41057, #178, #6105 ) ) ;
#23318=LINE ( 'NONE', #15583, #7290 ) ;
#23320=VECTOR ( 'NONE', #18014, 39.37007874015748143 ) ;
#23321=VECTOR ( 'NONE', #28863, 39.37007874015748143 ) ;
#23322=CARTESIAN_POINT ( 'NONE',  ( 0.000000000000000000, 3.346456692913386100, 0.000000000000000000 ) ) ;
#23323=EDGE_CURVE ( 'NONE', #44282, #50136, #51027, .T. ) ;
#23324=DIRECTION ( 'NONE',  ( 0.000000000000000000, 0.000000000000000000, -1.000000000000000000 ) ) ;
#23325=CARTESIAN_POINT ( 'NONE',  ( 0.000000000000000000, 3.267716535433071279, -1.259842519685035800 ) ) ;
#23326=ORIENTED_EDGE ( 'NONE', *, *, #28160, .F. ) ;
#23327=ORIENTED_EDGE ( 'NONE', *, *, #36314, .T. ) ;
#23329=CIRCLE ( 'NONE', #14268, 2.106299212598425008 ) ;
#23330=ORIENTED_EDGE ( 'NONE', *, *, #37818, .T. ) ;
#23331=PLANE ( 'NONE',  #35185 ) ;
#23332=CARTESIAN_POINT ( 'NONE',  ( 0.000000000000000000, 3.267716535433071279, 0.5905511811023579360 ) ) ;
#23333=PLANE ( 'NONE',  #19541 ) ;
#23334=DIRECTION ( 'NONE',  ( -3.469446951953613696E-16, 0.000000000000000000, -1.000000000000000000 ) ) ;
#23337=EDGE_CURVE ( 'NONE', #30055, #9679, #3852, .T. ) ;
#23338=PLANE ( 'NONE',  #9209 ) ;
#23340=DIRECTION ( 'NONE',  ( 1.000000000000000000, 0.000000000000000000, 0.000000000000000000 ) ) ;
#23341=EDGE_CURVE ( 'NONE', #17272, #43136, #27841, .T. ) ;
#23342=LINE ( 'NONE', #39101, #26157 ) ;
#23343=CARTESIAN_POINT ( 'NONE',  ( 0.000000000000000000, 3.267716535433071279, 0.3149606299212580063 ) ) ;
#23344=DIRECTION ( 'NONE',  ( 1.734723475976806848E-16, -0.000000000000000000, 1.000000000000000000 ) ) ;
#23346=CARTESIAN_POINT ( 'NONE',  ( -1.439733046521777027, 0.000000000000000000, 1.377952755905504256 ) ) ;
#23347=AXIS2_PLACEMENT_3D ( 'NONE', #6507, #22499, #50313 ) ;
#23349=ORIENTED_EDGE ( 'NONE', *, *, #45912, .F. ) ;
#23350=VECTOR ( 'NONE', #50915, 39.37007874015748143 ) ;
#23351=CARTESIAN_POINT ( 'NONE',  ( -1.636583440222563635, 0.000000000000000000, -0.1968503937007879123 ) ) ;
#23352=ORIENTED_EDGE ( 'NONE', *, *, #38216, .F. ) ;
#23353=CARTESIAN_POINT ( 'NONE',  ( 1.636583440222563635, 0.000000000000000000, -1.141732283464564013 ) ) ;
#23354=VECTOR ( 'NONE', #37706, 39.37007874015748143 ) ;
#23355=VECTOR ( 'NONE', #41635, 39.37007874015748143 ) ;
#23356=DIRECTION ( 'NONE',  ( -3.469446951953613696E-16, 0.000000000000000000, -1.000000000000000000 ) ) ;
#23357=DIRECTION ( 'NONE',  ( 1.734723475976806848E-16, 0.000000000000000000, 1.000000000000000000 ) ) ;
#23358=EDGE_LOOP ( 'NONE', ( #48505, #2096, #5427, #23963 ) ) ;
#23359=ORIENTED_EDGE ( 'NONE', *, *, #48415, .F. ) ;
#23360=CARTESIAN_POINT ( 'NONE',  ( -0.8182917201112819283, 0.000000000000000000, -1.929133858267710000 ) ) ;
#23361=CIRCLE ( 'NONE', #24222, 2.106299212598425008 ) ;
#23363=ORIENTED_EDGE ( 'NONE', *, *, #34770, .F. ) ;
#23365=CARTESIAN_POINT ( 'NONE',  ( -0.5455278134075208785, 3.346456692913386100, 1.574803149606291974 ) ) ;
#23366=DIRECTION ( 'NONE',  ( 1.000000000000000000, 0.000000000000000000, 0.000000000000000000 ) ) ;
#23368=ORIENTED_EDGE ( 'NONE', *, *, #29099, .F. ) ;
#23369=CARTESIAN_POINT ( 'NONE',  ( 1.833433833923351353, 3.267716535433071279, 0.7480314960629872445 ) ) ;
#23370=CARTESIAN_POINT ( 'NONE',  ( 1.953585199828834940, 3.267716535433071279, -0.7874015748031473194 ) ) ;
#23374=VERTEX_POINT ( 'NONE', #20087 ) ;
#23375=ORIENTED_EDGE ( 'NONE', *, *, #16757, .T. ) ;
#23376=LINE ( 'NONE', #11765, #33329 ) ;
#23379=DIRECTION ( 'NONE',  ( 1.000000000000000000, -0.000000000000000000, 0.000000000000000000 ) ) ;
#23380=ORIENTED_EDGE ( 'NONE', *, *, #36148, .F. ) ;
#23383=EDGE_CURVE ( 'NONE', #49655, #13594, #16233, .T. ) ;
#23384=AXIS2_PLACEMENT_3D ( 'NONE', #11043, #10539, #33796 ) ;
#23386=FACE_OUTER_BOUND ( 'NONE', #6138, .T. ) ;
#23387=EDGE_CURVE ( 'NONE', #8195, #7477, #44099, .T. ) ;
#23388=FACE_OUTER_BOUND ( 'NONE', #20963, .T. ) ;
#23389=AXIS2_PLACEMENT_3D ( 'NONE', #24904, #48354, #36022 ) ;
#23390=VECTOR ( 'NONE', #24813, 39.37007874015748143 ) ;
#23393=CARTESIAN_POINT ( 'NONE',  ( -1.909347346926324462, 3.346456692913386100, -0.1574803149606297248 ) ) ;
#23394=CARTESIAN_POINT ( 'NONE',  ( 0.000000000000000000, 3.267716535433071279, 0.000000000000000000 ) ) ;
#23395=VECTOR ( 'NONE', #23030, 39.37007874015748143 ) ;
#23396=ORIENTED_EDGE ( 'NONE', *, *, #20167, .F. ) ;
#23397=PLANE ( 'NONE',  #38986 ) ;
#23400=EDGE_LOOP ( 'NONE', ( #26652, #19620, #9258, #45505 ) ) ;
#23401=PLANE ( 'NONE',  #33118 ) ;
#23402=EDGE_CURVE ( 'NONE', #9101, #3769, #28350, .T. ) ;
#23405=DIRECTION ( 'NONE',  ( -0.000000000000000000, 1.000000000000000000, -0.000000000000000000 ) ) ;
#23408=DIRECTION ( 'NONE',  ( 1.000000000000000000, 0.000000000000000000, 0.000000000000000000 ) ) ;
#23409=VERTEX_POINT ( 'NONE', #5123 ) ;
#23410=DIRECTION ( 'NONE',  ( 1.000000000000000000, 0.000000000000000000, 0.000000000000000000 ) ) ;
#23411=DIRECTION ( 'NONE',  ( 1.734723475976806848E-16, -0.000000000000000000, 1.000000000000000000 ) ) ;
#23414=VERTEX_POINT ( 'NONE', #17008 ) ;
#23418=VECTOR ( 'NONE', #17193, 39.37007874015748143 ) ;
#23419=CARTESIAN_POINT ( 'NONE',  ( 0.000000000000000000, 3.267716535433071279, 0.3149606299212576177 ) ) ;
#23420=EDGE_LOOP ( 'NONE', ( #7743, #18343, #20940, #1086 ) ) ;
#23422=FACE_OUTER_BOUND ( 'NONE', #8416, .T. ) ;
#23423=EDGE_CURVE ( 'NONE', #11433, #34446, #8740, .T. ) ;
#23425=AXIS2_PLACEMENT_3D ( 'NONE', #38044, #26159, #6287 ) ;
#23427=LINE ( 'NONE', #39180, #37166 ) ;
#23428=ORIENTED_EDGE ( 'NONE', *, *, #28302, .F. ) ;
#23429=LINE ( 'NONE', #50489, #50422 ) ;
#23430=VECTOR ( 'NONE', #23099, 39.37007874015748143 ) ;
#23431=ORIENTED_EDGE ( 'NONE', *, *, #26096, .F. ) ;
#23432=ORIENTED_EDGE ( 'NONE', *, *, #50263, .T. ) ;
#23433=CARTESIAN_POINT ( 'NONE',  ( -2.182111253630085290, 3.267716535433071279, 0.1181102362204704270 ) ) ;
#23434=VERTEX_POINT ( 'NONE', #13640 ) ;
#23435=CARTESIAN_POINT ( 'NONE',  ( -0.5455278134075208785, 3.267716535433071279, 1.889763779527550369 ) ) ;
#23436=ORIENTED_EDGE ( 'NONE', *, *, #10050, .T. ) ;
#23438=DIRECTION ( 'NONE',  ( 1.000000000000000000, -0.000000000000000000, 0.000000000000000000 ) ) ;
#23439=EDGE_CURVE ( 'NONE', #27824, #41536, #17509, .T. ) ;
#23440=CARTESIAN_POINT ( 'NONE',  ( -1.985260859929297572, 3.346456692913386100, 0.8645800689071783118 ) ) ;
#23443=EDGE_LOOP ( 'NONE', ( #17161, #39511, #10435, #2614 ) ) ;
#23445=ADVANCED_FACE ( 'NONE', ( #33019 ), #21635, .F. ) ;
#23446=DIRECTION ( 'NONE',  ( 0.000000000000000000, 0.000000000000000000, -1.000000000000000000 ) ) ;
#23447=ADVANCED_FACE ( 'NONE', ( #994 ), #40245, .F. ) ;
#23448=EDGE_CURVE ( 'NONE', #43946, #34116, #21133, .T. ) ;
#23449=CARTESIAN_POINT ( 'NONE',  ( -0.3486774197067340486, 3.267716535433071279, -0.1968503937007883287 ) ) ;
#23450=VERTEX_POINT ( 'NONE', #1506 ) ;
#23451=VERTEX_POINT ( 'NONE', #21389 ) ;
#23452=CARTESIAN_POINT ( 'NONE',  ( 0.4696143004045482683, 3.267716535433071279, -1.629301903132388739E-16 ) ) ;
#23453=CARTESIAN_POINT ( 'NONE',  ( 1.363819533518803695, 0.000000000000000000, 1.535433070866133898 ) ) ;
#23454=VECTOR ( 'NONE', #1690, 39.37007874015748143 ) ;
#23460=AXIS2_PLACEMENT_3D ( 'NONE', #41517, #30410, #2278 ) ;
#23461=DIRECTION ( 'NONE',  ( -3.469446951953613696E-16, 0.000000000000000000, -1.000000000000000000 ) ) ;
#23464=LINE ( 'NONE', #15478, #7767 ) ;
#23465=VECTOR ( 'NONE', #4835, 39.37007874015748143 ) ;
#23466=VERTEX_POINT ( 'NONE', #20870 ) ;
#23468=ADVANCED_FACE ( 'NONE', ( #37140 ), #28609, .F. ) ;
#23470=ORIENTED_EDGE ( 'NONE', *, *, #36603, .F. ) ;
#23471=CARTESIAN_POINT ( 'NONE',  ( -1.166969139818015977, 0.000000000000000000, 1.732283464566920950 ) ) ;
#23473=EDGE_LOOP ( 'NONE', ( #47981, #32314, #33159, #4936 ) ) ;
#23474=EDGE_CURVE ( 'NONE', #19508, #37443, #33269, .T. ) ;
#23476=PLANE ( 'NONE',  #50139 ) ;
#23477=ORIENTED_EDGE ( 'NONE', *, *, #16125, .T. ) ;
#23479=EDGE_CURVE ( 'NONE', #18853, #25196, #2013, .T. ) ;
#23480=ORIENTED_EDGE ( 'NONE', *, *, #26777, .T. ) ;
#23481=DIRECTION ( 'NONE',  ( -0.000000000000000000, 0.000000000000000000, 1.000000000000000000 ) ) ;
#23482=LINE ( 'NONE', #3875, #10761 ) ;
#23485=AXIS2_PLACEMENT_3D ( 'NONE', #25, #8543, #47488 ) ;
#23489=ADVANCED_FACE ( 'NONE', ( #40496 ), #1250, .F. ) ;
#23491=FACE_OUTER_BOUND ( 'NONE', #6423, .T. ) ;
#23493=DIRECTION ( 'NONE',  ( 1.000000000000000000, 0.000000000000000000, 0.000000000000000000 ) ) ;
#23494=AXIS2_PLACEMENT_3D ( 'NONE', #16387, #4764, #36267 ) ;
#23495=EDGE_CURVE ( 'NONE', #26927, #35609, #38157, .T. ) ;
#23497=CARTESIAN_POINT ( 'NONE',  ( 1.363819533518803029, 3.267716535433071279, -2.365849761790804994E-16 ) ) ;
#23499=ORIENTED_EDGE ( 'NONE', *, *, #42591, .T. ) ;
#23502=ORIENTED_EDGE ( 'NONE', *, *, #29010, .T. ) ;
#23503=ORIENTED_EDGE ( 'NONE', *, *, #23439, .F. ) ;
#23505=LINE ( 'NONE', #39257, #12763 ) ;
#23506=EDGE_CURVE ( 'NONE', #26706, #49094, #18265, .T. ) ;
#23507=DIRECTION ( 'NONE',  ( 1.000000000000000000, 0.000000000000000000, -3.469446951953613696E-16 ) ) ;
#23508=CARTESIAN_POINT ( 'NONE',  ( -0.8182917201112817063, 3.267716535433071279, 1.419509857074483046E-16 ) ) ;
#23509=EDGE_CURVE ( 'NONE', #9566, #34698, #46578, .T. ) ;
#23510=LINE ( 'NONE', #15017, #43643 ) ;
#23512=ORIENTED_EDGE ( 'NONE', *, *, #14354, .F. ) ;
#23515=ORIENTED_EDGE ( 'NONE', *, *, #2845, .T. ) ;
#23516=PLANE ( 'NONE',  #10138 ) ;
#23517=CARTESIAN_POINT ( 'NONE',  ( 0.000000000000000000, 3.267716535433071279, 0.000000000000000000 ) ) ;
#23519=DIRECTION ( 'NONE',  ( 0.000000000000000000, 1.000000000000000000, 0.000000000000000000 ) ) ;
#23521=CARTESIAN_POINT ( 'NONE',  ( -1.909347346926325129, 3.267716535433071279, 3.312189666507129161E-16 ) ) ;
#23523=CARTESIAN_POINT ( 'NONE',  ( -1.091055626815042645, 3.346456692913386100, -0.9448818897637760728 ) ) ;
#23525=VECTOR ( 'NONE', #46071, 39.37007874015748143 ) ;
#23526=ORIENTED_EDGE ( 'NONE', *, *, #22716, .T. ) ;
#23527=AXIS2_PLACEMENT_3D ( 'NONE', #16058, #8310, #28432 ) ;
#23529=CARTESIAN_POINT ( 'NONE',  ( 0.8182917201112817063, 0.000000000000000000, -1.929133858267711110 ) ) ;
#23532=VECTOR ( 'NONE', #46458, 39.37007874015748143 ) ;
#23533=ORIENTED_EDGE ( 'NONE', *, *, #40207, .T. ) ;
#23534=ADVANCED_FACE ( 'NONE', ( #18528 ), #26015, .F. ) ;
#23536=ORIENTED_EDGE ( 'NONE', *, *, #44543, .T. ) ;
#23538=ORIENTED_EDGE ( 'NONE', *, *, #4846, .T. ) ;
#23539=CARTESIAN_POINT ( 'NONE',  ( 0.5455278134075212115, 3.267716535433071279, 0.9448818897637746295 ) ) ;
#23540=ADVANCED_FACE ( 'NONE', ( #21892 ), #22900, .F. ) ;
#23541=VERTEX_POINT ( 'NONE', #3279 ) ;
#23546=EDGE_CURVE ( 'NONE', #49534, #8198, #49715, .T. ) ;
#23547=EDGE_LOOP ( 'NONE', ( #49939, #50531, #1944, #46407 ) ) ;
#23550=DIRECTION ( 'NONE',  ( 0.000000000000000000, 1.000000000000000000, 0.000000000000000000 ) ) ;
#23551=CARTESIAN_POINT ( 'NONE',  ( 0.2727639067037604947, 3.267716535433071279, -1.417322834645664331 ) ) ;
#23552=ORIENTED_EDGE ( 'NONE', *, *, #9955, .T. ) ;
#23553=VERTEX_POINT ( 'NONE', #14651 ) ;
#23554=FACE_OUTER_BOUND ( 'NONE', #1485, .T. ) ;
#23555=LINE ( 'NONE', #39310, #21973 ) ;
#23556=CARTESIAN_POINT ( 'NONE',  ( -1.486187880958815377, 3.267716535433071279, -1.574803149606293307 ) ) ;
#23557=VERTEX_POINT ( 'NONE', #42516 ) ;
#23558=ORIENTED_EDGE ( 'NONE', *, *, #20400, .T. ) ;
#23560=CARTESIAN_POINT ( 'NONE',  ( -1.636583440222564301, 0.000000000000000000, -0.6299212598425177889 ) ) ;
#23563=( CONVERSION_BASED_UNIT ( 'INCH', #5802 ) LENGTH_UNIT ( ) NAMED_UNIT ( #32082 ) );
#23564=DIRECTION ( 'NONE',  ( 1.734723475976806848E-16, 0.000000000000000000, 1.000000000000000000 ) ) ;
#23565=VECTOR ( 'NONE', #43904, 39.37007874015748143 ) ;
#23566=EDGE_LOOP ( 'NONE', ( #36756, #44990, #37506, #23229 ) ) ;
#23567=VECTOR ( 'NONE', #31719, 39.37007874015748143 ) ;
#23568=CARTESIAN_POINT ( 'NONE',  ( -0.6214413264104939882, 3.346456692913386100, 0.9055118110236167750 ) ) ;
#23570=ORIENTED_EDGE ( 'NONE', *, *, #47454, .T. ) ;
#23572=CARTESIAN_POINT ( 'NONE',  ( 0.2727639067037602172, 0.000000000000000000, -1.929133858267710000 ) ) ;
#23573=AXIS2_PLACEMENT_3D ( 'NONE', #40152, #32153, #12515 ) ;
#23574=EDGE_CURVE ( 'NONE', #35899, #34255, #33781, .T. ) ;
#23579=DIRECTION ( 'NONE',  ( -3.469446951953613696E-16, 0.000000000000000000, -1.000000000000000000 ) ) ;
#23580=EDGE_LOOP ( 'NONE', ( #38000, #310, #44586, #47962 ) ) ;
#23582=VERTEX_POINT ( 'NONE', #34530 ) ;
#23583=VECTOR ( 'NONE', #15872, 39.37007874015748143 ) ;
#23584=EDGE_CURVE ( 'NONE', #18622, #31182, #10522, .T. ) ;
#23586=EDGE_LOOP ( 'NONE', ( #49211, #46782, #5548, #38521 ) ) ;
#23590=LINE ( 'NONE', #24620, #32700 ) ;
#23593=FACE_OUTER_BOUND ( 'NONE', #50007, .T. ) ;
#23594=CARTESIAN_POINT ( 'NONE',  ( -1.486187880958816931, 3.267716535433071279, 1.574803149606291530 ) ) ;
#23596=DIRECTION ( 'NONE',  ( 1.734723475976806848E-16, -0.000000000000000000, 1.000000000000000000 ) ) ;
#23597=DIRECTION ( 'NONE',  ( 1.000000000000000000, 0.000000000000000000, 0.000000000000000000 ) ) ;
#23598=LINE ( 'NONE', #50912, #33750 ) ;
#23599=EDGE_LOOP ( 'NONE', ( #33492, #30201, #47372, #48623 ) ) ;
#23600=PLANE ( 'NONE',  #24293 ) ;
#23601=CARTESIAN_POINT ( 'NONE',  ( 0.5455278134075212115, 3.346456692913386100, -1.259842519685035134 ) ) ;
#23603=VECTOR ( 'NONE', #42589, 39.37007874015748143 ) ;
#23604=VECTOR ( 'NONE', #1180, 39.37007874015748143 ) ;
#23606=DIRECTION ( 'NONE',  ( -1.000000000000000000, -0.000000000000000000, -0.000000000000000000 ) ) ;
#23608=CARTESIAN_POINT ( 'NONE',  ( 1.560669927219590747, 3.267716535433071279, -5.414661521997677271E-16 ) ) ;
#23609=VECTOR ( 'NONE', #2935, 39.37007874015748143 ) ;
#23610=DIRECTION ( 'NONE',  ( 0.000000000000000000, 0.000000000000000000, 1.000000000000000000 ) ) ;
#23615=EDGE_CURVE ( 'NONE', #18225, #17559, #29892, .T. ) ;
#23616=EDGE_CURVE ( 'NONE', #29102, #5349, #42258, .T. ) ;
#23618=ORIENTED_EDGE ( 'NONE', *, *, #40647, .T. ) ;
#23621=CARTESIAN_POINT ( 'NONE',  ( -1.091055626815042201, 3.346456692913386100, 1.574803149606291974 ) ) ;
#23623=FACE_OUTER_BOUND ( 'NONE', #27722, .T. ) ;
#23627=FACE_OUTER_BOUND ( 'NONE', #1404, .T. ) ;
#23628=VERTEX_POINT ( 'NONE', #10017 ) ;
#23629=EDGE_LOOP ( 'NONE', ( #28055, #40552, #33973, #981 ) ) ;
#23630=DIRECTION ( 'NONE',  ( -3.469446951953613696E-16, 0.000000000000000000, -1.000000000000000000 ) ) ;
#23635=ORIENTED_EDGE ( 'NONE', *, *, #47192, .F. ) ;
#23641=EDGE_LOOP ( 'NONE', ( #20505, #28146, #18623, #15136 ) ) ;
#23643=EDGE_CURVE ( 'NONE', #48864, #17840, #43263, .T. ) ;
#23645=CIRCLE ( 'NONE', #7148, 2.106299212598425008 ) ;
#23646=ADVANCED_FACE ( 'NONE', ( #12302 ), #3534, .F. ) ;
#23647=CARTESIAN_POINT ( 'NONE',  ( -1.439733046521776583, 0.000000000000000000, -0.6299212598425177889 ) ) ;
#23649=CARTESIAN_POINT ( 'NONE',  ( 1.091055626815042645, 0.000000000000000000, 1.259842519685033357 ) ) ;
#23651=AXIS2_PLACEMENT_3D ( 'NONE', #20724, #32882, #9877 ) ;
#23652=DIRECTION ( 'NONE',  ( 1.734723475976806848E-16, 0.000000000000000000, 1.000000000000000000 ) ) ;
#23654=CARTESIAN_POINT ( 'NONE',  ( 3.054013992583308121E-16, 3.346456692913386100, 2.493791675044291445 ) ) ;
#23656=VERTEX_POINT ( 'NONE', #50709 ) ;
#23657=LINE ( 'NONE', #15659, #32421 ) ;
#23659=LINE ( 'NONE', #12044, #24869 ) ;
#23661=CARTESIAN_POINT ( 'NONE',  ( -1.439733046521776583, 3.267716535433071279, 4.995077429881868843E-16 ) ) ;
#23662=CARTESIAN_POINT ( 'NONE',  ( 0.5455278134075212115, 0.000000000000000000, -0.6299212598425181220 ) ) ;
#23664=PLANE ( 'NONE',  #13905 ) ;
#23665=CARTESIAN_POINT ( 'NONE',  ( -0.6214413264104945434, 0.000000000000000000, -2.047244094488181343 ) ) ;
#23666=DIRECTION ( 'NONE',  ( 1.734723475976806848E-16, -0.000000000000000000, 1.000000000000000000 ) ) ;
#23668=ORIENTED_EDGE ( 'NONE', *, *, #46384, .T. ) ;
#23669=CARTESIAN_POINT ( 'NONE',  ( -0.07591351300297333182, 3.267716535433071279, -0.7874015748031470974 ) ) ;
#23670=LINE ( 'NONE', #7674, #17696 ) ;
#23674=VERTEX_POINT ( 'NONE', #31157 ) ;
#23675=VECTOR ( 'NONE', #1860, 39.37007874015748143 ) ;
#23676=AXIS2_PLACEMENT_3D ( 'NONE', #39859, #28487, #16376 ) ;
#23678=AXIS2_PLACEMENT_3D ( 'NONE', #15150, #43259, #46608 ) ;
#23680=ORIENTED_EDGE ( 'NONE', *, *, #47881, .T. ) ;
#23682=CARTESIAN_POINT ( 'NONE',  ( 0.000000000000000000, 3.267716535433071279, -0.1574803149606301411 ) ) ;
#23683=ORIENTED_EDGE ( 'NONE', *, *, #47192, .T. ) ;
#23684=CARTESIAN_POINT ( 'NONE',  ( -0.7053729475263631477, 3.346456692913386100, 2.047244094488179567 ) ) ;
#23689=VERTEX_POINT ( 'NONE', #24177 ) ;
#23691=DIRECTION ( 'NONE',  ( -0.000000000000000000, 1.000000000000000000, -0.000000000000000000 ) ) ;
#23692=EDGE_LOOP ( 'NONE', ( #7332, #158, #30740, #1983, #29389 ) ) ;
#23693=VERTEX_POINT ( 'NONE', #15156 ) ;
#23694=LINE ( 'NONE', #35578, #38913 ) ;
#23695=ORIENTED_EDGE ( 'NONE', *, *, #35654, .T. ) ;
#23696=VECTOR ( 'NONE', #26263, 39.37007874015748143 ) ;
#23697=CARTESIAN_POINT ( 'NONE',  ( -0.07591351300297284610, 3.346456692913386100, 1.535433070866133898 ) ) ;
#23698=EDGE_CURVE ( 'NONE', #11755, #33217, #39922, .T. ) ;
#23700=EDGE_LOOP ( 'NONE', ( #14730, #37982, #13601, #16599 ) ) ;
#23701=CARTESIAN_POINT ( 'NONE',  ( -1.909347346926324462, 3.346456692913386100, -0.03937007874015881204 ) ) ;
#23703=DIRECTION ( 'NONE',  ( -0.000000000000000000, 1.000000000000000000, -0.000000000000000000 ) ) ;
#23704=EDGE_CURVE ( 'NONE', #19800, #4856, #46615, .T. ) ;
#23706=DIRECTION ( 'NONE',  ( 0.000000000000000000, 0.000000000000000000, -1.000000000000000000 ) ) ;
#23708=CARTESIAN_POINT ( 'NONE',  ( 1.287906020515829919, 3.267716535433071279, -4.468321617281354090E-16 ) ) ;
#23709=DIRECTION ( 'NONE',  ( -1.000000000000000000, 0.000000000000000000, 1.734723475976806848E-16 ) ) ;
#23710=VECTOR ( 'NONE', #24058, 39.37007874015748143 ) ;
#23711=CIRCLE ( 'NONE', #1462, 2.106299212598425008 ) ;
#23713=ORIENTED_EDGE ( 'NONE', *, *, #27487, .F. ) ;
#23715=PLANE ( 'NONE',  #24469 ) ;
#23716=DIRECTION ( 'NONE',  ( 1.000000000000000000, 0.000000000000000000, 0.000000000000000000 ) ) ;
#23717=DIRECTION ( 'NONE',  ( -3.469446951953613696E-16, 0.000000000000000000, -1.000000000000000000 ) ) ;
#23718=VECTOR ( 'NONE', #23244, 39.37007874015748143 ) ;
#23720=CARTESIAN_POINT ( 'NONE',  ( 1.091055626815042867, 3.267716535433071279, -1.892679809432645129E-16 ) ) ;
#23721=CARTESIAN_POINT ( 'NONE',  ( 0.000000000000000000, 3.267716535433071279, -0.03937007874015868020 ) ) ;
#23722=VERTEX_POINT ( 'NONE', #31409 ) ;
#23724=VECTOR ( 'NONE', #13313, 39.37007874015748143 ) ;
#23727=VECTOR ( 'NONE', #8869, 39.37007874015748143 ) ;
#23728=VERTEX_POINT ( 'NONE', #42765 ) ;
#23730=DIRECTION ( 'NONE',  ( -0.000000000000000000, 1.000000000000000000, -0.000000000000000000 ) ) ;
#23731=ORIENTED_EDGE ( 'NONE', *, *, #49935, .F. ) ;
#23732=EDGE_CURVE ( 'NONE', #40030, #32732, #47364, .T. ) ;
#23733=DIRECTION ( 'NONE',  ( 1.734723475976806848E-16, 0.000000000000000000, 1.000000000000000000 ) ) ;
#23734=ADVANCED_FACE ( 'NONE', ( #27522 ), #20024, .F. ) ;
#23735=VERTEX_POINT ( 'NONE', #11780 ) ;
#23736=LINE ( 'NONE', #15235, #49338 ) ;
#23737=ORIENTED_EDGE ( 'NONE', *, *, #263, .T. ) ;
#23738=EDGE_CURVE ( 'NONE', #13805, #41605, #27269, .T. ) ;
#23740=DIRECTION ( 'NONE',  ( -0.000000000000000000, 0.000000000000000000, 1.000000000000000000 ) ) ;
#23742=EDGE_CURVE ( 'NONE', #32550, #13413, #50967, .T. ) ;
#23744=VECTOR ( 'NONE', #15168, 39.37007874015748143 ) ;
#23745=EDGE_CURVE ( 'NONE', #3425, #36591, #8172, .T. ) ;
#23746=EDGE_LOOP ( 'NONE', ( #14376, #28440, #17600, #34933 ) ) ;
#23748=ORIENTED_EDGE ( 'NONE', *, *, #49872, .T. ) ;
#23751=CARTESIAN_POINT ( 'NONE',  ( -1.363819533518803473, 0.000000000000000000, -0.7874015748031470974 ) ) ;
#23752=DIRECTION ( 'NONE',  ( 0.000000000000000000, -1.000000000000000000, 0.000000000000000000 ) ) ;
#23755=VECTOR ( 'NONE', #48529, 39.37007874015748143 ) ;
#23756=DIRECTION ( 'NONE',  ( 0.000000000000000000, 0.000000000000000000, -1.000000000000000000 ) ) ;
#23757=ADVANCED_FACE ( 'NONE', ( #35795 ), #16435, .F. ) ;
#23758=CARTESIAN_POINT ( 'NONE',  ( -0.07591351300297316529, 3.267716535433071279, 2.633779063002562669E-17 ) ) ;
#23759=ORIENTED_EDGE ( 'NONE', *, *, #33146, .F. ) ;
#23760=AXIS2_PLACEMENT_3D ( 'NONE', #3268, #46104, #19257 ) ;
#23761=CARTESIAN_POINT ( 'NONE',  ( 2.378961647330872786, 3.267716535433071279, -0.3149606299212596716 ) ) ;
#23762=EDGE_CURVE ( 'NONE', #45153, #46201, #6015, .T. ) ;
#23763=VERTEX_POINT ( 'NONE', #24435 ) ;
#23766=VECTOR ( 'NONE', #28988, 39.37007874015748143 ) ;
#23768=DIRECTION ( 'NONE',  ( -0.000000000000000000, 1.000000000000000000, -0.000000000000000000 ) ) ;
#23769=DIRECTION ( 'NONE',  ( -3.469446951953613696E-16, 0.000000000000000000, -1.000000000000000000 ) ) ;
#23770=EDGE_CURVE ( 'NONE', #17416, #47487, #1891, .T. ) ;
#23771=DIRECTION ( 'NONE',  ( -0.000000000000000000, 1.000000000000000000, -0.000000000000000000 ) ) ;
#23772=CARTESIAN_POINT ( 'NONE',  ( 1.636583440222563857, 0.000000000000000000, 0.1181102362204701633 ) ) ;
#23774=VERTEX_POINT ( 'NONE', #37525 ) ;
#23775=LINE ( 'NONE', #35401, #6532 ) ;
#23776=LINE ( 'NONE', #19886, #31729 ) ;
#23777=ORIENTED_EDGE ( 'NONE', *, *, #4640, .F. ) ;
#23778=ADVANCED_FACE ( 'NONE', ( #36055 ), #935, .F. ) ;
#23779=LINE ( 'NONE', #19638, #49840 ) ;
#23780=CARTESIAN_POINT ( 'NONE',  ( -1.712496953225537633, 3.267716535433071279, 1.220472440944875059 ) ) ;
#23781=VECTOR ( 'NONE', #34743, 39.37007874015748143 ) ;
#23782=DIRECTION ( 'NONE',  ( -0.000000000000000000, 1.000000000000000000, -0.000000000000000000 ) ) ;
#23783=DIRECTION ( 'NONE',  ( -3.469446951953613696E-16, 0.000000000000000000, -1.000000000000000000 ) ) ;
#23786=DIRECTION ( 'NONE',  ( -0.000000000000000000, 1.000000000000000000, -0.000000000000000000 ) ) ;
#23788=VECTOR ( 'NONE', #47187, 39.37007874015748143 ) ;
#23789=ORIENTED_EDGE ( 'NONE', *, *, #26537, .F. ) ;
#23790=ORIENTED_EDGE ( 'NONE', *, *, #32887, .T. ) ;
#23792=DIRECTION ( 'NONE',  ( 0.000000000000000000, -1.000000000000000000, 0.000000000000000000 ) ) ;
#23795=ORIENTED_EDGE ( 'NONE', *, *, #3013, .F. ) ;
#23798=CARTESIAN_POINT ( 'NONE',  ( 0.4696143004045484348, 3.267716535433071279, 1.220472440944875281 ) ) ;
#23800=CIRCLE ( 'NONE', #11425, 2.106299212598425008 ) ;
#23803=EDGE_CURVE ( 'NONE', #5523, #17338, #17638, .T. ) ;
#23804=CARTESIAN_POINT ( 'NONE',  ( 0.5455278134075212115, 3.267716535433071279, -0.3149606299212593941 ) ) ;
#23806=CARTESIAN_POINT ( 'NONE',  ( 0.000000000000000000, 3.267716535433071279, -0.3543307086614174151 ) ) ;
#23808=EDGE_CURVE ( 'NONE', #33436, #24648, #2149, .T. ) ;
#23809=EDGE_LOOP ( 'NONE', ( #16758, #555, #16583, #42520, #31112 ) ) ;
#23812=DIRECTION ( 'NONE',  ( 1.734723475976806848E-16, -0.000000000000000000, 1.000000000000000000 ) ) ;
#23813=CARTESIAN_POINT ( 'NONE',  ( -1.363819533518803473, 3.232777166330603524, 2.047244094488179567 ) ) ;
#23814=ORIENTED_EDGE ( 'NONE', *, *, #50798, .F. ) ;
#23815=ORIENTED_EDGE ( 'NONE', *, *, #41542, .T. ) ;
#23817=DIRECTION ( 'NONE',  ( -1.000000000000000000, 0.000000000000000000, -0.000000000000000000 ) ) ;
#23818=DIRECTION ( 'NONE',  ( -1.000000000000000000, -0.000000000000000000, -0.000000000000000000 ) ) ;
#23819=ORIENTED_EDGE ( 'NONE', *, *, #45589, .F. ) ;
#23821=CARTESIAN_POINT ( 'NONE',  ( 0.000000000000000000, 3.346456692913386100, 0.000000000000000000 ) ) ;
#23823=CARTESIAN_POINT ( 'NONE',  ( 1.015142113812069313, 0.000000000000000000, -0.4724409448818889246 ) ) ;
#23825=CARTESIAN_POINT ( 'NONE',  ( 1.363819533518803251, 0.000000000000000000, 0.9055118110236164419 ) ) ;
#23826=PLANE ( 'NONE',  #32679 ) ;
#23830=ORIENTED_EDGE ( 'NONE', *, *, #49301, .T. ) ;
#23831=CARTESIAN_POINT ( 'NONE',  ( 0.1968503937007872462, 0.000000000000000000, 0.4330708661417287386 ) ) ;
#23833=VECTOR ( 'NONE', #13739, 39.37007874015748143 ) ;
#23835=CARTESIAN_POINT ( 'NONE',  ( 1.287906020515830141, 3.267716535433071279, -4.468321617281355077E-16 ) ) ;
#23836=ADVANCED_FACE ( 'NONE', ( #5765 ), #44038, .F. ) ;
#23839=AXIS2_PLACEMENT_3D ( 'NONE', #16642, #50919, #4503 ) ;
#23844=DIRECTION ( 'NONE',  ( 0.000000000000000000, 0.000000000000000000, -1.000000000000000000 ) ) ;
#23848=DIRECTION ( 'NONE',  ( 1.000000000000000000, 0.000000000000000000, 0.000000000000000000 ) ) ;
#23850=VERTEX_POINT ( 'NONE', #20293 ) ;
#23852=EDGE_CURVE ( 'NONE', #28934, #44754, #21510, .T. ) ;
#23854=EDGE_CURVE ( 'NONE', #34255, #32050, #679, .T. ) ;
#23859=LINE ( 'NONE', #30282, #47685 ) ;
#23861=VERTEX_POINT ( 'NONE', #28548 ) ;
#23863=LINE ( 'NONE', #4500, #11817 ) ;
#23866=PLANE ( 'NONE',  #23839 ) ;
#23868=VERTEX_POINT ( 'NONE', #18149 ) ;
#23870=EDGE_CURVE ( 'NONE', #33556, #11186, #45737, .T. ) ;
#23873=DIRECTION ( 'NONE',  ( -1.000000000000000000, 0.000000000000000000, 0.000000000000000000 ) ) ;
#23874=CARTESIAN_POINT ( 'NONE',  ( 1.909347346926324684, 3.346456692913386100, -0.1574803149606304187 ) ) ;
#23875=EDGE_CURVE ( 'NONE', #31767, #44945, #45013, .T. ) ;
#23877=ORIENTED_EDGE ( 'NONE', *, *, #38867, .F. ) ;
#23880=CARTESIAN_POINT ( 'NONE',  ( 1.909347346926324684, 3.346456692913386100, -0.3543307086614178592 ) ) ;
#23882=DIRECTION ( 'NONE',  ( -0.000000000000000000, 1.000000000000000000, -0.000000000000000000 ) ) ;
#23883=CARTESIAN_POINT ( 'NONE',  ( 1.560669927219590747, 3.267716535433071279, 0.4724409448818871482 ) ) ;
#23884=AXIS2_PLACEMENT_3D ( 'NONE', #8044, #43656, #44173 ) ;
#23885=CARTESIAN_POINT ( 'NONE',  ( -0.8182917201112814842, 0.000000000000000000, 1.535433070866133898 ) ) ;
#23886=CARTESIAN_POINT ( 'NONE',  ( 1.833433833923351353, 3.267716535433071279, -6.361001426713998480E-16 ) ) ;
#23887=ORIENTED_EDGE ( 'NONE', *, *, #17622, .T. ) ;
#23889=ORIENTED_EDGE ( 'NONE', *, *, #18084, .T. ) ;
#23890=DIRECTION ( 'NONE',  ( 0.000000000000000000, -1.000000000000000000, 0.000000000000000000 ) ) ;
#23891=LINE ( 'NONE', #28010, #38722 ) ;
#23892=DIRECTION ( 'NONE',  ( -1.000000000000000000, 0.000000000000000000, 1.734723475976806848E-16 ) ) ;
#23893=FACE_BOUND ( 'NONE', #41363, .T. ) ;
#23894=ORIENTED_EDGE ( 'NONE', *, *, #28460, .T. ) ;
#23895=CARTESIAN_POINT ( 'NONE',  ( -1.363819533518803473, 3.346456692913386100, 1.681890501046756192 ) ) ;
#23896=ORIENTED_EDGE ( 'NONE', *, *, #49959, .T. ) ;
#23899=VECTOR ( 'NONE', #34445, 39.37007874015748143 ) ;
#23900=ORIENTED_EDGE ( 'NONE', *, *, #28651, .F. ) ;
#23901=EDGE_CURVE ( 'NONE', #20171, #6948, #18403, .T. ) ;
#23902=ORIENTED_EDGE ( 'NONE', *, *, #20404, .T. ) ;
#23903=DIRECTION ( 'NONE',  ( 1.734723475976806848E-16, -0.000000000000000000, 1.000000000000000000 ) ) ;
#23905=CARTESIAN_POINT ( 'NONE',  ( -1.363819533518803029, 3.346456692913386100, 1.220472440944875281 ) ) ;
#23908=VECTOR ( 'NONE', #2833, 39.37007874015748143 ) ;
#23910=EDGE_CURVE ( 'NONE', #48435, #13777, #26893, .T. ) ;
#23911=ADVANCED_FACE ( 'NONE', ( #14783 ), #42139, .F. ) ;
#23912=PLANE ( 'NONE',  #38796 ) ;
#23915=LINE ( 'NONE', #32185, #2296 ) ;
#23916=EDGE_LOOP ( 'NONE', ( #44530, #43648, #31266, #27057 ) ) ;
#23918=VECTOR ( 'NONE', #20177, 39.37007874015748143 ) ;
#23920=DIRECTION ( 'NONE',  ( -3.469446951953613696E-16, 0.000000000000000000, -1.000000000000000000 ) ) ;
#23924=ORIENTED_EDGE ( 'NONE', *, *, #28226, .F. ) ;
#23927=LINE ( 'NONE', #8689, #49843 ) ;
#23931=CARTESIAN_POINT ( 'NONE',  ( 0.000000000000000000, 3.267716535433071279, -0.1968503937007881899 ) ) ;
#23935=CARTESIAN_POINT ( 'NONE',  ( 1.560669927219590747, 3.346456692913386100, 0.7874015748031454320 ) ) ;
#23936=ORIENTED_EDGE ( 'NONE', *, *, #6201, .F. ) ;
#23938=ORIENTED_EDGE ( 'NONE', *, *, #18202, .T. ) ;
#23939=EDGE_LOOP ( 'NONE', ( #4691, #29304, #25008, #37417 ) ) ;
#23940=LINE ( 'NONE', #12578, #688 ) ;
#23942=VERTEX_POINT ( 'NONE', #46242 ) ;
#23944=PLANE ( 'NONE',  #1327 ) ;
#23945=ORIENTED_EDGE ( 'NONE', *, *, #14972, .T. ) ;
#23946=VECTOR ( 'NONE', #48636, 39.37007874015748143 ) ;
#23947=CARTESIAN_POINT ( 'NONE',  ( 1.282536922928985357, 3.255655746335629708, -2.086614173228339641 ) ) ;
#23949=VERTEX_POINT ( 'NONE', #15032 ) ;
#23950=CARTESIAN_POINT ( 'NONE',  ( -0.8182917201112819283, 0.000000000000000000, -0.9842519685039342603 ) ) ;
#23951=DIRECTION ( 'NONE',  ( -1.000000000000000000, 0.000000000000000000, 0.000000000000000000 ) ) ;
#23953=DIRECTION ( 'NONE',  ( -1.000000000000000000, 0.000000000000000000, -0.000000000000000000 ) ) ;
#23954=ORIENTED_EDGE ( 'NONE', *, *, #1185, .T. ) ;
#23955=VECTOR ( 'NONE', #4895, 39.37007874015748143 ) ;
#23957=VERTEX_POINT ( 'NONE', #10902 ) ;
#23958=ORIENTED_EDGE ( 'NONE', *, *, #25856, .F. ) ;
#23959=LINE ( 'NONE', #32228, #14950 ) ;
#23960=LINE ( 'NONE', #4596, #32823 ) ;
#23961=VERTEX_POINT ( 'NONE', #38289 ) ;
#23962=CARTESIAN_POINT ( 'NONE',  ( -1.091055626815042645, 0.000000000000000000, -1.889763779527552146 ) ) ;
#23963=ORIENTED_EDGE ( 'NONE', *, *, #34725, .F. ) ;
#23964=CARTESIAN_POINT ( 'NONE',  ( 0.8182917201112824834, 3.346456692913386100, 2.047244094488179567 ) ) ;
#23967=DIRECTION ( 'NONE',  ( -3.469446951953613696E-16, 0.000000000000000000, -1.000000000000000000 ) ) ;
#23969=VERTEX_POINT ( 'NONE', #18661 ) ;
#23970=EDGE_CURVE ( 'NONE', #216, #47008, #7535, .T. ) ;
#23975=CARTESIAN_POINT ( 'NONE',  ( -1.863748091109392879, 3.267716535433071279, 1.102362204724404160 ) ) ;
#23978=VECTOR ( 'NONE', #33842, 39.37007874015748143 ) ;
#23980=CARTESIAN_POINT ( 'NONE',  ( 0.000000000000000000, 3.346456692913386100, 0.000000000000000000 ) ) ;
#23982=PLANE ( 'NONE',  #30850 ) ;
#23984=DIRECTION ( 'NONE',  ( -0.000000000000000000, 1.000000000000000000, -0.000000000000000000 ) ) ;
#23985=VECTOR ( 'NONE', #33498, 39.37007874015748143 ) ;
#23986=EDGE_CURVE ( 'NONE', #43399, #32147, #3662, .T. ) ;
#23987=ORIENTED_EDGE ( 'NONE', *, *, #46676, .T. ) ;
#23989=CARTESIAN_POINT ( 'NONE',  ( -0.5455278134075214336, 3.267716535433071279, 2.095509194042718182 ) ) ;
#23991=DIRECTION ( 'NONE',  ( 1.000000000000000000, 0.000000000000000000, 0.000000000000000000 ) ) ;
#23994=EDGE_CURVE ( 'NONE', #41081, #13698, #28416, .T. ) ;
#23995=ORIENTED_EDGE ( 'NONE', *, *, #39029, .F. ) ;
#23996=DIRECTION ( 'NONE',  ( -1.000000000000000000, 0.000000000000000000, -0.000000000000000000 ) ) ;
#23997=ORIENTED_EDGE ( 'NONE', *, *, #18708, .F. ) ;
#24000=LINE ( 'NONE', #4385, #17280 ) ;
#24002=ORIENTED_EDGE ( 'NONE', *, *, #38311, .T. ) ;
#24004=LINE ( 'NONE', #20388, #42154 ) ;
#24005=DIRECTION ( 'NONE',  ( 1.000000000000000000, -0.000000000000000000, 0.000000000000000000 ) ) ;
#24006=VECTOR ( 'NONE', #32489, 39.37007874015748143 ) ;
#24007=AXIS2_PLACEMENT_3D ( 'NONE', #31934, #19777, #23920 ) ;
#24009=VECTOR ( 'NONE', #41240, 39.37007874015748143 ) ;
#24010=DIRECTION ( 'NONE',  ( -1.000000000000000000, 0.000000000000000000, 1.734723475976806848E-16 ) ) ;
#24011=CARTESIAN_POINT ( 'NONE',  ( -1.636583440222564301, 3.267716535433071279, -0.8267716535433052849 ) ) ;
#24012=ORIENTED_EDGE ( 'NONE', *, *, #19309, .T. ) ;
#24014=CIRCLE ( 'NONE', #42257, 2.443628662382284489 ) ;
#24016=VERTEX_POINT ( 'NONE', #47238 ) ;
#24017=VECTOR ( 'NONE', #49557, 39.37007874015748143 ) ;
#24019=VERTEX_POINT ( 'NONE', #40048 ) ;
#24020=CARTESIAN_POINT ( 'NONE',  ( -0.8942052331142552601, 3.346456692913386100, -1.972094414217999914 ) ) ;
#24021=AXIS2_PLACEMENT_3D ( 'NONE', #45053, #29585, #41457 ) ;
#24023=DIRECTION ( 'NONE',  ( -1.000000000000000000, 0.000000000000000000, 1.734723475976806848E-16 ) ) ;
#24024=FACE_OUTER_BOUND ( 'NONE', #35754, .T. ) ;
#24025=VERTEX_POINT ( 'NONE', #15779 ) ;
#24026=EDGE_LOOP ( 'NONE', ( #15723, #32999, #48284, #33074 ) ) ;
#24031=DIRECTION ( 'NONE',  ( -0.000000000000000000, 1.000000000000000000, -0.000000000000000000 ) ) ;
#24032=ORIENTED_EDGE ( 'NONE', *, *, #41954, .F. ) ;
#24033=CARTESIAN_POINT ( 'NONE',  ( 0.7423782071083085965, 3.346456692913386100, 0.4330708661417287386 ) ) ;
#24034=EDGE_CURVE ( 'NONE', #47245, #49325, #16042, .T. ) ;
#24035=CARTESIAN_POINT ( 'NONE',  ( 1.287906020515830363, 3.267716535433071279, -4.468321617281356063E-16 ) ) ;
#24036=DIRECTION ( 'NONE',  ( 1.000000000000000000, 0.000000000000000000, 0.000000000000000000 ) ) ;
#24037=EDGE_CURVE ( 'NONE', #16050, #1443, #31798, .T. ) ;
#24038=DIRECTION ( 'NONE',  ( 1.734723475976806848E-16, -0.000000000000000000, 1.000000000000000000 ) ) ;
#24044=ORIENTED_EDGE ( 'NONE', *, *, #24999, .F. ) ;
#24046=VERTEX_POINT ( 'NONE', #16301 ) ;
#24047=CARTESIAN_POINT ( 'NONE',  ( 1.636583440222563857, 0.000000000000000000, 1.259842519685033135 ) ) ;
#24048=CARTESIAN_POINT ( 'NONE',  ( -0.8942052331142552601, 0.000000000000000000, -1.574803149606293529 ) ) ;
#24049=EDGE_CURVE ( 'NONE', #4787, #30956, #39281, .T. ) ;
#24050=PLANE ( 'NONE',  #10702 ) ;
#24054=ORIENTED_EDGE ( 'NONE', *, *, #13841, .T. ) ;
#24055=CARTESIAN_POINT ( 'NONE',  ( -1.636583440222564301, 0.000000000000000000, -0.5118110236220466680 ) ) ;
#24058=DIRECTION ( 'NONE',  ( -0.000000000000000000, 1.000000000000000000, -0.000000000000000000 ) ) ;
#24060=VECTOR ( 'NONE', #32904, 39.37007874015748143 ) ;
#24062=DIRECTION ( 'NONE',  ( -1.000000000000000000, 0.000000000000000000, 1.734723475976806848E-16 ) ) ;
#24064=ORIENTED_EDGE ( 'NONE', *, *, #6091, .T. ) ;
#24065=ORIENTED_EDGE ( 'NONE', *, *, #35845, .T. ) ;
#24068=FACE_OUTER_BOUND ( 'NONE', #25622, .T. ) ;
#24070=ORIENTED_EDGE ( 'NONE', *, *, #21545, .F. ) ;
#24071=CARTESIAN_POINT ( 'NONE',  ( 0.8182917201112824834, 0.000000000000000000, 2.047244094488179567 ) ) ;
#24072=FACE_OUTER_BOUND ( 'NONE', #31324, .T. ) ;
#24074=EDGE_CURVE ( 'NONE', #9880, #11936, #20676, .T. ) ;
#24076=VERTEX_POINT ( 'NONE', #27394 ) ;
#24079=CARTESIAN_POINT ( 'NONE',  ( 0.000000000000000000, 3.267716535433071279, 1.732283464566920950 ) ) ;
#24080=ORIENTED_EDGE ( 'NONE', *, *, #39996, .T. ) ;
#24081=FACE_OUTER_BOUND ( 'NONE', #3201, .T. ) ;
#24082=LINE ( 'NONE', #5224, #45025 ) ;
#24083=EDGE_LOOP ( 'NONE', ( #29100, #22809, #44283, #49930 ) ) ;
#24085=ORIENTED_EDGE ( 'NONE', *, *, #15972, .T. ) ;
#24087=CARTESIAN_POINT ( 'NONE',  ( 0.000000000000000000, 3.267716535433071279, -0.1968503937007880511 ) ) ;
#24088=LENGTH_MEASURE_WITH_UNIT ( LENGTH_MEASURE( 0.02539999999999999897 ), #12465 );
#24090=CIRCLE ( 'NONE', #1834, 2.165354330708661568 ) ;
#24092=CARTESIAN_POINT ( 'NONE',  ( -0.8942052331142552601, 3.346456692913386100, -0.3149606299212593941 ) ) ;
#24094=ORIENTED_EDGE ( 'NONE', *, *, #11138, .T. ) ;
#24097=ORIENTED_EDGE ( 'NONE', *, *, #46295, .T. ) ;
#24099=LINE ( 'NONE', #31861, #42400 ) ;
#24100=EDGE_CURVE ( 'NONE', #3033, #45153, #1316, .T. ) ;
#24103=EDGE_CURVE ( 'NONE', #44707, #2087, #44424, .T. ) ;
#24106=LINE ( 'NONE', #39852, #33674 ) ;
#24107=ORIENTED_EDGE ( 'NONE', *, *, #40215, .F. ) ;
#24109=CARTESIAN_POINT ( 'NONE',  ( -0.3486774197067340486, 3.346456692913386100, -0.8267716535433049518 ) ) ;
#24110=ORIENTED_EDGE ( 'NONE', *, *, #4527, .T. ) ;
#24112=CARTESIAN_POINT ( 'NONE',  ( 1.909347346926324462, 0.000000000000000000, -1.102362204724406602 ) ) ;
#24113=EDGE_CURVE ( 'NONE', #35899, #39562, #48772, .T. ) ;
#24114=CARTESIAN_POINT ( 'NONE',  ( 0.4696143004045476022, 0.000000000000000000, -2.244094488188969727 ) ) ;
#24117=CARTESIAN_POINT ( 'NONE',  ( 0.5455278134075212115, 3.346456692913386100, -6.146657985744592735E-16 ) ) ;
#24118=DIRECTION ( 'NONE',  ( -3.469446951953613696E-16, 0.000000000000000000, -1.000000000000000000 ) ) ;
#24119=EDGE_CURVE ( 'NONE', #14632, #27097, #33850, .T. ) ;
#24120=ORIENTED_EDGE ( 'NONE', *, *, #27176, .F. ) ;
#24121=FACE_BOUND ( 'NONE', #19950, .T. ) ;
#24122=LINE ( 'NONE', #32392, #18356 ) ;
#24125=VECTOR ( 'NONE', #29162, 39.37007874015748143 ) ;
#24126=CARTESIAN_POINT ( 'NONE',  ( -1.909347346926324462, 0.000000000000000000, -0.3543307086614171930 ) ) ;
#24127=CARTESIAN_POINT ( 'NONE',  ( -0.3486774197067340486, 3.346456692913386100, -2.077238655036873549 ) ) ;
#24128=CARTESIAN_POINT ( 'NONE',  ( -1.166969139818016199, 0.000000000000000000, -0.3543307086614174151 ) ) ;
#24129=EDGE_CURVE ( 'NONE', #4890, #27417, #44670, .T. ) ;
#24130=VECTOR ( 'NONE', #26740, 39.37007874015748143 ) ;
#24131=ORIENTED_EDGE ( 'NONE', *, *, #7596, .T. ) ;
#24133=DIRECTION ( 'NONE',  ( -1.000000000000000000, 0.000000000000000000, -0.000000000000000000 ) ) ;
#24135=ORIENTED_EDGE ( 'NONE', *, *, #14673, .F. ) ;
#24136=VECTOR ( 'NONE', #45718, 39.37007874015748143 ) ;
#24137=PLANE ( 'NONE',  #16850 ) ;
#24139=DIRECTION ( 'NONE',  ( -0.000000000000000000, 1.000000000000000000, -0.000000000000000000 ) ) ;
#24140=EDGE_CURVE ( 'NONE', #39237, #16898, #5188, .T. ) ;
#24141=AXIS2_PLACEMENT_3D ( 'NONE', #3909, #742, #5375 ) ;
#24143=VECTOR ( 'NONE', #48254, 39.37007874015748143 ) ;
#24145=ORIENTED_EDGE ( 'NONE', *, *, #2591, .T. ) ;
#24146=LINE ( 'NONE', #21296, #35340 ) ;
#24147=DIRECTION ( 'NONE',  ( -0.000000000000000000, 1.000000000000000000, -0.000000000000000000 ) ) ;
#24148=CARTESIAN_POINT ( 'NONE',  ( -0.8942052331142552601, 0.000000000000000000, -2.086614173228339641 ) ) ;
#24149=LINE ( 'NONE', #4528, #49547 ) ;
#24150=FACE_BOUND ( 'NONE', #41336, .T. ) ;
#24152=EDGE_LOOP ( 'NONE', ( #11197, #33801, #27971, #14577 ) ) ;
#24155=ORIENTED_EDGE ( 'NONE', *, *, #22376, .T. ) ;
#24156=ORIENTED_EDGE ( 'NONE', *, *, #26926, .F. ) ;
#24157=FACE_OUTER_BOUND ( 'NONE', #29091, .T. ) ;
#24158=EDGE_CURVE ( 'NONE', #24016, #16727, #1829, .T. ) ;
#24159=ORIENTED_EDGE ( 'NONE', *, *, #17903, .F. ) ;
#24160=ORIENTED_EDGE ( 'NONE', *, *, #10915, .T. ) ;
#24161=CARTESIAN_POINT ( 'NONE',  ( -4.268512490100411402E-16, 3.346456692913386100, -2.086614173228339641 ) ) ;
#24162=UNCERTAINTY_MEASURE_WITH_UNIT (LENGTH_MEASURE( 1.000000000000000082E-05 ), #23563, 'distance_accuracy_value', 'NONE');
#24165=CARTESIAN_POINT ( 'NONE',  ( -1.909347346926324462, 0.000000000000000000, -0.1574803149606297248 ) ) ;
#24167=EDGE_CURVE ( 'NONE', #25499, #26189, #21968, .T. ) ;
#24170=ADVANCED_FACE ( 'NONE', ( #17079 ), #45172, .F. ) ;
#24171=EDGE_CURVE ( 'NONE', #28641, #16479, #48517, .T. ) ;
#24172=VECTOR ( 'NONE', #14566, 39.37007874015748143 ) ;
#24175=ORIENTED_EDGE ( 'NONE', *, *, #39965, .T. ) ;
#24176=DIRECTION ( 'NONE',  ( 1.734723475976806848E-16, 0.000000000000000000, 1.000000000000000000 ) ) ;
#24177=CARTESIAN_POINT ( 'NONE',  ( -0.6214413264104945434, 3.267716535433071279, -2.244094488188968395 ) ) ;
#24178=CARTESIAN_POINT ( 'NONE',  ( 1.833433833923350909, 3.346456692913386100, -1.456692913385823296 ) ) ;
#24180=VECTOR ( 'NONE', #49213, 39.37007874015748143 ) ;
#24182=FACE_OUTER_BOUND ( 'NONE', #46096, .T. ) ;
#24184=VERTEX_POINT ( 'NONE', #18092 ) ;
#24185=CARTESIAN_POINT ( 'NONE',  ( -0.7053729475263578186, 3.267716535433071279, -2.047244094488181343 ) ) ;
#24186=CARTESIAN_POINT ( 'NONE',  ( 2.182111253630085290, 3.346456692913386100, -1.161035397307311917E-15 ) ) ;
#24188=AXIS2_PLACEMENT_3D ( 'NONE', #20811, #8171, #4811 ) ;
#24189=DIRECTION ( 'NONE',  ( 1.734723475976806848E-16, -0.000000000000000000, 1.000000000000000000 ) ) ;
#24190=ORIENTED_EDGE ( 'NONE', *, *, #8137, .T. ) ;
#24191=LINE ( 'NONE', #4571, #41279 ) ;
#24193=CARTESIAN_POINT ( 'NONE',  ( -0.07591351300297415061, 3.267716535433071279, 2.633779063002596873E-17 ) ) ;
#24195=EDGE_CURVE ( 'NONE', #31800, #16772, #40821, .T. ) ;
#24196=ORIENTED_EDGE ( 'NONE', *, *, #12345, .T. ) ;
#24197=ORIENTED_EDGE ( 'NONE', *, *, #1012, .T. ) ;
#24198=LINE ( 'NONE', #43034, #48437 ) ;
#24201=ORIENTED_EDGE ( 'NONE', *, *, #7473, .T. ) ;
#24203=DIRECTION ( 'NONE',  ( 1.000000000000000000, 0.000000000000000000, 0.000000000000000000 ) ) ;
#24205=ORIENTED_EDGE ( 'NONE', *, *, #44063, .T. ) ;
#24206=CARTESIAN_POINT ( 'NONE',  ( 1.636583440222563857, 3.346456692913386100, 0.6299212598425164567 ) ) ;
#24208=VECTOR ( 'NONE', #5678, 39.37007874015748143 ) ;
#24209=CARTESIAN_POINT ( 'NONE',  ( 1.636583440222563857, 0.000000000000000000, 0.9448818897637746295 ) ) ;
#24210=ORIENTED_EDGE ( 'NONE', *, *, #4905, .T. ) ;
#24212=CARTESIAN_POINT ( 'NONE',  ( 0.2727639067037604392, 0.000000000000000000, -0.3543307086614173040 ) ) ;
#24213=AXIS2_PLACEMENT_3D ( 'NONE', #13272, #33416, #34604 ) ;
#24214=ORIENTED_EDGE ( 'NONE', *, *, #22132, .T. ) ;
#24215=VECTOR ( 'NONE', #3245, 39.37007874015748143 ) ;
#24216=VECTOR ( 'NONE', #22397, 39.37007874015748143 ) ;
#24217=DIRECTION ( 'NONE',  ( 0.000000000000000000, 1.000000000000000000, 0.000000000000000000 ) ) ;
#24218=ORIENTED_EDGE ( 'NONE', *, *, #41888, .T. ) ;
#24219=ORIENTED_EDGE ( 'NONE', *, *, #25329, .T. ) ;
#24222=AXIS2_PLACEMENT_3D ( 'NONE', #31602, #43199, #35476 ) ;
#24224=ORIENTED_EDGE ( 'NONE', *, *, #2481, .F. ) ;
#24226=ORIENTED_EDGE ( 'NONE', *, *, #17418, .F. ) ;
#24227=CARTESIAN_POINT ( 'NONE',  ( 2.017116292511733633, 3.346456692913386100, 0.7874015748031456541 ) ) ;
#24228=EDGE_CURVE ( 'NONE', #5661, #11518, #9579, .T. ) ;
#24229=DIRECTION ( 'NONE',  ( -1.000000000000000000, 0.000000000000000000, 1.734723475976806848E-16 ) ) ;
#24230=DIRECTION ( 'NONE',  ( -1.000000000000000000, 0.000000000000000000, -0.000000000000000000 ) ) ;
#24231=EDGE_CURVE ( 'NONE', #37886, #47515, #38727, .T. ) ;
#24232=ADVANCED_FACE ( 'NONE', ( #6977 ), #37975, .F. ) ;
#24234=EDGE_LOOP ( 'NONE', ( #10079, #4147, #4280, #2623 ) ) ;
#24237=EDGE_CURVE ( 'NONE', #15224, #22568, #29963, .T. ) ;
#24238=LINE ( 'NONE', #20355, #13459 ) ;
#24240=CARTESIAN_POINT ( 'NONE',  ( 1.909347346926324684, 0.000000000000000000, -0.03937007874015936021 ) ) ;
#24241=CARTESIAN_POINT ( 'NONE',  ( -0.3486774197067332715, 3.267716535433071279, 1.209717811016576613E-16 ) ) ;
#24243=LINE ( 'NONE', #9516, #26750 ) ;
#24244=VECTOR ( 'NONE', #45648, 39.37007874015748143 ) ;
#24245=ORIENTED_EDGE ( 'NONE', *, *, #25050, .F. ) ;
#24246=DIRECTION ( 'NONE',  ( 0.000000000000000000, -1.000000000000000000, 0.000000000000000000 ) ) ;
#24248=AXIS2_PLACEMENT_3D ( 'NONE', #17275, #47953, #28365 ) ;
#24250=VECTOR ( 'NONE', #6022, 39.37007874015748143 ) ;
#24252=CIRCLE ( 'NONE', #25911, 2.106299212598425008 ) ;
#24253=CARTESIAN_POINT ( 'NONE',  ( -0.8182917201112819283, 3.346456692913386100, -0.7874015748031467643 ) ) ;
#24254=PLANE ( 'NONE',  #34175 ) ;
#24256=LINE ( 'NONE', #41033, #11748 ) ;
#24257=VECTOR ( 'NONE', #17579, 39.37007874015748143 ) ;
#24258=FACE_BOUND ( 'NONE', #21688, .T. ) ;
#24259=ORIENTED_EDGE ( 'NONE', *, *, #5359, .T. ) ;
#24260=CARTESIAN_POINT ( 'NONE',  ( 1.833433833923351353, 3.346456692913386100, -0.8267716535433055070 ) ) ;
#24261=EDGE_LOOP ( 'NONE', ( #7146, #9838, #29843, #37739 ) ) ;
#24262=CARTESIAN_POINT ( 'NONE',  ( -1.057143431661240696, 3.346456692913386100, 1.889763779527550147 ) ) ;
#24263=DIRECTION ( 'NONE',  ( -3.469446951953613696E-16, 0.000000000000000000, -1.000000000000000000 ) ) ;
#24264=EDGE_CURVE ( 'NONE', #37147, #6991, #38479, .T. ) ;
#24268=ORIENTED_EDGE ( 'NONE', *, *, #48835, .F. ) ;
#24269=LINE ( 'NONE', #15744, #7840 ) ;
#24270=CARTESIAN_POINT ( 'NONE',  ( -0.5455278134075214336, 3.346456692913386100, -1.259842519685035134 ) ) ;
#24271=CARTESIAN_POINT ( 'NONE',  ( -1.636583440222563635, 0.000000000000000000, 0.9448818897637749625 ) ) ;
#24274=CARTESIAN_POINT ( 'NONE',  ( 0.4696143004045479352, 0.000000000000000000, 0.7874015748031454320 ) ) ;
#24275=ORIENTED_EDGE ( 'NONE', *, *, #42920, .T. ) ;
#24277=AXIS2_PLACEMENT_3D ( 'NONE', #10137, #9117, #28982 ) ;
#24278=ORIENTED_EDGE ( 'NONE', *, *, #11699, .T. ) ;
#24280=EDGE_CURVE ( 'NONE', #26280, #22951, #6723, .T. ) ;
#24281=B_SPLINE_CURVE_WITH_KNOTS ( 'NONE', 3,
 ( #11578, #38455, #42812, #38703 ),
 .UNSPECIFIED., .F., .F.,
 ( 4, 4 ),
 ( 0.05135061866764987354, 0.05233018460755119172 ),
 .UNSPECIFIED. ) ;
#24282=VECTOR ( 'NONE', #23991, 39.37007874015748143 ) ;
#24286=LINE ( 'NONE', #16542, #40658 ) ;
#24289=CARTESIAN_POINT ( 'NONE',  ( -0.8942052331142552601, 3.346456692913386100, -1.574803149606293529 ) ) ;
#24290=EDGE_CURVE ( 'NONE', #37439, #14063, #19090, .T. ) ;
#24291=VERTEX_POINT ( 'NONE', #14976 ) ;
#24293=AXIS2_PLACEMENT_3D ( 'NONE', #34981, #3484, #15358 ) ;
#24297=CARTESIAN_POINT ( 'NONE',  ( 1.833433833923351353, 0.000000000000000000, 0.3149606299212576177 ) ) ;
#24298=ORIENTED_EDGE ( 'NONE', *, *, #26732, .F. ) ;
#24300=DIRECTION ( 'NONE',  ( -1.000000000000000000, 0.000000000000000000, 1.734723475976806848E-16 ) ) ;
#24301=DIRECTION ( 'NONE',  ( -0.000000000000000000, 0.000000000000000000, 1.000000000000000000 ) ) ;
#24303=DIRECTION ( 'NONE',  ( 1.000000000000000000, 0.000000000000000000, 0.000000000000000000 ) ) ;
#24304=ORIENTED_EDGE ( 'NONE', *, *, #3133, .F. ) ;
#24305=DIRECTION ( 'NONE',  ( -0.000000000000000000, 0.000000000000000000, 1.000000000000000000 ) ) ;
#24307=ORIENTED_EDGE ( 'NONE', *, *, #6413, .F. ) ;
#24309=CARTESIAN_POINT ( 'NONE',  ( 1.909347346926324684, 0.000000000000000000, -0.1574803149606304187 ) ) ;
#24311=EDGE_LOOP ( 'NONE', ( #12434, #39719, #6559, #6784 ) ) ;
#24313=VERTEX_POINT ( 'NONE', #18341 ) ;
#24314=VECTOR ( 'NONE', #50329, 39.37007874015748143 ) ;
#24315=CARTESIAN_POINT ( 'NONE',  ( 1.833433833923351353, 3.267716535433071279, 0.9448818897637746295 ) ) ;
#24317=DIRECTION ( 'NONE',  ( 0.000000000000000000, 0.000000000000000000, 1.000000000000000000 ) ) ;
#24318=VECTOR ( 'NONE', #28758, 39.37007874015748143 ) ;
#24319=VERTEX_POINT ( 'NONE', #7234 ) ;
#24321=CARTESIAN_POINT ( 'NONE',  ( 0.2727639067037602172, 0.000000000000000000, -1.929133858267710000 ) ) ;
#24322=CARTESIAN_POINT ( 'NONE',  ( 1.833433833923351353, 3.346456692913386100, -1.259842519685035800 ) ) ;
#24324=EDGE_CURVE ( 'NONE', #10381, #47342, #14210, .T. ) ;
#24325=ORIENTED_EDGE ( 'NONE', *, *, #27689, .F. ) ;
#24327=VECTOR ( 'NONE', #4069, 39.37007874015748143 ) ;
#24328=CARTESIAN_POINT ( 'NONE',  ( 0.4696143004045478797, 0.000000000000000000, -1.614173228346451605 ) ) ;
#24329=EDGE_CURVE ( 'NONE', #16368, #35037, #14723, .T. ) ;
#24331=EDGE_LOOP ( 'NONE', ( #11953, #50382, #9420, #464 ) ) ;
#24332=CARTESIAN_POINT ( 'NONE',  ( -2.182111253630085290, 0.000000000000000000, -6.146657985744592735E-16 ) ) ;
#24333=FACE_OUTER_BOUND ( 'NONE', #23058, .T. ) ;
#24338=CARTESIAN_POINT ( 'NONE',  ( -0.3486774197067340486, 0.000000000000000000, 2.007874015748021268 ) ) ;
#24339=DIRECTION ( 'NONE',  ( -1.000000000000000000, 0.000000000000000000, -0.000000000000000000 ) ) ;
#24340=ORIENTED_EDGE ( 'NONE', *, *, #28978, .T. ) ;
#24343=ORIENTED_EDGE ( 'NONE', *, *, #24843, .T. ) ;
#24344=CARTESIAN_POINT ( 'NONE',  ( 4.268512490100411402E-16, 3.267716535433071279, 2.204724409448808764 ) ) ;
#24345=ORIENTED_EDGE ( 'NONE', *, *, #43319, .T. ) ;
#24347=DIRECTION ( 'NONE',  ( 1.000000000000000000, 0.000000000000000000, -3.469446951953613696E-16 ) ) ;
#24349=EDGE_CURVE ( 'NONE', #45498, #34106, #49788, .T. ) ;
#24350=DIRECTION ( 'NONE',  ( -3.469446951953613696E-16, 0.000000000000000000, -1.000000000000000000 ) ) ;
#24351=LINE ( 'NONE', #8858, #20558 ) ;
#24352=ORIENTED_EDGE ( 'NONE', *, *, #12283, .F. ) ;
#24353=ORIENTED_EDGE ( 'NONE', *, *, #28499, .F. ) ;
#24355=EDGE_CURVE ( 'NONE', #5323, #47624, #10845, .T. ) ;
#24356=DIRECTION ( 'NONE',  ( -0.000000000000000000, 0.000000000000000000, 1.000000000000000000 ) ) ;
#24357=EDGE_LOOP ( 'NONE', ( #4262, #4407, #18946, #15541 ) ) ;
#24362=PLANE ( 'NONE',  #49706 ) ;
#24364=CARTESIAN_POINT ( 'NONE',  ( 0.8182917201112819283, 3.267716535433071279, 0.4724409448818868706 ) ) ;
#24365=CIRCLE ( 'NONE', #35054, 2.165354330708661568 ) ;
#24366=ORIENTED_EDGE ( 'NONE', *, *, #43620, .T. ) ;
#24367=FACE_OUTER_BOUND ( 'NONE', #50883, .T. ) ;
#24368=EDGE_CURVE ( 'NONE', #17591, #4242, #40997, .T. ) ;
#24371=PLANE ( 'NONE',  #33152 ) ;
#24373=LINE ( 'NONE', #20231, #22203 ) ;
#24374=VERTEX_POINT ( 'NONE', #21878 ) ;
#24375=CARTESIAN_POINT ( 'NONE',  ( -1.091055626815042645, 3.267716535433071279, 2.007874015748021268 ) ) ;
#24377=LINE ( 'NONE', #15853, #50566 ) ;
#24378=ORIENTED_EDGE ( 'NONE', *, *, #26336, .T. ) ;
#24379=CARTESIAN_POINT ( 'NONE',  ( -1.439733046521776583, 3.346456692913386100, -1.574803149606293307 ) ) ;
#24380=FACE_OUTER_BOUND ( 'NONE', #41241, .T. ) ;
#24381=ORIENTED_EDGE ( 'NONE', *, *, #14574, .T. ) ;
#24383=FACE_OUTER_BOUND ( 'NONE', #4072, .T. ) ;
#24384=DIRECTION ( 'NONE',  ( -0.000000000000000000, 1.000000000000000000, -0.000000000000000000 ) ) ;
#24386=ORIENTED_EDGE ( 'NONE', *, *, #13321, .F. ) ;
#24387=ORIENTED_EDGE ( 'NONE', *, *, #30848, .T. ) ;
#24388=CARTESIAN_POINT ( 'NONE',  ( 0.7423782071083085965, 3.267716535433071279, -0.8267716535433055070 ) ) ;
#24389=VECTOR ( 'NONE', #36313, 39.37007874015748143 ) ;
#24392=VECTOR ( 'NONE', #50663, 39.37007874015748143 ) ;
#24393=VERTEX_POINT ( 'NONE', #29363 ) ;
#24394=DIRECTION ( 'NONE',  ( -0.000000000000000000, 1.000000000000000000, -0.000000000000000000 ) ) ;
#24395=DIRECTION ( 'NONE',  ( -1.000000000000000000, 0.000000000000000000, -0.000000000000000000 ) ) ;
#24397=AXIS2_PLACEMENT_3D ( 'NONE', #47451, #8512, #16519 ) ;
#24398=EDGE_CURVE ( 'NONE', #13922, #22651, #18252, .T. ) ;
#24399=LINE ( 'NONE', #28005, #3349 ) ;
#24401=ORIENTED_EDGE ( 'NONE', *, *, #24171, .F. ) ;
#24402=EDGE_CURVE ( 'NONE', #9083, #44588, #10254, .T. ) ;
#24404=CARTESIAN_POINT ( 'NONE',  ( -1.712496953225537633, 0.000000000000000000, 1.220472440944875059 ) ) ;
#24405=VECTOR ( 'NONE', #17868, 39.37007874015748143 ) ;
#24406=CARTESIAN_POINT ( 'NONE',  ( -2.182111253630085290, 3.267716535433071279, 0.7480314960629874665 ) ) ;
#24407=ADVANCED_FACE ( 'NONE', ( #33252 ), #18001, .F. ) ;
#24408=DIRECTION ( 'NONE',  ( -1.000000000000000000, 0.000000000000000000, 0.000000000000000000 ) ) ;
#24409=FACE_BOUND ( 'NONE', #44573, .T. ) ;
#24410=VERTEX_POINT ( 'NONE', #2515 ) ;
#24411=CARTESIAN_POINT ( 'NONE',  ( 1.560669927219590303, 3.346456692913386100, -1.732283464566923170 ) ) ;
#24413=VERTEX_POINT ( 'NONE', #5362 ) ;
#24415=EDGE_CURVE ( 'NONE', #37842, #26630, #26086, .T. ) ;
#24416=VERTEX_POINT ( 'NONE', #49447 ) ;
#24417=ORIENTED_EDGE ( 'NONE', *, *, #35349, .T. ) ;
#24418=CARTESIAN_POINT ( 'NONE',  ( 1.287906020515830141, 3.346456692913386100, 1.062992125984246083 ) ) ;
#24421=PLANE ( 'NONE',  #2361 ) ;
#24422=CARTESIAN_POINT ( 'NONE',  ( 0.5455278134075211005, 0.000000000000000000, -0.1968503937007880511 ) ) ;
#24423=CARTESIAN_POINT ( 'NONE',  ( 1.636583440222563857, 3.267716535433071279, 0.3149606299212576177 ) ) ;
#24426=EDGE_CURVE ( 'NONE', #4117, #27908, #22135, .T. ) ;
#24431=VECTOR ( 'NONE', #14468, 39.37007874015748143 ) ;
#24432=ORIENTED_EDGE ( 'NONE', *, *, #41077, .F. ) ;
#24433=CARTESIAN_POINT ( 'NONE',  ( 0.000000000000000000, 3.267716535433071279, 0.000000000000000000 ) ) ;
#24434=AXIS2_PLACEMENT_3D ( 'NONE', #23649, #19767, #35530 ) ;
#24435=CARTESIAN_POINT ( 'NONE',  ( -1.909347346926324906, 3.267716535433071279, -0.7874015748031470974 ) ) ;
#24437=DIRECTION ( 'NONE',  ( -3.469446951953613696E-16, 0.000000000000000000, -1.000000000000000000 ) ) ;
#24438=VERTEX_POINT ( 'NONE', #49698 ) ;
#24439=DIRECTION ( 'NONE',  ( 1.000000000000000000, -0.000000000000000000, 0.000000000000000000 ) ) ;
#24440=DIRECTION ( 'NONE',  ( 1.734723475976806848E-16, 0.000000000000000000, 1.000000000000000000 ) ) ;
#24441=ORIENTED_EDGE ( 'NONE', *, *, #22909, .F. ) ;
#24442=DIRECTION ( 'NONE',  ( 0.000000000000000000, 0.000000000000000000, 1.000000000000000000 ) ) ;
#24443=VECTOR ( 'NONE', #26033, 39.37007874015748143 ) ;
#24445=CARTESIAN_POINT ( 'NONE',  ( 0.000000000000000000, 3.267716535433071279, -0.5118110236220465570 ) ) ;
#24446=VECTOR ( 'NONE', #34746, 39.37007874015748143 ) ;
#24447=EDGE_CURVE ( 'NONE', #11420, #40469, #26002, .T. ) ;
#24448=ORIENTED_EDGE ( 'NONE', *, *, #35626, .T. ) ;
#24454=CARTESIAN_POINT ( 'NONE',  ( -1.091055626815042645, 0.000000000000000000, -7.512581982576723358E-16 ) ) ;
#24455=LINE ( 'NONE', #953, #1227 ) ;
#24456=VERTEX_POINT ( 'NONE', #9750 ) ;
#24457=VERTEX_POINT ( 'NONE', #14382 ) ;
#24458=DIRECTION ( 'NONE',  ( 1.734723475976806848E-16, -0.000000000000000000, 1.000000000000000000 ) ) ;
#24461=ORIENTED_EDGE ( 'NONE', *, *, #20476, .F. ) ;
#24462=EDGE_CURVE ( 'NONE', #16283, #25223, #45047, .T. ) ;
#24463=CARTESIAN_POINT ( 'NONE',  ( -0.07591351300297340121, 3.346456692913386100, -1.614173228346451605 ) ) ;
#24464=ORIENTED_EDGE ( 'NONE', *, *, #40019, .T. ) ;
#24465=PLANE ( 'NONE',  #49630 ) ;
#24466=VECTOR ( 'NONE', #1196, 39.37007874015748143 ) ;
#24467=EDGE_CURVE ( 'NONE', #28095, #41852, #37892, .T. ) ;
#24468=CARTESIAN_POINT ( 'NONE',  ( -1.363819533518803473, 0.000000000000000000, -0.7874015748031470974 ) ) ;
#24469=AXIS2_PLACEMENT_3D ( 'NONE', #15714, #19576, #11087 ) ;
#24472=CARTESIAN_POINT ( 'NONE',  ( -1.057143431661237143, 3.346456692913386100, -1.889763779527552146 ) ) ;
#24474=CARTESIAN_POINT ( 'NONE',  ( 1.560669927219590303, 3.186757942779276043, -1.929133858267710666 ) ) ;
#24475=AXIS2_PLACEMENT_3D ( 'NONE', #50571, #10127, #2636 ) ;
#24476=EDGE_LOOP ( 'NONE', ( #44691, #4621, #25117, #25969 ) ) ;
#24477=VERTEX_POINT ( 'NONE', #37124 ) ;
#24479=VECTOR ( 'NONE', #23818, 39.37007874015748143 ) ;
#24481=PLANE ( 'NONE',  #50106 ) ;
#24484=CARTESIAN_POINT ( 'NONE',  ( 0.000000000000000000, 3.267716535433071279, 0.2755905511810994302 ) ) ;
#24485=EDGE_CURVE ( 'NONE', #41751, #30226, #45342, .T. ) ;
#24487=ORIENTED_EDGE ( 'NONE', *, *, #44790, .T. ) ;
#24491=LINE ( 'NONE', #32503, #9291 ) ;
#24493=CARTESIAN_POINT ( 'NONE',  ( 1.091055626815042423, 0.000000000000000000, -1.889763779527552368 ) ) ;
#24494=EDGE_CURVE ( 'NONE', #43929, #11186, #17245, .T. ) ;
#24498=ORIENTED_EDGE ( 'NONE', *, *, #47676, .T. ) ;
#24500=DIRECTION ( 'NONE',  ( -3.469446951953613696E-16, 0.000000000000000000, -1.000000000000000000 ) ) ;
#24501=ORIENTED_EDGE ( 'NONE', *, *, #4840, .T. ) ;
#24502=AXIS2_PLACEMENT_3D ( 'NONE', #37847, #41448, #33206 ) ;
#24503=LINE ( 'NONE', #5647, #27559 ) ;
#24505=ORIENTED_EDGE ( 'NONE', *, *, #31235, .T. ) ;
#24506=EDGE_CURVE ( 'NONE', #49034, #39073, #49199, .T. ) ;
#24507=CARTESIAN_POINT ( 'NONE',  ( -1.439733046521777027, 3.267716535433071279, -0.8267716535433052849 ) ) ;
#24508=FACE_OUTER_BOUND ( 'NONE', #35170, .T. ) ;
#24511=VERTEX_POINT ( 'NONE', #30387 ) ;
#24512=CARTESIAN_POINT ( 'NONE',  ( 1.560669927219591191, 0.000000000000000000, 1.535433070866133898 ) ) ;
#24514=EDGE_LOOP ( 'NONE', ( #40086, #445, #42790, #44939 ) ) ;
#24515=FACE_OUTER_BOUND ( 'NONE', #34122, .T. ) ;
#24516=VECTOR ( 'NONE', #35599, 39.37007874015748143 ) ;
#24517=ORIENTED_EDGE ( 'NONE', *, *, #47048, .F. ) ;
#24518=EDGE_CURVE ( 'NONE', #29198, #10488, #15138, .T. ) ;
#24519=CARTESIAN_POINT ( 'NONE',  ( -1.536664496436148184E-16, 0.000000000000000000, -0.5118110236220465570 ) ) ;
#24520=CARTESIAN_POINT ( 'NONE',  ( 0.000000000000000000, 3.267716535433071279, -2.086614173228339641 ) ) ;
#24521=EDGE_CURVE ( 'NONE', #23541, #30890, #49951, .T. ) ;
#24522=LINE ( 'NONE', #1022, #18120 ) ;
#24523=ORIENTED_EDGE ( 'NONE', *, *, #29468, .F. ) ;
#24524=ORIENTED_EDGE ( 'NONE', *, *, #24231, .F. ) ;
#24525=DIRECTION ( 'NONE',  ( 0.000000000000000000, 0.000000000000000000, -1.000000000000000000 ) ) ;
#24527=FACE_BOUND ( 'NONE', #23692, .T. ) ;
#24528=LINE ( 'NONE', #11876, #45152 ) ;
#24530=VECTOR ( 'NONE', #20712, 39.37007874015748143 ) ;
#24531=VECTOR ( 'NONE', #37728, 39.37007874015748143 ) ;
#24534=ORIENTED_EDGE ( 'NONE', *, *, #14625, .F. ) ;
#24536=ORIENTED_EDGE ( 'NONE', *, *, #37744, .F. ) ;
#24540=FACE_OUTER_BOUND ( 'NONE', #36196, .T. ) ;
#24544=FACE_OUTER_BOUND ( 'NONE', #26967, .T. ) ;
#24546=VECTOR ( 'NONE', #50158, 39.37007874015748143 ) ;
#24547=CARTESIAN_POINT ( 'NONE',  ( 0.8182917201112819283, 0.000000000000000000, 0.1574803149606286423 ) ) ;
#24548=DIRECTION ( 'NONE',  ( 1.734723475976806848E-16, 0.000000000000000000, 1.000000000000000000 ) ) ;
#24549=EDGE_CURVE ( 'NONE', #25449, #7908, #7147, .T. ) ;
#24550=CARTESIAN_POINT ( 'NONE',  ( 1.091055626815042645, 3.346456692913386100, -0.5118110236220471121 ) ) ;
#24551=EDGE_CURVE ( 'NONE', #7984, #18957, #15395, .T. ) ;
#24553=CARTESIAN_POINT ( 'NONE',  ( 1.091055626815042645, 0.000000000000000000, -0.3149606299212596716 ) ) ;
#24554=EDGE_CURVE ( 'NONE', #34698, #26534, #3775, .T. ) ;
#24556=VERTEX_POINT ( 'NONE', #14640 ) ;
#24558=ORIENTED_EDGE ( 'NONE', *, *, #10913, .T. ) ;
#24560=DIRECTION ( 'NONE',  ( 1.000000000000000000, 0.000000000000000000, 0.000000000000000000 ) ) ;
#24561=LINE ( 'NONE', #43401, #8866 ) ;
#24564=ORIENTED_EDGE ( 'NONE', *, *, #21707, .T. ) ;
#24565=VECTOR ( 'NONE', #50229, 39.37007874015748143 ) ;
#24566=ORIENTED_EDGE ( 'NONE', *, *, #27329, .T. ) ;
#24567=DIRECTION ( 'NONE',  ( -1.000000000000000000, 0.000000000000000000, 0.000000000000000000 ) ) ;
#24568=VECTOR ( 'NONE', #38941, 39.37007874015748143 ) ;
#24571=CARTESIAN_POINT ( 'NONE',  ( -0.8182917201112814842, 3.346456692913386100, 1.417322834645662777 ) ) ;
#24573=VECTOR ( 'NONE', #15994, 39.37007874015748143 ) ;
#24574=CARTESIAN_POINT ( 'NONE',  ( -1.794796351285541602, 3.346456692913386100, -1.102362204724405492 ) ) ;
#24575=EDGE_CURVE ( 'NONE', #24669, #47335, #50202, .T. ) ;
#24576=PLANE ( 'NONE',  #37127 ) ;
#24577=CARTESIAN_POINT ( 'NONE',  ( 0.000000000000000000, 3.267716535433071279, 2.007874015748021268 ) ) ;
#24579=VECTOR ( 'NONE', #37951, 39.37007874015748143 ) ;
#24580=ORIENTED_EDGE ( 'NONE', *, *, #17903, .T. ) ;
#24581=ORIENTED_EDGE ( 'NONE', *, *, #3123, .T. ) ;
#24583=DIRECTION ( 'NONE',  ( -3.469446951953613696E-16, 0.000000000000000000, -1.000000000000000000 ) ) ;
#24584=EDGE_CURVE ( 'NONE', #337, #30787, #18514, .T. ) ;
#24585=EDGE_CURVE ( 'NONE', #5165, #47515, #3017, .T. ) ;
#24586=ORIENTED_EDGE ( 'NONE', *, *, #43404, .F. ) ;
#24588=DIRECTION ( 'NONE',  ( -0.000000000000000000, 1.000000000000000000, -0.000000000000000000 ) ) ;
#24589=LINE ( 'NONE', #319, #2991 ) ;
#24590=CARTESIAN_POINT ( 'NONE',  ( -0.8182917201112819283, 3.346456692913386100, 2.004783788421104163 ) ) ;
#24592=EDGE_LOOP ( 'NONE', ( #23090, #25230, #2886, #1963 ) ) ;
#24593=CARTESIAN_POINT ( 'NONE',  ( -1.712496953225537411, 3.267716535433071279, 5.941417334598190051E-16 ) ) ;
#24595=CARTESIAN_POINT ( 'NONE',  ( -1.439733046521776361, 3.267716535433071279, 4.995077429881866871E-16 ) ) ;
#24597=CARTESIAN_POINT ( 'NONE',  ( 2.182111253630085290, 3.346456692913386100, 0.3149606299212573401 ) ) ;
#24600=LINE ( 'NONE', #4975, #30627 ) ;
#24601=ORIENTED_EDGE ( 'NONE', *, *, #4347, .T. ) ;
#24603=FACE_OUTER_BOUND ( 'NONE', #31635, .T. ) ;
#24604=LINE ( 'NONE', #32357, #6150 ) ;
#24605=DIRECTION ( 'NONE',  ( 1.000000000000000000, 0.000000000000000000, -3.469446951953613696E-16 ) ) ;
#24609=ORIENTED_EDGE ( 'NONE', *, *, #15467, .T. ) ;
#24610=ORIENTED_EDGE ( 'NONE', *, *, #39443, .F. ) ;
#24613=EDGE_LOOP ( 'NONE', ( #41664, #34475, #11476, #13605 ) ) ;
#24614=FACE_OUTER_BOUND ( 'NONE', #10810, .T. ) ;
#24616=VECTOR ( 'NONE', #19546, 39.37007874015748143 ) ;
#24617=VECTOR ( 'NONE', #30388, 39.37007874015748143 ) ;
#24620=CARTESIAN_POINT ( 'NONE',  ( 0.000000000000000000, 3.267716535433071279, -1.102362204724405492 ) ) ;
#24622=ORIENTED_EDGE ( 'NONE', *, *, #14913, .T. ) ;
#24623=ADVANCED_FACE ( 'NONE', ( #34519 ), #3265, .F. ) ;
#24625=VECTOR ( 'NONE', #37597, 39.37007874015748143 ) ;
#24627=EDGE_CURVE ( 'NONE', #34259, #8195, #22889, .T. ) ;
#24628=VERTEX_POINT ( 'NONE', #11270 ) ;
#24629=CARTESIAN_POINT ( 'NONE',  ( -1.636583440222564301, 0.000000000000000000, -1.259842519685034468 ) ) ;
#24630=VECTOR ( 'NONE', #30136, 39.37007874015748143 ) ;
#24631=CARTESIAN_POINT ( 'NONE',  ( -1.439733046521777027, 3.267716535433071279, -1.141732283464563791 ) ) ;
#24632=LINE ( 'NONE', #44738, #50186 ) ;
#24633=VERTEX_POINT ( 'NONE', #23136 ) ;
#24634=PLANE ( 'NONE',  #35830 ) ;
#24637=ORIENTED_EDGE ( 'NONE', *, *, #46121, .F. ) ;
#24638=CARTESIAN_POINT ( 'NONE',  ( 0.2727639067037609943, 3.346456692913386100, 0.9055118110236167750 ) ) ;
#24640=LINE ( 'NONE', #36516, #34863 ) ;
#24642=FACE_OUTER_BOUND ( 'NONE', #7580, .T. ) ;
#24643=LINE ( 'NONE', #20511, #32590 ) ;
#24644=EDGE_CURVE ( 'NONE', #23774, #12300, #35020, .T. ) ;
#24645=DIRECTION ( 'NONE',  ( -0.000000000000000000, 1.000000000000000000, -0.000000000000000000 ) ) ;
#24647=AXIS2_PLACEMENT_3D ( 'NONE', #9923, #13797, #48098 ) ;
#24648=VERTEX_POINT ( 'NONE', #46851 ) ;
#24649=ORIENTED_EDGE ( 'NONE', *, *, #26104, .F. ) ;
#24650=CARTESIAN_POINT ( 'NONE',  ( 1.363819533518803029, 3.346456692913386100, -1.929133858267710666 ) ) ;
#24651=CARTESIAN_POINT ( 'NONE',  ( 0.000000000000000000, 3.346456692913386100, 0.000000000000000000 ) ) ;
#24652=EDGE_CURVE ( 'NONE', #4557, #33393, #22710, .T. ) ;
#24656=CARTESIAN_POINT ( 'NONE',  ( 1.015142113812069091, 0.000000000000000000, -1.732283464566923614 ) ) ;
#24658=VECTOR ( 'NONE', #20456, 39.37007874015748143 ) ;
#24661=VERTEX_POINT ( 'NONE', #26824 ) ;
#24662=DIRECTION ( 'NONE',  ( -3.469446951953613696E-16, 0.000000000000000000, -1.000000000000000000 ) ) ;
#24663=DIRECTION ( 'NONE',  ( 1.000000000000000000, -0.000000000000000000, 0.000000000000000000 ) ) ;
#24664=LINE ( 'NONE', #40419, #8235 ) ;
#24665=ORIENTED_EDGE ( 'NONE', *, *, #36834, .F. ) ;
#24666=AXIS2_PLACEMENT_3D ( 'NONE', #6712, #2333, #22711 ) ;
#24668=FACE_BOUND ( 'NONE', #3621, .T. ) ;
#24669=VERTEX_POINT ( 'NONE', #39210 ) ;
#24671=EDGE_LOOP ( 'NONE', ( #20584, #32087, #11551 ) ) ;
#24672=ORIENTED_EDGE ( 'NONE', *, *, #41077, .T. ) ;
#24673=VECTOR ( 'NONE', #13521, 39.37007874015748143 ) ;
#24674=CARTESIAN_POINT ( 'NONE',  ( -0.8182917201112819283, 3.346456692913386100, -1.929133858267710000 ) ) ;
#24675=EDGE_LOOP ( 'NONE', ( #46896, #32300, #24432, #6650 ) ) ;
#24676=VERTEX_POINT ( 'NONE', #42576 ) ;
#24677=DIRECTION ( 'NONE',  ( -3.469446951953613696E-16, 0.000000000000000000, -1.000000000000000000 ) ) ;
#24680=FACE_OUTER_BOUND ( 'NONE', #26816, .T. ) ;
#24683=VECTOR ( 'NONE', #28439, 39.37007874015748143 ) ;
#24684=FACE_OUTER_BOUND ( 'NONE', #40429, .T. ) ;
#24687=DIRECTION ( 'NONE',  ( -0.000000000000000000, 1.000000000000000000, -0.000000000000000000 ) ) ;
#24688=DIRECTION ( 'NONE',  ( -3.469446951953613696E-16, 0.000000000000000000, -1.000000000000000000 ) ) ;
#24690=EDGE_CURVE ( 'NONE', #14887, #30087, #32743, .T. ) ;
#24691=DIRECTION ( 'NONE',  ( -1.000000000000000000, 0.000000000000000000, 1.734723475976806848E-16 ) ) ;
#24692=DIRECTION ( 'NONE',  ( 1.734723475976806848E-16, -0.000000000000000000, 1.000000000000000000 ) ) ;
#24695=VECTOR ( 'NONE', #31784, 39.37007874015748143 ) ;
#24697=PLANE ( 'NONE',  #11640 ) ;
#24698=CARTESIAN_POINT ( 'NONE',  ( 1.015142113812069091, 3.267716535433071279, -1.845530509571139399 ) ) ;
#24699=ORIENTED_EDGE ( 'NONE', *, *, #34991, .F. ) ;
#24701=EDGE_CURVE ( 'NONE', #40553, #33305, #14964, .T. ) ;
#24703=VECTOR ( 'NONE', #8378, 39.37007874015748143 ) ;
#24705=ORIENTED_EDGE ( 'NONE', *, *, #2436, .F. ) ;
#24706=DIRECTION ( 'NONE',  ( 1.000000000000000000, -0.000000000000000000, 0.000000000000000000 ) ) ;
#24707=AXIS2_PLACEMENT_3D ( 'NONE', #8383, #47323, #3299 ) ;
#24708=ORIENTED_EDGE ( 'NONE', *, *, #44934, .T. ) ;
#24709=FACE_BOUND ( 'NONE', #5725, .T. ) ;
#24712=EDGE_CURVE ( 'NONE', #12127, #3016, #19828, .T. ) ;
#24713=CARTESIAN_POINT ( 'NONE',  ( 1.833433833923351353, 3.267716535433071279, -0.8267716535433055070 ) ) ;
#24714=EDGE_LOOP ( 'NONE', ( #30202, #48304, #7892, #19104 ) ) ;
#24715=VERTEX_POINT ( 'NONE', #3849 ) ;
#24716=DIRECTION ( 'NONE',  ( 1.000000000000000000, 0.000000000000000000, 0.000000000000000000 ) ) ;
#24717=VERTEX_POINT ( 'NONE', #30712 ) ;
#24718=ADVANCED_FACE ( 'NONE', ( #50518 ), #27324, .F. ) ;
#24720=EDGE_LOOP ( 'NONE', ( #29342, #46221, #39857, #28198 ) ) ;
#24722=AXIS2_PLACEMENT_3D ( 'NONE', #41801, #6687, #33814 ) ;
#24723=ORIENTED_EDGE ( 'NONE', *, *, #19147, .T. ) ;
#24724=DIRECTION ( 'NONE',  ( 1.000000000000000000, 0.000000000000000000, 0.000000000000000000 ) ) ;
#24725=LINE ( 'NONE', #5860, #8313 ) ;
#24726=ORIENTED_EDGE ( 'NONE', *, *, #46607, .F. ) ;
#24728=DIRECTION ( 'NONE',  ( -0.000000000000000000, 1.000000000000000000, -0.000000000000000000 ) ) ;
#24730=ADVANCED_FACE ( 'NONE', ( #27579 ), #23715, .F. ) ;
#24731=VECTOR ( 'NONE', #40807, 39.37007874015748143 ) ;
#24733=ORIENTED_EDGE ( 'NONE', *, *, #19139, .F. ) ;
#24735=ORIENTED_EDGE ( 'NONE', *, *, #45061, .F. ) ;
#24736=VECTOR ( 'NONE', #38309, 39.37007874015748143 ) ;
#24739=CARTESIAN_POINT ( 'NONE',  ( 1.091055626815042423, 3.267716535433071279, -1.771653543307081691 ) ) ;
#24741=DIRECTION ( 'NONE',  ( -3.469446951953613696E-16, 0.000000000000000000, -1.000000000000000000 ) ) ;
#24743=LINE ( 'NONE', #44347, #2212 ) ;
#24744=LINE ( 'NONE', #28861, #13911 ) ;
#24745=LINE ( 'NONE', #43127, #5157 ) ;
#24746=DIRECTION ( 'NONE',  ( 1.734723475976806848E-16, -0.000000000000000000, 1.000000000000000000 ) ) ;
#24747=CARTESIAN_POINT ( 'NONE',  ( -0.07591351300297284610, 0.000000000000000000, 0.9055118110236167750 ) ) ;
#24748=DIRECTION ( 'NONE',  ( -3.469446951953613696E-16, 0.000000000000000000, -1.000000000000000000 ) ) ;
#24750=DIRECTION ( 'NONE',  ( -1.000000000000000000, 0.000000000000000000, 0.000000000000000000 ) ) ;
#24753=CARTESIAN_POINT ( 'NONE',  ( 0.4696143004045476577, 3.267716535433071279, -2.047244094488182231 ) ) ;
#24754=EDGE_CURVE ( 'NONE', #33477, #10560, #35598, .T. ) ;
#24761=LINE ( 'NONE', #28623, #14337 ) ;
#24762=VECTOR ( 'NONE', #10583, 39.37007874015748143 ) ;
#24763=CARTESIAN_POINT ( 'NONE',  ( -1.166969139818015755, 3.346456692913386100, 0.2755905511810996522 ) ) ;
#24765=DIRECTION ( 'NONE',  ( 1.734723475976806848E-16, -0.000000000000000000, 1.000000000000000000 ) ) ;
#24766=DIRECTION ( 'NONE',  ( 1.000000000000000000, 0.000000000000000000, -3.469446951953613696E-16 ) ) ;
#24767=ORIENTED_EDGE ( 'NONE', *, *, #43048, .T. ) ;
#24768=CARTESIAN_POINT ( 'NONE',  ( 0.000000000000000000, 3.346456692913386100, 0.000000000000000000 ) ) ;
#24770=VERTEX_POINT ( 'NONE', #50768 ) ;
#24771=DIRECTION ( 'NONE',  ( 1.000000000000000000, 0.000000000000000000, -3.469446951953613696E-16 ) ) ;
#24772=AXIS2_PLACEMENT_3D ( 'NONE', #12643, #45133, #5146 ) ;
#24774=LINE ( 'NONE', #24519, #22735 ) ;
#24776=EDGE_CURVE ( 'NONE', #8443, #42166, #15966, .T. ) ;
#24780=VERTEX_POINT ( 'NONE', #217 ) ;
#24781=CARTESIAN_POINT ( 'NONE',  ( 1.091055626815042645, 3.267716535433071279, 1.062992125984246083 ) ) ;
#24782=DIRECTION ( 'NONE',  ( -1.000000000000000000, 0.000000000000000000, -0.000000000000000000 ) ) ;
#24784=EDGE_CURVE ( 'NONE', #22488, #25289, #7970, .T. ) ;
#24786=CARTESIAN_POINT ( 'NONE',  ( 0.000000000000000000, 3.267716535433071279, -1.614173228346451605 ) ) ;
#24788=DIRECTION ( 'NONE',  ( 0.000000000000000000, 1.000000000000000000, 0.000000000000000000 ) ) ;
#24789=ADVANCED_FACE ( 'NONE', ( #7714 ), #15211, .F. ) ;
#24790=ORIENTED_EDGE ( 'NONE', *, *, #49081, .F. ) ;
#24793=EDGE_CURVE ( 'NONE', #43930, #35527, #11340, .T. ) ;
#24795=VECTOR ( 'NONE', #7779, 39.37007874015748143 ) ;
#24797=VECTOR ( 'NONE', #11298, 39.37007874015748143 ) ;
#24798=FACE_OUTER_BOUND ( 'NONE', #43847, .T. ) ;
#24799=DIRECTION ( 'NONE',  ( 1.000000000000000000, 0.000000000000000000, -3.469446951953613696E-16 ) ) ;
#24800=ORIENTED_EDGE ( 'NONE', *, *, #33174, .F. ) ;
#24801=ORIENTED_EDGE ( 'NONE', *, *, #34331, .F. ) ;
#24803=CARTESIAN_POINT ( 'NONE',  ( 0.4696143004045479352, 0.000000000000000000, -0.1574803149606298636 ) ) ;
#24804=LINE ( 'NONE', #1307, #4348 ) ;
#24807=CARTESIAN_POINT ( 'NONE',  ( 1.636583440222563857, 0.000000000000000000, 1.574803149606291974 ) ) ;
#24810=FACE_OUTER_BOUND ( 'NONE', #30130, .T. ) ;
#24811=EDGE_CURVE ( 'NONE', #27417, #34340, #740, .T. ) ;
#24812=EDGE_CURVE ( 'NONE', #30339, #13697, #27836, .T. ) ;
#24813=DIRECTION ( 'NONE',  ( -0.000000000000000000, 1.000000000000000000, -0.000000000000000000 ) ) ;
#24815=EDGE_CURVE ( 'NONE', #4171, #24715, #44093, .T. ) ;
#24816=CARTESIAN_POINT ( 'NONE',  ( 1.015142113812069313, 3.346456692913386100, 0.9055118110236164419 ) ) ;
#24818=ORIENTED_EDGE ( 'NONE', *, *, #50439, .T. ) ;
#24821=DIRECTION ( 'NONE',  ( 1.000000000000000000, 0.000000000000000000, 0.000000000000000000 ) ) ;
#24823=EDGE_LOOP ( 'NONE', ( #31970, #8523, #22202, #41422 ) ) ;
#24824=CARTESIAN_POINT ( 'NONE',  ( 1.833433833923351353, 0.000000000000000000, -0.5118110236220471121 ) ) ;
#24828=VECTOR ( 'NONE', #42825, 39.37007874015748143 ) ;
#24830=LINE ( 'NONE', #17595, #11533 ) ;
#24831=CIRCLE ( 'NONE', #46248, 2.106299212598425008 ) ;
#24832=EDGE_CURVE ( 'NONE', #7771, #32210, #24743, .T. ) ;
#24833=ORIENTED_EDGE ( 'NONE', *, *, #29860, .T. ) ;
#24835=ORIENTED_EDGE ( 'NONE', *, *, #16986, .F. ) ;
#24837=DIRECTION ( 'NONE',  ( 0.000000000000000000, 1.000000000000000000, 0.000000000000000000 ) ) ;
#24838=ORIENTED_EDGE ( 'NONE', *, *, #3391, .F. ) ;
#24839=ORIENTED_EDGE ( 'NONE', *, *, #30041, .T. ) ;
#24842=LINE ( 'NONE', #8837, #32719 ) ;
#24843=EDGE_CURVE ( 'NONE', #1626, #26463, #23645, .T. ) ;
#24844=AXIS2_PLACEMENT_3D ( 'NONE', #21073, #29060, #36828 ) ;
#24845=VERTEX_POINT ( 'NONE', #20865 ) ;
#24848=DIRECTION ( 'NONE',  ( -0.000000000000000000, 1.000000000000000000, -0.000000000000000000 ) ) ;
#24849=CARTESIAN_POINT ( 'NONE',  ( 0.8182917201112819283, 3.346456692913386100, -0.6692913385826764205 ) ) ;
#24850=EDGE_CURVE ( 'NONE', #15713, #4024, #36878, .T. ) ;
#24852=FACE_OUTER_BOUND ( 'NONE', #25442, .T. ) ;
#24853=LINE ( 'NONE', #36733, #6270 ) ;
#24855=ORIENTED_EDGE ( 'NONE', *, *, #34924, .T. ) ;
#24856=VERTEX_POINT ( 'NONE', #1499 ) ;
#24858=CARTESIAN_POINT ( 'NONE',  ( -1.195183497228115035E-16, 3.346456692913386100, -1.574803149606293529 ) ) ;
#24860=EDGE_CURVE ( 'NONE', #4326, #28186, #39722, .T. ) ;
#24861=DIRECTION ( 'NONE',  ( -1.000000000000000000, 0.000000000000000000, 1.734723475976806848E-16 ) ) ;
#24862=VERTEX_POINT ( 'NONE', #4356 ) ;
#24863=VERTEX_POINT ( 'NONE', #4867 ) ;
#24866=VERTEX_POINT ( 'NONE', #31724 ) ;
#24867=LINE ( 'NONE', #33644, #26598 ) ;
#24868=DIRECTION ( 'NONE',  ( -1.000000000000000000, 0.000000000000000000, 0.000000000000000000 ) ) ;
#24869=VECTOR ( 'NONE', #27523, 39.37007874015748143 ) ;
#24870=ADVANCED_FACE ( 'NONE', ( #36109 ), #16489, .F. ) ;
#24874=DIRECTION ( 'NONE',  ( 1.000000000000000000, 0.000000000000000000, 0.000000000000000000 ) ) ;
#24875=VECTOR ( 'NONE', #7622, 39.37007874015748143 ) ;
#24877=ORIENTED_EDGE ( 'NONE', *, *, #369, .T. ) ;
#24878=LINE ( 'NONE', #40627, #10187 ) ;
#24880=AXIS2_PLACEMENT_3D ( 'NONE', #50008, #14434, #6943 ) ;
#24881=CARTESIAN_POINT ( 'NONE',  ( -0.6214413264104945434, 0.000000000000000000, -1.614173228346451605 ) ) ;
#24882=ORIENTED_EDGE ( 'NONE', *, *, #25629, .F. ) ;
#24883=VECTOR ( 'NONE', #42392, 39.37007874015748143 ) ;
#24884=DIRECTION ( 'NONE',  ( -1.000000000000000000, 0.000000000000000000, 1.734723475976806848E-16 ) ) ;
#24886=DIRECTION ( 'NONE',  ( -1.000000000000000000, -0.000000000000000000, -0.000000000000000000 ) ) ;
#24888=DIRECTION ( 'NONE',  ( -3.469446951953613696E-16, 0.000000000000000000, -1.000000000000000000 ) ) ;
#24889=DIRECTION ( 'NONE',  ( -3.469446951953613696E-16, 0.000000000000000000, -1.000000000000000000 ) ) ;
#24892=DIRECTION ( 'NONE',  ( -3.469446951953613696E-16, 0.000000000000000000, -1.000000000000000000 ) ) ;
#24894=CARTESIAN_POINT ( 'NONE',  ( 1.091055626815042645, 3.267716535433071279, -1.141732283464564013 ) ) ;
#24896=DIRECTION ( 'NONE',  ( 1.734723475976806848E-16, -0.000000000000000000, 1.000000000000000000 ) ) ;
#24898=DIRECTION ( 'NONE',  ( -1.000000000000000000, 0.000000000000000000, -0.000000000000000000 ) ) ;
#24899=ORIENTED_EDGE ( 'NONE', *, *, #6485, .T. ) ;
#24901=DIRECTION ( 'NONE',  ( -3.469446951953613696E-16, 0.000000000000000000, -1.000000000000000000 ) ) ;
#24902=CARTESIAN_POINT ( 'NONE',  ( -1.439733046521776583, 3.346456692913386100, -1.259842519685034468 ) ) ;
#24904=CARTESIAN_POINT ( 'NONE',  ( -0.8182917201112814842, 0.000000000000000000, 1.102362204724404160 ) ) ;
#24905=CARTESIAN_POINT ( 'NONE',  ( 1.560669927219590747, 0.000000000000000000, -0.7874015748031473194 ) ) ;
#24908=EDGE_LOOP ( 'NONE', ( #6920, #6299, #7186, #31904 ) ) ;
#24909=VECTOR ( 'NONE', #36475, 39.37007874015748143 ) ;
#24911=EDGE_CURVE ( 'NONE', #24416, #27748, #35183, .T. ) ;
#24913=LINE ( 'NONE', #48107, #29923 ) ;
#24914=CARTESIAN_POINT ( 'NONE',  ( -2.438548951736695170, 3.267716535433071279, 0.1574803149606286423 ) ) ;
#24915=ORIENTED_EDGE ( 'NONE', *, *, #45468, .F. ) ;
#24916=FACE_OUTER_BOUND ( 'NONE', #1930, .T. ) ;
#24917=EDGE_CURVE ( 'NONE', #9804, #49369, #1244, .T. ) ;
#24918=FACE_BOUND ( 'NONE', #32114, .T. ) ;
#24920=CARTESIAN_POINT ( 'NONE',  ( 0.000000000000000000, 3.267716535433071279, 0.000000000000000000 ) ) ;
#24921=ORIENTED_EDGE ( 'NONE', *, *, #46211, .F. ) ;
#24922=VECTOR ( 'NONE', #25419, 39.37007874015748143 ) ;
#24925=VECTOR ( 'NONE', #27024, 39.37007874015748143 ) ;
#24928=ORIENTED_EDGE ( 'NONE', *, *, #45299, .F. ) ;
#24929=EDGE_CURVE ( 'NONE', #49628, #9931, #28860, .T. ) ;
#24930=LINE ( 'NONE', #4800, #47645 ) ;
#24932=PLANE ( 'NONE',  #35817 ) ;
#24933=ADVANCED_FACE ( 'NONE', ( #2007 ), #13376, .F. ) ;
#24934=LINE ( 'NONE', #25190, #42081 ) ;
#24935=ADVANCED_FACE ( 'NONE', ( #37135 ), #29635, .F. ) ;
#24936=CARTESIAN_POINT ( 'NONE',  ( 2.105931235793975009, 3.346456692913386100, -0.03937007874015936021 ) ) ;
#24938=ORIENTED_EDGE ( 'NONE', *, *, #42275, .T. ) ;
#24940=EDGE_CURVE ( 'NONE', #33320, #42214, #7982, .T. ) ;
#24941=DIRECTION ( 'NONE',  ( -3.469446951953613696E-16, 0.000000000000000000, -1.000000000000000000 ) ) ;
#24942=ORIENTED_EDGE ( 'NONE', *, *, #39021, .F. ) ;
#24943=VECTOR ( 'NONE', #35896, 39.37007874015748143 ) ;
#24944=DIRECTION ( 'NONE',  ( -3.469446951953613696E-16, 0.000000000000000000, -1.000000000000000000 ) ) ;
#24945=LINE ( 'NONE', #4818, #5518 ) ;
#24946=VERTEX_POINT ( 'NONE', #48948 ) ;
#24948=DIRECTION ( 'NONE',  ( -0.000000000000000000, 0.000000000000000000, 1.000000000000000000 ) ) ;
#24949=LINE ( 'NONE', #17966, #34278 ) ;
#24951=VERTEX_POINT ( 'NONE', #38151 ) ;
#24953=CARTESIAN_POINT ( 'NONE',  ( 0.8182917201112824834, 3.346456692913386100, 2.047244094488179567 ) ) ;
#24954=ORIENTED_EDGE ( 'NONE', *, *, #23910, .F. ) ;
#24955=FACE_BOUND ( 'NONE', #19649, .T. ) ;
#24957=AXIS2_PLACEMENT_3D ( 'NONE', #34401, #42380, #22773 ) ;
#24959=CARTESIAN_POINT ( 'NONE',  ( -1.363819533518803029, 0.000000000000000000, -0.03937007874015868020 ) ) ;
#24960=CARTESIAN_POINT ( 'NONE',  ( 0.1968503937007870241, 3.346456692913386100, -1.889763779527552146 ) ) ;
#24961=ORIENTED_EDGE ( 'NONE', *, *, #46061, .T. ) ;
#24963=DIRECTION ( 'NONE',  ( -1.000000000000000000, -0.000000000000000000, -0.000000000000000000 ) ) ;
#24964=ORIENTED_EDGE ( 'NONE', *, *, #11187, .T. ) ;
#24965=DIRECTION ( 'NONE',  ( -1.000000000000000000, 0.000000000000000000, 1.734723475976806848E-16 ) ) ;
#24967=PLANE ( 'NONE',  #43762 ) ;
#24970=LINE ( 'NONE', #17235, #11626 ) ;
#24973=ADVANCED_FACE ( 'NONE', ( #10011 ), #41503, .F. ) ;
#24974=DIRECTION ( 'NONE',  ( -0.000000000000000000, 1.000000000000000000, -0.000000000000000000 ) ) ;
#24976=VERTEX_POINT ( 'NONE', #10261 ) ;
#24977=EDGE_CURVE ( 'NONE', #33927, #10658, #17257, .T. ) ;
#24980=ORIENTED_EDGE ( 'NONE', *, *, #31199, .T. ) ;
#24981=CARTESIAN_POINT ( 'NONE',  ( 0.000000000000000000, 3.267716535433071279, 0.000000000000000000 ) ) ;
#24982=DIRECTION ( 'NONE',  ( 0.000000000000000000, 0.000000000000000000, -1.000000000000000000 ) ) ;
#24984=ORIENTED_EDGE ( 'NONE', *, *, #12138, .T. ) ;
#24985=DIRECTION ( 'NONE',  ( 1.734723475976806848E-16, 0.000000000000000000, 1.000000000000000000 ) ) ;
#24986=ORIENTED_EDGE ( 'NONE', *, *, #17751, .T. ) ;
#24987=DIRECTION ( 'NONE',  ( -3.469446951953613696E-16, 0.000000000000000000, -1.000000000000000000 ) ) ;
#24990=VECTOR ( 'NONE', #28149, 39.37007874015748143 ) ;
#24992=CARTESIAN_POINT ( 'NONE',  ( 0.6363476328836782381, 3.346456692913386100, 2.007874015748021268 ) ) ;
#24993=ORIENTED_EDGE ( 'NONE', *, *, #3811, .T. ) ;
#24995=CARTESIAN_POINT ( 'NONE',  ( 1.287906020515830585, 3.346456692913386100, 1.574803149606291974 ) ) ;
#24996=VECTOR ( 'NONE', #45861, 39.37007874015748143 ) ;
#24997=DIRECTION ( 'NONE',  ( -3.469446951953613696E-16, 0.000000000000000000, -1.000000000000000000 ) ) ;
#24999=EDGE_CURVE ( 'NONE', #22693, #39559, #14389, .T. ) ;
#25000=DIRECTION ( 'NONE',  ( -0.000000000000000000, 1.000000000000000000, -0.000000000000000000 ) ) ;
#25001=DIRECTION ( 'NONE',  ( -0.000000000000000000, 1.000000000000000000, -0.000000000000000000 ) ) ;
#25007=CARTESIAN_POINT ( 'NONE',  ( -0.5455278134075214336, 0.000000000000000000, -0.6299212598425175669 ) ) ;
#25008=ORIENTED_EDGE ( 'NONE', *, *, #12964, .F. ) ;
#25010=DIRECTION ( 'NONE',  ( 0.000000000000000000, 1.000000000000000000, 0.000000000000000000 ) ) ;
#25011=DIRECTION ( 'NONE',  ( -1.000000000000000000, 0.000000000000000000, 1.734723475976806848E-16 ) ) ;
#25012=CARTESIAN_POINT ( 'NONE',  ( 0.5455278134075213226, 3.267716535433071279, -9.463399047163224412E-17 ) ) ;
#25013=LINE ( 'NONE', #40514, #48166 ) ;
#25016=DIRECTION ( 'NONE',  ( 1.734723475976806848E-16, -0.000000000000000000, 1.000000000000000000 ) ) ;
#25017=VECTOR ( 'NONE', #19365, 39.37007874015748143 ) ;
#25018=FACE_BOUND ( 'NONE', #12353, .T. ) ;
#25019=ORIENTED_EDGE ( 'NONE', *, *, #24119, .T. ) ;
#25022=ORIENTED_EDGE ( 'NONE', *, *, #36929, .F. ) ;
#25023=VECTOR ( 'NONE', #18991, 39.37007874015748143 ) ;
#25024=AXIS2_PLACEMENT_3D ( 'NONE', #34024, #2012, #29639 ) ;
#25025=LINE ( 'NONE', #36653, #46616 ) ;
#25026=DIRECTION ( 'NONE',  ( -1.000000000000000000, 0.000000000000000000, -0.000000000000000000 ) ) ;
#25027=DIRECTION ( 'NONE',  ( -0.000000000000000000, 1.000000000000000000, -0.000000000000000000 ) ) ;
#25032=ORIENTED_EDGE ( 'NONE', *, *, #6286, .F. ) ;
#25035=FACE_BOUND ( 'NONE', #25529, .T. ) ;
#25037=EDGE_CURVE ( 'NONE', #21877, #24313, #45599, .T. ) ;
#25039=LINE ( 'NONE', #33060, #11812 ) ;
#25040=EDGE_CURVE ( 'NONE', #35668, #10852, #22393, .T. ) ;
#25042=ORIENTED_EDGE ( 'NONE', *, *, #29651, .T. ) ;
#25043=LINE ( 'NONE', #29686, #6810 ) ;
#25045=ORIENTED_EDGE ( 'NONE', *, *, #35937, .T. ) ;
#25046=EDGE_LOOP ( 'NONE', ( #50543, #14816, #38178, #39039 ) ) ;
#25048=CARTESIAN_POINT ( 'NONE',  ( -1.195183497228115035E-16, 3.346456692913386100, -1.259842519685035134 ) ) ;
#25049=DIRECTION ( 'NONE',  ( 0.000000000000000000, 0.000000000000000000, 1.000000000000000000 ) ) ;
#25050=EDGE_CURVE ( 'NONE', #9761, #23674, #34020, .T. ) ;
#25051=DIRECTION ( 'NONE',  ( -0.000000000000000000, 1.000000000000000000, -0.000000000000000000 ) ) ;
#25053=ORIENTED_EDGE ( 'NONE', *, *, #28047, .T. ) ;
#25056=CARTESIAN_POINT ( 'NONE',  ( 1.833433833923351353, 3.267716535433071279, -0.6299212598425181220 ) ) ;
#25057=CARTESIAN_POINT ( 'NONE',  ( 1.287906020515830141, 0.000000000000000000, 0.6299212598425161236 ) ) ;
#25058=AXIS2_PLACEMENT_3D ( 'NONE', #40297, #16798, #32556 ) ;
#25059=CARTESIAN_POINT ( 'NONE',  ( 1.091055626815042645, 0.000000000000000000, -0.6299212598425181220 ) ) ;
#25061=VECTOR ( 'NONE', #20369, 39.37007874015748143 ) ;
#25062=CARTESIAN_POINT ( 'NONE',  ( 0.000000000000000000, 3.346456692913386100, 0.000000000000000000 ) ) ;
#25064=CARTESIAN_POINT ( 'NONE',  ( 1.833433833923351353, 0.000000000000000000, 1.259842519685033135 ) ) ;
#25065=AXIS2_PLACEMENT_3D ( 'NONE', #34902, #19641, #8290 ) ;
#25068=DIRECTION ( 'NONE',  ( 0.000000000000000000, 0.000000000000000000, -1.000000000000000000 ) ) ;
#25072=DIRECTION ( 'NONE',  ( 0.000000000000000000, 0.000000000000000000, -1.000000000000000000 ) ) ;
#25073=ORIENTED_EDGE ( 'NONE', *, *, #23006, .F. ) ;
#25075=ORIENTED_EDGE ( 'NONE', *, *, #49236, .T. ) ;
#25077=DIRECTION ( 'NONE',  ( 1.734723475976806848E-16, 0.000000000000000000, 1.000000000000000000 ) ) ;
#25079=ORIENTED_EDGE ( 'NONE', *, *, #47952, .F. ) ;
#25083=ORIENTED_EDGE ( 'NONE', *, *, #35626, .F. ) ;
#25085=DIRECTION ( 'NONE',  ( -1.000000000000000000, 0.000000000000000000, -0.000000000000000000 ) ) ;
#25086=LINE ( 'NONE', #5464, #21457 ) ;
#25088=ORIENTED_EDGE ( 'NONE', *, *, #23277, .T. ) ;
#25089=ORIENTED_EDGE ( 'NONE', *, *, #26663, .T. ) ;
#25090=PLANE ( 'NONE',  #35395 ) ;
#25091=VECTOR ( 'NONE', #27204, 39.37007874015748143 ) ;
#25093=ORIENTED_EDGE ( 'NONE', *, *, #10826, .T. ) ;
#25095=CARTESIAN_POINT ( 'NONE',  ( 0.8182917201112819283, 3.267716535433071279, 0.5905511811023579360 ) ) ;
#25096=CARTESIAN_POINT ( 'NONE',  ( 1.636583440222563857, 0.000000000000000000, -1.161035397307311917E-15 ) ) ;
#25097=CARTESIAN_POINT ( 'NONE',  ( 1.770012363201889594, 3.267716535433071279, -1.141732283464564013 ) ) ;
#25099=VECTOR ( 'NONE', #32725, 39.37007874015748143 ) ;
#25101=AXIS2_PLACEMENT_3D ( 'NONE', #12052, #43018, #35547 ) ;
#25103=CARTESIAN_POINT ( 'NONE',  ( 0.000000000000000000, 3.267716535433071279, -0.6299212598425177889 ) ) ;
#25105=DIRECTION ( 'NONE',  ( 1.734723475976806848E-16, -0.000000000000000000, 1.000000000000000000 ) ) ;
#25107=ORIENTED_EDGE ( 'NONE', *, *, #47196, .F. ) ;
#25108=PLANE ( 'NONE',  #38115 ) ;
#25109=CARTESIAN_POINT ( 'NONE',  ( -1.636583440222563635, 0.000000000000000000, 1.062992125984246083 ) ) ;
#25110=AXIS2_PLACEMENT_3D ( 'NONE', #25007, #37405, #16759 ) ;
#25111=PLANE ( 'NONE',  #13416 ) ;
#25113=ORIENTED_EDGE ( 'NONE', *, *, #24554, .T. ) ;
#25114=PLANE ( 'NONE',  #32182 ) ;
#25116=LINE ( 'NONE', #31854, #18899 ) ;
#25117=ORIENTED_EDGE ( 'NONE', *, *, #2663, .F. ) ;
#25118=ORIENTED_EDGE ( 'NONE', *, *, #3487, .F. ) ;
#25122=FACE_OUTER_BOUND ( 'NONE', #32038, .T. ) ;
#25123=EDGE_CURVE ( 'NONE', #10879, #12204, #18771, .T. ) ;
#25125=DIRECTION ( 'NONE',  ( -3.469446951953613696E-16, 0.000000000000000000, -1.000000000000000000 ) ) ;
#25127=VERTEX_POINT ( 'NONE', #27516 ) ;
#25129=LINE ( 'NONE', #40881, #34905 ) ;
#25130=VECTOR ( 'NONE', #40817, 39.37007874015748143 ) ;
#25131=LINE ( 'NONE', #49089, #16658 ) ;
#25132=EDGE_CURVE ( 'NONE', #25457, #41221, #19013, .T. ) ;
#25133=VECTOR ( 'NONE', #13024, 39.37007874015748143 ) ;
#25136=EDGE_CURVE ( 'NONE', #47240, #44618, #39148, .T. ) ;
#25139=ORIENTED_EDGE ( 'NONE', *, *, #3360, .T. ) ;
#25140=EDGE_CURVE ( 'NONE', #33320, #33364, #46359, .T. ) ;
#25142=PLANE ( 'NONE',  #18470 ) ;
#25144=ADVANCED_FACE ( 'NONE', ( #50454 ), #26761, .F. ) ;
#25145=ORIENTED_EDGE ( 'NONE', *, *, #39645, .F. ) ;
#25147=DIRECTION ( 'NONE',  ( -3.469446951953613696E-16, 0.000000000000000000, -1.000000000000000000 ) ) ;
#25148=ORIENTED_EDGE ( 'NONE', *, *, #11116, .F. ) ;
#25149=CARTESIAN_POINT ( 'NONE',  ( -1.091055626815042201, 0.000000000000000000, 0.7480314960629874665 ) ) ;
#25150=CARTESIAN_POINT ( 'NONE',  ( -0.2727639067037604392, 3.267716535433071279, 4.731699523581607892E-17 ) ) ;
#25151=DIRECTION ( 'NONE',  ( -0.000000000000000000, 0.000000000000000000, 1.000000000000000000 ) ) ;
#25152=FACE_OUTER_BOUND ( 'NONE', #38153, .T. ) ;
#25154=ORIENTED_EDGE ( 'NONE', *, *, #27, .T. ) ;
#25157=CARTESIAN_POINT ( 'NONE',  ( -1.636583440222564301, 3.346456692913386100, -1.141732283464563791 ) ) ;
#25158=EDGE_LOOP ( 'NONE', ( #46153, #38759, #24190, #22960 ) ) ;
#25160=CARTESIAN_POINT ( 'NONE',  ( 0.000000000000000000, 3.267716535433071279, 0.1574803149606280872 ) ) ;
#25162=ADVANCED_FACE ( 'NONE', ( #11280 ), #27008, .F. ) ;
#25163=CARTESIAN_POINT ( 'NONE',  ( 1.909347346926324684, 3.267716535433071279, -0.6692913385826764205 ) ) ;
#25164=VERTEX_POINT ( 'NONE', #15409 ) ;
#25165=ORIENTED_EDGE ( 'NONE', *, *, #44360, .T. ) ;
#25166=CARTESIAN_POINT ( 'NONE',  ( -1.166969139818015977, 0.000000000000000000, -0.4724409448818886470 ) ) ;
#25167=DIRECTION ( 'NONE',  ( -0.000000000000000000, 1.000000000000000000, -0.000000000000000000 ) ) ;
#25171=DIRECTION ( 'NONE',  ( 1.000000000000000000, 0.000000000000000000, 0.000000000000000000 ) ) ;
#25172=FACE_BOUND ( 'NONE', #34915, .T. ) ;
#25174=ORIENTED_EDGE ( 'NONE', *, *, #11037, .T. ) ;
#25176=CARTESIAN_POINT ( 'NONE',  ( 0.8182917201112817063, 3.346456692913386100, -1.614173228346451605 ) ) ;
#25178=VERTEX_POINT ( 'NONE', #23393 ) ;
#25179=ORIENTED_EDGE ( 'NONE', *, *, #49941, .T. ) ;
#25183=DIRECTION ( 'NONE',  ( 0.000000000000000000, 0.000000000000000000, 1.000000000000000000 ) ) ;
#25184=EDGE_CURVE ( 'NONE', #3567, #19884, #19518, .T. ) ;
#25188=DIRECTION ( 'NONE',  ( -0.000000000000000000, 1.000000000000000000, -0.000000000000000000 ) ) ;
#25189=CARTESIAN_POINT ( 'NONE',  ( 1.560669927219590747, 3.346456692913386100, 0.1574803149606283648 ) ) ;
#25190=CARTESIAN_POINT ( 'NONE',  ( 1.833433833923351353, 3.346456692913386100, 1.574803149606291974 ) ) ;
#25191=DIRECTION ( 'NONE',  ( 0.000000000000000000, 0.000000000000000000, -1.000000000000000000 ) ) ;
#25194=DIRECTION ( 'NONE',  ( 1.000000000000000000, 0.000000000000000000, 0.000000000000000000 ) ) ;
#25195=CARTESIAN_POINT ( 'NONE',  ( -1.363819533518803473, 0.000000000000000000, -0.4724409448818886470 ) ) ;
#25196=VERTEX_POINT ( 'NONE', #31405 ) ;
#25198=EDGE_CURVE ( 'NONE', #1172, #36221, #7905, .T. ) ;
#25199=LINE ( 'NONE', #40956, #40944 ) ;
#25200=VERTEX_POINT ( 'NONE', #15903 ) ;
#25201=LINE ( 'NONE', #13333, #7302 ) ;
#25202=EDGE_CURVE ( 'NONE', #22897, #536, #35536, .T. ) ;
#25208=VERTEX_POINT ( 'NONE', #20552 ) ;
#25209=FACE_OUTER_BOUND ( 'NONE', #46990, .T. ) ;
#25210=ORIENTED_EDGE ( 'NONE', *, *, #16667, .T. ) ;
#25211=FACE_BOUND ( 'NONE', #34861, .T. ) ;
#25212=VECTOR ( 'NONE', #26176, 39.37007874015748143 ) ;
#25216=CIRCLE ( 'NONE', #16150, 2.165354330708661568 ) ;
#25217=EDGE_LOOP ( 'NONE', ( #41885, #48991, #41439, #46502 ) ) ;
#25222=CARTESIAN_POINT ( 'NONE',  ( 0.5455278134075216556, 3.346456692913386100, 2.007874015748021268 ) ) ;
#25223=VERTEX_POINT ( 'NONE', #4044 ) ;
#25224=LINE ( 'NONE', #44571, #5013 ) ;
#25225=EDGE_CURVE ( 'NONE', #49076, #13566, #39404, .T. ) ;
#25226=VERTEX_POINT ( 'NONE', #36307 ) ;
#25227=PLANE ( 'NONE',  #23271 ) ;
#25228=EDGE_CURVE ( 'NONE', #15126, #29929, #30286, .T. ) ;
#25229=DIRECTION ( 'NONE',  ( 1.734723475976806848E-16, -0.000000000000000000, 1.000000000000000000 ) ) ;
#25230=ORIENTED_EDGE ( 'NONE', *, *, #42861, .T. ) ;
#25231=ADVANCED_FACE ( 'NONE', ( #20287 ), #8424, .F. ) ;
#25232=LINE ( 'NONE', #40991, #21603 ) ;
#25234=ORIENTED_EDGE ( 'NONE', *, *, #26415, .F. ) ;
#25235=VECTOR ( 'NONE', #12679, 39.37007874015748143 ) ;
#25236=ORIENTED_EDGE ( 'NONE', *, *, #33676, .F. ) ;
#25237=EDGE_LOOP ( 'NONE', ( #37347, #17333, #18436, #31651 ) ) ;
#25238=CARTESIAN_POINT ( 'NONE',  ( -0.2727639067037607723, 3.346456692913386100, 2.362204724409437961 ) ) ;
#25239=VECTOR ( 'NONE', #41334, 39.37007874015748143 ) ;
#25241=EDGE_LOOP ( 'NONE', ( #28259, #47689, #31216, #26573 ) ) ;
#25243=VECTOR ( 'NONE', #22552, 39.37007874015748143 ) ;
#25244=ORIENTED_EDGE ( 'NONE', *, *, #12323, .F. ) ;
#25245=CARTESIAN_POINT ( 'NONE',  ( 0.4696143004045479352, 0.000000000000000000, -1.417322834645664331 ) ) ;
#25246=AXIS2_PLACEMENT_3D ( 'NONE', #26935, #42681, #23072 ) ;
#25247=PLANE ( 'NONE',  #29705 ) ;
#25248=EDGE_LOOP ( 'NONE', ( #45340, #1369, #3941, #43410 ) ) ;
#25249=VECTOR ( 'NONE', #43487, 39.37007874015748143 ) ;
#25250=CARTESIAN_POINT ( 'NONE',  ( -1.091055626815042645, 0.000000000000000000, -0.3149606299212593941 ) ) ;
#25251=LINE ( 'NONE', #44094, #50827 ) ;
#25253=VERTEX_POINT ( 'NONE', #48384 ) ;
#25254=LINE ( 'NONE', #33267, #21678 ) ;
#25255=PLANE ( 'NONE',  #50536 ) ;
#25258=ORIENTED_EDGE ( 'NONE', *, *, #33795, .T. ) ;
#25259=CARTESIAN_POINT ( 'NONE',  ( 0.7423782071083084855, 3.267716535433071279, -2.575641807848709208E-16 ) ) ;
#25260=CARTESIAN_POINT ( 'NONE',  ( 2.106197740627111958, 3.267716535433071279, -7.307341331430321661E-16 ) ) ;
#25261=EDGE_CURVE ( 'NONE', #19068, #24661, #13072, .T. ) ;
#25264=EDGE_CURVE ( 'NONE', #6293, #33009, #8168, .T. ) ;
#25265=ORIENTED_EDGE ( 'NONE', *, *, #49143, .T. ) ;
#25266=LINE ( 'NONE', #37407, #17092 ) ;
#25267=ADVANCED_FACE ( 'NONE', ( #47359 ), #47622, .F. ) ;
#25268=CARTESIAN_POINT ( 'NONE',  ( -1.712496953225537188, 0.000000000000000000, 0.7874015748031456541 ) ) ;
#25271=LINE ( 'NONE', #38176, #30891 ) ;
#25272=DIRECTION ( 'NONE',  ( 1.000000000000000000, -0.000000000000000000, 0.000000000000000000 ) ) ;
#25273=ORIENTED_EDGE ( 'NONE', *, *, #19103, .T. ) ;
#25274=AXIS2_PLACEMENT_3D ( 'NONE', #9456, #21584, #38104 ) ;
#25276=VECTOR ( 'NONE', #19509, 39.37007874015748143 ) ;
#25277=FACE_BOUND ( 'NONE', #39805, .T. ) ;
#25279=ORIENTED_EDGE ( 'NONE', *, *, #22631, .F. ) ;
#25280=CARTESIAN_POINT ( 'NONE',  ( 2.378961647330872786, 3.255931344577397191, 0.5824936282491406381 ) ) ;
#25282=LINE ( 'NONE', #30111, #2954 ) ;
#25283=LINE ( 'NONE', #33048, #27224 ) ;
#25284=EDGE_CURVE ( 'NONE', #1622, #4594, #675, .T. ) ;
#25286=VECTOR ( 'NONE', #31065, 39.37007874015748143 ) ;
#25288=ORIENTED_EDGE ( 'NONE', *, *, #43360, .F. ) ;
#25289=VERTEX_POINT ( 'NONE', #5061 ) ;
#25293=FACE_BOUND ( 'NONE', #29917, .T. ) ;
#25294=EDGE_LOOP ( 'NONE', ( #7316, #11601, #6236, #48997 ) ) ;
#25296=CARTESIAN_POINT ( 'NONE',  ( 0.000000000000000000, 3.267716535433071279, 1.574803149606291974 ) ) ;
#25297=EDGE_LOOP ( 'NONE', ( #50870, #23219, #5221, #4426 ) ) ;
#25298=PLANE ( 'NONE',  #47965 ) ;
#25301=ORIENTED_EDGE ( 'NONE', *, *, #5442, .T. ) ;
#25303=CARTESIAN_POINT ( 'NONE',  ( 1.558105373646060388, 3.346456692913386100, 1.417322834645662777 ) ) ;
#25304=VECTOR ( 'NONE', #2977, 39.37007874015748143 ) ;
#25308=ORIENTED_EDGE ( 'NONE', *, *, #8200, .F. ) ;
#25312=FACE_OUTER_BOUND ( 'NONE', #47848, .T. ) ;
#25313=CARTESIAN_POINT ( 'NONE',  ( 1.636583440222563857, 3.346456692913386100, -0.8267716535433055070 ) ) ;
#25315=VECTOR ( 'NONE', #11141, 39.37007874015748143 ) ;
#25321=DIRECTION ( 'NONE',  ( 1.734723475976806848E-16, -0.000000000000000000, 1.000000000000000000 ) ) ;
#25322=CARTESIAN_POINT ( 'NONE',  ( 1.091055626815042423, 3.346456692913386100, -1.771653543307081691 ) ) ;
#25323=EDGE_CURVE ( 'NONE', #21738, #42844, #44033, .T. ) ;
#25324=ORIENTED_EDGE ( 'NONE', *, *, #46915, .F. ) ;
#25326=ORIENTED_EDGE ( 'NONE', *, *, #47608, .T. ) ;
#25328=CARTESIAN_POINT ( 'NONE',  ( -1.166969139818015977, 3.267716535433071279, 4.048737525165546155E-16 ) ) ;
#25329=EDGE_CURVE ( 'NONE', #31055, #31998, #35790, .T. ) ;
#25330=ORIENTED_EDGE ( 'NONE', *, *, #4983, .F. ) ;
#25331=EDGE_CURVE ( 'NONE', #10406, #45153, #43771, .T. ) ;
#25332=ORIENTED_EDGE ( 'NONE', *, *, #39312, .F. ) ;
#25333=DIRECTION ( 'NONE',  ( -0.000000000000000000, 1.000000000000000000, -0.000000000000000000 ) ) ;
#25334=ORIENTED_EDGE ( 'NONE', *, *, #45086, .T. ) ;
#25335=CARTESIAN_POINT ( 'NONE',  ( -1.985260859929297794, 3.346456692913386100, -0.1968503937007880511 ) ) ;
#25336=LINE ( 'NONE', #17849, #41252 ) ;
#25337=EDGE_CURVE ( 'NONE', #48833, #34963, #49405, .T. ) ;
#25340=ORIENTED_EDGE ( 'NONE', *, *, #26886, .T. ) ;
#25343=AXIS2_PLACEMENT_3D ( 'NONE', #42760, #7406, #50702 ) ;
#25344=CARTESIAN_POINT ( 'NONE',  ( 0.000000000000000000, 3.346456692913386100, 0.000000000000000000 ) ) ;
#25346=ORIENTED_EDGE ( 'NONE', *, *, #12542, .F. ) ;
#25347=EDGE_CURVE ( 'NONE', #30593, #41937, #29831, .T. ) ;
#25348=CARTESIAN_POINT ( 'NONE',  ( 0.000000000000000000, 3.267716535433071279, 0.000000000000000000 ) ) ;
#25349=PLANE ( 'NONE',  #41753 ) ;
#25351=EDGE_LOOP ( 'NONE', ( #22837, #37059, #26210, #11386 ) ) ;
#25352=DIRECTION ( 'NONE',  ( 0.000000000000000000, 1.000000000000000000, 0.000000000000000000 ) ) ;
#25354=EDGE_CURVE ( 'NONE', #35441, #40968, #9704, .T. ) ;
#25357=DIRECTION ( 'NONE',  ( -3.469446951953613696E-16, 0.000000000000000000, -1.000000000000000000 ) ) ;
#25358=CARTESIAN_POINT ( 'NONE',  ( -2.182111253630085290, 0.000000000000000000, 0.9448818897637749625 ) ) ;
#25359=PLANE ( 'NONE',  #40618 ) ;
#25360=EDGE_LOOP ( 'NONE', ( #27863, #11059, #16065, #35925 ) ) ;
#25361=ORIENTED_EDGE ( 'NONE', *, *, #35945, .F. ) ;
#25363=VECTOR ( 'NONE', #28288, 39.37007874015748143 ) ;
#25365=DIRECTION ( 'NONE',  ( 1.734723475976806848E-16, -0.000000000000000000, 1.000000000000000000 ) ) ;
#25368=ORIENTED_EDGE ( 'NONE', *, *, #7017, .F. ) ;
#25369=ORIENTED_EDGE ( 'NONE', *, *, #35422, .T. ) ;
#25371=ORIENTED_EDGE ( 'NONE', *, *, #10349, .T. ) ;
#25372=PLANE ( 'NONE',  #15080 ) ;
#25375=DIRECTION ( 'NONE',  ( 1.000000000000000000, 0.000000000000000000, 0.000000000000000000 ) ) ;
#25377=CARTESIAN_POINT ( 'NONE',  ( 0.7423782071083091516, 0.000000000000000000, 1.692913385826762873 ) ) ;
#25378=ORIENTED_EDGE ( 'NONE', *, *, #15177, .T. ) ;
#25379=DIRECTION ( 'NONE',  ( 1.000000000000000000, 0.000000000000000000, 0.000000000000000000 ) ) ;
#25381=FACE_OUTER_BOUND ( 'NONE', #1261, .T. ) ;
#25382=EDGE_CURVE ( 'NONE', #35273, #51000, #48637, .T. ) ;
#25383=ORIENTED_EDGE ( 'NONE', *, *, #43118, .T. ) ;
#25384=DIRECTION ( 'NONE',  ( -0.000000000000000000, 1.000000000000000000, -0.000000000000000000 ) ) ;
#25386=CARTESIAN_POINT ( 'NONE',  ( 1.909347346926324684, 0.000000000000000000, -0.6692913385826764205 ) ) ;
#25389=EDGE_CURVE ( 'NONE', #4391, #20592, #25697, .T. ) ;
#25390=VECTOR ( 'NONE', #6191, 39.37007874015748143 ) ;
#25391=CARTESIAN_POINT ( 'NONE',  ( -0.6214413264104939882, 3.346456692913386100, 0.7874015748031456541 ) ) ;
#25392=ORIENTED_EDGE ( 'NONE', *, *, #26161, .T. ) ;
#25393=CARTESIAN_POINT ( 'NONE',  ( -0.5455278134075214336, 3.346456692913386100, 0.1181102362204703021 ) ) ;
#25395=ORIENTED_EDGE ( 'NONE', *, *, #19491, .T. ) ;
#25396=VECTOR ( 'NONE', #5762, 39.37007874015748143 ) ;
#25397=CARTESIAN_POINT ( 'NONE',  ( 3.927031490892378253E-16, 3.267716535433071279, 1.377952755905504256 ) ) ;
#25398=CARTESIAN_POINT ( 'NONE',  ( -0.5455278134075214336, 0.000000000000000000, 0.1181102362204703021 ) ) ;
#25399=CARTESIAN_POINT ( 'NONE',  ( 1.091055626815042423, 0.000000000000000000, -1.456692913385822630 ) ) ;
#25400=LINE ( 'NONE', #21530, #40842 ) ;
#25402=ORIENTED_EDGE ( 'NONE', *, *, #18064, .F. ) ;
#25403=ORIENTED_EDGE ( 'NONE', *, *, #22890, .F. ) ;
#25404=DIRECTION ( 'NONE',  ( -0.000000000000000000, 1.000000000000000000, -0.000000000000000000 ) ) ;
#25405=DIRECTION ( 'NONE',  ( 0.000000000000000000, 0.000000000000000000, -1.000000000000000000 ) ) ;
#25406=ORIENTED_EDGE ( 'NONE', *, *, #13715, .F. ) ;
#25408=LINE ( 'NONE', #45511, #34356 ) ;
#25409=CARTESIAN_POINT ( 'NONE',  ( -1.091055626815042645, 3.346456692913386100, -2.086614173228339641 ) ) ;
#25410=EDGE_LOOP ( 'NONE', ( #15526, #35172, #45406, #31041 ) ) ;
#25411=VERTEX_POINT ( 'NONE', #9448 ) ;
#25412=CARTESIAN_POINT ( 'NONE',  ( 1.091055626815042645, 3.267716535433071279, 0.6299212598425161236 ) ) ;
#25413=DIRECTION ( 'NONE',  ( -1.000000000000000000, 0.000000000000000000, -0.000000000000000000 ) ) ;
#25414=ADVANCED_FACE ( 'NONE', ( #1950 ), #32961, .F. ) ;
#25415=DIRECTION ( 'NONE',  ( -3.469446951953613696E-16, 0.000000000000000000, -1.000000000000000000 ) ) ;
#25417=FACE_BOUND ( 'NONE', #35697, .T. ) ;
#25418=ORIENTED_EDGE ( 'NONE', *, *, #34783, .T. ) ;
#25419=DIRECTION ( 'NONE',  ( 1.734723475976806848E-16, -0.000000000000000000, 1.000000000000000000 ) ) ;
#25422=ORIENTED_EDGE ( 'NONE', *, *, #19402, .T. ) ;
#25424=DIRECTION ( 'NONE',  ( 0.000000000000000000, 0.000000000000000000, -1.000000000000000000 ) ) ;
#25425=EDGE_CURVE ( 'NONE', #32340, #18300, #21067, .T. ) ;
#25428=ORIENTED_EDGE ( 'NONE', *, *, #39312, .T. ) ;
#25430=AXIS2_PLACEMENT_3D ( 'NONE', #34269, #4036, #11273 ) ;
#25432=ORIENTED_EDGE ( 'NONE', *, *, #5325, .T. ) ;
#25433=ADVANCED_FACE ( 'NONE', ( #41204 ), #17703, .F. ) ;
#25435=LINE ( 'NONE', #40938, #32068 ) ;
#25436=DIRECTION ( 'NONE',  ( -0.000000000000000000, 1.000000000000000000, -0.000000000000000000 ) ) ;
#25437=DIRECTION ( 'NONE',  ( -0.000000000000000000, 1.000000000000000000, -0.000000000000000000 ) ) ;
#25438=ADVANCED_FACE ( 'NONE', ( #14080 ), #9956, .F. ) ;
#25439=CARTESIAN_POINT ( 'NONE',  ( 1.560669927219590525, 3.346456692913386100, 0.5905511811023579360 ) ) ;
#25442=EDGE_LOOP ( 'NONE', ( #11111, #31723, #3842, #26550 ) ) ;
#25444=LINE ( 'NONE', #41208, #42977 ) ;
#25447=CYLINDRICAL_SURFACE ( 'NONE', #43808, 2.165354330708661568 ) ;
#25449=VERTEX_POINT ( 'NONE', #24936 ) ;
#25450=DIRECTION ( 'NONE',  ( -0.000000000000000000, 1.000000000000000000, -0.000000000000000000 ) ) ;
#25451=VECTOR ( 'NONE', #27486, 39.37007874015748143 ) ;
#25453=EDGE_CURVE ( 'NONE', #10658, #20943, #22088, .T. ) ;
#25454=CARTESIAN_POINT ( 'NONE',  ( -0.5455278134075208785, 3.346456692913386100, 0.7480314960629874665 ) ) ;
#25455=EDGE_CURVE ( 'NONE', #37535, #2752, #14332, .T. ) ;
#25456=DIRECTION ( 'NONE',  ( -3.469446951953613696E-16, 0.000000000000000000, -1.000000000000000000 ) ) ;
#25457=VERTEX_POINT ( 'NONE', #45798 ) ;
#25458=LINE ( 'NONE', #1970, #8446 ) ;
#25459=EDGE_LOOP ( 'NONE', ( #29211, #29045, #33755, #10061, #41024 ) ) ;
#25460=FACE_BOUND ( 'NONE', #44379, .T. ) ;
#25461=DIRECTION ( 'NONE',  ( -0.000000000000000000, 1.000000000000000000, -0.000000000000000000 ) ) ;
#25463=FACE_OUTER_BOUND ( 'NONE', #44646, .T. ) ;
#25466=ORIENTED_EDGE ( 'NONE', *, *, #16668, .T. ) ;
#25467=EDGE_LOOP ( 'NONE', ( #20094, #32491, #11810, #49686 ) ) ;
#25468=CARTESIAN_POINT ( 'NONE',  ( -1.985260859929297572, 3.267716535433071279, 0.3149606299212578953 ) ) ;
#25470=VECTOR ( 'NONE', #14600, 39.37007874015748143 ) ;
#25472=ORIENTED_EDGE ( 'NONE', *, *, #17774, .F. ) ;
#25473=CARTESIAN_POINT ( 'NONE',  ( -1.363819533518803029, 0.000000000000000000, 1.220472440944875281 ) ) ;
#25474=ORIENTED_EDGE ( 'NONE', *, *, #42467, .T. ) ;
#25475=LINE ( 'NONE', #10242, #45521 ) ;
#25478=VERTEX_POINT ( 'NONE', #1441 ) ;
#25479=CARTESIAN_POINT ( 'NONE',  ( 0.1968503937007877735, 3.267716535433071279, 1.692913385826762873 ) ) ;
#25480=ORIENTED_EDGE ( 'NONE', *, *, #23448, .F. ) ;
#25482=ADVANCED_FACE ( 'NONE', ( #29316 ), #40688, .F. ) ;
#25483=EDGE_CURVE ( 'NONE', #48933, #47342, #18961, .T. ) ;
#25485=ADVANCED_FACE ( 'NONE', ( #34968 ), #23333, .F. ) ;
#25487=EDGE_LOOP ( 'NONE', ( #34305, #29854, #21689, #14135 ) ) ;
#25488=DIRECTION ( 'NONE',  ( -0.000000000000000000, 1.000000000000000000, -0.000000000000000000 ) ) ;
#25489=EDGE_CURVE ( 'NONE', #35180, #14599, #50648, .T. ) ;
#25492=PLANE ( 'NONE',  #12042 ) ;
#25493=VECTOR ( 'NONE', #42190, 39.37007874015748143 ) ;
#25494=DIRECTION ( 'NONE',  ( -1.000000000000000000, 0.000000000000000000, 1.734723475976806848E-16 ) ) ;
#25495=VECTOR ( 'NONE', #2486, 39.37007874015748143 ) ;
#25499=VERTEX_POINT ( 'NONE', #22842 ) ;
#25500=DIRECTION ( 'NONE',  ( -3.469446951953613696E-16, 0.000000000000000000, -1.000000000000000000 ) ) ;
#25501=LINE ( 'NONE', #45862, #26676 ) ;
#25502=ADVANCED_FACE ( 'NONE', ( #2969 ), #22339, .F. ) ;
#25503=CIRCLE ( 'NONE', #28002, 2.106299212598425008 ) ;
#25507=EDGE_CURVE ( 'NONE', #48833, #42740, #26208, .T. ) ;
#25508=CARTESIAN_POINT ( 'NONE',  ( 0.1968503937007878568, 3.346456692913386100, 0.9448818897637749625 ) ) ;
#25509=PLANE ( 'NONE',  #11267 ) ;
#25511=PLANE ( 'NONE',  #45200 ) ;
#25513=EDGE_CURVE ( 'NONE', #5893, #21285, #10717, .T. ) ;
#25515=DIRECTION ( 'NONE',  ( -1.000000000000000000, 0.000000000000000000, 0.000000000000000000 ) ) ;
#25516=ADVANCED_FACE ( 'NONE', ( #42199 ), #7597, .F. ) ;
#25519=DIRECTION ( 'NONE',  ( -0.000000000000000000, 1.000000000000000000, -0.000000000000000000 ) ) ;
#25522=PLANE ( 'NONE',  #27552 ) ;
#25525=ORIENTED_EDGE ( 'NONE', *, *, #31347, .F. ) ;
#25526=LINE ( 'NONE', #17783, #49550 ) ;
#25528=CARTESIAN_POINT ( 'NONE',  ( 1.363819533518803029, 3.346456692913386100, -1.299212598425193210 ) ) ;
#25529=EDGE_LOOP ( 'NONE', ( #18920, #24032, #47879, #47213 ) ) ;
#25530=DIRECTION ( 'NONE',  ( 1.000000000000000000, 0.000000000000000000, 0.000000000000000000 ) ) ;
#25531=CARTESIAN_POINT ( 'NONE',  ( -0.3486774197067339376, 3.346456692913386100, 0.3149606299212577287 ) ) ;
#25533=AXIS2_PLACEMENT_3D ( 'NONE', #41318, #37711, #18078 ) ;
#25534=LINE ( 'NONE', #20899, #42878 ) ;
#25536=LINE ( 'NONE', #26549, #37921 ) ;
#25537=VERTEX_POINT ( 'NONE', #30591 ) ;
#25538=VERTEX_POINT ( 'NONE', #19208 ) ;
#25540=FACE_BOUND ( 'NONE', #5581, .T. ) ;
#25542=AXIS2_PLACEMENT_3D ( 'NONE', #29723, #22738, #38492 ) ;
#25544=DIRECTION ( 'NONE',  ( -0.000000000000000000, 0.000000000000000000, 1.000000000000000000 ) ) ;
#25548=ORIENTED_EDGE ( 'NONE', *, *, #45976, .T. ) ;
#25549=CARTESIAN_POINT ( 'NONE',  ( 3.927031490892378253E-16, 3.346456692913386100, 0.7480314960629874665 ) ) ;
#25552=CARTESIAN_POINT ( 'NONE',  ( -1.439733046521776139, 3.346456692913386100, 0.6299212598425164567 ) ) ;
#25554=ORIENTED_EDGE ( 'NONE', *, *, #48210, .T. ) ;
#25555=ORIENTED_EDGE ( 'NONE', *, *, #50051, .T. ) ;
#25556=DIRECTION ( 'NONE',  ( -3.469446951953613696E-16, 0.000000000000000000, -1.000000000000000000 ) ) ;
#25557=CARTESIAN_POINT ( 'NONE',  ( -0.8182917201112819283, 3.346456692913386100, 2.047244094488179567 ) ) ;
#25558=VECTOR ( 'NONE', #17172, 39.37007874015748143 ) ;
#25562=EDGE_LOOP ( 'NONE', ( #15820, #14672, #33828, #29135 ) ) ;
#25563=CARTESIAN_POINT ( 'NONE',  ( 1.909347346926324684, 3.267716535433071279, -3.312189666507128175E-16 ) ) ;
#25564=DIRECTION ( 'NONE',  ( -1.000000000000000000, -0.000000000000000000, -0.000000000000000000 ) ) ;
#25565=LINE ( 'NONE', #21699, #9325 ) ;
#25570=EDGE_CURVE ( 'NONE', #40954, #32558, #31096, .T. ) ;
#25571=VECTOR ( 'NONE', #9365, 39.37007874015748143 ) ;
#25572=CARTESIAN_POINT ( 'NONE',  ( -0.6214413264104939882, 0.000000000000000000, 0.4724409448818872592 ) ) ;
#25573=CARTESIAN_POINT ( 'NONE',  ( -0.6214413264104945434, 3.346456692913386100, -0.03937007874015895081 ) ) ;
#25574=VERTEX_POINT ( 'NONE', #19456 ) ;
#25579=ADVANCED_FACE ( 'NONE', ( #46307 ), #34469, .F. ) ;
#25580=ORIENTED_EDGE ( 'NONE', *, *, #49401, .F. ) ;
#25582=CARTESIAN_POINT ( 'NONE',  ( 0.2727639067037604392, 3.346456692913386100, -0.03937007874015908959 ) ) ;
#25583=CARTESIAN_POINT ( 'NONE',  ( 0.9992734692680932396, 3.240154784483734396, -2.244094488188969283 ) ) ;
#25584=VERTEX_POINT ( 'NONE', #42945 ) ;
#25588=ORIENTED_EDGE ( 'NONE', *, *, #958, .F. ) ;
#25589=FACE_OUTER_BOUND ( 'NONE', #33306, .T. ) ;
#25590=CARTESIAN_POINT ( 'NONE',  ( -2.182111253630085290, 0.000000000000000000, -0.3149606299212589500 ) ) ;
#25591=ORIENTED_EDGE ( 'NONE', *, *, #20509, .F. ) ;
#25594=PLANE ( 'NONE',  #13993 ) ;
#25596=EDGE_LOOP ( 'NONE', ( #21755, #21631, #6359, #6223, #35651, #48525, #27791, #9284, #23432, #3823, #1838, #1237, #14315, #8961, #6463, #32186, #50409, #27800, #45774, #9995, #45065, #10042, #24564, #46535, #3590, #34336, #12489, #26763, #37563, #19730, #17725, #5297, #47591, #9102, #17425, #32290, #42036, #38261, #4208, #33092, #38779, #38120, #8793, #30539, #9817, #3747, #1168, #29637, #43228, #38766, #36827, #33194, #38895, #25660, #20156 ) ) ;
#25597=CARTESIAN_POINT ( 'NONE',  ( 0.5455278134075212115, 3.346456692913386100, -0.3149606299212593941 ) ) ;
#25599=CARTESIAN_POINT ( 'NONE',  ( 1.560669927219590303, 3.346456692913386100, -1.501022570047217508 ) ) ;
#25603=VECTOR ( 'NONE', #39054, 39.37007874015748143 ) ;
#25604=DIRECTION ( 'NONE',  ( -1.000000000000000000, 0.000000000000000000, 1.734723475976806848E-16 ) ) ;
#25605=CARTESIAN_POINT ( 'NONE',  ( 1.091055626815042423, 3.346456692913386100, -1.889763779527552368 ) ) ;
#25606=FACE_OUTER_BOUND ( 'NONE', #15090, .T. ) ;
#25610=EDGE_CURVE ( 'NONE', #10846, #10682, #10462, .T. ) ;
#25612=DIRECTION ( 'NONE',  ( -0.000000000000000000, 0.000000000000000000, 1.000000000000000000 ) ) ;
#25614=ORIENTED_EDGE ( 'NONE', *, *, #38003, .F. ) ;
#25616=ADVANCED_FACE ( 'NONE', ( #32375 ), #35986, .F. ) ;
#25617=EDGE_CURVE ( 'NONE', #31288, #49909, #23590, .T. ) ;
#25618=LINE ( 'NONE', #50081, #19803 ) ;
#25620=EDGE_CURVE ( 'NONE', #12778, #11040, #17828, .T. ) ;
#25622=EDGE_LOOP ( 'NONE', ( #9628, #40829, #37915, #40633 ) ) ;
#25623=EDGE_LOOP ( 'NONE', ( #14781, #51001, #19939, #44142 ) ) ;
#25624=DIRECTION ( 'NONE',  ( -3.469446951953613696E-16, 0.000000000000000000, -1.000000000000000000 ) ) ;
#25625=ORIENTED_EDGE ( 'NONE', *, *, #19498, .F. ) ;
#25626=DIRECTION ( 'NONE',  ( 1.734723475976806848E-16, -0.000000000000000000, 1.000000000000000000 ) ) ;
#25629=EDGE_CURVE ( 'NONE', #42940, #28023, #43964, .T. ) ;
#25630=FACE_OUTER_BOUND ( 'NONE', #36257, .T. ) ;
#25631=CARTESIAN_POINT ( 'NONE',  ( -0.8182917201112814842, 0.000000000000000000, 0.7874015748031456541 ) ) ;
#25632=DIRECTION ( 'NONE',  ( 1.734723475976806848E-16, -0.000000000000000000, 1.000000000000000000 ) ) ;
#25635=DIRECTION ( 'NONE',  ( -0.000000000000000000, 0.000000000000000000, 1.000000000000000000 ) ) ;
#25637=CARTESIAN_POINT ( 'NONE',  ( 0.000000000000000000, 3.267716535433071279, -0.03937007874015895081 ) ) ;
#25638=CIRCLE ( 'NONE', #3373, 2.165354330708661568 ) ;
#25639=ORIENTED_EDGE ( 'NONE', *, *, #34360, .T. ) ;
#25641=AXIS2_PLACEMENT_3D ( 'NONE', #24332, #28955, #33367 ) ;
#25643=DIRECTION ( 'NONE',  ( 0.000000000000000000, 1.000000000000000000, 0.000000000000000000 ) ) ;
#25644=EDGE_LOOP ( 'NONE', ( #9097, #23172, #18882, #28691 ) ) ;
#25645=CARTESIAN_POINT ( 'NONE',  ( 1.560669927219590747, 3.346456692913386100, 0.4724409448818871482 ) ) ;
#25649=AXIS2_PLACEMENT_3D ( 'NONE', #45077, #9738, #25732 ) ;
#25651=ORIENTED_EDGE ( 'NONE', *, *, #26403, .T. ) ;
#25653=EDGE_CURVE ( 'NONE', #33862, #10859, #19712, .T. ) ;
#25654=VECTOR ( 'NONE', #50713, 39.37007874015748143 ) ;
#25655=DIRECTION ( 'NONE',  ( -0.000000000000000000, 0.000000000000000000, 1.000000000000000000 ) ) ;
#25656=PLANE ( 'NONE',  #38705 ) ;
#25657=DIRECTION ( 'NONE',  ( -0.000000000000000000, 1.000000000000000000, -0.000000000000000000 ) ) ;
#25658=FACE_OUTER_BOUND ( 'NONE', #39246, .T. ) ;
#25659=VERTEX_POINT ( 'NONE', #40377 ) ;
#25660=ORIENTED_EDGE ( 'NONE', *, *, #21532, .T. ) ;
#25661=DIRECTION ( 'NONE',  ( -0.000000000000000000, 1.000000000000000000, -0.000000000000000000 ) ) ;
#25663=ORIENTED_EDGE ( 'NONE', *, *, #49599, .F. ) ;
#25664=PLANE ( 'NONE',  #19295 ) ;
#25665=LINE ( 'NONE', #2434, #17836 ) ;
#25668=EDGE_LOOP ( 'NONE', ( #23499, #2928, #51049, #8648 ) ) ;
#25669=LINE ( 'NONE', #14565, #1580 ) ;
#25671=DIRECTION ( 'NONE',  ( -1.000000000000000000, 0.000000000000000000, -0.000000000000000000 ) ) ;
#25673=CARTESIAN_POINT ( 'NONE',  ( 0.000000000000000000, 3.267716535433071279, 0.6299212598425161236 ) ) ;
#25675=VERTEX_POINT ( 'NONE', #28221 ) ;
#25676=ADVANCED_FACE ( 'NONE', ( #39341 ), #12745, .F. ) ;
#25680=FACE_OUTER_BOUND ( 'NONE', #19304, .T. ) ;
#25681=FACE_OUTER_BOUND ( 'NONE', #38476, .T. ) ;
#25682=ADVANCED_FACE ( 'NONE', ( #8102 ), #40114, .F. ) ;
#25683=VECTOR ( 'NONE', #34474, 39.37007874015748143 ) ;
#25684=ADVANCED_FACE ( 'NONE', ( #36498 ), #47297, .F. ) ;
#25685=ORIENTED_EDGE ( 'NONE', *, *, #35215, .T. ) ;
#25686=DIRECTION ( 'NONE',  ( 0.000000000000000000, 1.000000000000000000, 0.000000000000000000 ) ) ;
#25687=EDGE_CURVE ( 'NONE', #19566, #27803, #36245, .T. ) ;
#25688=CARTESIAN_POINT ( 'NONE',  ( 1.287906020515829919, 3.267716535433071279, -1.740706023381844547 ) ) ;
#25689=ORIENTED_EDGE ( 'NONE', *, *, #26254, .T. ) ;
#25690=CIRCLE ( 'NONE', #12526, 2.106299212598425008 ) ;
#25691=VECTOR ( 'NONE', #5030, 39.37007874015748143 ) ;
#25692=DIRECTION ( 'NONE',  ( -1.000000000000000000, 0.000000000000000000, -0.000000000000000000 ) ) ;
#25693=CARTESIAN_POINT ( 'NONE',  ( -1.439733046521776583, 3.267716535433071279, -0.3149606299212592275 ) ) ;
#25694=VECTOR ( 'NONE', #17139, 39.37007874015748143 ) ;
#25697=LINE ( 'NONE', #40946, #22880 ) ;
#25700=CARTESIAN_POINT ( 'NONE',  ( 2.106197740627111958, 3.267716535433071279, -7.307341331430321661E-16 ) ) ;
#25701=EDGE_CURVE ( 'NONE', #46139, #39964, #4995, .T. ) ;
#25702=LINE ( 'NONE', #1702, #33951 ) ;
#25703=ORIENTED_EDGE ( 'NONE', *, *, #48688, .T. ) ;
#25704=CARTESIAN_POINT ( 'NONE',  ( 0.000000000000000000, 3.267716535433071279, -0.6299212598425177889 ) ) ;
#25706=EDGE_LOOP ( 'NONE', ( #31319, #15374, #11760, #28869 ) ) ;
#25709=PLANE ( 'NONE',  #42331 ) ;
#25711=LINE ( 'NONE', #37089, #31799 ) ;
#25712=ORIENTED_EDGE ( 'NONE', *, *, #10716, .F. ) ;
#25713=CARTESIAN_POINT ( 'NONE',  ( -1.712496953225537633, 3.346456692913386100, 1.220472440944875059 ) ) ;
#25714=ORIENTED_EDGE ( 'NONE', *, *, #17227, .F. ) ;
#25718=CIRCLE ( 'NONE', #47929, 2.165354330708661568 ) ;
#25720=DIRECTION ( 'NONE',  ( 1.000000000000000000, 0.000000000000000000, 0.000000000000000000 ) ) ;
#25721=DIRECTION ( 'NONE',  ( 1.000000000000000000, 0.000000000000000000, 0.000000000000000000 ) ) ;
#25722=AXIS2_PLACEMENT_3D ( 'NONE', #38806, #23298, #26668 ) ;
#25725=CARTESIAN_POINT ( 'NONE',  ( 0.5455278134075213226, 3.267716535433071279, -9.463399047163221947E-17 ) ) ;
#25727=EDGE_CURVE ( 'NONE', #6760, #33442, #44982, .T. ) ;
#25728=VECTOR ( 'NONE', #38136, 39.37007874015748143 ) ;
#25729=DIRECTION ( 'NONE',  ( -1.000000000000000000, 0.000000000000000000, -0.000000000000000000 ) ) ;
#25731=EDGE_CURVE ( 'NONE', #40564, #12580, #17891, .T. ) ;
#25732=DIRECTION ( 'NONE',  ( 1.000000000000000000, 0.000000000000000000, 0.000000000000000000 ) ) ;
#25734=EDGE_LOOP ( 'NONE', ( #20450, #20877, #20697, #26250 ) ) ;
#25735=CARTESIAN_POINT ( 'NONE',  ( 2.052631463899901920, 3.346456692913386100, -0.4724409448818889246 ) ) ;
#25737=VERTEX_POINT ( 'NONE', #5761 ) ;
#25739=ORIENTED_EDGE ( 'NONE', *, *, #24103, .T. ) ;
#25740=EDGE_LOOP ( 'NONE', ( #38230, #8202, #39455, #40483 ) ) ;
#25746=VERTEX_POINT ( 'NONE', #6272 ) ;
#25748=CARTESIAN_POINT ( 'NONE',  ( 0.7423782071083087075, 3.346456692913386100, -0.3149606299212593941 ) ) ;
#25750=CARTESIAN_POINT ( 'NONE',  ( 1.909347346926324462, 0.000000000000000000, -0.9842519685039348154 ) ) ;
#25752=AXIS2_PLACEMENT_3D ( 'NONE', #32994, #714, #21104 ) ;
#25753=DIRECTION ( 'NONE',  ( 1.000000000000000000, -0.000000000000000000, 0.000000000000000000 ) ) ;
#25754=CARTESIAN_POINT ( 'NONE',  ( 0.7423782071083091516, 3.267716535433071279, 2.034117492951036166 ) ) ;
#25757=CARTESIAN_POINT ( 'NONE',  ( 1.636583440222563857, 3.346456692913386100, 0.4330708661417290162 ) ) ;
#25761=VECTOR ( 'NONE', #45753, 39.37007874015748143 ) ;
#25762=DIRECTION ( 'NONE',  ( -0.000000000000000000, 1.000000000000000000, -0.000000000000000000 ) ) ;
#25763=CARTESIAN_POINT ( 'NONE',  ( 0.5455278134075212115, 3.346456692913386100, -0.9448818897637765168 ) ) ;
#25764=VERTEX_POINT ( 'NONE', #45227 ) ;
#25765=CARTESIAN_POINT ( 'NONE',  ( 0.000000000000000000, 3.267716535433071279, -0.03937007874015908959 ) ) ;
#25766=EDGE_CURVE ( 'NONE', #36675, #20192, #29510, .T. ) ;
#25767=PLANE ( 'NONE',  #1184 ) ;
#25768=ORIENTED_EDGE ( 'NONE', *, *, #14784, .T. ) ;
#25769=CARTESIAN_POINT ( 'NONE',  ( 0.2727639067037604947, 0.000000000000000000, -1.417322834645664331 ) ) ;
#25770=ORIENTED_EDGE ( 'NONE', *, *, #14839, .F. ) ;
#25772=ADVANCED_FACE ( 'NONE', ( #33650 ), #13765, .F. ) ;
#25773=FACE_OUTER_BOUND ( 'NONE', #12501, .T. ) ;
#25774=CARTESIAN_POINT ( 'NONE',  ( 0.8182917201112821504, 3.267716535433071279, -1.419509857074483539E-16 ) ) ;
#25776=DIRECTION ( 'NONE',  ( -1.000000000000000000, 0.000000000000000000, 0.000000000000000000 ) ) ;
#25777=LINE ( 'NONE', #30162, #2184 ) ;
#25778=ORIENTED_EDGE ( 'NONE', *, *, #48659, .T. ) ;
#25779=ADVANCED_FACE ( 'NONE', ( #41384 ), #37776, .F. ) ;
#25780=CARTESIAN_POINT ( 'NONE',  ( -0.5455278134075208785, 3.346456692913386100, 1.377952755905504256 ) ) ;
#25785=CARTESIAN_POINT ( 'NONE',  ( 0.000000000000000000, 3.267716535433071279, 0.000000000000000000 ) ) ;
#25786=DIRECTION ( 'NONE',  ( -3.469446951953613696E-16, 0.000000000000000000, -1.000000000000000000 ) ) ;
#25787=ORIENTED_EDGE ( 'NONE', *, *, #14733, .T. ) ;
#25788=CARTESIAN_POINT ( 'NONE',  ( -0.8942052331142552601, 3.346456692913386100, 1.889763779527550147 ) ) ;
#25789=DIRECTION ( 'NONE',  ( -3.469446951953613696E-16, 0.000000000000000000, -1.000000000000000000 ) ) ;
#25790=EDGE_CURVE ( 'NONE', #24, #29095, #17131, .T. ) ;
#25793=VERTEX_POINT ( 'NONE', #9378 ) ;
#25796=DIRECTION ( 'NONE',  ( 1.734723475976806848E-16, -0.000000000000000000, 1.000000000000000000 ) ) ;
#25797=FACE_BOUND ( 'NONE', #4666, .T. ) ;
#25798=VERTEX_POINT ( 'NONE', #17380 ) ;
#25799=AXIS2_PLACEMENT_3D ( 'NONE', #14260, #45729, #10394 ) ;
#25800=EDGE_CURVE ( 'NONE', #6620, #25903, #5506, .T. ) ;
#25804=VERTEX_POINT ( 'NONE', #21256 ) ;
#25806=EDGE_CURVE ( 'NONE', #19022, #49191, #37014, .T. ) ;
#25809=AXIS2_PLACEMENT_3D ( 'NONE', #10467, #33471, #40691 ) ;
#25811=ORIENTED_EDGE ( 'NONE', *, *, #16193, .T. ) ;
#25814=CARTESIAN_POINT ( 'NONE',  ( -1.602125192864240821, 3.346456692913386100, -1.456692913385822186 ) ) ;
#25815=DIRECTION ( 'NONE',  ( 1.000000000000000000, -0.000000000000000000, 0.000000000000000000 ) ) ;
#25816=DIRECTION ( 'NONE',  ( -0.000000000000000000, 1.000000000000000000, -0.000000000000000000 ) ) ;
#25817=CARTESIAN_POINT ( 'NONE',  ( 0.2727639067037609943, 3.267716535433071279, 0.9055118110236167750 ) ) ;
#25821=CARTESIAN_POINT ( 'NONE',  ( 1.833433833923351353, 3.267716535433071279, -6.361001426713998480E-16 ) ) ;
#25822=LINE ( 'NONE', #33591, #21715 ) ;
#25823=CARTESIAN_POINT ( 'NONE',  ( 1.287906020515829919, 3.255645222919215431, -2.083306009933192371 ) ) ;
#25825=DIRECTION ( 'NONE',  ( 1.000000000000000000, 0.000000000000000000, -3.469446951953613696E-16 ) ) ;
#25827=CARTESIAN_POINT ( 'NONE',  ( -0.8942052331142552601, 0.000000000000000000, -1.889763779527552146 ) ) ;
#25828=CIRCLE ( 'NONE', #2760, 2.165354330708661568 ) ;
#25829=ORIENTED_EDGE ( 'NONE', *, *, #2335, .T. ) ;
#25832=VECTOR ( 'NONE', #24888, 39.37007874015748143 ) ;
#25834=CIRCLE ( 'NONE', #34065, 2.106299212598425008 ) ;
#25835=ORIENTED_EDGE ( 'NONE', *, *, #5634, .F. ) ;
#25836=AXIS2_PLACEMENT_3D ( 'NONE', #38716, #47428, #19327 ) ;
#25837=CARTESIAN_POINT ( 'NONE',  ( -0.07591351300297359550, 0.000000000000000000, -2.047244094488181343 ) ) ;
#25839=ORIENTED_EDGE ( 'NONE', *, *, #22621, .F. ) ;
#25840=EDGE_CURVE ( 'NONE', #1622, #40318, #13004, .T. ) ;
#25841=ADVANCED_FACE ( 'NONE', ( #20997 ), #33142, .F. ) ;
#25843=CARTESIAN_POINT ( 'NONE',  ( 0.000000000000000000, 3.267716535433071279, 0.000000000000000000 ) ) ;
#25845=ADVANCED_FACE ( 'NONE', ( #1885 ), #42639, .F. ) ;
#25846=PLANE ( 'NONE',  #14480 ) ;
#25847=CARTESIAN_POINT ( 'NONE',  ( -1.636583440222564301, 0.000000000000000000, -0.5118110236220466680 ) ) ;
#25851=VERTEX_POINT ( 'NONE', #7531 ) ;
#25852=ORIENTED_EDGE ( 'NONE', *, *, #24812, .F. ) ;
#25853=CARTESIAN_POINT ( 'NONE',  ( -0.2727639067037607723, 0.000000000000000000, -0.7874015748031470974 ) ) ;
#25854=PLANE ( 'NONE',  #35155 ) ;
#25855=PLANE ( 'NONE',  #36751 ) ;
#25856=EDGE_CURVE ( 'NONE', #12446, #10888, #30016, .T. ) ;
#25859=FACE_OUTER_BOUND ( 'NONE', #2876, .T. ) ;
#25860=DIRECTION ( 'NONE',  ( 1.734723475976806848E-16, -0.000000000000000000, 1.000000000000000000 ) ) ;
#25866=VECTOR ( 'NONE', #42439, 39.37007874015748143 ) ;
#25868=EDGE_CURVE ( 'NONE', #13111, #16270, #41893, .T. ) ;
#25869=CARTESIAN_POINT ( 'NONE',  ( 0.4696143004045479352, 3.346456692913386100, -0.7874015748031473194 ) ) ;
#25870=ORIENTED_EDGE ( 'NONE', *, *, #40594, .T. ) ;
#25871=VECTOR ( 'NONE', #19790, 39.37007874015748143 ) ;
#25875=VECTOR ( 'NONE', #611, 39.37007874015748143 ) ;
#25876=LINE ( 'NONE', #6517, #42301 ) ;
#25880=VERTEX_POINT ( 'NONE', #6534 ) ;
#25881=VECTOR ( 'NONE', #38032, 39.37007874015748143 ) ;
#25882=LINE ( 'NONE', #26385, #18506 ) ;
#25883=ORIENTED_EDGE ( 'NONE', *, *, #3758, .F. ) ;
#25885=LINE ( 'NONE', #49336, #38299 ) ;
#25886=CARTESIAN_POINT ( 'NONE',  ( -0.5455278134075208785, 0.000000000000000000, 0.6299212598425164567 ) ) ;
#25887=DIRECTION ( 'NONE',  ( -0.000000000000000000, 0.000000000000000000, 1.000000000000000000 ) ) ;
#25889=ORIENTED_EDGE ( 'NONE', *, *, #41239, .T. ) ;
#25890=DIRECTION ( 'NONE',  ( -1.000000000000000000, 0.000000000000000000, -0.000000000000000000 ) ) ;
#25892=DIRECTION ( 'NONE',  ( 0.000000000000000000, 1.000000000000000000, 0.000000000000000000 ) ) ;
#25893=VERTEX_POINT ( 'NONE', #11405 ) ;
#25894=DIRECTION ( 'NONE',  ( 0.000000000000000000, 0.000000000000000000, -1.000000000000000000 ) ) ;
#25895=PLANE ( 'NONE',  #8828 ) ;
#25900=ADVANCED_FACE ( 'NONE', ( #22779 ), #7285, .F. ) ;
#25901=AXIS2_PLACEMENT_3D ( 'NONE', #6202, #19514, #49271 ) ;
#25902=ADVANCED_FACE ( 'NONE', ( #49587 ), #22275, .F. ) ;
#25903=VERTEX_POINT ( 'NONE', #2647 ) ;
#25904=AXIS2_PLACEMENT_3D ( 'NONE', #31423, #1207, #13091 ) ;
#25905=FACE_OUTER_BOUND ( 'NONE', #42283, .T. ) ;
#25906=DIRECTION ( 'NONE',  ( -1.000000000000000000, 0.000000000000000000, 1.734723475976806848E-16 ) ) ;
#25909=EDGE_CURVE ( 'NONE', #27651, #30226, #34903, .T. ) ;
#25910=AXIS2_PLACEMENT_3D ( 'NONE', #13545, #45017, #41172 ) ;
#25911=AXIS2_PLACEMENT_3D ( 'NONE', #7529, #39024, #3657 ) ;
#25912=CARTESIAN_POINT ( 'NONE',  ( -1.091055626815042645, 3.346456692913386100, 2.007874015748021268 ) ) ;
#25913=CARTESIAN_POINT ( 'NONE',  ( 0.8182917201112817063, 0.000000000000000000, -2.047244094488181343 ) ) ;
#25914=CARTESIAN_POINT ( 'NONE',  ( 1.015142113812069979, 3.267716535433071279, 1.535433070866133898 ) ) ;
#25915=LINE ( 'NONE', #41408, #43605 ) ;
#25916=VERTEX_POINT ( 'NONE', #18656 ) ;
#25917=ORIENTED_EDGE ( 'NONE', *, *, #22195, .T. ) ;
#25918=LINE ( 'NONE', #48855, #28133 ) ;
#25919=CIRCLE ( 'NONE', #16028, 2.165354330708661568 ) ;
#25920=DIRECTION ( 'NONE',  ( -3.469446951953613696E-16, 0.000000000000000000, -1.000000000000000000 ) ) ;
#25921=ORIENTED_EDGE ( 'NONE', *, *, #19139, .T. ) ;
#25922=DIRECTION ( 'NONE',  ( -0.000000000000000000, 0.000000000000000000, 1.000000000000000000 ) ) ;
#25923=CARTESIAN_POINT ( 'NONE',  ( 1.287906020515830141, 3.346456692913386100, 1.259842519685033357 ) ) ;
#25925=ORIENTED_EDGE ( 'NONE', *, *, #29598, .F. ) ;
#25928=DIRECTION ( 'NONE',  ( 1.000000000000000000, 0.000000000000000000, 0.000000000000000000 ) ) ;
#25929=LINE ( 'NONE', #17677, #28245 ) ;
#25930=PLANE ( 'NONE',  #46746 ) ;
#25931=VERTEX_POINT ( 'NONE', #18398 ) ;
#25933=DIRECTION ( 'NONE',  ( 1.734723475976806848E-16, -0.000000000000000000, 1.000000000000000000 ) ) ;
#25934=ORIENTED_EDGE ( 'NONE', *, *, #2754, .F. ) ;
#25935=EDGE_CURVE ( 'NONE', #13751, #49632, #26641, .T. ) ;
#25937=LINE ( 'NONE', #45033, #18319 ) ;
#25938=VERTEX_POINT ( 'NONE', #34404 ) ;
#25940=DIRECTION ( 'NONE',  ( -1.000000000000000000, 0.000000000000000000, 0.000000000000000000 ) ) ;
#25941=PLANE ( 'NONE',  #11049 ) ;
#25944=CARTESIAN_POINT ( 'NONE',  ( 0.000000000000000000, 3.267716535433071279, 0.000000000000000000 ) ) ;
#25946=ORIENTED_EDGE ( 'NONE', *, *, #33563, .F. ) ;
#25948=VECTOR ( 'NONE', #45222, 39.37007874015748143 ) ;
#25949=CIRCLE ( 'NONE', #27583, 2.165354330708661568 ) ;
#25950=EDGE_LOOP ( 'NONE', ( #23477, #10095, #18644, #45983 ) ) ;
#25951=CARTESIAN_POINT ( 'NONE',  ( 0.000000000000000000, 3.267716535433071279, -1.299212598425192544 ) ) ;
#25952=PLANE ( 'NONE',  #39944 ) ;
#25954=VECTOR ( 'NONE', #18275, 39.37007874015748143 ) ;
#25957=VECTOR ( 'NONE', #22919, 39.37007874015748143 ) ;
#25958=ORIENTED_EDGE ( 'NONE', *, *, #13900, .F. ) ;
#25960=CARTESIAN_POINT ( 'NONE',  ( -3.927031490892378253E-16, 3.346456692913386100, -2.204724409448811429 ) ) ;
#25961=EDGE_LOOP ( 'NONE', ( #29212, #27609, #26283, #15836 ) ) ;
#25962=LINE ( 'NONE', #37339, #47051 ) ;
#25965=LINE ( 'NONE', #45305, #24625 ) ;
#25966=CARTESIAN_POINT ( 'NONE',  ( 2.182111253630085290, 3.267716535433071279, 0.1181102362204698858 ) ) ;
#25967=CARTESIAN_POINT ( 'NONE',  ( 0.000000000000000000, 3.267716535433071279, -1.771653543307081025 ) ) ;
#25969=ORIENTED_EDGE ( 'NONE', *, *, #18809, .F. ) ;
#25970=FACE_OUTER_BOUND ( 'NONE', #43556, .T. ) ;
#25971=VERTEX_POINT ( 'NONE', #31028 ) ;
#25972=FACE_BOUND ( 'NONE', #27088, .T. ) ;
#25973=EDGE_CURVE ( 'NONE', #19682, #47308, #42883, .T. ) ;
#25974=CARTESIAN_POINT ( 'NONE',  ( -0.5455278134075217666, 3.226699998040866824, -2.401574803149598036 ) ) ;
#25975=CARTESIAN_POINT ( 'NONE',  ( 1.287906020515830141, 3.267716535433071279, 1.062992125984246083 ) ) ;
#25976=DIRECTION ( 'NONE',  ( -1.000000000000000000, -0.000000000000000000, -0.000000000000000000 ) ) ;
#25978=EDGE_CURVE ( 'NONE', #30890, #15224, #8550, .T. ) ;
#25980=ORIENTED_EDGE ( 'NONE', *, *, #36362, .F. ) ;
#25981=AXIS2_PLACEMENT_3D ( 'NONE', #30466, #29956, #11092 ) ;
#25982=FACE_OUTER_BOUND ( 'NONE', #25297, .T. ) ;
#25983=VECTOR ( 'NONE', #21540, 39.37007874015748143 ) ;
#25984=AXIS2_PLACEMENT_3D ( 'NONE', #25572, #25825, #37467 ) ;
#25985=LINE ( 'NONE', #37877, #44221 ) ;
#25986=ORIENTED_EDGE ( 'NONE', *, *, #45059, .F. ) ;
#25987=VECTOR ( 'NONE', #38612, 39.37007874015748143 ) ;
#25988=DIRECTION ( 'NONE',  ( 1.734723475976806848E-16, -0.000000000000000000, 1.000000000000000000 ) ) ;
#25989=EDGE_CURVE ( 'NONE', #373, #713, #39787, .T. ) ;
#25990=ORIENTED_EDGE ( 'NONE', *, *, #41993, .F. ) ;
#25991=CARTESIAN_POINT ( 'NONE',  ( 1.287906020515829919, 0.000000000000000000, -1.889763779527552368 ) ) ;
#25992=DIRECTION ( 'NONE',  ( 1.000000000000000000, 0.000000000000000000, 0.000000000000000000 ) ) ;
#25993=VECTOR ( 'NONE', #13027, 39.37007874015748143 ) ;
#25999=ADVANCED_FACE ( 'NONE', ( #35920 ), #28413, .F. ) ;
#26002=LINE ( 'NONE', #37380, #7944 ) ;
#26003=VERTEX_POINT ( 'NONE', #32310 ) ;
#26004=DIRECTION ( 'NONE',  ( -3.469446951953613696E-16, 0.000000000000000000, -1.000000000000000000 ) ) ;
#26010=VECTOR ( 'NONE', #48700, 39.37007874015748143 ) ;
#26011=ORIENTED_EDGE ( 'NONE', *, *, #43364, .T. ) ;
#26012=DIRECTION ( 'NONE',  ( -1.000000000000000000, 0.000000000000000000, 1.734723475976806848E-16 ) ) ;
#26013=CARTESIAN_POINT ( 'NONE',  ( -0.5455278134075214336, 0.000000000000000000, 0.3149606299212577287 ) ) ;
#26015=PLANE ( 'NONE',  #16095 ) ;
#26017=CARTESIAN_POINT ( 'NONE',  ( 0.8182917201112819283, 3.267716535433071279, 1.102362204724403938 ) ) ;
#26019=DIRECTION ( 'NONE',  ( 0.000000000000000000, -1.000000000000000000, 0.000000000000000000 ) ) ;
#26020=PLANE ( 'NONE',  #35998 ) ;
#26021=ORIENTED_EDGE ( 'NONE', *, *, #44483, .F. ) ;
#26025=AXIS2_PLACEMENT_3D ( 'NONE', #30296, #46017, #1652 ) ;
#26026=ORIENTED_EDGE ( 'NONE', *, *, #10399, .T. ) ;
#26027=ORIENTED_EDGE ( 'NONE', *, *, #44685, .T. ) ;
#26028=LINE ( 'NONE', #41778, #51 ) ;
#26033=DIRECTION ( 'NONE',  ( -1.000000000000000000, 0.000000000000000000, 0.000000000000000000 ) ) ;
#26034=ORIENTED_EDGE ( 'NONE', *, *, #18926, .T. ) ;
#26035=ADVANCED_FACE ( 'NONE', ( #7783 ), #28155, .F. ) ;
#26038=ORIENTED_EDGE ( 'NONE', *, *, #40317, .F. ) ;
#26039=DIRECTION ( 'NONE',  ( 0.000000000000000000, -1.000000000000000000, 0.000000000000000000 ) ) ;
#26040=EDGE_LOOP ( 'NONE', ( #44021, #27985, #29981 ) ) ;
#26041=LINE ( 'NONE', #49995, #41134 ) ;
#26043=ORIENTED_EDGE ( 'NONE', *, *, #25617, .T. ) ;
#26044=CARTESIAN_POINT ( 'NONE',  ( -1.299212598425207865, 3.267716535433071279, 1.732283464566920950 ) ) ;
#26045=LINE ( 'NONE', #22433, #34788 ) ;
#26046=DIRECTION ( 'NONE',  ( -0.000000000000000000, 1.000000000000000000, -0.000000000000000000 ) ) ;
#26047=VECTOR ( 'NONE', #29766, 39.37007874015748143 ) ;
#26052=FACE_BOUND ( 'NONE', #8426, .T. ) ;
#26053=ORIENTED_EDGE ( 'NONE', *, *, #34088, .T. ) ;
#26054=AXIS2_PLACEMENT_3D ( 'NONE', #8255, #23740, #36137 ) ;
#26055=LINE ( 'NONE', #6183, #37781 ) ;
#26058=EDGE_CURVE ( 'NONE', #14448, #42497, #11906, .T. ) ;
#26060=ORIENTED_EDGE ( 'NONE', *, *, #37683, .F. ) ;
#26062=AXIS2_PLACEMENT_3D ( 'NONE', #32474, #5089, #49681 ) ;
#26063=PLANE ( 'NONE',  #39715 ) ;
#26064=ORIENTED_EDGE ( 'NONE', *, *, #6497, .F. ) ;
#26065=ORIENTED_EDGE ( 'NONE', *, *, #21728, .T. ) ;
#26066=EDGE_CURVE ( 'NONE', #11553, #48423, #15775, .T. ) ;
#26068=DIRECTION ( 'NONE',  ( 1.000000000000000000, 0.000000000000000000, 0.000000000000000000 ) ) ;
#26069=CARTESIAN_POINT ( 'NONE',  ( -0.8182917201112819283, 0.000000000000000000, -1.614173228346451605 ) ) ;
#26073=CARTESIAN_POINT ( 'NONE',  ( -1.091055626815042201, 0.000000000000000000, 0.9448818897637749625 ) ) ;
#26074=VERTEX_POINT ( 'NONE', #46980 ) ;
#26077=CARTESIAN_POINT ( 'NONE',  ( -1.363819533518803473, 3.346456692913386100, -0.6692913385826760875 ) ) ;
#26078=ADVANCED_FACE ( 'NONE', ( #12420 ), #19642, .F. ) ;
#26082=CARTESIAN_POINT ( 'NONE',  ( -1.091055626815042201, 0.000000000000000000, 1.062992125984246083 ) ) ;
#26084=DIRECTION ( 'NONE',  ( -0.000000000000000000, 0.000000000000000000, 1.000000000000000000 ) ) ;
#26086=CIRCLE ( 'NONE', #37632, 2.443628662382284489 ) ;
#26087=DIRECTION ( 'NONE',  ( 0.000000000000000000, 0.000000000000000000, -1.000000000000000000 ) ) ;
#26090=VECTOR ( 'NONE', #6242, 39.37007874015748143 ) ;
#26092=EDGE_CURVE ( 'NONE', #45803, #11936, #16039, .T. ) ;
#26094=VECTOR ( 'NONE', #14832, 39.37007874015748143 ) ;
#26095=ORIENTED_EDGE ( 'NONE', *, *, #45120, .F. ) ;
#26096=EDGE_CURVE ( 'NONE', #21949, #8694, #47494, .T. ) ;
#26097=VECTOR ( 'NONE', #9417, 39.37007874015748143 ) ;
#26101=ORIENTED_EDGE ( 'NONE', *, *, #9144, .F. ) ;
#26102=DIRECTION ( 'NONE',  ( 1.000000000000000000, -0.000000000000000000, 0.000000000000000000 ) ) ;
#26103=LINE ( 'NONE', #46449, #32154 ) ;
#26104=EDGE_CURVE ( 'NONE', #912, #36517, #8291, .T. ) ;
#26106=ORIENTED_EDGE ( 'NONE', *, *, #8465, .T. ) ;
#26110=CARTESIAN_POINT ( 'NONE',  ( 1.091055626815042645, 0.000000000000000000, -0.9448818897637765168 ) ) ;
#26114=ORIENTED_EDGE ( 'NONE', *, *, #42774, .F. ) ;
#26115=CARTESIAN_POINT ( 'NONE',  ( 0.8182917201112819283, 0.000000000000000000, 1.102362204724403938 ) ) ;
#26116=DIRECTION ( 'NONE',  ( -1.000000000000000000, 0.000000000000000000, 1.734723475976806848E-16 ) ) ;
#26117=DIRECTION ( 'NONE',  ( 0.000000000000000000, 0.000000000000000000, -1.000000000000000000 ) ) ;
#26121=DIRECTION ( 'NONE',  ( -0.000000000000000000, 0.000000000000000000, 1.000000000000000000 ) ) ;
#26123=LINE ( 'NONE', #25869, #31540 ) ;
#26124=EDGE_LOOP ( 'NONE', ( #34694, #50271, #28323, #46817, #48042 ) ) ;
#26125=VERTEX_POINT ( 'NONE', #42023 ) ;
#26127=LINE ( 'NONE', #38016, #16 ) ;
#26130=AXIS2_PLACEMENT_3D ( 'NONE', #1362, #13247, #2126 ) ;
#26131=ADVANCED_FACE ( 'NONE', ( #45360 ), #26020, .F. ) ;
#26135=ORIENTED_EDGE ( 'NONE', *, *, #35178, .T. ) ;
#26136=EDGE_CURVE ( 'NONE', #43954, #26976, #50774, .T. ) ;
#26139=ORIENTED_EDGE ( 'NONE', *, *, #22592, .T. ) ;
#26141=DIRECTION ( 'NONE',  ( 0.000000000000000000, 0.000000000000000000, -1.000000000000000000 ) ) ;
#26146=CARTESIAN_POINT ( 'NONE',  ( 0.000000000000000000, 3.267716535433071279, -0.5118110236220471121 ) ) ;
#26148=ADVANCED_FACE ( 'NONE', ( #41513 ), #25509, .F. ) ;
#26149=CARTESIAN_POINT ( 'NONE',  ( -0.5455278134075208785, 3.346456692913386100, 0.6299212598425164567 ) ) ;
#26151=CARTESIAN_POINT ( 'NONE',  ( -0.5455278134075214336, 0.000000000000000000, -1.456692913385822630 ) ) ;
#26152=EDGE_CURVE ( 'NONE', #22204, #19885, #17767, .T. ) ;
#26153=DIRECTION ( 'NONE',  ( 0.000000000000000000, -1.000000000000000000, 0.000000000000000000 ) ) ;
#26154=PLANE ( 'NONE',  #7347 ) ;
#26156=ORIENTED_EDGE ( 'NONE', *, *, #914, .T. ) ;
#26157=VECTOR ( 'NONE', #3732, 39.37007874015748143 ) ;
#26158=EDGE_CURVE ( 'NONE', #42434, #30956, #40311, .T. ) ;
#26159=DIRECTION ( 'NONE',  ( -1.000000000000000000, 0.000000000000000000, 1.734723475976806848E-16 ) ) ;
#26160=VECTOR ( 'NONE', #38594, 39.37007874015748143 ) ;
#26161=EDGE_CURVE ( 'NONE', #28900, #39490, #6146, .T. ) ;
#26162=EDGE_CURVE ( 'NONE', #44897, #19562, #18532, .T. ) ;
#26163=VERTEX_POINT ( 'NONE', #2780 ) ;
#26166=DIRECTION ( 'NONE',  ( -3.469446951953613696E-16, 0.000000000000000000, -1.000000000000000000 ) ) ;
#26169=DIRECTION ( 'NONE',  ( 0.000000000000000000, -1.000000000000000000, 0.000000000000000000 ) ) ;
#26171=EDGE_LOOP ( 'NONE', ( #39181, #42127, #20011, #32475 ) ) ;
#26174=ORIENTED_EDGE ( 'NONE', *, *, #11830, .T. ) ;
#26176=DIRECTION ( 'NONE',  ( -0.000000000000000000, 1.000000000000000000, -0.000000000000000000 ) ) ;
#26179=VERTEX_POINT ( 'NONE', #20673 ) ;
#26180=CARTESIAN_POINT ( 'NONE',  ( -2.174914189033237299, 3.240375350693514456, -1.141732283464563791 ) ) ;
#26184=DIRECTION ( 'NONE',  ( 1.000000000000000000, -0.000000000000000000, 0.000000000000000000 ) ) ;
#26185=CARTESIAN_POINT ( 'NONE',  ( -3.414809992080329023E-17, 0.000000000000000000, -0.1968503937007874405 ) ) ;
#26186=ORIENTED_EDGE ( 'NONE', *, *, #39726, .F. ) ;
#26187=LINE ( 'NONE', #18446, #2653 ) ;
#26188=EDGE_LOOP ( 'NONE', ( #48227, #41736, #14433, #26387 ) ) ;
#26189=VERTEX_POINT ( 'NONE', #34284 ) ;
#26190=CARTESIAN_POINT ( 'NONE',  ( -1.439733046521776361, 3.267716535433071279, 1.062992125984246083 ) ) ;
#26191=DIRECTION ( 'NONE',  ( -1.000000000000000000, 0.000000000000000000, -0.000000000000000000 ) ) ;
#26192=CARTESIAN_POINT ( 'NONE',  ( -0.5455278134075208785, 0.000000000000000000, 1.692913385826762873 ) ) ;
#26196=DIRECTION ( 'NONE',  ( -1.000000000000000000, 0.000000000000000000, 1.734723475976806848E-16 ) ) ;
#26198=ORIENTED_EDGE ( 'NONE', *, *, #20054, .T. ) ;
#26199=EDGE_CURVE ( 'NONE', #50303, #6760, #6338, .T. ) ;
#26201=VECTOR ( 'NONE', #46656, 39.37007874015748143 ) ;
#26204=EDGE_CURVE ( 'NONE', #11067, #19232, #14655, .T. ) ;
#26207=CIRCLE ( 'NONE', #50075, 2.443628662382284489 ) ;
#26208=LINE ( 'NONE', #11474, #40174 ) ;
#26210=ORIENTED_EDGE ( 'NONE', *, *, #45086, .F. ) ;
#26211=DIRECTION ( 'NONE',  ( 1.000000000000000000, 0.000000000000000000, 0.000000000000000000 ) ) ;
#26213=PLANE ( 'NONE',  #37263 ) ;
#26214=VERTEX_POINT ( 'NONE', #1054 ) ;
#26215=CARTESIAN_POINT ( 'NONE',  ( 0.4696143004045476577, 0.000000000000000000, -2.047244094488182231 ) ) ;
#26216=EDGE_CURVE ( 'NONE', #19232, #12600, #29898, .T. ) ;
#26217=DIRECTION ( 'NONE',  ( 1.000000000000000000, 0.000000000000000000, -3.469446951953613696E-16 ) ) ;
#26218=ORIENTED_EDGE ( 'NONE', *, *, #19307, .T. ) ;
#26219=CARTESIAN_POINT ( 'NONE',  ( -2.001301579076982584, 3.267716535433071279, -0.8267716535433052849 ) ) ;
#26220=CARTESIAN_POINT ( 'NONE',  ( 1.636583440222563857, 0.000000000000000000, 1.259842519685033135 ) ) ;
#26222=EDGE_CURVE ( 'NONE', #4005, #22546, #533, .T. ) ;
#26223=ORIENTED_EDGE ( 'NONE', *, *, #26912, .T. ) ;
#26224=PLANE ( 'NONE',  #18901 ) ;
#26225=ORIENTED_EDGE ( 'NONE', *, *, #18868, .F. ) ;
#26226=FACE_BOUND ( 'NONE', #14126, .T. ) ;
#26227=LINE ( 'NONE', #41976, #15215 ) ;
#26228=LINE ( 'NONE', #14613, #11128 ) ;
#26230=VECTOR ( 'NONE', #39175, 39.37007874015748143 ) ;
#26232=VERTEX_POINT ( 'NONE', #37400 ) ;
#26233=VERTEX_POINT ( 'NONE', #33533 ) ;
#26235=LINE ( 'NONE', #14620, #41122 ) ;
#26236=VECTOR ( 'NONE', #39328, 39.37007874015748143 ) ;
#26237=DIRECTION ( 'NONE',  ( -1.000000000000000000, -0.000000000000000000, -0.000000000000000000 ) ) ;
#26239=DIRECTION ( 'NONE',  ( -1.000000000000000000, -0.000000000000000000, -0.000000000000000000 ) ) ;
#26240=VECTOR ( 'NONE', #43406, 39.37007874015748143 ) ;
#26241=ORIENTED_EDGE ( 'NONE', *, *, #37449, .F. ) ;
#26242=LINE ( 'NONE', #29352, #15071 ) ;
#26243=VECTOR ( 'NONE', #40682, 39.37007874015748143 ) ;
#26245=ORIENTED_EDGE ( 'NONE', *, *, #39477, .T. ) ;
#26246=LINE ( 'NONE', #18758, #37319 ) ;
#26247=ORIENTED_EDGE ( 'NONE', *, *, #6058, .F. ) ;
#26248=ORIENTED_EDGE ( 'NONE', *, *, #13256, .F. ) ;
#26249=VECTOR ( 'NONE', #5642, 39.37007874015748143 ) ;
#26250=ORIENTED_EDGE ( 'NONE', *, *, #36408, .F. ) ;
#26251=ORIENTED_EDGE ( 'NONE', *, *, #42412, .F. ) ;
#26254=EDGE_CURVE ( 'NONE', #44436, #2513, #2273, .T. ) ;
#26255=ORIENTED_EDGE ( 'NONE', *, *, #7946, .F. ) ;
#26258=EDGE_CURVE ( 'NONE', #18949, #7323, #50715, .T. ) ;
#26259=CIRCLE ( 'NONE', #4003, 2.106299212598425008 ) ;
#26261=CARTESIAN_POINT ( 'NONE',  ( 1.091055626815042645, 3.346456692913386100, 0.9448818897637746295 ) ) ;
#26263=DIRECTION ( 'NONE',  ( -3.469446951953613696E-16, 0.000000000000000000, -1.000000000000000000 ) ) ;
#26266=DIRECTION ( 'NONE',  ( -1.000000000000000000, -0.000000000000000000, -0.000000000000000000 ) ) ;
#26267=VECTOR ( 'NONE', #27599, 39.37007874015748143 ) ;
#26268=DIRECTION ( 'NONE',  ( -3.469446951953613696E-16, 0.000000000000000000, -1.000000000000000000 ) ) ;
#26269=DIRECTION ( 'NONE',  ( 1.000000000000000000, -0.000000000000000000, 0.000000000000000000 ) ) ;
#26270=VECTOR ( 'NONE', #42489, 39.37007874015748143 ) ;
#26271=VECTOR ( 'NONE', #2804, 39.37007874015748143 ) ;
#26272=EDGE_LOOP ( 'NONE', ( #6816, #31666, #26590, #12819 ) ) ;
#26273=DIRECTION ( 'NONE',  ( -0.000000000000000000, 1.000000000000000000, -0.000000000000000000 ) ) ;
#26274=EDGE_CURVE ( 'NONE', #29685, #33217, #30658, .T. ) ;
#26275=DIRECTION ( 'NONE',  ( 1.734723475976806848E-16, -0.000000000000000000, 1.000000000000000000 ) ) ;
#26276=VERTEX_POINT ( 'NONE', #42265 ) ;
#26277=DIRECTION ( 'NONE',  ( -1.000000000000000000, 0.000000000000000000, 0.000000000000000000 ) ) ;
#26278=CARTESIAN_POINT ( 'NONE',  ( 0.000000000000000000, 3.267716535433071279, 0.7480314960629874665 ) ) ;
#26280=VERTEX_POINT ( 'NONE', #39157 ) ;
#26283=ORIENTED_EDGE ( 'NONE', *, *, #23732, .F. ) ;
#26286=DIRECTION ( 'NONE',  ( 1.000000000000000000, 0.000000000000000000, 0.000000000000000000 ) ) ;
#26287=PLANE ( 'NONE',  #50889 ) ;
#26289=CARTESIAN_POINT ( 'NONE',  ( -0.8182917201112814842, 0.000000000000000000, 0.5905511811023582691 ) ) ;
#26291=FACE_OUTER_BOUND ( 'NONE', #8914, .T. ) ;
#26293=EDGE_LOOP ( 'NONE', ( #9198, #17980, #36580, #20420 ) ) ;
#26294=CARTESIAN_POINT ( 'NONE',  ( -1.353122744573580727, 3.346456692913386100, -1.614173228346451605 ) ) ;
#26297=CARTESIAN_POINT ( 'NONE',  ( 1.015142113812069091, 3.267716535433071279, -1.912654141836395816 ) ) ;
#26298=EDGE_CURVE ( 'NONE', #47500, #41777, #38907, .T. ) ;
#26301=VECTOR ( 'NONE', #2237, 39.37007874015748143 ) ;
#26302=LINE ( 'NONE', #37687, #50393 ) ;
#26303=CARTESIAN_POINT ( 'NONE',  ( 1.636583440222563635, 3.346456692913386100, -1.417869535855832419 ) ) ;
#26304=ORIENTED_EDGE ( 'NONE', *, *, #9644, .T. ) ;
#26307=FACE_BOUND ( 'NONE', #45932, .T. ) ;
#26308=EDGE_LOOP ( 'NONE', ( #49292, #2107, #12282, #33670 ) ) ;
#26309=VECTOR ( 'NONE', #4203, 39.37007874015748143 ) ;
#26310=LINE ( 'NONE', #38201, #15472 ) ;
#26311=LINE ( 'NONE', #33823, #24244 ) ;
#26312=ORIENTED_EDGE ( 'NONE', *, *, #9663, .F. ) ;
#26313=ORIENTED_EDGE ( 'NONE', *, *, #23252, .T. ) ;
#26314=VECTOR ( 'NONE', #21782, 39.37007874015748143 ) ;
#26315=DIRECTION ( 'NONE',  ( -3.469446951953613696E-16, 0.000000000000000000, -1.000000000000000000 ) ) ;
#26316=LINE ( 'NONE', #7208, #5608 ) ;
#26317=VERTEX_POINT ( 'NONE', #11033 ) ;
#26318=EDGE_LOOP ( 'NONE', ( #40957, #23502, #14381, #13366 ) ) ;
#26319=VECTOR ( 'NONE', #33977, 39.37007874015748143 ) ;
#26320=ORIENTED_EDGE ( 'NONE', *, *, #46451, .F. ) ;
#26322=EDGE_CURVE ( 'NONE', #5168, #5952, #46371, .T. ) ;
#26323=CARTESIAN_POINT ( 'NONE',  ( 1.091055626815042645, 3.346456692913386100, -0.8267716535433055070 ) ) ;
#26325=ADVANCED_FACE ( 'NONE', ( #35544 ), #7665, .F. ) ;
#26326=DIRECTION ( 'NONE',  ( 1.734723475976806848E-16, -0.000000000000000000, 1.000000000000000000 ) ) ;
#26328=ORIENTED_EDGE ( 'NONE', *, *, #16184, .F. ) ;
#26329=LINE ( 'NONE', #41568, #39796 ) ;
#26332=B_SPLINE_CURVE_WITH_KNOTS ( 'NONE', 3,
 ( #192, #47402, #15942, #43299 ),
 .UNSPECIFIED., .F., .F.,
 ( 4, 4 ),
 ( 0.04410919144784399004, 0.04667637874967021927 ),
 .UNSPECIFIED. ) ;
#26333=CARTESIAN_POINT ( 'NONE',  ( 1.363819533518803029, 3.346456692913386100, -1.102362204724405714 ) ) ;
#26334=CARTESIAN_POINT ( 'NONE',  ( 1.015142113812069313, 0.000000000000000000, 0.5905511811023579360 ) ) ;
#26335=LINE ( 'NONE', #22968, #18578 ) ;
#26336=EDGE_CURVE ( 'NONE', #20150, #28628, #47114, .T. ) ;
#26338=LINE ( 'NONE', #49530, #10251 ) ;
#26339=EDGE_LOOP ( 'NONE', ( #29431, #23815, #34985, #30113 ) ) ;
#26340=LINE ( 'NONE', #10844, #42376 ) ;
#26341=CARTESIAN_POINT ( 'NONE',  ( -1.985260859929298016, 0.000000000000000000, -0.6299212598425177889 ) ) ;
#26342=ORIENTED_EDGE ( 'NONE', *, *, #50750, .F. ) ;
#26344=VECTOR ( 'NONE', #34890, 39.37007874015748143 ) ;
#26346=EDGE_LOOP ( 'NONE', ( #2199, #18021, #27308, #46027 ) ) ;
#26347=ADVANCED_FACE ( 'NONE', ( #34536 ), #50467, .F. ) ;
#26348=VERTEX_POINT ( 'NONE', #50220 ) ;
#26351=ADVANCED_FACE ( 'NONE', ( #38662 ), #26770, .F. ) ;
#26352=ORIENTED_EDGE ( 'NONE', *, *, #12734, .T. ) ;
#26354=DIRECTION ( 'NONE',  ( 1.734723475976806848E-16, -0.000000000000000000, 1.000000000000000000 ) ) ;
#26357=ORIENTED_EDGE ( 'NONE', *, *, #262, .F. ) ;
#26359=EDGE_CURVE ( 'NONE', #49030, #25746, #30911, .T. ) ;
#26361=DIRECTION ( 'NONE',  ( -1.000000000000000000, 0.000000000000000000, 1.734723475976806848E-16 ) ) ;
#26362=CARTESIAN_POINT ( 'NONE',  ( 0.1968503937007873017, 0.000000000000000000, 0.3149606299212576177 ) ) ;
#26365=ORIENTED_EDGE ( 'NONE', *, *, #35349, .F. ) ;
#26367=CARTESIAN_POINT ( 'NONE',  ( 0.4696143004045478797, 3.267716535433071279, -0.6692913385826760875 ) ) ;
#26369=CARTESIAN_POINT ( 'NONE',  ( 0.4696143004045484903, 3.267716535433071279, 2.047244094488179567 ) ) ;
#26370=ORIENTED_EDGE ( 'NONE', *, *, #1770, .T. ) ;
#26371=FACE_OUTER_BOUND ( 'NONE', #37770, .T. ) ;
#26372=DIRECTION ( 'NONE',  ( -3.469446951953613696E-16, 0.000000000000000000, -1.000000000000000000 ) ) ;
#26373=ORIENTED_EDGE ( 'NONE', *, *, #45912, .T. ) ;
#26374=ORIENTED_EDGE ( 'NONE', *, *, #5388, .F. ) ;
#26376=VECTOR ( 'NONE', #7711, 39.37007874015748143 ) ;
#26378=CARTESIAN_POINT ( 'NONE',  ( -1.091055626815042201, 3.267716535433071279, 0.3149606299212580063 ) ) ;
#26380=EDGE_CURVE ( 'NONE', #1599, #30123, #7917, .T. ) ;
#26381=CARTESIAN_POINT ( 'NONE',  ( -1.091055626815042201, 0.000000000000000000, 0.3149606299212580063 ) ) ;
#26382=ORIENTED_EDGE ( 'NONE', *, *, #24551, .T. ) ;
#26384=CARTESIAN_POINT ( 'NONE',  ( -0.5455278134075208785, 3.346456692913386100, 1.574803149606291974 ) ) ;
#26385=CARTESIAN_POINT ( 'NONE',  ( -0.8942052331142548161, 3.267716535433071279, 3.102397620449221988E-16 ) ) ;
#26387=ORIENTED_EDGE ( 'NONE', *, *, #24398, .F. ) ;
#26388=CARTESIAN_POINT ( 'NONE',  ( 0.4696143004045484903, 0.000000000000000000, 2.047244094488179567 ) ) ;
#26389=DIRECTION ( 'NONE',  ( -0.000000000000000000, 1.000000000000000000, -0.000000000000000000 ) ) ;
#26390=EDGE_CURVE ( 'NONE', #17201, #17605, #40697, .T. ) ;
#26394=EDGE_LOOP ( 'NONE', ( #17173, #12797, #45391, #36264 ) ) ;
#26395=LINE ( 'NONE', #31032, #30861 ) ;
#26396=CARTESIAN_POINT ( 'NONE',  ( -2.182111253630085290, 0.000000000000000000, 0.4330708661417290162 ) ) ;
#26397=PLANE ( 'NONE',  #14177 ) ;
#26398=ORIENTED_EDGE ( 'NONE', *, *, #36729, .T. ) ;
#26401=CARTESIAN_POINT ( 'NONE',  ( 0.8182917201112824834, 3.267716535433071279, 1.220472440944875281 ) ) ;
#26403=EDGE_CURVE ( 'NONE', #272, #18980, #32713, .T. ) ;
#26406=CARTESIAN_POINT ( 'NONE',  ( -1.521361932310741016, 3.267716535433071279, -1.456692913385822186 ) ) ;
#26408=DIRECTION ( 'NONE',  ( -3.469446951953613696E-16, 0.000000000000000000, -1.000000000000000000 ) ) ;
#26409=EDGE_CURVE ( 'NONE', #27965, #42803, #13080, .T. ) ;
#26410=VECTOR ( 'NONE', #37074, 39.37007874015748143 ) ;
#26411=DIRECTION ( 'NONE',  ( -0.000000000000000000, 1.000000000000000000, -0.000000000000000000 ) ) ;
#26412=FACE_OUTER_BOUND ( 'NONE', #16840, .T. ) ;
#26415=EDGE_CURVE ( 'NONE', #24633, #16952, #39669, .T. ) ;
#26416=EDGE_CURVE ( 'NONE', #19157, #19280, #4300, .T. ) ;
#26418=ORIENTED_EDGE ( 'NONE', *, *, #41745, .F. ) ;
#26419=FACE_OUTER_BOUND ( 'NONE', #31447, .T. ) ;
#26420=LINE ( 'NONE', #46271, #27128 ) ;
#26421=EDGE_LOOP ( 'NONE', ( #9576, #22311, #3134, #8704 ) ) ;
#26422=CARTESIAN_POINT ( 'NONE',  ( 0.4696143004045478797, 3.267716535433071279, -1.299212598425193210 ) ) ;
#26423=PLANE ( 'NONE',  #39271 ) ;
#26426=ORIENTED_EDGE ( 'NONE', *, *, #32373, .T. ) ;
#26427=ORIENTED_EDGE ( 'NONE', *, *, #25483, .T. ) ;
#26430=CARTESIAN_POINT ( 'NONE',  ( -1.363819533518803473, 3.346456692913386100, -0.4724409448818886470 ) ) ;
#26431=VERTEX_POINT ( 'NONE', #36318 ) ;
#26433=FACE_BOUND ( 'NONE', #14012, .T. ) ;
#26434=EDGE_LOOP ( 'NONE', ( #11132, #38537, #22802, #6424 ) ) ;
#26435=DIRECTION ( 'NONE',  ( -0.000000000000000000, 1.000000000000000000, -0.000000000000000000 ) ) ;
#26439=CARTESIAN_POINT ( 'NONE',  ( -0.5455278134075214336, 3.346456692913386100, -8.878505979408855953E-16 ) ) ;
#26442=LINE ( 'NONE', #38083, #9624 ) ;
#26443=EDGE_CURVE ( 'NONE', #44444, #23181, #5322, .T. ) ;
#26445=DIRECTION ( 'NONE',  ( -3.469446951953613696E-16, 0.000000000000000000, -1.000000000000000000 ) ) ;
#26446=ORIENTED_EDGE ( 'NONE', *, *, #45500, .F. ) ;
#26448=ORIENTED_EDGE ( 'NONE', *, *, #29716, .T. ) ;
#26449=FACE_OUTER_BOUND ( 'NONE', #16209, .T. ) ;
#26450=CARTESIAN_POINT ( 'NONE',  ( -1.166969139818015533, 3.267716535433071279, 4.048737525165544183E-16 ) ) ;
#26451=VECTOR ( 'NONE', #30717, 39.37007874015748143 ) ;
#26452=VECTOR ( 'NONE', #23410, 39.37007874015748143 ) ;
#26459=CARTESIAN_POINT ( 'NONE',  ( -1.439733046521776361, 3.267716535433071279, 0.4330708661417290162 ) ) ;
#26463=VERTEX_POINT ( 'NONE', #24698 ) ;
#26464=DIRECTION ( 'NONE',  ( 0.000000000000000000, 1.000000000000000000, 0.000000000000000000 ) ) ;
#26465=LINE ( 'NONE', #50168, #46432 ) ;
#26469=ORIENTED_EDGE ( 'NONE', *, *, #37763, .F. ) ;
#26470=FACE_BOUND ( 'NONE', #6187, .T. ) ;
#26471=CARTESIAN_POINT ( 'NONE',  ( -0.8182917201112819283, 3.346456692913386100, -0.6692913385826760875 ) ) ;
#26472=FACE_OUTER_BOUND ( 'NONE', #31916, .T. ) ;
#26473=EDGE_CURVE ( 'NONE', #19997, #26534, #32970, .T. ) ;
#26475=EDGE_LOOP ( 'NONE', ( #11969, #45118, #37540, #19447 ) ) ;
#26476=VERTEX_POINT ( 'NONE', #5069 ) ;
#26477=CARTESIAN_POINT ( 'NONE',  ( 1.636583440222563857, 3.346456692913386100, 0.3149606299212576177 ) ) ;
#26478=DIRECTION ( 'NONE',  ( 1.734723475976806848E-16, 0.000000000000000000, 1.000000000000000000 ) ) ;
#26480=CARTESIAN_POINT ( 'NONE',  ( 1.091055626815042645, 3.346456692913386100, 0.6299212598425161236 ) ) ;
#26481=VECTOR ( 'NONE', #30451, 39.37007874015748143 ) ;
#26482=VECTOR ( 'NONE', #40693, 39.37007874015748143 ) ;
#26485=ORIENTED_EDGE ( 'NONE', *, *, #7655, .T. ) ;
#26486=ORIENTED_EDGE ( 'NONE', *, *, #24549, .F. ) ;
#26487=CARTESIAN_POINT ( 'NONE',  ( 0.000000000000000000, 3.267716535433071279, -0.4724409448818886470 ) ) ;
#26490=EDGE_LOOP ( 'NONE', ( #36459, #18094, #38973, #24790 ) ) ;
#26492=VERTEX_POINT ( 'NONE', #43779 ) ;
#26493=VECTOR ( 'NONE', #28124, 39.37007874015748143 ) ;
#26496=VECTOR ( 'NONE', #49659, 39.37007874015748143 ) ;
#26497=EDGE_CURVE ( 'NONE', #26476, #7771, #20298, .T. ) ;
#26499=ORIENTED_EDGE ( 'NONE', *, *, #16958, .T. ) ;
#26501=ADVANCED_FACE ( 'NONE', ( #20816 ), #9197, .F. ) ;
#26502=EDGE_CURVE ( 'NONE', #43652, #35947, #24945, .T. ) ;
#26504=EDGE_CURVE ( 'NONE', #272, #43925, #16696, .T. ) ;
#26505=DIRECTION ( 'NONE',  ( -0.000000000000000000, 1.000000000000000000, -0.000000000000000000 ) ) ;
#26509=ORIENTED_EDGE ( 'NONE', *, *, #49825, .F. ) ;
#26510=CARTESIAN_POINT ( 'NONE',  ( -2.082617625631827174, 3.346456692913386100, 0.3149606299212578953 ) ) ;
#26511=DIRECTION ( 'NONE',  ( -3.469446951953613696E-16, 0.000000000000000000, -1.000000000000000000 ) ) ;
#26515=VECTOR ( 'NONE', #26646, 39.37007874015748143 ) ;
#26518=CARTESIAN_POINT ( 'NONE',  ( -0.6214413264104939882, 3.346456692913386100, 0.4724409448818872592 ) ) ;
#26522=LINE ( 'NONE', #45112, #41611 ) ;
#26523=AXIS2_PLACEMENT_3D ( 'NONE', #22613, #38865, #50672 ) ;
#26524=VERTEX_POINT ( 'NONE', #10218 ) ;
#26525=AXIS2_PLACEMENT_3D ( 'NONE', #41243, #16983, #13361 ) ;
#26529=CARTESIAN_POINT ( 'NONE',  ( -0.2727639067037606613, 3.267716535433071279, 4.731699523581610974E-17 ) ) ;
#26533=LINE ( 'NONE', #22670, #45855 ) ;
#26534=VERTEX_POINT ( 'NONE', #5580 ) ;
#26537=EDGE_CURVE ( 'NONE', #25449, #15789, #12074, .T. ) ;
#26538=VERTEX_POINT ( 'NONE', #41212 ) ;
#26539=EDGE_LOOP ( 'NONE', ( #40735, #7259, #35073, #20852 ) ) ;
#26540=EDGE_CURVE ( 'NONE', #18808, #22242, #25199, .T. ) ;
#26544=LINE ( 'NONE', #10799, #19401 ) ;
#26545=ORIENTED_EDGE ( 'NONE', *, *, #37733, .F. ) ;
#26546=EDGE_CURVE ( 'NONE', #49624, #48094, #33975, .T. ) ;
#26548=DIRECTION ( 'NONE',  ( -1.000000000000000000, 0.000000000000000000, 0.000000000000000000 ) ) ;
#26549=CARTESIAN_POINT ( 'NONE',  ( -1.636583440222563635, 3.267716535433071279, 2.839019714148966584E-16 ) ) ;
#26550=ORIENTED_EDGE ( 'NONE', *, *, #50886, .F. ) ;
#26553=FACE_BOUND ( 'NONE', #18692, .T. ) ;
#26555=AXIS2_PLACEMENT_3D ( 'NONE', #28450, #8845, #1351 ) ;
#26556=DIRECTION ( 'NONE',  ( 0.000000000000000000, 0.000000000000000000, -1.000000000000000000 ) ) ;
#26559=ORIENTED_EDGE ( 'NONE', *, *, #49603, .F. ) ;
#26562=FACE_OUTER_BOUND ( 'NONE', #947, .T. ) ;
#26564=ORIENTED_EDGE ( 'NONE', *, *, #22316, .T. ) ;
#26566=LINE ( 'NONE', #46663, #37790 ) ;
#26567=ORIENTED_EDGE ( 'NONE', *, *, #46831, .T. ) ;
#26568=CARTESIAN_POINT ( 'NONE',  ( 1.091055626815042645, 3.346456692913386100, 0.9448818897637746295 ) ) ;
#26570=DIRECTION ( 'NONE',  ( 0.000000000000000000, 0.000000000000000000, 1.000000000000000000 ) ) ;
#26571=LINE ( 'NONE', #35342, #14849 ) ;
#26572=EDGE_LOOP ( 'NONE', ( #9670, #11183, #13064, #17477 ) ) ;
#26573=ORIENTED_EDGE ( 'NONE', *, *, #2252, .F. ) ;
#26574=CARTESIAN_POINT ( 'NONE',  ( -1.909347346926324462, 3.346456692913386100, 0.1574803149606286423 ) ) ;
#26576=DIRECTION ( 'NONE',  ( -3.469446951953613696E-16, 0.000000000000000000, -1.000000000000000000 ) ) ;
#26580=CARTESIAN_POINT ( 'NONE',  ( -1.091055626815042201, 3.346456692913386100, 0.4330708661417290162 ) ) ;
#26581=CARTESIAN_POINT ( 'NONE',  ( 0.5455278134075212115, 0.000000000000000000, 0.9448818897637746295 ) ) ;
#26583=CARTESIAN_POINT ( 'NONE',  ( 0.000000000000000000, 3.267716535433071279, -1.456692913385822630 ) ) ;
#26584=DIRECTION ( 'NONE',  ( -1.000000000000000000, -0.000000000000000000, -0.000000000000000000 ) ) ;
#26586=VERTEX_POINT ( 'NONE', #37595 ) ;
#26587=DIRECTION ( 'NONE',  ( 1.734723475976806848E-16, 0.000000000000000000, 1.000000000000000000 ) ) ;
#26589=LINE ( 'NONE', #14216, #49221 ) ;
#26590=ORIENTED_EDGE ( 'NONE', *, *, #38815, .F. ) ;
#26591=VECTOR ( 'NONE', #12332, 39.37007874015748143 ) ;
#26592=EDGE_CURVE ( 'NONE', #33429, #5817, #33216, .T. ) ;
#26593=ORIENTED_EDGE ( 'NONE', *, *, #33689, .F. ) ;
#26594=CARTESIAN_POINT ( 'NONE',  ( -1.091055626815042645, 0.000000000000000000, 2.204724409448808764 ) ) ;
#26595=VECTOR ( 'NONE', #13490, 39.37007874015748143 ) ;
#26596=ORIENTED_EDGE ( 'NONE', *, *, #1904, .T. ) ;
#26597=EDGE_CURVE ( 'NONE', #44234, #27935, #21332, .T. ) ;
#26598=VECTOR ( 'NONE', #1627, 39.37007874015748143 ) ;
#26599=AXIS2_PLACEMENT_3D ( 'NONE', #13193, #17321, #12668 ) ;
#26601=CARTESIAN_POINT ( 'NONE',  ( 0.8182917201112819283, 3.267716535433071279, -1.419509857074483292E-16 ) ) ;
#26604=EDGE_LOOP ( 'NONE', ( #21367, #26903, #30415, #49518 ) ) ;
#26607=ORIENTED_EDGE ( 'NONE', *, *, #27974, .F. ) ;
#26608=EDGE_LOOP ( 'NONE', ( #34669, #45441, #49331, #29684 ) ) ;
#26611=FACE_OUTER_BOUND ( 'NONE', #30008, .T. ) ;
#26617=PLANE ( 'NONE',  #5557 ) ;
#26618=VERTEX_POINT ( 'NONE', #45303 ) ;
#26619=CARTESIAN_POINT ( 'NONE',  ( -1.363819533518803473, 0.000000000000000000, -1.417322834645664109 ) ) ;
#26621=ORIENTED_EDGE ( 'NONE', *, *, #20433, .F. ) ;
#26624=DIRECTION ( 'NONE',  ( 0.000000000000000000, 0.000000000000000000, -1.000000000000000000 ) ) ;
#26625=CARTESIAN_POINT ( 'NONE',  ( -0.6214413264104945434, 0.000000000000000000, -0.1574803149606301411 ) ) ;
#26626=EDGE_CURVE ( 'NONE', #1213, #27411, #5833, .T. ) ;
#26627=DIRECTION ( 'NONE',  ( 1.000000000000000000, -0.000000000000000000, 0.000000000000000000 ) ) ;
#26629=VERTEX_POINT ( 'NONE', #41712 ) ;
#26630=VERTEX_POINT ( 'NONE', #48645 ) ;
#26631=VECTOR ( 'NONE', #28261, 39.37007874015748143 ) ;
#26632=DIRECTION ( 'NONE',  ( 1.734723475976806848E-16, 0.000000000000000000, 1.000000000000000000 ) ) ;
#26636=ADVANCED_FACE ( 'NONE', ( #13589 ), #2221, .F. ) ;
#26638=AXIS2_PLACEMENT_3D ( 'NONE', #42625, #38762, #3139 ) ;
#26639=AXIS2_PLACEMENT_3D ( 'NONE', #20085, #32504, #13131 ) ;
#26640=DIRECTION ( 'NONE',  ( -0.000000000000000000, 1.000000000000000000, -0.000000000000000000 ) ) ;
#26641=LINE ( 'NONE', #42135, #12035 ) ;
#26642=DIRECTION ( 'NONE',  ( 0.000000000000000000, 0.000000000000000000, -1.000000000000000000 ) ) ;
#26644=CARTESIAN_POINT ( 'NONE',  ( -0.5455278134075214336, 0.000000000000000000, -1.889763779527552146 ) ) ;
#26645=EDGE_CURVE ( 'NONE', #35815, #25253, #6084, .T. ) ;
#26646=DIRECTION ( 'NONE',  ( -3.469446951953613696E-16, 0.000000000000000000, -1.000000000000000000 ) ) ;
#26648=ORIENTED_EDGE ( 'NONE', *, *, #1655, .F. ) ;
#26650=DIRECTION ( 'NONE',  ( -1.000000000000000000, 0.000000000000000000, 1.734723475976806848E-16 ) ) ;
#26652=ORIENTED_EDGE ( 'NONE', *, *, #31505, .F. ) ;
#26653=DIRECTION ( 'NONE',  ( -0.000000000000000000, 1.000000000000000000, -0.000000000000000000 ) ) ;
#26655=CARTESIAN_POINT ( 'NONE',  ( 1.015142113812069313, 0.000000000000000000, 0.4724409448818868706 ) ) ;
#26656=ORIENTED_EDGE ( 'NONE', *, *, #31159, .T. ) ;
#26658=EDGE_LOOP ( 'NONE', ( #41411, #6482, #46230, #11269 ) ) ;
#26661=DIRECTION ( 'NONE',  ( -0.000000000000000000, 1.000000000000000000, -0.000000000000000000 ) ) ;
#26663=EDGE_CURVE ( 'NONE', #37648, #43368, #46810, .T. ) ;
#26664=ORIENTED_EDGE ( 'NONE', *, *, #33205, .T. ) ;
#26665=AXIS2_PLACEMENT_3D ( 'NONE', #46216, #26116, #41866 ) ;
#26666=ORIENTED_EDGE ( 'NONE', *, *, #31680, .T. ) ;
#26668=DIRECTION ( 'NONE',  ( 1.000000000000000000, 0.000000000000000000, 0.000000000000000000 ) ) ;
#26669=DIRECTION ( 'NONE',  ( 1.000000000000000000, 0.000000000000000000, 0.000000000000000000 ) ) ;
#26670=ORIENTED_EDGE ( 'NONE', *, *, #164, .F. ) ;
#26671=AXIS2_PLACEMENT_3D ( 'NONE', #31610, #3485, #42211 ) ;
#26672=DIRECTION ( 'NONE',  ( 0.000000000000000000, 0.000000000000000000, 1.000000000000000000 ) ) ;
#26674=CARTESIAN_POINT ( 'NONE',  ( -0.8182917201112814842, 3.346456692913386100, 1.535433070866133898 ) ) ;
#26676=VECTOR ( 'NONE', #10521, 39.37007874015748143 ) ;
#26677=EDGE_LOOP ( 'NONE', ( #37419, #1993, #22105, #33857 ) ) ;
#26680=DIRECTION ( 'NONE',  ( -3.469446951953613696E-16, 0.000000000000000000, -1.000000000000000000 ) ) ;
#26682=EDGE_LOOP ( 'NONE', ( #29208, #25474, #14926, #26446 ) ) ;
#26684=FACE_BOUND ( 'NONE', #3015, .T. ) ;
#26686=ORIENTED_EDGE ( 'NONE', *, *, #50594, .T. ) ;
#26687=CARTESIAN_POINT ( 'NONE',  ( 2.182111253630085290, 3.346456692913386100, -0.1968503937007886062 ) ) ;
#26688=VERTEX_POINT ( 'NONE', #30854 ) ;
#26689=ORIENTED_EDGE ( 'NONE', *, *, #42330, .F. ) ;
#26690=CARTESIAN_POINT ( 'NONE',  ( 0.7423782071083084855, 3.346456692913386100, -1.889763779527552812 ) ) ;
#26691=CARTESIAN_POINT ( 'NONE',  ( 0.000000000000000000, 3.267716535433071279, -1.141732283464564013 ) ) ;
#26693=EDGE_CURVE ( 'NONE', #42860, #28536, #27217, .T. ) ;
#26694=CARTESIAN_POINT ( 'NONE',  ( 0.4696143004045479352, 0.000000000000000000, 0.4724409448818868706 ) ) ;
#26696=ORIENTED_EDGE ( 'NONE', *, *, #9069, .F. ) ;
#26697=EDGE_LOOP ( 'NONE', ( #21258, #40566, #21490, #7432 ) ) ;
#26698=DIRECTION ( 'NONE',  ( -0.000000000000000000, 1.000000000000000000, -0.000000000000000000 ) ) ;
#26699=EDGE_CURVE ( 'NONE', #13594, #30262, #14855, .T. ) ;
#26700=CARTESIAN_POINT ( 'NONE',  ( -1.439733046521776361, 0.000000000000000000, 1.062992125984246083 ) ) ;
#26701=EDGE_CURVE ( 'NONE', #43417, #47601, #50658, .T. ) ;
#26705=FACE_OUTER_BOUND ( 'NONE', #45314, .T. ) ;
#26706=VERTEX_POINT ( 'NONE', #38353 ) ;
#26707=AXIS2_PLACEMENT_3D ( 'NONE', #13573, #44787, #5307 ) ;
#26709=EDGE_CURVE ( 'NONE', #37439, #6627, #50411, .T. ) ;
#26710=VECTOR ( 'NONE', #13780, 39.37007874015748143 ) ;
#26711=LINE ( 'NONE', #42458, #32280 ) ;
#26712=VECTOR ( 'NONE', #8376, 39.37007874015748143 ) ;
#26713=VECTOR ( 'NONE', #18089, 39.37007874015748143 ) ;
#26715=LINE ( 'NONE', #15099, #10033 ) ;
#26716=FACE_OUTER_BOUND ( 'NONE', #38692, .T. ) ;
#26720=VECTOR ( 'NONE', #33849, 39.37007874015748143 ) ;
#26721=EDGE_LOOP ( 'NONE', ( #48806, #22925, #36973, #20912 ) ) ;
#26722=CARTESIAN_POINT ( 'NONE',  ( -0.3486774197067339376, 0.000000000000000000, 2.204724409448808764 ) ) ;
#26724=FACE_BOUND ( 'NONE', #39569, .T. ) ;
#26725=ADVANCED_FACE ( 'NONE', ( #23097 ), #18728, .F. ) ;
#26726=LINE ( 'NONE', #42473, #25987 ) ;
#26728=ADVANCED_FACE ( 'NONE', ( #39351 ), #3482, .F. ) ;
#26730=ORIENTED_EDGE ( 'NONE', *, *, #6683, .T. ) ;
#26732=EDGE_CURVE ( 'NONE', #37481, #16476, #23342, .T. ) ;
#26733=CARTESIAN_POINT ( 'NONE',  ( 0.5455278134075212115, 3.346456692913386100, -6.146657985744592735E-16 ) ) ;
#26737=FACE_OUTER_BOUND ( 'NONE', #40147, .T. ) ;
#26739=CARTESIAN_POINT ( 'NONE',  ( -2.082617625631827174, 3.346456692913386100, -0.3149606299212589500 ) ) ;
#26740=DIRECTION ( 'NONE',  ( -3.469446951953613696E-16, 0.000000000000000000, -1.000000000000000000 ) ) ;
#26741=AXIS2_PLACEMENT_3D ( 'NONE', #20984, #20467, #36229 ) ;
#26742=CARTESIAN_POINT ( 'NONE',  ( 3.927031490892378253E-16, 0.000000000000000000, 1.062992125984246083 ) ) ;
#26743=VECTOR ( 'NONE', #34215, 39.37007874015748143 ) ;
#26745=DIRECTION ( 'NONE',  ( -1.000000000000000000, 0.000000000000000000, 0.000000000000000000 ) ) ;
#26747=VERTEX_POINT ( 'NONE', #19465 ) ;
#26750=VECTOR ( 'NONE', #13140, 39.37007874015748143 ) ;
#26751=VERTEX_POINT ( 'NONE', #26962 ) ;
#26752=ORIENTED_EDGE ( 'NONE', *, *, #28395, .F. ) ;
#26754=VECTOR ( 'NONE', #44240, 39.37007874015748143 ) ;
#26755=DIRECTION ( 'NONE',  ( -0.000000000000000000, 1.000000000000000000, -0.000000000000000000 ) ) ;
#26756=CARTESIAN_POINT ( 'NONE',  ( 0.8182917201112819283, 0.000000000000000000, -1.299212598425193210 ) ) ;
#26761=PLANE ( 'NONE',  #23678 ) ;
#26763=ORIENTED_EDGE ( 'NONE', *, *, #6392, .T. ) ;
#26765=CARTESIAN_POINT ( 'NONE',  ( 0.7423782071083092626, 3.346456692913386100, 2.204724409448808764 ) ) ;
#26766=DIRECTION ( 'NONE',  ( 1.734723475976806848E-16, -0.000000000000000000, 1.000000000000000000 ) ) ;
#26767=PLANE ( 'NONE',  #12477 ) ;
#26768=ORIENTED_EDGE ( 'NONE', *, *, #11352, .T. ) ;
#26769=DIRECTION ( 'NONE',  ( -3.469446951953613696E-16, 0.000000000000000000, -1.000000000000000000 ) ) ;
#26770=PLANE ( 'NONE',  #21999 ) ;
#26771=ORIENTED_EDGE ( 'NONE', *, *, #9592, .T. ) ;
#26772=DIRECTION ( 'NONE',  ( -1.000000000000000000, 0.000000000000000000, 1.734723475976806848E-16 ) ) ;
#26773=DIRECTION ( 'NONE',  ( -0.000000000000000000, 0.000000000000000000, 1.000000000000000000 ) ) ;
#26774=VECTOR ( 'NONE', #22516, 39.37007874015748143 ) ;
#26776=DIRECTION ( 'NONE',  ( -0.000000000000000000, 0.000000000000000000, 1.000000000000000000 ) ) ;
#26777=EDGE_CURVE ( 'NONE', #19545, #37274, #6849, .T. ) ;
#26778=ORIENTED_EDGE ( 'NONE', *, *, #8111, .T. ) ;
#26779=CARTESIAN_POINT ( 'NONE',  ( 0.7423782071083085965, 3.346456692913386100, 0.1181102362204701633 ) ) ;
#26782=CARTESIAN_POINT ( 'NONE',  ( 1.363819533518803251, 0.000000000000000000, -0.9842519685039348154 ) ) ;
#26783=ADVANCED_FACE ( 'NONE', ( #26716 ), #42462, .F. ) ;
#26784=PLANE ( 'NONE',  #3677 ) ;
#26786=ORIENTED_EDGE ( 'NONE', *, *, #21441, .T. ) ;
#26788=CARTESIAN_POINT ( 'NONE',  ( -1.091055626815042645, 0.000000000000000000, -0.9448818897637760728 ) ) ;
#26789=VECTOR ( 'NONE', #19879, 39.37007874015748143 ) ;
#26790=EDGE_LOOP ( 'NONE', ( #39398, #46446, #9155, #40268 ) ) ;
#26795=FACE_OUTER_BOUND ( 'NONE', #25734, .T. ) ;
#26796=CARTESIAN_POINT ( 'NONE',  ( -2.182111253630085290, 3.346456692913386100, -0.3149606299212589500 ) ) ;
#26797=ORIENTED_EDGE ( 'NONE', *, *, #34288, .T. ) ;
#26798=CARTESIAN_POINT ( 'NONE',  ( 1.271755610052043295, 3.267716535433071279, -2.086614173228339641 ) ) ;
#26799=CARTESIAN_POINT ( 'NONE',  ( 0.000000000000000000, 3.346456692913386100, 0.000000000000000000 ) ) ;
#26802=ORIENTED_EDGE ( 'NONE', *, *, #45928, .F. ) ;
#26804=FACE_BOUND ( 'NONE', #40467, .T. ) ;
#26805=ORIENTED_EDGE ( 'NONE', *, *, #4647, .F. ) ;
#26807=VERTEX_POINT ( 'NONE', #35482 ) ;
#26809=DIRECTION ( 'NONE',  ( -1.000000000000000000, 0.000000000000000000, 1.734723475976806848E-16 ) ) ;
#26810=VECTOR ( 'NONE', #25000, 39.37007874015748143 ) ;
#26814=ORIENTED_EDGE ( 'NONE', *, *, #17152, .T. ) ;
#26815=DIRECTION ( 'NONE',  ( -3.469446951953613696E-16, 0.000000000000000000, -1.000000000000000000 ) ) ;
#26816=EDGE_LOOP ( 'NONE', ( #38210, #26053, #14173, #7059 ) ) ;
#26817=DIRECTION ( 'NONE',  ( 0.000000000000000000, 0.000000000000000000, -1.000000000000000000 ) ) ;
#26818=CARTESIAN_POINT ( 'NONE',  ( 1.909347346926324684, 0.000000000000000000, -0.4724409448818889246 ) ) ;
#26819=DIRECTION ( 'NONE',  ( -3.469446951953613696E-16, 0.000000000000000000, -1.000000000000000000 ) ) ;
#26820=VERTEX_POINT ( 'NONE', #102 ) ;
#26821=ORIENTED_EDGE ( 'NONE', *, *, #40326, .T. ) ;
#26824=CARTESIAN_POINT ( 'NONE',  ( 0.1968503937007878568, 3.346456692913386100, 1.574803149606291974 ) ) ;
#26825=CARTESIAN_POINT ( 'NONE',  ( -1.909347346926324906, 3.346456692913386100, -0.6692913385826758654 ) ) ;
#26826=EDGE_CURVE ( 'NONE', #46112, #7183, #9132, .T. ) ;
#26827=CARTESIAN_POINT ( 'NONE',  ( -1.166969139818015977, 3.346456692913386100, -1.732283464566922726 ) ) ;
#26828=CARTESIAN_POINT ( 'NONE',  ( 0.8182917201112819283, 3.346456692913386100, -0.1574803149606301411 ) ) ;
#26830=DIRECTION ( 'NONE',  ( -3.469446951953613696E-16, 0.000000000000000000, -1.000000000000000000 ) ) ;
#26833=ORIENTED_EDGE ( 'NONE', *, *, #21998, .F. ) ;
#26834=DIRECTION ( 'NONE',  ( -1.000000000000000000, -0.000000000000000000, -0.000000000000000000 ) ) ;
#26835=CARTESIAN_POINT ( 'NONE',  ( -0.8182917201112814842, 3.346456692913386100, 1.102362204724404160 ) ) ;
#26836=ORIENTED_EDGE ( 'NONE', *, *, #2056, .T. ) ;
#26837=ORIENTED_EDGE ( 'NONE', *, *, #43048, .F. ) ;
#26838=CARTESIAN_POINT ( 'NONE',  ( 0.2727639067037604392, 3.346456692913386100, -1.299212598425193210 ) ) ;
#26839=DIRECTION ( 'NONE',  ( -0.000000000000000000, 1.000000000000000000, -0.000000000000000000 ) ) ;
#26841=ORIENTED_EDGE ( 'NONE', *, *, #15085, .F. ) ;
#26842=VECTOR ( 'NONE', #29592, 39.37007874015748143 ) ;
#26843=ADVANCED_FACE ( 'NONE', ( #43462 ), #622, .F. ) ;
#26844=ORIENTED_EDGE ( 'NONE', *, *, #19626, .F. ) ;
#26845=CARTESIAN_POINT ( 'NONE',  ( 0.5455278134075208785, 3.267716535433071279, -2.034427629037600660 ) ) ;
#26846=AXIS2_PLACEMENT_3D ( 'NONE', #9157, #44513, #19992 ) ;
#26847=ORIENTED_EDGE ( 'NONE', *, *, #3477, .T. ) ;
#26848=DIRECTION ( 'NONE',  ( 1.000000000000000000, 0.000000000000000000, 0.000000000000000000 ) ) ;
#26851=ORIENTED_EDGE ( 'NONE', *, *, #17947, .T. ) ;
#26854=VERTEX_POINT ( 'NONE', #15847 ) ;
#26855=ORIENTED_EDGE ( 'NONE', *, *, #39021, .T. ) ;
#26860=CARTESIAN_POINT ( 'NONE',  ( -0.2727639067037607723, 3.267716535433071279, -0.7874015748031470974 ) ) ;
#26861=CARTESIAN_POINT ( 'NONE',  ( 1.363819533518803251, 3.346456692913386100, -0.4724409448818889246 ) ) ;
#26862=ORIENTED_EDGE ( 'NONE', *, *, #13225, .T. ) ;
#26864=ORIENTED_EDGE ( 'NONE', *, *, #37744, .T. ) ;
#26867=LINE ( 'NONE', #27630, #409 ) ;
#26869=VECTOR ( 'NONE', #21506, 39.37007874015748143 ) ;
#26870=LINE ( 'NONE', #37762, #9662 ) ;
#26871=CARTESIAN_POINT ( 'NONE',  ( -0.8182917201112814842, 3.346456692913386100, 1.732283464566921172 ) ) ;
#26873=ORIENTED_EDGE ( 'NONE', *, *, #12254, .F. ) ;
#26875=VECTOR ( 'NONE', #31144, 39.37007874015748143 ) ;
#26878=DIRECTION ( 'NONE',  ( -3.469446951953613696E-16, 0.000000000000000000, -1.000000000000000000 ) ) ;
#26879=ORIENTED_EDGE ( 'NONE', *, *, #29921, .F. ) ;
#26880=DIRECTION ( 'NONE',  ( 1.734723475976806848E-16, -0.000000000000000000, 1.000000000000000000 ) ) ;
#26881=CARTESIAN_POINT ( 'NONE',  ( -0.5455278134075214336, 0.000000000000000000, -0.1968503937007883287 ) ) ;
#26882=AXIS2_PLACEMENT_3D ( 'NONE', #30305, #11189, #39055 ) ;
#26885=VECTOR ( 'NONE', #21402, 39.37007874015748143 ) ;
#26886=EDGE_CURVE ( 'NONE', #15755, #48506, #47566, .T. ) ;
#26888=DIRECTION ( 'NONE',  ( -1.000000000000000000, 0.000000000000000000, 1.734723475976806848E-16 ) ) ;
#26889=LINE ( 'NONE', #38030, #32001 ) ;
#26890=AXIS2_PLACEMENT_3D ( 'NONE', #14874, #22368, #25729 ) ;
#26892=CARTESIAN_POINT ( 'NONE',  ( 1.909347346926324684, 0.000000000000000000, -0.4724409448818889246 ) ) ;
#26893=LINE ( 'NONE', #27147, #7076 ) ;
#26894=CARTESIAN_POINT ( 'NONE',  ( -0.07591351300297340121, 3.267716535433071279, 0.2755905511810995412 ) ) ;
#26895=EDGE_LOOP ( 'NONE', ( #28087, #43822, #37712, #2331 ) ) ;
#26896=CARTESIAN_POINT ( 'NONE',  ( 0.5455278134075217666, 0.000000000000000000, 1.259842519685033357 ) ) ;
#26898=ADVANCED_FACE ( 'NONE', ( #16113 ), #28745, .F. ) ;
#26901=LINE ( 'NONE', #42652, #13533 ) ;
#26902=EDGE_CURVE ( 'NONE', #37337, #23253, #31872, .T. ) ;
#26903=ORIENTED_EDGE ( 'NONE', *, *, #37539, .F. ) ;
#26904=LINE ( 'NONE', #34916, #20484 ) ;
#26906=B_SPLINE_CURVE_WITH_KNOTS ( 'NONE', 3,
 ( #50628, #19432, #47537, #31579 ),
 .UNSPECIFIED., .F., .F.,
 ( 4, 4 ),
 ( 0.02719747141717294286, 0.02819803343359124012 ),
 .UNSPECIFIED. ) ;
#26909=CARTESIAN_POINT ( 'NONE',  ( -1.636583440222564301, 3.267716535433071279, -0.3149606299212592275 ) ) ;
#26910=FACE_OUTER_BOUND ( 'NONE', #46949, .T. ) ;
#26911=DIRECTION ( 'NONE',  ( -1.000000000000000000, 0.000000000000000000, 1.734723475976806848E-16 ) ) ;
#26912=EDGE_CURVE ( 'NONE', #47979, #24374, #40121, .T. ) ;
#26914=VERTEX_POINT ( 'NONE', #24631 ) ;
#26916=VERTEX_POINT ( 'NONE', #17644 ) ;
#26919=CARTESIAN_POINT ( 'NONE',  ( -0.5145850802035816240, 3.241398795825266355, -2.401574803149598036 ) ) ;
#26920=VECTOR ( 'NONE', #41952, 39.37007874015748143 ) ;
#26921=ORIENTED_EDGE ( 'NONE', *, *, #39480, .F. ) ;
#26922=ORIENTED_EDGE ( 'NONE', *, *, #18510, .F. ) ;
#26924=DIRECTION ( 'NONE',  ( 1.000000000000000000, 0.000000000000000000, 0.000000000000000000 ) ) ;
#26925=FACE_OUTER_BOUND ( 'NONE', #12156, .T. ) ;
#26926=EDGE_CURVE ( 'NONE', #30123, #34792, #6019, .T. ) ;
#26927=VERTEX_POINT ( 'NONE', #33413 ) ;
#26929=CARTESIAN_POINT ( 'NONE',  ( -1.909347346926324462, 3.346456692913386100, 0.9055118110236167750 ) ) ;
#26931=VECTOR ( 'NONE', #12538, 39.37007874015748143 ) ;
#26932=FACE_OUTER_BOUND ( 'NONE', #40981, .T. ) ;
#26933=VERTEX_POINT ( 'NONE', #30024 ) ;
#26935=CARTESIAN_POINT ( 'NONE',  ( 1.091055626815042645, 0.000000000000000000, 0.3149606299212578953 ) ) ;
#26938=CARTESIAN_POINT ( 'NONE',  ( -0.8182917201112814842, 0.000000000000000000, 0.5905511811023582691 ) ) ;
#26939=EDGE_LOOP ( 'NONE', ( #37004, #7496, #31343, #33747 ) ) ;
#26940=ORIENTED_EDGE ( 'NONE', *, *, #25978, .F. ) ;
#26941=DIRECTION ( 'NONE',  ( 1.000000000000000000, 0.000000000000000000, 0.000000000000000000 ) ) ;
#26942=DIRECTION ( 'NONE',  ( -3.469446951953613696E-16, 0.000000000000000000, -1.000000000000000000 ) ) ;
#26944=FACE_OUTER_BOUND ( 'NONE', #42675, .T. ) ;
#26946=ORIENTED_EDGE ( 'NONE', *, *, #8137, .F. ) ;
#26947=ORIENTED_EDGE ( 'NONE', *, *, #27520, .T. ) ;
#26948=CARTESIAN_POINT ( 'NONE',  ( -1.363819533518803473, 0.000000000000000000, -0.3543307086614174151 ) ) ;
#26949=LINE ( 'NONE', #26450, #27581 ) ;
#26951=EDGE_CURVE ( 'NONE', #814, #45623, #5254, .T. ) ;
#26955=LINE ( 'NONE', #7352, #41877 ) ;
#26956=VECTOR ( 'NONE', #11776, 39.37007874015748143 ) ;
#26958=PLANE ( 'NONE',  #31628 ) ;
#26959=DIRECTION ( 'NONE',  ( 1.000000000000000000, -0.000000000000000000, 0.000000000000000000 ) ) ;
#26961=DIRECTION ( 'NONE',  ( -3.469446951953613696E-16, 0.000000000000000000, -1.000000000000000000 ) ) ;
#26962=CARTESIAN_POINT ( 'NONE',  ( -0.8942052331142552601, 3.267716535433071279, -1.889763779527552146 ) ) ;
#26963=CARTESIAN_POINT ( 'NONE',  ( -1.909347346926324462, 3.346456692913386100, 0.2755905511810996522 ) ) ;
#26964=LINE ( 'NONE', #19219, #23430 ) ;
#26965=DIRECTION ( 'NONE',  ( -3.469446951953613696E-16, 0.000000000000000000, -1.000000000000000000 ) ) ;
#26967=EDGE_LOOP ( 'NONE', ( #39071, #50239, #1335, #446 ) ) ;
#26968=CARTESIAN_POINT ( 'NONE',  ( 0.7423782071083087075, 3.346456692913386100, -0.6299212598425181220 ) ) ;
#26970=VECTOR ( 'NONE', #10262, 39.37007874015748143 ) ;
#26971=DIRECTION ( 'NONE',  ( 1.000000000000000000, -0.000000000000000000, 0.000000000000000000 ) ) ;
#26972=DIRECTION ( 'NONE',  ( -0.000000000000000000, 1.000000000000000000, -0.000000000000000000 ) ) ;
#26973=CARTESIAN_POINT ( 'NONE',  ( -1.091055626815042645, 3.346456692913386100, -0.6299212598425177889 ) ) ;
#26975=ORIENTED_EDGE ( 'NONE', *, *, #50962, .F. ) ;
#26976=VERTEX_POINT ( 'NONE', #37022 ) ;
#26977=FACE_OUTER_BOUND ( 'NONE', #8259, .T. ) ;
#26979=CARTESIAN_POINT ( 'NONE',  ( -0.2727639067037610499, 3.346456692913386100, -2.047244094488181343 ) ) ;
#26981=CARTESIAN_POINT ( 'NONE',  ( 0.000000000000000000, 3.267716535433071279, 1.220472440944875059 ) ) ;
#26982=ADVANCED_FACE ( 'NONE', ( #32905 ), #41149, .F. ) ;
#26984=ORIENTED_EDGE ( 'NONE', *, *, #4351, .T. ) ;
#26987=VECTOR ( 'NONE', #4204, 39.37007874015748143 ) ;
#26989=CIRCLE ( 'NONE', #18753, 2.165354330708661568 ) ;
#26992=ADVANCED_FACE ( 'NONE', ( #17899 ), #1896, .F. ) ;
#26994=ORIENTED_EDGE ( 'NONE', *, *, #10772, .T. ) ;
#26995=ORIENTED_EDGE ( 'NONE', *, *, #47070, .F. ) ;
#26996=EDGE_CURVE ( 'NONE', #16457, #14773, #49598, .T. ) ;
#26998=EDGE_LOOP ( 'NONE', ( #37978, #34189, #38948, #38354 ) ) ;
#27000=VECTOR ( 'NONE', #10208, 39.37007874015748143 ) ;
#27001=PLANE ( 'NONE',  #1515 ) ;
#27004=EDGE_CURVE ( 'NONE', #27036, #4710, #45491, .T. ) ;
#27005=FACE_OUTER_BOUND ( 'NONE', #43998, .T. ) ;
#27007=EDGE_CURVE ( 'NONE', #39256, #43417, #48836, .T. ) ;
#27008=PLANE ( 'NONE',  #25343 ) ;
#27010=ORIENTED_EDGE ( 'NONE', *, *, #49492, .T. ) ;
#27012=CARTESIAN_POINT ( 'NONE',  ( -0.2727639067037602727, 3.346456692913386100, 0.5905511811023582691 ) ) ;
#27013=CARTESIAN_POINT ( 'NONE',  ( 0.000000000000000000, 3.267716535433071279, -0.3149606299212593941 ) ) ;
#27015=ORIENTED_EDGE ( 'NONE', *, *, #23277, .F. ) ;
#27016=DIRECTION ( 'NONE',  ( -0.000000000000000000, 0.000000000000000000, 1.000000000000000000 ) ) ;
#27018=ORIENTED_EDGE ( 'NONE', *, *, #6503, .T. ) ;
#27021=AXIS2_PLACEMENT_3D ( 'NONE', #26782, #22419, #18034 ) ;
#27022=LINE ( 'NONE', #165, #10284 ) ;
#27023=AXIS2_PLACEMENT_3D ( 'NONE', #42858, #31260, #46954 ) ;
#27024=DIRECTION ( 'NONE',  ( -1.000000000000000000, 0.000000000000000000, 0.000000000000000000 ) ) ;
#27025=ORIENTED_EDGE ( 'NONE', *, *, #43702, .F. ) ;
#27028=VECTOR ( 'NONE', #36005, 39.37007874015748143 ) ;
#27031=DIRECTION ( 'NONE',  ( 0.000000000000000000, 0.000000000000000000, 1.000000000000000000 ) ) ;
#27032=ORIENTED_EDGE ( 'NONE', *, *, #32761, .T. ) ;
#27033=ADVANCED_FACE ( 'NONE', ( #17140 ), #25895, .F. ) ;
#27036=VERTEX_POINT ( 'NONE', #40887 ) ;
#27037=ORIENTED_EDGE ( 'NONE', *, *, #9130, .F. ) ;
#27038=DIRECTION ( 'NONE',  ( -0.000000000000000000, 1.000000000000000000, -0.000000000000000000 ) ) ;
#27039=ORIENTED_EDGE ( 'NONE', *, *, #5558, .T. ) ;
#27041=AXIS2_PLACEMENT_3D ( 'NONE', #5507, #14267, #21257 ) ;
#27043=EDGE_LOOP ( 'NONE', ( #6513, #10045, #23618, #5032 ) ) ;
#27045=CARTESIAN_POINT ( 'NONE',  ( 4.268512490100411402E-16, 0.000000000000000000, 0.9448818897637749625 ) ) ;
#27047=ORIENTED_EDGE ( 'NONE', *, *, #8592, .F. ) ;
#27050=ORIENTED_EDGE ( 'NONE', *, *, #24103, .F. ) ;
#27051=ORIENTED_EDGE ( 'NONE', *, *, #49234, .F. ) ;
#27053=ORIENTED_EDGE ( 'NONE', *, *, #12467, .F. ) ;
#27054=LINE ( 'NONE', #18570, #44320 ) ;
#27055=CIRCLE ( 'NONE', #4821, 2.106299212598425008 ) ;
#27057=ORIENTED_EDGE ( 'NONE', *, *, #37328, .F. ) ;
#27059=DIRECTION ( 'NONE',  ( 1.000000000000000000, -0.000000000000000000, 0.000000000000000000 ) ) ;
#27064=DIRECTION ( 'NONE',  ( 1.000000000000000000, 0.000000000000000000, 0.000000000000000000 ) ) ;
#27066=LINE ( 'NONE', #31461, #3789 ) ;
#27067=CARTESIAN_POINT ( 'NONE',  ( -1.909347346926324906, 3.267716535433071279, 1.220472440944875059 ) ) ;
#27068=AXIS2_PLACEMENT_3D ( 'NONE', #49036, #21211, #40831 ) ;
#27069=CARTESIAN_POINT ( 'NONE',  ( 0.1968503937007878568, 3.346456692913386100, 1.574803149606291974 ) ) ;
#27072=ORIENTED_EDGE ( 'NONE', *, *, #16505, .T. ) ;
#27073=EDGE_LOOP ( 'NONE', ( #7559, #8903, #45650, #48986 ) ) ;
#27077=CARTESIAN_POINT ( 'NONE',  ( -1.091055626815042645, 3.267716535433071279, -1.574803149606293529 ) ) ;
#27078=VECTOR ( 'NONE', #39415, 39.37007874015748143 ) ;
#27079=LINE ( 'NONE', #46923, #17757 ) ;
#27082=VECTOR ( 'NONE', #28606, 39.37007874015748143 ) ;
#27083=CARTESIAN_POINT ( 'NONE',  ( -2.430161915918442439, 3.241492618072995047, -0.3543307086614173040 ) ) ;
#27084=DIRECTION ( 'NONE',  ( 1.000000000000000000, 0.000000000000000000, 0.000000000000000000 ) ) ;
#27085=EDGE_LOOP ( 'NONE', ( #29426, #6979, #16151, #25958 ) ) ;
#27086=CARTESIAN_POINT ( 'NONE',  ( 0.000000000000000000, 3.267716535433071279, -1.141732283464563791 ) ) ;
#27088=EDGE_LOOP ( 'NONE', ( #267, #24609, #17719, #22161 ) ) ;
#27089=ORIENTED_EDGE ( 'NONE', *, *, #22295, .F. ) ;
#27090=LINE ( 'NONE', #39483, #21748 ) ;
#27091=CARTESIAN_POINT ( 'NONE',  ( 2.378961647330872786, 3.346456692913386100, -0.5118110236220471121 ) ) ;
#27092=VECTOR ( 'NONE', #121, 39.37007874015748143 ) ;
#27093=VERTEX_POINT ( 'NONE', #42146 ) ;
#27094=LINE ( 'NONE', #7736, #46038 ) ;
#27095=ORIENTED_EDGE ( 'NONE', *, *, #35407, .T. ) ;
#27096=DIRECTION ( 'NONE',  ( 1.000000000000000000, 0.000000000000000000, 0.000000000000000000 ) ) ;
#27097=VERTEX_POINT ( 'NONE', #15038 ) ;
#27098=AXIS2_PLACEMENT_3D ( 'NONE', #20973, #32607, #48292 ) ;
#27099=AXIS2_PLACEMENT_3D ( 'NONE', #9023, #24771, #1273 ) ;
#27102=EDGE_CURVE ( 'NONE', #9419, #8409, #46988, .T. ) ;
#27104=VECTOR ( 'NONE', #28923, 39.37007874015748143 ) ;
#27105=ORIENTED_EDGE ( 'NONE', *, *, #6758, .F. ) ;
#27107=CARTESIAN_POINT ( 'NONE',  ( 0.2727639067037604392, 3.267716535433071279, -0.6692913385826760875 ) ) ;
#27108=EDGE_CURVE ( 'NONE', #9748, #2103, #7294, .T. ) ;
#27109=ORIENTED_EDGE ( 'NONE', *, *, #33293, .T. ) ;
#27110=ORIENTED_EDGE ( 'NONE', *, *, #27754, .F. ) ;
#27112=LINE ( 'NONE', #37046, #3424 ) ;
#27115=ORIENTED_EDGE ( 'NONE', *, *, #22322, .T. ) ;
#27116=CARTESIAN_POINT ( 'NONE',  ( -0.2727639067037607168, 3.267716535433071279, 4.731699523581612206E-17 ) ) ;
#27117=CARTESIAN_POINT ( 'NONE',  ( -1.091055626815042645, 3.267716535433071279, 1.892679809432644882E-16 ) ) ;
#27118=ORIENTED_EDGE ( 'NONE', *, *, #7210, .T. ) ;
#27119=CARTESIAN_POINT ( 'NONE',  ( 0.000000000000000000, 3.267716535433071279, 0.7480314960629872445 ) ) ;
#27121=ORIENTED_EDGE ( 'NONE', *, *, #41175, .T. ) ;
#27122=ORIENTED_EDGE ( 'NONE', *, *, #44697, .T. ) ;
#27124=VERTEX_POINT ( 'NONE', #19152 ) ;
#27127=ADVANCED_FACE ( 'NONE', ( #15289 ), #15544, .F. ) ;
#27128=VECTOR ( 'NONE', #2172, 39.37007874015748143 ) ;
#27129=CARTESIAN_POINT ( 'NONE',  ( -1.091055626815042645, 0.000000000000000000, -2.086614173228339641 ) ) ;
#27130=CARTESIAN_POINT ( 'NONE',  ( 0.7423782071083087075, 3.267716535433071279, 0.6299212598425161236 ) ) ;
#27133=ORIENTED_EDGE ( 'NONE', *, *, #16465, .F. ) ;
#27134=EDGE_CURVE ( 'NONE', #27935, #25931, #34412, .T. ) ;
#27139=LINE ( 'NONE', #30771, #16922 ) ;
#27141=VECTOR ( 'NONE', #33918, 39.37007874015748143 ) ;
#27142=CARTESIAN_POINT ( 'NONE',  ( 0.4696143004045484903, 3.346456692913386100, 2.047244094488179567 ) ) ;
#27143=CARTESIAN_POINT ( 'NONE',  ( -0.8182917201112819283, 3.346456692913386100, -0.1574803149606301411 ) ) ;
#27144=DIRECTION ( 'NONE',  ( 0.000000000000000000, 1.000000000000000000, 0.000000000000000000 ) ) ;
#27146=LINE ( 'NONE', #26146, #48905 ) ;
#27147=CARTESIAN_POINT ( 'NONE',  ( 0.000000000000000000, 3.267716535433071279, -1.929133858267710000 ) ) ;
#27150=DIRECTION ( 'NONE',  ( -1.000000000000000000, -0.000000000000000000, -0.000000000000000000 ) ) ;
#27153=ORIENTED_EDGE ( 'NONE', *, *, #36299, .T. ) ;
#27154=ORIENTED_EDGE ( 'NONE', *, *, #45460, .F. ) ;
#27158=DIRECTION ( 'NONE',  ( -3.469446951953613696E-16, 0.000000000000000000, -1.000000000000000000 ) ) ;
#27159=ORIENTED_EDGE ( 'NONE', *, *, #15184, .T. ) ;
#27160=DIRECTION ( 'NONE',  ( -0.000000000000000000, 0.000000000000000000, 1.000000000000000000 ) ) ;
#27161=CARTESIAN_POINT ( 'NONE',  ( -0.2727639067037602172, 3.346456692913386100, 0.7874015748031456541 ) ) ;
#27162=FACE_OUTER_BOUND ( 'NONE', #39843, .T. ) ;
#27164=EDGE_LOOP ( 'NONE', ( #50943, #32899, #21099, #19413 ) ) ;
#27165=ADVANCED_FACE ( 'NONE', ( #50103 ), #46743, .F. ) ;
#27167=EDGE_LOOP ( 'NONE', ( #26038, #12630, #30869, #18612 ) ) ;
#27170=EDGE_CURVE ( 'NONE', #4133, #46268, #3665, .T. ) ;
#27171=ORIENTED_EDGE ( 'NONE', *, *, #3770, .F. ) ;
#27173=CARTESIAN_POINT ( 'NONE',  ( 0.000000000000000000, 3.267716535433071279, -0.4724409448818889246 ) ) ;
#27176=EDGE_CURVE ( 'NONE', #48689, #46386, #38539, .T. ) ;
#27177=EDGE_CURVE ( 'NONE', #34110, #47282, #14790, .T. ) ;
#27179=ORIENTED_EDGE ( 'NONE', *, *, #22601, .T. ) ;
#27180=ORIENTED_EDGE ( 'NONE', *, *, #10625, .F. ) ;
#27182=LINE ( 'NONE', #38569, #43941 ) ;
#27183=CARTESIAN_POINT ( 'NONE',  ( 1.363819533518803251, 3.346456692913386100, -0.7874015748031473194 ) ) ;
#27184=EDGE_CURVE ( 'NONE', #39372, #44367, #23282, .T. ) ;
#27187=CARTESIAN_POINT ( 'NONE',  ( 0.5455278134075216556, 0.000000000000000000, 1.377952755905504256 ) ) ;
#27188=ORIENTED_EDGE ( 'NONE', *, *, #39204, .F. ) ;
#27189=DIRECTION ( 'NONE',  ( -0.000000000000000000, 1.000000000000000000, -0.000000000000000000 ) ) ;
#27190=ORIENTED_EDGE ( 'NONE', *, *, #44999, .T. ) ;
#27192=VECTOR ( 'NONE', #50116, 39.37007874015748143 ) ;
#27195=CARTESIAN_POINT ( 'NONE',  ( 2.052631463899902364, 3.267716535433071279, 0.4724409448818868706 ) ) ;
#27196=EDGE_CURVE ( 'NONE', #8227, #16479, #7792, .T. ) ;
#27198=DIRECTION ( 'NONE',  ( 1.734723475976806848E-16, -0.000000000000000000, 1.000000000000000000 ) ) ;
#27199=VERTEX_POINT ( 'NONE', #47756 ) ;
#27200=ORIENTED_EDGE ( 'NONE', *, *, #2010, .T. ) ;
#27202=EDGE_LOOP ( 'NONE', ( #1465, #16064, #44820, #14586 ) ) ;
#27203=CARTESIAN_POINT ( 'NONE',  ( -1.909347346926324462, 0.000000000000000000, 0.5905511811023582691 ) ) ;
#27204=DIRECTION ( 'NONE',  ( -0.000000000000000000, 1.000000000000000000, -0.000000000000000000 ) ) ;
#27207=DIRECTION ( 'NONE',  ( 1.734723475976806848E-16, -0.000000000000000000, 1.000000000000000000 ) ) ;
#27211=EDGE_CURVE ( 'NONE', #37648, #47182, #8559, .T. ) ;
#27212=LINE ( 'NONE', #15351, #50343 ) ;
#27213=VECTOR ( 'NONE', #10515, 39.37007874015748143 ) ;
#27214=ORIENTED_EDGE ( 'NONE', *, *, #43191, .F. ) ;
#27216=VECTOR ( 'NONE', #40738, 39.37007874015748143 ) ;
#27217=LINE ( 'NONE', #35231, #7179 ) ;
#27219=CARTESIAN_POINT ( 'NONE',  ( 1.636583440222563857, 3.346456692913386100, 1.574803149606291974 ) ) ;
#27220=LINE ( 'NONE', #38356, #23350 ) ;
#27221=DIRECTION ( 'NONE',  ( 0.000000000000000000, 0.000000000000000000, -1.000000000000000000 ) ) ;
#27224=VECTOR ( 'NONE', #13162, 39.37007874015748143 ) ;
#27225=ORIENTED_EDGE ( 'NONE', *, *, #36722, .T. ) ;
#27227=CARTESIAN_POINT ( 'NONE',  ( 1.363819533518803251, 3.346456692913386100, 0.5905511811023579360 ) ) ;
#27228=LINE ( 'NONE', #30867, #36718 ) ;
#27230=ORIENTED_EDGE ( 'NONE', *, *, #9861, .F. ) ;
#27231=LINE ( 'NONE', #35248, #34754 ) ;
#27232=CARTESIAN_POINT ( 'NONE',  ( -1.091055626815042645, 3.346456692913386100, -0.3149606299212593941 ) ) ;
#27233=EDGE_CURVE ( 'NONE', #4317, #1599, #559, .T. ) ;
#27234=LINE ( 'NONE', #46827, #1958 ) ;
#27236=LINE ( 'NONE', #7630, #1366 ) ;
#27237=EDGE_CURVE ( 'NONE', #28536, #21352, #39541, .T. ) ;
#27238=DIRECTION ( 'NONE',  ( -1.000000000000000000, 0.000000000000000000, 1.734723475976806848E-16 ) ) ;
#27240=EDGE_CURVE ( 'NONE', #40680, #47575, #31546, .T. ) ;
#27241=LINE ( 'NONE', #31905, #22152 ) ;
#27242=LINE ( 'NONE', #34507, #24130 ) ;
#27244=LINE ( 'NONE', #15129, #14143 ) ;
#27247=VERTEX_POINT ( 'NONE', #47502 ) ;
#27250=VECTOR ( 'NONE', #14897, 39.37007874015748143 ) ;
#27251=AXIS2_PLACEMENT_3D ( 'NONE', #172, #11794, #4065 ) ;
#27252=EDGE_CURVE ( 'NONE', #44810, #28145, #20680, .T. ) ;
#27254=ORIENTED_EDGE ( 'NONE', *, *, #23074, .T. ) ;
#27255=CARTESIAN_POINT ( 'NONE',  ( 0.5455278134075217666, 3.346456692913386100, 2.204724409448808764 ) ) ;
#27256=EDGE_LOOP ( 'NONE', ( #32591, #39927, #7818, #22823 ) ) ;
#27257=ADVANCED_FACE ( 'NONE', ( #43655 ), #35929, .F. ) ;
#27258=VECTOR ( 'NONE', #26239, 39.37007874015748143 ) ;
#27260=DIRECTION ( 'NONE',  ( 1.000000000000000000, 0.000000000000000000, 0.000000000000000000 ) ) ;
#27263=DIRECTION ( 'NONE',  ( 1.000000000000000000, 0.000000000000000000, 0.000000000000000000 ) ) ;
#27265=DIRECTION ( 'NONE',  ( -3.469446951953613696E-16, 0.000000000000000000, -1.000000000000000000 ) ) ;
#27267=DIRECTION ( 'NONE',  ( -0.000000000000000000, 1.000000000000000000, -0.000000000000000000 ) ) ;
#27268=DIRECTION ( 'NONE',  ( -3.469446951953613696E-16, 0.000000000000000000, -1.000000000000000000 ) ) ;
#27269=LINE ( 'NONE', #43009, #50673 ) ;
#27270=ADVANCED_FACE ( 'NONE', ( #19654 ), #36444, .F. ) ;
#27272=ORIENTED_EDGE ( 'NONE', *, *, #43736, .F. ) ;
#27275=ORIENTED_EDGE ( 'NONE', *, *, #36350, .F. ) ;
#27276=LINE ( 'NONE', #46622, #32901 ) ;
#27281=CARTESIAN_POINT ( 'NONE',  ( -1.909347346926324906, 3.267716535433071279, 3.312189666507128668E-16 ) ) ;
#27282=ADVANCED_FACE ( 'NONE', ( #39 ), #12427, .F. ) ;
#27284=VECTOR ( 'NONE', #33531, 39.37007874015748143 ) ;
#27285=VECTOR ( 'NONE', #37491, 39.37007874015748143 ) ;
#27287=DIRECTION ( 'NONE',  ( -0.000000000000000000, 1.000000000000000000, -0.000000000000000000 ) ) ;
#27288=ORIENTED_EDGE ( 'NONE', *, *, #32144, .T. ) ;
#27289=ORIENTED_EDGE ( 'NONE', *, *, #31102, .T. ) ;
#27290=ORIENTED_EDGE ( 'NONE', *, *, #32995, .T. ) ;
#27291=LINE ( 'NONE', #20581, #19605 ) ;
#27292=VERTEX_POINT ( 'NONE', #36190 ) ;
#27294=CIRCLE ( 'NONE', #19080, 2.165354330708661568 ) ;
#27295=CARTESIAN_POINT ( 'NONE',  ( -1.363819533518803473, 3.346456692913386100, 1.732283464566920950 ) ) ;
#27297=EDGE_CURVE ( 'NONE', #49569, #40529, #48272, .T. ) ;
#27299=AXIS2_PLACEMENT_3D ( 'NONE', #28297, #16694, #8683 ) ;
#27301=CARTESIAN_POINT ( 'NONE',  ( -0.3486774197067334935, 3.267716535433071279, 1.062992125984246083 ) ) ;
#27302=EDGE_CURVE ( 'NONE', #11317, #30078, #24561, .T. ) ;
#27305=PLANE ( 'NONE',  #37272 ) ;
#27306=VERTEX_POINT ( 'NONE', #16046 ) ;
#27308=ORIENTED_EDGE ( 'NONE', *, *, #27878, .T. ) ;
#27309=ORIENTED_EDGE ( 'NONE', *, *, #33529, .T. ) ;
#27312=ORIENTED_EDGE ( 'NONE', *, *, #17875, .F. ) ;
#27313=DIRECTION ( 'NONE',  ( -1.000000000000000000, 0.000000000000000000, -0.000000000000000000 ) ) ;
#27317=LINE ( 'NONE', #11082, #18433 ) ;
#27319=ADVANCED_FACE ( 'NONE', ( #31805 ), #40322, .F. ) ;
#27322=ORIENTED_EDGE ( 'NONE', *, *, #31878, .T. ) ;
#27323=AXIS2_PLACEMENT_3D ( 'NONE', #14870, #30613, #46331 ) ;
#27324=PLANE ( 'NONE',  #17869 ) ;
#27325=CARTESIAN_POINT ( 'NONE',  ( -0.07591351300297284610, 0.000000000000000000, 1.850393700787392293 ) ) ;
#27326=LINE ( 'NONE', #18840, #6861 ) ;
#27327=CIRCLE ( 'NONE', #5088, 2.165354330708661568 ) ;
#27329=EDGE_CURVE ( 'NONE', #48815, #36606, #37214, .T. ) ;
#27331=VECTOR ( 'NONE', #36761, 39.37007874015748143 ) ;
#27332=EDGE_CURVE ( 'NONE', #25208, #37754, #21461, .T. ) ;
#27334=ORIENTED_EDGE ( 'NONE', *, *, #9534, .T. ) ;
#27335=EDGE_CURVE ( 'NONE', #41731, #19367, #32842, .T. ) ;
#27337=ORIENTED_EDGE ( 'NONE', *, *, #33400, .T. ) ;
#27340=ORIENTED_EDGE ( 'NONE', *, *, #17975, .T. ) ;
#27341=FACE_OUTER_BOUND ( 'NONE', #42407, .T. ) ;
#27342=LINE ( 'NONE', #43082, #40236 ) ;
#27344=ADVANCED_FACE ( 'NONE', ( #33605 ), #1583, .F. ) ;
#27346=EDGE_LOOP ( 'NONE', ( #33860, #11396, #48798, #12856 ) ) ;
#27347=CARTESIAN_POINT ( 'NONE',  ( 3.927031490892378253E-16, 3.346456692913386100, 1.692913385826762873 ) ) ;
#27348=ORIENTED_EDGE ( 'NONE', *, *, #38710, .T. ) ;
#27349=AXIS2_PLACEMENT_3D ( 'NONE', #50907, #47813, #20226 ) ;
#27350=EDGE_CURVE ( 'NONE', #26630, #1152, #22123, .T. ) ;
#27351=CARTESIAN_POINT ( 'NONE',  ( 0.4696143004045476022, 3.346456692913386100, -1.929133858267710000 ) ) ;
#27352=LINE ( 'NONE', #43094, #13243 ) ;
#27353=AXIS2_PLACEMENT_3D ( 'NONE', #35702, #330, #18944 ) ;
#27354=ADVANCED_FACE ( 'NONE', ( #5715 ), #20946, .F. ) ;
#27355=VERTEX_POINT ( 'NONE', #44675 ) ;
#27356=VECTOR ( 'NONE', #43420, 39.37007874015748143 ) ;
#27357=CARTESIAN_POINT ( 'NONE',  ( -1.363819533518803029, 3.346456692913386100, 0.4724409448818871482 ) ) ;
#27358=ORIENTED_EDGE ( 'NONE', *, *, #49196, .T. ) ;
#27361=VECTOR ( 'NONE', #41685, 39.37007874015748143 ) ;
#27362=DIRECTION ( 'NONE',  ( -3.469446951953613696E-16, 0.000000000000000000, -1.000000000000000000 ) ) ;
#27363=CARTESIAN_POINT ( 'NONE',  ( 0.000000000000000000, 3.267716535433071279, 1.102362204724404160 ) ) ;
#27364=VECTOR ( 'NONE', #34293, 39.37007874015748143 ) ;
#27367=DIRECTION ( 'NONE',  ( -3.469446951953613696E-16, 0.000000000000000000, -1.000000000000000000 ) ) ;
#27368=ORIENTED_EDGE ( 'NONE', *, *, #26409, .T. ) ;
#27369=CARTESIAN_POINT ( 'NONE',  ( -0.07591351300297333182, 3.346456692913386100, 2.362204724409437961 ) ) ;
#27370=EDGE_LOOP ( 'NONE', ( #8265, #42961, #21142, #10256 ) ) ;
#27374=CARTESIAN_POINT ( 'NONE',  ( -0.2727639067037608278, 3.346456692913386100, -0.9842519685039344823 ) ) ;
#27376=DIRECTION ( 'NONE',  ( 1.734723475976806848E-16, -0.000000000000000000, 1.000000000000000000 ) ) ;
#27378=ORIENTED_EDGE ( 'NONE', *, *, #11354, .F. ) ;
#27382=DIRECTION ( 'NONE',  ( 0.000000000000000000, 0.000000000000000000, 1.000000000000000000 ) ) ;
#27383=CARTESIAN_POINT ( 'NONE',  ( 2.182111253630085290, 3.267716535433071279, 0.3149606299212573401 ) ) ;
#27384=VECTOR ( 'NONE', #47469, 39.37007874015748143 ) ;
#27387=CARTESIAN_POINT ( 'NONE',  ( -1.363819533518803473, 3.346456692913386100, -1.732283464566922726 ) ) ;
#27388=EDGE_CURVE ( 'NONE', #31389, #23409, #50055, .T. ) ;
#27390=VECTOR ( 'NONE', #27809, 39.37007874015748143 ) ;
#27391=DIRECTION ( 'NONE',  ( -0.000000000000000000, 1.000000000000000000, -0.000000000000000000 ) ) ;
#27392=ORIENTED_EDGE ( 'NONE', *, *, #38383, .T. ) ;
#27394=CARTESIAN_POINT ( 'NONE',  ( -1.536664496436148184E-16, 3.267716535433071279, -0.5118110236220465570 ) ) ;
#27396=VECTOR ( 'NONE', #47539, 39.37007874015748143 ) ;
#27397=VERTEX_POINT ( 'NONE', #29458 ) ;
#27399=EDGE_LOOP ( 'NONE', ( #24002, #45952, #402, #5896 ) ) ;
#27400=ADVANCED_FACE ( 'NONE', ( #44430 ), #40569, .F. ) ;
#27401=AXIS2_PLACEMENT_3D ( 'NONE', #20928, #12934, #44410 ) ;
#27404=DIRECTION ( 'NONE',  ( 0.000000000000000000, 1.000000000000000000, 0.000000000000000000 ) ) ;
#27406=ORIENTED_EDGE ( 'NONE', *, *, #34331, .T. ) ;
#27408=EDGE_CURVE ( 'NONE', #23850, #12580, #17084, .T. ) ;
#27409=VERTEX_POINT ( 'NONE', #21716 ) ;
#27410=LINE ( 'NONE', #42899, #47634 ) ;
#27411=VERTEX_POINT ( 'NONE', #28938 ) ;
#27412=DIRECTION ( 'NONE',  ( 1.734723475976806848E-16, -0.000000000000000000, 1.000000000000000000 ) ) ;
#27413=ADVANCED_FACE ( 'NONE', ( #40825 ), #13719, .F. ) ;
#27414=CARTESIAN_POINT ( 'NONE',  ( 2.106197740627112402, 3.346456692913386100, -0.5026832550384014997 ) ) ;
#27417=VERTEX_POINT ( 'NONE', #10094 ) ;
#27418=ORIENTED_EDGE ( 'NONE', *, *, #2777, .T. ) ;
#27419=ORIENTED_EDGE ( 'NONE', *, *, #4544, .T. ) ;
#27420=DIRECTION ( 'NONE',  ( -0.000000000000000000, 1.000000000000000000, -0.000000000000000000 ) ) ;
#27421=DIRECTION ( 'NONE',  ( -0.000000000000000000, 1.000000000000000000, -0.000000000000000000 ) ) ;
#27422=EDGE_CURVE ( 'NONE', #10879, #49655, #44861, .T. ) ;
#27425=DIRECTION ( 'NONE',  ( 1.000000000000000000, -0.000000000000000000, 0.000000000000000000 ) ) ;
#27426=CARTESIAN_POINT ( 'NONE',  ( -1.363819533518803473, 0.000000000000000000, -1.417322834645664109 ) ) ;
#27427=CARTESIAN_POINT ( 'NONE',  ( -2.454875160333845674, 3.346456692913386100, 0.1574803149606286423 ) ) ;
#27428=EDGE_CURVE ( 'NONE', #24184, #12127, #29715, .T. ) ;
#27429=EDGE_LOOP ( 'NONE', ( #3109, #27653, #12147, #36226 ) ) ;
#27431=DIRECTION ( 'NONE',  ( -3.469446951953613696E-16, 0.000000000000000000, -1.000000000000000000 ) ) ;
#27432=DIRECTION ( 'NONE',  ( 1.734723475976806848E-16, 0.000000000000000000, 1.000000000000000000 ) ) ;
#27433=CARTESIAN_POINT ( 'NONE',  ( 1.363819533518803251, 3.267716535433071279, -2.365849761790805487E-16 ) ) ;
#27436=AXIS2_PLACEMENT_3D ( 'NONE', #34192, #18941, #42427 ) ;
#27437=LINE ( 'NONE', #4974, #12869 ) ;
#27440=ORIENTED_EDGE ( 'NONE', *, *, #40019, .F. ) ;
#27442=CARTESIAN_POINT ( 'NONE',  ( 1.687984952120843207, 3.267716535433071279, -1.259842519685035800 ) ) ;
#27444=VECTOR ( 'NONE', #2384, 39.37007874015748143 ) ;
#27449=LINE ( 'NONE', #27702, #37047 ) ;
#27450=ORIENTED_EDGE ( 'NONE', *, *, #38437, .T. ) ;
#27451=EDGE_LOOP ( 'NONE', ( #45607, #33752, #40045, #11941 ) ) ;
#27453=ORIENTED_EDGE ( 'NONE', *, *, #39324, .F. ) ;
#27457=CARTESIAN_POINT ( 'NONE',  ( 1.287906020515830141, 3.346456692913386100, -0.5118110236220471121 ) ) ;
#27459=EDGE_CURVE ( 'NONE', #18566, #456, #26989, .T. ) ;
#27461=DIRECTION ( 'NONE',  ( 1.000000000000000000, 0.000000000000000000, -3.469446951953613696E-16 ) ) ;
#27462=EDGE_CURVE ( 'NONE', #17026, #6745, #30481, .T. ) ;
#27463=VERTEX_POINT ( 'NONE', #10850 ) ;
#27466=CARTESIAN_POINT ( 'NONE',  ( 0.8182917201112824834, 3.267716535433071279, 1.417322834645662777 ) ) ;
#27467=EDGE_LOOP ( 'NONE', ( #37939, #39150, #47390, #38400 ) ) ;
#27468=DIRECTION ( 'NONE',  ( 1.734723475976806848E-16, -0.000000000000000000, 1.000000000000000000 ) ) ;
#27470=CARTESIAN_POINT ( 'NONE',  ( -1.166969139818015533, 3.346456692913386100, 0.1574803149606287811 ) ) ;
#27471=VECTOR ( 'NONE', #42859, 39.37007874015748143 ) ;
#27473=AXIS2_PLACEMENT_3D ( 'NONE', #6726, #50290, #17392 ) ;
#27474=DIRECTION ( 'NONE',  ( -0.000000000000000000, 1.000000000000000000, -0.000000000000000000 ) ) ;
#27475=ORIENTED_EDGE ( 'NONE', *, *, #44190, .T. ) ;
#27476=FACE_OUTER_BOUND ( 'NONE', #46596, .T. ) ;
#27477=AXIS2_PLACEMENT_3D ( 'NONE', #38461, #19318, #10824 ) ;
#27478=AXIS2_PLACEMENT_3D ( 'NONE', #9636, #1629, #17379 ) ;
#27479=PLANE ( 'NONE',  #33410 ) ;
#27481=LINE ( 'NONE', #34990, #19369 ) ;
#27483=ORIENTED_EDGE ( 'NONE', *, *, #15333, .F. ) ;
#27484=PLANE ( 'NONE',  #10860 ) ;
#27486=DIRECTION ( 'NONE',  ( -0.000000000000000000, 1.000000000000000000, -0.000000000000000000 ) ) ;
#27487=EDGE_CURVE ( 'NONE', #45462, #43417, #14728, .T. ) ;
#27488=EDGE_CURVE ( 'NONE', #19566, #32968, #26589, .T. ) ;
#27491=PLANE ( 'NONE',  #18653 ) ;
#27492=LINE ( 'NONE', #7879, #23583 ) ;
#27495=EDGE_LOOP ( 'NONE', ( #47822, #26670, #45240, #40995 ) ) ;
#27499=DIRECTION ( 'NONE',  ( 0.000000000000000000, 0.000000000000000000, -1.000000000000000000 ) ) ;
#27502=LINE ( 'NONE', #2310, #6924 ) ;
#27503=ORIENTED_EDGE ( 'NONE', *, *, #33854, .T. ) ;
#27504=ORIENTED_EDGE ( 'NONE', *, *, #23970, .T. ) ;
#27505=CARTESIAN_POINT ( 'NONE',  ( -0.8942052331142547050, 3.267716535433071279, 0.4330708661417290162 ) ) ;
#27509=CARTESIAN_POINT ( 'NONE',  ( 4.200216290258821831E-16, 3.267716535433071279, 2.165354330708661568 ) ) ;
#27510=LINE ( 'NONE', #24165, #11237 ) ;
#27513=VECTOR ( 'NONE', #13960, 39.37007874015748143 ) ;
#27514=CARTESIAN_POINT ( 'NONE',  ( 0.8182917201112821504, 3.267716535433071279, -1.419509857074483539E-16 ) ) ;
#27516=CARTESIAN_POINT ( 'NONE',  ( -0.3486774197067343262, 3.267716535433071279, -2.401574803149598036 ) ) ;
#27520=EDGE_CURVE ( 'NONE', #36182, #27786, #14471, .T. ) ;
#27521=CARTESIAN_POINT ( 'NONE',  ( 0.000000000000000000, 3.267716535433071279, -0.3149606299212596716 ) ) ;
#27522=FACE_OUTER_BOUND ( 'NONE', #48846, .T. ) ;
#27523=DIRECTION ( 'NONE',  ( -1.000000000000000000, 0.000000000000000000, 0.000000000000000000 ) ) ;
#27524=EDGE_CURVE ( 'NONE', #4242, #3379, #49536, .T. ) ;
#27525=ORIENTED_EDGE ( 'NONE', *, *, #16352, .F. ) ;
#27526=CARTESIAN_POINT ( 'NONE',  ( 0.4696143004045476022, 3.267716535433071279, -1.929133858267710000 ) ) ;
#27527=ADVANCED_FACE ( 'NONE', ( #29968 ), #42595, .F. ) ;
#27529=ORIENTED_EDGE ( 'NONE', *, *, #255, .F. ) ;
#27530=CARTESIAN_POINT ( 'NONE',  ( -2.182111253630085290, 3.267716535433071279, 0.6299212598425164567 ) ) ;
#27534=CARTESIAN_POINT ( 'NONE',  ( -1.712496953225537633, 3.267716535433071279, -0.9842519685039344823 ) ) ;
#27535=ORIENTED_EDGE ( 'NONE', *, *, #34491, .T. ) ;
#27537=DIRECTION ( 'NONE',  ( 1.734723475976806848E-16, -0.000000000000000000, 1.000000000000000000 ) ) ;
#27541=FACE_OUTER_BOUND ( 'NONE', #17223, .T. ) ;
#27543=ORIENTED_EDGE ( 'NONE', *, *, #16564, .T. ) ;
#27544=ORIENTED_EDGE ( 'NONE', *, *, #49540, .T. ) ;
#27545=AXIS2_PLACEMENT_3D ( 'NONE', #19630, #31783, #17 ) ;
#27546=CARTESIAN_POINT ( 'NONE',  ( 0.000000000000000000, 3.346456692913386100, 0.000000000000000000 ) ) ;
#27547=ORIENTED_EDGE ( 'NONE', *, *, #34593, .T. ) ;
#27551=ORIENTED_EDGE ( 'NONE', *, *, #18587, .T. ) ;
#27552=AXIS2_PLACEMENT_3D ( 'NONE', #49479, #41280, #10286 ) ;
#27553=VECTOR ( 'NONE', #31675, 39.37007874015748143 ) ;
#27554=CARTESIAN_POINT ( 'NONE',  ( 1.277153579995027988, 3.261691961121675920, -2.086614173228339641 ) ) ;
#27555=ORIENTED_EDGE ( 'NONE', *, *, #34206, .F. ) ;
#27556=EDGE_CURVE ( 'NONE', #32615, #19355, #15230, .T. ) ;
#27558=DIRECTION ( 'NONE',  ( -3.469446951953613696E-16, 0.000000000000000000, -1.000000000000000000 ) ) ;
#27559=VECTOR ( 'NONE', #17773, 39.37007874015748143 ) ;
#27561=EDGE_LOOP ( 'NONE', ( #22178, #4887, #35163, #24921 ) ) ;
#27562=CARTESIAN_POINT ( 'NONE',  ( -1.299212598425205423, 3.346456692913386100, -1.732283464566922726 ) ) ;
#27563=EDGE_LOOP ( 'NONE', ( #19728, #21935, #16523, #44103 ) ) ;
#27564=EDGE_CURVE ( 'NONE', #36460, #12460, #46688, .T. ) ;
#27568=DIRECTION ( 'NONE',  ( 1.000000000000000000, 0.000000000000000000, 0.000000000000000000 ) ) ;
#27569=DIRECTION ( 'NONE',  ( -0.000000000000000000, 1.000000000000000000, -0.000000000000000000 ) ) ;
#27570=ORIENTED_EDGE ( 'NONE', *, *, #16930, .T. ) ;
#27571=CARTESIAN_POINT ( 'NONE',  ( -2.454875160333845674, 3.232777166330581320, -0.1574803149606298636 ) ) ;
#27572=ORIENTED_EDGE ( 'NONE', *, *, #40317, .T. ) ;
#27574=DIRECTION ( 'NONE',  ( 1.000000000000000000, 0.000000000000000000, 0.000000000000000000 ) ) ;
#27575=CARTESIAN_POINT ( 'NONE',  ( 2.106197740627111514, 3.267716535433071279, -1.102362204724406602 ) ) ;
#27576=ORIENTED_EDGE ( 'NONE', *, *, #2955, .F. ) ;
#27577=VERTEX_POINT ( 'NONE', #27091 ) ;
#27579=FACE_OUTER_BOUND ( 'NONE', #9239, .T. ) ;
#27580=DIRECTION ( 'NONE',  ( 1.000000000000000000, -0.000000000000000000, 0.000000000000000000 ) ) ;
#27581=VECTOR ( 'NONE', #15595, 39.37007874015748143 ) ;
#27582=CARTESIAN_POINT ( 'NONE',  ( 1.006250229852934774, 3.267716535433071279, 1.850393700787392293 ) ) ;
#27583=AXIS2_PLACEMENT_3D ( 'NONE', #14519, #29754, #33895 ) ;
#27584=DIRECTION ( 'NONE',  ( -3.469446951953613696E-16, 0.000000000000000000, -1.000000000000000000 ) ) ;
#27592=VECTOR ( 'NONE', #32294, 39.37007874015748143 ) ;
#27593=ORIENTED_EDGE ( 'NONE', *, *, #18071, .F. ) ;
#27594=DIRECTION ( 'NONE',  ( 1.000000000000000000, 0.000000000000000000, -3.469446951953613696E-16 ) ) ;
#27595=VERTEX_POINT ( 'NONE', #2599 ) ;
#27599=DIRECTION ( 'NONE',  ( -3.469446951953613696E-16, 0.000000000000000000, -1.000000000000000000 ) ) ;
#27601=CARTESIAN_POINT ( 'NONE',  ( -0.2727639067037611054, 0.000000000000000000, -2.244094488188968395 ) ) ;
#27602=ORIENTED_EDGE ( 'NONE', *, *, #28273, .F. ) ;
#27603=CARTESIAN_POINT ( 'NONE',  ( -2.106299212598425008, 3.346456692913386100, -6.146657985744592735E-16 ) ) ;
#27604=DIRECTION ( 'NONE',  ( 1.000000000000000000, -0.000000000000000000, 0.000000000000000000 ) ) ;
#27608=VECTOR ( 'NONE', #16290, 39.37007874015748143 ) ;
#27609=ORIENTED_EDGE ( 'NONE', *, *, #46266, .F. ) ;
#27610=VERTEX_POINT ( 'NONE', #15485 ) ;
#27611=VECTOR ( 'NONE', #12135, 39.37007874015748143 ) ;
#27612=AXIS2_PLACEMENT_3D ( 'NONE', #36374, #27843, #4363 ) ;
#27615=DIRECTION ( 'NONE',  ( 1.734723475976806848E-16, -0.000000000000000000, 1.000000000000000000 ) ) ;
#27616=EDGE_CURVE ( 'NONE', #47811, #27355, #44111, .T. ) ;
#27617=ORIENTED_EDGE ( 'NONE', *, *, #17584, .F. ) ;
#27618=FACE_OUTER_BOUND ( 'NONE', #43675, .T. ) ;
#27619=PLANE ( 'NONE',  #29960 ) ;
#27620=ADVANCED_FACE ( 'NONE', ( #31484 ), #35614, .F. ) ;
#27621=ORIENTED_EDGE ( 'NONE', *, *, #40523, .F. ) ;
#27623=VECTOR ( 'NONE', #38117, 39.37007874015748143 ) ;
#27625=ORIENTED_EDGE ( 'NONE', *, *, #6836, .F. ) ;
#27626=ORIENTED_EDGE ( 'NONE', *, *, #3873, .F. ) ;
#27629=EDGE_CURVE ( 'NONE', #4171, #50731, #23711, .T. ) ;
#27630=CARTESIAN_POINT ( 'NONE',  ( 0.8182917201112819283, 0.000000000000000000, -0.4724409448818889246 ) ) ;
#27631=CARTESIAN_POINT ( 'NONE',  ( -0.5455278134075214336, 0.000000000000000000, -1.771653543307081025 ) ) ;
#27633=DIRECTION ( 'NONE',  ( -1.000000000000000000, 0.000000000000000000, -0.000000000000000000 ) ) ;
#27635=ORIENTED_EDGE ( 'NONE', *, *, #12638, .T. ) ;
#27636=DIRECTION ( 'NONE',  ( 1.000000000000000000, 0.000000000000000000, -3.469446951953613696E-16 ) ) ;
#27638=LINE ( 'NONE', #31530, #35043 ) ;
#27639=CARTESIAN_POINT ( 'NONE',  ( 0.2727639067037609943, 0.000000000000000000, 2.165354330708650910 ) ) ;
#27640=EDGE_CURVE ( 'NONE', #11147, #388, #35869, .T. ) ;
#27641=EDGE_CURVE ( 'NONE', #18496, #21759, #35104, .T. ) ;
#27642=DIRECTION ( 'NONE',  ( -3.469446951953613696E-16, 0.000000000000000000, -1.000000000000000000 ) ) ;
#27643=CARTESIAN_POINT ( 'NONE',  ( -0.8942052331142552601, 0.000000000000000000, -0.3149606299212593941 ) ) ;
#27645=ORIENTED_EDGE ( 'NONE', *, *, #46571, .F. ) ;
#27646=AXIS2_PLACEMENT_3D ( 'NONE', #13891, #6142, #10266 ) ;
#27647=EDGE_CURVE ( 'NONE', #12822, #10269, #4627, .T. ) ;
#27648=CARTESIAN_POINT ( 'NONE',  ( -0.07591351300297333182, 3.346456692913386100, 0.1574803149606283648 ) ) ;
#27650=AXIS2_PLACEMENT_3D ( 'NONE', #23195, #46665, #26817 ) ;
#27651=VERTEX_POINT ( 'NONE', #8751 ) ;
#27653=ORIENTED_EDGE ( 'NONE', *, *, #43668, .F. ) ;
#27654=CARTESIAN_POINT ( 'NONE',  ( -1.091055626815042645, 3.346456692913386100, -1.574803149606293529 ) ) ;
#27655=DIRECTION ( 'NONE',  ( 0.000000000000000000, 0.000000000000000000, -1.000000000000000000 ) ) ;
#27656=DIRECTION ( 'NONE',  ( -0.000000000000000000, 1.000000000000000000, -0.000000000000000000 ) ) ;
#27657=AXIS2_PLACEMENT_3D ( 'NONE', #7000, #22748, #23493 ) ;
#27658=ORIENTED_EDGE ( 'NONE', *, *, #46475, .F. ) ;
#27659=AXIS2_PLACEMENT_3D ( 'NONE', #2045, #20443, #39553 ) ;
#27661=CARTESIAN_POINT ( 'NONE',  ( -1.091055626815042645, 3.346456692913386100, -1.141732283464563569 ) ) ;
#27664=VERTEX_POINT ( 'NONE', #24253 ) ;
#27665=CARTESIAN_POINT ( 'NONE',  ( -1.636583440222563857, 3.267716535433071279, 2.839019714148966584E-16 ) ) ;
#27666=LINE ( 'NONE', #4185, #2487 ) ;
#27670=ORIENTED_EDGE ( 'NONE', *, *, #48125, .F. ) ;
#27671=ORIENTED_EDGE ( 'NONE', *, *, #27762, .F. ) ;
#27672=ORIENTED_EDGE ( 'NONE', *, *, #20623, .T. ) ;
#27674=DIRECTION ( 'NONE',  ( 1.000000000000000000, 0.000000000000000000, -3.469446951953613696E-16 ) ) ;
#27675=ORIENTED_EDGE ( 'NONE', *, *, #45061, .T. ) ;
#27676=ORIENTED_EDGE ( 'NONE', *, *, #10267, .T. ) ;
#27677=CARTESIAN_POINT ( 'NONE',  ( 1.091055626815043311, 0.000000000000000000, 1.574803149606291974 ) ) ;
#27678=PLANE ( 'NONE',  #49956 ) ;
#27681=ADVANCED_FACE ( 'NONE', ( #24508 ), #35363, .F. ) ;
#27682=LINE ( 'NONE', #39572, #40319 ) ;
#27684=CARTESIAN_POINT ( 'NONE',  ( 1.363819533518803029, 0.000000000000000000, -1.417322834645665219 ) ) ;
#27685=EDGE_CURVE ( 'NONE', #43930, #31646, #20370, .T. ) ;
#27686=VECTOR ( 'NONE', #48068, 39.37007874015748143 ) ;
#27687=ORIENTED_EDGE ( 'NONE', *, *, #33648, .F. ) ;
#27688=FACE_OUTER_BOUND ( 'NONE', #3399, .T. ) ;
#27689=EDGE_CURVE ( 'NONE', #16904, #5663, #27342, .T. ) ;
#27694=CARTESIAN_POINT ( 'NONE',  ( -1.985260859929298016, 3.346456692913386100, -0.6299212598425177889 ) ) ;
#27701=CARTESIAN_POINT ( 'NONE',  ( -0.5455278134075208785, 3.346456692913386100, 1.574803149606291974 ) ) ;
#27702=CARTESIAN_POINT ( 'NONE',  ( 1.091055626815042423, 0.000000000000000000, -1.574803149606294417 ) ) ;
#27710=EDGE_CURVE ( 'NONE', #21459, #25499, #11856, .T. ) ;
#27711=EDGE_CURVE ( 'NONE', #35391, #4326, #16508, .T. ) ;
#27712=CARTESIAN_POINT ( 'NONE',  ( -0.5455278134075214336, 0.000000000000000000, -0.5118110236220467790 ) ) ;
#27713=LINE ( 'NONE', #32637, #21239 ) ;
#27714=EDGE_LOOP ( 'NONE', ( #20537, #25714, #17396 ) ) ;
#27716=EDGE_CURVE ( 'NONE', #3654, #16745, #47440, .T. ) ;
#27718=ORIENTED_EDGE ( 'NONE', *, *, #50317, .F. ) ;
#27721=CARTESIAN_POINT ( 'NONE',  ( -1.536664496436148184E-16, 3.267716535433071279, -1.456692913385822630 ) ) ;
#27722=EDGE_LOOP ( 'NONE', ( #9853, #19714, #23428, #15063 ) ) ;
#27723=VECTOR ( 'NONE', #22348, 39.37007874015748143 ) ;
#27725=CARTESIAN_POINT ( 'NONE',  ( 1.287906020515830141, 0.000000000000000000, -1.141732283464564013 ) ) ;
#27728=AXIS2_PLACEMENT_3D ( 'NONE', #607, #3974, #3721 ) ;
#27729=ORIENTED_EDGE ( 'NONE', *, *, #40449, .T. ) ;
#27730=LINE ( 'NONE', #371, #27028 ) ;
#27734=CARTESIAN_POINT ( 'NONE',  ( -2.182111253630085290, 0.000000000000000000, 0.9448818897637749625 ) ) ;
#27736=CARTESIAN_POINT ( 'NONE',  ( 1.909347346926324684, 0.000000000000000000, 0.7874015748031456541 ) ) ;
#27737=AXIS2_PLACEMENT_3D ( 'NONE', #2287, #6670, #11046 ) ;
#27739=ORIENTED_EDGE ( 'NONE', *, *, #4953, .F. ) ;
#27740=CARTESIAN_POINT ( 'NONE',  ( -0.07591351300297305427, 3.267716535433071279, 2.633779063002558971E-17 ) ) ;
#27741=DIRECTION ( 'NONE',  ( -1.000000000000000000, -0.000000000000000000, -0.000000000000000000 ) ) ;
#27742=ORIENTED_EDGE ( 'NONE', *, *, #22281, .T. ) ;
#27744=CARTESIAN_POINT ( 'NONE',  ( -1.091055626815042645, 3.346456692913386100, 2.204724409448808764 ) ) ;
#27746=CARTESIAN_POINT ( 'NONE',  ( -2.182111253630085734, 3.346456692913386100, -0.9448818897637762948 ) ) ;
#27748=VERTEX_POINT ( 'NONE', #23989 ) ;
#27749=EDGE_CURVE ( 'NONE', #34275, #49325, #5654, .T. ) ;
#27750=LINE ( 'NONE', #19241, #42737 ) ;
#27751=LINE ( 'NONE', #392, #47186 ) ;
#27752=CARTESIAN_POINT ( 'NONE',  ( 1.363819533518803251, 3.346456692913386100, -0.7874015748031473194 ) ) ;
#27753=DIRECTION ( 'NONE',  ( 1.000000000000000000, 0.000000000000000000, 0.000000000000000000 ) ) ;
#27754=EDGE_CURVE ( 'NONE', #13831, #11518, #12889, .T. ) ;
#27755=FACE_BOUND ( 'NONE', #19159, .T. ) ;
#27760=EDGE_LOOP ( 'NONE', ( #5139, #33482, #15957, #45430 ) ) ;
#27762=EDGE_CURVE ( 'NONE', #25457, #31775, #36383, .T. ) ;
#27763=AXIS2_PLACEMENT_3D ( 'NONE', #16954, #28298, #24440 ) ;
#27764=ORIENTED_EDGE ( 'NONE', *, *, #48624, .T. ) ;
#27765=ORIENTED_EDGE ( 'NONE', *, *, #4041, .T. ) ;
#27770=CARTESIAN_POINT ( 'NONE',  ( 0.8182917201112819283, 3.346456692913386100, -0.03937007874015881204 ) ) ;
#27771=PLANE ( 'NONE',  #24434 ) ;
#27772=CARTESIAN_POINT ( 'NONE',  ( 0.000000000000000000, 3.267716535433071279, 0.7480314960629874665 ) ) ;
#27773=EDGE_CURVE ( 'NONE', #13787, #3556, #45373, .T. ) ;
#27774=VECTOR ( 'NONE', #17371, 39.37007874015748143 ) ;
#27776=DIRECTION ( 'NONE',  ( 1.000000000000000000, -0.000000000000000000, 0.000000000000000000 ) ) ;
#27778=EDGE_LOOP ( 'NONE', ( #25685, #10148, #38682, #44005 ) ) ;
#27780=ADVANCED_FACE ( 'NONE', ( #10034 ), #5900, .F. ) ;
#27781=DIRECTION ( 'NONE',  ( 1.734723475976806848E-16, -0.000000000000000000, 1.000000000000000000 ) ) ;
#27782=DIRECTION ( 'NONE',  ( 1.734723475976806848E-16, -0.000000000000000000, 1.000000000000000000 ) ) ;
#27783=ORIENTED_EDGE ( 'NONE', *, *, #46050, .T. ) ;
#27784=DIRECTION ( 'NONE',  ( -1.000000000000000000, 0.000000000000000000, 0.000000000000000000 ) ) ;
#27786=VERTEX_POINT ( 'NONE', #24763 ) ;
#27791=ORIENTED_EDGE ( 'NONE', *, *, #37067, .F. ) ;
#27792=DIRECTION ( 'NONE',  ( 1.734723475976806848E-16, -0.000000000000000000, 1.000000000000000000 ) ) ;
#27793=CARTESIAN_POINT ( 'NONE',  ( -1.091055626815042201, 3.267716535433071279, 1.574803149606291974 ) ) ;
#27795=CARTESIAN_POINT ( 'NONE',  ( 1.363819533518803251, 3.346456692913386100, -0.4724409448818889246 ) ) ;
#27796=ORIENTED_EDGE ( 'NONE', *, *, #26592, .T. ) ;
#27797=VECTOR ( 'NONE', #30313, 39.37007874015748143 ) ;
#27798=VECTOR ( 'NONE', #37340, 39.37007874015748143 ) ;
#27799=VECTOR ( 'NONE', #48134, 39.37007874015748143 ) ;
#27800=ORIENTED_EDGE ( 'NONE', *, *, #38239, .T. ) ;
#27803=VERTEX_POINT ( 'NONE', #48972 ) ;
#27804=LINE ( 'NONE', #31436, #44392 ) ;
#27805=LINE ( 'NONE', #39437, #12838 ) ;
#27806=ORIENTED_EDGE ( 'NONE', *, *, #47854, .F. ) ;
#27808=VERTEX_POINT ( 'NONE', #36643 ) ;
#27809=DIRECTION ( 'NONE',  ( -3.469446951953613696E-16, 0.000000000000000000, -1.000000000000000000 ) ) ;
#27810=DIRECTION ( 'NONE',  ( 1.734723475976806848E-16, 0.000000000000000000, 1.000000000000000000 ) ) ;
#27812=VERTEX_POINT ( 'NONE', #17276 ) ;
#27813=EDGE_CURVE ( 'NONE', #6103, #35018, #42693, .T. ) ;
#27814=DIRECTION ( 'NONE',  ( 1.000000000000000000, 0.000000000000000000, 0.000000000000000000 ) ) ;
#27815=ORIENTED_EDGE ( 'NONE', *, *, #12609, .T. ) ;
#27816=VECTOR ( 'NONE', #10718, 39.37007874015748143 ) ;
#27819=EDGE_CURVE ( 'NONE', #22703, #32862, #49228, .T. ) ;
#27820=EDGE_LOOP ( 'NONE', ( #40066, #16672, #29519, #49823 ) ) ;
#27821=ORIENTED_EDGE ( 'NONE', *, *, #8752, .T. ) ;
#27822=DIRECTION ( 'NONE',  ( 0.000000000000000000, -1.000000000000000000, 0.000000000000000000 ) ) ;
#27823=PLANE ( 'NONE',  #22922 ) ;
#27824=VERTEX_POINT ( 'NONE', #44614 ) ;
#27826=CARTESIAN_POINT ( 'NONE',  ( 0.000000000000000000, 3.267716535433071279, -1.929133858267710666 ) ) ;
#27827=ORIENTED_EDGE ( 'NONE', *, *, #34088, .F. ) ;
#27828=CARTESIAN_POINT ( 'NONE',  ( 1.015142113812069313, 0.000000000000000000, 1.102362204724403938 ) ) ;
#27829=DIRECTION ( 'NONE',  ( 0.000000000000000000, 0.000000000000000000, 1.000000000000000000 ) ) ;
#27830=EDGE_CURVE ( 'NONE', #33278, #10643, #9267, .T. ) ;
#27832=AXIS2_PLACEMENT_3D ( 'NONE', #11662, #26650, #19397 ) ;
#27833=CARTESIAN_POINT ( 'NONE',  ( 0.000000000000000000, 3.267716535433071279, -0.1968503937007880511 ) ) ;
#27834=VERTEX_POINT ( 'NONE', #41525 ) ;
#27835=VERTEX_POINT ( 'NONE', #21145 ) ;
#27836=LINE ( 'NONE', #8995, #20328 ) ;
#27837=DIRECTION ( 'NONE',  ( -3.469446951953613696E-16, 0.000000000000000000, -1.000000000000000000 ) ) ;
#27838=LINE ( 'NONE', #50520, #35711 ) ;
#27839=EDGE_CURVE ( 'NONE', #25226, #9823, #46787, .T. ) ;
#27840=VECTOR ( 'NONE', #13423, 39.37007874015748143 ) ;
#27841=LINE ( 'NONE', #484, #30137 ) ;
#27843=DIRECTION ( 'NONE',  ( 0.000000000000000000, -1.000000000000000000, 0.000000000000000000 ) ) ;
#27845=CARTESIAN_POINT ( 'NONE',  ( -1.712496953225537411, 3.267716535433071279, 5.941417334598190051E-16 ) ) ;
#27846=VECTOR ( 'NONE', #30700, 39.37007874015748143 ) ;
#27853=CARTESIAN_POINT ( 'NONE',  ( -0.8182917201112819283, 0.000000000000000000, -0.9842519685039342603 ) ) ;
#27854=FACE_OUTER_BOUND ( 'NONE', #9850, .T. ) ;
#27856=PLANE ( 'NONE',  #43571 ) ;
#27857=ORIENTED_EDGE ( 'NONE', *, *, #6585, .F. ) ;
#27858=LINE ( 'NONE', #46939, #24573 ) ;
#27859=ORIENTED_EDGE ( 'NONE', *, *, #15999, .F. ) ;
#27860=DIRECTION ( 'NONE',  ( -3.469446951953613696E-16, 0.000000000000000000, -1.000000000000000000 ) ) ;
#27861=DIRECTION ( 'NONE',  ( -3.469446951953613696E-16, 0.000000000000000000, -1.000000000000000000 ) ) ;
#27862=VECTOR ( 'NONE', #32327, 39.37007874015748143 ) ;
#27863=ORIENTED_EDGE ( 'NONE', *, *, #20802, .T. ) ;
#27865=DIRECTION ( 'NONE',  ( -3.469446951953613696E-16, 0.000000000000000000, -1.000000000000000000 ) ) ;
#27867=ORIENTED_EDGE ( 'NONE', *, *, #46102, .T. ) ;
#27869=CARTESIAN_POINT ( 'NONE',  ( 1.091055626815043311, 3.346456692913386100, 1.574803149606291974 ) ) ;
#27870=CARTESIAN_POINT ( 'NONE',  ( 0.000000000000000000, 0.000000000000000000, 0.000000000000000000 ) ) ;
#27872=EDGE_CURVE ( 'NONE', #24676, #29929, #44871, .T. ) ;
#27873=VECTOR ( 'NONE', #17168, 39.37007874015748143 ) ;
#27875=FACE_OUTER_BOUND ( 'NONE', #19273, .T. ) ;
#27876=LINE ( 'NONE', #43621, #6885 ) ;
#27878=EDGE_CURVE ( 'NONE', #15242, #27924, #9523, .T. ) ;
#27879=ORIENTED_EDGE ( 'NONE', *, *, #14103, .T. ) ;
#27880=VECTOR ( 'NONE', #17249, 39.37007874015748143 ) ;
#27881=CARTESIAN_POINT ( 'NONE',  ( 2.052631463899902364, 3.346456692913386100, 0.4724409448818868706 ) ) ;
#27882=EDGE_LOOP ( 'NONE', ( #13475, #37513, #48929, #809, #43994, #31687, #17310, #17758, #28193, #7915, #30744, #40273, #6107, #41817, #1712, #37894, #13207, #23814, #751, #406, #17242, #8603, #11469, #44824, #9092, #19267, #12013, #3313, #17735, #49896, #37750, #47244, #27047, #14043, #26593, #171, #19075, #2892, #32668, #15703, #28907, #13856, #46183, #2314, #5361, #38660, #24461, #22549, #15894, #6866, #45827, #19097, #47424, #1090, #23310, #28086, #1894, #33274, #25244, #32824, #34722, #15439, #16515, #41182, #21556, #19961, #11763, #47066, #43969, #25361, #31377, #45180, #46505, #10966, #1070, #45561, #38879, #27718, #3451, #13658, #22874, #49154, #50315, #20516 ) ) ;
#27883=ORIENTED_EDGE ( 'NONE', *, *, #28489, .T. ) ;
#27885=VECTOR ( 'NONE', #687, 39.37007874015748143 ) ;
#27886=ORIENTED_EDGE ( 'NONE', *, *, #14496, .T. ) ;
#27887=DIRECTION ( 'NONE',  ( -1.000000000000000000, 0.000000000000000000, 0.000000000000000000 ) ) ;
#27889=ADVANCED_FACE ( 'NONE', ( #10540 ), #6916, .F. ) ;
#27891=LINE ( 'NONE', #12407, #10686 ) ;
#27892=ORIENTED_EDGE ( 'NONE', *, *, #8204, .F. ) ;
#27893=ORIENTED_EDGE ( 'NONE', *, *, #28389, .F. ) ;
#27894=DIRECTION ( 'NONE',  ( -3.469446951953613696E-16, 0.000000000000000000, -1.000000000000000000 ) ) ;
#27898=DIRECTION ( 'NONE',  ( 1.000000000000000000, 0.000000000000000000, -3.469446951953613696E-16 ) ) ;
#27899=CARTESIAN_POINT ( 'NONE',  ( 0.000000000000000000, 3.267716535433071279, 1.062992125984246083 ) ) ;
#27900=CARTESIAN_POINT ( 'NONE',  ( -0.8182917201112815953, 3.267716535433071279, 1.419509857074482553E-16 ) ) ;
#27902=ADVANCED_FACE ( 'NONE', ( #45877 ), #26287, .F. ) ;
#27903=LINE ( 'NONE', #16037, #6081 ) ;
#27905=ORIENTED_EDGE ( 'NONE', *, *, #39185, .T. ) ;
#27906=CARTESIAN_POINT ( 'NONE',  ( 1.770012363201889594, 3.346456692913386100, -1.141732283464564013 ) ) ;
#27908=VERTEX_POINT ( 'NONE', #38420 ) ;
#27912=VECTOR ( 'NONE', #14041, 39.37007874015748143 ) ;
#27913=DIRECTION ( 'NONE',  ( 1.000000000000000000, 0.000000000000000000, -3.469446951953613696E-16 ) ) ;
#27915=CARTESIAN_POINT ( 'NONE',  ( -1.909347346926324462, 0.000000000000000000, 0.4724409448818871482 ) ) ;
#27917=VECTOR ( 'NONE', #43888, 39.37007874015748143 ) ;
#27918=EDGE_CURVE ( 'NONE', #29175, #14008, #42032, .T. ) ;
#27919=ORIENTED_EDGE ( 'NONE', *, *, #40487, .T. ) ;
#27920=DIRECTION ( 'NONE',  ( 1.734723475976806848E-16, -0.000000000000000000, 1.000000000000000000 ) ) ;
#27922=AXIS2_PLACEMENT_3D ( 'NONE', #2660, #18409, #2154 ) ;
#27923=LINE ( 'NONE', #18919, #2350 ) ;
#27924=VERTEX_POINT ( 'NONE', #2285 ) ;
#27925=ADVANCED_FACE ( 'NONE', ( #14920 ), #34796, .F. ) ;
#27927=DIRECTION ( 'NONE',  ( 0.000000000000000000, -1.000000000000000000, 0.000000000000000000 ) ) ;
#27928=CARTESIAN_POINT ( 'NONE',  ( 0.8182917201112819283, 3.267716535433071279, -1.299212598425193210 ) ) ;
#27929=ORIENTED_EDGE ( 'NONE', *, *, #50604, .F. ) ;
#27930=ORIENTED_EDGE ( 'NONE', *, *, #20237, .T. ) ;
#27933=LINE ( 'NONE', #50862, #42797 ) ;
#27934=EDGE_LOOP ( 'NONE', ( #14538, #32907, #7199, #26821 ) ) ;
#27935=VERTEX_POINT ( 'NONE', #30668 ) ;
#27936=LINE ( 'NONE', #48034, #14886 ) ;
#27937=CARTESIAN_POINT ( 'NONE',  ( -0.5455278134075208785, 0.000000000000000000, 1.889763779527550369 ) ) ;
#27938=DIRECTION ( 'NONE',  ( 1.000000000000000000, 0.000000000000000000, 0.000000000000000000 ) ) ;
#27941=ORIENTED_EDGE ( 'NONE', *, *, #48899, .T. ) ;
#27942=DIRECTION ( 'NONE',  ( -1.000000000000000000, 0.000000000000000000, -0.000000000000000000 ) ) ;
#27945=LINE ( 'NONE', #23823, #4739 ) ;
#27948=ORIENTED_EDGE ( 'NONE', *, *, #21837, .T. ) ;
#27950=CARTESIAN_POINT ( 'NONE',  ( 1.833433833923351353, 0.000000000000000000, -1.161035397307311917E-15 ) ) ;
#27951=VERTEX_POINT ( 'NONE', #21911 ) ;
#27952=CARTESIAN_POINT ( 'NONE',  ( -0.2727639067037602727, 3.267716535433071279, 1.220472440944875281 ) ) ;
#27955=FACE_OUTER_BOUND ( 'NONE', #28696, .T. ) ;
#27956=LINE ( 'NONE', #39585, #38298 ) ;
#27957=VECTOR ( 'NONE', #37037, 39.37007874015748143 ) ;
#27960=CARTESIAN_POINT ( 'NONE',  ( 1.636583440222563857, 3.267716535433071279, 1.417869535855831975 ) ) ;
#27963=ORIENTED_EDGE ( 'NONE', *, *, #6068, .F. ) ;
#27965=VERTEX_POINT ( 'NONE', #34044 ) ;
#27967=DIRECTION ( 'NONE',  ( -0.000000000000000000, 1.000000000000000000, -0.000000000000000000 ) ) ;
#27968=EDGE_CURVE ( 'NONE', #39361, #45523, #46133, .T. ) ;
#27969=DIRECTION ( 'NONE',  ( 1.000000000000000000, -0.000000000000000000, 0.000000000000000000 ) ) ;
#27971=ORIENTED_EDGE ( 'NONE', *, *, #4905, .F. ) ;
#27972=DIRECTION ( 'NONE',  ( -1.000000000000000000, 0.000000000000000000, 0.000000000000000000 ) ) ;
#27974=EDGE_CURVE ( 'NONE', #34792, #47654, #3292, .T. ) ;
#27975=VERTEX_POINT ( 'NONE', #41780 ) ;
#27977=EDGE_CURVE ( 'NONE', #904, #41852, #18544, .T. ) ;
#27980=ORIENTED_EDGE ( 'NONE', *, *, #27762, .T. ) ;
#27981=EDGE_CURVE ( 'NONE', #49063, #46927, #49984, .T. ) ;
#27984=CARTESIAN_POINT ( 'NONE',  ( -1.363819533518803029, 3.346456692913386100, 0.9055118110236167750 ) ) ;
#27985=ORIENTED_EDGE ( 'NONE', *, *, #6503, .F. ) ;
#27986=DIRECTION ( 'NONE',  ( -0.000000000000000000, 1.000000000000000000, -0.000000000000000000 ) ) ;
#27988=VERTEX_POINT ( 'NONE', #6418 ) ;
#27989=FACE_OUTER_BOUND ( 'NONE', #46595, .T. ) ;
#27990=VECTOR ( 'NONE', #3141, 39.37007874015748143 ) ;
#27992=CARTESIAN_POINT ( 'NONE',  ( 2.378961647330872786, 3.346456692913386100, -1.161035397307311917E-15 ) ) ;
#27994=EDGE_CURVE ( 'NONE', #21949, #3678, #49728, .T. ) ;
#27997=DIRECTION ( 'NONE',  ( 1.000000000000000000, -0.000000000000000000, 0.000000000000000000 ) ) ;
#28000=CARTESIAN_POINT ( 'NONE',  ( -1.985260859929297794, 3.267716535433071279, -0.5118110236220464460 ) ) ;
#28002=AXIS2_PLACEMENT_3D ( 'NONE', #12689, #32065, #16306 ) ;
#28005=CARTESIAN_POINT ( 'NONE',  ( 1.833433833923351353, 0.000000000000000000, -0.1968503937007886062 ) ) ;
#28006=EDGE_LOOP ( 'NONE', ( #34977, #8397, #17739, #11556 ) ) ;
#28007=ORIENTED_EDGE ( 'NONE', *, *, #16035, .F. ) ;
#28009=CARTESIAN_POINT ( 'NONE',  ( -1.862188077367287642, 3.346456692913386100, -0.9842519685039344823 ) ) ;
#28010=CARTESIAN_POINT ( 'NONE',  ( -0.8182917201112814842, 0.000000000000000000, 0.7874015748031456541 ) ) ;
#28011=EDGE_CURVE ( 'NONE', #3260, #11491, #33797, .T. ) ;
#28014=FACE_BOUND ( 'NONE', #32207, .T. ) ;
#28015=VERTEX_POINT ( 'NONE', #32912 ) ;
#28016=EDGE_CURVE ( 'NONE', #26276, #8950, #44497, .T. ) ;
#28017=ADVANCED_FACE ( 'NONE', ( #24380 ), #12500, .F. ) ;
#28019=ORIENTED_EDGE ( 'NONE', *, *, #197, .F. ) ;
#28020=EDGE_LOOP ( 'NONE', ( #1857, #38138, #33619, #46576 ) ) ;
#28021=DIRECTION ( 'NONE',  ( 0.000000000000000000, 0.000000000000000000, -1.000000000000000000 ) ) ;
#28022=VECTOR ( 'NONE', #50133, 39.37007874015748143 ) ;
#28023=VERTEX_POINT ( 'NONE', #47830 ) ;
#28025=CARTESIAN_POINT ( 'NONE',  ( -0.6214413264104945434, 3.346456692913386100, -1.732283464566922726 ) ) ;
#28026=ORIENTED_EDGE ( 'NONE', *, *, #49067, .T. ) ;
#28028=DIRECTION ( 'NONE',  ( 1.000000000000000000, -0.000000000000000000, 0.000000000000000000 ) ) ;
#28029=CARTESIAN_POINT ( 'NONE',  ( 0.000000000000000000, 3.267716535433071279, 0.2755905511810996522 ) ) ;
#28030=VECTOR ( 'NONE', #23967, 39.37007874015748143 ) ;
#28034=CARTESIAN_POINT ( 'NONE',  ( -0.2727639067037607723, 3.267716535433071279, 2.362204724409437961 ) ) ;
#28036=DIRECTION ( 'NONE',  ( -1.000000000000000000, 0.000000000000000000, 1.734723475976806848E-16 ) ) ;
#28037=VECTOR ( 'NONE', #22799, 39.37007874015748143 ) ;
#28040=ORIENTED_EDGE ( 'NONE', *, *, #1670, .T. ) ;
#28041=DIRECTION ( 'NONE',  ( -3.469446951953613696E-16, 0.000000000000000000, -1.000000000000000000 ) ) ;
#28042=EDGE_CURVE ( 'NONE', #30813, #16270, #1133, .T. ) ;
#28043=CARTESIAN_POINT ( 'NONE',  ( 0.5455278134075217666, 0.000000000000000000, 2.204724409448808764 ) ) ;
#28044=ORIENTED_EDGE ( 'NONE', *, *, #12221, .F. ) ;
#28046=DIRECTION ( 'NONE',  ( -3.469446951953613696E-16, 0.000000000000000000, -1.000000000000000000 ) ) ;
#28047=EDGE_CURVE ( 'NONE', #41410, #38137, #1394, .T. ) ;
#28049=CARTESIAN_POINT ( 'NONE',  ( -2.182111253630085290, 0.000000000000000000, 0.3149606299212578953 ) ) ;
#28050=ORIENTED_EDGE ( 'NONE', *, *, #26336, .F. ) ;
#28051=DIRECTION ( 'NONE',  ( 1.734723475976806848E-16, -0.000000000000000000, 1.000000000000000000 ) ) ;
#28052=DIRECTION ( 'NONE',  ( -0.000000000000000000, 1.000000000000000000, -0.000000000000000000 ) ) ;
#28053=CARTESIAN_POINT ( 'NONE',  ( -1.909347346926324462, 3.346456692913386100, 0.1574803149606286423 ) ) ;
#28055=ORIENTED_EDGE ( 'NONE', *, *, #29307, .T. ) ;
#28061=ORIENTED_EDGE ( 'NONE', *, *, #1473, .F. ) ;
#28065=ORIENTED_EDGE ( 'NONE', *, *, #42060, .F. ) ;
#28066=CARTESIAN_POINT ( 'NONE',  ( -1.909347346926324462, 0.000000000000000000, 0.1574803149606286423 ) ) ;
#28069=ORIENTED_EDGE ( 'NONE', *, *, #46673, .T. ) ;
#28070=EDGE_CURVE ( 'NONE', #12066, #24845, #5014, .T. ) ;
#28071=CARTESIAN_POINT ( 'NONE',  ( 1.015142113812069979, 0.000000000000000000, 1.535433070866133898 ) ) ;
#28072=EDGE_LOOP ( 'NONE', ( #11845, #7141, #19887, #47734 ) ) ;
#28074=ADVANCED_FACE ( 'NONE', ( #20507 ), #21019, .F. ) ;
#28075=CARTESIAN_POINT ( 'NONE',  ( 1.833433833923350909, 0.000000000000000000, -1.456692913385823296 ) ) ;
#28077=EDGE_LOOP ( 'NONE', ( #41803, #49575, #39303, #10753 ) ) ;
#28080=ORIENTED_EDGE ( 'NONE', *, *, #34645, .F. ) ;
#28082=VERTEX_POINT ( 'NONE', #885 ) ;
#28083=CARTESIAN_POINT ( 'NONE',  ( -3.927031490892378253E-16, 3.267716535433071279, -2.204724409448811429 ) ) ;
#28085=PLANE ( 'NONE',  #46147 ) ;
#28086=ORIENTED_EDGE ( 'NONE', *, *, #26222, .T. ) ;
#28087=ORIENTED_EDGE ( 'NONE', *, *, #2326, .T. ) ;
#28088=CARTESIAN_POINT ( 'NONE',  ( -1.363819533518803029, 3.346456692913386100, 0.4724409448818871482 ) ) ;
#28090=LINE ( 'NONE', #36368, #34901 ) ;
#28092=LINE ( 'NONE', #28610, #39646 ) ;
#28095=VERTEX_POINT ( 'NONE', #16643 ) ;
#28096=DIRECTION ( 'NONE',  ( 0.000000000000000000, 0.000000000000000000, -1.000000000000000000 ) ) ;
#28099=VERTEX_POINT ( 'NONE', #8885 ) ;
#28100=CARTESIAN_POINT ( 'NONE',  ( 0.000000000000000000, 3.267716535433071279, -1.299212598425194320 ) ) ;
#28101=EDGE_CURVE ( 'NONE', #2103, #43399, #24122, .T. ) ;
#28102=VECTOR ( 'NONE', #31381, 39.37007874015748143 ) ;
#28104=EDGE_CURVE ( 'NONE', #13984, #4136, #24640, .T. ) ;
#28110=CARTESIAN_POINT ( 'NONE',  ( -1.636583440222564301, 3.346456692913386100, -1.574803149606293307 ) ) ;
#28111=DIRECTION ( 'NONE',  ( 1.734723475976806848E-16, -0.000000000000000000, 1.000000000000000000 ) ) ;
#28112=VERTEX_POINT ( 'NONE', #47574 ) ;
#28113=FACE_OUTER_BOUND ( 'NONE', #2019, .T. ) ;
#28114=ORIENTED_EDGE ( 'NONE', *, *, #40882, .T. ) ;
#28115=DIRECTION ( 'NONE',  ( -1.000000000000000000, -0.000000000000000000, -0.000000000000000000 ) ) ;
#28116=CARTESIAN_POINT ( 'NONE',  ( -1.636583440222563635, 3.346456692913386100, 0.4330708661417290162 ) ) ;
#28119=VERTEX_POINT ( 'NONE', #4244 ) ;
#28124=DIRECTION ( 'NONE',  ( 1.000000000000000000, 0.000000000000000000, 0.000000000000000000 ) ) ;
#28125=FACE_BOUND ( 'NONE', #22457, .T. ) ;
#28127=VECTOR ( 'NONE', #18725, 39.37007874015748143 ) ;
#28128=AXIS2_PLACEMENT_3D ( 'NONE', #50942, #23892, #39638 ) ;
#28129=PLANE ( 'NONE',  #4790 ) ;
#28130=DIRECTION ( 'NONE',  ( -3.469446951953613696E-16, 0.000000000000000000, -1.000000000000000000 ) ) ;
#28131=EDGE_LOOP ( 'NONE', ( #40094, #27742, #35513, #42711 ) ) ;
#28132=CARTESIAN_POINT ( 'NONE',  ( -2.182111253630085290, 0.000000000000000000, -0.5118110236220464460 ) ) ;
#28133=VECTOR ( 'NONE', #37806, 39.37007874015748143 ) ;
#28135=ORIENTED_EDGE ( 'NONE', *, *, #3540, .T. ) ;
#28136=VECTOR ( 'NONE', #21170, 39.37007874015748143 ) ;
#28138=EDGE_CURVE ( 'NONE', #903, #20943, #20240, .T. ) ;
#28141=AXIS2_PLACEMENT_3D ( 'NONE', #49910, #41711, #3480 ) ;
#28142=DIRECTION ( 'NONE',  ( 1.000000000000000000, -0.000000000000000000, 0.000000000000000000 ) ) ;
#28143=DIRECTION ( 'NONE',  ( -0.000000000000000000, 0.000000000000000000, 1.000000000000000000 ) ) ;
#28144=LINE ( 'NONE', #39520, #24695 ) ;
#28145=VERTEX_POINT ( 'NONE', #9397 ) ;
#28146=ORIENTED_EDGE ( 'NONE', *, *, #49335, .F. ) ;
#28148=PLANE ( 'NONE',  #37871 ) ;
#28149=DIRECTION ( 'NONE',  ( -0.000000000000000000, 1.000000000000000000, -0.000000000000000000 ) ) ;
#28151=CARTESIAN_POINT ( 'NONE',  ( -0.5455278134075214336, 3.346456692913386100, -1.456692913385822630 ) ) ;
#28152=DIRECTION ( 'NONE',  ( -0.000000000000000000, 1.000000000000000000, -0.000000000000000000 ) ) ;
#28155=PLANE ( 'NONE',  #38438 ) ;
#28156=ORIENTED_EDGE ( 'NONE', *, *, #36175, .T. ) ;
#28157=DIRECTION ( 'NONE',  ( -1.000000000000000000, 0.000000000000000000, 1.734723475976806848E-16 ) ) ;
#28158=EDGE_CURVE ( 'NONE', #28712, #14290, #2420, .T. ) ;
#28160=EDGE_CURVE ( 'NONE', #18938, #36157, #41656, .T. ) ;
#28161=AXIS2_PLACEMENT_3D ( 'NONE', #98, #15844, #871 ) ;
#28163=PLANE ( 'NONE',  #19114 ) ;
#28164=VECTOR ( 'NONE', #43109, 39.37007874015748143 ) ;
#28165=DIRECTION ( 'NONE',  ( -1.000000000000000000, 0.000000000000000000, -0.000000000000000000 ) ) ;
#28170=VECTOR ( 'NONE', #29674, 39.37007874015748143 ) ;
#28171=EDGE_LOOP ( 'NONE', ( #34710, #290, #14979, #6800 ) ) ;
#28173=VECTOR ( 'NONE', #27814, 39.37007874015748143 ) ;
#28175=CARTESIAN_POINT ( 'NONE',  ( 0.1968503937007873017, 0.000000000000000000, -0.9448818897637765168 ) ) ;
#28177=AXIS2_PLACEMENT_3D ( 'NONE', #28486, #1636, #29520 ) ;
#28178=CARTESIAN_POINT ( 'NONE',  ( -1.166969139818016199, 3.267716535433071279, -0.6692913385826760875 ) ) ;
#28180=LINE ( 'NONE', #24322, #6274 ) ;
#28181=EDGE_CURVE ( 'NONE', #49388, #19556, #33421, .T. ) ;
#28182=VERTEX_POINT ( 'NONE', #29529 ) ;
#28183=ORIENTED_EDGE ( 'NONE', *, *, #19086, .T. ) ;
#28184=ORIENTED_EDGE ( 'NONE', *, *, #9664, .T. ) ;
#28185=LINE ( 'NONE', #33362, #46891 ) ;
#28186=VERTEX_POINT ( 'NONE', #44745 ) ;
#28187=ORIENTED_EDGE ( 'NONE', *, *, #20765, .T. ) ;
#28191=CARTESIAN_POINT ( 'NONE',  ( -1.091055626815042645, 3.267716535433071279, -1.889763779527552146 ) ) ;
#28193=ORIENTED_EDGE ( 'NONE', *, *, #19596, .F. ) ;
#28197=CARTESIAN_POINT ( 'NONE',  ( -0.8942052331142552601, 3.267716535433071279, -0.3149606299212593941 ) ) ;
#28198=ORIENTED_EDGE ( 'NONE', *, *, #19147, .F. ) ;
#28200=CARTESIAN_POINT ( 'NONE',  ( -0.8942052331142552601, 0.000000000000000000, 1.889763779527550147 ) ) ;
#28201=ORIENTED_EDGE ( 'NONE', *, *, #16552, .T. ) ;
#28205=CARTESIAN_POINT ( 'NONE',  ( -0.2727639067037608278, 0.000000000000000000, -0.3543307086614175816 ) ) ;
#28206=EDGE_CURVE ( 'NONE', #47575, #8060, #14282, .T. ) ;
#28207=DIRECTION ( 'NONE',  ( -1.000000000000000000, 0.000000000000000000, 1.734723475976806848E-16 ) ) ;
#28210=CARTESIAN_POINT ( 'NONE',  ( 0.8182917201112824834, 0.000000000000000000, 1.850393700787392293 ) ) ;
#28211=ORIENTED_EDGE ( 'NONE', *, *, #17621, .F. ) ;
#28212=ORIENTED_EDGE ( 'NONE', *, *, #7890, .F. ) ;
#28213=VECTOR ( 'NONE', #2746, 39.37007874015748143 ) ;
#28216=ORIENTED_EDGE ( 'NONE', *, *, #7310, .T. ) ;
#28220=FACE_OUTER_BOUND ( 'NONE', #19822, .T. ) ;
#28221=CARTESIAN_POINT ( 'NONE',  ( 0.8182917201112819283, 3.267716535433071279, -0.03937007874015881204 ) ) ;
#28222=LINE ( 'NONE', #47298, #4799 ) ;
#28223=ORIENTED_EDGE ( 'NONE', *, *, #3257, .T. ) ;
#28224=DIRECTION ( 'NONE',  ( 1.734723475976806848E-16, 0.000000000000000000, 1.000000000000000000 ) ) ;
#28225=CARTESIAN_POINT ( 'NONE',  ( -1.091055626815042645, 3.346456692913386100, -1.574803149606293529 ) ) ;
#28226=EDGE_CURVE ( 'NONE', #18884, #2388, #1903, .T. ) ;
#28227=ORIENTED_EDGE ( 'NONE', *, *, #35690, .F. ) ;
#28228=CARTESIAN_POINT ( 'NONE',  ( 0.000000000000000000, 0.000000000000000000, -2.952755905511811552 ) ) ;
#28230=CARTESIAN_POINT ( 'NONE',  ( -0.8182917201112814842, 3.346456692913386100, 1.220472440944875281 ) ) ;
#28233=LINE ( 'NONE', #39611, #39016 ) ;
#28235=CARTESIAN_POINT ( 'NONE',  ( 0.4696143004045479352, 3.267716535433071279, -0.1574803149606298636 ) ) ;
#28237=PLANE ( 'NONE',  #18098 ) ;
#28240=CARTESIAN_POINT ( 'NONE',  ( 0.5786196242795136335, 3.267716535433071279, -2.086614173228340086 ) ) ;
#28241=VECTOR ( 'NONE', #18574, 39.37007874015748143 ) ;
#28242=FACE_OUTER_BOUND ( 'NONE', #515, .T. ) ;
#28245=VECTOR ( 'NONE', #6313, 39.37007874015748143 ) ;
#28246=ORIENTED_EDGE ( 'NONE', *, *, #32502, .T. ) ;
#28247=ORIENTED_EDGE ( 'NONE', *, *, #11756, .F. ) ;
#28248=CARTESIAN_POINT ( 'NONE',  ( 1.636583440222563857, 0.000000000000000000, 0.1181102362204701633 ) ) ;
#28249=FACE_OUTER_BOUND ( 'NONE', #40052, .T. ) ;
#28250=ORIENTED_EDGE ( 'NONE', *, *, #8488, .F. ) ;
#28252=CARTESIAN_POINT ( 'NONE',  ( -0.6214413264104945434, 3.346456692913386100, -0.1574803149606301411 ) ) ;
#28253=LINE ( 'NONE', #4775, #47449 ) ;
#28255=CIRCLE ( 'NONE', #22483, 2.106299212598425008 ) ;
#28256=CARTESIAN_POINT ( 'NONE',  ( -0.6214413264104945434, 3.346456692913386100, -0.9842519685039342603 ) ) ;
#28258=ORIENTED_EDGE ( 'NONE', *, *, #7820, .T. ) ;
#28259=ORIENTED_EDGE ( 'NONE', *, *, #36794, .T. ) ;
#28260=CARTESIAN_POINT ( 'NONE',  ( -0.8942052331142552601, 3.346456692913386100, -1.574803149606293529 ) ) ;
#28261=DIRECTION ( 'NONE',  ( 1.000000000000000000, -0.000000000000000000, 0.000000000000000000 ) ) ;
#28264=CARTESIAN_POINT ( 'NONE',  ( 0.000000000000000000, 3.267716535433071279, -0.6692913385826758654 ) ) ;
#28265=FACE_BOUND ( 'NONE', #47499, .T. ) ;
#28269=ORIENTED_EDGE ( 'NONE', *, *, #47229, .T. ) ;
#28270=ORIENTED_EDGE ( 'NONE', *, *, #20423, .F. ) ;
#28272=ADVANCED_FACE ( 'NONE', ( #49100 ), #45246, .F. ) ;
#28273=EDGE_CURVE ( 'NONE', #25449, #5602, #36944, .T. ) ;
#28275=ORIENTED_EDGE ( 'NONE', *, *, #1423, .T. ) ;
#28276=ORIENTED_EDGE ( 'NONE', *, *, #39649, .F. ) ;
#28279=EDGE_LOOP ( 'NONE', ( #35263, #41185, #21860, #21486 ) ) ;
#28281=CARTESIAN_POINT ( 'NONE',  ( 0.8182917201112819283, 3.346456692913386100, 0.1574803149606286423 ) ) ;
#28283=DIRECTION ( 'NONE',  ( -0.000000000000000000, 0.000000000000000000, 1.000000000000000000 ) ) ;
#28285=DIRECTION ( 'NONE',  ( 1.000000000000000000, 0.000000000000000000, -3.469446951953613696E-16 ) ) ;
#28286=AXIS2_PLACEMENT_3D ( 'NONE', #4460, #35450, #27432 ) ;
#28287=DIRECTION ( 'NONE',  ( 0.000000000000000000, 1.000000000000000000, 0.000000000000000000 ) ) ;
#28288=DIRECTION ( 'NONE',  ( -0.000000000000000000, 1.000000000000000000, -0.000000000000000000 ) ) ;
#28290=CARTESIAN_POINT ( 'NONE',  ( -0.8942052331142547050, 3.346456692913386100, 1.259842519685033357 ) ) ;
#28291=AXIS2_PLACEMENT_3D ( 'NONE', #19220, #34982, #11729 ) ;
#28294=AXIS2_PLACEMENT_3D ( 'NONE', #43881, #48502, #44404 ) ;
#28296=VERTEX_POINT ( 'NONE', #9055 ) ;
#28297=CARTESIAN_POINT ( 'NONE',  ( -1.091055626815042645, 0.000000000000000000, 2.204724409448808764 ) ) ;
#28298=DIRECTION ( 'NONE',  ( -1.000000000000000000, 0.000000000000000000, 1.734723475976806848E-16 ) ) ;
#28301=LINE ( 'NONE', #44045, #48049 ) ;
#28302=EDGE_CURVE ( 'NONE', #54, #9880, #36170, .T. ) ;
#28304=VECTOR ( 'NONE', #28990, 39.37007874015748143 ) ;
#28308=CARTESIAN_POINT ( 'NONE',  ( 0.8182917201112817063, 0.000000000000000000, -1.732283464566923614 ) ) ;
#28309=DIRECTION ( 'NONE',  ( -1.000000000000000000, 0.000000000000000000, 1.734723475976806848E-16 ) ) ;
#28310=CARTESIAN_POINT ( 'NONE',  ( 0.2727639067037610499, 0.000000000000000000, 2.362204724409437961 ) ) ;
#28311=DIRECTION ( 'NONE',  ( 1.734723475976806848E-16, -0.000000000000000000, 1.000000000000000000 ) ) ;
#28313=ORIENTED_EDGE ( 'NONE', *, *, #11822, .T. ) ;
#28314=CARTESIAN_POINT ( 'NONE',  ( 0.000000000000000000, 3.267716535433071279, -1.889763779527552146 ) ) ;
#28317=ORIENTED_EDGE ( 'NONE', *, *, #23122, .F. ) ;
#28318=DIRECTION ( 'NONE',  ( -3.469446951953613696E-16, 0.000000000000000000, -1.000000000000000000 ) ) ;
#28319=ORIENTED_EDGE ( 'NONE', *, *, #49585, .F. ) ;
#28320=FACE_OUTER_BOUND ( 'NONE', #47403, .T. ) ;
#28322=FACE_OUTER_BOUND ( 'NONE', #29660, .T. ) ;
#28323=ORIENTED_EDGE ( 'NONE', *, *, #21703, .F. ) ;
#28325=VECTOR ( 'NONE', #35613, 39.37007874015748143 ) ;
#28326=ORIENTED_EDGE ( 'NONE', *, *, #15655, .T. ) ;
#28327=VECTOR ( 'NONE', #24394, 39.37007874015748143 ) ;
#28329=CARTESIAN_POINT ( 'NONE',  ( 1.015142113812069313, 3.267716535433071279, -3.521981712565032882E-16 ) ) ;
#28332=ORIENTED_EDGE ( 'NONE', *, *, #29410, .T. ) ;
#28333=ORIENTED_EDGE ( 'NONE', *, *, #44186, .T. ) ;
#28335=ADVANCED_FACE ( 'NONE', ( #48252 ), #47736, .F. ) ;
#28338=CARTESIAN_POINT ( 'NONE',  ( 2.106197740627111514, 3.346456692913386100, -0.7874015748031473194 ) ) ;
#28341=LINE ( 'NONE', #24484, #39874 ) ;
#28343=ORIENTED_EDGE ( 'NONE', *, *, #36353, .F. ) ;
#28348=CARTESIAN_POINT ( 'NONE',  ( -1.909347346926324906, 3.346456692913386100, -1.102362204724405492 ) ) ;
#28350=LINE ( 'NONE', #48953, #10350 ) ;
#28352=ADVANCED_FACE ( 'NONE', ( #20665 ), #48761, .F. ) ;
#28353=DIRECTION ( 'NONE',  ( -1.000000000000000000, 0.000000000000000000, 0.000000000000000000 ) ) ;
#28354=ORIENTED_EDGE ( 'NONE', *, *, #45134, .T. ) ;
#28358=EDGE_LOOP ( 'NONE', ( #42074, #22265, #48059, #6365 ) ) ;
#28359=DIRECTION ( 'NONE',  ( 0.000000000000000000, -1.000000000000000000, 0.000000000000000000 ) ) ;
#28360=AXIS2_PLACEMENT_3D ( 'NONE', #41066, #9564, #36679 ) ;
#28363=ORIENTED_EDGE ( 'NONE', *, *, #30297, .F. ) ;
#28365=DIRECTION ( 'NONE',  ( 1.000000000000000000, 0.000000000000000000, 0.000000000000000000 ) ) ;
#28366=VECTOR ( 'NONE', #35918, 39.37007874015748143 ) ;
#28367=DIRECTION ( 'NONE',  ( 1.000000000000000000, 0.000000000000000000, 0.000000000000000000 ) ) ;
#28368=FACE_OUTER_BOUND ( 'NONE', #34041, .T. ) ;
#28369=CARTESIAN_POINT ( 'NONE',  ( 1.363819533518803029, 3.267716535433071279, -1.417322834645665219 ) ) ;
#28370=ORIENTED_EDGE ( 'NONE', *, *, #31430, .F. ) ;
#28371=LINE ( 'NONE', #33040, #43905 ) ;
#28374=VERTEX_POINT ( 'NONE', #44658 ) ;
#28375=CARTESIAN_POINT ( 'NONE',  ( -1.909347346926324906, 3.346456692913386100, 1.220472440944875059 ) ) ;
#28377=FACE_OUTER_BOUND ( 'NONE', #6603, .T. ) ;
#28378=CARTESIAN_POINT ( 'NONE',  ( 1.636583440222563857, 3.346456692913386100, -1.161035397307311917E-15 ) ) ;
#28379=CARTESIAN_POINT ( 'NONE',  ( -0.8182917201112814842, 3.346456692913386100, 0.5905511811023582691 ) ) ;
#28381=ORIENTED_EDGE ( 'NONE', *, *, #41481, .F. ) ;
#28382=CARTESIAN_POINT ( 'NONE',  ( 0.1968503937007877735, 3.267716535433071279, 0.7480314960629874665 ) ) ;
#28383=CARTESIAN_POINT ( 'NONE',  ( -2.182111253630085290, 0.000000000000000000, 0.6299212598425164567 ) ) ;
#28384=CARTESIAN_POINT ( 'NONE',  ( 0.2727639067037602172, 3.346456692913386100, -1.732283464566922726 ) ) ;
#28385=CARTESIAN_POINT ( 'NONE',  ( 0.000000000000000000, 3.267716535433071279, 0.9448818897637749625 ) ) ;
#28386=CARTESIAN_POINT ( 'NONE',  ( -1.439733046521776361, 3.267716535433071279, 0.7480314960629874665 ) ) ;
#28387=VERTEX_POINT ( 'NONE', #25056 ) ;
#28389=EDGE_CURVE ( 'NONE', #3623, #28112, #40811, .T. ) ;
#28391=ADVANCED_FACE ( 'NONE', ( #44914 ), #37200, .F. ) ;
#28392=VERTEX_POINT ( 'NONE', #45665 ) ;
#28393=VECTOR ( 'NONE', #40559, 39.37007874015748143 ) ;
#28395=EDGE_CURVE ( 'NONE', #43099, #30730, #33330, .T. ) ;
#28397=ORIENTED_EDGE ( 'NONE', *, *, #48118, .T. ) ;
#28402=CARTESIAN_POINT ( 'NONE',  ( 0.000000000000000000, 3.267716535433071279, 0.000000000000000000 ) ) ;
#28404=EDGE_LOOP ( 'NONE', ( #38045, #49971, #10920, #16027 ) ) ;
#28406=DIRECTION ( 'NONE',  ( 0.000000000000000000, -1.000000000000000000, 0.000000000000000000 ) ) ;
#28407=LINE ( 'NONE', #9057, #24990 ) ;
#28408=FACE_OUTER_BOUND ( 'NONE', #14676, .T. ) ;
#28410=EDGE_CURVE ( 'NONE', #13181, #45498, #21697, .T. ) ;
#28411=DIRECTION ( 'NONE',  ( 1.000000000000000000, 0.000000000000000000, -3.469446951953613696E-16 ) ) ;
#28413=PLANE ( 'NONE',  #36816 ) ;
#28414=ORIENTED_EDGE ( 'NONE', *, *, #40394, .T. ) ;
#28416=LINE ( 'NONE', #35666, #44972 ) ;
#28417=EDGE_CURVE ( 'NONE', #329, #6620, #22459, .T. ) ;
#28419=ORIENTED_EDGE ( 'NONE', *, *, #14414, .F. ) ;
#28420=CARTESIAN_POINT ( 'NONE',  ( 1.091055626815042645, 0.000000000000000000, 1.062992125984246083 ) ) ;
#28421=DIRECTION ( 'NONE',  ( -0.000000000000000000, 1.000000000000000000, -0.000000000000000000 ) ) ;
#28422=DIRECTION ( 'NONE',  ( -3.469446951953613696E-16, 0.000000000000000000, -1.000000000000000000 ) ) ;
#28423=ORIENTED_EDGE ( 'NONE', *, *, #12176, .F. ) ;
#28426=VECTOR ( 'NONE', #28353, 39.37007874015748143 ) ;
#28428=ORIENTED_EDGE ( 'NONE', *, *, #45054, .F. ) ;
#28429=CARTESIAN_POINT ( 'NONE',  ( -0.07591351300297333182, 3.267716535433071279, -1.732283464566922726 ) ) ;
#28430=VECTOR ( 'NONE', #34489, 39.37007874015748143 ) ;
#28432=DIRECTION ( 'NONE',  ( 1.734723475976806848E-16, 0.000000000000000000, 1.000000000000000000 ) ) ;
#28433=FACE_OUTER_BOUND ( 'NONE', #6426, .T. ) ;
#28434=LINE ( 'NONE', #4438, #34290 ) ;
#28435=ORIENTED_EDGE ( 'NONE', *, *, #17457, .F. ) ;
#28437=ORIENTED_EDGE ( 'NONE', *, *, #6581, .T. ) ;
#28439=DIRECTION ( 'NONE',  ( 1.734723475976806848E-16, -0.000000000000000000, 1.000000000000000000 ) ) ;
#28440=ORIENTED_EDGE ( 'NONE', *, *, #45460, .T. ) ;
#28441=ORIENTED_EDGE ( 'NONE', *, *, #49031, .F. ) ;
#28442=PLANE ( 'NONE',  #36339 ) ;
#28443=CARTESIAN_POINT ( 'NONE',  ( 1.091055626815042645, 0.000000000000000000, -1.141732283464564013 ) ) ;
#28446=LINE ( 'NONE', #24593, #42767 ) ;
#28448=CARTESIAN_POINT ( 'NONE',  ( -0.8942052331142552601, 3.346456692913386100, -0.6299212598425177889 ) ) ;
#28450=CARTESIAN_POINT ( 'NONE',  ( 0.5455278134075211005, 0.000000000000000000, -1.141732283464564013 ) ) ;
#28451=DIRECTION ( 'NONE',  ( 1.000000000000000000, 0.000000000000000000, -3.469446951953613696E-16 ) ) ;
#28452=EDGE_CURVE ( 'NONE', #12460, #1675, #13953, .T. ) ;
#28453=EDGE_LOOP ( 'NONE', ( #43865, #23021, #37512, #22287 ) ) ;
#28456=EDGE_LOOP ( 'NONE', ( #17487, #10482, #2717, #39678 ) ) ;
#28458=CARTESIAN_POINT ( 'NONE',  ( 1.363819533518803251, 0.000000000000000000, 0.4724409448818871482 ) ) ;
#28459=FACE_OUTER_BOUND ( 'NONE', #40542, .T. ) ;
#28460=EDGE_CURVE ( 'NONE', #42073, #15363, #45161, .T. ) ;
#28461=LINE ( 'NONE', #48809, #16509 ) ;
#28463=EDGE_CURVE ( 'NONE', #17559, #21385, #6464, .T. ) ;
#28466=ORIENTED_EDGE ( 'NONE', *, *, #140, .T. ) ;
#28467=VECTOR ( 'NONE', #27781, 39.37007874015748143 ) ;
#28469=FACE_OUTER_BOUND ( 'NONE', #11303, .T. ) ;
#28471=ORIENTED_EDGE ( 'NONE', *, *, #28417, .T. ) ;
#28472=DIRECTION ( 'NONE',  ( -0.000000000000000000, 1.000000000000000000, -0.000000000000000000 ) ) ;
#28476=AXIS2_PLACEMENT_3D ( 'NONE', #29986, #5979, #45703 ) ;
#28477=DIRECTION ( 'NONE',  ( -0.000000000000000000, 1.000000000000000000, -0.000000000000000000 ) ) ;
#28478=DIRECTION ( 'NONE',  ( -1.000000000000000000, 0.000000000000000000, 1.734723475976806848E-16 ) ) ;
#28479=DIRECTION ( 'NONE',  ( 1.000000000000000000, 0.000000000000000000, -3.469446951953613696E-16 ) ) ;
#28480=VECTOR ( 'NONE', #44562, 39.37007874015748143 ) ;
#28482=DIRECTION ( 'NONE',  ( -1.000000000000000000, 0.000000000000000000, 1.734723475976806848E-16 ) ) ;
#28486=CARTESIAN_POINT ( 'NONE',  ( 0.8182917201112817063, 0.000000000000000000, -1.417322834645664331 ) ) ;
#28487=DIRECTION ( 'NONE',  ( 0.000000000000000000, 0.000000000000000000, -1.000000000000000000 ) ) ;
#28489=EDGE_CURVE ( 'NONE', #44295, #46164, #49276, .T. ) ;
#28490=ORIENTED_EDGE ( 'NONE', *, *, #7548, .F. ) ;
#28492=DIRECTION ( 'NONE',  ( -1.000000000000000000, 0.000000000000000000, 1.734723475976806848E-16 ) ) ;
#28495=DIRECTION ( 'NONE',  ( -3.469446951953613696E-16, 0.000000000000000000, -1.000000000000000000 ) ) ;
#28496=DIRECTION ( 'NONE',  ( 1.000000000000000000, 0.000000000000000000, 0.000000000000000000 ) ) ;
#28497=ORIENTED_EDGE ( 'NONE', *, *, #49576, .F. ) ;
#28498=DIRECTION ( 'NONE',  ( -0.000000000000000000, 1.000000000000000000, -0.000000000000000000 ) ) ;
#28499=EDGE_CURVE ( 'NONE', #16378, #32340, #49772, .T. ) ;
#28500=DIRECTION ( 'NONE',  ( -1.000000000000000000, 0.000000000000000000, -0.000000000000000000 ) ) ;
#28501=DIRECTION ( 'NONE',  ( 0.000000000000000000, 0.000000000000000000, -1.000000000000000000 ) ) ;
#28504=ORIENTED_EDGE ( 'NONE', *, *, #5607, .F. ) ;
#28505=DIRECTION ( 'NONE',  ( 1.000000000000000000, 0.000000000000000000, 0.000000000000000000 ) ) ;
#28507=LINE ( 'NONE', #13543, #2385 ) ;
#28511=CARTESIAN_POINT ( 'NONE',  ( -2.182111253630085290, 3.346456692913386100, 0.3149606299212578953 ) ) ;
#28514=LINE ( 'NONE', #44264, #25691 ) ;
#28515=ORIENTED_EDGE ( 'NONE', *, *, #3050, .F. ) ;
#28517=DIRECTION ( 'NONE',  ( 1.734723475976806848E-16, -0.000000000000000000, 1.000000000000000000 ) ) ;
#28518=CARTESIAN_POINT ( 'NONE',  ( 0.7423782071083087075, 3.267716535433071279, -0.9448818897637765168 ) ) ;
#28520=DIRECTION ( 'NONE',  ( -0.000000000000000000, 1.000000000000000000, -0.000000000000000000 ) ) ;
#28521=ORIENTED_EDGE ( 'NONE', *, *, #33568, .T. ) ;
#28522=CARTESIAN_POINT ( 'NONE',  ( -0.07591351300297340121, 3.267716535433071279, -0.3543307086614175816 ) ) ;
#28523=FACE_BOUND ( 'NONE', #44765, .T. ) ;
#28524=VECTOR ( 'NONE', #4701, 39.37007874015748143 ) ;
#28526=LINE ( 'NONE', #44276, #1840 ) ;
#28529=LINE ( 'NONE', #44279, #9391 ) ;
#28531=EDGE_CURVE ( 'NONE', #31184, #37535, #2332, .T. ) ;
#28532=ORIENTED_EDGE ( 'NONE', *, *, #4455, .T. ) ;
#28533=EDGE_LOOP ( 'NONE', ( #42055, #47464, #31556, #15424 ) ) ;
#28534=LINE ( 'NONE', #19763, #17839 ) ;
#28535=EDGE_CURVE ( 'NONE', #50863, #33328, #29698, .T. ) ;
#28536=VERTEX_POINT ( 'NONE', #45922 ) ;
#28537=FACE_OUTER_BOUND ( 'NONE', #46641, .T. ) ;
#28538=DIRECTION ( 'NONE',  ( -0.000000000000000000, 1.000000000000000000, -0.000000000000000000 ) ) ;
#28539=DIRECTION ( 'NONE',  ( -0.000000000000000000, 1.000000000000000000, -0.000000000000000000 ) ) ;
#28540=VECTOR ( 'NONE', #29, 39.37007874015748143 ) ;
#28543=CARTESIAN_POINT ( 'NONE',  ( 0.000000000000000000, 3.267716535433071279, 0.7874015748031456541 ) ) ;
#28546=DIRECTION ( 'NONE',  ( 1.000000000000000000, 0.000000000000000000, 0.000000000000000000 ) ) ;
#28547=VECTOR ( 'NONE', #36102, 39.37007874015748143 ) ;
#28548=CARTESIAN_POINT ( 'NONE',  ( -1.363819533518803029, 3.346456692913386100, 0.1574803149606287811 ) ) ;
#28549=AXIS2_PLACEMENT_3D ( 'NONE', #18688, #19173, #50617 ) ;
#28551=ORIENTED_EDGE ( 'NONE', *, *, #37368, .T. ) ;
#28553=DIRECTION ( 'NONE',  ( 1.734723475976806848E-16, -0.000000000000000000, 1.000000000000000000 ) ) ;
#28554=ORIENTED_EDGE ( 'NONE', *, *, #31514, .F. ) ;
#28555=CARTESIAN_POINT ( 'NONE',  ( -1.166969139818015977, 3.346456692913386100, 1.732283464566920950 ) ) ;
#28556=VECTOR ( 'NONE', #40678, 39.37007874015748143 ) ;
#28557=EDGE_CURVE ( 'NONE', #41994, #1801, #26329, .T. ) ;
#28559=CARTESIAN_POINT ( 'NONE',  ( 2.017116292511733189, 3.267716535433071279, -0.7874015748031473194 ) ) ;
#28560=AXIS2_PLACEMENT_3D ( 'NONE', #48918, #24965, #1219 ) ;
#28562=PLANE ( 'NONE',  #10072 ) ;
#28563=ORIENTED_EDGE ( 'NONE', *, *, #24349, .F. ) ;
#28564=FACE_BOUND ( 'NONE', #23566, .T. ) ;
#28565=ADVANCED_FACE ( 'NONE', ( #18081 ), #42075, .F. ) ;
#28566=PLANE ( 'NONE',  #43201 ) ;
#28567=CARTESIAN_POINT ( 'NONE',  ( 0.000000000000000000, 3.267716535433071279, -1.732283464566922726 ) ) ;
#28570=EDGE_LOOP ( 'NONE', ( #48414, #17519, #48123, #34007 ) ) ;
#28572=ORIENTED_EDGE ( 'NONE', *, *, #28104, .T. ) ;
#28573=ADVANCED_FACE ( 'NONE', ( #2836 ), #40303, .F. ) ;
#28574=CARTESIAN_POINT ( 'NONE',  ( 1.015142113812069091, 3.267716535433071279, -3.521981712565031896E-16 ) ) ;
#28575=VERTEX_POINT ( 'NONE', #21193 ) ;
#28576=ADVANCED_FACE ( 'NONE', ( #9569 ), #36427, .F. ) ;
#28577=CARTESIAN_POINT ( 'NONE',  ( -1.712496953225537188, 3.346456692913386100, 0.2755905511810996522 ) ) ;
#28579=DIRECTION ( 'NONE',  ( 0.000000000000000000, -1.000000000000000000, 0.000000000000000000 ) ) ;
#28580=VECTOR ( 'NONE', #3035, 39.37007874015748143 ) ;
#28581=LINE ( 'NONE', #21106, #41316 ) ;
#28584=AXIS2_PLACEMENT_3D ( 'NONE', #15594, #39084, #19955 ) ;
#28587=ADVANCED_FACE ( 'NONE', ( #36946, #36172 ), #32829, .F. ) ;
#28588=CARTESIAN_POINT ( 'NONE',  ( 0.000000000000000000, 3.346456692913386100, 0.000000000000000000 ) ) ;
#28589=VECTOR ( 'NONE', #20209, 39.37007874015748143 ) ;
#28590=ORIENTED_EDGE ( 'NONE', *, *, #24521, .T. ) ;
#28591=ORIENTED_EDGE ( 'NONE', *, *, #2960, .T. ) ;
#28592=EDGE_CURVE ( 'NONE', #5349, #28852, #9312, .T. ) ;
#28596=EDGE_CURVE ( 'NONE', #35032, #50405, #44156, .T. ) ;
#28597=ORIENTED_EDGE ( 'NONE', *, *, #42702, .F. ) ;
#28600=CARTESIAN_POINT ( 'NONE',  ( 0.7423782071083082634, 0.000000000000000000, -2.086614173228340086 ) ) ;
#28601=LINE ( 'NONE', #44087, #34938 ) ;
#28604=VERTEX_POINT ( 'NONE', #4926 ) ;
#28605=DIRECTION ( 'NONE',  ( 0.000000000000000000, 1.000000000000000000, 0.000000000000000000 ) ) ;
#28606=DIRECTION ( 'NONE',  ( -0.000000000000000000, 1.000000000000000000, -0.000000000000000000 ) ) ;
#28609=PLANE ( 'NONE',  #49882 ) ;
#28610=CARTESIAN_POINT ( 'NONE',  ( 0.000000000000000000, 3.267716535433071279, -0.1968503937007886062 ) ) ;
#28612=ORIENTED_EDGE ( 'NONE', *, *, #28592, .F. ) ;
#28613=CARTESIAN_POINT ( 'NONE',  ( -1.985260859929297572, 3.346456692913386100, -6.146657985744592735E-16 ) ) ;
#28614=VECTOR ( 'NONE', #49092, 39.37007874015748143 ) ;
#28615=EDGE_CURVE ( 'NONE', #10739, #46962, #24804, .T. ) ;
#28617=ORIENTED_EDGE ( 'NONE', *, *, #8744, .T. ) ;
#28618=VECTOR ( 'NONE', #15656, 39.37007874015748143 ) ;
#28619=LINE ( 'NONE', #9262, #44876 ) ;
#28621=CARTESIAN_POINT ( 'NONE',  ( 0.000000000000000000, 3.267716535433071279, 0.000000000000000000 ) ) ;
#28623=CARTESIAN_POINT ( 'NONE',  ( 0.000000000000000000, 3.267716535433071279, -0.6692913385826760875 ) ) ;
#28624=DIRECTION ( 'NONE',  ( 1.000000000000000000, 0.000000000000000000, 0.000000000000000000 ) ) ;
#28625=EDGE_CURVE ( 'NONE', #514, #10053, #1569, .T. ) ;
#28628=VERTEX_POINT ( 'NONE', #33078 ) ;
#28632=EDGE_LOOP ( 'NONE', ( #22055, #42002, #42641, #11769 ) ) ;
#28635=EDGE_LOOP ( 'NONE', ( #15878, #40135, #18237, #26545 ) ) ;
#28636=DIRECTION ( 'NONE',  ( 1.000000000000000000, 0.000000000000000000, 0.000000000000000000 ) ) ;
#28638=EDGE_CURVE ( 'NONE', #14307, #26807, #28669, .T. ) ;
#28641=VERTEX_POINT ( 'NONE', #41075 ) ;
#28642=DIRECTION ( 'NONE',  ( -1.000000000000000000, -0.000000000000000000, -0.000000000000000000 ) ) ;
#28643=CARTESIAN_POINT ( 'NONE',  ( -2.182111253630085290, 0.000000000000000000, -0.1968503937007880511 ) ) ;
#28644=DIRECTION ( 'NONE',  ( -1.000000000000000000, 0.000000000000000000, 1.734723475976806848E-16 ) ) ;
#28646=DIRECTION ( 'NONE',  ( 0.000000000000000000, 0.000000000000000000, -1.000000000000000000 ) ) ;
#28647=CARTESIAN_POINT ( 'NONE',  ( 0.5455278134075216556, 3.346456692913386100, 2.095509194042718626 ) ) ;
#28648=VECTOR ( 'NONE', #38508, 39.37007874015748143 ) ;
#28649=VECTOR ( 'NONE', #49029, 39.37007874015748143 ) ;
#28650=ORIENTED_EDGE ( 'NONE', *, *, #32831, .T. ) ;
#28651=EDGE_CURVE ( 'NONE', #22611, #44092, #37202, .T. ) ;
#28652=EDGE_CURVE ( 'NONE', #44838, #40529, #28407, .T. ) ;
#28654=EDGE_CURVE ( 'NONE', #924, #7692, #43890, .T. ) ;
#28656=VERTEX_POINT ( 'NONE', #41830 ) ;
#28657=ORIENTED_EDGE ( 'NONE', *, *, #12467, .T. ) ;
#28659=EDGE_LOOP ( 'NONE', ( #40576, #41967, #42885, #44 ) ) ;
#28661=DIRECTION ( 'NONE',  ( 0.000000000000000000, 1.000000000000000000, 0.000000000000000000 ) ) ;
#28662=CARTESIAN_POINT ( 'NONE',  ( -2.258024766633058622, 0.000000000000000000, -0.1574803149606298636 ) ) ;
#28663=CARTESIAN_POINT ( 'NONE',  ( -0.5455278134075208785, 0.000000000000000000, 0.4330708661417290162 ) ) ;
#28665=EDGE_LOOP ( 'NONE', ( #9030, #23330, #43403, #32559 ) ) ;
#28669=LINE ( 'NONE', #40039, #34066 ) ;
#28670=LINE ( 'NONE', #5948, #33405 ) ;
#28671=CARTESIAN_POINT ( 'NONE',  ( 0.000000000000000000, 3.267716535433071279, 0.7874015748031454320 ) ) ;
#28673=CARTESIAN_POINT ( 'NONE',  ( -2.182111253630085290, 0.000000000000000000, 0.7480314960629874665 ) ) ;
#28674=ORIENTED_EDGE ( 'NONE', *, *, #44645, .T. ) ;
#28678=ORIENTED_EDGE ( 'NONE', *, *, #28843, .F. ) ;
#28680=CARTESIAN_POINT ( 'NONE',  ( -1.195183497228115035E-16, 0.000000000000000000, -1.259842519685035134 ) ) ;
#28681=EDGE_CURVE ( 'NONE', #30948, #2778, #2839, .T. ) ;
#28682=CIRCLE ( 'NONE', #6442, 2.443628662382284489 ) ;
#28683=ORIENTED_EDGE ( 'NONE', *, *, #47845, .T. ) ;
#28684=VECTOR ( 'NONE', #10787, 39.37007874015748143 ) ;
#28687=ORIENTED_EDGE ( 'NONE', *, *, #29760, .T. ) ;
#28688=LINE ( 'NONE', #10353, #2325 ) ;
#28689=AXIS2_PLACEMENT_3D ( 'NONE', #28458, #1098, #28719 ) ;
#28690=ORIENTED_EDGE ( 'NONE', *, *, #10614, .T. ) ;
#28691=ORIENTED_EDGE ( 'NONE', *, *, #13652, .F. ) ;
#28694=DIRECTION ( 'NONE',  ( 0.000000000000000000, 0.000000000000000000, -1.000000000000000000 ) ) ;
#28696=EDGE_LOOP ( 'NONE', ( #1109, #16651, #19660, #40786 ) ) ;
#28697=VERTEX_POINT ( 'NONE', #30465 ) ;
#28699=LINE ( 'NONE', #17098, #31272 ) ;
#28700=ORIENTED_EDGE ( 'NONE', *, *, #3984, .F. ) ;
#28701=ORIENTED_EDGE ( 'NONE', *, *, #41668, .T. ) ;
#28702=LINE ( 'NONE', #24071, #33105 ) ;
#28703=LINE ( 'NONE', #21477, #8764 ) ;
#28704=LINE ( 'NONE', #44452, #29415 ) ;
#28705=ADVANCED_FACE ( 'NONE', ( #5947 ), #37717, .F. ) ;
#28706=ORIENTED_EDGE ( 'NONE', *, *, #14831, .T. ) ;
#28707=EDGE_CURVE ( 'NONE', #17115, #11080, #13955, .T. ) ;
#28709=DIRECTION ( 'NONE',  ( -0.000000000000000000, 1.000000000000000000, -0.000000000000000000 ) ) ;
#28711=LINE ( 'NONE', #28448, #23675 ) ;
#28712=VERTEX_POINT ( 'NONE', #45163 ) ;
#28713=DIRECTION ( 'NONE',  ( 1.000000000000000000, 0.000000000000000000, 0.000000000000000000 ) ) ;
#28716=CARTESIAN_POINT ( 'NONE',  ( 0.000000000000000000, 3.267716535433071279, 0.000000000000000000 ) ) ;
#28717=ORIENTED_EDGE ( 'NONE', *, *, #7097, .T. ) ;
#28719=DIRECTION ( 'NONE',  ( 1.000000000000000000, 0.000000000000000000, 0.000000000000000000 ) ) ;
#28720=DIRECTION ( 'NONE',  ( -0.000000000000000000, 1.000000000000000000, -0.000000000000000000 ) ) ;
#28722=AXIS2_PLACEMENT_3D ( 'NONE', #20438, #37163, #24317 ) ;
#28725=VERTEX_POINT ( 'NONE', #9828 ) ;
#28728=VECTOR ( 'NONE', #32104, 39.37007874015748143 ) ;
#28731=DIRECTION ( 'NONE',  ( -0.000000000000000000, 1.000000000000000000, -0.000000000000000000 ) ) ;
#28732=VECTOR ( 'NONE', #3761, 39.37007874015748143 ) ;
#28733=AXIS2_PLACEMENT_3D ( 'NONE', #3871, #19600, #15491 ) ;
#28734=VECTOR ( 'NONE', #37895, 39.37007874015748143 ) ;
#28735=PLANE ( 'NONE',  #27478 ) ;
#28737=LINE ( 'NONE', #12482, #8028 ) ;
#28738=ORIENTED_EDGE ( 'NONE', *, *, #29046, .F. ) ;
#28739=CARTESIAN_POINT ( 'NONE',  ( -1.024442997624234601E-17, 3.267716535433071279, 1.777125317778812071E-33 ) ) ;
#28741=PLANE ( 'NONE',  #49582 ) ;
#28742=ORIENTED_EDGE ( 'NONE', *, *, #15486, .F. ) ;
#28743=LINE ( 'NONE', #36505, #10870 ) ;
#28744=VECTOR ( 'NONE', #17004, 39.37007874015748143 ) ;
#28745=PLANE ( 'NONE',  #23676 ) ;
#28746=CARTESIAN_POINT ( 'NONE',  ( -1.636583440222563635, 3.346456692913386100, -4.780733988912460139E-16 ) ) ;
#28748=DIRECTION ( 'NONE',  ( 1.000000000000000000, 0.000000000000000000, 0.000000000000000000 ) ) ;
#28749=CARTESIAN_POINT ( 'NONE',  ( -0.2727639067037608278, 0.000000000000000000, -1.299212598425193210 ) ) ;
#28750=EDGE_CURVE ( 'NONE', #29680, #46268, #45416, .T. ) ;
#28751=EDGE_CURVE ( 'NONE', #49645, #43429, #22712, .T. ) ;
#28753=CARTESIAN_POINT ( 'NONE',  ( 0.4696143004045479352, 0.000000000000000000, -1.417322834645664331 ) ) ;
#28754=DIRECTION ( 'NONE',  ( 1.000000000000000000, -0.000000000000000000, 0.000000000000000000 ) ) ;
#28756=LINE ( 'NONE', #33164, #17976 ) ;
#28757=EDGE_CURVE ( 'NONE', #27988, #9844, #6713, .T. ) ;
#28758=DIRECTION ( 'NONE',  ( -0.000000000000000000, 1.000000000000000000, -0.000000000000000000 ) ) ;
#28759=LINE ( 'NONE', #49105, #30485 ) ;
#28760=DIRECTION ( 'NONE',  ( 1.734723475976806848E-16, 0.000000000000000000, 1.000000000000000000 ) ) ;
#28761=VECTOR ( 'NONE', #43483, 39.37007874015748143 ) ;
#28762=EDGE_CURVE ( 'NONE', #35037, #50954, #25565, .T. ) ;
#28764=ORIENTED_EDGE ( 'NONE', *, *, #40056, .F. ) ;
#28766=CARTESIAN_POINT ( 'NONE',  ( 0.1968503937007872462, 3.346456692913386100, -0.5118110236220465570 ) ) ;
#28767=DIRECTION ( 'NONE',  ( 1.734723475976806848E-16, -0.000000000000000000, 1.000000000000000000 ) ) ;
#28768=ORIENTED_EDGE ( 'NONE', *, *, #14983, .F. ) ;
#28769=DIRECTION ( 'NONE',  ( -1.000000000000000000, 0.000000000000000000, -0.000000000000000000 ) ) ;
#28771=CARTESIAN_POINT ( 'NONE',  ( -1.712496953225537188, 3.346456692913386100, 0.7874015748031456541 ) ) ;
#28773=VECTOR ( 'NONE', #8841, 39.37007874015748143 ) ;
#28774=AXIS2_PLACEMENT_3D ( 'NONE', #40864, #21242, #12222 ) ;
#28776=EDGE_LOOP ( 'NONE', ( #24833, #23680, #41675, #37227 ) ) ;
#28777=EDGE_CURVE ( 'NONE', #24413, #32550, #25822, .T. ) ;
#28778=ADVANCED_FACE ( 'NONE', ( #18333 ), #1818, .F. ) ;
#28779=LINE ( 'NONE', #13298, #18019 ) ;
#28781=CARTESIAN_POINT ( 'NONE',  ( 1.091055626815042645, 3.267716535433071279, -1.892679809432644882E-16 ) ) ;
#28782=VERTEX_POINT ( 'NONE', #49018 ) ;
#28784=DIRECTION ( 'NONE',  ( -0.000000000000000000, 1.000000000000000000, -0.000000000000000000 ) ) ;
#28785=FACE_BOUND ( 'NONE', #37722, .T. ) ;
#28787=EDGE_CURVE ( 'NONE', #38287, #9419, #13701, .T. ) ;
#28788=CARTESIAN_POINT ( 'NONE',  ( 2.083268748869757658, 3.346456692913386100, 0.5905511811023582691 ) ) ;
#28789=ORIENTED_EDGE ( 'NONE', *, *, #49403, .T. ) ;
#28791=VECTOR ( 'NONE', #37342, 39.37007874015748143 ) ;
#28794=CARTESIAN_POINT ( 'NONE',  ( -0.6214413264104945434, 0.000000000000000000, -2.244094488188968395 ) ) ;
#28795=EDGE_LOOP ( 'NONE', ( #30314, #49737, #16663, #10830 ) ) ;
#28797=DIRECTION ( 'NONE',  ( 1.734723475976806848E-16, 0.000000000000000000, 1.000000000000000000 ) ) ;
#28798=EDGE_CURVE ( 'NONE', #187, #14069, #38219, .T. ) ;
#28799=LINE ( 'NONE', #14074, #8798 ) ;
#28800=LINE ( 'NONE', #28029, #1989 ) ;
#28801=AXIS2_PLACEMENT_3D ( 'NONE', #48792, #13223, #13473 ) ;
#28804=DIRECTION ( 'NONE',  ( -0.000000000000000000, 1.000000000000000000, -0.000000000000000000 ) ) ;
#28808=CARTESIAN_POINT ( 'NONE',  ( 0.5455278134075208785, 0.000000000000000000, -1.889763779527552812 ) ) ;
#28809=CIRCLE ( 'NONE', #37081, 2.443628662382284489 ) ;
#28810=ORIENTED_EDGE ( 'NONE', *, *, #33851, .T. ) ;
#28811=DIRECTION ( 'NONE',  ( -0.000000000000000000, 1.000000000000000000, -0.000000000000000000 ) ) ;
#28813=ORIENTED_EDGE ( 'NONE', *, *, #18206, .F. ) ;
#28814=CARTESIAN_POINT ( 'NONE',  ( 0.000000000000000000, 3.267716535433071279, 0.000000000000000000 ) ) ;
#28815=CARTESIAN_POINT ( 'NONE',  ( 1.833433833923351353, 3.346456692913386100, 1.259842519685033135 ) ) ;
#28817=DIRECTION ( 'NONE',  ( -1.000000000000000000, 0.000000000000000000, -0.000000000000000000 ) ) ;
#28819=ORIENTED_EDGE ( 'NONE', *, *, #46890, .F. ) ;
#28820=DIRECTION ( 'NONE',  ( -3.469446951953613696E-16, 0.000000000000000000, -1.000000000000000000 ) ) ;
#28821=AXIS2_PLACEMENT_3D ( 'NONE', #6554, #38551, #14802 ) ;
#28822=VERTEX_POINT ( 'NONE', #10333 ) ;
#28823=FACE_BOUND ( 'NONE', #42404, .T. ) ;
#28824=EDGE_CURVE ( 'NONE', #23728, #28782, #22461, .T. ) ;
#28825=CARTESIAN_POINT ( 'NONE',  ( 1.560669927219590303, 0.000000000000000000, -1.102362204724405714 ) ) ;
#28827=LINE ( 'NONE', #29078, #28480 ) ;
#28829=EDGE_CURVE ( 'NONE', #1905, #1056, #18594, .T. ) ;
#28832=CARTESIAN_POINT ( 'NONE',  ( -0.6214413264104945434, 3.267716535433071279, 2.156057715732901026E-16 ) ) ;
#28833=ORIENTED_EDGE ( 'NONE', *, *, #8952, .T. ) ;
#28834=CARTESIAN_POINT ( 'NONE',  ( -1.712496953225537188, 3.267716535433071279, 1.102362204724404160 ) ) ;
#28835=EDGE_LOOP ( 'NONE', ( #31, #28363, #39334, #21101 ) ) ;
#28836=FACE_OUTER_BOUND ( 'NONE', #50848, .T. ) ;
#28837=EDGE_CURVE ( 'NONE', #16144, #5349, #27326, .T. ) ;
#28839=EDGE_LOOP ( 'NONE', ( #18804, #27796, #15800, #2750 ) ) ;
#28842=VERTEX_POINT ( 'NONE', #11590 ) ;
#28843=EDGE_CURVE ( 'NONE', #4283, #15792, #43583, .T. ) ;
#28844=CARTESIAN_POINT ( 'NONE',  ( -2.258024766633058622, 0.000000000000000000, -0.03937007874015881204 ) ) ;
#28845=ORIENTED_EDGE ( 'NONE', *, *, #29220, .T. ) ;
#28846=VERTEX_POINT ( 'NONE', #39212 ) ;
#28848=EDGE_CURVE ( 'NONE', #17243, #24661, #12104, .T. ) ;
#28850=ORIENTED_EDGE ( 'NONE', *, *, #42960, .F. ) ;
#28852=VERTEX_POINT ( 'NONE', #35601 ) ;
#28853=CIRCLE ( 'NONE', #1664, 2.165354330708661568 ) ;
#28854=CARTESIAN_POINT ( 'NONE',  ( -0.8182917201112819283, 3.346456692913386100, 2.047244094488179567 ) ) ;
#28857=DIRECTION ( 'NONE',  ( 1.000000000000000000, 0.000000000000000000, 0.000000000000000000 ) ) ;
#28859=ORIENTED_EDGE ( 'NONE', *, *, #40590, .F. ) ;
#28860=LINE ( 'NONE', #44592, #48338 ) ;
#28861=CARTESIAN_POINT ( 'NONE',  ( 1.909347346926324684, 3.346456692913386100, -0.4724409448818889246 ) ) ;
#28862=LINE ( 'NONE', #3655, #32411 ) ;
#28863=DIRECTION ( 'NONE',  ( -0.000000000000000000, 1.000000000000000000, -0.000000000000000000 ) ) ;
#28865=CARTESIAN_POINT ( 'NONE',  ( 0.5455278134075212115, 3.346456692913386100, 0.3149606299212576177 ) ) ;
#28866=EDGE_CURVE ( 'NONE', #9684, #17906, #38470, .T. ) ;
#28867=CARTESIAN_POINT ( 'NONE',  ( -1.439733046521777027, 3.346456692913386100, -1.141732283464563791 ) ) ;
#28868=CARTESIAN_POINT ( 'NONE',  ( -1.363819533518803029, 0.000000000000000000, 0.7874015748031456541 ) ) ;
#28869=ORIENTED_EDGE ( 'NONE', *, *, #19309, .F. ) ;
#28872=ORIENTED_EDGE ( 'NONE', *, *, #9592, .F. ) ;
#28875=DIRECTION ( 'NONE',  ( -0.000000000000000000, 1.000000000000000000, -0.000000000000000000 ) ) ;
#28878=VECTOR ( 'NONE', #42759, 39.37007874015748143 ) ;
#28879=DIRECTION ( 'NONE',  ( -3.469446951953613696E-16, 0.000000000000000000, -1.000000000000000000 ) ) ;
#28880=VECTOR ( 'NONE', #21752, 39.37007874015748143 ) ;
#28881=PLANE ( 'NONE',  #35822 ) ;
#28882=DIRECTION ( 'NONE',  ( 1.000000000000000000, 0.000000000000000000, 0.000000000000000000 ) ) ;
#28883=EDGE_LOOP ( 'NONE', ( #7276, #561, #18508, #47082 ) ) ;
#28885=LINE ( 'NONE', #16769, #32407 ) ;
#28886=DIRECTION ( 'NONE',  ( -3.469446951953613696E-16, 0.000000000000000000, -1.000000000000000000 ) ) ;
#28889=VECTOR ( 'NONE', #50246, 39.37007874015748143 ) ;
#28890=VERTEX_POINT ( 'NONE', #27582 ) ;
#28891=PLANE ( 'NONE',  #20258 ) ;
#28892=CARTESIAN_POINT ( 'NONE',  ( -1.636583440222564301, 3.346456692913386100, -1.259842519685034468 ) ) ;
#28895=EDGE_LOOP ( 'NONE', ( #3865, #19302, #37819, #47914 ) ) ;
#28896=ORIENTED_EDGE ( 'NONE', *, *, #10869, .F. ) ;
#28897=LINE ( 'NONE', #12913, #15284 ) ;
#28898=CARTESIAN_POINT ( 'NONE',  ( 1.636583440222563857, 3.267716535433071279, 1.574803149606291974 ) ) ;
#28900=VERTEX_POINT ( 'NONE', #27077 ) ;
#28901=DIRECTION ( 'NONE',  ( -0.000000000000000000, 1.000000000000000000, -0.000000000000000000 ) ) ;
#28902=LINE ( 'NONE', #48996, #24208 ) ;
#28904=ORIENTED_EDGE ( 'NONE', *, *, #6642, .T. ) ;
#28905=LINE ( 'NONE', #48494, #29059 ) ;
#28907=ORIENTED_EDGE ( 'NONE', *, *, #30878, .F. ) ;
#28909=ADVANCED_FACE ( 'NONE', ( #7467 ), #11342, .F. ) ;
#28910=EDGE_LOOP ( 'NONE', ( #31301, #43498, #8015, #4468 ) ) ;
#28911=DIRECTION ( 'NONE',  ( 1.734723475976806848E-16, -0.000000000000000000, 1.000000000000000000 ) ) ;
#28912=AXIS2_PLACEMENT_3D ( 'NONE', #23211, #35096, #47171 ) ;
#28913=CARTESIAN_POINT ( 'NONE',  ( 1.636583440222563857, 3.346456692913386100, -0.3149606299212596716 ) ) ;
#28914=B_SPLINE_CURVE_WITH_KNOTS ( 'NONE', 3,
 ( #30056, #45771, #26180, #41926 ),
 .UNSPECIFIED., .F., .F.,
 ( 4, 4 ),
 ( 0.02729311668581372446, 0.02847067742387721784 ),
 .UNSPECIFIED. ) ;
#28915=VECTOR ( 'NONE', #435, 39.37007874015748143 ) ;
#28916=EDGE_CURVE ( 'NONE', #6701, #25223, #31471, .T. ) ;
#28917=EDGE_CURVE ( 'NONE', #16822, #16156, #27838, .T. ) ;
#28918=CARTESIAN_POINT ( 'NONE',  ( 1.287906020515830141, 3.346456692913386100, 0.9448818897637746295 ) ) ;
#28920=EDGE_LOOP ( 'NONE', ( #5163, #17481, #4322, #39711 ) ) ;
#28923=DIRECTION ( 'NONE',  ( -3.469446951953613696E-16, 0.000000000000000000, -1.000000000000000000 ) ) ;
#28924=DIRECTION ( 'NONE',  ( -1.000000000000000000, 0.000000000000000000, 1.734723475976806848E-16 ) ) ;
#28925=ADVANCED_FACE ( 'NONE', ( #15968 ), #50275, .F. ) ;
#28927=PLANE ( 'NONE',  #48192 ) ;
#28930=DIRECTION ( 'NONE',  ( -0.000000000000000000, 1.000000000000000000, -0.000000000000000000 ) ) ;
#28931=VERTEX_POINT ( 'NONE', #47168 ) ;
#28934=VERTEX_POINT ( 'NONE', #7972 ) ;
#28935=EDGE_CURVE ( 'NONE', #29992, #18572, #4109, .T. ) ;
#28937=CARTESIAN_POINT ( 'NONE',  ( 0.000000000000000000, 3.267716535433071279, 1.850393700787392293 ) ) ;
#28938=CARTESIAN_POINT ( 'NONE',  ( 1.287906020515830141, 3.267716535433071279, 0.3149606299212578953 ) ) ;
#28943=DIRECTION ( 'NONE',  ( -1.000000000000000000, 0.000000000000000000, 1.734723475976806848E-16 ) ) ;
#28945=VECTOR ( 'NONE', #24692, 39.37007874015748143 ) ;
#28946=DIRECTION ( 'NONE',  ( 1.734723475976806848E-16, -0.000000000000000000, 1.000000000000000000 ) ) ;
#28947=LINE ( 'NONE', #20954, #35459 ) ;
#28948=VECTOR ( 'NONE', #4588, 39.37007874015748143 ) ;
#28950=VERTEX_POINT ( 'NONE', #26827 ) ;
#28951=ORIENTED_EDGE ( 'NONE', *, *, #38050, .T. ) ;
#28953=ORIENTED_EDGE ( 'NONE', *, *, #3778, .F. ) ;
#28955=DIRECTION ( 'NONE',  ( -0.000000000000000000, 0.000000000000000000, 1.000000000000000000 ) ) ;
#28956=DIRECTION ( 'NONE',  ( 0.000000000000000000, 0.000000000000000000, -1.000000000000000000 ) ) ;
#28958=CARTESIAN_POINT ( 'NONE',  ( -1.909347346926324462, 3.346456692913386100, -0.3543307086614171930 ) ) ;
#28959=VECTOR ( 'NONE', #39156, 39.37007874015748143 ) ;
#28960=VERTEX_POINT ( 'NONE', #47939 ) ;
#28961=LINE ( 'NONE', #47784, #45223 ) ;
#28963=CARTESIAN_POINT ( 'NONE',  ( 1.909347346926324684, 3.267716535433071279, 0.5905511811023582691 ) ) ;
#28965=CARTESIAN_POINT ( 'NONE',  ( 2.106197740627111514, 0.000000000000000000, -1.102362204724406602 ) ) ;
#28967=CARTESIAN_POINT ( 'NONE',  ( -1.091055626815042645, 0.000000000000000000, 1.889763779527550147 ) ) ;
#28970=CARTESIAN_POINT ( 'NONE',  ( -0.8942052331142547050, 3.267716535433071279, 0.7480314960629874665 ) ) ;
#28971=LINE ( 'NONE', #44709, #25571 ) ;
#28974=DIRECTION ( 'NONE',  ( -0.000000000000000000, 1.000000000000000000, -0.000000000000000000 ) ) ;
#28975=FACE_OUTER_BOUND ( 'NONE', #44170, .T. ) ;
#28977=ORIENTED_EDGE ( 'NONE', *, *, #16728, .F. ) ;
#28978=EDGE_CURVE ( 'NONE', #46962, #4005, #48697, .T. ) ;
#28979=CARTESIAN_POINT ( 'NONE',  ( -0.6214413264104945434, 3.346456692913386100, -0.7874015748031467643 ) ) ;
#28980=ORIENTED_EDGE ( 'NONE', *, *, #23337, .F. ) ;
#28981=CARTESIAN_POINT ( 'NONE',  ( 1.833433833923351353, 0.000000000000000000, -0.3149606299212596716 ) ) ;
#28982=DIRECTION ( 'NONE',  ( -1.000000000000000000, 0.000000000000000000, -0.000000000000000000 ) ) ;
#28984=VECTOR ( 'NONE', #19750, 39.37007874015748143 ) ;
#28985=LINE ( 'NONE', #6009, #6890 ) ;
#28987=VECTOR ( 'NONE', #9668, 39.37007874015748143 ) ;
#28988=DIRECTION ( 'NONE',  ( -0.000000000000000000, 1.000000000000000000, -0.000000000000000000 ) ) ;
#28990=DIRECTION ( 'NONE',  ( -0.000000000000000000, 1.000000000000000000, -0.000000000000000000 ) ) ;
#28992=EDGE_CURVE ( 'NONE', #50367, #30196, #8487, .T. ) ;
#28994=DIRECTION ( 'NONE',  ( -0.000000000000000000, 1.000000000000000000, -0.000000000000000000 ) ) ;
#28995=ORIENTED_EDGE ( 'NONE', *, *, #49941, .F. ) ;
#28997=CARTESIAN_POINT ( 'NONE',  ( 1.244991204790707684, 3.346456692913386100, -1.771653543307081691 ) ) ;
#28999=DIRECTION ( 'NONE',  ( 1.734723475976806848E-16, 0.000000000000000000, 1.000000000000000000 ) ) ;
#29000=DIRECTION ( 'NONE',  ( -3.469446951953613696E-16, 0.000000000000000000, -1.000000000000000000 ) ) ;
#29002=DIRECTION ( 'NONE',  ( -3.469446951953613696E-16, 0.000000000000000000, -1.000000000000000000 ) ) ;
#29003=ADVANCED_FACE ( 'NONE', ( #48194 ), #8998, .F. ) ;
#29004=DIRECTION ( 'NONE',  ( 1.000000000000000000, -0.000000000000000000, 0.000000000000000000 ) ) ;
#29005=EDGE_CURVE ( 'NONE', #48104, #4710, #44595, .T. ) ;
#29006=ORIENTED_EDGE ( 'NONE', *, *, #17752, .F. ) ;
#29007=CARTESIAN_POINT ( 'NONE',  ( 0.000000000000000000, 3.267716535433071279, -1.889763779527552146 ) ) ;
#29009=VERTEX_POINT ( 'NONE', #4360 ) ;
#29010=EDGE_CURVE ( 'NONE', #7441, #6293, #24238, .T. ) ;
#29011=DIRECTION ( 'NONE',  ( 0.000000000000000000, 0.000000000000000000, -1.000000000000000000 ) ) ;
#29012=DIRECTION ( 'NONE',  ( -3.469446951953613696E-16, 0.000000000000000000, -1.000000000000000000 ) ) ;
#29013=PLANE ( 'NONE',  #34578 ) ;
#29015=DIRECTION ( 'NONE',  ( 1.734723475976806848E-16, -0.000000000000000000, 1.000000000000000000 ) ) ;
#29016=EDGE_LOOP ( 'NONE', ( #9498, #34537, #13006, #477 ) ) ;
#29018=LINE ( 'NONE', #29792, #43797 ) ;
#29019=DIRECTION ( 'NONE',  ( -3.469446951953613696E-16, 0.000000000000000000, -1.000000000000000000 ) ) ;
#29021=DIRECTION ( 'NONE',  ( 0.000000000000000000, 0.000000000000000000, -1.000000000000000000 ) ) ;
#29022=LINE ( 'NONE', #21036, #7951 ) ;
#29023=LINE ( 'NONE', #901, #45857 ) ;
#29025=ORIENTED_EDGE ( 'NONE', *, *, #50395, .T. ) ;
#29027=ORIENTED_EDGE ( 'NONE', *, *, #47374, .T. ) ;
#29028=DIRECTION ( 'NONE',  ( 0.000000000000000000, 0.000000000000000000, -1.000000000000000000 ) ) ;
#29030=DIRECTION ( 'NONE',  ( -1.000000000000000000, 0.000000000000000000, 0.000000000000000000 ) ) ;
#29033=AXIS2_PLACEMENT_3D ( 'NONE', #31191, #30681, #46893 ) ;
#29034=FACE_BOUND ( 'NONE', #45586, .T. ) ;
#29037=ORIENTED_EDGE ( 'NONE', *, *, #4623, .F. ) ;
#29041=VECTOR ( 'NONE', #44673, 39.37007874015748143 ) ;
#29042=ORIENTED_EDGE ( 'NONE', *, *, #4548, .F. ) ;
#29045=ORIENTED_EDGE ( 'NONE', *, *, #39645, .T. ) ;
#29046=EDGE_CURVE ( 'NONE', #8962, #19997, #39724, .T. ) ;
#29047=ADVANCED_FACE ( 'NONE', ( #39980 ), #9251, .F. ) ;
#29049=FACE_OUTER_BOUND ( 'NONE', #13608, .T. ) ;
#29050=EDGE_CURVE ( 'NONE', #35680, #38409, #35852, .T. ) ;
#29052=CARTESIAN_POINT ( 'NONE',  ( -1.909347346926324906, 3.267716535433071279, -1.299212598425193210 ) ) ;
#29058=ORIENTED_EDGE ( 'NONE', *, *, #5967, .T. ) ;
#29059=VECTOR ( 'NONE', #44642, 39.37007874015748143 ) ;
#29060=DIRECTION ( 'NONE',  ( -1.000000000000000000, 0.000000000000000000, 1.734723475976806848E-16 ) ) ;
#29063=ORIENTED_EDGE ( 'NONE', *, *, #43554, .F. ) ;
#29065=LINE ( 'NONE', #20565, #4493 ) ;
#29066=DIRECTION ( 'NONE',  ( 1.000000000000000000, -0.000000000000000000, 0.000000000000000000 ) ) ;
#29067=AXIS2_PLACEMENT_3D ( 'NONE', #37881, #5606, #13866 ) ;
#29068=ADVANCED_FACE ( 'NONE', ( #40751 ), #20869, .F. ) ;
#29071=DIRECTION ( 'NONE',  ( 1.000000000000000000, -0.000000000000000000, 0.000000000000000000 ) ) ;
#29072=ORIENTED_EDGE ( 'NONE', *, *, #49196, .F. ) ;
#29073=FACE_BOUND ( 'NONE', #9246, .T. ) ;
#29074=CARTESIAN_POINT ( 'NONE',  ( -1.363819533518803029, 3.346456692913386100, 1.102362204724404160 ) ) ;
#29077=CARTESIAN_POINT ( 'NONE',  ( -0.5455278134075216556, 3.267716535433071279, -2.381957271744193250 ) ) ;
#29078=CARTESIAN_POINT ( 'NONE',  ( 0.000000000000000000, 3.267716535433071279, 0.2755905511810998187 ) ) ;
#29081=DIRECTION ( 'NONE',  ( -0.000000000000000000, 1.000000000000000000, -0.000000000000000000 ) ) ;
#29082=EDGE_LOOP ( 'NONE', ( #48560, #1888, #19165, #33553 ) ) ;
#29083=CARTESIAN_POINT ( 'NONE',  ( 2.182111253630085290, 3.346456692913386100, 0.6299212598425161236 ) ) ;
#29084=ORIENTED_EDGE ( 'NONE', *, *, #48484, .F. ) ;
#29085=CARTESIAN_POINT ( 'NONE',  ( 2.106197740627111958, 3.267716535433071279, 0.5905511811023582691 ) ) ;
#29087=CARTESIAN_POINT ( 'NONE',  ( -0.8182917201112814842, 3.267716535433071279, 0.2755905511810998187 ) ) ;
#29088=DIRECTION ( 'NONE',  ( 1.734723475976806848E-16, -0.000000000000000000, 1.000000000000000000 ) ) ;
#29089=ORIENTED_EDGE ( 'NONE', *, *, #16176, .F. ) ;
#29090=CARTESIAN_POINT ( 'NONE',  ( 1.015142113812069313, 3.346456692913386100, 0.4724409448818868706 ) ) ;
#29091=EDGE_LOOP ( 'NONE', ( #3219, #36549, #1836, #4229 ) ) ;
#29092=ORIENTED_EDGE ( 'NONE', *, *, #29349, .F. ) ;
#29095=VERTEX_POINT ( 'NONE', #20614 ) ;
#29096=DIRECTION ( 'NONE',  ( 1.000000000000000000, 0.000000000000000000, 0.000000000000000000 ) ) ;
#29099=EDGE_CURVE ( 'NONE', #35527, #31327, #28090, .T. ) ;
#29100=ORIENTED_EDGE ( 'NONE', *, *, #48486, .T. ) ;
#29101=CARTESIAN_POINT ( 'NONE',  ( 0.5455278134075212115, 0.000000000000000000, -6.146657985744592735E-16 ) ) ;
#29102=VERTEX_POINT ( 'NONE', #992 ) ;
#29103=DIRECTION ( 'NONE',  ( 1.000000000000000000, 0.000000000000000000, -3.469446951953613696E-16 ) ) ;
#29105=CIRCLE ( 'NONE', #4378, 2.952755905511811552 ) ;
#29107=VECTOR ( 'NONE', #44097, 39.37007874015748143 ) ;
#29108=B_SPLINE_CURVE_WITH_KNOTS ( 'NONE', 3,
 ( #15950, #36352, #8464, #24474 ),
 .UNSPECIFIED., .F., .F.,
 ( 4, 4 ),
 ( 0.02871092247522269783, 0.03111204650372608252 ),
 .UNSPECIFIED. ) ;
#29110=EDGE_CURVE ( 'NONE', #44277, #35815, #33779, .T. ) ;
#29112=EDGE_LOOP ( 'NONE', ( #37759, #40521, #46843, #47837 ) ) ;
#29115=AXIS2_PLACEMENT_3D ( 'NONE', #2472, #29319, #37335 ) ;
#29118=CARTESIAN_POINT ( 'NONE',  ( -0.2727639067037602727, 0.000000000000000000, 1.850393700787392293 ) ) ;
#29119=DIRECTION ( 'NONE',  ( -0.000000000000000000, 1.000000000000000000, -0.000000000000000000 ) ) ;
#29120=DIRECTION ( 'NONE',  ( -0.000000000000000000, 1.000000000000000000, -0.000000000000000000 ) ) ;
#29121=CARTESIAN_POINT ( 'NONE',  ( -1.166969139818015977, 3.267716535433071279, -0.1574803149606300023 ) ) ;
#29122=EDGE_CURVE ( 'NONE', #37129, #34200, #29890, .T. ) ;
#29123=ORIENTED_EDGE ( 'NONE', *, *, #45464, .T. ) ;
#29125=CARTESIAN_POINT ( 'NONE',  ( -0.5455278134075208785, 3.346456692913386100, 0.7480314960629874665 ) ) ;
#29126=ORIENTED_EDGE ( 'NONE', *, *, #8466, .F. ) ;
#29127=CARTESIAN_POINT ( 'NONE',  ( 2.106197740627111514, 3.201134874551266218, -1.299212598425194320 ) ) ;
#29128=EDGE_CURVE ( 'NONE', #50633, #36517, #30773, .T. ) ;
#29129=EDGE_LOOP ( 'NONE', ( #2800, #8268, #1165, #6194 ) ) ;
#29130=DIRECTION ( 'NONE',  ( 1.000000000000000000, 0.000000000000000000, 0.000000000000000000 ) ) ;
#29131=DIRECTION ( 'NONE',  ( -1.000000000000000000, 0.000000000000000000, 0.000000000000000000 ) ) ;
#29134=DIRECTION ( 'NONE',  ( 0.000000000000000000, 0.000000000000000000, 1.000000000000000000 ) ) ;
#29135=ORIENTED_EDGE ( 'NONE', *, *, #1010, .F. ) ;
#29136=ADVANCED_FACE ( 'NONE', ( #38155 ), #18527, .F. ) ;
#29141=ORIENTED_EDGE ( 'NONE', *, *, #10007, .F. ) ;
#29145=ORIENTED_EDGE ( 'NONE', *, *, #27977, .T. ) ;
#29146=VECTOR ( 'NONE', #7628, 39.37007874015748143 ) ;
#29147=VECTOR ( 'NONE', #29509, 39.37007874015748143 ) ;
#29148=FACE_OUTER_BOUND ( 'NONE', #30163, .T. ) ;
#29151=AXIS2_PLACEMENT_3D ( 'NONE', #1117, #28482, #12484 ) ;
#29152=CARTESIAN_POINT ( 'NONE',  ( -0.3486774197067340486, 3.346456692913386100, 2.077238655036873549 ) ) ;
#29154=VERTEX_POINT ( 'NONE', #14650 ) ;
#29156=CARTESIAN_POINT ( 'NONE',  ( 0.4696143004045484348, 3.267716535433071279, 0.9055118110236167750 ) ) ;
#29157=FACE_BOUND ( 'NONE', #18232, .T. ) ;
#29158=ORIENTED_EDGE ( 'NONE', *, *, #2217, .T. ) ;
#29159=CARTESIAN_POINT ( 'NONE',  ( -0.5455278134075208785, 0.000000000000000000, 0.6299212598425164567 ) ) ;
#29160=DIRECTION ( 'NONE',  ( -1.000000000000000000, 0.000000000000000000, 0.000000000000000000 ) ) ;
#29161=ORIENTED_EDGE ( 'NONE', *, *, #9830, .T. ) ;
#29162=DIRECTION ( 'NONE',  ( 1.000000000000000000, -0.000000000000000000, 0.000000000000000000 ) ) ;
#29163=FACE_OUTER_BOUND ( 'NONE', #44309, .T. ) ;
#29166=ORIENTED_EDGE ( 'NONE', *, *, #31102, .F. ) ;
#29168=EDGE_CURVE ( 'NONE', #1172, #23037, #48090, .T. ) ;
#29169=CARTESIAN_POINT ( 'NONE',  ( 0.5455278134075216556, 3.267716535433071279, 2.095509194042718626 ) ) ;
#29170=EDGE_CURVE ( 'NONE', #1675, #3555, #22147, .T. ) ;
#29172=EDGE_CURVE ( 'NONE', #3461, #50816, #49714, .T. ) ;
#29174=ORIENTED_EDGE ( 'NONE', *, *, #15655, .F. ) ;
#29175=VERTEX_POINT ( 'NONE', #18015 ) ;
#29177=DIRECTION ( 'NONE',  ( -0.000000000000000000, 1.000000000000000000, -0.000000000000000000 ) ) ;
#29181=VECTOR ( 'NONE', #47641, 39.37007874015748143 ) ;
#29182=DIRECTION ( 'NONE',  ( 0.000000000000000000, 0.000000000000000000, -1.000000000000000000 ) ) ;
#29183=AXIS2_PLACEMENT_3D ( 'NONE', #30540, #37791, #42398 ) ;
#29187=DIRECTION ( 'NONE',  ( 0.000000000000000000, 0.000000000000000000, -1.000000000000000000 ) ) ;
#29190=DIRECTION ( 'NONE',  ( -1.000000000000000000, 0.000000000000000000, -0.000000000000000000 ) ) ;
#29191=CARTESIAN_POINT ( 'NONE',  ( 0.000000000000000000, 3.267716535433071279, 0.1181102362204701633 ) ) ;
#29192=ORIENTED_EDGE ( 'NONE', *, *, #32699, .T. ) ;
#29193=EDGE_LOOP ( 'NONE', ( #24622, #27879, #37812, #20424 ) ) ;
#29194=CARTESIAN_POINT ( 'NONE',  ( -0.2727639067037602727, 0.000000000000000000, 0.5905511811023582691 ) ) ;
#29195=DIRECTION ( 'NONE',  ( 1.734723475976806848E-16, 0.000000000000000000, 1.000000000000000000 ) ) ;
#29198=VERTEX_POINT ( 'NONE', #48952 ) ;
#29199=FACE_OUTER_BOUND ( 'NONE', #23169, .T. ) ;
#29203=DIRECTION ( 'NONE',  ( 1.734723475976806848E-16, 0.000000000000000000, 1.000000000000000000 ) ) ;
#29204=EDGE_CURVE ( 'NONE', #24856, #19187, #10265, .T. ) ;
#29207=ORIENTED_EDGE ( 'NONE', *, *, #11608, .F. ) ;
#29208=ORIENTED_EDGE ( 'NONE', *, *, #14977, .T. ) ;
#29209=DIRECTION ( 'NONE',  ( 1.000000000000000000, 0.000000000000000000, 0.000000000000000000 ) ) ;
#29210=AXIS2_PLACEMENT_3D ( 'NONE', #36749, #32892, #9376 ) ;
#29211=ORIENTED_EDGE ( 'NONE', *, *, #46888, .T. ) ;
#29212=ORIENTED_EDGE ( 'NONE', *, *, #6289, .F. ) ;
#29213=ADVANCED_FACE ( 'NONE', ( #30140 ), #25255, .F. ) ;
#29214=VECTOR ( 'NONE', #25461, 39.37007874015748143 ) ;
#29215=DIRECTION ( 'NONE',  ( -0.000000000000000000, 1.000000000000000000, -0.000000000000000000 ) ) ;
#29216=PLANE ( 'NONE',  #50751 ) ;
#29217=CARTESIAN_POINT ( 'NONE',  ( -1.091055626815042645, 3.267716535433071279, -0.3149606299212593941 ) ) ;
#29219=VECTOR ( 'NONE', #15169, 39.37007874015748143 ) ;
#29220=EDGE_CURVE ( 'NONE', #14432, #11679, #25501, .T. ) ;
#29221=VECTOR ( 'NONE', #33788, 39.37007874015748143 ) ;
#29222=ORIENTED_EDGE ( 'NONE', *, *, #43632, .F. ) ;
#29223=CARTESIAN_POINT ( 'NONE',  ( 0.000000000000000000, 3.267716535433071279, 0.000000000000000000 ) ) ;
#29225=CARTESIAN_POINT ( 'NONE',  ( 1.006250229852934774, 3.346456692913386100, 1.850393700787392293 ) ) ;
#29226=VERTEX_POINT ( 'NONE', #33268 ) ;
#29227=CARTESIAN_POINT ( 'NONE',  ( 1.363819533518803251, 3.346456692913386100, 0.7874015748031454320 ) ) ;
#29229=VECTOR ( 'NONE', #42830, 39.37007874015748143 ) ;
#29231=VERTEX_POINT ( 'NONE', #13637 ) ;
#29232=ORIENTED_EDGE ( 'NONE', *, *, #21146, .F. ) ;
#29233=EDGE_CURVE ( 'NONE', #8254, #15045, #29380, .T. ) ;
#29234=DIRECTION ( 'NONE',  ( -3.469446951953613696E-16, 0.000000000000000000, -1.000000000000000000 ) ) ;
#29235=LINE ( 'NONE', #1103, #14601 ) ;
#29236=EDGE_CURVE ( 'NONE', #32813, #42496, #10016, .T. ) ;
#29237=LINE ( 'NONE', #26381, #36266 ) ;
#29238=EDGE_LOOP ( 'NONE', ( #34379, #14490, #45265, #3443 ) ) ;
#29239=ORIENTED_EDGE ( 'NONE', *, *, #24037, .F. ) ;
#29245=DIRECTION ( 'NONE',  ( 0.000000000000000000, -1.000000000000000000, 0.000000000000000000 ) ) ;
#29246=DIRECTION ( 'NONE',  ( -0.000000000000000000, 0.000000000000000000, 1.000000000000000000 ) ) ;
#29248=ORIENTED_EDGE ( 'NONE', *, *, #6480, .T. ) ;
#29249=VECTOR ( 'NONE', #31790, 39.37007874015748143 ) ;
#29250=LINE ( 'NONE', #14019, #20073 ) ;
#29251=AXIS2_PLACEMENT_3D ( 'NONE', #12676, #28411, #44160 ) ;
#29252=CYLINDRICAL_SURFACE ( 'NONE', #1796, 2.874015748031496731 ) ;
#29253=VECTOR ( 'NONE', #21852, 39.37007874015748143 ) ;
#29256=LINE ( 'NONE', #13011, #44652 ) ;
#29258=DIRECTION ( 'NONE',  ( 1.000000000000000000, 0.000000000000000000, -3.469446951953613696E-16 ) ) ;
#29259=ORIENTED_EDGE ( 'NONE', *, *, #18628, .F. ) ;
#29260=EDGE_CURVE ( 'NONE', #50954, #10852, #41763, .T. ) ;
#29262=LINE ( 'NONE', #25391, #40731 ) ;
#29263=VECTOR ( 'NONE', #27887, 39.37007874015748143 ) ;
#29265=DIRECTION ( 'NONE',  ( 1.000000000000000000, 0.000000000000000000, -3.469446951953613696E-16 ) ) ;
#29266=CARTESIAN_POINT ( 'NONE',  ( -0.07591351300297333182, 3.346456692913386100, -0.7874015748031470974 ) ) ;
#29267=ORIENTED_EDGE ( 'NONE', *, *, #40257, .T. ) ;
#29268=LINE ( 'NONE', #1906, #42692 ) ;
#29269=EDGE_CURVE ( 'NONE', #43429, #10488, #38402, .T. ) ;
#29270=FACE_OUTER_BOUND ( 'NONE', #19676, .T. ) ;
#29271=CARTESIAN_POINT ( 'NONE',  ( 2.182111253630085290, 3.267716535433071279, -3.785359618865289765E-16 ) ) ;
#29272=CARTESIAN_POINT ( 'NONE',  ( -1.439733046521776361, 0.000000000000000000, 0.1181102362204704270 ) ) ;
#29278=VERTEX_POINT ( 'NONE', #32120 ) ;
#29279=DIRECTION ( 'NONE',  ( -1.000000000000000000, -0.000000000000000000, -0.000000000000000000 ) ) ;
#29281=EDGE_LOOP ( 'NONE', ( #27941, #47802, #41378, #10115 ) ) ;
#29282=LINE ( 'NONE', #17923, #20100 ) ;
#29284=CARTESIAN_POINT ( 'NONE',  ( -0.2727639067037610499, 3.346456692913386100, -2.088563196121306476 ) ) ;
#29285=ORIENTED_EDGE ( 'NONE', *, *, #41734, .T. ) ;
#29286=ORIENTED_EDGE ( 'NONE', *, *, #7135, .T. ) ;
#29287=DIRECTION ( 'NONE',  ( 1.000000000000000000, 0.000000000000000000, 0.000000000000000000 ) ) ;
#29289=LINE ( 'NONE', #33185, #25558 ) ;
#29290=ORIENTED_EDGE ( 'NONE', *, *, #33582, .T. ) ;
#29291=CARTESIAN_POINT ( 'NONE',  ( -0.3486774197067339376, 3.346456692913386100, -8.878505979408855953E-16 ) ) ;
#29292=FACE_BOUND ( 'NONE', #43820, .T. ) ;
#29295=VECTOR ( 'NONE', #16525, 39.37007874015748143 ) ;
#29296=CARTESIAN_POINT ( 'NONE',  ( -1.909347346926324906, 3.346456692913386100, 1.417322834645662333 ) ) ;
#29297=CIRCLE ( 'NONE', #27612, 2.165354330708661568 ) ;
#29298=ORIENTED_EDGE ( 'NONE', *, *, #39673, .T. ) ;
#29300=EDGE_CURVE ( 'NONE', #25793, #24046, #50213, .T. ) ;
#29302=CIRCLE ( 'NONE', #30955, 2.874015748031496731 ) ;
#29303=ADVANCED_FACE ( 'NONE', ( #28220 ), #24362, .F. ) ;
#29304=ORIENTED_EDGE ( 'NONE', *, *, #33179, .T. ) ;
#29305=DIRECTION ( 'NONE',  ( 1.734723475976806848E-16, -0.000000000000000000, 1.000000000000000000 ) ) ;
#29307=EDGE_CURVE ( 'NONE', #20045, #10888, #35034, .T. ) ;
#29308=PLANE ( 'NONE',  #15585 ) ;
#29309=ORIENTED_EDGE ( 'NONE', *, *, #20126, .F. ) ;
#29310=VECTOR ( 'NONE', #47835, 39.37007874015748143 ) ;
#29311=EDGE_CURVE ( 'NONE', #47095, #8152, #50707, .T. ) ;
#29313=LINE ( 'NONE', #17697, #36003 ) ;
#29314=CARTESIAN_POINT ( 'NONE',  ( -0.5455278134075208785, 3.346456692913386100, 1.377952755905504256 ) ) ;
#29315=PLANE ( 'NONE',  #14 ) ;
#29316=FACE_OUTER_BOUND ( 'NONE', #15603, .T. ) ;
#29319=DIRECTION ( 'NONE',  ( 1.000000000000000000, 0.000000000000000000, -3.469446951953613696E-16 ) ) ;
#29320=LINE ( 'NONE', #25195, #26482 ) ;
#29322=CARTESIAN_POINT ( 'NONE',  ( 1.761123562704336232, 3.346456692913386100, -1.259842519685035800 ) ) ;
#29323=DIRECTION ( 'NONE',  ( -3.469446951953613696E-16, 0.000000000000000000, -1.000000000000000000 ) ) ;
#29324=EDGE_LOOP ( 'NONE', ( #39380, #23987, #6995, #19251 ) ) ;
#29325=CARTESIAN_POINT ( 'NONE',  ( 0.2727639067037604392, 3.267716535433071279, -0.3543307086614173040 ) ) ;
#29326=LINE ( 'NONE', #45556, #31615 ) ;
#29327=LINE ( 'NONE', #45062, #43311 ) ;
#29330=ORIENTED_EDGE ( 'NONE', *, *, #25840, .T. ) ;
#29331=PLANE ( 'NONE',  #23242 ) ;
#29333=FACE_BOUND ( 'NONE', #25237, .T. ) ;
#29334=VECTOR ( 'NONE', #39748, 39.37007874015748143 ) ;
#29335=DIRECTION ( 'NONE',  ( -3.469446951953613696E-16, 0.000000000000000000, -1.000000000000000000 ) ) ;
#29336=CARTESIAN_POINT ( 'NONE',  ( -1.363819533518803029, 0.000000000000000000, 0.7874015748031456541 ) ) ;
#29337=CARTESIAN_POINT ( 'NONE',  ( 0.000000000000000000, 3.267716535433071279, 0.7480314960629872445 ) ) ;
#29338=ADVANCED_FACE ( 'NONE', ( #42764 ), #42256, .F. ) ;
#29339=AXIS2_PLACEMENT_3D ( 'NONE', #29555, #17681, #49631 ) ;
#29340=EDGE_CURVE ( 'NONE', #35616, #39217, #3532, .T. ) ;
#29341=AXIS2_PLACEMENT_3D ( 'NONE', #35176, #3681, #7055 ) ;
#29342=ORIENTED_EDGE ( 'NONE', *, *, #23207, .F. ) ;
#29345=DIRECTION ( 'NONE',  ( 1.734723475976806848E-16, -0.000000000000000000, 1.000000000000000000 ) ) ;
#29346=ORIENTED_EDGE ( 'NONE', *, *, #29703, .T. ) ;
#29347=LINE ( 'NONE', #12581, #34333 ) ;
#29349=EDGE_CURVE ( 'NONE', #50789, #18957, #5232, .T. ) ;
#29350=LINE ( 'NONE', #45325, #27258 ) ;
#29351=ORIENTED_EDGE ( 'NONE', *, *, #38283, .T. ) ;
#29352=CARTESIAN_POINT ( 'NONE',  ( 1.636583440222563857, 3.267716535433071279, -2.839019714148966584E-16 ) ) ;
#29354=VERTEX_POINT ( 'NONE', #38654 ) ;
#29355=DIRECTION ( 'NONE',  ( 0.000000000000000000, 0.000000000000000000, 1.000000000000000000 ) ) ;
#29358=EDGE_CURVE ( 'NONE', #660, #9566, #7162, .T. ) ;
#29359=EDGE_CURVE ( 'NONE', #13304, #48175, #22899, .T. ) ;
#29361=ORIENTED_EDGE ( 'NONE', *, *, #18220, .F. ) ;
#29363=CARTESIAN_POINT ( 'NONE',  ( -0.8942052331142552601, 3.346456692913386100, -0.1968503937007881899 ) ) ;
#29365=VECTOR ( 'NONE', #7648, 39.37007874015748143 ) ;
#29369=EDGE_CURVE ( 'NONE', #19691, #6703, #12479, .T. ) ;
#29370=VERTEX_POINT ( 'NONE', #11284 ) ;
#29371=CARTESIAN_POINT ( 'NONE',  ( 1.526828301548457834, 3.267716535433071279, 1.535433070866133898 ) ) ;
#29372=VECTOR ( 'NONE', #8589, 39.37007874015748143 ) ;
#29373=CARTESIAN_POINT ( 'NONE',  ( 1.363819533518803029, 3.346456692913386100, -1.605145679676863724 ) ) ;
#29374=ORIENTED_EDGE ( 'NONE', *, *, #48241, .F. ) ;
#29378=ORIENTED_EDGE ( 'NONE', *, *, #6289, .T. ) ;
#29380=LINE ( 'NONE', #45103, #17619 ) ;
#29382=DIRECTION ( 'NONE',  ( 1.734723475976806848E-16, -0.000000000000000000, 1.000000000000000000 ) ) ;
#29383=LINE ( 'NONE', #37398, #126 ) ;
#29385=DIRECTION ( 'NONE',  ( 0.000000000000000000, 0.000000000000000000, -1.000000000000000000 ) ) ;
#29386=VERTEX_POINT ( 'NONE', #27012 ) ;
#29388=CARTESIAN_POINT ( 'NONE',  ( 0.000000000000000000, 3.267716535433071279, -0.7874015748031473194 ) ) ;
#29389=ORIENTED_EDGE ( 'NONE', *, *, #12328, .F. ) ;
#29390=LINE ( 'NONE', #1002, #15189 ) ;
#29392=PLANE ( 'NONE',  #41017 ) ;
#29393=LINE ( 'NONE', #25268, #25061 ) ;
#29395=CARTESIAN_POINT ( 'NONE',  ( 0.5455278134075216556, 3.346456692913386100, 1.692913385826762873 ) ) ;
#29397=VERTEX_POINT ( 'NONE', #40376 ) ;
#29398=VECTOR ( 'NONE', #41268, 39.37007874015748143 ) ;
#29403=ADVANCED_FACE ( 'NONE', ( #40876 ), #28735, .F. ) ;
#29404=CARTESIAN_POINT ( 'NONE',  ( -1.486187880958816931, 3.346456692913386100, 1.574803149606291530 ) ) ;
#29405=VECTOR ( 'NONE', #6069, 39.37007874015748143 ) ;
#29406=ORIENTED_EDGE ( 'NONE', *, *, #21703, .T. ) ;
#29408=CARTESIAN_POINT ( 'NONE',  ( -1.195183497228115035E-16, 3.267716535433071279, 0.6299212598425161236 ) ) ;
#29410=EDGE_CURVE ( 'NONE', #28112, #47130, #17130, .T. ) ;
#29411=DIRECTION ( 'NONE',  ( 0.000000000000000000, 0.000000000000000000, -1.000000000000000000 ) ) ;
#29412=VECTOR ( 'NONE', #32694, 39.37007874015748143 ) ;
#29413=CARTESIAN_POINT ( 'NONE',  ( -0.6214413264104944323, 3.267716535433071279, 2.156057715732900533E-16 ) ) ;
#29414=ADVANCED_FACE ( 'NONE', ( #25630 ), #1375, .F. ) ;
#29415=VECTOR ( 'NONE', #836, 39.37007874015748143 ) ;
#29420=FACE_BOUND ( 'NONE', #39670, .T. ) ;
#29421=ORIENTED_EDGE ( 'NONE', *, *, #36660, .F. ) ;
#29422=DIRECTION ( 'NONE',  ( -0.000000000000000000, 1.000000000000000000, -0.000000000000000000 ) ) ;
#29423=EDGE_CURVE ( 'NONE', #44234, #17956, #32896, .T. ) ;
#29424=FACE_OUTER_BOUND ( 'NONE', #3816, .T. ) ;
#29426=ORIENTED_EDGE ( 'NONE', *, *, #40059, .T. ) ;
#29428=FACE_OUTER_BOUND ( 'NONE', #34913, .T. ) ;
#29430=EDGE_CURVE ( 'NONE', #23868, #4959, #5504, .T. ) ;
#29431=ORIENTED_EDGE ( 'NONE', *, *, #9344, .T. ) ;
#29432=ORIENTED_EDGE ( 'NONE', *, *, #14318, .T. ) ;
#29434=DIRECTION ( 'NONE',  ( -3.469446951953613696E-16, 0.000000000000000000, -1.000000000000000000 ) ) ;
#29435=CARTESIAN_POINT ( 'NONE',  ( -1.439733046521776583, 0.000000000000000000, -1.259842519685034468 ) ) ;
#29437=CARTESIAN_POINT ( 'NONE',  ( -1.363819533518803473, 0.000000000000000000, 1.732283464566920950 ) ) ;
#29439=ORIENTED_EDGE ( 'NONE', *, *, #37012, .F. ) ;
#29440=ORIENTED_EDGE ( 'NONE', *, *, #37072, .T. ) ;
#29441=DIRECTION ( 'NONE',  ( -0.000000000000000000, 1.000000000000000000, -0.000000000000000000 ) ) ;
#29443=DIRECTION ( 'NONE',  ( -1.000000000000000000, 0.000000000000000000, 0.000000000000000000 ) ) ;
#29444=CARTESIAN_POINT ( 'NONE',  ( 0.000000000000000000, 3.267716535433071279, 0.1574803149606283648 ) ) ;
#29445=EDGE_CURVE ( 'NONE', #28145, #29278, #44478, .T. ) ;
#29446=CARTESIAN_POINT ( 'NONE',  ( 0.000000000000000000, 3.346456692913386100, -2.493791675044291445 ) ) ;
#29451=LINE ( 'NONE', #48259, #23390 ) ;
#29452=ORIENTED_EDGE ( 'NONE', *, *, #10869, .T. ) ;
#29456=VERTEX_POINT ( 'NONE', #44228 ) ;
#29458=CARTESIAN_POINT ( 'NONE',  ( 1.015142113812069313, 3.267716535433071279, -0.3543307086614175816 ) ) ;
#29459=ORIENTED_EDGE ( 'NONE', *, *, #23193, .T. ) ;
#29462=LINE ( 'NONE', #33097, #9768 ) ;
#29463=ORIENTED_EDGE ( 'NONE', *, *, #3262, .T. ) ;
#29464=EDGE_CURVE ( 'NONE', #15158, #29676, #28985, .T. ) ;
#29465=CARTESIAN_POINT ( 'NONE',  ( 1.909347346926324462, 3.267716535433071279, -3.312189666507127188E-16 ) ) ;
#29467=DIRECTION ( 'NONE',  ( -1.000000000000000000, -0.000000000000000000, -0.000000000000000000 ) ) ;
#29468=EDGE_CURVE ( 'NONE', #36377, #16144, #37013, .T. ) ;
#29469=VECTOR ( 'NONE', #49817, 39.37007874015748143 ) ;
#29470=AXIS2_PLACEMENT_3D ( 'NONE', #49289, #48778, #24821 ) ;
#29473=ORIENTED_EDGE ( 'NONE', *, *, #29172, .F. ) ;
#29476=ORIENTED_EDGE ( 'NONE', *, *, #29753, .F. ) ;
#29477=ORIENTED_EDGE ( 'NONE', *, *, #28935, .T. ) ;
#29479=DIRECTION ( 'NONE',  ( 1.000000000000000000, 0.000000000000000000, 0.000000000000000000 ) ) ;
#29480=DIRECTION ( 'NONE',  ( 1.000000000000000000, 0.000000000000000000, 0.000000000000000000 ) ) ;
#29484=DIRECTION ( 'NONE',  ( 0.000000000000000000, 1.000000000000000000, 0.000000000000000000 ) ) ;
#29485=CARTESIAN_POINT ( 'NONE',  ( 2.106197740627111958, 3.346456692913386100, -0.6692913385826764205 ) ) ;
#29486=ORIENTED_EDGE ( 'NONE', *, *, #29110, .T. ) ;
#29489=LINE ( 'NONE', #48805, #26595 ) ;
#29491=ORIENTED_EDGE ( 'NONE', *, *, #49335, .T. ) ;
#29495=CARTESIAN_POINT ( 'NONE',  ( 1.287906020515830363, 3.267716535433071279, -4.468321617281356063E-16 ) ) ;
#29496=ADVANCED_FACE ( 'NONE', ( #48323 ), #9377, .F. ) ;
#29501=ORIENTED_EDGE ( 'NONE', *, *, #45468, .T. ) ;
#29502=PLANE ( 'NONE',  #14374 ) ;
#29503=ORIENTED_EDGE ( 'NONE', *, *, #16710, .T. ) ;
#29504=LINE ( 'NONE', #44476, #20828 ) ;
#29505=EDGE_CURVE ( 'NONE', #34486, #11040, #9891, .T. ) ;
#29507=VECTOR ( 'NONE', #374, 39.37007874015748143 ) ;
#29508=VECTOR ( 'NONE', #41278, 39.37007874015748143 ) ;
#29509=DIRECTION ( 'NONE',  ( 1.000000000000000000, -0.000000000000000000, 0.000000000000000000 ) ) ;
#29510=LINE ( 'NONE', #9892, #26869 ) ;
#29511=LINE ( 'NONE', #22024, #23766 ) ;
#29512=VERTEX_POINT ( 'NONE', #45226 ) ;
#29513=LINE ( 'NONE', #45230, #5238 ) ;
#29514=DIRECTION ( 'NONE',  ( 1.000000000000000000, 0.000000000000000000, 0.000000000000000000 ) ) ;
#29518=EDGE_CURVE ( 'NONE', #17531, #38065, #37519, .T. ) ;
#29519=ORIENTED_EDGE ( 'NONE', *, *, #45839, .T. ) ;
#29520=DIRECTION ( 'NONE',  ( 1.000000000000000000, 0.000000000000000000, 0.000000000000000000 ) ) ;
#29526=DIRECTION ( 'NONE',  ( -3.469446951953613696E-16, 0.000000000000000000, -1.000000000000000000 ) ) ;
#29528=PLANE ( 'NONE',  #2446 ) ;
#29529=CARTESIAN_POINT ( 'NONE',  ( -0.07591351300297333182, 3.267716535433071279, -1.102362204724405714 ) ) ;
#29532=DIRECTION ( 'NONE',  ( -0.000000000000000000, 1.000000000000000000, -0.000000000000000000 ) ) ;
#29534=CARTESIAN_POINT ( 'NONE',  ( 1.833433833923351353, 3.346456692913386100, -1.036830145017913596 ) ) ;
#29535=DIRECTION ( 'NONE',  ( -0.000000000000000000, 1.000000000000000000, -0.000000000000000000 ) ) ;
#29538=LINE ( 'NONE', #45254, #46899 ) ;
#29539=ORIENTED_EDGE ( 'NONE', *, *, #18299, .T. ) ;
#29540=ORIENTED_EDGE ( 'NONE', *, *, #50776, .F. ) ;
#29541=CARTESIAN_POINT ( 'NONE',  ( 0.000000000000000000, 3.267716535433071279, -0.6299212598425181220 ) ) ;
#29542=CARTESIAN_POINT ( 'NONE',  ( 2.182111253630085290, 3.346456692913386100, 0.4330708661417287386 ) ) ;
#29544=LINE ( 'NONE', #13799, #10250 ) ;
#29547=EDGE_LOOP ( 'NONE', ( #43358, #45789, #38751, #47693 ) ) ;
#29549=LINE ( 'NONE', #18437, #33741 ) ;
#29550=CARTESIAN_POINT ( 'NONE',  ( 0.1968503937007872462, 3.267716535433071279, -1.456692913385822630 ) ) ;
#29555=CARTESIAN_POINT ( 'NONE',  ( -1.091055626815042201, 0.000000000000000000, 1.574803149606291974 ) ) ;
#29556=ORIENTED_EDGE ( 'NONE', *, *, #21839, .T. ) ;
#29557=DIRECTION ( 'NONE',  ( 1.734723475976806848E-16, -0.000000000000000000, 1.000000000000000000 ) ) ;
#29558=ORIENTED_EDGE ( 'NONE', *, *, #14003, .T. ) ;
#29560=ORIENTED_EDGE ( 'NONE', *, *, #10841, .T. ) ;
#29562=DIRECTION ( 'NONE',  ( -1.000000000000000000, 0.000000000000000000, -0.000000000000000000 ) ) ;
#29563=VECTOR ( 'NONE', #2353, 39.37007874015748143 ) ;
#29564=ADVANCED_FACE ( 'NONE', ( #49586 ), #11150, .F. ) ;
#29565=ORIENTED_EDGE ( 'NONE', *, *, #28638, .T. ) ;
#29566=CARTESIAN_POINT ( 'NONE',  ( 0.8182917201112819283, 0.000000000000000000, -1.102362204724405714 ) ) ;
#29567=VECTOR ( 'NONE', #1179, 39.37007874015748143 ) ;
#29568=CARTESIAN_POINT ( 'NONE',  ( 1.636583440222563857, 3.346456692913386100, -0.6299212598425181220 ) ) ;
#29569=ORIENTED_EDGE ( 'NONE', *, *, #29887, .F. ) ;
#29574=VECTOR ( 'NONE', #21630, 39.37007874015748143 ) ;
#29576=ADVANCED_FACE ( 'NONE', ( #10896 ), #30271, .F. ) ;
#29578=CARTESIAN_POINT ( 'NONE',  ( -1.363819533518803473, 3.346456692913386100, -1.929133858267710000 ) ) ;
#29581=FACE_OUTER_BOUND ( 'NONE', #25740, .T. ) ;
#29584=ORIENTED_EDGE ( 'NONE', *, *, #28829, .T. ) ;
#29585=DIRECTION ( 'NONE',  ( 1.000000000000000000, 0.000000000000000000, -3.469446951953613696E-16 ) ) ;
#29587=ORIENTED_EDGE ( 'NONE', *, *, #45941, .F. ) ;
#29588=CARTESIAN_POINT ( 'NONE',  ( -1.091055626815042201, 3.346456692913386100, 1.062992125984246083 ) ) ;
#29589=VECTOR ( 'NONE', #37875, 39.37007874015748143 ) ;
#29590=EDGE_CURVE ( 'NONE', #4720, #47282, #14778, .T. ) ;
#29591=CARTESIAN_POINT ( 'NONE',  ( 4.268512490100411402E-16, 3.346456692913386100, 2.204724409448808764 ) ) ;
#29592=DIRECTION ( 'NONE',  ( -0.000000000000000000, 1.000000000000000000, -0.000000000000000000 ) ) ;
#29593=VERTEX_POINT ( 'NONE', #38775 ) ;
#29595=EDGE_LOOP ( 'NONE', ( #13425, #10698, #11314, #33447 ) ) ;
#29596=FACE_BOUND ( 'NONE', #43625, .T. ) ;
#29598=EDGE_CURVE ( 'NONE', #4856, #13403, #22022, .T. ) ;
#29599=VECTOR ( 'NONE', #3444, 39.37007874015748143 ) ;
#29600=AXIS2_PLACEMENT_3D ( 'NONE', #27601, #4376, #7992 ) ;
#29602=CARTESIAN_POINT ( 'NONE',  ( -2.182111253630085290, 0.000000000000000000, 0.3149606299212578953 ) ) ;
#29606=ORIENTED_EDGE ( 'NONE', *, *, #29172, .T. ) ;
#29607=ORIENTED_EDGE ( 'NONE', *, *, #41598, .F. ) ;
#29608=LINE ( 'NONE', #41475, #8978 ) ;
#29610=VECTOR ( 'NONE', #39860, 39.37007874015748143 ) ;
#29612=ORIENTED_EDGE ( 'NONE', *, *, #36156, .F. ) ;
#29613=CARTESIAN_POINT ( 'NONE',  ( -0.07591351300297333182, 0.000000000000000000, 0.4724409448818869817 ) ) ;
#29615=DIRECTION ( 'NONE',  ( -1.000000000000000000, -0.000000000000000000, -0.000000000000000000 ) ) ;
#29618=VERTEX_POINT ( 'NONE', #38529 ) ;
#29620=ORIENTED_EDGE ( 'NONE', *, *, #2597, .T. ) ;
#29621=ORIENTED_EDGE ( 'NONE', *, *, #30782, .F. ) ;
#29622=VECTOR ( 'NONE', #2431, 39.37007874015748143 ) ;
#29623=EDGE_LOOP ( 'NONE', ( #43777, #39497, #50926, #13456 ) ) ;
#29624=ORIENTED_EDGE ( 'NONE', *, *, #9663, .T. ) ;
#29625=DIRECTION ( 'NONE',  ( 0.000000000000000000, -1.000000000000000000, 0.000000000000000000 ) ) ;
#29627=PLANE ( 'NONE',  #16364 ) ;
#29631=LINE ( 'NONE', #1240, #19769 ) ;
#29632=AXIS2_PLACEMENT_3D ( 'NONE', #8631, #47828, #48085 ) ;
#29633=ORIENTED_EDGE ( 'NONE', *, *, #31340, .F. ) ;
#29635=PLANE ( 'NONE',  #22003 ) ;
#29636=DIRECTION ( 'NONE',  ( -3.469446951953613696E-16, 0.000000000000000000, -1.000000000000000000 ) ) ;
#29637=ORIENTED_EDGE ( 'NONE', *, *, #17981, .T. ) ;
#29639=DIRECTION ( 'NONE',  ( 0.000000000000000000, 0.000000000000000000, 1.000000000000000000 ) ) ;
#29640=CIRCLE ( 'NONE', #43651, 2.165354330708661568 ) ;
#29645=CARTESIAN_POINT ( 'NONE',  ( 1.558105373646058167, 3.346456692913386100, -1.417322834645665219 ) ) ;
#29647=CARTESIAN_POINT ( 'NONE',  ( 2.106197740627112402, 3.346456692913386100, 0.7874015748031456541 ) ) ;
#29648=CARTESIAN_POINT ( 'NONE',  ( 0.000000000000000000, 3.313179664429866556, 0.000000000000000000 ) ) ;
#29650=DIRECTION ( 'NONE',  ( 0.000000000000000000, 1.000000000000000000, 0.000000000000000000 ) ) ;
#29651=EDGE_CURVE ( 'NONE', #30246, #49658, #22778, .T. ) ;
#29653=LINE ( 'NONE', #21398, #41821 ) ;
#29654=CARTESIAN_POINT ( 'NONE',  ( 0.5455278134075216556, 3.346456692913386100, 2.034427629037600660 ) ) ;
#29656=EDGE_CURVE ( 'NONE', #606, #26629, #27903, .T. ) ;
#29657=PLANE ( 'NONE',  #20137 ) ;
#29660=EDGE_LOOP ( 'NONE', ( #16302, #23436, #32663, #25770 ) ) ;
#29661=EDGE_CURVE ( 'NONE', #42568, #43159, #31793, .T. ) ;
#29662=LINE ( 'NONE', #25780, #42192 ) ;
#29663=ORIENTED_EDGE ( 'NONE', *, *, #40368, .T. ) ;
#29664=VERTEX_POINT ( 'NONE', #42882 ) ;
#29665=CARTESIAN_POINT ( 'NONE',  ( 0.2727639067037609943, 3.346456692913386100, 1.220472440944875281 ) ) ;
#29666=EDGE_CURVE ( 'NONE', #15435, #1405, #39275, .T. ) ;
#29667=EDGE_LOOP ( 'NONE', ( #48151, #19176, #19804, #44387 ) ) ;
#29668=DIRECTION ( 'NONE',  ( 1.000000000000000000, 0.000000000000000000, 0.000000000000000000 ) ) ;
#29671=ORIENTED_EDGE ( 'NONE', *, *, #41891, .T. ) ;
#29674=DIRECTION ( 'NONE',  ( 1.000000000000000000, 0.000000000000000000, 0.000000000000000000 ) ) ;
#29675=CARTESIAN_POINT ( 'NONE',  ( 1.833433833923350909, 3.267716535433071279, -6.361001426713997494E-16 ) ) ;
#29676=VERTEX_POINT ( 'NONE', #12419 ) ;
#29679=FACE_BOUND ( 'NONE', #26040, .T. ) ;
#29680=VERTEX_POINT ( 'NONE', #50582 ) ;
#29682=CARTESIAN_POINT ( 'NONE',  ( 0.8182917201112817063, 0.000000000000000000, -1.732283464566923614 ) ) ;
#29683=CARTESIAN_POINT ( 'NONE',  ( -0.3486774197067340486, 3.346456692913386100, -2.077238655036873549 ) ) ;
#29684=ORIENTED_EDGE ( 'NONE', *, *, #2217, .F. ) ;
#29685=VERTEX_POINT ( 'NONE', #11905 ) ;
#29686=CARTESIAN_POINT ( 'NONE',  ( -1.985260859929297794, 0.000000000000000000, 0.4330708661417290162 ) ) ;
#29687=DIRECTION ( 'NONE',  ( -0.000000000000000000, 1.000000000000000000, -0.000000000000000000 ) ) ;
#29688=VERTEX_POINT ( 'NONE', #15277 ) ;
#29689=EDGE_LOOP ( 'NONE', ( #47702, #21308, #33723, #38549 ) ) ;
#29692=PLANE ( 'NONE',  #44761 ) ;
#29694=CARTESIAN_POINT ( 'NONE',  ( 1.909347346926324684, 3.346456692913386100, -0.3543307086614178592 ) ) ;
#29696=EDGE_LOOP ( 'NONE', ( #27418, #34734, #36204, #18691 ) ) ;
#29697=EDGE_CURVE ( 'NONE', #1162, #5904, #4165, .T. ) ;
#29698=LINE ( 'NONE', #18591, #46368 ) ;
#29701=DIRECTION ( 'NONE',  ( -0.000000000000000000, 1.000000000000000000, -0.000000000000000000 ) ) ;
#29702=CARTESIAN_POINT ( 'NONE',  ( -0.6214413264104939882, 3.346456692913386100, 0.7874015748031456541 ) ) ;
#29703=EDGE_CURVE ( 'NONE', #30894, #49397, #47493, .T. ) ;
#29704=CARTESIAN_POINT ( 'NONE',  ( 0.000000000000000000, 3.267716535433071279, -1.771653543307081691 ) ) ;
#29705=AXIS2_PLACEMENT_3D ( 'NONE', #41756, #2005, #33521 ) ;
#29707=LINE ( 'NONE', #14464, #44098 ) ;
#29708=CARTESIAN_POINT ( 'NONE',  ( 3.616083068348484413E-16, 0.000000000000000000, 2.952755905511811552 ) ) ;
#29709=VERTEX_POINT ( 'NONE', #35660 ) ;
#29710=CARTESIAN_POINT ( 'NONE',  ( 1.636583440222563857, 3.346456692913386100, -0.1968503937007886062 ) ) ;
#29714=ORIENTED_EDGE ( 'NONE', *, *, #35823, .T. ) ;
#29715=LINE ( 'NONE', #9842, #17944 ) ;
#29716=EDGE_CURVE ( 'NONE', #30486, #17428, #39786, .T. ) ;
#29717=VERTEX_POINT ( 'NONE', #31285 ) ;
#29718=EDGE_CURVE ( 'NONE', #25537, #2388, #19891, .T. ) ;
#29719=ORIENTED_EDGE ( 'NONE', *, *, #334, .F. ) ;
#29720=LINE ( 'NONE', #22480, #36969 ) ;
#29721=ORIENTED_EDGE ( 'NONE', *, *, #13060, .F. ) ;
#29722=CARTESIAN_POINT ( 'NONE',  ( 0.1968503937007872184, 3.267716535433071279, -6.829619984160650651E-17 ) ) ;
#29723=CARTESIAN_POINT ( 'NONE',  ( 0.5455278134075212115, 0.000000000000000000, 0.3149606299212576177 ) ) ;
#29724=ORIENTED_EDGE ( 'NONE', *, *, #820, .T. ) ;
#29727=EDGE_LOOP ( 'NONE', ( #27180, #442, #36529, #9070 ) ) ;
#29730=DIRECTION ( 'NONE',  ( -0.000000000000000000, 1.000000000000000000, -0.000000000000000000 ) ) ;
#29731=PLANE ( 'NONE',  #30151 ) ;
#29732=EDGE_CURVE ( 'NONE', #33442, #19657, #3403, .T. ) ;
#29733=VECTOR ( 'NONE', #545, 39.37007874015748143 ) ;
#29734=ORIENTED_EDGE ( 'NONE', *, *, #14763, .F. ) ;
#29735=CIRCLE ( 'NONE', #42111, 2.165354330708661568 ) ;
#29736=DIRECTION ( 'NONE',  ( -0.000000000000000000, 1.000000000000000000, -0.000000000000000000 ) ) ;
#29737=CARTESIAN_POINT ( 'NONE',  ( -4.268512490100411402E-16, 0.000000000000000000, -2.086614173228339641 ) ) ;
#29738=CARTESIAN_POINT ( 'NONE',  ( -0.2727639067037608278, 3.267716535433071279, 4.731699523581614055E-17 ) ) ;
#29739=ORIENTED_EDGE ( 'NONE', *, *, #44122, .F. ) ;
#29740=DIRECTION ( 'NONE',  ( -1.000000000000000000, 0.000000000000000000, -0.000000000000000000 ) ) ;
#29744=ORIENTED_EDGE ( 'NONE', *, *, #28158, .F. ) ;
#29745=AXIS2_PLACEMENT_3D ( 'NONE', #38872, #7881, #39631 ) ;
#29746=DIRECTION ( 'NONE',  ( 1.000000000000000000, 0.000000000000000000, 0.000000000000000000 ) ) ;
#29750=DIRECTION ( 'NONE',  ( -0.000000000000000000, 1.000000000000000000, -0.000000000000000000 ) ) ;
#29751=ORIENTED_EDGE ( 'NONE', *, *, #5959, .T. ) ;
#29752=VERTEX_POINT ( 'NONE', #27142 ) ;
#29753=EDGE_CURVE ( 'NONE', #50330, #3427, #6936, .T. ) ;
#29754=DIRECTION ( 'NONE',  ( 0.000000000000000000, -1.000000000000000000, 0.000000000000000000 ) ) ;
#29756=DIRECTION ( 'NONE',  ( -3.469446951953613696E-16, 0.000000000000000000, -1.000000000000000000 ) ) ;
#29757=LINE ( 'NONE', #45475, #8614 ) ;
#29758=EDGE_CURVE ( 'NONE', #8254, #28950, #47231, .T. ) ;
#29759=EDGE_CURVE ( 'NONE', #44082, #15287, #49742, .T. ) ;
#29760=EDGE_CURVE ( 'NONE', #18530, #3406, #11404, .T. ) ;
#29761=DIRECTION ( 'NONE',  ( 1.734723475976806848E-16, 0.000000000000000000, 1.000000000000000000 ) ) ;
#29764=ORIENTED_EDGE ( 'NONE', *, *, #42008, .F. ) ;
#29765=DIRECTION ( 'NONE',  ( -0.000000000000000000, 1.000000000000000000, -0.000000000000000000 ) ) ;
#29766=DIRECTION ( 'NONE',  ( -3.469446951953613696E-16, 0.000000000000000000, -1.000000000000000000 ) ) ;
#29767=DIRECTION ( 'NONE',  ( -3.469446951953613696E-16, 0.000000000000000000, -1.000000000000000000 ) ) ;
#29770=CARTESIAN_POINT ( 'NONE',  ( -0.8182917201112819283, 3.267716535433071279, -0.4724409448818886470 ) ) ;
#29771=AXIS2_PLACEMENT_3D ( 'NONE', #12448, #4452, #16328 ) ;
#29772=DIRECTION ( 'NONE',  ( 1.734723475976806848E-16, -0.000000000000000000, 1.000000000000000000 ) ) ;
#29773=ADVANCED_FACE ( 'NONE', ( #15533 ), #46979, .F. ) ;
#29774=FACE_OUTER_BOUND ( 'NONE', #27760, .T. ) ;
#29775=EDGE_LOOP ( 'NONE', ( #13596, #40934, #7679, #34581 ) ) ;
#29777=EDGE_CURVE ( 'NONE', #16605, #20587, #24252, .T. ) ;
#29779=DIRECTION ( 'NONE',  ( 0.000000000000000000, 1.000000000000000000, 0.000000000000000000 ) ) ;
#29780=VECTOR ( 'NONE', #23240, 39.37007874015748143 ) ;
#29781=CARTESIAN_POINT ( 'NONE',  ( 0.5455278134075212115, 0.000000000000000000, -0.6299212598425181220 ) ) ;
#29783=DIRECTION ( 'NONE',  ( 1.000000000000000000, 0.000000000000000000, -3.469446951953613696E-16 ) ) ;
#29784=CIRCLE ( 'NONE', #30635, 2.165354330708661568 ) ;
#29785=CARTESIAN_POINT ( 'NONE',  ( -1.363819533518803473, 3.346456692913386100, 1.850393700787392293 ) ) ;
#29786=CARTESIAN_POINT ( 'NONE',  ( 2.106197740627112402, 0.000000000000000000, -0.4724409448818889246 ) ) ;
#29787=FACE_OUTER_BOUND ( 'NONE', #10575, .T. ) ;
#29792=CARTESIAN_POINT ( 'NONE',  ( 1.091055626815042645, 3.346456692913386100, -1.141732283464564013 ) ) ;
#29793=CARTESIAN_POINT ( 'NONE',  ( 1.363819533518803251, 3.346456692913386100, -0.3543307086614178592 ) ) ;
#29795=LINE ( 'NONE', #9925, #7763 ) ;
#29796=CARTESIAN_POINT ( 'NONE',  ( 1.015142113812069091, 3.346456692913386100, -2.244094488188969283 ) ) ;
#29797=CARTESIAN_POINT ( 'NONE',  ( 0.000000000000000000, 3.267716535433071279, -0.8267716535433049518 ) ) ;
#29798=ADVANCED_FACE ( 'NONE', ( #17327 ), #33343, .F. ) ;
#29799=ORIENTED_EDGE ( 'NONE', *, *, #36596, .T. ) ;
#29800=ORIENTED_EDGE ( 'NONE', *, *, #25140, .F. ) ;
#29801=DIRECTION ( 'NONE',  ( 1.734723475976806848E-16, 0.000000000000000000, 1.000000000000000000 ) ) ;
#29804=ORIENTED_EDGE ( 'NONE', *, *, #11732, .F. ) ;
#29806=CARTESIAN_POINT ( 'NONE',  ( 1.091055626815043311, 3.346456692913386100, 1.889763779527550369 ) ) ;
#29807=VERTEX_POINT ( 'NONE', #21453 ) ;
#29809=CARTESIAN_POINT ( 'NONE',  ( -1.363819533518803251, 3.267716535433071279, 2.365849761790805487E-16 ) ) ;
#29812=DIRECTION ( 'NONE',  ( -1.000000000000000000, 0.000000000000000000, 1.734723475976806848E-16 ) ) ;
#29813=DIRECTION ( 'NONE',  ( 0.000000000000000000, 0.000000000000000000, -1.000000000000000000 ) ) ;
#29814=VECTOR ( 'NONE', #26269, 39.37007874015748143 ) ;
#29815=PLANE ( 'NONE',  #17358 ) ;
#29816=VECTOR ( 'NONE', #11449, 39.37007874015748143 ) ;
#29817=ORIENTED_EDGE ( 'NONE', *, *, #30694, .F. ) ;
#29818=PLANE ( 'NONE',  #48311 ) ;
#29819=LINE ( 'NONE', #29568, #10652 ) ;
#29821=ORIENTED_EDGE ( 'NONE', *, *, #26258, .F. ) ;
#29823=VECTOR ( 'NONE', #41742, 39.37007874015748143 ) ;
#29825=CARTESIAN_POINT ( 'NONE',  ( -0.6214413264104945434, 3.346456692913386100, -1.417322834645664331 ) ) ;
#29826=CARTESIAN_POINT ( 'NONE',  ( -1.636583440222564301, 0.000000000000000000, -0.9448818897637762948 ) ) ;
#29828=AXIS2_PLACEMENT_3D ( 'NONE', #34162, #22031, #30023 ) ;
#29831=LINE ( 'NONE', #37332, #42618 ) ;
#29833=EDGE_LOOP ( 'NONE', ( #19006, #8274, #12663, #48084 ) ) ;
#29834=DIRECTION ( 'NONE',  ( -3.469446951953613696E-16, 0.000000000000000000, -1.000000000000000000 ) ) ;
#29835=CARTESIAN_POINT ( 'NONE',  ( -0.07591351300297277671, 0.000000000000000000, 1.417322834645662777 ) ) ;
#29836=EDGE_LOOP ( 'NONE', ( #17248, #32345, #45832, #48998, #19223 ) ) ;
#29837=CARTESIAN_POINT ( 'NONE',  ( 0.000000000000000000, 3.267716535433071279, -1.614173228346452715 ) ) ;
#29839=ORIENTED_EDGE ( 'NONE', *, *, #44280, .F. ) ;
#29840=LINE ( 'NONE', #17454, #18030 ) ;
#29841=FACE_OUTER_BOUND ( 'NONE', #2695, .T. ) ;
#29842=CARTESIAN_POINT ( 'NONE',  ( 0.5455278134075216556, 0.000000000000000000, 1.062992125984246083 ) ) ;
#29843=ORIENTED_EDGE ( 'NONE', *, *, #8600, .T. ) ;
#29844=LINE ( 'NONE', #1455, #37323 ) ;
#29845=EDGE_LOOP ( 'NONE', ( #25165, #29452, #32352, #14744, #28819 ) ) ;
#29846=FACE_BOUND ( 'NONE', #29281, .T. ) ;
#29848=AXIS2_PLACEMENT_3D ( 'NONE', #18662, #30278, #34659 ) ;
#29850=DIRECTION ( 'NONE',  ( -3.469446951953613696E-16, 0.000000000000000000, -1.000000000000000000 ) ) ;
#29851=CARTESIAN_POINT ( 'NONE',  ( 0.000000000000000000, 3.267716535433071279, 0.7874015748031456541 ) ) ;
#29852=EDGE_CURVE ( 'NONE', #7564, #34607, #9063, .T. ) ;
#29854=ORIENTED_EDGE ( 'NONE', *, *, #16338, .F. ) ;
#29856=CARTESIAN_POINT ( 'NONE',  ( 1.636583440222563857, 3.267716535433071279, -2.839019714148966584E-16 ) ) ;
#29860=EDGE_CURVE ( 'NONE', #23969, #36096, #29451, .T. ) ;
#29862=VECTOR ( 'NONE', #5194, 39.37007874015748143 ) ;
#29863=EDGE_CURVE ( 'NONE', #9844, #48933, #45168, .T. ) ;
#29865=FACE_OUTER_BOUND ( 'NONE', #39544, .T. ) ;
#29866=ADVANCED_FACE ( 'NONE', ( #9317 ), #36690, .F. ) ;
#29868=ORIENTED_EDGE ( 'NONE', *, *, #37927, .T. ) ;
#29869=EDGE_CURVE ( 'NONE', #22692, #22325, #22593, .T. ) ;
#29871=ORIENTED_EDGE ( 'NONE', *, *, #36299, .F. ) ;
#29874=EDGE_LOOP ( 'NONE', ( #19932, #29406, #32676, #32261 ) ) ;
#29875=ORIENTED_EDGE ( 'NONE', *, *, #46799, .F. ) ;
#29877=ORIENTED_EDGE ( 'NONE', *, *, #33209, .T. ) ;
#29879=CARTESIAN_POINT ( 'NONE',  ( 0.000000000000000000, 3.267716535433071279, 0.1181102362204701633 ) ) ;
#29883=EDGE_CURVE ( 'NONE', #706, #8583, #40818, .T. ) ;
#29886=DIRECTION ( 'NONE',  ( 1.000000000000000000, 0.000000000000000000, 0.000000000000000000 ) ) ;
#29887=EDGE_CURVE ( 'NONE', #39537, #13500, #39915, .T. ) ;
#29888=ORIENTED_EDGE ( 'NONE', *, *, #4644, .F. ) ;
#29889=DIRECTION ( 'NONE',  ( 1.734723475976806848E-16, -0.000000000000000000, 1.000000000000000000 ) ) ;
#29890=LINE ( 'NONE', #18264, #24180 ) ;
#29891=VECTOR ( 'NONE', #25016, 39.37007874015748143 ) ;
#29892=LINE ( 'NONE', #45357, #7031 ) ;
#29897=FACE_OUTER_BOUND ( 'NONE', #9229, .T. ) ;
#29898=LINE ( 'NONE', #45107, #17062 ) ;
#29899=ORIENTED_EDGE ( 'NONE', *, *, #28535, .T. ) ;
#29900=DIRECTION ( 'NONE',  ( -0.000000000000000000, 1.000000000000000000, -0.000000000000000000 ) ) ;
#29901=DIRECTION ( 'NONE',  ( -1.000000000000000000, 0.000000000000000000, -0.000000000000000000 ) ) ;
#29902=ORIENTED_EDGE ( 'NONE', *, *, #10507, .F. ) ;
#29903=ORIENTED_EDGE ( 'NONE', *, *, #3588, .T. ) ;
#29909=ORIENTED_EDGE ( 'NONE', *, *, #3758, .T. ) ;
#29910=CARTESIAN_POINT ( 'NONE',  ( 2.182111253630085290, 3.346456692913386100, -0.3149606299212596716 ) ) ;
#29912=ORIENTED_EDGE ( 'NONE', *, *, #39296, .T. ) ;
#29913=CARTESIAN_POINT ( 'NONE',  ( 0.8182917201112819283, 3.346456692913386100, 1.102362204724403938 ) ) ;
#29914=ORIENTED_EDGE ( 'NONE', *, *, #27974, .T. ) ;
#29915=LINE ( 'NONE', #6931, #8955 ) ;
#29916=CARTESIAN_POINT ( 'NONE',  ( 1.287906020515830141, 3.267716535433071279, -0.5118110236220471121 ) ) ;
#29917=EDGE_LOOP ( 'NONE', ( #17601, #21712, #37122 ) ) ;
#29919=ADVANCED_FACE ( 'NONE', ( #44161 ), #40310, .F. ) ;
#29921=EDGE_CURVE ( 'NONE', #16323, #6701, #1574, .T. ) ;
#29922=ADVANCED_FACE ( 'NONE', ( #16812 ), #48769, .F. ) ;
#29923=VECTOR ( 'NONE', #36540, 39.37007874015748143 ) ;
#29925=ORIENTED_EDGE ( 'NONE', *, *, #45397, .T. ) ;
#29926=EDGE_LOOP ( 'NONE', ( #3087, #45052, #47381, #49977 ) ) ;
#29927=CARTESIAN_POINT ( 'NONE',  ( -1.636583440222564301, 3.346456692913386100, -1.259842519685034468 ) ) ;
#29928=FACE_BOUND ( 'NONE', #31583, .T. ) ;
#29929=VERTEX_POINT ( 'NONE', #1825 ) ;
#29932=DIRECTION ( 'NONE',  ( 1.000000000000000000, -0.000000000000000000, 0.000000000000000000 ) ) ;
#29935=VERTEX_POINT ( 'NONE', #30472 ) ;
#29936=CARTESIAN_POINT ( 'NONE',  ( -1.166969139818015977, 0.000000000000000000, 2.047244094488179567 ) ) ;
#29937=VECTOR ( 'NONE', #27267, 39.37007874015748143 ) ;
#29939=ORIENTED_EDGE ( 'NONE', *, *, #9976, .F. ) ;
#29940=ORIENTED_EDGE ( 'NONE', *, *, #14695, .T. ) ;
#29941=ADVANCED_FACE ( 'NONE', ( #29959 ), #10842, .F. ) ;
#29942=ORIENTED_EDGE ( 'NONE', *, *, #26416, .F. ) ;
#29943=LINE ( 'NONE', #41560, #35924 ) ;
#29944=CARTESIAN_POINT ( 'NONE',  ( 4.268512490100411402E-16, 0.000000000000000000, 2.204724409448808764 ) ) ;
#29945=EDGE_CURVE ( 'NONE', #3065, #13301, #42324, .T. ) ;
#29946=LINE ( 'NONE', #2327, #49774 ) ;
#29947=DIRECTION ( 'NONE',  ( -3.469446951953613696E-16, 0.000000000000000000, -1.000000000000000000 ) ) ;
#29948=EDGE_CURVE ( 'NONE', #46776, #5726, #10087, .T. ) ;
#29949=ORIENTED_EDGE ( 'NONE', *, *, #39245, .T. ) ;
#29950=ORIENTED_EDGE ( 'NONE', *, *, #28652, .F. ) ;
#29951=DIRECTION ( 'NONE',  ( 1.734723475976806848E-16, -0.000000000000000000, 1.000000000000000000 ) ) ;
#29952=PLANE ( 'NONE',  #24666 ) ;
#29953=EDGE_CURVE ( 'NONE', #12349, #38065, #30720, .T. ) ;
#29955=DIRECTION ( 'NONE',  ( -0.000000000000000000, 1.000000000000000000, -0.000000000000000000 ) ) ;
#29956=DIRECTION ( 'NONE',  ( 0.000000000000000000, 1.000000000000000000, 0.000000000000000000 ) ) ;
#29959=FACE_OUTER_BOUND ( 'NONE', #28020, .T. ) ;
#29960=AXIS2_PLACEMENT_3D ( 'NONE', #20391, #15508, #40282 ) ;
#29961=VERTEX_POINT ( 'NONE', #29708 ) ;
#29962=CARTESIAN_POINT ( 'NONE',  ( 0.4696143004045479352, 0.000000000000000000, 0.4724409448818868706 ) ) ;
#29963=LINE ( 'NONE', #26835, #31018 ) ;
#29964=VECTOR ( 'NONE', #7609, 39.37007874015748143 ) ;
#29965=EDGE_LOOP ( 'NONE', ( #22197, #33598, #22277, #31077 ) ) ;
#29966=VECTOR ( 'NONE', #25365, 39.37007874015748143 ) ;
#29967=VERTEX_POINT ( 'NONE', #18598 ) ;
#29968=FACE_OUTER_BOUND ( 'NONE', #35337, .T. ) ;
#29969=ORIENTED_EDGE ( 'NONE', *, *, #50798, .T. ) ;
#29970=VECTOR ( 'NONE', #10403, 39.37007874015748143 ) ;
#29971=ORIENTED_EDGE ( 'NONE', *, *, #24832, .T. ) ;
#29972=CARTESIAN_POINT ( 'NONE',  ( 1.015142113812069091, 3.267716535433071279, -1.929133858267711110 ) ) ;
#29973=EDGE_LOOP ( 'NONE', ( #37605, #15546, #2250, #3232 ) ) ;
#29975=CARTESIAN_POINT ( 'NONE',  ( 0.1968503937007873017, 3.267716535433071279, 0.3149606299212576177 ) ) ;
#29976=VERTEX_POINT ( 'NONE', #42085 ) ;
#29977=EDGE_CURVE ( 'NONE', #26751, #42980, #45424, .T. ) ;
#29979=DIRECTION ( 'NONE',  ( 1.734723475976806848E-16, 0.000000000000000000, 1.000000000000000000 ) ) ;
#29981=ORIENTED_EDGE ( 'NONE', *, *, #4158, .F. ) ;
#29982=ORIENTED_EDGE ( 'NONE', *, *, #2347, .T. ) ;
#29983=PLANE ( 'NONE',  #18240 ) ;
#29984=CARTESIAN_POINT ( 'NONE',  ( 1.271755610052043295, 3.267716535433071279, -2.086614173228339641 ) ) ;
#29986=CARTESIAN_POINT ( 'NONE',  ( 0.8182917201112819283, 0.000000000000000000, 0.7874015748031454320 ) ) ;
#29987=EDGE_CURVE ( 'NONE', #49734, #29198, #14973, .T. ) ;
#29988=ORIENTED_EDGE ( 'NONE', *, *, #32580, .T. ) ;
#29989=PLANE ( 'NONE',  #8139 ) ;
#29991=DIRECTION ( 'NONE',  ( 1.000000000000000000, 0.000000000000000000, 0.000000000000000000 ) ) ;
#29992=VERTEX_POINT ( 'NONE', #17829 ) ;
#29994=CIRCLE ( 'NONE', #44826, 2.165354330708661568 ) ;
#29995=DIRECTION ( 'NONE',  ( -1.000000000000000000, -0.000000000000000000, -0.000000000000000000 ) ) ;
#29996=CARTESIAN_POINT ( 'NONE',  ( 0.8182917201112817063, 0.000000000000000000, -1.929133858267711110 ) ) ;
#30000=AXIS2_PLACEMENT_3D ( 'NONE', #39203, #43318, #27574 ) ;
#30001=AXIS2_PLACEMENT_3D ( 'NONE', #35608, #47435, #12111 ) ;
#30002=DIRECTION ( 'NONE',  ( 1.000000000000000000, 0.000000000000000000, -3.469446951953613696E-16 ) ) ;
#30003=EDGE_CURVE ( 'NONE', #19400, #16457, #6471, .T. ) ;
#30004=LINE ( 'NONE', #46476, #25315 ) ;
#30007=ORIENTED_EDGE ( 'NONE', *, *, #5033, .T. ) ;
#30008=EDGE_LOOP ( 'NONE', ( #5724, #39954, #40698, #7728 ) ) ;
#30010=ADVANCED_FACE ( 'NONE', ( #34093 ), #21966, .F. ) ;
#30011=DIRECTION ( 'NONE',  ( -0.000000000000000000, 1.000000000000000000, -0.000000000000000000 ) ) ;
#30013=CARTESIAN_POINT ( 'NONE',  ( -1.712496953225537633, 3.346456692913386100, -0.6692913385826758654 ) ) ;
#30016=LINE ( 'NONE', #27143, #19469 ) ;
#30018=VERTEX_POINT ( 'NONE', #41836 ) ;
#30019=DIRECTION ( 'NONE',  ( 1.734723475976806848E-16, -0.000000000000000000, 1.000000000000000000 ) ) ;
#30022=ORIENTED_EDGE ( 'NONE', *, *, #38861, .F. ) ;
#30023=DIRECTION ( 'NONE',  ( 1.000000000000000000, 0.000000000000000000, 0.000000000000000000 ) ) ;
#30024=CARTESIAN_POINT ( 'NONE',  ( -1.166969139818015533, 3.267716535433071279, 0.4724409448818871482 ) ) ;
#30025=LINE ( 'NONE', #37534, #24673 ) ;
#30026=ORIENTED_EDGE ( 'NONE', *, *, #7121, .F. ) ;
#30027=DIRECTION ( 'NONE',  ( 0.000000000000000000, 0.000000000000000000, -1.000000000000000000 ) ) ;
#30029=VECTOR ( 'NONE', #48503, 39.37007874015748143 ) ;
#30030=ORIENTED_EDGE ( 'NONE', *, *, #1260, .F. ) ;
#30031=AXIS2_PLACEMENT_3D ( 'NONE', #16967, #21087, #20827 ) ;
#30032=CARTESIAN_POINT ( 'NONE',  ( -0.8182917201112819283, 3.346456692913386100, -0.1574803149606301411 ) ) ;
#30034=ORIENTED_EDGE ( 'NONE', *, *, #50962, .T. ) ;
#30036=VECTOR ( 'NONE', #14558, 39.37007874015748143 ) ;
#30039=LINE ( 'NONE', #34922, #28037 ) ;
#30040=DIRECTION ( 'NONE',  ( -1.000000000000000000, -0.000000000000000000, -0.000000000000000000 ) ) ;
#30041=EDGE_CURVE ( 'NONE', #20069, #37431, #41581, .T. ) ;
#30042=VERTEX_POINT ( 'NONE', #22222 ) ;
#30044=LINE ( 'NONE', #11184, #43019 ) ;
#30045=VECTOR ( 'NONE', #48963, 39.37007874015748143 ) ;
#30046=DIRECTION ( 'NONE',  ( -3.469446951953613696E-16, 0.000000000000000000, -1.000000000000000000 ) ) ;
#30047=EDGE_CURVE ( 'NONE', #4877, #2471, #26338, .T. ) ;
#30048=ORIENTED_EDGE ( 'NONE', *, *, #16427, .F. ) ;
#30049=DIRECTION ( 'NONE',  ( -1.000000000000000000, 0.000000000000000000, -0.000000000000000000 ) ) ;
#30050=DIRECTION ( 'NONE',  ( -1.000000000000000000, 0.000000000000000000, 0.000000000000000000 ) ) ;
#30051=CARTESIAN_POINT ( 'NONE',  ( 0.8182917201112819283, 3.346456692913386100, -0.9842519685039348154 ) ) ;
#30052=EDGE_CURVE ( 'NONE', #38746, #388, #14720, .T. ) ;
#30055=VERTEX_POINT ( 'NONE', #14207 ) ;
#30056=CARTESIAN_POINT ( 'NONE',  ( -2.160501893660597084, 3.267716535433071279, -1.141732283464563791 ) ) ;
#30058=DIRECTION ( 'NONE',  ( 1.734723475976806848E-16, -0.000000000000000000, 1.000000000000000000 ) ) ;
#30059=PLANE ( 'NONE',  #45326 ) ;
#30063=FACE_BOUND ( 'NONE', #3715, .T. ) ;
#30064=EDGE_LOOP ( 'NONE', ( #22007, #21948, #34451, #10672 ) ) ;
#30067=VERTEX_POINT ( 'NONE', #25573 ) ;
#30070=FACE_OUTER_BOUND ( 'NONE', #11835, .T. ) ;
#30072=ORIENTED_EDGE ( 'NONE', *, *, #50908, .T. ) ;
#30077=ADVANCED_FACE ( 'NONE', ( #5951 ), #21706, .F. ) ;
#30078=VERTEX_POINT ( 'NONE', #46928 ) ;
#30079=CARTESIAN_POINT ( 'NONE',  ( 2.106197740627112402, 3.346456692913386100, -0.4724409448818889246 ) ) ;
#30081=VECTOR ( 'NONE', #16452, 39.37007874015748143 ) ;
#30082=VECTOR ( 'NONE', #10221, 39.37007874015748143 ) ;
#30084=DIRECTION ( 'NONE',  ( 0.000000000000000000, -1.000000000000000000, 0.000000000000000000 ) ) ;
#30085=FACE_OUTER_BOUND ( 'NONE', #33577, .T. ) ;
#30087=VERTEX_POINT ( 'NONE', #20092 ) ;
#30088=FACE_OUTER_BOUND ( 'NONE', #1301, .T. ) ;
#30089=EDGE_CURVE ( 'NONE', #19068, #9489, #35098, .T. ) ;
#30090=LINE ( 'NONE', #45802, #46290 ) ;
#30091=ORIENTED_EDGE ( 'NONE', *, *, #29430, .F. ) ;
#30094=ORIENTED_EDGE ( 'NONE', *, *, #32177, .T. ) ;
#30096=FACE_OUTER_BOUND ( 'NONE', #42800, .T. ) ;
#30099=CARTESIAN_POINT ( 'NONE',  ( 0.000000000000000000, 3.267716535433071279, 1.850393700787392293 ) ) ;
#30101=FACE_BOUND ( 'NONE', #42172, .T. ) ;
#30102=LINE ( 'NONE', #2732, #20134 ) ;
#30103=LINE ( 'NONE', #45821, #44100 ) ;
#30104=DIRECTION ( 'NONE',  ( 1.000000000000000000, 0.000000000000000000, 0.000000000000000000 ) ) ;
#30106=EDGE_LOOP ( 'NONE', ( #43945, #818, #32231, #5763 ) ) ;
#30108=DIRECTION ( 'NONE',  ( 1.000000000000000000, 0.000000000000000000, 0.000000000000000000 ) ) ;
#30109=VECTOR ( 'NONE', #14233, 39.37007874015748143 ) ;
#30111=CARTESIAN_POINT ( 'NONE',  ( -1.091055626815042201, 3.346456692913386100, 0.1181102362204705658 ) ) ;
#30112=FACE_OUTER_BOUND ( 'NONE', #2254, .T. ) ;
#30113=ORIENTED_EDGE ( 'NONE', *, *, #41186, .T. ) ;
#30115=EDGE_CURVE ( 'NONE', #37496, #46482, #11597, .T. ) ;
#30118=VERTEX_POINT ( 'NONE', #7230 ) ;
#30121=DIRECTION ( 'NONE',  ( -0.000000000000000000, 1.000000000000000000, -0.000000000000000000 ) ) ;
#30122=VECTOR ( 'NONE', #2993, 39.37007874015748143 ) ;
#30123=VERTEX_POINT ( 'NONE', #30969 ) ;
#30126=ORIENTED_EDGE ( 'NONE', *, *, #25868, .T. ) ;
#30128=ORIENTED_EDGE ( 'NONE', *, *, #16576, .F. ) ;
#30130=EDGE_LOOP ( 'NONE', ( #3696, #40870, #46681, #37993 ) ) ;
#30132=CARTESIAN_POINT ( 'NONE',  ( 1.560669927219590303, 3.267716535433071279, -1.102362204724405714 ) ) ;
#30133=EDGE_CURVE ( 'NONE', #11950, #34431, #47177, .T. ) ;
#30135=DIRECTION ( 'NONE',  ( -0.000000000000000000, 0.000000000000000000, 1.000000000000000000 ) ) ;
#30136=DIRECTION ( 'NONE',  ( -0.000000000000000000, 1.000000000000000000, -0.000000000000000000 ) ) ;
#30137=VECTOR ( 'NONE', #31473, 39.37007874015748143 ) ;
#30138=EDGE_LOOP ( 'NONE', ( #1450, #6092, #469, #33379 ) ) ;
#30139=LINE ( 'NONE', #48951, #4151 ) ;
#30140=FACE_OUTER_BOUND ( 'NONE', #12619, .T. ) ;
#30141=AXIS2_PLACEMENT_3D ( 'NONE', #30705, #10822, #50020 ) ;
#30143=ADVANCED_FACE ( 'NONE', ( #34843 ), #23982, .F. ) ;
#30145=CARTESIAN_POINT ( 'NONE',  ( 0.000000000000000000, 3.346456692913386100, 0.000000000000000000 ) ) ;
#30146=ORIENTED_EDGE ( 'NONE', *, *, #40263, .F. ) ;
#30148=DIRECTION ( 'NONE',  ( 0.000000000000000000, 0.000000000000000000, -1.000000000000000000 ) ) ;
#30149=ORIENTED_EDGE ( 'NONE', *, *, #4616, .T. ) ;
#30150=LINE ( 'NONE', #45611, #8157 ) ;
#30151=AXIS2_PLACEMENT_3D ( 'NONE', #44952, #45199, #41108 ) ;
#30152=LINE ( 'NONE', #3039, #43205 ) ;
#30153=AXIS2_PLACEMENT_3D ( 'NONE', #2927, #23050, #46513 ) ;
#30154=VERTEX_POINT ( 'NONE', #31997 ) ;
#30157=PLANE ( 'NONE',  #12404 ) ;
#30158=EDGE_CURVE ( 'NONE', #11553, #37676, #39058, .T. ) ;
#30159=CARTESIAN_POINT ( 'NONE',  ( 1.363819533518803251, 0.000000000000000000, 0.1574803149606283648 ) ) ;
#30160=CARTESIAN_POINT ( 'NONE',  ( -0.5455278134075208785, 0.000000000000000000, 0.6299212598425164567 ) ) ;
#30162=CARTESIAN_POINT ( 'NONE',  ( 1.636583440222563857, 0.000000000000000000, -0.8267716535433055070 ) ) ;
#30163=EDGE_LOOP ( 'NONE', ( #31895, #1003, #37891, #45452 ) ) ;
#30166=ORIENTED_EDGE ( 'NONE', *, *, #49200, .T. ) ;
#30167=CARTESIAN_POINT ( 'NONE',  ( 0.7423782071083084855, 3.346456692913386100, -1.889763779527552812 ) ) ;
#30168=ORIENTED_EDGE ( 'NONE', *, *, #32880, .T. ) ;
#30170=DIRECTION ( 'NONE',  ( -0.000000000000000000, 1.000000000000000000, -0.000000000000000000 ) ) ;
#30175=EDGE_CURVE ( 'NONE', #47149, #49034, #39218, .T. ) ;
#30176=EDGE_CURVE ( 'NONE', #23735, #17928, #23464, .T. ) ;
#30177=FACE_OUTER_BOUND ( 'NONE', #28895, .T. ) ;
#30179=VERTEX_POINT ( 'NONE', #3857 ) ;
#30180=VERTEX_POINT ( 'NONE', #19584 ) ;
#30182=DIRECTION ( 'NONE',  ( -0.000000000000000000, 1.000000000000000000, -0.000000000000000000 ) ) ;
#30183=FACE_BOUND ( 'NONE', #31007, .T. ) ;
#30184=ORIENTED_EDGE ( 'NONE', *, *, #27830, .T. ) ;
#30186=CARTESIAN_POINT ( 'NONE',  ( -0.6214413264104945434, 3.267716535433071279, -1.929133858267710000 ) ) ;
#30187=CARTESIAN_POINT ( 'NONE',  ( -1.363819533518803029, 3.267716535433071279, 1.220472440944875281 ) ) ;
#30188=VECTOR ( 'NONE', #28882, 39.37007874015748143 ) ;
#30190=ORIENTED_EDGE ( 'NONE', *, *, #28787, .T. ) ;
#30191=LINE ( 'NONE', #9297, #33214 ) ;
#30193=DIRECTION ( 'NONE',  ( -0.000000000000000000, 1.000000000000000000, -0.000000000000000000 ) ) ;
#30195=VERTEX_POINT ( 'NONE', #35358 ) ;
#30196=VERTEX_POINT ( 'NONE', #11348 ) ;
#30197=PLANE ( 'NONE',  #19435 ) ;
#30199=EDGE_CURVE ( 'NONE', #3379, #22305, #51034, .T. ) ;
#30200=LINE ( 'NONE', #35088, #5782 ) ;
#30201=ORIENTED_EDGE ( 'NONE', *, *, #36220, .T. ) ;
#30202=ORIENTED_EDGE ( 'NONE', *, *, #8958, .T. ) ;
#30203=DIRECTION ( 'NONE',  ( -3.469446951953613696E-16, 0.000000000000000000, -1.000000000000000000 ) ) ;
#30207=EDGE_CURVE ( 'NONE', #45537, #13877, #19087, .T. ) ;
#30209=EDGE_CURVE ( 'NONE', #12590, #38358, #15724, .T. ) ;
#30212=AXIS2_PLACEMENT_3D ( 'NONE', #8868, #31599, #349 ) ;
#30214=ORIENTED_EDGE ( 'NONE', *, *, #6392, .F. ) ;
#30215=VECTOR ( 'NONE', #42996, 39.37007874015748143 ) ;
#30217=CARTESIAN_POINT ( 'NONE',  ( 1.909347346926324684, 0.000000000000000000, 0.1574803149606280872 ) ) ;
#30220=VECTOR ( 'NONE', #50127, 39.37007874015748143 ) ;
#30226=VERTEX_POINT ( 'NONE', #5643 ) ;
#30230=EDGE_CURVE ( 'NONE', #46754, #17428, #17701, .T. ) ;
#30231=LINE ( 'NONE', #50544, #2098 ) ;
#30232=DIRECTION ( 'NONE',  ( -0.000000000000000000, 0.000000000000000000, 1.000000000000000000 ) ) ;
#30234=EDGE_CURVE ( 'NONE', #33364, #45220, #44361, .T. ) ;
#30235=ORIENTED_EDGE ( 'NONE', *, *, #11452, .F. ) ;
#30243=CARTESIAN_POINT ( 'NONE',  ( -1.299212598425205423, 3.267716535433071279, -1.732283464566922726 ) ) ;
#30244=DIRECTION ( 'NONE',  ( -0.000000000000000000, 1.000000000000000000, -0.000000000000000000 ) ) ;
#30245=DIRECTION ( 'NONE',  ( -0.000000000000000000, 1.000000000000000000, -0.000000000000000000 ) ) ;
#30246=VERTEX_POINT ( 'NONE', #36892 ) ;
#30247=DIRECTION ( 'NONE',  ( -3.469446951953613696E-16, 0.000000000000000000, -1.000000000000000000 ) ) ;
#30248=CARTESIAN_POINT ( 'NONE',  ( -4.268512490100411402E-16, 0.000000000000000000, -2.401574803149598480 ) ) ;
#30249=DIRECTION ( 'NONE',  ( -1.000000000000000000, 0.000000000000000000, 0.000000000000000000 ) ) ;
#30250=AXIS2_PLACEMENT_3D ( 'NONE', #31162, #19527, #31672 ) ;
#30251=EDGE_LOOP ( 'NONE', ( #15204, #38195, #49578, #29888 ) ) ;
#30252=DIRECTION ( 'NONE',  ( -0.000000000000000000, 1.000000000000000000, -0.000000000000000000 ) ) ;
#30253=CARTESIAN_POINT ( 'NONE',  ( 1.560669927219590747, 3.267716535433071279, -5.414661521997677271E-16 ) ) ;
#30254=AXIS2_PLACEMENT_3D ( 'NONE', #36365, #28605, #35849 ) ;
#30255=ORIENTED_EDGE ( 'NONE', *, *, #8710, .F. ) ;
#30261=DIRECTION ( 'NONE',  ( -1.000000000000000000, 0.000000000000000000, 1.734723475976806848E-16 ) ) ;
#30262=VERTEX_POINT ( 'NONE', #32774 ) ;
#30263=ORIENTED_EDGE ( 'NONE', *, *, #50407, .T. ) ;
#30267=ORIENTED_EDGE ( 'NONE', *, *, #37357, .T. ) ;
#30269=DIRECTION ( 'NONE',  ( -0.000000000000000000, 1.000000000000000000, -0.000000000000000000 ) ) ;
#30271=PLANE ( 'NONE',  #43987 ) ;
#30272=EDGE_CURVE ( 'NONE', #12169, #7654, #48453, .T. ) ;
#30273=CARTESIAN_POINT ( 'NONE',  ( 0.8182917201112817063, 0.000000000000000000, -1.732283464566923614 ) ) ;
#30274=CARTESIAN_POINT ( 'NONE',  ( -0.6214413264104945434, 3.267716535433071279, -1.417322834645664331 ) ) ;
#30275=EDGE_LOOP ( 'NONE', ( #15337, #36355, #38823, #37698 ) ) ;
#30278=DIRECTION ( 'NONE',  ( 0.000000000000000000, -1.000000000000000000, 0.000000000000000000 ) ) ;
#30279=VERTEX_POINT ( 'NONE', #13390 ) ;
#30282=CARTESIAN_POINT ( 'NONE',  ( 1.091055626815042645, 0.000000000000000000, 1.062992125984246083 ) ) ;
#30285=DIRECTION ( 'NONE',  ( -3.469446951953613696E-16, 0.000000000000000000, -1.000000000000000000 ) ) ;
#30286=CIRCLE ( 'NONE', #46713, 2.106299212598425008 ) ;
#30287=VERTEX_POINT ( 'NONE', #29125 ) ;
#30292=DIRECTION ( 'NONE',  ( 0.000000000000000000, 0.000000000000000000, 1.000000000000000000 ) ) ;
#30295=CARTESIAN_POINT ( 'NONE',  ( 2.106197740627111958, 0.000000000000000000, 0.9055118110236164419 ) ) ;
#30296=CARTESIAN_POINT ( 'NONE',  ( -2.182111253630085290, 0.000000000000000000, -0.5118110236220464460 ) ) ;
#30297=EDGE_CURVE ( 'NONE', #30067, #25537, #24243, .T. ) ;
#30299=ORIENTED_EDGE ( 'NONE', *, *, #40711, .F. ) ;
#30301=DIRECTION ( 'NONE',  ( 1.000000000000000000, 0.000000000000000000, -3.469446951953613696E-16 ) ) ;
#30302=EDGE_CURVE ( 'NONE', #17684, #39256, #44105, .T. ) ;
#30303=ORIENTED_EDGE ( 'NONE', *, *, #18421, .F. ) ;
#30304=LINE ( 'NONE', #42167, #11060 ) ;
#30305=CARTESIAN_POINT ( 'NONE',  ( 1.363819533518803029, 0.000000000000000000, -1.299212598425193210 ) ) ;
#30307=VECTOR ( 'NONE', #1115, 39.37007874015748143 ) ;
#30308=VERTEX_POINT ( 'NONE', #36376 ) ;
#30312=FACE_OUTER_BOUND ( 'NONE', #12213, .T. ) ;
#30313=DIRECTION ( 'NONE',  ( 1.734723475976806848E-16, -0.000000000000000000, 1.000000000000000000 ) ) ;
#30314=ORIENTED_EDGE ( 'NONE', *, *, #21537, .T. ) ;
#30315=DIRECTION ( 'NONE',  ( -1.000000000000000000, -0.000000000000000000, -0.000000000000000000 ) ) ;
#30316=FACE_BOUND ( 'NONE', #49469, .T. ) ;
#30317=ORIENTED_EDGE ( 'NONE', *, *, #21093, .T. ) ;
#30318=DIRECTION ( 'NONE',  ( 1.000000000000000000, -0.000000000000000000, 0.000000000000000000 ) ) ;
#30322=CARTESIAN_POINT ( 'NONE',  ( -1.166969139818015755, 3.346456692913386100, 0.5905511811023582691 ) ) ;
#30324=VECTOR ( 'NONE', #49423, 39.37007874015748143 ) ;
#30325=AXIS2_PLACEMENT_3D ( 'NONE', #16567, #8043, #8299 ) ;
#30328=CARTESIAN_POINT ( 'NONE',  ( 0.4696143004045484348, 0.000000000000000000, 1.850393700787392293 ) ) ;
#30329=ORIENTED_EDGE ( 'NONE', *, *, #12383, .T. ) ;
#30330=AXIS2_PLACEMENT_3D ( 'NONE', #519, #23756, #8778 ) ;
#30331=ORIENTED_EDGE ( 'NONE', *, *, #21062, .F. ) ;
#30336=EDGE_CURVE ( 'NONE', #47970, #22386, #1513, .T. ) ;
#30338=DIRECTION ( 'NONE',  ( -1.000000000000000000, 0.000000000000000000, -0.000000000000000000 ) ) ;
#30339=VERTEX_POINT ( 'NONE', #21394 ) ;
#30340=ADVANCED_FACE ( 'NONE', ( #4879 ), #12363, .F. ) ;
#30341=FACE_OUTER_BOUND ( 'NONE', #5366, .T. ) ;
#30343=VECTOR ( 'NONE', #1442, 39.37007874015748143 ) ;
#30344=DIRECTION ( 'NONE',  ( -1.000000000000000000, 0.000000000000000000, 0.000000000000000000 ) ) ;
#30346=ORIENTED_EDGE ( 'NONE', *, *, #41523, .F. ) ;
#30347=DIRECTION ( 'NONE',  ( -1.000000000000000000, 0.000000000000000000, 0.000000000000000000 ) ) ;
#30350=LINE ( 'NONE', #14091, #12236 ) ;
#30351=DIRECTION ( 'NONE',  ( -1.000000000000000000, 0.000000000000000000, 0.000000000000000000 ) ) ;
#30352=DIRECTION ( 'NONE',  ( 1.000000000000000000, 0.000000000000000000, 0.000000000000000000 ) ) ;
#30354=DIRECTION ( 'NONE',  ( 1.000000000000000000, 0.000000000000000000, 0.000000000000000000 ) ) ;
#30355=ORIENTED_EDGE ( 'NONE', *, *, #25040, .T. ) ;
#30356=FACE_BOUND ( 'NONE', #42850, .T. ) ;
#30359=DIRECTION ( 'NONE',  ( -0.000000000000000000, 1.000000000000000000, -0.000000000000000000 ) ) ;
#30361=VECTOR ( 'NONE', #12696, 39.37007874015748143 ) ;
#30362=VECTOR ( 'NONE', #28754, 39.37007874015748143 ) ;
#30364=ORIENTED_EDGE ( 'NONE', *, *, #29236, .T. ) ;
#30365=ORIENTED_EDGE ( 'NONE', *, *, #3229, .T. ) ;
#30366=CARTESIAN_POINT ( 'NONE',  ( -0.2727639067037602727, 3.267716535433071279, 1.850393700787392293 ) ) ;
#30368=EDGE_CURVE ( 'NONE', #32019, #37382, #6909, .T. ) ;
#30369=VECTOR ( 'NONE', #44077, 39.37007874015748143 ) ;
#30370=CARTESIAN_POINT ( 'NONE',  ( 1.015142113812069091, 0.000000000000000000, -1.614173228346451605 ) ) ;
#30372=CARTESIAN_POINT ( 'NONE',  ( -1.091055626815042645, 3.346456692913386100, 1.889763779527550147 ) ) ;
#30374=ORIENTED_EDGE ( 'NONE', *, *, #14346, .T. ) ;
#30375=ORIENTED_EDGE ( 'NONE', *, *, #22604, .F. ) ;
#30378=CARTESIAN_POINT ( 'NONE',  ( -1.363819533518803029, 3.346456692913386100, 0.1574803149606287811 ) ) ;
#30383=AXIS2_PLACEMENT_3D ( 'NONE', #39277, #36889, #1512 ) ;
#30385=ORIENTED_EDGE ( 'NONE', *, *, #43802, .F. ) ;
#30386=ORIENTED_EDGE ( 'NONE', *, *, #39873, .F. ) ;
#30387=CARTESIAN_POINT ( 'NONE',  ( -1.636583440222563635, 3.267716535433071279, -0.1968503937007879123 ) ) ;
#30388=DIRECTION ( 'NONE',  ( -0.000000000000000000, 1.000000000000000000, -0.000000000000000000 ) ) ;
#30390=AXIS2_PLACEMENT_3D ( 'NONE', #40715, #5849, #24716 ) ;
#30391=CARTESIAN_POINT ( 'NONE',  ( -0.6214413264104939882, 3.346456692913386100, 0.4724409448818872592 ) ) ;
#30395=EDGE_CURVE ( 'NONE', #34149, #41494, #9773, .T. ) ;
#30396=LINE ( 'NONE', #34528, #7670 ) ;
#30397=CARTESIAN_POINT ( 'NONE',  ( -0.07591351300297333182, 3.346456692913386100, -0.1574803149606301411 ) ) ;
#30399=CARTESIAN_POINT ( 'NONE',  ( -0.3486774197067347147, 3.267716535433071279, 1.209717811016581790E-16 ) ) ;
#30400=FACE_OUTER_BOUND ( 'NONE', #38610, .T. ) ;
#30401=ADVANCED_FACE ( 'NONE', ( #45870 ), #25767, .F. ) ;
#30404=LINE ( 'NONE', #42521, #6718 ) ;
#30406=DIRECTION ( 'NONE',  ( -0.000000000000000000, 0.000000000000000000, 1.000000000000000000 ) ) ;
#30408=LINE ( 'NONE', #2782, #38639 ) ;
#30409=EDGE_CURVE ( 'NONE', #47890, #23722, #2032, .T. ) ;
#30410=DIRECTION ( 'NONE',  ( 0.000000000000000000, 1.000000000000000000, 0.000000000000000000 ) ) ;
#30411=VECTOR ( 'NONE', #25564, 39.37007874015748143 ) ;
#30412=ORIENTED_EDGE ( 'NONE', *, *, #34608, .F. ) ;
#30413=CARTESIAN_POINT ( 'NONE',  ( -0.07591351300297284610, 3.346456692913386100, 0.9055118110236167750 ) ) ;
#30414=VECTOR ( 'NONE', #2020, 39.37007874015748143 ) ;
#30415=ORIENTED_EDGE ( 'NONE', *, *, #49537, .F. ) ;
#30416=DIRECTION ( 'NONE',  ( -1.000000000000000000, -0.000000000000000000, -0.000000000000000000 ) ) ;
#30417=DIRECTION ( 'NONE',  ( -1.000000000000000000, 0.000000000000000000, -0.000000000000000000 ) ) ;
#30418=DIRECTION ( 'NONE',  ( -1.000000000000000000, 0.000000000000000000, 1.734723475976806848E-16 ) ) ;
#30420=ADVANCED_FACE ( 'NONE', ( #49468 ), #14379, .F. ) ;
#30421=LINE ( 'NONE', #46135, #5494 ) ;
#30424=VERTEX_POINT ( 'NONE', #33277 ) ;
#30426=DIRECTION ( 'NONE',  ( -1.000000000000000000, -0.000000000000000000, -0.000000000000000000 ) ) ;
#30428=EDGE_CURVE ( 'NONE', #5151, #40849, #30152, .T. ) ;
#30429=CARTESIAN_POINT ( 'NONE',  ( -2.182111253630085734, 3.267716535433071279, -0.9448818897637762948 ) ) ;
#30431=EDGE_LOOP ( 'NONE', ( #6942, #10190, #22405, #10263 ) ) ;
#30432=LINE ( 'NONE', #10801, #15696 ) ;
#30433=VECTOR ( 'NONE', #10861, 39.37007874015748143 ) ;
#30434=EDGE_CURVE ( 'NONE', #122, #16050, #21644, .T. ) ;
#30436=DIRECTION ( 'NONE',  ( -0.000000000000000000, 1.000000000000000000, -0.000000000000000000 ) ) ;
#30439=B_SPLINE_CURVE_WITH_KNOTS ( 'NONE', 3,
 ( #1267, #32783, #13150, #6163 ),
 .UNSPECIFIED., .F., .F.,
 ( 4, 4 ),
 ( 0.03325564439065060995, 0.03551576279684434678 ),
 .UNSPECIFIED. ) ;
#30440=CARTESIAN_POINT ( 'NONE',  ( 1.560669927219590303, 3.186757942779276043, -1.929133858267710666 ) ) ;
#30441=FACE_BOUND ( 'NONE', #49912, .T. ) ;
#30443=EDGE_CURVE ( 'NONE', #47349, #9370, #37913, .T. ) ;
#30445=VECTOR ( 'NONE', #23579, 39.37007874015748143 ) ;
#30448=ORIENTED_EDGE ( 'NONE', *, *, #14763, .T. ) ;
#30449=ORIENTED_EDGE ( 'NONE', *, *, #40611, .F. ) ;
#30450=VECTOR ( 'NONE', #50417, 39.37007874015748143 ) ;
#30451=DIRECTION ( 'NONE',  ( -0.000000000000000000, 1.000000000000000000, -0.000000000000000000 ) ) ;
#30452=LINE ( 'NONE', #46410, #36121 ) ;
#30453=ADVANCED_FACE ( 'NONE', ( #14148 ), #45613, .F. ) ;
#30454=ORIENTED_EDGE ( 'NONE', *, *, #43731, .T. ) ;
#30455=AXIS2_PLACEMENT_3D ( 'NONE', #33912, #38042, #49600 ) ;
#30457=EDGE_CURVE ( 'NONE', #50243, #9222, #37659, .T. ) ;
#30461=VERTEX_POINT ( 'NONE', #2785 ) ;
#30464=CARTESIAN_POINT ( 'NONE',  ( 0.2727639067037602172, 3.267716535433071279, -1.732283464566922726 ) ) ;
#30465=CARTESIAN_POINT ( 'NONE',  ( -0.8182917201112821504, 3.346456692913386100, 1.940849049717691344 ) ) ;
#30466=CARTESIAN_POINT ( 'NONE',  ( 0.000000000000000000, 3.267716535433071279, 0.000000000000000000 ) ) ;
#30467=CARTESIAN_POINT ( 'NONE',  ( -1.091055626815042201, 3.346456692913386100, 0.6299212598425164567 ) ) ;
#30468=EDGE_CURVE ( 'NONE', #35037, #35668, #26522, .T. ) ;
#30472=CARTESIAN_POINT ( 'NONE',  ( -0.5455278134075214336, 3.267716535433071279, 2.007874015748021268 ) ) ;
#30474=CARTESIAN_POINT ( 'NONE',  ( -1.091055626815042645, 3.346456692913386100, -0.1968503937007881899 ) ) ;
#30475=CARTESIAN_POINT ( 'NONE',  ( -1.166969139818015755, 3.267716535433071279, 4.048737525165545662E-16 ) ) ;
#30476=VERTEX_POINT ( 'NONE', #18535 ) ;
#30478=FACE_OUTER_BOUND ( 'NONE', #11072, .T. ) ;
#30479=VECTOR ( 'NONE', #41124, 39.37007874015748143 ) ;
#30481=LINE ( 'NONE', #6981, #43494 ) ;
#30484=CARTESIAN_POINT ( 'NONE',  ( 1.287906020515830141, 0.000000000000000000, 0.1181102362204704270 ) ) ;
#30485=VECTOR ( 'NONE', #41406, 39.37007874015748143 ) ;
#30486=VERTEX_POINT ( 'NONE', #49976 ) ;
#30488=CARTESIAN_POINT ( 'NONE',  ( -1.536664496436148184E-16, 0.000000000000000000, -0.5118110236220465570 ) ) ;
#30490=VERTEX_POINT ( 'NONE', #14402 ) ;
#30491=CARTESIAN_POINT ( 'NONE',  ( 1.909347346926324684, 3.346456692913386100, 1.102362204724403938 ) ) ;
#30492=ORIENTED_EDGE ( 'NONE', *, *, #15883, .T. ) ;
#30493=ORIENTED_EDGE ( 'NONE', *, *, #6405, .F. ) ;
#30494=DIRECTION ( 'NONE',  ( -1.000000000000000000, -0.000000000000000000, -0.000000000000000000 ) ) ;
#30497=CARTESIAN_POINT ( 'NONE',  ( 3.927031490892378253E-16, 3.346456692913386100, 1.377952755905504256 ) ) ;
#30498=EDGE_CURVE ( 'NONE', #35392, #31998, #42268, .T. ) ;
#30501=CARTESIAN_POINT ( 'NONE',  ( -2.182111253630085734, 0.000000000000000000, -0.6299212598425177889 ) ) ;
#30502=DIRECTION ( 'NONE',  ( -1.000000000000000000, 0.000000000000000000, 1.734723475976806848E-16 ) ) ;
#30504=DIRECTION ( 'NONE',  ( -3.469446951953613696E-16, 0.000000000000000000, -1.000000000000000000 ) ) ;
#30511=DIRECTION ( 'NONE',  ( 0.000000000000000000, -1.000000000000000000, 0.000000000000000000 ) ) ;
#30512=VECTOR ( 'NONE', #39718, 39.37007874015748143 ) ;
#30513=LINE ( 'NONE', #46225, #29966 ) ;
#30514=VECTOR ( 'NONE', #46292, 39.37007874015748143 ) ;
#30516=DIRECTION ( 'NONE',  ( 0.000000000000000000, 0.000000000000000000, -1.000000000000000000 ) ) ;
#30517=EDGE_LOOP ( 'NONE', ( #8625, #21873, #48875, #9073 ) ) ;
#30521=VECTOR ( 'NONE', #49041, 39.37007874015748143 ) ;
#30523=LINE ( 'NONE', #38025, #18355 ) ;
#30525=EDGE_CURVE ( 'NONE', #11498, #37571, #27022, .T. ) ;
#30528=DIRECTION ( 'NONE',  ( 1.000000000000000000, 0.000000000000000000, 0.000000000000000000 ) ) ;
#30529=FACE_OUTER_BOUND ( 'NONE', #40443, .T. ) ;
#30530=ORIENTED_EDGE ( 'NONE', *, *, #16592, .T. ) ;
#30532=CARTESIAN_POINT ( 'NONE',  ( -2.454875160333845674, 0.000000000000000000, -0.1574803149606298636 ) ) ;
#30534=DIRECTION ( 'NONE',  ( 1.000000000000000000, 0.000000000000000000, 0.000000000000000000 ) ) ;
#30535=EDGE_LOOP ( 'NONE', ( #593, #2402, #2796, #26666 ) ) ;
#30538=DIRECTION ( 'NONE',  ( -3.469446951953613696E-16, 0.000000000000000000, -1.000000000000000000 ) ) ;
#30539=ORIENTED_EDGE ( 'NONE', *, *, #14149, .T. ) ;
#30540=CARTESIAN_POINT ( 'NONE',  ( -0.2727639067037608278, 0.000000000000000000, -0.6692913385826758654 ) ) ;
#30541=ORIENTED_EDGE ( 'NONE', *, *, #20368, .F. ) ;
#30543=ORIENTED_EDGE ( 'NONE', *, *, #32585, .F. ) ;
#30544=CARTESIAN_POINT ( 'NONE',  ( 0.000000000000000000, 3.267716535433071279, 0.000000000000000000 ) ) ;
#30548=LINE ( 'NONE', #18924, #36755 ) ;
#30549=VECTOR ( 'NONE', #15807, 39.37007874015748143 ) ;
#30551=EDGE_LOOP ( 'NONE', ( #6446, #46137, #686, #22545 ) ) ;
#30552=ORIENTED_EDGE ( 'NONE', *, *, #14564, .T. ) ;
#30554=FACE_OUTER_BOUND ( 'NONE', #21059, .T. ) ;
#30555=VERTEX_POINT ( 'NONE', #30661 ) ;
#30556=CARTESIAN_POINT ( 'NONE',  ( -0.6214413264104945434, 3.346456692913386100, -0.4724409448818886470 ) ) ;
#30558=VECTOR ( 'NONE', #2555, 39.37007874015748143 ) ;
#30562=ADVANCED_FACE ( 'NONE', ( #8182 ), #50977, .F. ) ;
#30563=CARTESIAN_POINT ( 'NONE',  ( -0.8182917201112819283, 3.267716535433071279, 2.004783788421104163 ) ) ;
#30564=DIRECTION ( 'NONE',  ( -1.000000000000000000, 0.000000000000000000, 0.000000000000000000 ) ) ;
#30567=ORIENTED_EDGE ( 'NONE', *, *, #25610, .F. ) ;
#30568=LINE ( 'NONE', #46282, #7585 ) ;
#30569=ADVANCED_FACE ( 'NONE', ( #31168 ), #7170, .F. ) ;
#30570=LINE ( 'NONE', #37565, #19399 ) ;
#30571=ORIENTED_EDGE ( 'NONE', *, *, #4062, .F. ) ;
#30573=EDGE_LOOP ( 'NONE', ( #43111, #21075, #1575, #43151 ) ) ;
#30575=DIRECTION ( 'NONE',  ( 1.734723475976806848E-16, 0.000000000000000000, 1.000000000000000000 ) ) ;
#30578=FACE_OUTER_BOUND ( 'NONE', #49717, .T. ) ;
#30579=FACE_OUTER_BOUND ( 'NONE', #36862, .T. ) ;
#30580=CARTESIAN_POINT ( 'NONE',  ( -1.439733046521777027, 3.346456692913386100, -1.456692913385822186 ) ) ;
#30583=ORIENTED_EDGE ( 'NONE', *, *, #10934, .F. ) ;
#30584=CARTESIAN_POINT ( 'NONE',  ( -0.8182917201112819283, 0.000000000000000000, -2.047244094488181343 ) ) ;
#30587=ADVANCED_FACE ( 'NONE', ( #42527 ), #23156, .F. ) ;
#30589=DIRECTION ( 'NONE',  ( -0.000000000000000000, 1.000000000000000000, -0.000000000000000000 ) ) ;
#30591=CARTESIAN_POINT ( 'NONE',  ( -0.8182917201112819283, 3.346456692913386100, -0.03937007874015895081 ) ) ;
#30593=VERTEX_POINT ( 'NONE', #22910 ) ;
#30594=DIRECTION ( 'NONE',  ( 0.000000000000000000, -1.000000000000000000, 0.000000000000000000 ) ) ;
#30596=VECTOR ( 'NONE', #2240, 39.37007874015748143 ) ;
#30598=ORIENTED_EDGE ( 'NONE', *, *, #36542, .T. ) ;
#30599=CARTESIAN_POINT ( 'NONE',  ( -0.8942052331142552601, 3.346456692913386100, -7.512581982576723358E-16 ) ) ;
#30600=DIRECTION ( 'NONE',  ( -0.000000000000000000, 0.000000000000000000, 1.000000000000000000 ) ) ;
#30602=DIRECTION ( 'NONE',  ( 0.000000000000000000, 0.000000000000000000, 1.000000000000000000 ) ) ;
#30603=DIRECTION ( 'NONE',  ( -3.469446951953613696E-16, 0.000000000000000000, -1.000000000000000000 ) ) ;
#30605=ORIENTED_EDGE ( 'NONE', *, *, #1727, .F. ) ;
#30607=ORIENTED_EDGE ( 'NONE', *, *, #37802, .F. ) ;
#30608=FACE_BOUND ( 'NONE', #28533, .T. ) ;
#30611=ORIENTED_EDGE ( 'NONE', *, *, #29948, .F. ) ;
#30613=DIRECTION ( 'NONE',  ( -0.000000000000000000, 0.000000000000000000, 1.000000000000000000 ) ) ;
#30614=CARTESIAN_POINT ( 'NONE',  ( 0.2727639067037604947, 0.000000000000000000, 0.1574803149606283648 ) ) ;
#30615=LINE ( 'NONE', #22869, #29146 ) ;
#30616=CARTESIAN_POINT ( 'NONE',  ( -1.712496953225537633, 3.267716535433071279, -0.7874015748031470974 ) ) ;
#30618=VECTOR ( 'NONE', #8724, 39.37007874015748143 ) ;
#30619=AXIS2_PLACEMENT_3D ( 'NONE', #22901, #46866, #3535 ) ;
#30620=LINE ( 'NONE', #23886, #28102 ) ;
#30621=VECTOR ( 'NONE', #13734, 39.37007874015748143 ) ;
#30625=CARTESIAN_POINT ( 'NONE',  ( 0.4696143004045484903, 0.000000000000000000, 1.417322834645662777 ) ) ;
#30626=ADVANCED_FACE ( 'NONE', ( #19530 ), #43273, .F. ) ;
#30627=VECTOR ( 'NONE', #48303, 39.37007874015748143 ) ;
#30630=LINE ( 'NONE', #49192, #25728 ) ;
#30632=VECTOR ( 'NONE', #4389, 39.37007874015748143 ) ;
#30635=AXIS2_PLACEMENT_3D ( 'NONE', #5640, #48705, #13385 ) ;
#30637=ORIENTED_EDGE ( 'NONE', *, *, #31882, .F. ) ;
#30638=DIRECTION ( 'NONE',  ( -1.000000000000000000, -0.000000000000000000, -0.000000000000000000 ) ) ;
#30640=FACE_OUTER_BOUND ( 'NONE', #23586, .T. ) ;
#30642=ADVANCED_FACE ( 'NONE', ( #20302 ), #31941, .F. ) ;
#30643=PLANE ( 'NONE',  #33034 ) ;
#30645=CARTESIAN_POINT ( 'NONE',  ( 1.015142113812069091, 0.000000000000000000, -2.244094488188969283 ) ) ;
#30647=VERTEX_POINT ( 'NONE', #4303 ) ;
#30648=CARTESIAN_POINT ( 'NONE',  ( -1.166969139818016199, 3.346456692913386100, -1.299212598425192544 ) ) ;
#30652=ADVANCED_FACE ( 'NONE', ( #40193 ), #48395, .F. ) ;
#30654=AXIS2_PLACEMENT_3D ( 'NONE', #2150, #33656, #49348 ) ;
#30655=ORIENTED_EDGE ( 'NONE', *, *, #964, .F. ) ;
#30656=AXIS2_PLACEMENT_3D ( 'NONE', #908, #9167, #21045 ) ;
#30657=DIRECTION ( 'NONE',  ( 1.734723475976806848E-16, 0.000000000000000000, 1.000000000000000000 ) ) ;
#30658=LINE ( 'NONE', #11538, #15392 ) ;
#30659=ORIENTED_EDGE ( 'NONE', *, *, #25323, .F. ) ;
#30661=CARTESIAN_POINT ( 'NONE',  ( -2.032045338671488288, 3.346456692913386100, 0.7480314960629874665 ) ) ;
#30662=VECTOR ( 'NONE', #40221, 39.37007874015748143 ) ;
#30665=DIRECTION ( 'NONE',  ( 0.000000000000000000, 0.000000000000000000, -1.000000000000000000 ) ) ;
#30668=CARTESIAN_POINT ( 'NONE',  ( -1.712496953225537188, 3.346456692913386100, 1.102362204724404160 ) ) ;
#30669=DIRECTION ( 'NONE',  ( 1.000000000000000000, 0.000000000000000000, 0.000000000000000000 ) ) ;
#30670=CARTESIAN_POINT ( 'NONE',  ( 0.000000000000000000, 3.267716535433071279, 0.000000000000000000 ) ) ;
#30671=ORIENTED_EDGE ( 'NONE', *, *, #49108, .T. ) ;
#30673=ORIENTED_EDGE ( 'NONE', *, *, #19116, .T. ) ;
#30674=ORIENTED_EDGE ( 'NONE', *, *, #28452, .T. ) ;
#30677=DIRECTION ( 'NONE',  ( 1.734723475976806848E-16, -0.000000000000000000, 1.000000000000000000 ) ) ;
#30678=CARTESIAN_POINT ( 'NONE',  ( 1.287906020515830141, 3.346456692913386100, -1.141732283464564013 ) ) ;
#30679=ORIENTED_EDGE ( 'NONE', *, *, #30690, .T. ) ;
#30680=LINE ( 'NONE', #49244, #37976 ) ;
#30681=DIRECTION ( 'NONE',  ( -0.000000000000000000, 0.000000000000000000, 1.000000000000000000 ) ) ;
#30682=EDGE_CURVE ( 'NONE', #42385, #11104, #32973, .T. ) ;
#30683=PLANE ( 'NONE',  #39555 ) ;
#30686=VERTEX_POINT ( 'NONE', #28815 ) ;
#30687=CARTESIAN_POINT ( 'NONE',  ( 0.7423782071083091516, 3.267716535433071279, 1.692913385826762873 ) ) ;
#30688=FACE_BOUND ( 'NONE', #37616, .T. ) ;
#30689=ORIENTED_EDGE ( 'NONE', *, *, #37580, .T. ) ;
#30690=EDGE_CURVE ( 'NONE', #11339, #33436, #29065, .T. ) ;
#30692=VECTOR ( 'NONE', #39000, 39.37007874015748143 ) ;
#30694=EDGE_CURVE ( 'NONE', #36614, #46376, #4562, .T. ) ;
#30696=VERTEX_POINT ( 'NONE', #44807 ) ;
#30698=FACE_OUTER_BOUND ( 'NONE', #35966, .T. ) ;
#30700=DIRECTION ( 'NONE',  ( 1.734723475976806848E-16, -0.000000000000000000, 1.000000000000000000 ) ) ;
#30701=EDGE_LOOP ( 'NONE', ( #7981, #47265, #26879, #3099, #38198 ) ) ;
#30703=DIRECTION ( 'NONE',  ( 0.000000000000000000, 0.000000000000000000, -1.000000000000000000 ) ) ;
#30705=CARTESIAN_POINT ( 'NONE',  ( -0.5455278134075216556, 0.000000000000000000, -2.401574803149598036 ) ) ;
#30706=VECTOR ( 'NONE', #14097, 39.37007874015748143 ) ;
#30707=CARTESIAN_POINT ( 'NONE',  ( 0.000000000000000000, 3.267716535433071279, 1.574803149606291974 ) ) ;
#30708=ADVANCED_FACE ( 'NONE', ( #44553 ), #16443, .F. ) ;
#30711=ORIENTED_EDGE ( 'NONE', *, *, #13763, .F. ) ;
#30712=CARTESIAN_POINT ( 'NONE',  ( 2.100403847690402337, 3.267716535433071279, 0.1574803149606280872 ) ) ;
#30713=DIRECTION ( 'NONE',  ( -0.000000000000000000, 1.000000000000000000, -0.000000000000000000 ) ) ;
#30714=DIRECTION ( 'NONE',  ( 1.000000000000000000, 0.000000000000000000, 0.000000000000000000 ) ) ;
#30715=EDGE_CURVE ( 'NONE', #12697, #21513, #28301, .T. ) ;
#30717=DIRECTION ( 'NONE',  ( 1.734723475976806848E-16, -0.000000000000000000, 1.000000000000000000 ) ) ;
#30719=EDGE_CURVE ( 'NONE', #21756, #32019, #5326, .T. ) ;
#30720=LINE ( 'NONE', #37721, #3644 ) ;
#30721=ORIENTED_EDGE ( 'NONE', *, *, #13570, .F. ) ;
#30724=ORIENTED_EDGE ( 'NONE', *, *, #10049, .T. ) ;
#30726=EDGE_LOOP ( 'NONE', ( #17180, #42787, #6899, #15446 ) ) ;
#30727=PLANE ( 'NONE',  #27473 ) ;
#30729=DIRECTION ( 'NONE',  ( -0.000000000000000000, 1.000000000000000000, -0.000000000000000000 ) ) ;
#30730=VERTEX_POINT ( 'NONE', #9459 ) ;
#30732=ORIENTED_EDGE ( 'NONE', *, *, #13783, .F. ) ;
#30733=CARTESIAN_POINT ( 'NONE',  ( 2.059322335531026837, 3.267716535433071279, -0.6692913385826764205 ) ) ;
#30734=AXIS2_PLACEMENT_3D ( 'NONE', #5487, #36734, #8338 ) ;
#30735=ORIENTED_EDGE ( 'NONE', *, *, #29518, .F. ) ;
#30736=VECTOR ( 'NONE', #19637, 39.37007874015748143 ) ;
#30737=VECTOR ( 'NONE', #29177, 39.37007874015748143 ) ;
#30738=PLANE ( 'NONE',  #15286 ) ;
#30739=LINE ( 'NONE', #41849, #38737 ) ;
#30740=ORIENTED_EDGE ( 'NONE', *, *, #47301, .F. ) ;
#30744=ORIENTED_EDGE ( 'NONE', *, *, #36807, .F. ) ;
#30748=EDGE_CURVE ( 'NONE', #14850, #23656, #16185, .T. ) ;
#30750=CARTESIAN_POINT ( 'NONE',  ( 2.182111253630085290, 0.000000000000000000, 0.6299212598425161236 ) ) ;
#30752=EDGE_CURVE ( 'NONE', #17416, #11581, #13842, .T. ) ;
#30753=EDGE_CURVE ( 'NONE', #19187, #48689, #5837, .T. ) ;
#30754=ORIENTED_EDGE ( 'NONE', *, *, #44650, .T. ) ;
#30755=CARTESIAN_POINT ( 'NONE',  ( 0.1968503937007870241, 3.346456692913386100, -1.889763779527552146 ) ) ;
#30756=ORIENTED_EDGE ( 'NONE', *, *, #8555, .F. ) ;
#30757=ORIENTED_EDGE ( 'NONE', *, *, #1423, .F. ) ;
#30760=DIRECTION ( 'NONE',  ( 1.000000000000000000, 0.000000000000000000, 0.000000000000000000 ) ) ;
#30763=DIRECTION ( 'NONE',  ( -1.000000000000000000, 0.000000000000000000, -0.000000000000000000 ) ) ;
#30765=ORIENTED_EDGE ( 'NONE', *, *, #7421, .T. ) ;
#30766=VECTOR ( 'NONE', #39573, 39.37007874015748143 ) ;
#30767=LINE ( 'NONE', #3144, #36193 ) ;
#30768=CARTESIAN_POINT ( 'NONE',  ( 0.000000000000000000, 3.267716535433071279, 1.259842519685033135 ) ) ;
#30769=ORIENTED_EDGE ( 'NONE', *, *, #26902, .F. ) ;
#30770=LINE ( 'NONE', #33897, #6827 ) ;
#30771=CARTESIAN_POINT ( 'NONE',  ( -0.5455278134075214336, 3.346456692913386100, 2.095509194042718182 ) ) ;
#30772=AXIS2_PLACEMENT_3D ( 'NONE', #46416, #34583, #14705 ) ;
#30773=CIRCLE ( 'NONE', #37387, 2.106299212598425008 ) ;
#30777=DIRECTION ( 'NONE',  ( 0.000000000000000000, 0.000000000000000000, -1.000000000000000000 ) ) ;
#30779=CARTESIAN_POINT ( 'NONE',  ( -1.636583440222563857, 3.267716535433071279, 2.839019714148966584E-16 ) ) ;
#30781=CARTESIAN_POINT ( 'NONE',  ( 1.909347346926324684, 3.346456692913386100, 0.5905511811023582691 ) ) ;
#30782=EDGE_CURVE ( 'NONE', #9931, #43660, #33220, .T. ) ;
#30783=EDGE_LOOP ( 'NONE', ( #48208, #11710, #3833, #9694 ) ) ;
#30784=PLANE ( 'NONE',  #2622 ) ;
#30785=CARTESIAN_POINT ( 'NONE',  ( -1.636583440222564301, 0.000000000000000000, -0.3149606299212592275 ) ) ;
#30787=VERTEX_POINT ( 'NONE', #14602 ) ;
#30789=FACE_OUTER_BOUND ( 'NONE', #46063, .T. ) ;
#30790=EDGE_CURVE ( 'NONE', #23693, #34628, #29326, .T. ) ;
#30793=ORIENTED_EDGE ( 'NONE', *, *, #12567, .F. ) ;
#30794=CARTESIAN_POINT ( 'NONE',  ( -0.8182917201112819283, 3.346456692913386100, -0.4724409448818886470 ) ) ;
#30795=EDGE_LOOP ( 'NONE', ( #30454, #34970, #48915, #15863 ) ) ;
#30796=EDGE_CURVE ( 'NONE', #8785, #15117, #48903, .T. ) ;
#30797=DIRECTION ( 'NONE',  ( -0.000000000000000000, 1.000000000000000000, -0.000000000000000000 ) ) ;
#30798=FACE_OUTER_BOUND ( 'NONE', #44482, .T. ) ;
#30799=CARTESIAN_POINT ( 'NONE',  ( -1.195183497228115035E-16, 3.346456692913386100, -0.3149606299212591165 ) ) ;
#30801=VECTOR ( 'NONE', #44456, 39.37007874015748143 ) ;
#30802=ORIENTED_EDGE ( 'NONE', *, *, #23387, .T. ) ;
#30803=ORIENTED_EDGE ( 'NONE', *, *, #15711, .T. ) ;
#30805=CARTESIAN_POINT ( 'NONE',  ( -0.5455278134075217666, 3.226699998040866824, -2.401574803149598036 ) ) ;
#30808=PLANE ( 'NONE',  #26882 ) ;
#30809=CARTESIAN_POINT ( 'NONE',  ( 0.5455278134075208785, 3.346456692913386100, -2.034427629037600660 ) ) ;
#30811=EDGE_CURVE ( 'NONE', #6824, #17653, #2723, .T. ) ;
#30813=VERTEX_POINT ( 'NONE', #25966 ) ;
#30816=DIRECTION ( 'NONE',  ( -1.000000000000000000, 0.000000000000000000, 1.734723475976806848E-16 ) ) ;
#30819=EDGE_CURVE ( 'NONE', #8060, #23582, #13592, .T. ) ;
#30820=ORIENTED_EDGE ( 'NONE', *, *, #1603, .T. ) ;
#30822=LINE ( 'NONE', #16083, #22777 ) ;
#30823=VECTOR ( 'NONE', #3728, 39.37007874015748143 ) ;
#30825=ADVANCED_FACE ( 'NONE', ( #29841 ), #2225, .F. ) ;
#30827=ORIENTED_EDGE ( 'NONE', *, *, #6922, .F. ) ;
#30831=CARTESIAN_POINT ( 'NONE',  ( 0.7423782071083091516, 3.267716535433071279, -2.575641807848711673E-16 ) ) ;
#30834=CARTESIAN_POINT ( 'NONE',  ( 2.106197740627111958, 0.000000000000000000, -0.6692913385826764205 ) ) ;
#30837=CARTESIAN_POINT ( 'NONE',  ( 1.287906020515830141, 3.267716535433071279, -8.878505979408855953E-16 ) ) ;
#30840=VECTOR ( 'NONE', #11207, 39.37007874015748143 ) ;
#30841=DIRECTION ( 'NONE',  ( 1.000000000000000000, 0.000000000000000000, -3.469446951953613696E-16 ) ) ;
#30843=ORIENTED_EDGE ( 'NONE', *, *, #29300, .F. ) ;
#30844=AXIS2_PLACEMENT_3D ( 'NONE', #12406, #28143, #5172 ) ;
#30845=DIRECTION ( 'NONE',  ( 1.734723475976806848E-16, -0.000000000000000000, 1.000000000000000000 ) ) ;
#30846=AXIS2_PLACEMENT_3D ( 'NONE', #50727, #35810, #4310 ) ;
#30848=EDGE_CURVE ( 'NONE', #30279, #14307, #49915, .T. ) ;
#30849=VECTOR ( 'NONE', #628, 39.37007874015748143 ) ;
#30850=AXIS2_PLACEMENT_3D ( 'NONE', #19335, #46680, #27084 ) ;
#30852=CARTESIAN_POINT ( 'NONE',  ( -1.166969139818015755, 3.267716535433071279, 0.9055118110236167750 ) ) ;
#30854=CARTESIAN_POINT ( 'NONE',  ( 1.636583440222563635, 3.267716535433071279, -0.9448818897637765168 ) ) ;
#30856=EDGE_CURVE ( 'NONE', #42332, #30287, #21336, .T. ) ;
#30857=CARTESIAN_POINT ( 'NONE',  ( -1.909347346926324906, 0.000000000000000000, -1.102362204724405492 ) ) ;
#30858=PLANE ( 'NONE',  #28291 ) ;
#30859=ADVANCED_FACE ( 'NONE', ( #30096 ), #25709, .F. ) ;
#30860=FACE_OUTER_BOUND ( 'NONE', #43545, .T. ) ;
#30861=VECTOR ( 'NONE', #6537, 39.37007874015748143 ) ;
#30863=PLANE ( 'NONE',  #1585 ) ;
#30866=CARTESIAN_POINT ( 'NONE',  ( 0.4696143004045476577, 3.267716535433071279, -1.629301903132386767E-16 ) ) ;
#30867=CARTESIAN_POINT ( 'NONE',  ( -1.363819533518803473, 3.346456692913386100, -1.102362204724405270 ) ) ;
#30868=EDGE_CURVE ( 'NONE', #49388, #47496, #6353, .T. ) ;
#30869=ORIENTED_EDGE ( 'NONE', *, *, #10596, .T. ) ;
#30874=DIRECTION ( 'NONE',  ( -1.000000000000000000, 0.000000000000000000, -0.000000000000000000 ) ) ;
#30875=ADVANCED_FACE ( 'NONE', ( #46813 ), #15103, .F. ) ;
#30876=DIRECTION ( 'NONE',  ( 1.000000000000000000, 0.000000000000000000, 0.000000000000000000 ) ) ;
#30878=EDGE_CURVE ( 'NONE', #43653, #15242, #15359, .T. ) ;
#30879=EDGE_LOOP ( 'NONE', ( #25548, #26771, #4837, #46272 ) ) ;
#30882=EDGE_CURVE ( 'NONE', #42090, #33404, #7362, .T. ) ;
#30884=VECTOR ( 'NONE', #48823, 39.37007874015748143 ) ;
#30885=ORIENTED_EDGE ( 'NONE', *, *, #42419, .F. ) ;
#30889=ORIENTED_EDGE ( 'NONE', *, *, #8547, .T. ) ;
#30890=VERTEX_POINT ( 'NONE', #14858 ) ;
#30891=VECTOR ( 'NONE', #25776, 39.37007874015748143 ) ;
#30892=VECTOR ( 'NONE', #43334, 39.37007874015748143 ) ;
#30893=ORIENTED_EDGE ( 'NONE', *, *, #42412, .T. ) ;
#30894=VERTEX_POINT ( 'NONE', #18732 ) ;
#30896=AXIS2_PLACEMENT_3D ( 'NONE', #31481, #24246, #39991 ) ;
#30899=LINE ( 'NONE', #15402, #48124 ) ;
#30901=CARTESIAN_POINT ( 'NONE',  ( 0.000000000000000000, 3.267716535433071279, 1.889763779527550147 ) ) ;
#30902=CARTESIAN_POINT ( 'NONE',  ( 1.833433833923351353, 3.267716535433071279, 1.377952755905504256 ) ) ;
#30903=ORIENTED_EDGE ( 'NONE', *, *, #21647, .F. ) ;
#30907=FACE_OUTER_BOUND ( 'NONE', #45379, .T. ) ;
#30911=LINE ( 'NONE', #46620, #48335 ) ;
#30912=ORIENTED_EDGE ( 'NONE', *, *, #31110, .T. ) ;
#30913=LINE ( 'NONE', #47116, #50947 ) ;
#30915=ADVANCED_FACE ( 'NONE', ( #38854 ), #11487, .F. ) ;
#30916=VECTOR ( 'NONE', #43128, 39.37007874015748143 ) ;
#30919=CARTESIAN_POINT ( 'NONE',  ( 0.000000000000000000, 3.267716535433071279, -1.259842519685035134 ) ) ;
#30921=LINE ( 'NONE', #22415, #17388 ) ;
#30922=VECTOR ( 'NONE', #29850, 39.37007874015748143 ) ;
#30928=AXIS2_PLACEMENT_3D ( 'NONE', #177, #31683, #8193 ) ;
#30929=ORIENTED_EDGE ( 'NONE', *, *, #8071, .T. ) ;
#30930=VERTEX_POINT ( 'NONE', #6852 ) ;
#30931=DIRECTION ( 'NONE',  ( 0.000000000000000000, 0.000000000000000000, -1.000000000000000000 ) ) ;
#30934=ADVANCED_FACE ( 'NONE', ( #19725 ), #30858, .F. ) ;
#30935=CARTESIAN_POINT ( 'NONE',  ( -0.2727639067037607723, 3.346456692913386100, 0.1574803149606283648 ) ) ;
#30942=EDGE_CURVE ( 'NONE', #20401, #47345, #27220, .T. ) ;
#30943=DIRECTION ( 'NONE',  ( 1.734723475976806848E-16, -0.000000000000000000, 1.000000000000000000 ) ) ;
#30944=FACE_BOUND ( 'NONE', #35969, .T. ) ;
#30945=ORIENTED_EDGE ( 'NONE', *, *, #34491, .F. ) ;
#30947=CARTESIAN_POINT ( 'NONE',  ( 0.8182917201112819283, 3.346456692913386100, -1.102362204724405714 ) ) ;
#30948=VERTEX_POINT ( 'NONE', #7109 ) ;
#30949=ORIENTED_EDGE ( 'NONE', *, *, #39385, .F. ) ;
#30952=CIRCLE ( 'NONE', #47378, 2.165354330708661568 ) ;
#30953=EDGE_LOOP ( 'NONE', ( #13458, #27883, #50904, #29063 ) ) ;
#30954=LINE ( 'NONE', #42311, #41870 ) ;
#30955=AXIS2_PLACEMENT_3D ( 'NONE', #41596, #34368, #7244 ) ;
#30956=VERTEX_POINT ( 'NONE', #43213 ) ;
#30957=PLANE ( 'NONE',  #30141 ) ;
#30958=PLANE ( 'NONE',  #27477 ) ;
#30961=ORIENTED_EDGE ( 'NONE', *, *, #46005, .T. ) ;
#30962=VECTOR ( 'NONE', #10676, 39.37007874015748143 ) ;
#30963=DIRECTION ( 'NONE',  ( 1.000000000000000000, 0.000000000000000000, 0.000000000000000000 ) ) ;
#30967=DIRECTION ( 'NONE',  ( 0.000000000000000000, 0.000000000000000000, -1.000000000000000000 ) ) ;
#30969=CARTESIAN_POINT ( 'NONE',  ( 0.5455278134075212115, 3.346456692913386100, -0.6299212598425181220 ) ) ;
#30970=EDGE_CURVE ( 'NONE', #36606, #19754, #31363, .T. ) ;
#30971=ORIENTED_EDGE ( 'NONE', *, *, #35650, .F. ) ;
#30972=CARTESIAN_POINT ( 'NONE',  ( 0.7423782071083087075, 3.346456692913386100, -6.146657985744592735E-16 ) ) ;
#30973=ADVANCED_FACE ( 'NONE', ( #2982 ), #38606, .F. ) ;
#30974=ORIENTED_EDGE ( 'NONE', *, *, #19384, .F. ) ;
#30975=EDGE_CURVE ( 'NONE', #8227, #48919, #22855, .T. ) ;
#30976=EDGE_CURVE ( 'NONE', #1350, #22076, #35487, .T. ) ;
#30979=CARTESIAN_POINT ( 'NONE',  ( 0.000000000000000000, 3.267716535433071279, -0.6299212598425175669 ) ) ;
#30980=ORIENTED_EDGE ( 'NONE', *, *, #33980, .F. ) ;
#30981=EDGE_CURVE ( 'NONE', #49145, #27965, #26465, .T. ) ;
#30982=DIRECTION ( 'NONE',  ( -0.000000000000000000, 1.000000000000000000, -0.000000000000000000 ) ) ;
#30983=VECTOR ( 'NONE', #7110, 39.37007874015748143 ) ;
#30984=EDGE_LOOP ( 'NONE', ( #7832, #31808, #31275, #24054 ) ) ;
#30985=PLANE ( 'NONE',  #50936 ) ;
#30986=VECTOR ( 'NONE', #31379, 39.37007874015748143 ) ;
#30988=CARTESIAN_POINT ( 'NONE',  ( 1.015142113812069091, 3.346456692913386100, -2.047244094488181343 ) ) ;
#30989=LINE ( 'NONE', #11867, #46974 ) ;
#30990=EDGE_CURVE ( 'NONE', #42728, #14441, #20752, .T. ) ;
#30991=VECTOR ( 'NONE', #37756, 39.37007874015748143 ) ;
#30993=VECTOR ( 'NONE', #824, 39.37007874015748143 ) ;
#30994=PLANE ( 'NONE',  #33800 ) ;
#30996=ORIENTED_EDGE ( 'NONE', *, *, #45422, .T. ) ;
#31000=CARTESIAN_POINT ( 'NONE',  ( 1.997134316236881091, 3.267716535433071279, -0.6692913385826764205 ) ) ;
#31001=ORIENTED_EDGE ( 'NONE', *, *, #140, .F. ) ;
#31004=VERTEX_POINT ( 'NONE', #32388 ) ;
#31006=ORIENTED_EDGE ( 'NONE', *, *, #42585, .F. ) ;
#31007=EDGE_LOOP ( 'NONE', ( #29804, #31090, #5808, #16252 ) ) ;
#31008=ADVANCED_FACE ( 'NONE', ( #32648 ), #48080, .F. ) ;
#31009=ORIENTED_EDGE ( 'NONE', *, *, #21580, .F. ) ;
#31012=LINE ( 'NONE', #34637, #21713 ) ;
#31014=LINE ( 'NONE', #8534, #11882 ) ;
#31015=DIRECTION ( 'NONE',  ( 1.000000000000000000, 0.000000000000000000, 0.000000000000000000 ) ) ;
#31017=VERTEX_POINT ( 'NONE', #12761 ) ;
#31018=VECTOR ( 'NONE', #6474, 39.37007874015748143 ) ;
#31019=CARTESIAN_POINT ( 'NONE',  ( -1.909347346926324462, 3.267716535433071279, 0.5905511811023582691 ) ) ;
#31022=ORIENTED_EDGE ( 'NONE', *, *, #10764, .F. ) ;
#31024=CARTESIAN_POINT ( 'NONE',  ( -0.8182917201112819283, 3.267716535433071279, 2.047244094488179567 ) ) ;
#31026=AXIS2_PLACEMENT_3D ( 'NONE', #14159, #6919, #45622 ) ;
#31027=CARTESIAN_POINT ( 'NONE',  ( -0.8182917201112819283, 3.346456692913386100, 0.1574803149606285035 ) ) ;
#31028=CARTESIAN_POINT ( 'NONE',  ( -0.5455278134075216556, 3.346456692913386100, -2.401574803149598036 ) ) ;
#31031=EDGE_LOOP ( 'NONE', ( #43464, #20732, #30769, #12955 ) ) ;
#31032=CARTESIAN_POINT ( 'NONE',  ( 2.106197740627112402, 3.346456692913386100, -0.5026832550384014997 ) ) ;
#31034=EDGE_CURVE ( 'NONE', #45523, #34367, #365, .T. ) ;
#31035=ADVANCED_FACE ( 'NONE', ( #47825 ), #44241, .F. ) ;
#31036=ORIENTED_EDGE ( 'NONE', *, *, #40882, .F. ) ;
#31037=DIRECTION ( 'NONE',  ( -3.469446951953613696E-16, 0.000000000000000000, -1.000000000000000000 ) ) ;
#31041=ORIENTED_EDGE ( 'NONE', *, *, #37032, .F. ) ;
#31042=EDGE_CURVE ( 'NONE', #41514, #44911, #28233, .T. ) ;
#31043=VERTEX_POINT ( 'NONE', #11988 ) ;
#31044=LINE ( 'NONE', #18916, #27141 ) ;
#31045=ORIENTED_EDGE ( 'NONE', *, *, #3521, .T. ) ;
#31046=CARTESIAN_POINT ( 'NONE',  ( 1.091055626815042645, 3.267716535433071279, -1.892679809432644882E-16 ) ) ;
#31050=CARTESIAN_POINT ( 'NONE',  ( 0.000000000000000000, 3.267716535433071279, -1.417322834645664331 ) ) ;
#31051=EDGE_CURVE ( 'NONE', #20003, #31330, #5009, .T. ) ;
#31053=EDGE_LOOP ( 'NONE', ( #45569, #19458, #31387, #50058 ) ) ;
#31055=VERTEX_POINT ( 'NONE', #32133 ) ;
#31056=CARTESIAN_POINT ( 'NONE',  ( -0.8182917201112814842, 0.000000000000000000, 1.732283464566921172 ) ) ;
#31057=VECTOR ( 'NONE', #46671, 39.37007874015748143 ) ;
#31058=DIRECTION ( 'NONE',  ( 0.000000000000000000, 0.000000000000000000, -1.000000000000000000 ) ) ;
#31059=VECTOR ( 'NONE', #25188, 39.37007874015748143 ) ;
#31061=ORIENTED_EDGE ( 'NONE', *, *, #30234, .F. ) ;
#31062=EDGE_CURVE ( 'NONE', #37485, #19157, #1127, .T. ) ;
#31063=DIRECTION ( 'NONE',  ( 0.000000000000000000, 1.000000000000000000, 0.000000000000000000 ) ) ;
#31064=CARTESIAN_POINT ( 'NONE',  ( -1.636583440222564301, 3.346456692913386100, -1.417869535855831975 ) ) ;
#31065=DIRECTION ( 'NONE',  ( -1.000000000000000000, -0.000000000000000000, -0.000000000000000000 ) ) ;
#31067=VERTEX_POINT ( 'NONE', #16891 ) ;
#31069=DIRECTION ( 'NONE',  ( -1.000000000000000000, -0.000000000000000000, -0.000000000000000000 ) ) ;
#31072=CARTESIAN_POINT ( 'NONE',  ( 0.4696143004045479352, 3.267716535433071279, -0.4724409448818886470 ) ) ;
#31075=PLANE ( 'NONE',  #41729 ) ;
#31077=ORIENTED_EDGE ( 'NONE', *, *, #45721, .F. ) ;
#31078=LINE ( 'NONE', #46285, #39792 ) ;
#31079=ORIENTED_EDGE ( 'NONE', *, *, #45651, .T. ) ;
#31080=ORIENTED_EDGE ( 'NONE', *, *, #36585, .T. ) ;
#31081=LINE ( 'NONE', #23831, #26236 ) ;
#31082=LINE ( 'NONE', #23572, #13525 ) ;
#31084=DIRECTION ( 'NONE',  ( 0.000000000000000000, 0.000000000000000000, -1.000000000000000000 ) ) ;
#31088=VERTEX_POINT ( 'NONE', #24117 ) ;
#31090=ORIENTED_EDGE ( 'NONE', *, *, #19890, .F. ) ;
#31091=DIRECTION ( 'NONE',  ( -0.000000000000000000, 0.000000000000000000, 1.000000000000000000 ) ) ;
#31092=LINE ( 'NONE', #46795, #25091 ) ;
#31093=EDGE_CURVE ( 'NONE', #728, #19354, #19972, .T. ) ;
#31095=CARTESIAN_POINT ( 'NONE',  ( -1.909347346926324906, 3.346456692913386100, -0.4724409448818884805 ) ) ;
#31096=LINE ( 'NONE', #34219, #47559 ) ;
#31098=AXIS2_PLACEMENT_3D ( 'NONE', #39088, #38096, #6841 ) ;
#31100=DIRECTION ( 'NONE',  ( -3.469446951953613696E-16, 0.000000000000000000, -1.000000000000000000 ) ) ;
#31101=CARTESIAN_POINT ( 'NONE',  ( -0.2727639067037607723, 3.346456692913386100, -0.4724409448818883694 ) ) ;
#31102=EDGE_CURVE ( 'NONE', #1336, #18633, #880, .T. ) ;
#31103=ORIENTED_EDGE ( 'NONE', *, *, #16362, .T. ) ;
#31104=LINE ( 'NONE', #42712, #34723 ) ;
#31110=EDGE_CURVE ( 'NONE', #44277, #35032, #23863, .T. ) ;
#31111=CARTESIAN_POINT ( 'NONE',  ( -1.439733046521776361, 3.267716535433071279, -0.1968503937007879123 ) ) ;
#31112=ORIENTED_EDGE ( 'NONE', *, *, #6619, .F. ) ;
#31113=CARTESIAN_POINT ( 'NONE',  ( 0.1968503937007878568, 3.267716535433071279, 2.204724409448808764 ) ) ;
#31114=ORIENTED_EDGE ( 'NONE', *, *, #35445, .F. ) ;
#31115=VECTOR ( 'NONE', #23716, 39.37007874015748143 ) ;
#31116=CARTESIAN_POINT ( 'NONE',  ( -0.6214413264104945434, 3.267716535433071279, -2.074263738136479240 ) ) ;
#31118=LINE ( 'NONE', #42724, #48199 ) ;
#31119=DIRECTION ( 'NONE',  ( -0.000000000000000000, 0.000000000000000000, 1.000000000000000000 ) ) ;
#31121=ORIENTED_EDGE ( 'NONE', *, *, #39094, .F. ) ;
#31122=DIRECTION ( 'NONE',  ( -1.000000000000000000, -0.000000000000000000, -0.000000000000000000 ) ) ;
#31124=CARTESIAN_POINT ( 'NONE',  ( 0.4696143004045476577, 0.000000000000000000, -2.047244094488182231 ) ) ;
#31125=PLANE ( 'NONE',  #17801 ) ;
#31127=DIRECTION ( 'NONE',  ( -3.469446951953613696E-16, 0.000000000000000000, -1.000000000000000000 ) ) ;
#31129=EDGE_LOOP ( 'NONE', ( #9424, #4505, #4608, #32582 ) ) ;
#31130=DIRECTION ( 'NONE',  ( -3.469446951953613696E-16, 0.000000000000000000, -1.000000000000000000 ) ) ;
#31131=VECTOR ( 'NONE', #68, 39.37007874015748143 ) ;
#31134=LINE ( 'NONE', #3509, #20736 ) ;
#31135=EDGE_LOOP ( 'NONE', ( #32744, #25139, #5037, #2187 ) ) ;
#31136=CARTESIAN_POINT ( 'NONE',  ( 0.4696143004045479352, 3.267716535433071279, 0.1574803149606283648 ) ) ;
#31137=VERTEX_POINT ( 'NONE', #38730 ) ;
#31141=ADVANCED_FACE ( 'NONE', ( #46190 ), #30727, .F. ) ;
#31142=ORIENTED_EDGE ( 'NONE', *, *, #34159, .F. ) ;
#31143=ORIENTED_EDGE ( 'NONE', *, *, #23643, .F. ) ;
#31144=DIRECTION ( 'NONE',  ( -0.000000000000000000, 1.000000000000000000, -0.000000000000000000 ) ) ;
#31145=VERTEX_POINT ( 'NONE', #25645 ) ;
#31148=DIRECTION ( 'NONE',  ( -0.000000000000000000, 0.000000000000000000, 1.000000000000000000 ) ) ;
#31150=LINE ( 'NONE', #18258, #4964 ) ;
#31151=ADVANCED_FACE ( 'NONE', ( #45241 ), #17647, .F. ) ;
#31153=DIRECTION ( 'NONE',  ( 0.000000000000000000, 0.000000000000000000, 1.000000000000000000 ) ) ;
#31154=ORIENTED_EDGE ( 'NONE', *, *, #10507, .T. ) ;
#31155=DIRECTION ( 'NONE',  ( 0.000000000000000000, 0.000000000000000000, -1.000000000000000000 ) ) ;
#31157=CARTESIAN_POINT ( 'NONE',  ( -0.8182917201112814842, 3.346456692913386100, 1.220472440944875281 ) ) ;
#31159=EDGE_CURVE ( 'NONE', #47282, #23728, #1641, .T. ) ;
#31161=CARTESIAN_POINT ( 'NONE',  ( -0.07591351300297333182, 3.346456692913386100, 0.4724409448818869817 ) ) ;
#31162=CARTESIAN_POINT ( 'NONE',  ( 1.015142113812069313, 0.000000000000000000, -0.1574803149606301411 ) ) ;
#31168=FACE_OUTER_BOUND ( 'NONE', #50920, .T. ) ;
#31171=VECTOR ( 'NONE', #34570, 39.37007874015748143 ) ;
#31172=DIRECTION ( 'NONE',  ( -3.469446951953613696E-16, 0.000000000000000000, -1.000000000000000000 ) ) ;
#31173=VERTEX_POINT ( 'NONE', #50045 ) ;
#31175=LINE ( 'NONE', #11547, #40728 ) ;
#31176=AXIS2_PLACEMENT_3D ( 'NONE', #47703, #12377, #43602 ) ;
#31177=CARTESIAN_POINT ( 'NONE',  ( -0.2727639067037608278, 3.346456692913386100, -0.6692913385826758654 ) ) ;
#31178=FACE_OUTER_BOUND ( 'NONE', #677, .T. ) ;
#31182=VERTEX_POINT ( 'NONE', #1899 ) ;
#31184=VERTEX_POINT ( 'NONE', #5519 ) ;
#31187=DIRECTION ( 'NONE',  ( 1.734723475976806848E-16, 0.000000000000000000, 1.000000000000000000 ) ) ;
#31189=FACE_OUTER_BOUND ( 'NONE', #19528, .T. ) ;
#31191=CARTESIAN_POINT ( 'NONE',  ( 4.268512490100411402E-16, 0.000000000000000000, 1.574803149606291974 ) ) ;
#31192=ORIENTED_EDGE ( 'NONE', *, *, #25136, .T. ) ;
#31193=ORIENTED_EDGE ( 'NONE', *, *, #45874, .T. ) ;
#31195=VERTEX_POINT ( 'NONE', #3353 ) ;
#31196=DIRECTION ( 'NONE',  ( 1.000000000000000000, 0.000000000000000000, 0.000000000000000000 ) ) ;
#31197=ADVANCED_FACE ( 'NONE', ( #21268 ), #48587, .F. ) ;
#31199=EDGE_CURVE ( 'NONE', #47188, #45998, #19093, .T. ) ;
#31202=DIRECTION ( 'NONE',  ( 0.000000000000000000, 0.000000000000000000, 1.000000000000000000 ) ) ;
#31203=ADVANCED_FACE ( 'NONE', ( #30478 ), #9905, .F. ) ;
#31206=AXIS2_PLACEMENT_3D ( 'NONE', #46158, #34067, #26556 ) ;
#31207=PLANE ( 'NONE',  #45965 ) ;
#31208=ORIENTED_EDGE ( 'NONE', *, *, #36996, .T. ) ;
#31209=FACE_OUTER_BOUND ( 'NONE', #36848, .T. ) ;
#31211=DIRECTION ( 'NONE',  ( 1.000000000000000000, 0.000000000000000000, 0.000000000000000000 ) ) ;
#31212=VECTOR ( 'NONE', #13028, 39.37007874015748143 ) ;
#31216=ORIENTED_EDGE ( 'NONE', *, *, #5967, .F. ) ;
#31217=ORIENTED_EDGE ( 'NONE', *, *, #15240, .F. ) ;
#31222=AXIS2_PLACEMENT_3D ( 'NONE', #49913, #37856, #9966 ) ;
#31224=PLANE ( 'NONE',  #23162 ) ;
#31225=EDGE_CURVE ( 'NONE', #35542, #10793, #5774, .T. ) ;
#31227=DIRECTION ( 'NONE',  ( -1.000000000000000000, 0.000000000000000000, 1.734723475976806848E-16 ) ) ;
#31231=ADVANCED_FACE ( 'NONE', ( #31238 ), #19342, .F. ) ;
#31232=VERTEX_POINT ( 'NONE', #31483 ) ;
#31233=LINE ( 'NONE', #752, #21797 ) ;
#31235=EDGE_CURVE ( 'NONE', #19884, #6227, #12117, .T. ) ;
#31236=ORIENTED_EDGE ( 'NONE', *, *, #19547, .F. ) ;
#31237=ORIENTED_EDGE ( 'NONE', *, *, #14068, .T. ) ;
#31238=FACE_OUTER_BOUND ( 'NONE', #44635, .T. ) ;
#31239=CARTESIAN_POINT ( 'NONE',  ( 0.1968503937007877735, 0.000000000000000000, 0.7480314960629874665 ) ) ;
#31240=VECTOR ( 'NONE', #28767, 39.37007874015748143 ) ;
#31241=ORIENTED_EDGE ( 'NONE', *, *, #20167, .T. ) ;
#31243=ORIENTED_EDGE ( 'NONE', *, *, #25198, .F. ) ;
#31245=ORIENTED_EDGE ( 'NONE', *, *, #5679, .T. ) ;
#31246=VECTOR ( 'NONE', #5217, 39.37007874015748143 ) ;
#31248=CARTESIAN_POINT ( 'NONE',  ( 4.268512490100411402E-16, 3.346456692913386100, 1.574803149606291974 ) ) ;
#31249=LINE ( 'NONE', #19603, #38770 ) ;
#31250=VECTOR ( 'NONE', #21060, 39.37007874015748143 ) ;
#31252=CARTESIAN_POINT ( 'NONE',  ( 0.7423782071083091516, 3.267716535433071279, 1.062992125984246083 ) ) ;
#31254=ORIENTED_EDGE ( 'NONE', *, *, #34925, .F. ) ;
#31256=LINE ( 'NONE', #777, #23174 ) ;
#31260=DIRECTION ( 'NONE',  ( 1.000000000000000000, 0.000000000000000000, -3.469446951953613696E-16 ) ) ;
#31266=ORIENTED_EDGE ( 'NONE', *, *, #8958, .F. ) ;
#31269=ORIENTED_EDGE ( 'NONE', *, *, #40385, .F. ) ;
#31271=CARTESIAN_POINT ( 'NONE',  ( 0.2727639067037604947, 3.346456692913386100, -0.4724409448818886470 ) ) ;
#31272=VECTOR ( 'NONE', #48540, 39.37007874015748143 ) ;
#31274=LINE ( 'NONE', #39261, #31282 ) ;
#31275=ORIENTED_EDGE ( 'NONE', *, *, #16264, .T. ) ;
#31278=CARTESIAN_POINT ( 'NONE',  ( 1.833433833923351353, 0.000000000000000000, -1.259842519685035800 ) ) ;
#31280=LINE ( 'NONE', #5880, #45565 ) ;
#31282=VECTOR ( 'NONE', #27376, 39.37007874015748143 ) ;
#31284=VECTOR ( 'NONE', #6549, 39.37007874015748143 ) ;
#31285=CARTESIAN_POINT ( 'NONE',  ( 0.4696143004045478797, 3.346456692913386100, -0.6692913385826760875 ) ) ;
#31286=DIRECTION ( 'NONE',  ( 1.000000000000000000, 0.000000000000000000, 0.000000000000000000 ) ) ;
#31287=DIRECTION ( 'NONE',  ( -1.000000000000000000, 0.000000000000000000, -0.000000000000000000 ) ) ;
#31288=VERTEX_POINT ( 'NONE', #46687 ) ;
#31289=CARTESIAN_POINT ( 'NONE',  ( -0.8942052331142552601, 0.000000000000000000, -1.141732283464563569 ) ) ;
#31291=ADVANCED_FACE ( 'NONE', ( #27341 ), #43339, .F. ) ;
#31292=AXIS2_PLACEMENT_3D ( 'NONE', #49363, #33425, #40643 ) ;
#31293=EDGE_LOOP ( 'NONE', ( #23179, #18339, #48686, #20014 ) ) ;
#31294=ORIENTED_EDGE ( 'NONE', *, *, #17215, .F. ) ;
#31295=LINE ( 'NONE', #27654, #13384 ) ;
#31296=DIRECTION ( 'NONE',  ( -0.000000000000000000, 1.000000000000000000, -0.000000000000000000 ) ) ;
#31299=VERTEX_POINT ( 'NONE', #11854 ) ;
#31301=ORIENTED_EDGE ( 'NONE', *, *, #20305, .T. ) ;
#31303=VERTEX_POINT ( 'NONE', #23221 ) ;
#31304=LINE ( 'NONE', #11676, #41690 ) ;
#31305=LINE ( 'NONE', #50855, #23918 ) ;
#31306=CARTESIAN_POINT ( 'NONE',  ( 2.378961647330872786, 3.267716535433071279, -8.253681236146643855E-16 ) ) ;
#31308=EDGE_LOOP ( 'NONE', ( #27368, #25301, #2382, #25839 ) ) ;
#31310=ORIENTED_EDGE ( 'NONE', *, *, #7848, .T. ) ;
#31311=DIRECTION ( 'NONE',  ( 1.000000000000000000, 0.000000000000000000, 0.000000000000000000 ) ) ;
#31312=CARTESIAN_POINT ( 'NONE',  ( -1.439733046521776583, 0.000000000000000000, -1.259842519685034468 ) ) ;
#31313=VERTEX_POINT ( 'NONE', #39994 ) ;
#31314=EDGE_LOOP ( 'NONE', ( #1742, #22671, #15348, #28250 ) ) ;
#31315=CARTESIAN_POINT ( 'NONE',  ( -1.788632549858358844, 3.346456692913386100, 1.220472440944875059 ) ) ;
#31317=LINE ( 'NONE', #8069, #6355 ) ;
#31319=ORIENTED_EDGE ( 'NONE', *, *, #39791, .T. ) ;
#31320=ORIENTED_EDGE ( 'NONE', *, *, #35758, .F. ) ;
#31322=LINE ( 'NONE', #50132, #44752 ) ;
#31323=LINE ( 'NONE', #36219, #38541 ) ;
#31324=EDGE_LOOP ( 'NONE', ( #3005, #6178, #33567, #50418 ) ) ;
#31326=CARTESIAN_POINT ( 'NONE',  ( 0.1968503937007874405, 0.000000000000000000, 0.000000000000000000 ) ) ;
#31327=VERTEX_POINT ( 'NONE', #4626 ) ;
#31328=ADVANCED_FACE ( 'NONE', ( #19846 ), #43848, .F. ) ;
#31330=VERTEX_POINT ( 'NONE', #32003 ) ;
#31331=ORIENTED_EDGE ( 'NONE', *, *, #1216, .T. ) ;
#31332=VECTOR ( 'NONE', #6296, 39.37007874015748143 ) ;
#31333=DIRECTION ( 'NONE',  ( 1.000000000000000000, -0.000000000000000000, 0.000000000000000000 ) ) ;
#31334=CARTESIAN_POINT ( 'NONE',  ( 1.636583440222563635, 0.000000000000000000, -1.141732283464564013 ) ) ;
#31337=LINE ( 'NONE', #50887, #11564 ) ;
#31340=EDGE_CURVE ( 'NONE', #33624, #37378, #27090, .T. ) ;
#31341=CARTESIAN_POINT ( 'NONE',  ( 0.8182917201112819283, 3.346456692913386100, -1.102362204724405714 ) ) ;
#31343=ORIENTED_EDGE ( 'NONE', *, *, #27007, .F. ) ;
#31344=VERTEX_POINT ( 'NONE', #43593 ) ;
#31345=FACE_OUTER_BOUND ( 'NONE', #38488, .T. ) ;
#31347=EDGE_CURVE ( 'NONE', #8483, #19508, #7482, .T. ) ;
#31348=DIRECTION ( 'NONE',  ( 1.734723475976806848E-16, 0.000000000000000000, 1.000000000000000000 ) ) ;
#31351=CARTESIAN_POINT ( 'NONE',  ( 0.2727639067037609943, 3.267716535433071279, 1.220472440944875281 ) ) ;
#31352=ADVANCED_FACE ( 'NONE', ( #20881 ), #33033, .F. ) ;
#31355=EDGE_LOOP ( 'NONE', ( #42233, #46560, #29744, #21020 ) ) ;
#31356=CARTESIAN_POINT ( 'NONE',  ( -0.2727639067037607168, 3.267716535433071279, 4.731699523581612823E-17 ) ) ;
#31357=CIRCLE ( 'NONE', #33844, 2.165354330708661568 ) ;
#31360=ADVANCED_FACE ( 'NONE', ( #48970 ), #12625, .F. ) ;
#31362=LINE ( 'NONE', #11486, #48136 ) ;
#31363=LINE ( 'NONE', #11233, #6041 ) ;
#31364=DIRECTION ( 'NONE',  ( -0.000000000000000000, 1.000000000000000000, -0.000000000000000000 ) ) ;
#31365=VERTEX_POINT ( 'NONE', #5392 ) ;
#31366=FACE_OUTER_BOUND ( 'NONE', #5966, .T. ) ;
#31367=AXIS2_PLACEMENT_3D ( 'NONE', #17535, #33300, #48224 ) ;
#31368=VERTEX_POINT ( 'NONE', #17022 ) ;
#31369=DIRECTION ( 'NONE',  ( 0.000000000000000000, 0.000000000000000000, -1.000000000000000000 ) ) ;
#31370=EDGE_CURVE ( 'NONE', #11723, #12457, #44110, .T. ) ;
#31372=LINE ( 'NONE', #39622, #22709 ) ;
#31375=LINE ( 'NONE', #22364, #37229 ) ;
#31377=ORIENTED_EDGE ( 'NONE', *, *, #39951, .F. ) ;
#31378=PLANE ( 'NONE',  #36567 ) ;
#31379=DIRECTION ( 'NONE',  ( -0.000000000000000000, 1.000000000000000000, -0.000000000000000000 ) ) ;
#31380=DIRECTION ( 'NONE',  ( 0.000000000000000000, 0.000000000000000000, -1.000000000000000000 ) ) ;
#31381=DIRECTION ( 'NONE',  ( -3.469446951953613696E-16, 0.000000000000000000, -1.000000000000000000 ) ) ;
#31382=ORIENTED_EDGE ( 'NONE', *, *, #7563, .T. ) ;
#31385=CARTESIAN_POINT ( 'NONE',  ( 0.8182917201112819283, 3.346456692913386100, 0.5905511811023579360 ) ) ;
#31386=CARTESIAN_POINT ( 'NONE',  ( 1.091055626815042423, 0.000000000000000000, -1.259842519685035134 ) ) ;
#31387=ORIENTED_EDGE ( 'NONE', *, *, #24584, .F. ) ;
#31389=VERTEX_POINT ( 'NONE', #12888 ) ;
#31390=ORIENTED_EDGE ( 'NONE', *, *, #14027, .T. ) ;
#31391=CARTESIAN_POINT ( 'NONE',  ( -1.985260859929298016, 3.267716535433071279, -0.7037298423582233342 ) ) ;
#31392=ADVANCED_FACE ( 'NONE', ( #8750 ), #32780, .F. ) ;
#31393=AXIS2_PLACEMENT_3D ( 'NONE', #13320, #33720, #45044 ) ;
#31396=ORIENTED_EDGE ( 'NONE', *, *, #3340, .F. ) ;
#31400=PLANE ( 'NONE',  #25430 ) ;
#31404=LINE ( 'NONE', #27514, #21480 ) ;
#31405=CARTESIAN_POINT ( 'NONE',  ( -0.6214413264104945434, 3.346456692913386100, 0.1574803149606285035 ) ) ;
#31407=VERTEX_POINT ( 'NONE', #16763 ) ;
#31408=CARTESIAN_POINT ( 'NONE',  ( 1.363819533518803251, 3.267716535433071279, -0.1574803149606304187 ) ) ;
#31409=CARTESIAN_POINT ( 'NONE',  ( 2.361042194882304379, 3.267716535433071279, 0.6299212598425161236 ) ) ;
#31410=PLANE ( 'NONE',  #30619 ) ;
#31414=VERTEX_POINT ( 'NONE', #24507 ) ;
#31415=DIRECTION ( 'NONE',  ( 1.734723475976806848E-16, 0.000000000000000000, 1.000000000000000000 ) ) ;
#31416=ADVANCED_FACE ( 'NONE', ( #5135 ), #41026, .F. ) ;
#31417=DIRECTION ( 'NONE',  ( 1.000000000000000000, 0.000000000000000000, 0.000000000000000000 ) ) ;
#31420=ORIENTED_EDGE ( 'NONE', *, *, #22288, .T. ) ;
#31421=CARTESIAN_POINT ( 'NONE',  ( 1.139183960333101098, 3.346456692913386100, -1.771653543307081691 ) ) ;
#31423=CARTESIAN_POINT ( 'NONE',  ( -1.091055626815042645, 0.000000000000000000, -0.3149606299212593941 ) ) ;
#31424=CIRCLE ( 'NONE', #1724, 2.165354330708661568 ) ;
#31425=VECTOR ( 'NONE', #14115, 39.37007874015748143 ) ;
#31429=EDGE_LOOP ( 'NONE', ( #35099, #28590, #41491, #3932 ) ) ;
#31430=EDGE_CURVE ( 'NONE', #50129, #4115, #24761, .T. ) ;
#31434=EDGE_LOOP ( 'NONE', ( #27675, #18629, #43468, #19815 ) ) ;
#31435=EDGE_CURVE ( 'NONE', #29680, #2567, #48461, .T. ) ;
#31436=CARTESIAN_POINT ( 'NONE',  ( 0.000000000000000000, 3.267716535433071279, -0.3543307086614175816 ) ) ;
#31438=CARTESIAN_POINT ( 'NONE',  ( 0.5455278134075208785, 0.000000000000000000, -1.889763779527552812 ) ) ;
#31439=VERTEX_POINT ( 'NONE', #9522 ) ;
#31440=EDGE_CURVE ( 'NONE', #12590, #19157, #29393, .T. ) ;
#31441=PLANE ( 'NONE',  #47829 ) ;
#31443=EDGE_LOOP ( 'NONE', ( #21306, #40337, #4130, #7762 ) ) ;
#31444=CARTESIAN_POINT ( 'NONE',  ( 0.000000000000000000, 3.267716535433071279, 0.2755905511810995412 ) ) ;
#31447=EDGE_LOOP ( 'NONE', ( #8844, #12521, #29174, #33075 ) ) ;
#31449=LINE ( 'NONE', #47145, #4275 ) ;
#31450=ORIENTED_EDGE ( 'NONE', *, *, #36085, .T. ) ;
#31452=CARTESIAN_POINT ( 'NONE',  ( 1.636583440222563857, 0.000000000000000000, 0.3149606299212576177 ) ) ;
#31453=ORIENTED_EDGE ( 'NONE', *, *, #17998, .T. ) ;
#31454=ORIENTED_EDGE ( 'NONE', *, *, #43889, .T. ) ;
#31456=CARTESIAN_POINT ( 'NONE',  ( 1.909347346926324684, 3.346456692913386100, -0.03937007874015936021 ) ) ;
#31458=VERTEX_POINT ( 'NONE', #36126 ) ;
#31459=CARTESIAN_POINT ( 'NONE',  ( -0.07591351300297327631, 3.267716535433071279, 2.633779063002566366E-17 ) ) ;
#31461=CARTESIAN_POINT ( 'NONE',  ( 1.091055626815042423, 3.346456692913386100, -1.259842519685035134 ) ) ;
#31462=AXIS2_PLACEMENT_3D ( 'NONE', #16436, #2218, #22095 ) ;
#31463=CARTESIAN_POINT ( 'NONE',  ( 1.560669927219590525, 3.267716535433071279, 0.9055118110236164419 ) ) ;
#31465=FACE_OUTER_BOUND ( 'NONE', #7009, .T. ) ;
#31466=EDGE_LOOP ( 'NONE', ( #23327, #13172, #37109, #2055 ) ) ;
#31467=ORIENTED_EDGE ( 'NONE', *, *, #34303, .T. ) ;
#31470=LINE ( 'NONE', #11088, #46848 ) ;
#31471=LINE ( 'NONE', #11839, #32413 ) ;
#31472=VECTOR ( 'NONE', #6690, 39.37007874015748143 ) ;
#31473=DIRECTION ( 'NONE',  ( 1.734723475976806848E-16, -0.000000000000000000, 1.000000000000000000 ) ) ;
#31474=PLANE ( 'NONE',  #4183 ) ;
#31475=AXIS2_PLACEMENT_3D ( 'NONE', #2913, #2409, #34661 ) ;
#31476=CARTESIAN_POINT ( 'NONE',  ( -0.07591351300297363713, 3.267716535433071279, -2.164023224473873963 ) ) ;
#31478=ADVANCED_FACE ( 'NONE', ( #755 ), #32256, .F. ) ;
#31479=DIRECTION ( 'NONE',  ( -3.469446951953613696E-16, 0.000000000000000000, -1.000000000000000000 ) ) ;
#31481=CARTESIAN_POINT ( 'NONE',  ( 0.000000000000000000, 3.346456692913386100, 0.000000000000000000 ) ) ;
#31482=ORIENTED_EDGE ( 'NONE', *, *, #5250, .F. ) ;
#31483=CARTESIAN_POINT ( 'NONE',  ( -1.091055626815042201, 3.267716535433071279, 0.9448818897637749625 ) ) ;
#31484=FACE_OUTER_BOUND ( 'NONE', #38989, .T. ) ;
#31486=EDGE_LOOP ( 'NONE', ( #48046, #20479, #10373, #5729 ) ) ;
#31487=EDGE_CURVE ( 'NONE', #37100, #2160, #41779, .T. ) ;
#31489=CARTESIAN_POINT ( 'NONE',  ( 0.2727639067037609943, 3.267716535433071279, 2.165354330708650910 ) ) ;
#31493=CARTESIAN_POINT ( 'NONE',  ( 1.363819533518803251, 0.000000000000000000, 0.7874015748031454320 ) ) ;
#31494=DIRECTION ( 'NONE',  ( -3.469446951953613696E-16, 0.000000000000000000, -1.000000000000000000 ) ) ;
#31496=ORIENTED_EDGE ( 'NONE', *, *, #16667, .F. ) ;
#31502=VECTOR ( 'NONE', #30318, 39.37007874015748143 ) ;
#31503=CARTESIAN_POINT ( 'NONE',  ( 1.091055626815042645, 3.346456692913386100, -1.141732283464564013 ) ) ;
#31504=LINE ( 'NONE', #30497, #48236 ) ;
#31505=EDGE_CURVE ( 'NONE', #29688, #27355, #45618, .T. ) ;
#31506=VECTOR ( 'NONE', #42777, 39.37007874015748143 ) ;
#31507=ORIENTED_EDGE ( 'NONE', *, *, #50492, .T. ) ;
#31508=EDGE_CURVE ( 'NONE', #48466, #28575, #18793, .T. ) ;
#31512=ADVANCED_FACE ( 'NONE', ( #25773 ), #14411, .F. ) ;
#31513=DIRECTION ( 'NONE',  ( 0.000000000000000000, -1.000000000000000000, 0.000000000000000000 ) ) ;
#31514=EDGE_CURVE ( 'NONE', #14497, #850, #37666, .T. ) ;
#31516=ADVANCED_FACE ( 'NONE', ( #2284 ), #49983, .F. ) ;
#31517=ORIENTED_EDGE ( 'NONE', *, *, #20694, .T. ) ;
#31518=VERTEX_POINT ( 'NONE', #45875 ) ;
#31522=LINE ( 'NONE', #27374, #43948 ) ;
#31523=LINE ( 'NONE', #27129, #34393 ) ;
#31524=LINE ( 'NONE', #50083, #21411 ) ;
#31525=ORIENTED_EDGE ( 'NONE', *, *, #6771, .F. ) ;
#31526=ORIENTED_EDGE ( 'NONE', *, *, #31732, .T. ) ;
#31527=FACE_OUTER_BOUND ( 'NONE', #18024, .T. ) ;
#31528=LINE ( 'NONE', #46481, #35011 ) ;
#31529=ORIENTED_EDGE ( 'NONE', *, *, #41261, .T. ) ;
#31530=CARTESIAN_POINT ( 'NONE',  ( 0.1968503937007873850, 0.000000000000000000, -0.1968503937007874405 ) ) ;
#31532=AXIS2_PLACEMENT_3D ( 'NONE', #46219, #10878, #42362 ) ;
#31534=CARTESIAN_POINT ( 'NONE',  ( -0.3486774197067347147, 3.267716535433071279, 1.209717811016581790E-16 ) ) ;
#31535=VECTOR ( 'NONE', #29615, 39.37007874015748143 ) ;
#31538=CARTESIAN_POINT ( 'NONE',  ( -0.2727639067037607723, 3.346456692913386100, -1.102362204724405714 ) ) ;
#31539=DIRECTION ( 'NONE',  ( 1.000000000000000000, 0.000000000000000000, 0.000000000000000000 ) ) ;
#31540=VECTOR ( 'NONE', #2122, 39.37007874015748143 ) ;
#31542=VECTOR ( 'NONE', #23265, 39.37007874015748143 ) ;
#31543=ORIENTED_EDGE ( 'NONE', *, *, #26216, .T. ) ;
#31544=VECTOR ( 'NONE', #17569, 39.37007874015748143 ) ;
#31546=LINE ( 'NONE', #4428, #9688 ) ;
#31548=ORIENTED_EDGE ( 'NONE', *, *, #48938, .F. ) ;
#31549=ADVANCED_FACE ( 'NONE', ( #42276 ), #2031, .F. ) ;
#31551=ORIENTED_EDGE ( 'NONE', *, *, #37671, .T. ) ;
#31553=EDGE_LOOP ( 'NONE', ( #6383, #11808, #32738, #18342 ) ) ;
#31554=CARTESIAN_POINT ( 'NONE',  ( 1.015142113812069313, 0.000000000000000000, -1.102362204724405714 ) ) ;
#31556=ORIENTED_EDGE ( 'NONE', *, *, #3887, .T. ) ;
#31559=CARTESIAN_POINT ( 'NONE',  ( 1.953585199828835828, 3.267716535433071279, 0.7874015748031456541 ) ) ;
#31560=ORIENTED_EDGE ( 'NONE', *, *, #14546, .F. ) ;
#31563=LINE ( 'NONE', #35949, #33188 ) ;
#31564=DIRECTION ( 'NONE',  ( -0.000000000000000000, 1.000000000000000000, -0.000000000000000000 ) ) ;
#31565=VERTEX_POINT ( 'NONE', #14155 ) ;
#31566=ORIENTED_EDGE ( 'NONE', *, *, #295, .F. ) ;
#31567=CARTESIAN_POINT ( 'NONE',  ( 0.000000000000000000, 3.267716535433071279, 0.000000000000000000 ) ) ;
#31569=DIRECTION ( 'NONE',  ( 1.734723475976806848E-16, -0.000000000000000000, 1.000000000000000000 ) ) ;
#31570=ORIENTED_EDGE ( 'NONE', *, *, #16352, .T. ) ;
#31571=EDGE_LOOP ( 'NONE', ( #27815, #13518, #37454, #12315 ) ) ;
#31573=CARTESIAN_POINT ( 'NONE',  ( -1.636583440222564301, 3.346456692913386100, -0.3149606299212592275 ) ) ;
#31575=LINE ( 'NONE', #32097, #26987 ) ;
#31579=CARTESIAN_POINT ( 'NONE',  ( -1.091055626815042645, 3.232777166330607521, 2.204724409448808764 ) ) ;
#31580=ORIENTED_EDGE ( 'NONE', *, *, #36162, .F. ) ;
#31581=EDGE_CURVE ( 'NONE', #18573, #12446, #22165, .T. ) ;
#31582=FACE_OUTER_BOUND ( 'NONE', #17460, .T. ) ;
#31583=EDGE_LOOP ( 'NONE', ( #18513, #30721, #20048 ) ) ;
#31584=ORIENTED_EDGE ( 'NONE', *, *, #11557, .T. ) ;
#31585=CARTESIAN_POINT ( 'NONE',  ( 0.000000000000000000, 3.267716535433071279, -1.771653543307081025 ) ) ;
#31587=VECTOR ( 'NONE', #47729, 39.37007874015748143 ) ;
#31588=VECTOR ( 'NONE', #29701, 39.37007874015748143 ) ;
#31591=LINE ( 'NONE', #43951, #18731 ) ;
#31593=ORIENTED_EDGE ( 'NONE', *, *, #1893, .F. ) ;
#31594=ORIENTED_EDGE ( 'NONE', *, *, #4703, .F. ) ;
#31599=DIRECTION ( 'NONE',  ( -0.000000000000000000, 0.000000000000000000, 1.000000000000000000 ) ) ;
#31600=CARTESIAN_POINT ( 'NONE',  ( 2.378961647330872786, 3.346456692913386100, -0.3149606299212596716 ) ) ;
#31601=ORIENTED_EDGE ( 'NONE', *, *, #13043, .T. ) ;
#31602=CARTESIAN_POINT ( 'NONE',  ( 0.000000000000000000, 3.267716535433071279, 0.000000000000000000 ) ) ;
#31603=DIRECTION ( 'NONE',  ( 1.000000000000000000, -0.000000000000000000, 0.000000000000000000 ) ) ;
#31604=ORIENTED_EDGE ( 'NONE', *, *, #47852, .F. ) ;
#31605=DIRECTION ( 'NONE',  ( -1.000000000000000000, 0.000000000000000000, 0.000000000000000000 ) ) ;
#31608=VERTEX_POINT ( 'NONE', #38419 ) ;
#31609=LINE ( 'NONE', #16379, #22639 ) ;
#31610=CARTESIAN_POINT ( 'NONE',  ( 1.091055626815042423, 0.000000000000000000, -1.889763779527552368 ) ) ;
#31611=DIRECTION ( 'NONE',  ( 0.000000000000000000, -1.000000000000000000, 0.000000000000000000 ) ) ;
#31613=EDGE_CURVE ( 'NONE', #3678, #14290, #16191, .T. ) ;
#31614=VERTEX_POINT ( 'NONE', #27793 ) ;
#31615=VECTOR ( 'NONE', #1708, 39.37007874015748143 ) ;
#31616=FACE_OUTER_BOUND ( 'NONE', #28006, .T. ) ;
#31617=ORIENTED_EDGE ( 'NONE', *, *, #38433, .T. ) ;
#31618=LINE ( 'NONE', #47320, #8908 ) ;
#31619=ADVANCED_FACE ( 'NONE', ( #7174 ), #35553, .F. ) ;
#31620=AXIS2_PLACEMENT_3D ( 'NONE', #46167, #7214, #31211 ) ;
#31621=AXIS2_PLACEMENT_3D ( 'NONE', #43703, #8358, #38898 ) ;
#31623=FACE_OUTER_BOUND ( 'NONE', #27561, .T. ) ;
#31624=CARTESIAN_POINT ( 'NONE',  ( -2.454875160333845674, 3.346456692913386100, 0.1574803149606286423 ) ) ;
#31626=EDGE_LOOP ( 'NONE', ( #38979, #32971, #41622, #7317 ) ) ;
#31628=AXIS2_PLACEMENT_3D ( 'NONE', #50161, #50406, #23091 ) ;
#31629=CARTESIAN_POINT ( 'NONE',  ( 2.106197740627111514, 3.346456692913386100, -0.7874015748031473194 ) ) ;
#31630=ORIENTED_EDGE ( 'NONE', *, *, #24815, .T. ) ;
#31631=CARTESIAN_POINT ( 'NONE',  ( 0.2727639067037604947, 3.267716535433071279, -0.1574803149606298636 ) ) ;
#31633=CARTESIAN_POINT ( 'NONE',  ( -1.091055626815042645, 0.000000000000000000, -2.086614173228339641 ) ) ;
#31634=LINE ( 'NONE', #27746, #14931 ) ;
#31635=EDGE_LOOP ( 'NONE', ( #27309, #41347, #29839, #40502 ) ) ;
#31638=ORIENTED_EDGE ( 'NONE', *, *, #24447, .F. ) ;
#31639=CARTESIAN_POINT ( 'NONE',  ( -0.3486774197067339376, 3.346456692913386100, -0.9448818897637762948 ) ) ;
#31640=DIRECTION ( 'NONE',  ( -1.000000000000000000, 0.000000000000000000, 1.734723475976806848E-16 ) ) ;
#31641=LINE ( 'NONE', #47340, #17465 ) ;
#31642=ORIENTED_EDGE ( 'NONE', *, *, #31225, .T. ) ;
#31644=LINE ( 'NONE', #11762, #9252 ) ;
#31645=ORIENTED_EDGE ( 'NONE', *, *, #16214, .T. ) ;
#31646=VERTEX_POINT ( 'NONE', #43283 ) ;
#31649=ORIENTED_EDGE ( 'NONE', *, *, #38723, .F. ) ;
#31651=ORIENTED_EDGE ( 'NONE', *, *, #17402, .T. ) ;
#31654=AXIS2_PLACEMENT_3D ( 'NONE', #495, #3608, #50535 ) ;
#31655=PLANE ( 'NONE',  #38633 ) ;
#31657=CARTESIAN_POINT ( 'NONE',  ( -0.2727639067037608278, 3.267716535433071279, -0.6692913385826758654 ) ) ;
#31659=VECTOR ( 'NONE', #26653, 39.37007874015748143 ) ;
#31661=VECTOR ( 'NONE', #2342, 39.37007874015748143 ) ;
#31662=LINE ( 'NONE', #16429, #1691 ) ;
#31663=CARTESIAN_POINT ( 'NONE',  ( 1.091055626815042645, 0.000000000000000000, 0.7480314960629872445 ) ) ;
#31666=ORIENTED_EDGE ( 'NONE', *, *, #2496, .F. ) ;
#31669=CARTESIAN_POINT ( 'NONE',  ( 1.287906020515829919, 3.267716535433071279, -1.574803149606294417 ) ) ;
#31670=VERTEX_POINT ( 'NONE', #20042 ) ;
#31671=DIRECTION ( 'NONE',  ( -0.000000000000000000, 1.000000000000000000, -0.000000000000000000 ) ) ;
#31672=DIRECTION ( 'NONE',  ( -3.469446951953613696E-16, 0.000000000000000000, -1.000000000000000000 ) ) ;
#31673=EDGE_LOOP ( 'NONE', ( #45633, #6804, #35137, #4145 ) ) ;
#31675=DIRECTION ( 'NONE',  ( 1.000000000000000000, 0.000000000000000000, 0.000000000000000000 ) ) ;
#31676=DIRECTION ( 'NONE',  ( 0.000000000000000000, -1.000000000000000000, 0.000000000000000000 ) ) ;
#31678=ORIENTED_EDGE ( 'NONE', *, *, #3000, .T. ) ;
#31680=EDGE_CURVE ( 'NONE', #40996, #7498, #15925, .T. ) ;
#31682=DIRECTION ( 'NONE',  ( -0.000000000000000000, 1.000000000000000000, -0.000000000000000000 ) ) ;
#31683=DIRECTION ( 'NONE',  ( -1.000000000000000000, 0.000000000000000000, 1.734723475976806848E-16 ) ) ;
#31687=ORIENTED_EDGE ( 'NONE', *, *, #24911, .F. ) ;
#31688=ORIENTED_EDGE ( 'NONE', *, *, #27685, .T. ) ;
#31689=VECTOR ( 'NONE', #11471, 39.37007874015748143 ) ;
#31691=ORIENTED_EDGE ( 'NONE', *, *, #26473, .F. ) ;
#31698=CARTESIAN_POINT ( 'NONE',  ( -0.8182917201112819283, 0.000000000000000000, -1.417322834645664331 ) ) ;
#31699=EDGE_CURVE ( 'NONE', #24770, #22865, #11796, .T. ) ;
#31702=CARTESIAN_POINT ( 'NONE',  ( 1.015142113812069313, 3.346456692913386100, -0.4724409448818889246 ) ) ;
#31703=CIRCLE ( 'NONE', #30896, 2.106299212598425008 ) ;
#31704=VERTEX_POINT ( 'NONE', #19033 ) ;
#31707=ORIENTED_EDGE ( 'NONE', *, *, #46492, .F. ) ;
#31711=ORIENTED_EDGE ( 'NONE', *, *, #8204, .T. ) ;
#31712=ORIENTED_EDGE ( 'NONE', *, *, #6132, .F. ) ;
#31713=LINE ( 'NONE', #2457, #50341 ) ;
#31714=CARTESIAN_POINT ( 'NONE',  ( 4.268512490100411402E-16, 3.267716535433071279, 1.574803149606291974 ) ) ;
#31719=DIRECTION ( 'NONE',  ( 1.734723475976806848E-16, -0.000000000000000000, 1.000000000000000000 ) ) ;
#31721=LINE ( 'NONE', #44088, #9091 ) ;
#31723=ORIENTED_EDGE ( 'NONE', *, *, #20331, .T. ) ;
#31724=CARTESIAN_POINT ( 'NONE',  ( -0.5455278134075208785, 3.267716535433071279, 0.7480314960629874665 ) ) ;
#31725=DIRECTION ( 'NONE',  ( -3.469446951953613696E-16, 0.000000000000000000, -1.000000000000000000 ) ) ;
#31728=EDGE_CURVE ( 'NONE', #2530, #17636, #31175, .T. ) ;
#31729=VECTOR ( 'NONE', #24031, 39.37007874015748143 ) ;
#31730=CARTESIAN_POINT ( 'NONE',  ( 0.2727639067037604947, 0.000000000000000000, -1.417322834645664331 ) ) ;
#31731=VECTOR ( 'NONE', #10159, 39.37007874015748143 ) ;
#31732=EDGE_CURVE ( 'NONE', #26914, #38732, #46630, .T. ) ;
#31734=DIRECTION ( 'NONE',  ( -3.469446951953613696E-16, 0.000000000000000000, -1.000000000000000000 ) ) ;
#31735=ORIENTED_EDGE ( 'NONE', *, *, #19596, .T. ) ;
#31736=CARTESIAN_POINT ( 'NONE',  ( -0.2727639067037605503, 3.267716535433071279, 4.731699523581609125E-17 ) ) ;
#31739=ORIENTED_EDGE ( 'NONE', *, *, #31508, .T. ) ;
#31740=LINE ( 'NONE', #47437, #11899 ) ;
#31741=EDGE_LOOP ( 'NONE', ( #14391, #22528, #32066, #26320 ) ) ;
#31742=EDGE_CURVE ( 'NONE', #44911, #18980, #23670, .T. ) ;
#31744=DIRECTION ( 'NONE',  ( -0.000000000000000000, 1.000000000000000000, -0.000000000000000000 ) ) ;
#31746=EDGE_LOOP ( 'NONE', ( #37980, #9531, #8142, #17429 ) ) ;
#31748=ADVANCED_FACE ( 'NONE', ( #35302 ), #50983, .F. ) ;
#31751=ORIENTED_EDGE ( 'NONE', *, *, #17818, .T. ) ;
#31752=DIRECTION ( 'NONE',  ( 0.000000000000000000, 0.000000000000000000, 1.000000000000000000 ) ) ;
#31753=ORIENTED_EDGE ( 'NONE', *, *, #19497, .T. ) ;
#31754=LINE ( 'NONE', #31248, #44978 ) ;
#31755=LINE ( 'NONE', #40008, #9927 ) ;
#31759=ORIENTED_EDGE ( 'NONE', *, *, #1440, .F. ) ;
#31761=AXIS2_PLACEMENT_3D ( 'NONE', #6499, #50066, #3626 ) ;
#31764=CARTESIAN_POINT ( 'NONE',  ( -0.5455278134075214336, 0.000000000000000000, -0.1968503937007883287 ) ) ;
#31766=VECTOR ( 'NONE', #49299, 39.37007874015748143 ) ;
#31767=VERTEX_POINT ( 'NONE', #16709 ) ;
#31768=FACE_OUTER_BOUND ( 'NONE', #14344, .T. ) ;
#31770=ADVANCED_FACE ( 'NONE', ( #4830 ), #1714, .F. ) ;
#31771=ORIENTED_EDGE ( 'NONE', *, *, #47549, .T. ) ;
#31773=VECTOR ( 'NONE', #42725, 39.37007874015748143 ) ;
#31775=VERTEX_POINT ( 'NONE', #48155 ) ;
#31777=EDGE_CURVE ( 'NONE', #12815, #28950, #949, .T. ) ;
#31778=ORIENTED_EDGE ( 'NONE', *, *, #13202, .T. ) ;
#31780=FACE_OUTER_BOUND ( 'NONE', #5103, .T. ) ;
#31781=ADVANCED_FACE ( 'NONE', ( #48402 ), #40461, .F. ) ;
#31782=EDGE_CURVE ( 'NONE', #49534, #216, #21342, .T. ) ;
#31783=DIRECTION ( 'NONE',  ( 0.000000000000000000, 0.000000000000000000, -1.000000000000000000 ) ) ;
#31784=DIRECTION ( 'NONE',  ( -0.000000000000000000, 1.000000000000000000, -0.000000000000000000 ) ) ;
#31785=ORIENTED_EDGE ( 'NONE', *, *, #9125, .F. ) ;
#31788=LINE ( 'NONE', #23020, #4533 ) ;
#31789=EDGE_LOOP ( 'NONE', ( #45860, #22435, #34857, #41679 ) ) ;
#31790=DIRECTION ( 'NONE',  ( 1.000000000000000000, 0.000000000000000000, 0.000000000000000000 ) ) ;
#31793=LINE ( 'NONE', #43899, #14300 ) ;
#31795=DIRECTION ( 'NONE',  ( -0.000000000000000000, 1.000000000000000000, -0.000000000000000000 ) ) ;
#31796=VERTEX_POINT ( 'NONE', #44814 ) ;
#31797=LINE ( 'NONE', #4169, #20939 ) ;
#31798=LINE ( 'NONE', #4938, #34317 ) ;
#31799=VECTOR ( 'NONE', #9460, 39.37007874015748143 ) ;
#31800=VERTEX_POINT ( 'NONE', #5333 ) ;
#31801=VECTOR ( 'NONE', #14362, 39.37007874015748143 ) ;
#31802=ADVANCED_FACE ( 'NONE', ( #20575 ), #28566, .F. ) ;
#31805=FACE_OUTER_BOUND ( 'NONE', #37117, .T. ) ;
#31806=FACE_OUTER_BOUND ( 'NONE', #2493, .T. ) ;
#31808=ORIENTED_EDGE ( 'NONE', *, *, #24627, .F. ) ;
#31809=ADVANCED_FACE ( 'NONE', ( #13340 ), #32980, .F. ) ;
#31811=AXIS2_PLACEMENT_3D ( 'NONE', #46757, #46264, #42905 ) ;
#31812=EDGE_CURVE ( 'NONE', #33606, #37376, #48656, .T. ) ;
#31813=ORIENTED_EDGE ( 'NONE', *, *, #5243, .T. ) ;
#31814=DIRECTION ( 'NONE',  ( 1.000000000000000000, 0.000000000000000000, -3.469446951953613696E-16 ) ) ;
#31816=ORIENTED_EDGE ( 'NONE', *, *, #30175, .F. ) ;
#31819=DIRECTION ( 'NONE',  ( -1.000000000000000000, 0.000000000000000000, -0.000000000000000000 ) ) ;
#31820=LINE ( 'NONE', #32332, #4129 ) ;
#31821=PLANE ( 'NONE',  #27659 ) ;
#31822=ORIENTED_EDGE ( 'NONE', *, *, #49246, .F. ) ;
#31823=ORIENTED_EDGE ( 'NONE', *, *, #22853, .T. ) ;
#31825=PLANE ( 'NONE',  #43832 ) ;
#31831=DIRECTION ( 'NONE',  ( 1.734723475976806848E-16, 0.000000000000000000, 1.000000000000000000 ) ) ;
#31832=ORIENTED_EDGE ( 'NONE', *, *, #27616, .F. ) ;
#31833=ORIENTED_EDGE ( 'NONE', *, *, #27994, .F. ) ;
#31834=DIRECTION ( 'NONE',  ( 0.000000000000000000, 0.000000000000000000, -1.000000000000000000 ) ) ;
#31835=CARTESIAN_POINT ( 'NONE',  ( -1.091055626815042645, 3.346456692913386100, -1.456692913385822186 ) ) ;
#31837=VECTOR ( 'NONE', #39597, 39.37007874015748143 ) ;
#31838=VERTEX_POINT ( 'NONE', #29074 ) ;
#31840=LINE ( 'NONE', #23313, #4643 ) ;
#31843=VECTOR ( 'NONE', #42247, 39.37007874015748143 ) ;
#31844=DIRECTION ( 'NONE',  ( -0.000000000000000000, 1.000000000000000000, -0.000000000000000000 ) ) ;
#31845=ORIENTED_EDGE ( 'NONE', *, *, #41324, .T. ) ;
#31846=ORIENTED_EDGE ( 'NONE', *, *, #42791, .T. ) ;
#31849=AXIS2_PLACEMENT_3D ( 'NONE', #48796, #13477, #28956 ) ;
#31853=PLANE ( 'NONE',  #17074 ) ;
#31854=CARTESIAN_POINT ( 'NONE',  ( 0.5455278134075208785, 3.346456692913386100, -2.086614173228340086 ) ) ;
#31856=ORIENTED_EDGE ( 'NONE', *, *, #8465, .F. ) ;
#31858=VECTOR ( 'NONE', #19993, 39.37007874015748143 ) ;
#31860=FACE_OUTER_BOUND ( 'NONE', #27563, .T. ) ;
#31861=CARTESIAN_POINT ( 'NONE',  ( -1.439733046521776361, 0.000000000000000000, 0.7480314960629874665 ) ) ;
#31864=DIRECTION ( 'NONE',  ( -3.469446951953613696E-16, 0.000000000000000000, -1.000000000000000000 ) ) ;
#31866=LINE ( 'NONE', #19715, #33303 ) ;
#31867=EDGE_CURVE ( 'NONE', #18498, #49569, #40970, .T. ) ;
#31869=VERTEX_POINT ( 'NONE', #44051 ) ;
#31872=LINE ( 'NONE', #43715, #45918 ) ;
#31873=CARTESIAN_POINT ( 'NONE',  ( 0.2727639067037604392, 3.346456692913386100, -1.614173228346451605 ) ) ;
#31875=AXIS2_PLACEMENT_3D ( 'NONE', #45609, #22156, #18272 ) ;
#31878=EDGE_CURVE ( 'NONE', #2160, #12958, #49924, .T. ) ;
#31879=DIRECTION ( 'NONE',  ( 1.734723475976806848E-16, 0.000000000000000000, 1.000000000000000000 ) ) ;
#31881=AXIS2_PLACEMENT_3D ( 'NONE', #87, #23844, #43193 ) ;
#31882=EDGE_CURVE ( 'NONE', #22897, #37873, #26227, .T. ) ;
#31883=ORIENTED_EDGE ( 'NONE', *, *, #35558, .T. ) ;
#31884=FACE_BOUND ( 'NONE', #41550, .T. ) ;
#31886=ORIENTED_EDGE ( 'NONE', *, *, #6096, .F. ) ;
#31889=DIRECTION ( 'NONE',  ( 1.000000000000000000, 0.000000000000000000, -3.469446951953613696E-16 ) ) ;
#31890=DIRECTION ( 'NONE',  ( -3.469446951953613696E-16, 0.000000000000000000, -1.000000000000000000 ) ) ;
#31891=CARTESIAN_POINT ( 'NONE',  ( -0.07591351300297333182, 0.000000000000000000, -1.417322834645664331 ) ) ;
#31892=AXIS2_PLACEMENT_3D ( 'NONE', #42034, #17780, #46381 ) ;
#31893=AXIS2_PLACEMENT_3D ( 'NONE', #32344, #9090, #27938 ) ;
#31894=ORIENTED_EDGE ( 'NONE', *, *, #24549, .T. ) ;
#31895=ORIENTED_EDGE ( 'NONE', *, *, #42839, .T. ) ;
#31896=CARTESIAN_POINT ( 'NONE',  ( 1.443330927545150910, 3.267716535433071279, -1.614173228346452715 ) ) ;
#31897=CARTESIAN_POINT ( 'NONE',  ( -1.636583440222564301, 0.000000000000000000, -1.141732283464563791 ) ) ;
#31898=VERTEX_POINT ( 'NONE', #6615 ) ;
#31899=DIRECTION ( 'NONE',  ( 1.734723475976806848E-16, -0.000000000000000000, 1.000000000000000000 ) ) ;
#31900=DIRECTION ( 'NONE',  ( 1.734723475976806848E-16, -0.000000000000000000, 1.000000000000000000 ) ) ;
#31901=DIRECTION ( 'NONE',  ( -0.000000000000000000, 1.000000000000000000, -0.000000000000000000 ) ) ;
#31902=CARTESIAN_POINT ( 'NONE',  ( 1.560669927219590747, 3.267716535433071279, -5.414661521997677271E-16 ) ) ;
#31903=VERTEX_POINT ( 'NONE', #17972 ) ;
#31904=ORIENTED_EDGE ( 'NONE', *, *, #3295, .F. ) ;
#31905=CARTESIAN_POINT ( 'NONE',  ( -0.5455278134075214336, 3.346456692913386100, -0.6299212598425175669 ) ) ;
#31906=CARTESIAN_POINT ( 'NONE',  ( 0.000000000000000000, 3.267716535433071279, -0.7874015748031473194 ) ) ;
#31908=CARTESIAN_POINT ( 'NONE',  ( 1.015142113812069979, 3.346456692913386100, 1.732283464566921172 ) ) ;
#31909=FACE_BOUND ( 'NONE', #26539, .T. ) ;
#31912=ORIENTED_EDGE ( 'NONE', *, *, #12254, .T. ) ;
#31914=PLANE ( 'NONE',  #35779 ) ;
#31915=AXIS2_PLACEMENT_3D ( 'NONE', #30785, #2914, #3161 ) ;
#31916=EDGE_LOOP ( 'NONE', ( #44948, #25428, #30026, #33917 ) ) ;
#31920=EDGE_CURVE ( 'NONE', #18819, #27935, #22107, .T. ) ;
#31922=EDGE_CURVE ( 'NONE', #46790, #5893, #45820, .T. ) ;
#31923=DIRECTION ( 'NONE',  ( -1.000000000000000000, 0.000000000000000000, 1.734723475976806848E-16 ) ) ;
#31924=PLANE ( 'NONE',  #5448 ) ;
#31927=VECTOR ( 'NONE', #42124, 39.37007874015748143 ) ;
#31928=FACE_OUTER_BOUND ( 'NONE', #39320, .T. ) ;
#31929=CARTESIAN_POINT ( 'NONE',  ( 0.1968503937007878568, 0.000000000000000000, 1.574803149606291974 ) ) ;
#31930=LINE ( 'NONE', #20809, #45130 ) ;
#31932=DIRECTION ( 'NONE',  ( 0.000000000000000000, 1.000000000000000000, 0.000000000000000000 ) ) ;
#31934=CARTESIAN_POINT ( 'NONE',  ( -0.8942052331142552601, 0.000000000000000000, -1.889763779527552146 ) ) ;
#31936=DIRECTION ( 'NONE',  ( -0.000000000000000000, 1.000000000000000000, -0.000000000000000000 ) ) ;
#31937=EDGE_CURVE ( 'NONE', #44082, #48833, #49424, .T. ) ;
#31939=ORIENTED_EDGE ( 'NONE', *, *, #29128, .F. ) ;
#31940=CARTESIAN_POINT ( 'NONE',  ( 1.091055626815043311, 0.000000000000000000, 1.889763779527550369 ) ) ;
#31941=PLANE ( 'NONE',  #6971 ) ;
#31942=CARTESIAN_POINT ( 'NONE',  ( 1.909347346926324684, 3.267716535433071279, -0.03937007874015936021 ) ) ;
#31943=EDGE_CURVE ( 'NONE', #39739, #45623, #1973, .T. ) ;
#31944=LINE ( 'NONE', #32459, #43026 ) ;
#31948=LINE ( 'NONE', #36586, #35015 ) ;
#31950=VECTOR ( 'NONE', #17361, 39.37007874015748143 ) ;
#31951=VECTOR ( 'NONE', #31296, 39.37007874015748143 ) ;
#31953=VERTEX_POINT ( 'NONE', #25974 ) ;
#31955=CARTESIAN_POINT ( 'NONE',  ( -0.2727639067037611609, 3.267716535433071279, 4.731699523581620218E-17 ) ) ;
#31956=EDGE_LOOP ( 'NONE', ( #9520, #7643, #12470, #8176 ) ) ;
#31959=ORIENTED_EDGE ( 'NONE', *, *, #18872, .F. ) ;
#31961=ORIENTED_EDGE ( 'NONE', *, *, #4999, .F. ) ;
#31962=DIRECTION ( 'NONE',  ( 0.000000000000000000, -1.000000000000000000, 0.000000000000000000 ) ) ;
#31963=LINE ( 'NONE', #24209, #32248 ) ;
#31965=DIRECTION ( 'NONE',  ( 0.000000000000000000, 0.000000000000000000, -1.000000000000000000 ) ) ;
#31967=AXIS2_PLACEMENT_3D ( 'NONE', #5062, #32962, #17704 ) ;
#31968=DIRECTION ( 'NONE',  ( 0.000000000000000000, 0.000000000000000000, 1.000000000000000000 ) ) ;
#31970=ORIENTED_EDGE ( 'NONE', *, *, #50176, .T. ) ;
#31971=DIRECTION ( 'NONE',  ( -1.000000000000000000, 0.000000000000000000, 0.000000000000000000 ) ) ;
#31972=B_SPLINE_CURVE_WITH_KNOTS ( 'NONE', 3,
 ( #3339, #14203, #25823, #21960 ),
 .UNSPECIFIED., .F., .F.,
 ( 4, 4 ),
 ( 0.02763470841684000437, 0.02815926868579550144 ),
 .UNSPECIFIED. ) ;
#31974=CARTESIAN_POINT ( 'NONE',  ( 0.4696143004045476577, 0.000000000000000000, -1.732283464566922726 ) ) ;
#31975=ORIENTED_EDGE ( 'NONE', *, *, #12544, .F. ) ;
#31976=LINE ( 'NONE', #40742, #15547 ) ;
#31977=ORIENTED_EDGE ( 'NONE', *, *, #13124, .T. ) ;
#31980=DIRECTION ( 'NONE',  ( -1.000000000000000000, 0.000000000000000000, 0.000000000000000000 ) ) ;
#31983=VECTOR ( 'NONE', #4884, 39.37007874015748143 ) ;
#31984=EDGE_CURVE ( 'NONE', #44346, #29618, #30102, .T. ) ;
#31985=CARTESIAN_POINT ( 'NONE',  ( 0.4696143004045478797, 0.000000000000000000, -0.6692913385826760875 ) ) ;
#31988=DIRECTION ( 'NONE',  ( -1.000000000000000000, -0.000000000000000000, -0.000000000000000000 ) ) ;
#31991=VECTOR ( 'NONE', #3631, 39.37007874015748143 ) ;
#31993=CARTESIAN_POINT ( 'NONE',  ( -0.8942052331142547050, 3.267716535433071279, 3.102397620449221495E-16 ) ) ;
#31996=ORIENTED_EDGE ( 'NONE', *, *, #45682, .F. ) ;
#31997=CARTESIAN_POINT ( 'NONE',  ( 0.1968503937007877735, 3.346456692913386100, 1.692913385826762873 ) ) ;
#31998=VERTEX_POINT ( 'NONE', #44974 ) ;
#31999=DIRECTION ( 'NONE',  ( -1.000000000000000000, 0.000000000000000000, 0.000000000000000000 ) ) ;
#32000=EDGE_CURVE ( 'NONE', #49676, #26927, #48819, .T. ) ;
#32001=VECTOR ( 'NONE', #46737, 39.37007874015748143 ) ;
#32002=ORIENTED_EDGE ( 'NONE', *, *, #27754, .T. ) ;
#32003=CARTESIAN_POINT ( 'NONE',  ( 0.4696143004045476577, 3.346456692913386100, -1.732283464566922726 ) ) ;
#32005=LINE ( 'NONE', #47697, #49780 ) ;
#32007=EDGE_CURVE ( 'NONE', #12716, #41514, #40617, .T. ) ;
#32008=DIRECTION ( 'NONE',  ( -3.469446951953613696E-16, 0.000000000000000000, -1.000000000000000000 ) ) ;
#32010=VERTEX_POINT ( 'NONE', #5239 ) ;
#32014=PLANE ( 'NONE',  #41724 ) ;
#32017=VECTOR ( 'NONE', #39432, 39.37007874015748143 ) ;
#32018=CARTESIAN_POINT ( 'NONE',  ( -0.5455278134075208785, 3.267716535433071279, 1.259842519685033357 ) ) ;
#32019=VERTEX_POINT ( 'NONE', #44716 ) ;
#32023=LINE ( 'NONE', #19613, #38845 ) ;
#32024=FACE_BOUND ( 'NONE', #8904, .T. ) ;
#32025=VECTOR ( 'NONE', #43304, 39.37007874015748143 ) ;
#32026=ADVANCED_FACE ( 'NONE', ( #28469 ), #41128, .F. ) ;
#32029=DIRECTION ( 'NONE',  ( -1.000000000000000000, 0.000000000000000000, -0.000000000000000000 ) ) ;
#32030=DIRECTION ( 'NONE',  ( -3.469446951953613696E-16, 0.000000000000000000, -1.000000000000000000 ) ) ;
#32032=VECTOR ( 'NONE', #32432, 39.37007874015748143 ) ;
#32033=CARTESIAN_POINT ( 'NONE',  ( 0.000000000000000000, 3.267716535433071279, 1.417322834645662777 ) ) ;
#32034=ORIENTED_EDGE ( 'NONE', *, *, #26222, .F. ) ;
#32038=EDGE_LOOP ( 'NONE', ( #26352, #29145, #41811, #14227 ) ) ;
#32039=CARTESIAN_POINT ( 'NONE',  ( 0.1968503937007874405, 3.346456692913386100, 0.000000000000000000 ) ) ;
#32042=CARTESIAN_POINT ( 'NONE',  ( -2.182111253630085290, 3.346456692913386100, -0.5118110236220464460 ) ) ;
#32044=DIRECTION ( 'NONE',  ( -0.000000000000000000, 1.000000000000000000, -0.000000000000000000 ) ) ;
#32045=VERTEX_POINT ( 'NONE', #4987 ) ;
#32046=ORIENTED_EDGE ( 'NONE', *, *, #39861, .T. ) ;
#32048=DIRECTION ( 'NONE',  ( -0.000000000000000000, -1.000000000000000000, -0.000000000000000000 ) ) ;
#32050=VERTEX_POINT ( 'NONE', #17375 ) ;
#32052=LINE ( 'NONE', #44415, #19004 ) ;
#32054=AXIS2_PLACEMENT_3D ( 'NONE', #43997, #36018, #642 ) ;
#32056=DIRECTION ( 'NONE',  ( -3.469446951953613696E-16, 0.000000000000000000, -1.000000000000000000 ) ) ;
#32057=ORIENTED_EDGE ( 'NONE', *, *, #45356, .T. ) ;
#32058=DIRECTION ( 'NONE',  ( 1.734723475976806848E-16, 0.000000000000000000, 1.000000000000000000 ) ) ;
#32059=DIRECTION ( 'NONE',  ( -0.000000000000000000, 1.000000000000000000, -0.000000000000000000 ) ) ;
#32063=CARTESIAN_POINT ( 'NONE',  ( 1.287906020515830363, 3.267716535433071279, -4.468321617281356063E-16 ) ) ;
#32065=DIRECTION ( 'NONE',  ( 0.000000000000000000, -1.000000000000000000, 0.000000000000000000 ) ) ;
#32066=ORIENTED_EDGE ( 'NONE', *, *, #33444, .F. ) ;
#32068=VECTOR ( 'NONE', #14517, 39.37007874015748143 ) ;
#32071=VERTEX_POINT ( 'NONE', #28979 ) ;
#32075=EDGE_LOOP ( 'NONE', ( #25555, #47035, #42654, #44409 ) ) ;
#32078=LINE ( 'NONE', #19916, #40879 ) ;
#32079=EDGE_CURVE ( 'NONE', #27812, #29397, #16613, .T. ) ;
#32080=ADVANCED_FACE ( 'NONE', ( #8604 ), #29502, .F. ) ;
#32081=ORIENTED_EDGE ( 'NONE', *, *, #23439, .T. ) ;
#32082=DIMENSIONAL_EXPONENTS ( 1.000000000000000000, 0.000000000000000000, 0.000000000000000000, 0.000000000000000000, 0.000000000000000000, 0.000000000000000000, 0.000000000000000000 ) ;
#32083=ORIENTED_EDGE ( 'NONE', *, *, #3269, .F. ) ;
#32084=ORIENTED_EDGE ( 'NONE', *, *, #27102, .F. ) ;
#32087=ORIENTED_EDGE ( 'NONE', *, *, #24167, .F. ) ;
#32088=EDGE_CURVE ( 'NONE', #12444, #8496, #4735, .T. ) ;
#32089=CARTESIAN_POINT ( 'NONE',  ( -0.3486774197067339376, 0.000000000000000000, -1.259842519685035134 ) ) ;
#32091=LINE ( 'NONE', #24590, #3025 ) ;
#32092=EDGE_CURVE ( 'NONE', #31670, #48175, #34170, .T. ) ;
#32093=ORIENTED_EDGE ( 'NONE', *, *, #46206, .F. ) ;
#32095=PLANE ( 'NONE',  #28286 ) ;
#32096=VECTOR ( 'NONE', #37230, 39.37007874015748143 ) ;
#32097=CARTESIAN_POINT ( 'NONE',  ( -1.439733046521776139, 3.346456692913386100, 0.9448818897637749625 ) ) ;
#32098=VERTEX_POINT ( 'NONE', #8861 ) ;
#32099=CARTESIAN_POINT ( 'NONE',  ( -0.2727639067037607723, 3.346456692913386100, -1.417322834645664331 ) ) ;
#32103=ORIENTED_EDGE ( 'NONE', *, *, #40056, .T. ) ;
#32104=DIRECTION ( 'NONE',  ( -1.000000000000000000, -0.000000000000000000, -0.000000000000000000 ) ) ;
#32107=VECTOR ( 'NONE', #3714, 39.37007874015748143 ) ;
#32108=CARTESIAN_POINT ( 'NONE',  ( -1.439733046521776583, 0.000000000000000000, -1.574803149606293307 ) ) ;
#32111=LINE ( 'NONE', #16092, #12304 ) ;
#32112=AXIS2_PLACEMENT_3D ( 'NONE', #21082, #40704, #36839 ) ;
#32114=EDGE_LOOP ( 'NONE', ( #39241, #48078, #1657, #39591 ) ) ;
#32117=ORIENTED_EDGE ( 'NONE', *, *, #16564, .F. ) ;
#32118=DIRECTION ( 'NONE',  ( 1.000000000000000000, 0.000000000000000000, -3.469446951953613696E-16 ) ) ;
#32120=CARTESIAN_POINT ( 'NONE',  ( 0.1968503937007869686, 3.346456692913386100, -2.086614173228339641 ) ) ;
#32122=CARTESIAN_POINT ( 'NONE',  ( 1.560669927219590303, 0.000000000000000000, -1.929133858267710666 ) ) ;
#32124=CARTESIAN_POINT ( 'NONE',  ( 0.2727639067037610499, 3.267716535433071279, 1.102362204724404160 ) ) ;
#32125=DIRECTION ( 'NONE',  ( 1.734723475976806848E-16, -0.000000000000000000, 1.000000000000000000 ) ) ;
#32126=ORIENTED_EDGE ( 'NONE', *, *, #48394, .F. ) ;
#32133=CARTESIAN_POINT ( 'NONE',  ( -0.8942052331142552601, 3.267716535433071279, -7.512581982576723358E-16 ) ) ;
#32134=LINE ( 'NONE', #36260, #30849 ) ;
#32135=ORIENTED_EDGE ( 'NONE', *, *, #35014, .T. ) ;
#32136=LINE ( 'NONE', #24638, #41183 ) ;
#32137=DIRECTION ( 'NONE',  ( 1.734723475976806848E-16, -0.000000000000000000, 1.000000000000000000 ) ) ;
#32138=ORIENTED_EDGE ( 'NONE', *, *, #39968, .F. ) ;
#32139=CARTESIAN_POINT ( 'NONE',  ( 0.2727639067037604392, 3.346456692913386100, 0.5905511811023579360 ) ) ;
#32141=CARTESIAN_POINT ( 'NONE',  ( 0.000000000000000000, 3.267716535433071279, 0.000000000000000000 ) ) ;
#32142=CARTESIAN_POINT ( 'NONE',  ( 0.2727639067037602172, 3.267716535433071279, -2.088563196121306476 ) ) ;
#32143=CARTESIAN_POINT ( 'NONE',  ( -1.091055626815042645, 3.346456692913386100, 2.204724409448808764 ) ) ;
#32144=EDGE_CURVE ( 'NONE', #37337, #4877, #25882, .T. ) ;
#32146=EDGE_CURVE ( 'NONE', #4115, #23868, #18895, .T. ) ;
#32147=VERTEX_POINT ( 'NONE', #3145 ) ;
#32148=ORIENTED_EDGE ( 'NONE', *, *, #9180, .T. ) ;
#32150=FACE_OUTER_BOUND ( 'NONE', #18663, .T. ) ;
#32151=ORIENTED_EDGE ( 'NONE', *, *, #26951, .F. ) ;
#32152=DIRECTION ( 'NONE',  ( -1.000000000000000000, -0.000000000000000000, -0.000000000000000000 ) ) ;
#32153=DIRECTION ( 'NONE',  ( 1.000000000000000000, 0.000000000000000000, -3.469446951953613696E-16 ) ) ;
#32154=VECTOR ( 'NONE', #10358, 39.37007874015748143 ) ;
#32156=DIRECTION ( 'NONE',  ( 0.000000000000000000, -1.000000000000000000, 0.000000000000000000 ) ) ;
#32157=ORIENTED_EDGE ( 'NONE', *, *, #29945, .T. ) ;
#32159=CARTESIAN_POINT ( 'NONE',  ( -1.091055626815042645, 0.000000000000000000, -1.259842519685034690 ) ) ;
#32161=LINE ( 'NONE', #18814, #23051 ) ;
#32162=PLANE ( 'NONE',  #47895 ) ;
#32163=FACE_BOUND ( 'NONE', #47772, .T. ) ;
#32164=ORIENTED_EDGE ( 'NONE', *, *, #15068, .F. ) ;
#32165=DIRECTION ( 'NONE',  ( -1.000000000000000000, 0.000000000000000000, 0.000000000000000000 ) ) ;
#32168=EDGE_CURVE ( 'NONE', #351, #44517, #25949, .T. ) ;
#32169=FACE_OUTER_BOUND ( 'NONE', #21052, .T. ) ;
#32171=VECTOR ( 'NONE', #44769, 39.37007874015748143 ) ;
#32172=VERTEX_POINT ( 'NONE', #49832 ) ;
#32173=ORIENTED_EDGE ( 'NONE', *, *, #24037, .T. ) ;
#32174=DIRECTION ( 'NONE',  ( -3.469446951953613696E-16, 0.000000000000000000, -1.000000000000000000 ) ) ;
#32175=EDGE_CURVE ( 'NONE', #39052, #23451, #10646, .T. ) ;
#32176=ORIENTED_EDGE ( 'NONE', *, *, #50307, .F. ) ;
#32177=EDGE_CURVE ( 'NONE', #38883, #49063, #38525, .T. ) ;
#32178=LINE ( 'NONE', #32696, #3979 ) ;
#32179=DIRECTION ( 'NONE',  ( -0.000000000000000000, 1.000000000000000000, -0.000000000000000000 ) ) ;
#32181=VECTOR ( 'NONE', #45348, 39.37007874015748143 ) ;
#32182=AXIS2_PLACEMENT_3D ( 'NONE', #20208, #599, #20468 ) ;
#32184=DIRECTION ( 'NONE',  ( -0.000000000000000000, 1.000000000000000000, -0.000000000000000000 ) ) ;
#32185=CARTESIAN_POINT ( 'NONE',  ( 1.909347346926324684, 3.267716535433071279, -3.312189666507128175E-16 ) ) ;
#32186=ORIENTED_EDGE ( 'NONE', *, *, #7617, .T. ) ;
#32188=VECTOR ( 'NONE', #31494, 39.37007874015748143 ) ;
#32189=DIRECTION ( 'NONE',  ( 0.000000000000000000, 0.000000000000000000, -1.000000000000000000 ) ) ;
#32191=ORIENTED_EDGE ( 'NONE', *, *, #32007, .T. ) ;
#32196=CARTESIAN_POINT ( 'NONE',  ( -1.363819533518803473, 0.000000000000000000, -1.102362204724405270 ) ) ;
#32198=ORIENTED_EDGE ( 'NONE', *, *, #10527, .T. ) ;
#32199=CARTESIAN_POINT ( 'NONE',  ( 0.000000000000000000, 3.267716535433071279, -0.1574803149606297248 ) ) ;
#32200=ORIENTED_EDGE ( 'NONE', *, *, #2967, .T. ) ;
#32201=FACE_OUTER_BOUND ( 'NONE', #40328, .T. ) ;
#32203=LINE ( 'NONE', #13093, #38306 ) ;
#32204=DIRECTION ( 'NONE',  ( -3.469446951953613696E-16, 0.000000000000000000, -1.000000000000000000 ) ) ;
#32206=ORIENTED_EDGE ( 'NONE', *, *, #42239, .F. ) ;
#32207=EDGE_LOOP ( 'NONE', ( #3601, #44225, #24120, #9112 ) ) ;
#32208=EDGE_CURVE ( 'NONE', #2168, #27199, #41884, .T. ) ;
#32210=VERTEX_POINT ( 'NONE', #45219 ) ;
#32211=CARTESIAN_POINT ( 'NONE',  ( -1.909347346926324462, 3.346456692913386100, 0.5905511811023582691 ) ) ;
#32212=ORIENTED_EDGE ( 'NONE', *, *, #19340, .F. ) ;
#32214=AXIS2_PLACEMENT_3D ( 'NONE', #40685, #33465, #5060 ) ;
#32215=LINE ( 'NONE', #40214, #22343 ) ;
#32216=VECTOR ( 'NONE', #12058, 39.37007874015748143 ) ;
#32220=ORIENTED_EDGE ( 'NONE', *, *, #532, .T. ) ;
#32222=ORIENTED_EDGE ( 'NONE', *, *, #23994, .F. ) ;
#32226=ORIENTED_EDGE ( 'NONE', *, *, #6118, .F. ) ;
#32227=ORIENTED_EDGE ( 'NONE', *, *, #17244, .T. ) ;
#32228=CARTESIAN_POINT ( 'NONE',  ( 0.1968503937007876625, 3.267716535433071279, -6.829619984160665442E-17 ) ) ;
#32229=LINE ( 'NONE', #47924, #23724 ) ;
#32231=ORIENTED_EDGE ( 'NONE', *, *, #9901, .F. ) ;
#32234=ORIENTED_EDGE ( 'NONE', *, *, #20471, .T. ) ;
#32235=CARTESIAN_POINT ( 'NONE',  ( 1.909347346926324684, 3.346456692913386100, 0.4724409448818868706 ) ) ;
#32242=CARTESIAN_POINT ( 'NONE',  ( 0.4696143004045484903, 0.000000000000000000, 2.362204724409437961 ) ) ;
#32246=CARTESIAN_POINT ( 'NONE',  ( 1.091055626815042645, 3.346456692913386100, -0.6299212598425181220 ) ) ;
#32247=CIRCLE ( 'NONE', #38837, 2.165354330708661568 ) ;
#32248=VECTOR ( 'NONE', #22493, 39.37007874015748143 ) ;
#32250=EDGE_LOOP ( 'NONE', ( #14128, #4082, #48790, #3973 ) ) ;
#32252=ORIENTED_EDGE ( 'NONE', *, *, #44685, .F. ) ;
#32253=LINE ( 'NONE', #35360, #36648 ) ;
#32256=PLANE ( 'NONE',  #317 ) ;
#32259=DIRECTION ( 'NONE',  ( 1.000000000000000000, 0.000000000000000000, -3.469446951953613696E-16 ) ) ;
#32260=DIRECTION ( 'NONE',  ( 1.000000000000000000, -0.000000000000000000, 0.000000000000000000 ) ) ;
#32261=ORIENTED_EDGE ( 'NONE', *, *, #41371, .F. ) ;
#32263=ADVANCED_FACE ( 'NONE', ( #22016 ), #38276, .F. ) ;
#32267=ORIENTED_EDGE ( 'NONE', *, *, #23495, .F. ) ;
#32268=CARTESIAN_POINT ( 'NONE',  ( -1.636583440222564301, 3.267716535433071279, 1.574803149606291530 ) ) ;
#32269=ORIENTED_EDGE ( 'NONE', *, *, #49803, .F. ) ;
#32270=EDGE_CURVE ( 'NONE', #25764, #15688, #45727, .T. ) ;
#32271=LINE ( 'NONE', #12128, #29334 ) ;
#32272=CARTESIAN_POINT ( 'NONE',  ( 0.2727639067037604947, 0.000000000000000000, -0.1574803149606298636 ) ) ;
#32274=LINE ( 'NONE', #13165, #50199 ) ;
#32275=ORIENTED_EDGE ( 'NONE', *, *, #13763, .T. ) ;
#32276=ORIENTED_EDGE ( 'NONE', *, *, #26274, .F. ) ;
#32277=CARTESIAN_POINT ( 'NONE',  ( 0.2727639067037610499, 3.346456692913386100, 1.102362204724404160 ) ) ;
#32278=DIRECTION ( 'NONE',  ( 1.000000000000000000, 0.000000000000000000, 0.000000000000000000 ) ) ;
#32279=FACE_BOUND ( 'NONE', #31486, .T. ) ;
#32280=VECTOR ( 'NONE', #42710, 39.37007874015748143 ) ;
#32283=EDGE_CURVE ( 'NONE', #7558, #42367, #23776, .T. ) ;
#32285=VERTEX_POINT ( 'NONE', #11901 ) ;
#32286=LINE ( 'NONE', #47980, #27384 ) ;
#32289=ORIENTED_EDGE ( 'NONE', *, *, #17240, .F. ) ;
#32290=ORIENTED_EDGE ( 'NONE', *, *, #43894, .F. ) ;
#32293=EDGE_LOOP ( 'NONE', ( #49290, #45404, #7069, #2090 ) ) ;
#32294=DIRECTION ( 'NONE',  ( -3.469446951953613696E-16, 0.000000000000000000, -1.000000000000000000 ) ) ;
#32295=VECTOR ( 'NONE', #1895, 39.37007874015748143 ) ;
#32297=EDGE_CURVE ( 'NONE', #24184, #4725, #31528, .T. ) ;
#32298=LINE ( 'NONE', #17063, #40761 ) ;
#32299=DIRECTION ( 'NONE',  ( -3.469446951953613696E-16, 0.000000000000000000, -1.000000000000000000 ) ) ;
#32300=ORIENTED_EDGE ( 'NONE', *, *, #15999, .T. ) ;
#32305=EDGE_CURVE ( 'NONE', #36336, #15273, #11146, .T. ) ;
#32306=DIRECTION ( 'NONE',  ( -3.469446951953613696E-16, 0.000000000000000000, -1.000000000000000000 ) ) ;
#32307=PLANE ( 'NONE',  #14077 ) ;
#32308=PLANE ( 'NONE',  #29251 ) ;
#32310=CARTESIAN_POINT ( 'NONE',  ( 1.687984952120845428, 3.346456692913386100, 1.259842519685033135 ) ) ;
#32311=ORIENTED_EDGE ( 'NONE', *, *, #25347, .T. ) ;
#32312=CARTESIAN_POINT ( 'NONE',  ( 2.182111253630085290, 3.346456692913386100, 0.1181102362204698858 ) ) ;
#32314=ORIENTED_EDGE ( 'NONE', *, *, #11737, .T. ) ;
#32316=ORIENTED_EDGE ( 'NONE', *, *, #33540, .T. ) ;
#32318=VECTOR ( 'NONE', #30252, 39.37007874015748143 ) ;
#32319=DIRECTION ( 'NONE',  ( 1.734723475976806848E-16, -0.000000000000000000, 1.000000000000000000 ) ) ;
#32320=PLANE ( 'NONE',  #9035 ) ;
#32323=ORIENTED_EDGE ( 'NONE', *, *, #37245, .T. ) ;
#32324=CARTESIAN_POINT ( 'NONE',  ( -0.6214413264104939882, 0.000000000000000000, 0.7874015748031456541 ) ) ;
#32325=AXIS2_PLACEMENT_3D ( 'NONE', #38694, #45643, #46400 ) ;
#32326=ORIENTED_EDGE ( 'NONE', *, *, #49425, .F. ) ;
#32327=DIRECTION ( 'NONE',  ( 1.000000000000000000, 0.000000000000000000, 0.000000000000000000 ) ) ;
#32329=ADVANCED_FACE ( 'NONE', ( #39015 ), #22, .F. ) ;
#32332=CARTESIAN_POINT ( 'NONE',  ( -0.5455278134075214336, 3.346456692913386100, -0.9448818897637762948 ) ) ;
#32333=CARTESIAN_POINT ( 'NONE',  ( -1.636583440222564301, 3.267716535433071279, -1.141732283464563791 ) ) ;
#32334=ADVANCED_FACE ( 'NONE', ( #35403 ), #43385, .F. ) ;
#32336=EDGE_LOOP ( 'NONE', ( #35265, #22068, #20144, #41825 ) ) ;
#32338=ORIENTED_EDGE ( 'NONE', *, *, #49471, .T. ) ;
#32339=DIRECTION ( 'NONE',  ( -0.000000000000000000, 1.000000000000000000, -0.000000000000000000 ) ) ;
#32340=VERTEX_POINT ( 'NONE', #19380 ) ;
#32341=ORIENTED_EDGE ( 'NONE', *, *, #44032, .F. ) ;
#32344=CARTESIAN_POINT ( 'NONE',  ( 0.5455278134075217666, 0.000000000000000000, 2.204724409448808764 ) ) ;
#32345=ORIENTED_EDGE ( 'NONE', *, *, #30230, .F. ) ;
#32347=DIRECTION ( 'NONE',  ( 0.000000000000000000, -1.000000000000000000, 0.000000000000000000 ) ) ;
#32351=PLANE ( 'NONE',  #9585 ) ;
#32352=ORIENTED_EDGE ( 'NONE', *, *, #25123, .F. ) ;
#32354=ORIENTED_EDGE ( 'NONE', *, *, #29718, .T. ) ;
#32355=ORIENTED_EDGE ( 'NONE', *, *, #24140, .F. ) ;
#32357=CARTESIAN_POINT ( 'NONE',  ( 0.000000000000000000, 3.267716535433071279, 1.062992125984245639 ) ) ;
#32358=DIRECTION ( 'NONE',  ( -3.469446951953613696E-16, 0.000000000000000000, -1.000000000000000000 ) ) ;
#32359=AXIS2_PLACEMENT_3D ( 'NONE', #19063, #43051, #50756 ) ;
#32360=EDGE_CURVE ( 'NONE', #31903, #35616, #23263, .T. ) ;
#32361=CARTESIAN_POINT ( 'NONE',  ( -0.5455278134075214336, 3.346456692913386100, -0.6299212598425175669 ) ) ;
#32364=ORIENTED_EDGE ( 'NONE', *, *, #5871, .T. ) ;
#32366=DIRECTION ( 'NONE',  ( -1.000000000000000000, 0.000000000000000000, 0.000000000000000000 ) ) ;
#32367=VECTOR ( 'NONE', #41936, 39.37007874015748143 ) ;
#32370=EDGE_CURVE ( 'NONE', #38936, #3690, #31788, .T. ) ;
#32371=DIRECTION ( 'NONE',  ( 1.734723475976806848E-16, 0.000000000000000000, 1.000000000000000000 ) ) ;
#32373=EDGE_CURVE ( 'NONE', #30180, #24438, #19135, .T. ) ;
#32375=FACE_OUTER_BOUND ( 'NONE', #50563, .T. ) ;
#32376=CARTESIAN_POINT ( 'NONE',  ( -1.536664496436148184E-16, 0.000000000000000000, -0.8267716535433052849 ) ) ;
#32377=ORIENTED_EDGE ( 'NONE', *, *, #37582, .T. ) ;
#32378=CARTESIAN_POINT ( 'NONE',  ( -1.363819533518803029, 3.346456692913386100, 1.102362204724404160 ) ) ;
#32381=EDGE_CURVE ( 'NONE', #20129, #33855, #34895, .T. ) ;
#32385=LINE ( 'NONE', #40122, #16417 ) ;
#32387=DIRECTION ( 'NONE',  ( 1.000000000000000000, 0.000000000000000000, -3.469446951953613696E-16 ) ) ;
#32388=CARTESIAN_POINT ( 'NONE',  ( -0.6214413264104939882, 3.267716535433071279, 1.220472440944875281 ) ) ;
#32390=ORIENTED_EDGE ( 'NONE', *, *, #9558, .F. ) ;
#32391=PLANE ( 'NONE',  #43610 ) ;
#32392=CARTESIAN_POINT ( 'NONE',  ( 0.000000000000000000, 3.267716535433071279, -0.3543307086614173040 ) ) ;
#32394=CARTESIAN_POINT ( 'NONE',  ( -0.3486774197067334380, 0.000000000000000000, 1.889763779527550369 ) ) ;
#32396=CARTESIAN_POINT ( 'NONE',  ( -1.712496953225537188, 3.346456692913386100, -0.3543307086614171930 ) ) ;
#32398=DIRECTION ( 'NONE',  ( -3.469446951953613696E-16, 0.000000000000000000, -1.000000000000000000 ) ) ;
#32399=EDGE_CURVE ( 'NONE', #27803, #30813, #50577, .T. ) ;
#32402=ORIENTED_EDGE ( 'NONE', *, *, #40714, .F. ) ;
#32403=VERTEX_POINT ( 'NONE', #42877 ) ;
#32405=FACE_OUTER_BOUND ( 'NONE', #23599, .T. ) ;
#32407=VECTOR ( 'NONE', #13153, 39.37007874015748143 ) ;
#32409=CARTESIAN_POINT ( 'NONE',  ( 0.5455278134075211005, 0.000000000000000000, -1.456692913385822630 ) ) ;
#32411=VECTOR ( 'NONE', #7777, 39.37007874015748143 ) ;
#32412=CARTESIAN_POINT ( 'NONE',  ( 0.2727639067037604392, 3.346456692913386100, -1.299212598425193210 ) ) ;
#32413=VECTOR ( 'NONE', #35094, 39.37007874015748143 ) ;
#32414=ORIENTED_EDGE ( 'NONE', *, *, #27252, .T. ) ;
#32415=ORIENTED_EDGE ( 'NONE', *, *, #16544, .T. ) ;
#32416=DIRECTION ( 'NONE',  ( -0.000000000000000000, 1.000000000000000000, -0.000000000000000000 ) ) ;
#32417=DIRECTION ( 'NONE',  ( 1.000000000000000000, 0.000000000000000000, 0.000000000000000000 ) ) ;
#32419=LINE ( 'NONE', #17423, #33953 ) ;
#32420=FACE_BOUND ( 'NONE', #48251, .T. ) ;
#32421=VECTOR ( 'NONE', #22646, 39.37007874015748143 ) ;
#32422=ORIENTED_EDGE ( 'NONE', *, *, #44835, .F. ) ;
#32424=VERTEX_POINT ( 'NONE', #50826 ) ;
#32425=ORIENTED_EDGE ( 'NONE', *, *, #13450, .T. ) ;
#32427=ORIENTED_EDGE ( 'NONE', *, *, #39146, .T. ) ;
#32430=CARTESIAN_POINT ( 'NONE',  ( 1.363819533518803251, 3.346456692913386100, 1.220472440944875281 ) ) ;
#32432=DIRECTION ( 'NONE',  ( 0.000000000000000000, -1.000000000000000000, 0.000000000000000000 ) ) ;
#32434=ADVANCED_FACE ( 'NONE', ( #3906 ), #19635, .F. ) ;
#32435=CARTESIAN_POINT ( 'NONE',  ( -1.439733046521776583, 3.267716535433071279, 4.995077429881868843E-16 ) ) ;
#32436=EDGE_CURVE ( 'NONE', #38137, #2677, #4676, .T. ) ;
#32439=AXIS2_PLACEMENT_3D ( 'NONE', #13175, #9551, #17550 ) ;
#32440=DIRECTION ( 'NONE',  ( -1.000000000000000000, 0.000000000000000000, -0.000000000000000000 ) ) ;
#32441=LINE ( 'NONE', #28543, #18766 ) ;
#32442=VERTEX_POINT ( 'NONE', #8289 ) ;
#32443=DIRECTION ( 'NONE',  ( -3.469446951953613696E-16, 0.000000000000000000, -1.000000000000000000 ) ) ;
#32444=AXIS2_PLACEMENT_3D ( 'NONE', #40126, #36259, #8879 ) ;
#32448=VECTOR ( 'NONE', #43963, 39.37007874015748143 ) ;
#32451=DIRECTION ( 'NONE',  ( -0.000000000000000000, 1.000000000000000000, -0.000000000000000000 ) ) ;
#32452=ORIENTED_EDGE ( 'NONE', *, *, #47909, .F. ) ;
#32453=CARTESIAN_POINT ( 'NONE',  ( 1.909347346926324684, 3.346456692913386100, 1.102362204724403938 ) ) ;
#32455=CARTESIAN_POINT ( 'NONE',  ( 0.8182917201112824834, 0.000000000000000000, 1.220472440944875281 ) ) ;
#32456=DIRECTION ( 'NONE',  ( -1.000000000000000000, 0.000000000000000000, 0.000000000000000000 ) ) ;
#32457=VECTOR ( 'NONE', #13261, 39.37007874015748143 ) ;
#32459=CARTESIAN_POINT ( 'NONE',  ( -1.363819533518803695, 3.267716535433071279, 2.365849761790806473E-16 ) ) ;
#32460=EDGE_CURVE ( 'NONE', #19826, #18320, #803, .T. ) ;
#32461=ORIENTED_EDGE ( 'NONE', *, *, #35407, .F. ) ;
#32462=FACE_BOUND ( 'NONE', #20822, .T. ) ;
#32464=DIRECTION ( 'NONE',  ( -1.000000000000000000, 0.000000000000000000, 0.000000000000000000 ) ) ;
#32470=CARTESIAN_POINT ( 'NONE',  ( -0.6214413264104939882, 3.346456692913386100, 1.220472440944875281 ) ) ;
#32474=CARTESIAN_POINT ( 'NONE',  ( 1.909347346926324684, 0.000000000000000000, 0.1574803149606280872 ) ) ;
#32475=ORIENTED_EDGE ( 'NONE', *, *, #9758, .F. ) ;
#32476=CARTESIAN_POINT ( 'NONE',  ( 1.015142113812069091, 3.346456692913386100, -1.732283464566923614 ) ) ;
#32477=ORIENTED_EDGE ( 'NONE', *, *, #15002, .T. ) ;
#32478=CARTESIAN_POINT ( 'NONE',  ( -1.712496953225537188, 0.000000000000000000, 0.4724409448818871482 ) ) ;
#32481=VERTEX_POINT ( 'NONE', #47997 ) ;
#32482=DIRECTION ( 'NONE',  ( 1.000000000000000000, 0.000000000000000000, 0.000000000000000000 ) ) ;
#32483=ORIENTED_EDGE ( 'NONE', *, *, #16695, .F. ) ;
#32484=VECTOR ( 'NONE', #8731, 39.37007874015748143 ) ;
#32485=VECTOR ( 'NONE', #17760, 39.37007874015748143 ) ;
#32487=ORIENTED_EDGE ( 'NONE', *, *, #42585, .T. ) ;
#32489=DIRECTION ( 'NONE',  ( -1.000000000000000000, -0.000000000000000000, -0.000000000000000000 ) ) ;
#32490=VECTOR ( 'NONE', #31999, 39.37007874015748143 ) ;
#32491=ORIENTED_EDGE ( 'NONE', *, *, #17695, .T. ) ;
#32492=LINE ( 'NONE', #36358, #7297 ) ;
#32493=ORIENTED_EDGE ( 'NONE', *, *, #19937, .F. ) ;
#32499=EDGE_CURVE ( 'NONE', #6449, #9844, #1311, .T. ) ;
#32500=DIRECTION ( 'NONE',  ( -3.469446951953613696E-16, 0.000000000000000000, -1.000000000000000000 ) ) ;
#32501=LINE ( 'NONE', #33015, #28744 ) ;
#32502=EDGE_CURVE ( 'NONE', #39048, #36296, #43897, .T. ) ;
#32503=CARTESIAN_POINT ( 'NONE',  ( -1.439733046521776139, 3.346456692913386100, -4.780733988912460139E-16 ) ) ;
#32504=DIRECTION ( 'NONE',  ( 0.000000000000000000, 0.000000000000000000, -1.000000000000000000 ) ) ;
#32508=ORIENTED_EDGE ( 'NONE', *, *, #12757, .T. ) ;
#32510=DIRECTION ( 'NONE',  ( -0.000000000000000000, 1.000000000000000000, -0.000000000000000000 ) ) ;
#32513=PLANE ( 'NONE',  #25110 ) ;
#32514=AXIS2_PLACEMENT_3D ( 'NONE', #3524, #19259, #45411 ) ;
#32516=ADVANCED_FACE ( 'NONE', ( #24810 ), #32834, .F. ) ;
#32517=ORIENTED_EDGE ( 'NONE', *, *, #40974, .F. ) ;
#32518=CARTESIAN_POINT ( 'NONE',  ( -1.712496953225537633, 0.000000000000000000, -0.4724409448818884805 ) ) ;
#32519=VECTOR ( 'NONE', #44758, 39.37007874015748143 ) ;
#32523=ADVANCED_FACE ( 'NONE', ( #16556 ), #32308, .F. ) ;
#32526=ORIENTED_EDGE ( 'NONE', *, *, #24584, .T. ) ;
#32527=CARTESIAN_POINT ( 'NONE',  ( 1.363819533518803251, 3.346456692913386100, -0.03937007874015908959 ) ) ;
#32529=FACE_BOUND ( 'NONE', #4630, .T. ) ;
#32530=EDGE_CURVE ( 'NONE', #42995, #45311, #48512, .T. ) ;
#32531=EDGE_LOOP ( 'NONE', ( #29719, #25308, #11514, #48990, #49070 ) ) ;
#32535=DIRECTION ( 'NONE',  ( 0.000000000000000000, 0.000000000000000000, -1.000000000000000000 ) ) ;
#32537=ORIENTED_EDGE ( 'NONE', *, *, #6096, .T. ) ;
#32540=CARTESIAN_POINT ( 'NONE',  ( 1.560669927219590747, 3.267716535433071279, -5.414661521997677271E-16 ) ) ;
#32541=FACE_BOUND ( 'NONE', #7330, .T. ) ;
#32542=PLANE ( 'NONE',  #39391 ) ;
#32543=DIRECTION ( 'NONE',  ( -0.000000000000000000, 1.000000000000000000, -0.000000000000000000 ) ) ;
#32546=DIRECTION ( 'NONE',  ( 0.000000000000000000, 0.000000000000000000, 1.000000000000000000 ) ) ;
#32548=VERTEX_POINT ( 'NONE', #24550 ) ;
#32549=VECTOR ( 'NONE', #5704, 39.37007874015748143 ) ;
#32550=VERTEX_POINT ( 'NONE', #40306 ) ;
#32551=VECTOR ( 'NONE', #19036, 39.37007874015748143 ) ;
#32552=ORIENTED_EDGE ( 'NONE', *, *, #11007, .T. ) ;
#32554=AXIS2_PLACEMENT_3D ( 'NONE', #23665, #40453, #28046 ) ;
#32556=DIRECTION ( 'NONE',  ( -3.469446951953613696E-16, 0.000000000000000000, -1.000000000000000000 ) ) ;
#32557=LINE ( 'NONE', #9051, #32967 ) ;
#32558=VERTEX_POINT ( 'NONE', #48258 ) ;
#32559=ORIENTED_EDGE ( 'NONE', *, *, #1623, .F. ) ;
#32561=AXIS2_PLACEMENT_3D ( 'NONE', #43285, #19792, #27031 ) ;
#32564=EDGE_CURVE ( 'NONE', #9285, #35070, #3471, .T. ) ;
#32566=LINE ( 'NONE', #24807, #21858 ) ;
#32567=EDGE_CURVE ( 'NONE', #47504, #42496, #50647, .T. ) ;
#32568=DIRECTION ( 'NONE',  ( -1.000000000000000000, 0.000000000000000000, 1.734723475976806848E-16 ) ) ;
#32569=CARTESIAN_POINT ( 'NONE',  ( 1.909347346926324462, 0.000000000000000000, -0.7874015748031473194 ) ) ;
#32570=EDGE_CURVE ( 'NONE', #24648, #34110, #10339, .T. ) ;
#32572=DIRECTION ( 'NONE',  ( 0.000000000000000000, 1.000000000000000000, 0.000000000000000000 ) ) ;
#32573=ORIENTED_EDGE ( 'NONE', *, *, #27977, .F. ) ;
#32575=CARTESIAN_POINT ( 'NONE',  ( 1.636583440222563857, 3.346456692913386100, 0.7480314960629872445 ) ) ;
#32577=ORIENTED_EDGE ( 'NONE', *, *, #40903, .T. ) ;
#32578=LINE ( 'NONE', #36960, #48786 ) ;
#32579=CARTESIAN_POINT ( 'NONE',  ( 3.927031490892378253E-16, 0.000000000000000000, 1.062992125984246083 ) ) ;
#32580=EDGE_CURVE ( 'NONE', #19845, #43301, #45673, .T. ) ;
#32581=CARTESIAN_POINT ( 'NONE',  ( -0.2727639067037602172, 0.000000000000000000, 1.102362204724404160 ) ) ;
#32582=ORIENTED_EDGE ( 'NONE', *, *, #24506, .F. ) ;
#32585=EDGE_CURVE ( 'NONE', #13057, #24863, #41834, .T. ) ;
#32586=ORIENTED_EDGE ( 'NONE', *, *, #17274, .F. ) ;
#32587=AXIS2_PLACEMENT_3D ( 'NONE', #38964, #31227, #42583 ) ;
#32588=DIRECTION ( 'NONE',  ( -1.000000000000000000, 0.000000000000000000, 1.734723475976806848E-16 ) ) ;
#32590=VECTOR ( 'NONE', #15859, 39.37007874015748143 ) ;
#32591=ORIENTED_EDGE ( 'NONE', *, *, #43544, .T. ) ;
#32592=DIRECTION ( 'NONE',  ( -0.000000000000000000, 1.000000000000000000, -0.000000000000000000 ) ) ;
#32593=DIRECTION ( 'NONE',  ( -0.000000000000000000, 1.000000000000000000, -0.000000000000000000 ) ) ;
#32594=CARTESIAN_POINT ( 'NONE',  ( 0.1968503937007878568, 3.346456692913386100, 0.9448818897637749625 ) ) ;
#32595=ORIENTED_EDGE ( 'NONE', *, *, #9303, .F. ) ;
#32596=ORIENTED_EDGE ( 'NONE', *, *, #50163, .T. ) ;
#32597=ORIENTED_EDGE ( 'NONE', *, *, #43360, .T. ) ;
#32598=VECTOR ( 'NONE', #36073, 39.37007874015748143 ) ;
#32599=FACE_OUTER_BOUND ( 'NONE', #31673, .T. ) ;
#32600=ORIENTED_EDGE ( 'NONE', *, *, #29046, .T. ) ;
#32602=CARTESIAN_POINT ( 'NONE',  ( 0.1968503937007877735, 3.346456692913386100, 1.062992125984246083 ) ) ;
#32603=CARTESIAN_POINT ( 'NONE',  ( -0.2727639067037607723, 0.000000000000000000, -0.7874015748031470974 ) ) ;
#32606=EDGE_LOOP ( 'NONE', ( #39179, #18909, #32945, #8084 ) ) ;
#32607=DIRECTION ( 'NONE',  ( -1.000000000000000000, 0.000000000000000000, 1.734723475976806848E-16 ) ) ;
#32608=CARTESIAN_POINT ( 'NONE',  ( 0.1968503937007872462, 0.000000000000000000, -0.8267716535433052849 ) ) ;
#32611=LINE ( 'NONE', #40856, #24909 ) ;
#32613=CARTESIAN_POINT ( 'NONE',  ( -0.8182917201112819283, 0.000000000000000000, -0.03937007874015895081 ) ) ;
#32615=VERTEX_POINT ( 'NONE', #2084 ) ;
#32616=LINE ( 'NONE', #48562, #17211 ) ;
#32617=CARTESIAN_POINT ( 'NONE',  ( -2.454875160333845674, 0.000000000000000000, 0.1574803149606286423 ) ) ;
#32618=CARTESIAN_POINT ( 'NONE',  ( -0.8182917201112819283, 3.346456692913386100, 2.047244094488179567 ) ) ;
#32619=PLANE ( 'NONE',  #28774 ) ;
#32620=VERTEX_POINT ( 'NONE', #14206 ) ;
#32621=EDGE_LOOP ( 'NONE', ( #34264, #16801, #23363, #32267 ) ) ;
#32622=VECTOR ( 'NONE', #27584, 39.37007874015748143 ) ;
#32624=ADVANCED_FACE ( 'NONE', ( #21452 ), #34092, .F. ) ;
#32629=LINE ( 'NONE', #48321, #2838 ) ;
#32632=EDGE_CURVE ( 'NONE', #46669, #50716, #29707, .T. ) ;
#32633=VECTOR ( 'NONE', #47975, 39.37007874015748143 ) ;
#32634=EDGE_CURVE ( 'NONE', #44754, #814, #21197, .T. ) ;
#32637=CARTESIAN_POINT ( 'NONE',  ( -1.636583440222564301, 0.000000000000000000, -1.574803149606293307 ) ) ;
#32638=VECTOR ( 'NONE', #25657, 39.37007874015748143 ) ;
#32639=ORIENTED_EDGE ( 'NONE', *, *, #12047, .F. ) ;
#32640=LINE ( 'NONE', #32378, #1933 ) ;
#32641=DIRECTION ( 'NONE',  ( -1.000000000000000000, 0.000000000000000000, -0.000000000000000000 ) ) ;
#32642=EDGE_LOOP ( 'NONE', ( #32526, #19477, #2950, #12281 ) ) ;
#32643=DIRECTION ( 'NONE',  ( -3.469446951953613696E-16, 0.000000000000000000, -1.000000000000000000 ) ) ;
#32644=CARTESIAN_POINT ( 'NONE',  ( 0.2727639067037609943, 0.000000000000000000, 1.220472440944875281 ) ) ;
#32646=DIRECTION ( 'NONE',  ( -3.469446951953613696E-16, 0.000000000000000000, -1.000000000000000000 ) ) ;
#32647=ORIENTED_EDGE ( 'NONE', *, *, #18132, .F. ) ;
#32648=FACE_OUTER_BOUND ( 'NONE', #27399, .T. ) ;
#32653=CARTESIAN_POINT ( 'NONE',  ( -1.166969139818015755, 3.267716535433071279, 0.5905511811023582691 ) ) ;
#32654=CARTESIAN_POINT ( 'NONE',  ( -1.985260859929298016, 0.000000000000000000, -0.9448818897637762948 ) ) ;
#32656=DIRECTION ( 'NONE',  ( -0.000000000000000000, 1.000000000000000000, -0.000000000000000000 ) ) ;
#32657=LINE ( 'NONE', #11739, #16056 ) ;
#32659=CARTESIAN_POINT ( 'NONE',  ( -1.363819533518803473, 0.000000000000000000, -1.102362204724405270 ) ) ;
#32661=CARTESIAN_POINT ( 'NONE',  ( -0.07591351300297340121, 3.346456692913386100, -0.9842519685039344823 ) ) ;
#32663=ORIENTED_EDGE ( 'NONE', *, *, #11799, .F. ) ;
#32666=DIRECTION ( 'NONE',  ( -3.469446951953613696E-16, 0.000000000000000000, -1.000000000000000000 ) ) ;
#32667=VECTOR ( 'NONE', #38460, 39.37007874015748143 ) ;
#32668=ORIENTED_EDGE ( 'NONE', *, *, #44695, .F. ) ;
#32669=CARTESIAN_POINT ( 'NONE',  ( 1.091055626815042423, 0.000000000000000000, -2.086614173228339641 ) ) ;
#32670=PLANE ( 'NONE',  #35112 ) ;
#32674=DIRECTION ( 'NONE',  ( -3.469446951953613696E-16, 0.000000000000000000, -1.000000000000000000 ) ) ;
#32675=ORIENTED_EDGE ( 'NONE', *, *, #48182, .T. ) ;
#32676=ORIENTED_EDGE ( 'NONE', *, *, #2268, .F. ) ;
#32677=CARTESIAN_POINT ( 'NONE',  ( -0.8942052331142552601, 3.267716535433071279, -0.8267716535433052849 ) ) ;
#32678=LINE ( 'NONE', #40664, #7651 ) ;
#32679=AXIS2_PLACEMENT_3D ( 'NONE', #19934, #35704, #15321 ) ;
#32680=DIRECTION ( 'NONE',  ( -0.000000000000000000, 1.000000000000000000, -0.000000000000000000 ) ) ;
#32683=FACE_BOUND ( 'NONE', #23641, .T. ) ;
#32685=ORIENTED_EDGE ( 'NONE', *, *, #36596, .F. ) ;
#32686=EDGE_CURVE ( 'NONE', #23722, #39604, #6481, .T. ) ;
#32691=EDGE_CURVE ( 'NONE', #12432, #4560, #17575, .T. ) ;
#32693=ORIENTED_EDGE ( 'NONE', *, *, #44666, .F. ) ;
#32694=DIRECTION ( 'NONE',  ( -0.000000000000000000, 1.000000000000000000, -0.000000000000000000 ) ) ;
#32695=ORIENTED_EDGE ( 'NONE', *, *, #32796, .F. ) ;
#32696=CARTESIAN_POINT ( 'NONE',  ( 1.636583440222563635, 3.267716535433071279, -2.839019714148966584E-16 ) ) ;
#32697=LINE ( 'NONE', #1945, #4671 ) ;
#32699=EDGE_CURVE ( 'NONE', #30287, #22389, #49021, .T. ) ;
#32700=VECTOR ( 'NONE', #27969, 39.37007874015748143 ) ;
#32701=FACE_OUTER_BOUND ( 'NONE', #41432, .T. ) ;
#32702=ADVANCED_FACE ( 'NONE', ( #2339 ), #9832, .F. ) ;
#32704=LINE ( 'NONE', #21068, #3098 ) ;
#32705=VECTOR ( 'NONE', #14127, 39.37007874015748143 ) ;
#32707=DIRECTION ( 'NONE',  ( 0.000000000000000000, 0.000000000000000000, 1.000000000000000000 ) ) ;
#32710=LINE ( 'NONE', #33725, #2605 ) ;
#32711=ORIENTED_EDGE ( 'NONE', *, *, #35989, .T. ) ;
#32712=LINE ( 'NONE', #5832, #46261 ) ;
#32713=LINE ( 'NONE', #43527, #3014 ) ;
#32714=ORIENTED_EDGE ( 'NONE', *, *, #1693, .F. ) ;
#32715=CARTESIAN_POINT ( 'NONE',  ( 0.000000000000000000, 3.267716535433071279, 0.000000000000000000 ) ) ;
#32719=VECTOR ( 'NONE', #43678, 39.37007874015748143 ) ;
#32721=DIRECTION ( 'NONE',  ( 1.000000000000000000, 0.000000000000000000, 0.000000000000000000 ) ) ;
#32722=VERTEX_POINT ( 'NONE', #49282 ) ;
#32723=FACE_BOUND ( 'NONE', #26339, .T. ) ;
#32724=DIRECTION ( 'NONE',  ( 1.000000000000000000, 0.000000000000000000, -3.469446951953613696E-16 ) ) ;
#32725=DIRECTION ( 'NONE',  ( 1.000000000000000000, -0.000000000000000000, 0.000000000000000000 ) ) ;
#32726=CARTESIAN_POINT ( 'NONE',  ( 0.8182917201112817063, 3.346456692913386100, -1.732283464566923614 ) ) ;
#32729=ORIENTED_EDGE ( 'NONE', *, *, #36893, .T. ) ;
#32730=ORIENTED_EDGE ( 'NONE', *, *, #39385, .T. ) ;
#32731=DIRECTION ( 'NONE',  ( -1.000000000000000000, 0.000000000000000000, 1.734723475976806848E-16 ) ) ;
#32732=VERTEX_POINT ( 'NONE', #49529 ) ;
#32733=DIRECTION ( 'NONE',  ( -1.000000000000000000, -0.000000000000000000, -0.000000000000000000 ) ) ;
#32735=EDGE_CURVE ( 'NONE', #39288, #16952, #39216, .T. ) ;
#32738=ORIENTED_EDGE ( 'NONE', *, *, #1306, .F. ) ;
#32740=EDGE_CURVE ( 'NONE', #27093, #42728, #33450, .T. ) ;
#32742=PLANE ( 'NONE',  #13310 ) ;
#32743=CIRCLE ( 'NONE', #36002, 2.165354330708661568 ) ;
#32744=ORIENTED_EDGE ( 'NONE', *, *, #10934, .T. ) ;
#32746=ORIENTED_EDGE ( 'NONE', *, *, #32761, .F. ) ;
#32747=ORIENTED_EDGE ( 'NONE', *, *, #47162, .F. ) ;
#32749=ORIENTED_EDGE ( 'NONE', *, *, #47684, .T. ) ;
#32757=ORIENTED_EDGE ( 'NONE', *, *, #6109, .T. ) ;
#32758=LINE ( 'NONE', #28600, #28547 ) ;
#32760=LINE ( 'NONE', #48439, #15652 ) ;
#32761=EDGE_CURVE ( 'NONE', #46834, #528, #40965, .T. ) ;
#32764=LINE ( 'NONE', #36621, #27082 ) ;
#32765=PLANE ( 'NONE',  #24141 ) ;
#32767=CARTESIAN_POINT ( 'NONE',  ( 0.000000000000000000, 3.346456692913386100, 0.000000000000000000 ) ) ;
#32768=DIRECTION ( 'NONE',  ( 1.734723475976806848E-16, -0.000000000000000000, 1.000000000000000000 ) ) ;
#32773=VECTOR ( 'NONE', #7606, 39.37007874015748143 ) ;
#32774=CARTESIAN_POINT ( 'NONE',  ( 0.8182917201112817063, 3.267716535433071279, -2.047244094488181343 ) ) ;
#32776=ORIENTED_EDGE ( 'NONE', *, *, #6224, .F. ) ;
#32777=FACE_OUTER_BOUND ( 'NONE', #45676, .T. ) ;
#32778=ORIENTED_EDGE ( 'NONE', *, *, #22868, .F. ) ;
#32779=DIRECTION ( 'NONE',  ( 0.000000000000000000, 0.000000000000000000, 1.000000000000000000 ) ) ;
#32780=PLANE ( 'NONE',  #47266 ) ;
#32781=CARTESIAN_POINT ( 'NONE',  ( 0.000000000000000000, 3.346456692913386100, 0.000000000000000000 ) ) ;
#32782=PLANE ( 'NONE',  #6969 ) ;
#32783=CARTESIAN_POINT ( 'NONE',  ( 2.106197740627111514, 3.245701213390774331, -1.259299084540527192 ) ) ;
#32784=ORIENTED_EDGE ( 'NONE', *, *, #42347, .T. ) ;
#32787=VERTEX_POINT ( 'NONE', #31476 ) ;
#32788=DIRECTION ( 'NONE',  ( -0.000000000000000000, 1.000000000000000000, -0.000000000000000000 ) ) ;
#32789=VECTOR ( 'NONE', #8737, 39.37007874015748143 ) ;
#32790=ORIENTED_EDGE ( 'NONE', *, *, #10338, .T. ) ;
#32792=LINE ( 'NONE', #28892, #42089 ) ;
#32793=ADVANCED_FACE ( 'NONE', ( #51030 ), #11096, .F. ) ;
#32795=EDGE_CURVE ( 'NONE', #514, #12754, #34249, .T. ) ;
#32796=EDGE_CURVE ( 'NONE', #22538, #45311, #26335, .T. ) ;
#32798=ORIENTED_EDGE ( 'NONE', *, *, #50032, .T. ) ;
#32800=LINE ( 'NONE', #48481, #43276 ) ;
#32801=DIRECTION ( 'NONE',  ( -1.000000000000000000, 0.000000000000000000, 0.000000000000000000 ) ) ;
#32803=VERTEX_POINT ( 'NONE', #3597 ) ;
#32804=EDGE_CURVE ( 'NONE', #31365, #16345, #35097, .T. ) ;
#32807=VECTOR ( 'NONE', #41160, 39.37007874015748143 ) ;
#32808=VECTOR ( 'NONE', #26839, 39.37007874015748143 ) ;
#32811=LINE ( 'NONE', #41059, #25390 ) ;
#32812=ORIENTED_EDGE ( 'NONE', *, *, #46211, .T. ) ;
#32813=VERTEX_POINT ( 'NONE', #42083 ) ;
#32814=AXIS2_PLACEMENT_3D ( 'NONE', #29682, #25544, #37180 ) ;
#32817=CARTESIAN_POINT ( 'NONE',  ( 0.8455406139730251569, 3.346456692913386100, -1.929133858267711110 ) ) ;
#32823=VECTOR ( 'NONE', #4340, 39.37007874015748143 ) ;
#32824=ORIENTED_EDGE ( 'NONE', *, *, #29887, .T. ) ;
#32825=VERTEX_POINT ( 'NONE', #18597 ) ;
#32829=PLANE ( 'NONE',  #26599 ) ;
#32830=VECTOR ( 'NONE', #14333, 39.37007874015748143 ) ;
#32831=EDGE_CURVE ( 'NONE', #31608, #22729, #9004, .T. ) ;
#32833=DIRECTION ( 'NONE',  ( -3.469446951953613696E-16, 0.000000000000000000, -1.000000000000000000 ) ) ;
#32834=PLANE ( 'NONE',  #47344 ) ;
#32838=DIRECTION ( 'NONE',  ( -0.000000000000000000, 1.000000000000000000, -0.000000000000000000 ) ) ;
#32839=ORIENTED_EDGE ( 'NONE', *, *, #4963, .T. ) ;
#32841=LINE ( 'NONE', #28937, #24925 ) ;
#32842=LINE ( 'NONE', #9327, #24531 ) ;
#32843=VECTOR ( 'NONE', #48663, 39.37007874015748143 ) ;
#32844=ORIENTED_EDGE ( 'NONE', *, *, #16828, .F. ) ;
#32846=EDGE_LOOP ( 'NONE', ( #28717, #26427, #15260, #39687, #30827 ) ) ;
#32847=LINE ( 'NONE', #9332, #23755 ) ;
#32850=EDGE_LOOP ( 'NONE', ( #41874, #37778, #27617, #2665 ) ) ;
#32854=VECTOR ( 'NONE', #36300, 39.37007874015748143 ) ;
#32855=EDGE_LOOP ( 'NONE', ( #11078, #46882, #50642, #16955 ) ) ;
#32856=EDGE_CURVE ( 'NONE', #5165, #11356, #45739, .T. ) ;
#32857=EDGE_LOOP ( 'NONE', ( #44206, #5401, #4435, #17346 ) ) ;
#32858=ORIENTED_EDGE ( 'NONE', *, *, #39734, .T. ) ;
#32861=ORIENTED_EDGE ( 'NONE', *, *, #42637, .F. ) ;
#32862=VERTEX_POINT ( 'NONE', #12618 ) ;
#32869=CARTESIAN_POINT ( 'NONE',  ( -1.091055626815042645, 3.346456692913386100, 1.870389530743259199 ) ) ;
#32870=LINE ( 'NONE', #48550, #15140 ) ;
#32871=CARTESIAN_POINT ( 'NONE',  ( 1.287906020515830585, 0.000000000000000000, 1.377952755905504256 ) ) ;
#32873=DIRECTION ( 'NONE',  ( 1.000000000000000000, 0.000000000000000000, 0.000000000000000000 ) ) ;
#32874=LINE ( 'NONE', #48556, #35118 ) ;
#32875=FACE_OUTER_BOUND ( 'NONE', #27882, .T. ) ;
#32878=CARTESIAN_POINT ( 'NONE',  ( -1.166969139818015977, 3.267716535433071279, -1.102362204724405270 ) ) ;
#32879=LINE ( 'NONE', #1616, #9093 ) ;
#32880=EDGE_CURVE ( 'NONE', #38641, #46852, #29297, .T. ) ;
#32881=AXIS2_PLACEMENT_3D ( 'NONE', #30614, #7375, #26478 ) ;
#32882=DIRECTION ( 'NONE',  ( 1.000000000000000000, 0.000000000000000000, -3.469446951953613696E-16 ) ) ;
#32883=DIRECTION ( 'NONE',  ( 1.734723475976806848E-16, -0.000000000000000000, 1.000000000000000000 ) ) ;
#32884=ORIENTED_EDGE ( 'NONE', *, *, #39347, .F. ) ;
#32885=ORIENTED_EDGE ( 'NONE', *, *, #24652, .F. ) ;
#32887=EDGE_CURVE ( 'NONE', #17616, #22523, #1253, .T. ) ;
#32888=DIRECTION ( 'NONE',  ( 0.000000000000000000, 0.000000000000000000, -1.000000000000000000 ) ) ;
#32890=EDGE_LOOP ( 'NONE', ( #8295, #34055, #34849, #48028 ) ) ;
#32892=DIRECTION ( 'NONE',  ( 0.000000000000000000, 1.000000000000000000, 0.000000000000000000 ) ) ;
#32893=VECTOR ( 'NONE', #5287, 39.37007874015748143 ) ;
#32894=AXIS2_PLACEMENT_3D ( 'NONE', #39434, #19798, #35563 ) ;
#32895=VECTOR ( 'NONE', #41323, 39.37007874015748143 ) ;
#32896=LINE ( 'NONE', #12743, #34104 ) ;
#32897=DIRECTION ( 'NONE',  ( -0.000000000000000000, 1.000000000000000000, -0.000000000000000000 ) ) ;
#32899=ORIENTED_EDGE ( 'NONE', *, *, #24811, .T. ) ;
#32900=LINE ( 'NONE', #48580, #32457 ) ;
#32901=VECTOR ( 'NONE', #23405, 39.37007874015748143 ) ;
#32902=CARTESIAN_POINT ( 'NONE',  ( 0.2727639067037609943, 0.000000000000000000, 2.165354330708650910 ) ) ;
#32903=ORIENTED_EDGE ( 'NONE', *, *, #27819, .T. ) ;
#32904=DIRECTION ( 'NONE',  ( -3.469446951953613696E-16, 0.000000000000000000, -1.000000000000000000 ) ) ;
#32905=FACE_OUTER_BOUND ( 'NONE', #31571, .T. ) ;
#32906=DIRECTION ( 'NONE',  ( -1.000000000000000000, 0.000000000000000000, 0.000000000000000000 ) ) ;
#32907=ORIENTED_EDGE ( 'NONE', *, *, #33669, .T. ) ;
#32908=DIRECTION ( 'NONE',  ( -1.000000000000000000, -0.000000000000000000, -0.000000000000000000 ) ) ;
#32910=ORIENTED_EDGE ( 'NONE', *, *, #26826, .T. ) ;
#32912=CARTESIAN_POINT ( 'NONE',  ( 0.7423782071083092626, 3.267716535433071279, 1.574803149606291974 ) ) ;
#32914=CARTESIAN_POINT ( 'NONE',  ( 1.833433833923351353, 0.000000000000000000, 0.1181102362204701633 ) ) ;
#32916=CARTESIAN_POINT ( 'NONE',  ( -1.712496953225538077, 3.267716535433071279, 5.941417334598193996E-16 ) ) ;
#32918=VECTOR ( 'NONE', #12445, 39.37007874015748143 ) ;
#32919=DIRECTION ( 'NONE',  ( -1.000000000000000000, 0.000000000000000000, -0.000000000000000000 ) ) ;
#32921=EDGE_LOOP ( 'NONE', ( #12655, #26621, #40662, #36340, #50180 ) ) ;
#32922=VERTEX_POINT ( 'NONE', #747 ) ;
#32924=CARTESIAN_POINT ( 'NONE',  ( -1.712496953225537188, 0.000000000000000000, 0.4724409448818871482 ) ) ;
#32926=EDGE_LOOP ( 'NONE', ( #7212, #24196, #10294, #41486 ) ) ;
#32927=PLANE ( 'NONE',  #41537 ) ;
#32931=CARTESIAN_POINT ( 'NONE',  ( -1.363819533518803473, 0.000000000000000000, -0.1574803149606300023 ) ) ;
#32933=VECTOR ( 'NONE', #34460, 39.37007874015748143 ) ;
#32934=ORIENTED_EDGE ( 'NONE', *, *, #24467, .T. ) ;
#32935=EDGE_LOOP ( 'NONE', ( #42501, #39977, #24838, #16154 ) ) ;
#32936=EDGE_CURVE ( 'NONE', #50505, #41557, #11844, .T. ) ;
#32937=CARTESIAN_POINT ( 'NONE',  ( -0.8942052331142552601, 3.267716535433071279, -0.5118110236220467790 ) ) ;
#32939=PLANE ( 'NONE',  #3296 ) ;
#32941=EDGE_LOOP ( 'NONE', ( #38858, #3766, #28423, #18079 ) ) ;
#32942=VECTOR ( 'NONE', #22356, 39.37007874015748143 ) ;
#32943=CARTESIAN_POINT ( 'NONE',  ( 1.761123562704336232, 3.267716535433071279, -1.259842519685035800 ) ) ;
#32944=FACE_BOUND ( 'NONE', #15806, .T. ) ;
#32945=ORIENTED_EDGE ( 'NONE', *, *, #31922, .F. ) ;
#32950=EDGE_CURVE ( 'NONE', #10560, #24016, #36626, .T. ) ;
#32951=ORIENTED_EDGE ( 'NONE', *, *, #49492, .F. ) ;
#32952=CARTESIAN_POINT ( 'NONE',  ( 2.106197740627112402, 3.267716535433071279, -0.02067487291359444701 ) ) ;
#32954=EDGE_CURVE ( 'NONE', #7498, #39188, #16497, .T. ) ;
#32956=CARTESIAN_POINT ( 'NONE',  ( -0.6214413264104945434, 3.267716535433071279, -0.1574803149606301411 ) ) ;
#32959=EDGE_CURVE ( 'NONE', #36931, #34717, #19837, .T. ) ;
#32960=CARTESIAN_POINT ( 'NONE',  ( 0.000000000000000000, 3.267716535433071279, -1.614173228346451605 ) ) ;
#32961=PLANE ( 'NONE',  #24502 ) ;
#32962=DIRECTION ( 'NONE',  ( 1.000000000000000000, 0.000000000000000000, -3.469446951953613696E-16 ) ) ;
#32963=ORIENTED_EDGE ( 'NONE', *, *, #6333, .T. ) ;
#32964=CARTESIAN_POINT ( 'NONE',  ( 1.091055626815042645, 0.000000000000000000, 0.9448818897637746295 ) ) ;
#32966=CARTESIAN_POINT ( 'NONE',  ( 1.909347346926324684, 3.346456692913386100, -0.6692913385826764205 ) ) ;
#32967=VECTOR ( 'NONE', #20143, 39.37007874015748143 ) ;
#32968=VERTEX_POINT ( 'NONE', #12107 ) ;
#32969=PLANE ( 'NONE',  #24844 ) ;
#32970=LINE ( 'NONE', #28043, #24466 ) ;
#32971=ORIENTED_EDGE ( 'NONE', *, *, #24158, .T. ) ;
#32972=DIRECTION ( 'NONE',  ( 1.000000000000000000, 0.000000000000000000, 0.000000000000000000 ) ) ;
#32973=LINE ( 'NONE', #24186, #20140 ) ;
#32975=ORIENTED_EDGE ( 'NONE', *, *, #46228, .T. ) ;
#32976=CARTESIAN_POINT ( 'NONE',  ( 0.7423782071083087075, 3.346456692913386100, 0.6299212598425161236 ) ) ;
#32978=ORIENTED_EDGE ( 'NONE', *, *, #30336, .T. ) ;
#32979=FACE_BOUND ( 'NONE', #35224, .T. ) ;
#32980=PLANE ( 'NONE',  #30031 ) ;
#32981=CARTESIAN_POINT ( 'NONE',  ( 0.2727639067037604392, 0.000000000000000000, 0.2755905511810994302 ) ) ;
#32982=DIRECTION ( 'NONE',  ( -1.000000000000000000, -0.000000000000000000, -0.000000000000000000 ) ) ;
#32983=ORIENTED_EDGE ( 'NONE', *, *, #3887, .F. ) ;
#32985=LINE ( 'NONE', #25725, #32843 ) ;
#32986=ORIENTED_EDGE ( 'NONE', *, *, #8889, .F. ) ;
#32987=PLANE ( 'NONE',  #19483 ) ;
#32988=ORIENTED_EDGE ( 'NONE', *, *, #34593, .F. ) ;
#32990=DIRECTION ( 'NONE',  ( 1.000000000000000000, -0.000000000000000000, 0.000000000000000000 ) ) ;
#32993=EDGE_LOOP ( 'NONE', ( #31245, #23887, #39795, #42414 ) ) ;
#32994=CARTESIAN_POINT ( 'NONE',  ( -0.3486774197067339376, 0.000000000000000000, -0.6299212598425175669 ) ) ;
#32995=EDGE_CURVE ( 'NONE', #31067, #11355, #37399, .T. ) ;
#32996=CARTESIAN_POINT ( 'NONE',  ( -1.363819533518803473, 3.267716535433071279, -0.1574803149606300023 ) ) ;
#32997=ORIENTED_EDGE ( 'NONE', *, *, #48596, .F. ) ;
#32999=ORIENTED_EDGE ( 'NONE', *, *, #6619, .T. ) ;
#33000=ORIENTED_EDGE ( 'NONE', *, *, #39730, .F. ) ;
#33001=VECTOR ( 'NONE', #26326, 39.37007874015748143 ) ;
#33003=ORIENTED_EDGE ( 'NONE', *, *, #22189, .T. ) ;
#33004=CARTESIAN_POINT ( 'NONE',  ( 0.8182917201112824834, 0.000000000000000000, 1.220472440944875281 ) ) ;
#33005=DIRECTION ( 'NONE',  ( -1.000000000000000000, 0.000000000000000000, -0.000000000000000000 ) ) ;
#33008=DIRECTION ( 'NONE',  ( 1.734723475976806848E-16, -0.000000000000000000, 1.000000000000000000 ) ) ;
#33009=VERTEX_POINT ( 'NONE', #29121 ) ;
#33012=CARTESIAN_POINT ( 'NONE',  ( 4.097771990496411591E-16, 3.267716535433071279, 2.106299212598425008 ) ) ;
#33015=CARTESIAN_POINT ( 'NONE',  ( -1.091055626815042201, 3.267716535433071279, 1.892679809432643896E-16 ) ) ;
#33019=FACE_OUTER_BOUND ( 'NONE', #15639, .T. ) ;
#33020=EDGE_CURVE ( 'NONE', #36398, #30647, #14144, .T. ) ;
#33021=LINE ( 'NONE', #13382, #21512 ) ;
#33023=ORIENTED_EDGE ( 'NONE', *, *, #33872, .T. ) ;
#33024=PLANE ( 'NONE',  #30383 ) ;
#33025=ADVANCED_FACE ( 'NONE', ( #29897 ), #21391, .F. ) ;
#33026=DIRECTION ( 'NONE',  ( 0.000000000000000000, 0.000000000000000000, -1.000000000000000000 ) ) ;
#33028=CARTESIAN_POINT ( 'NONE',  ( 1.363819533518803251, 3.267716535433071279, 0.2755905511810996522 ) ) ;
#33031=LINE ( 'NONE', #32518, #9953 ) ;
#33033=PLANE ( 'NONE',  #9395 ) ;
#33034=AXIS2_PLACEMENT_3D ( 'NONE', #14388, #23142, #46357 ) ;
#33037=CARTESIAN_POINT ( 'NONE',  ( -1.363819533518803473, 0.000000000000000000, 1.732283464566920950 ) ) ;
#33040=CARTESIAN_POINT ( 'NONE',  ( 0.1968503937007878568, 3.346456692913386100, 2.204724409448808764 ) ) ;
#33041=FACE_BOUND ( 'NONE', #43371, .T. ) ;
#33042=VERTEX_POINT ( 'NONE', #45106 ) ;
#33045=ORIENTED_EDGE ( 'NONE', *, *, #29005, .T. ) ;
#33046=ADVANCED_FACE ( 'NONE', ( #41014 ), #5886, .F. ) ;
#33048=CARTESIAN_POINT ( 'NONE',  ( 0.2727639067037610499, 3.346456692913386100, 1.732283464566921172 ) ) ;
#33052=EDGE_CURVE ( 'NONE', #6227, #9948, #29784, .T. ) ;
#33054=ORIENTED_EDGE ( 'NONE', *, *, #44150, .T. ) ;
#33056=FACE_OUTER_BOUND ( 'NONE', #99, .T. ) ;
#33057=FACE_BOUND ( 'NONE', #40712, .T. ) ;
#33060=CARTESIAN_POINT ( 'NONE',  ( 0.000000000000000000, 3.267716535433071279, 0.6299212598425164567 ) ) ;
#33063=CARTESIAN_POINT ( 'NONE',  ( 0.4696143004045484348, 3.346456692913386100, 1.220472440944875281 ) ) ;
#33066=ORIENTED_EDGE ( 'NONE', *, *, #21726, .F. ) ;
#33067=CARTESIAN_POINT ( 'NONE',  ( -1.195183497228115035E-16, 0.000000000000000000, -0.6299212598425177889 ) ) ;
#33068=VECTOR ( 'NONE', #38719, 39.37007874015748143 ) ;
#33069=LINE ( 'NONE', #49513, #20860 ) ;
#33070=AXIS2_PLACEMENT_3D ( 'NONE', #27677, #23302, #3184 ) ;
#33071=CARTESIAN_POINT ( 'NONE',  ( -1.909347346926324906, 0.000000000000000000, -0.4724409448818884805 ) ) ;
#33072=EDGE_CURVE ( 'NONE', #39002, #1491, #41768, .T. ) ;
#33073=LINE ( 'NONE', #37959, #24731 ) ;
#33074=ORIENTED_EDGE ( 'NONE', *, *, #5649, .F. ) ;
#33075=ORIENTED_EDGE ( 'NONE', *, *, #30975, .F. ) ;
#33077=LINE ( 'NONE', #34343, #4022 ) ;
#33078=CARTESIAN_POINT ( 'NONE',  ( 1.560669927219590525, 3.346456692913386100, -0.3543307086614178592 ) ) ;
#33079=AXIS2_PLACEMENT_3D ( 'NONE', #38375, #13610, #37879 ) ;
#33080=DIRECTION ( 'NONE',  ( -1.000000000000000000, 0.000000000000000000, 1.734723475976806848E-16 ) ) ;
#33081=CARTESIAN_POINT ( 'NONE',  ( 0.000000000000000000, 3.267716535433071279, -2.086614173228340086 ) ) ;
#33087=EDGE_CURVE ( 'NONE', #38641, #20960, #9769, .T. ) ;
#33088=ORIENTED_EDGE ( 'NONE', *, *, #8115, .F. ) ;
#33091=ORIENTED_EDGE ( 'NONE', *, *, #44080, .F. ) ;
#33092=ORIENTED_EDGE ( 'NONE', *, *, #46890, .T. ) ;
#33093=CARTESIAN_POINT ( 'NONE',  ( 0.5455278134075212115, 3.346456692913386100, 0.9448818897637746295 ) ) ;
#33094=CARTESIAN_POINT ( 'NONE',  ( 0.2727639067037610499, 0.000000000000000000, 2.362204724409437961 ) ) ;
#33096=VERTEX_POINT ( 'NONE', #25508 ) ;
#33097=CARTESIAN_POINT ( 'NONE',  ( 1.363819533518803251, 0.000000000000000000, -0.1574803149606304187 ) ) ;
#33102=DIRECTION ( 'NONE',  ( 1.734723475976806848E-16, -0.000000000000000000, 1.000000000000000000 ) ) ;
#33103=EDGE_CURVE ( 'NONE', #35993, #42801, #10021, .T. ) ;
#33104=DIRECTION ( 'NONE',  ( -0.000000000000000000, 0.000000000000000000, 1.000000000000000000 ) ) ;
#33105=VECTOR ( 'NONE', #4960, 39.37007874015748143 ) ;
#33106=ADVANCED_FACE ( 'NONE', ( #19274 ), #23152, .F. ) ;
#33107=EDGE_LOOP ( 'NONE', ( #50495, #20951, #44672, #2378 ) ) ;
#33110=PLANE ( 'NONE',  #28801 ) ;
#33111=ADVANCED_FACE ( 'NONE', ( #22403 ), #23401, .F. ) ;
#33112=ORIENTED_EDGE ( 'NONE', *, *, #41761, .F. ) ;
#33113=ORIENTED_EDGE ( 'NONE', *, *, #16531, .F. ) ;
#33115=CARTESIAN_POINT ( 'NONE',  ( 1.833433833923351353, 0.000000000000000000, -0.8267716535433055070 ) ) ;
#33118=AXIS2_PLACEMENT_3D ( 'NONE', #3539, #27016, #22903 ) ;
#33119=ORIENTED_EDGE ( 'NONE', *, *, #47662, .T. ) ;
#33122=LINE ( 'NONE', #5480, #8865 ) ;
#33124=PLANE ( 'NONE',  #33988 ) ;
#33125=CARTESIAN_POINT ( 'NONE',  ( -0.8182917201112815953, 3.267716535433071279, 1.419509857074482553E-16 ) ) ;
#33126=FACE_OUTER_BOUND ( 'NONE', #27451, .T. ) ;
#33128=ORIENTED_EDGE ( 'NONE', *, *, #9181, .T. ) ;
#33129=DIRECTION ( 'NONE',  ( -1.000000000000000000, 0.000000000000000000, 0.000000000000000000 ) ) ;
#33130=CARTESIAN_POINT ( 'NONE',  ( 0.2727639067037604392, 0.000000000000000000, -0.9842519685039348154 ) ) ;
#33132=ORIENTED_EDGE ( 'NONE', *, *, #4614, .T. ) ;
#33135=VERTEX_POINT ( 'NONE', #35038 ) ;
#33136=LINE ( 'NONE', #4990, #36494 ) ;
#33138=VECTOR ( 'NONE', #32125, 39.37007874015748143 ) ;
#33139=EDGE_CURVE ( 'NONE', #1125, #16455, #34283, .T. ) ;
#33140=CARTESIAN_POINT ( 'NONE',  ( 1.363819533518803029, 3.346456692913386100, -1.732283464566923170 ) ) ;
#33141=EDGE_CURVE ( 'NONE', #39828, #23227, #34535, .T. ) ;
#33142=PLANE ( 'NONE',  #43376 ) ;
#33143=VECTOR ( 'NONE', #16393, 39.37007874015748143 ) ;
#33144=FACE_OUTER_BOUND ( 'NONE', #21733, .T. ) ;
#33145=EDGE_LOOP ( 'NONE', ( #12980, #3998, #45513, #18211 ) ) ;
#33146=EDGE_CURVE ( 'NONE', #26629, #4890, #38905, .T. ) ;
#33147=CARTESIAN_POINT ( 'NONE',  ( 0.2727639067037604392, 0.000000000000000000, -1.614173228346451605 ) ) ;
#33148=AXIS2_PLACEMENT_3D ( 'NONE', #24212, #31965, #15945 ) ;
#33149=FACE_OUTER_BOUND ( 'NONE', #3671, .T. ) ;
#33151=EDGE_LOOP ( 'NONE', ( #1926, #23301, #46302, #50527 ) ) ;
#33152=AXIS2_PLACEMENT_3D ( 'NONE', #4495, #359, #39605 ) ;
#33153=CARTESIAN_POINT ( 'NONE',  ( -1.712496953225537188, 3.346456692913386100, -0.1574803149606297248 ) ) ;
#33155=DIRECTION ( 'NONE',  ( 0.000000000000000000, 0.000000000000000000, 1.000000000000000000 ) ) ;
#33158=LINE ( 'NONE', #14279, #45670 ) ;
#33159=ORIENTED_EDGE ( 'NONE', *, *, #41453, .F. ) ;
#33161=DIRECTION ( 'NONE',  ( -0.000000000000000000, 1.000000000000000000, -0.000000000000000000 ) ) ;
#33164=CARTESIAN_POINT ( 'NONE',  ( -1.909347346926324462, 0.000000000000000000, 1.102362204724404160 ) ) ;
#33165=LINE ( 'NONE', #36773, #25133 ) ;
#33166=EDGE_CURVE ( 'NONE', #16772, #19508, #49972, .T. ) ;
#33167=CARTESIAN_POINT ( 'NONE',  ( 0.1968503937007878568, 0.000000000000000000, 0.9448818897637749625 ) ) ;
#33170=VERTEX_POINT ( 'NONE', #49718 ) ;
#33171=EDGE_LOOP ( 'NONE', ( #48793, #5501, #23151, #7672 ) ) ;
#33173=LINE ( 'NONE', #48856, #12255 ) ;
#33174=EDGE_CURVE ( 'NONE', #46419, #46902, #46120, .T. ) ;
#33175=ORIENTED_EDGE ( 'NONE', *, *, #15883, .F. ) ;
#33176=PLANE ( 'NONE',  #25910 ) ;
#33177=DIRECTION ( 'NONE',  ( 1.000000000000000000, -0.000000000000000000, 0.000000000000000000 ) ) ;
#33178=CARTESIAN_POINT ( 'NONE',  ( -1.439733046521776139, 3.267716535433071279, 0.3149606299212578953 ) ) ;
#33179=EDGE_CURVE ( 'NONE', #37754, #45470, #14397, .T. ) ;
#33185=CARTESIAN_POINT ( 'NONE',  ( -1.636583440222563635, 3.346456692913386100, 0.9448818897637749625 ) ) ;
#33187=CARTESIAN_POINT ( 'NONE',  ( -1.091055626815042201, 0.000000000000000000, 0.1181102362204705658 ) ) ;
#33188=VECTOR ( 'NONE', #16066, 39.37007874015748143 ) ;
#33189=FACE_BOUND ( 'NONE', #29727, .T. ) ;
#33191=LINE ( 'NONE', #8657, #22451 ) ;
#33194=ORIENTED_EDGE ( 'NONE', *, *, #16620, .T. ) ;
#33195=FACE_OUTER_BOUND ( 'NONE', #2363, .T. ) ;
#33196=VECTOR ( 'NONE', #16963, 39.37007874015748143 ) ;
#33198=CARTESIAN_POINT ( 'NONE',  ( -0.8942052331142552601, 3.267716535433071279, 3.102397620449223960E-16 ) ) ;
#33199=LINE ( 'NONE', #23440, #16321 ) ;
#33200=EDGE_LOOP ( 'NONE', ( #19681, #1925, #17729, #17717 ) ) ;
#33201=FACE_OUTER_BOUND ( 'NONE', #39899, .T. ) ;
#33204=CARTESIAN_POINT ( 'NONE',  ( 1.091055626815042645, 0.000000000000000000, -0.1968503937007883287 ) ) ;
#33205=EDGE_CURVE ( 'NONE', #19810, #904, #42263, .T. ) ;
#33206=DIRECTION ( 'NONE',  ( 1.000000000000000000, 0.000000000000000000, 0.000000000000000000 ) ) ;
#33209=EDGE_CURVE ( 'NONE', #9222, #16455, #30404, .T. ) ;
#33210=PLANE ( 'NONE',  #3546 ) ;
#33213=ORIENTED_EDGE ( 'NONE', *, *, #46005, .F. ) ;
#33214=VECTOR ( 'NONE', #21176, 39.37007874015748143 ) ;
#33215=DIRECTION ( 'NONE',  ( 0.000000000000000000, -1.000000000000000000, 0.000000000000000000 ) ) ;
#33216=LINE ( 'NONE', #33476, #2207 ) ;
#33217=VERTEX_POINT ( 'NONE', #7416 ) ;
#33218=LINE ( 'NONE', #49163, #2370 ) ;
#33219=EDGE_CURVE ( 'NONE', #4697, #48815, #46370, .T. ) ;
#33220=LINE ( 'NONE', #18477, #13492 ) ;
#33221=LINE ( 'NONE', #25967, #12004 ) ;
#33222=VECTOR ( 'NONE', #36853, 39.37007874015748143 ) ;
#33223=ORIENTED_EDGE ( 'NONE', *, *, #25731, .T. ) ;
#33225=DIRECTION ( 'NONE',  ( -0.000000000000000000, 0.000000000000000000, 1.000000000000000000 ) ) ;
#33227=FACE_BOUND ( 'NONE', #49568, .T. ) ;
#33232=EDGE_CURVE ( 'NONE', #6075, #27292, #38407, .T. ) ;
#33233=LINE ( 'NONE', #13345, #37538 ) ;
#33235=ORIENTED_EDGE ( 'NONE', *, *, #23970, .F. ) ;
#33236=LINE ( 'NONE', #8963, #48513 ) ;
#33240=ORIENTED_EDGE ( 'NONE', *, *, #43117, .T. ) ;
#33242=EDGE_LOOP ( 'NONE', ( #30765, #4030, #863, #9599 ) ) ;
#33243=CARTESIAN_POINT ( 'NONE',  ( -0.2727639067037602172, 3.346456692913386100, 1.102362204724404160 ) ) ;
#33245=ORIENTED_EDGE ( 'NONE', *, *, #11674, .F. ) ;
#33246=DIRECTION ( 'NONE',  ( 1.000000000000000000, 0.000000000000000000, -3.469446951953613696E-16 ) ) ;
#33249=ADVANCED_FACE ( 'NONE', ( #46619 ), #24697, .F. ) ;
#33250=ORIENTED_EDGE ( 'NONE', *, *, #14094, .F. ) ;
#33251=ORIENTED_EDGE ( 'NONE', *, *, #22834, .T. ) ;
#33252=FACE_OUTER_BOUND ( 'NONE', #19322, .T. ) ;
#33254=ORIENTED_EDGE ( 'NONE', *, *, #17112, .T. ) ;
#33255=CARTESIAN_POINT ( 'NONE',  ( -0.6214413264104945434, 3.346456692913386100, -1.614173228346451605 ) ) ;
#33257=LINE ( 'NONE', #49703, #22770 ) ;
#33258=AXIS2_PLACEMENT_3D ( 'NONE', #42817, #15708, #23446 ) ;
#33260=DIRECTION ( 'NONE',  ( -3.469446951953613696E-16, 0.000000000000000000, -1.000000000000000000 ) ) ;
#33262=DIRECTION ( 'NONE',  ( -0.000000000000000000, 1.000000000000000000, -0.000000000000000000 ) ) ;
#33264=VECTOR ( 'NONE', #32443, 39.37007874015748143 ) ;
#33266=EDGE_CURVE ( 'NONE', #47436, #35629, #36059, .T. ) ;
#33267=CARTESIAN_POINT ( 'NONE',  ( 0.1968503937007878568, 3.346456692913386100, 2.156388021673882438 ) ) ;
#33268=CARTESIAN_POINT ( 'NONE',  ( -0.8942052331142552601, 3.346456692913386100, -1.907064071829739582 ) ) ;
#33269=LINE ( 'NONE', #37397, #33446 ) ;
#33270=DIRECTION ( 'NONE',  ( -0.000000000000000000, 1.000000000000000000, -0.000000000000000000 ) ) ;
#33273=EDGE_CURVE ( 'NONE', #10342, #11574, #4817, .T. ) ;
#33274=ORIENTED_EDGE ( 'NONE', *, *, #37001, .F. ) ;
#33276=EDGE_CURVE ( 'NONE', #18135, #25893, #4299, .T. ) ;
#33277=CARTESIAN_POINT ( 'NONE',  ( 1.015142113812069091, 3.267716535433071279, -2.047244094488181343 ) ) ;
#33278=VERTEX_POINT ( 'NONE', #43526 ) ;
#33280=ORIENTED_EDGE ( 'NONE', *, *, #6405, .T. ) ;
#33282=DIRECTION ( 'NONE',  ( 1.000000000000000000, -0.000000000000000000, 0.000000000000000000 ) ) ;
#33285=ADVANCED_FACE ( 'NONE', ( #39925 ), #35799, .F. ) ;
#33286=LINE ( 'NONE', #17525, #50718 ) ;
#33288=FACE_OUTER_BOUND ( 'NONE', #7445, .T. ) ;
#33289=VECTOR ( 'NONE', #49056, 39.37007874015748143 ) ;
#33290=LINE ( 'NONE', #13154, #12184 ) ;
#33291=DIRECTION ( 'NONE',  ( 0.000000000000000000, 0.000000000000000000, -1.000000000000000000 ) ) ;
#33292=ORIENTED_EDGE ( 'NONE', *, *, #45620, .F. ) ;
#33293=EDGE_CURVE ( 'NONE', #17266, #49145, #422, .T. ) ;
#33294=CARTESIAN_POINT ( 'NONE',  ( 0.7423782071083084855, 3.346456692913386100, -1.574803149606293529 ) ) ;
#33295=AXIS2_PLACEMENT_3D ( 'NONE', #26220, #22101, #49165 ) ;
#33298=VECTOR ( 'NONE', #20486, 39.37007874015748143 ) ;
#33299=CARTESIAN_POINT ( 'NONE',  ( 0.8182917201112819283, 3.346456692913386100, 0.9055118110236164419 ) ) ;
#33300=DIRECTION ( 'NONE',  ( -0.000000000000000000, 0.000000000000000000, 1.000000000000000000 ) ) ;
#33303=VECTOR ( 'NONE', #12749, 39.37007874015748143 ) ;
#33305=VERTEX_POINT ( 'NONE', #27526 ) ;
#33306=EDGE_LOOP ( 'NONE', ( #25651, #7262, #41847, #45911 ) ) ;
#33307=CARTESIAN_POINT ( 'NONE',  ( 0.000000000000000000, 3.267716535433071279, 1.417322834645662333 ) ) ;
#33308=LINE ( 'NONE', #32540, #28136 ) ;
#33309=FACE_BOUND ( 'NONE', #18759, .T. ) ;
#33311=EDGE_CURVE ( 'NONE', #49369, #29685, #36317, .T. ) ;
#33312=DIRECTION ( 'NONE',  ( 1.734723475976806848E-16, -0.000000000000000000, 1.000000000000000000 ) ) ;
#33314=EDGE_LOOP ( 'NONE', ( #10119, #43234, #1764, #23114 ) ) ;
#33315=ORIENTED_EDGE ( 'NONE', *, *, #23074, .F. ) ;
#33316=CARTESIAN_POINT ( 'NONE',  ( -1.363819533518803695, 3.267716535433071279, 2.365849761790806473E-16 ) ) ;
#33318=EDGE_CURVE ( 'NONE', #35927, #38936, #12306, .T. ) ;
#33319=ORIENTED_EDGE ( 'NONE', *, *, #1309, .T. ) ;
#33320=VERTEX_POINT ( 'NONE', #40188 ) ;
#33321=EDGE_LOOP ( 'NONE', ( #37878, #27676, #8377, #27483 ) ) ;
#33323=PLANE ( 'NONE',  #21080 ) ;
#33325=DIRECTION ( 'NONE',  ( 1.734723475976806848E-16, 0.000000000000000000, 1.000000000000000000 ) ) ;
#33327=VERTEX_POINT ( 'NONE', #50973 ) ;
#33328=VERTEX_POINT ( 'NONE', #12556 ) ;
#33329=VECTOR ( 'NONE', #6441, 39.37007874015748143 ) ;
#33330=LINE ( 'NONE', #5698, #19995 ) ;
#33331=DIRECTION ( 'NONE',  ( 1.000000000000000000, 0.000000000000000000, -3.469446951953613696E-16 ) ) ;
#33333=DIRECTION ( 'NONE',  ( 1.734723475976806848E-16, 0.000000000000000000, 1.000000000000000000 ) ) ;
#33334=AXIS2_PLACEMENT_3D ( 'NONE', #49227, #10785, #30417 ) ;
#33335=DIRECTION ( 'NONE',  ( -0.000000000000000000, 1.000000000000000000, -0.000000000000000000 ) ) ;
#33339=VECTOR ( 'NONE', #28930, 39.37007874015748143 ) ;
#33340=CARTESIAN_POINT ( 'NONE',  ( 1.363819533518803029, 3.346456692913386100, -1.614173228346452715 ) ) ;
#33341=ADVANCED_FACE ( 'NONE', ( #24182 ), #20297, .F. ) ;
#33343=PLANE ( 'NONE',  #45635 ) ;
#33344=VECTOR ( 'NONE', #49841, 39.37007874015748143 ) ;
#33346=CARTESIAN_POINT ( 'NONE',  ( -1.363819533518803473, 3.346456692913386100, -1.732283464566922726 ) ) ;
#33347=CARTESIAN_POINT ( 'NONE',  ( -0.5455278134075208785, 3.346456692913386100, 1.062992125984246083 ) ) ;
#33349=EDGE_LOOP ( 'NONE', ( #29988, #32858, #49694, #11010 ) ) ;
#33350=CARTESIAN_POINT ( 'NONE',  ( -1.636583440222564301, 3.346456692913386100, 1.574803149606291530 ) ) ;
#33355=VERTEX_POINT ( 'NONE', #8939 ) ;
#33356=PLANE ( 'NONE',  #40874 ) ;
#33357=LINE ( 'NONE', #13728, #15660 ) ;
#33358=EDGE_CURVE ( 'NONE', #17616, #1486, #43266, .T. ) ;
#33361=ORIENTED_EDGE ( 'NONE', *, *, #13398, .F. ) ;
#33362=CARTESIAN_POINT ( 'NONE',  ( 0.8182917201112819283, 3.346456692913386100, -0.3543307086614175816 ) ) ;
#33364=VERTEX_POINT ( 'NONE', #11785 ) ;
#33365=VERTEX_POINT ( 'NONE', #19780 ) ;
#33366=VECTOR ( 'NONE', #22915, 39.37007874015748143 ) ;
#33367=DIRECTION ( 'NONE',  ( 1.000000000000000000, 0.000000000000000000, 0.000000000000000000 ) ) ;
#33368=DIRECTION ( 'NONE',  ( 0.000000000000000000, 1.000000000000000000, 0.000000000000000000 ) ) ;
#33369=DIRECTION ( 'NONE',  ( -0.000000000000000000, 1.000000000000000000, -0.000000000000000000 ) ) ;
#33370=EDGE_CURVE ( 'NONE', #5323, #38936, #32712, .T. ) ;
#33371=VECTOR ( 'NONE', #48718, 39.37007874015748143 ) ;
#33372=VECTOR ( 'NONE', #36321, 39.37007874015748143 ) ;
#33373=VERTEX_POINT ( 'NONE', #5579 ) ;
#33374=EDGE_CURVE ( 'NONE', #3361, #40300, #13836, .T. ) ;
#33375=PLANE ( 'NONE',  #17252 ) ;
#33376=DIRECTION ( 'NONE',  ( -0.000000000000000000, 1.000000000000000000, -0.000000000000000000 ) ) ;
#33377=DIRECTION ( 'NONE',  ( 1.000000000000000000, 0.000000000000000000, -3.469446951953613696E-16 ) ) ;
#33378=EDGE_CURVE ( 'NONE', #23218, #37644, #9711, .T. ) ;
#33379=ORIENTED_EDGE ( 'NONE', *, *, #37460, .F. ) ;
#33381=FACE_OUTER_BOUND ( 'NONE', #47847, .T. ) ;
#33382=VECTOR ( 'NONE', #23344, 39.37007874015748143 ) ;
#33383=LINE ( 'NONE', #17367, #1026 ) ;
#33384=ORIENTED_EDGE ( 'NONE', *, *, #9596, .F. ) ;
#33387=CARTESIAN_POINT ( 'NONE',  ( 0.8182917201112819283, 3.346456692913386100, 0.1574803149606286423 ) ) ;
#33388=CARTESIAN_POINT ( 'NONE',  ( 0.2727639067037602172, 3.267716535433071279, -2.148105963102950877 ) ) ;
#33390=DIRECTION ( 'NONE',  ( -0.000000000000000000, 1.000000000000000000, -0.000000000000000000 ) ) ;
#33393=VERTEX_POINT ( 'NONE', #40955 ) ;
#33395=ORIENTED_EDGE ( 'NONE', *, *, #29860, .F. ) ;
#33396=DIRECTION ( 'NONE',  ( 1.000000000000000000, 0.000000000000000000, 0.000000000000000000 ) ) ;
#33398=ADVANCED_FACE ( 'NONE', ( #33727 ), #41211, .F. ) ;
#33399=EDGE_CURVE ( 'NONE', #22612, #3488, #17710, .T. ) ;
#33400=EDGE_CURVE ( 'NONE', #20580, #39173, #17451, .T. ) ;
#33404=VERTEX_POINT ( 'NONE', #33475 ) ;
#33405=VECTOR ( 'NONE', #17573, 39.37007874015748143 ) ;
#33406=DIRECTION ( 'NONE',  ( -3.469446951953613696E-16, 0.000000000000000000, -1.000000000000000000 ) ) ;
#33407=DIRECTION ( 'NONE',  ( -1.000000000000000000, 0.000000000000000000, 1.734723475976806848E-16 ) ) ;
#33408=VECTOR ( 'NONE', #9315, 39.37007874015748143 ) ;
#33410=AXIS2_PLACEMENT_3D ( 'NONE', #8636, #40402, #636 ) ;
#33411=ORIENTED_EDGE ( 'NONE', *, *, #32436, .T. ) ;
#33413=CARTESIAN_POINT ( 'NONE',  ( -1.091055626815042201, 3.346456692913386100, 0.6299212598425164567 ) ) ;
#33414=CARTESIAN_POINT ( 'NONE',  ( 0.5455278134075216556, 0.000000000000000000, 1.692913385826762873 ) ) ;
#33416=DIRECTION ( 'NONE',  ( 0.000000000000000000, 0.000000000000000000, -1.000000000000000000 ) ) ;
#33418=VECTOR ( 'NONE', #47476, 39.37007874015748143 ) ;
#33421=LINE ( 'NONE', #9910, #37354 ) ;
#33422=ORIENTED_EDGE ( 'NONE', *, *, #10803, .T. ) ;
#33424=LINE ( 'NONE', #25150, #34216 ) ;
#33425=DIRECTION ( 'NONE',  ( 0.000000000000000000, 0.000000000000000000, -1.000000000000000000 ) ) ;
#33426=PLANE ( 'NONE',  #26025 ) ;
#33428=ORIENTED_EDGE ( 'NONE', *, *, #7376, .F. ) ;
#33429=VERTEX_POINT ( 'NONE', #14088 ) ;
#33431=DIRECTION ( 'NONE',  ( -1.000000000000000000, 0.000000000000000000, -0.000000000000000000 ) ) ;
#33433=DIRECTION ( 'NONE',  ( 1.734723475976806848E-16, -0.000000000000000000, 1.000000000000000000 ) ) ;
#33434=DIRECTION ( 'NONE',  ( 0.000000000000000000, 1.000000000000000000, 0.000000000000000000 ) ) ;
#33435=DIRECTION ( 'NONE',  ( 1.734723475976806848E-16, 0.000000000000000000, 1.000000000000000000 ) ) ;
#33436=VERTEX_POINT ( 'NONE', #21331 ) ;
#33438=ADVANCED_FACE ( 'NONE', ( #21583 ), #25447, .T. ) ;
#33440=DIRECTION ( 'NONE',  ( -3.469446951953613696E-16, 0.000000000000000000, -1.000000000000000000 ) ) ;
#33441=CARTESIAN_POINT ( 'NONE',  ( 1.287906020515829919, 3.346456692913386100, -1.259842519685035134 ) ) ;
#33442=VERTEX_POINT ( 'NONE', #29322 ) ;
#33444=EDGE_CURVE ( 'NONE', #38287, #24025, #25962, .T. ) ;
#33445=DIRECTION ( 'NONE',  ( 0.000000000000000000, -1.000000000000000000, 0.000000000000000000 ) ) ;
#33446=VECTOR ( 'NONE', #29382, 39.37007874015748143 ) ;
#33447=ORIENTED_EDGE ( 'NONE', *, *, #17112, .F. ) ;
#33450=CIRCLE ( 'NONE', #49035, 2.165354330708661568 ) ;
#33451=ORIENTED_EDGE ( 'NONE', *, *, #32570, .F. ) ;
#33452=ORIENTED_EDGE ( 'NONE', *, *, #9235, .F. ) ;
#33453=CARTESIAN_POINT ( 'NONE',  ( -0.07591351300297277671, 0.000000000000000000, 1.732283464566921172 ) ) ;
#33457=CARTESIAN_POINT ( 'NONE',  ( -0.6214413264104945434, 3.267716535433071279, -1.614173228346451605 ) ) ;
#33459=ORIENTED_EDGE ( 'NONE', *, *, #40902, .T. ) ;
#33460=AXIS2_PLACEMENT_3D ( 'NONE', #32659, #47580, #28760 ) ;
#33461=EDGE_CURVE ( 'NONE', #32285, #48286, #13079, .T. ) ;
#33463=LINE ( 'NONE', #33718, #2867 ) ;
#33464=EDGE_CURVE ( 'NONE', #39618, #24556, #5068, .T. ) ;
#33465=DIRECTION ( 'NONE',  ( 0.000000000000000000, 0.000000000000000000, -1.000000000000000000 ) ) ;
#33467=ADVANCED_FACE ( 'NONE', ( #44549 ), #45551, .F. ) ;
#33468=DIRECTION ( 'NONE',  ( -0.000000000000000000, 1.000000000000000000, -0.000000000000000000 ) ) ;
#33471=DIRECTION ( 'NONE',  ( 1.000000000000000000, 0.000000000000000000, -3.469446951953613696E-16 ) ) ;
#33472=ADVANCED_FACE ( 'NONE', ( #2220 ), #32969, .F. ) ;
#33473=CARTESIAN_POINT ( 'NONE',  ( 1.560669927219591413, 0.000000000000000000, 1.732283464566921172 ) ) ;
#33475=CARTESIAN_POINT ( 'NONE',  ( 0.5455278134075212115, 3.346456692913386100, -1.259842519685035134 ) ) ;
#33476=CARTESIAN_POINT ( 'NONE',  ( 0.1968503937007878568, 3.346456692913386100, 1.259842519685033357 ) ) ;
#33477=VERTEX_POINT ( 'NONE', #17202 ) ;
#33478=CARTESIAN_POINT ( 'NONE',  ( 1.015142113812069313, 3.346456692913386100, -0.4724409448818889246 ) ) ;
#33480=CARTESIAN_POINT ( 'NONE',  ( 1.015142113812069979, 3.267716535433071279, 2.047244094488179567 ) ) ;
#33481=AXIS2_PLACEMENT_3D ( 'NONE', #46415, #18830, #14704 ) ;
#33482=ORIENTED_EDGE ( 'NONE', *, *, #2724, .T. ) ;
#33483=CARTESIAN_POINT ( 'NONE',  ( 0.000000000000000000, 3.267716535433071279, 0.000000000000000000 ) ) ;
#33485=FACE_BOUND ( 'NONE', #23009, .T. ) ;
#33486=VECTOR ( 'NONE', #4641, 39.37007874015748143 ) ;
#33487=DIRECTION ( 'NONE',  ( -1.000000000000000000, 0.000000000000000000, 0.000000000000000000 ) ) ;
#33488=DIRECTION ( 'NONE',  ( 1.000000000000000000, 0.000000000000000000, 0.000000000000000000 ) ) ;
#33489=CARTESIAN_POINT ( 'NONE',  ( -3.927031490892378253E-16, 3.346456692913386100, -2.204724409448811429 ) ) ;
#33491=VECTOR ( 'NONE', #34677, 39.37007874015748143 ) ;
#33492=ORIENTED_EDGE ( 'NONE', *, *, #41032, .F. ) ;
#33496=FACE_OUTER_BOUND ( 'NONE', #37472, .T. ) ;
#33497=ORIENTED_EDGE ( 'NONE', *, *, #4544, .F. ) ;
#33498=DIRECTION ( 'NONE',  ( -0.000000000000000000, 1.000000000000000000, -0.000000000000000000 ) ) ;
#33500=FACE_OUTER_BOUND ( 'NONE', #35323, .T. ) ;
#33501=LINE ( 'NONE', #45837, #42944 ) ;
#33504=ADVANCED_FACE ( 'NONE', ( #13330 ), #18216, .F. ) ;
#33505=CARTESIAN_POINT ( 'NONE',  ( -1.909347346926324906, 3.346456692913386100, -1.102362204724405492 ) ) ;
#33509=VECTOR ( 'NONE', #13511, 39.37007874015748143 ) ;
#33510=ORIENTED_EDGE ( 'NONE', *, *, #4043, .F. ) ;
#33512=DIRECTION ( 'NONE',  ( -0.000000000000000000, 1.000000000000000000, -0.000000000000000000 ) ) ;
#33515=ORIENTED_EDGE ( 'NONE', *, *, #5516, .F. ) ;
#33519=EDGE_CURVE ( 'NONE', #50364, #5669, #10725, .T. ) ;
#33521=DIRECTION ( 'NONE',  ( 1.000000000000000000, 0.000000000000000000, 0.000000000000000000 ) ) ;
#33526=EDGE_LOOP ( 'NONE', ( #45751, #48816, #50149, #12921 ) ) ;
#33529=EDGE_CURVE ( 'NONE', #6756, #3555, #2718, .T. ) ;
#33530=CARTESIAN_POINT ( 'NONE',  ( -1.091055626815042201, 3.346456692913386100, 0.6299212598425164567 ) ) ;
#33531=DIRECTION ( 'NONE',  ( 1.734723475976806848E-16, -0.000000000000000000, 1.000000000000000000 ) ) ;
#33533=CARTESIAN_POINT ( 'NONE',  ( 3.927031490892378253E-16, 3.267716535433071279, 0.7480314960629874665 ) ) ;
#33534=ORIENTED_EDGE ( 'NONE', *, *, #35642, .T. ) ;
#33535=DIRECTION ( 'NONE',  ( 0.000000000000000000, 1.000000000000000000, 0.000000000000000000 ) ) ;
#33536=CARTESIAN_POINT ( 'NONE',  ( -1.712496953225537633, 0.000000000000000000, -1.102362204724405492 ) ) ;
#33538=LINE ( 'NONE', #40760, #30045 ) ;
#33540=EDGE_CURVE ( 'NONE', #31998, #24393, #46313, .T. ) ;
#33544=DIRECTION ( 'NONE',  ( -1.000000000000000000, 0.000000000000000000, 1.734723475976806848E-16 ) ) ;
#33545=CARTESIAN_POINT ( 'NONE',  ( 1.833433833923350686, 3.267716535433071279, -6.361001426713997494E-16 ) ) ;
#33547=VECTOR ( 'NONE', #31795, 39.37007874015748143 ) ;
#33548=DIRECTION ( 'NONE',  ( -1.000000000000000000, 0.000000000000000000, 0.000000000000000000 ) ) ;
#33549=VECTOR ( 'NONE', #17502, 39.37007874015748143 ) ;
#33550=ORIENTED_EDGE ( 'NONE', *, *, #25132, .T. ) ;
#33551=CARTESIAN_POINT ( 'NONE',  ( -0.2727639067037607723, 0.000000000000000000, 0.1574803149606283648 ) ) ;
#33553=ORIENTED_EDGE ( 'NONE', *, *, #11322, .F. ) ;
#33555=LINE ( 'NONE', #8827, #12019 ) ;
#33556=VERTEX_POINT ( 'NONE', #11481 ) ;
#33557=CARTESIAN_POINT ( 'NONE',  ( -1.299212598425205423, 3.346456692913386100, -1.732283464566922726 ) ) ;
#33560=VECTOR ( 'NONE', #17673, 39.37007874015748143 ) ;
#33561=LINE ( 'NONE', #29675, #48585 ) ;
#33562=VERTEX_POINT ( 'NONE', #18473 ) ;
#33563=EDGE_CURVE ( 'NONE', #10447, #49658, #7104, .T. ) ;
#33566=FACE_BOUND ( 'NONE', #46039, .T. ) ;
#33567=ORIENTED_EDGE ( 'NONE', *, *, #50057, .F. ) ;
#33568=EDGE_CURVE ( 'NONE', #24413, #1162, #31104, .T. ) ;
#33570=DIRECTION ( 'NONE',  ( -1.000000000000000000, 0.000000000000000000, 0.000000000000000000 ) ) ;
#33571=ADVANCED_FACE ( 'NONE', ( #46561 ), #50410, .F. ) ;
#33573=ORIENTED_EDGE ( 'NONE', *, *, #49982, .T. ) ;
#33574=ORIENTED_EDGE ( 'NONE', *, *, #22909, .T. ) ;
#33575=CARTESIAN_POINT ( 'NONE',  ( 0.000000000000000000, 3.267716535433071279, -0.3543307086614178592 ) ) ;
#33576=CARTESIAN_POINT ( 'NONE',  ( -1.166969139818015977, 0.000000000000000000, -1.417322834645664109 ) ) ;
#33577=EDGE_LOOP ( 'NONE', ( #49642, #43570, #31517, #36778 ) ) ;
#33578=EDGE_LOOP ( 'NONE', ( #14825, #9526, #12258, #32377 ) ) ;
#33580=DIRECTION ( 'NONE',  ( -0.000000000000000000, 1.000000000000000000, -0.000000000000000000 ) ) ;
#33582=EDGE_CURVE ( 'NONE', #2713, #41904, #3220, .T. ) ;
#33585=PLANE ( 'NONE',  #7403 ) ;
#33590=LINE ( 'NONE', #2583, #33719 ) ;
#33591=CARTESIAN_POINT ( 'NONE',  ( -0.5455278134075208785, 0.000000000000000000, 1.692913385826762873 ) ) ;
#33592=ADVANCED_FACE ( 'NONE', ( #14597 ), #2976, .F. ) ;
#33593=PLANE ( 'NONE',  #49000 ) ;
#33597=CARTESIAN_POINT ( 'NONE',  ( -1.166969139818015977, 3.346456692913386100, -1.753476375576570323 ) ) ;
#33598=ORIENTED_EDGE ( 'NONE', *, *, #27176, .T. ) ;
#33599=PLANE ( 'NONE',  #40739 ) ;
#33601=VECTOR ( 'NONE', #39979, 39.37007874015748143 ) ;
#33602=ORIENTED_EDGE ( 'NONE', *, *, #15352, .F. ) ;
#33603=EDGE_CURVE ( 'NONE', #24456, #15064, #18970, .T. ) ;
#33604=ORIENTED_EDGE ( 'NONE', *, *, #32007, .F. ) ;
#33605=FACE_OUTER_BOUND ( 'NONE', #28632, .T. ) ;
#33606=VERTEX_POINT ( 'NONE', #46064 ) ;
#33607=ADVANCED_FACE ( 'NONE', ( #38352 ), #18727, .F. ) ;
#33608=ORIENTED_EDGE ( 'NONE', *, *, #36996, .F. ) ;
#33609=DIRECTION ( 'NONE',  ( 1.734723475976806848E-16, 0.000000000000000000, 1.000000000000000000 ) ) ;
#33613=VECTOR ( 'NONE', #15815, 39.37007874015748143 ) ;
#33614=VECTOR ( 'NONE', #41843, 39.37007874015748143 ) ;
#33615=ORIENTED_EDGE ( 'NONE', *, *, #42715, .F. ) ;
#33616=ORIENTED_EDGE ( 'NONE', *, *, #34764, .F. ) ;
#33618=EDGE_LOOP ( 'NONE', ( #24505, #42052, #21130, #48712 ) ) ;
#33619=ORIENTED_EDGE ( 'NONE', *, *, #15843, .F. ) ;
#33620=LINE ( 'NONE', #17602, #5047 ) ;
#33621=CARTESIAN_POINT ( 'NONE',  ( -0.6214413264104945434, 3.346456692913386100, -2.074263738136479240 ) ) ;
#33623=EDGE_CURVE ( 'NONE', #40629, #30339, #26715, .T. ) ;
#33624=VERTEX_POINT ( 'NONE', #30852 ) ;
#33628=EDGE_CURVE ( 'NONE', #20757, #43312, #7358, .T. ) ;
#33629=VERTEX_POINT ( 'NONE', #28228 ) ;
#33631=DIRECTION ( 'NONE',  ( -1.000000000000000000, 0.000000000000000000, 1.734723475976806848E-16 ) ) ;
#33632=CARTESIAN_POINT ( 'NONE',  ( -1.536664496436148184E-16, 3.267716535433071279, -1.141732283464564013 ) ) ;
#33633=ORIENTED_EDGE ( 'NONE', *, *, #43554, .T. ) ;
#33634=VERTEX_POINT ( 'NONE', #8369 ) ;
#33638=DIRECTION ( 'NONE',  ( -0.000000000000000000, 1.000000000000000000, -0.000000000000000000 ) ) ;
#33641=ORIENTED_EDGE ( 'NONE', *, *, #22981, .F. ) ;
#33643=ORIENTED_EDGE ( 'NONE', *, *, #33219, .T. ) ;
#33644=CARTESIAN_POINT ( 'NONE',  ( 1.091055626815042423, 3.267716535433071279, -1.892679809432644143E-16 ) ) ;
#33645=CARTESIAN_POINT ( 'NONE',  ( 0.000000000000000000, 3.267716535433071279, 0.4724409448818871482 ) ) ;
#33646=VECTOR ( 'NONE', #28498, 39.37007874015748143 ) ;
#33648=EDGE_CURVE ( 'NONE', #7189, #44444, #20495, .T. ) ;
#33650=FACE_OUTER_BOUND ( 'NONE', #17077, .T. ) ;
#33652=ORIENTED_EDGE ( 'NONE', *, *, #4765, .F. ) ;
#33654=CARTESIAN_POINT ( 'NONE',  ( -1.909347346926324462, 0.000000000000000000, 0.4724409448818871482 ) ) ;
#33655=VECTOR ( 'NONE', #2057, 39.37007874015748143 ) ;
#33656=DIRECTION ( 'NONE',  ( -1.000000000000000000, 0.000000000000000000, 1.734723475976806848E-16 ) ) ;
#33658=EDGE_LOOP ( 'NONE', ( #49430, #42126, #18305, #37826 ) ) ;
#33659=VECTOR ( 'NONE', #34366, 39.37007874015748143 ) ;
#33660=LINE ( 'NONE', #17387, #33965 ) ;
#33663=PLANE ( 'NONE',  #30455 ) ;
#33668=B_SPLINE_CURVE_WITH_KNOTS ( 'NONE', 3,
 ( #15058, #46021, #26919, #30805 ),
 .UNSPECIFIED., .F., .F.,
 ( 4, 4 ),
 ( 0.01169383523547795622, 0.01426672609628482080 ),
 .UNSPECIFIED. ) ;
#33669=EDGE_CURVE ( 'NONE', #1365, #36675, #35230, .T. ) ;
#33670=ORIENTED_EDGE ( 'NONE', *, *, #40507, .F. ) ;
#33673=ORIENTED_EDGE ( 'NONE', *, *, #47720, .F. ) ;
#33674=VECTOR ( 'NONE', #40115, 39.37007874015748143 ) ;
#33676=EDGE_CURVE ( 'NONE', #25851, #38575, #3731, .T. ) ;
#33677=LINE ( 'NONE', #40898, #11928 ) ;
#33678=FACE_OUTER_BOUND ( 'NONE', #9354, .T. ) ;
#33679=CARTESIAN_POINT ( 'NONE',  ( 0.000000000000000000, 0.000000000000000000, 0.000000000000000000 ) ) ;
#33681=EDGE_LOOP ( 'NONE', ( #26567, #5841, #30945, #26248 ) ) ;
#33682=EDGE_LOOP ( 'NONE', ( #48692, #8, #31036, #46140 ) ) ;
#33684=CARTESIAN_POINT ( 'NONE',  ( 0.8182917201112817063, 3.346456692913386100, -1.614173228346451605 ) ) ;
#33686=DIRECTION ( 'NONE',  ( -0.000000000000000000, 1.000000000000000000, -0.000000000000000000 ) ) ;
#33687=CARTESIAN_POINT ( 'NONE',  ( 0.1968503937007872462, 3.267716535433071279, -1.771653543307081025 ) ) ;
#33688=LINE ( 'NONE', #9673, #11279 ) ;
#33689=EDGE_CURVE ( 'NONE', #14887, #14557, #4234, .T. ) ;
#33690=EDGE_LOOP ( 'NONE', ( #36866, #4479, #37653, #29351 ) ) ;
#33691=VERTEX_POINT ( 'NONE', #47052 ) ;
#33694=VECTOR ( 'NONE', #43801, 39.37007874015748143 ) ;
#33695=DIRECTION ( 'NONE',  ( -3.469446951953613696E-16, 0.000000000000000000, -1.000000000000000000 ) ) ;
#33700=ORIENTED_EDGE ( 'NONE', *, *, #14212, .T. ) ;
#33701=ADVANCED_FACE ( 'NONE', ( #43461 ), #16112, .F. ) ;
#33702=DIRECTION ( 'NONE',  ( -0.000000000000000000, 1.000000000000000000, -0.000000000000000000 ) ) ;
#33705=VERTEX_POINT ( 'NONE', #43207 ) ;
#33706=PLANE ( 'NONE',  #22952 ) ;
#33709=VECTOR ( 'NONE', #21979, 39.37007874015748143 ) ;
#33710=ORIENTED_EDGE ( 'NONE', *, *, #13585, .T. ) ;
#33712=EDGE_CURVE ( 'NONE', #10053, #17342, #101, .T. ) ;
#33714=DIRECTION ( 'NONE',  ( -0.000000000000000000, 1.000000000000000000, -0.000000000000000000 ) ) ;
#33715=ORIENTED_EDGE ( 'NONE', *, *, #40374, .F. ) ;
#33718=CARTESIAN_POINT ( 'NONE',  ( -1.439733046521776583, 3.346456692913386100, 1.537421584259135443 ) ) ;
#33719=VECTOR ( 'NONE', #18331, 39.37007874015748143 ) ;
#33720=DIRECTION ( 'NONE',  ( -0.000000000000000000, 0.000000000000000000, 1.000000000000000000 ) ) ;
#33721=DIRECTION ( 'NONE',  ( -1.000000000000000000, -0.000000000000000000, -0.000000000000000000 ) ) ;
#33723=ORIENTED_EDGE ( 'NONE', *, *, #32297, .F. ) ;
#33725=CARTESIAN_POINT ( 'NONE',  ( -0.5455278134075208785, 0.000000000000000000, 1.889763779527550369 ) ) ;
#33727=FACE_OUTER_BOUND ( 'NONE', #42460, .T. ) ;
#33728=ADVANCED_FACE ( 'NONE', ( #8110 ), #24371, .F. ) ;
#33730=ORIENTED_EDGE ( 'NONE', *, *, #1274, .F. ) ;
#33731=LINE ( 'NONE', #46068, #40289 ) ;
#33733=DIRECTION ( 'NONE',  ( -1.000000000000000000, 0.000000000000000000, -0.000000000000000000 ) ) ;
#33736=EDGE_LOOP ( 'NONE', ( #32714, #2024, #37149, #34517 ) ) ;
#33737=CARTESIAN_POINT ( 'NONE',  ( -1.985260859929298016, 0.000000000000000000, -0.6299212598425177889 ) ) ;
#33739=CARTESIAN_POINT ( 'NONE',  ( -1.909347346926324462, 0.000000000000000000, 0.4724409448818871482 ) ) ;
#33741=VECTOR ( 'NONE', #10180, 39.37007874015748143 ) ;
#33743=CARTESIAN_POINT ( 'NONE',  ( -0.2727639067037607723, 0.000000000000000000, 2.362204724409437961 ) ) ;
#33744=CARTESIAN_POINT ( 'NONE',  ( -1.985260859929297794, 0.000000000000000000, 0.1181102362204704270 ) ) ;
#33745=VECTOR ( 'NONE', #29443, 39.37007874015748143 ) ;
#33746=ORIENTED_EDGE ( 'NONE', *, *, #34362, .F. ) ;
#33747=ORIENTED_EDGE ( 'NONE', *, *, #30302, .F. ) ;
#33749=EDGE_CURVE ( 'NONE', #5813, #25880, #16375, .T. ) ;
#33750=VECTOR ( 'NONE', #11726, 39.37007874015748143 ) ;
#33752=ORIENTED_EDGE ( 'NONE', *, *, #50034, .T. ) ;
#33753=DIRECTION ( 'NONE',  ( -3.469446951953613696E-16, 0.000000000000000000, -1.000000000000000000 ) ) ;
#33755=ORIENTED_EDGE ( 'NONE', *, *, #9388, .F. ) ;
#33759=EDGE_LOOP ( 'NONE', ( #2236, #29909, #9501, #37486 ) ) ;
#33761=EDGE_CURVE ( 'NONE', #42844, #13877, #42953, .T. ) ;
#33764=ORIENTED_EDGE ( 'NONE', *, *, #3770, .T. ) ;
#33766=EDGE_LOOP ( 'NONE', ( #6127, #46958, #47527, #29607 ) ) ;
#33767=DIRECTION ( 'NONE',  ( 0.000000000000000000, 0.000000000000000000, 1.000000000000000000 ) ) ;
#33768=ORIENTED_EDGE ( 'NONE', *, *, #29269, .F. ) ;
#33769=DIRECTION ( 'NONE',  ( -0.000000000000000000, 1.000000000000000000, -0.000000000000000000 ) ) ;
#33771=AXIS2_PLACEMENT_3D ( 'NONE', #21028, #9149, #24898 ) ;
#33772=CARTESIAN_POINT ( 'NONE',  ( -1.363819533518803473, 0.000000000000000000, -1.417322834645664109 ) ) ;
#33774=VECTOR ( 'NONE', #49855, 39.37007874015748143 ) ;
#33775=DIRECTION ( 'NONE',  ( 1.000000000000000000, 0.000000000000000000, 0.000000000000000000 ) ) ;
#33776=CARTESIAN_POINT ( 'NONE',  ( -0.2727639067037602172, 3.346456692913386100, 1.417322834645662777 ) ) ;
#33777=ORIENTED_EDGE ( 'NONE', *, *, #33266, .F. ) ;
#33779=LINE ( 'NONE', #21633, #39837 ) ;
#33780=VECTOR ( 'NONE', #813, 39.37007874015748143 ) ;
#33781=LINE ( 'NONE', #34027, #7873 ) ;
#33783=ORIENTED_EDGE ( 'NONE', *, *, #21768, .F. ) ;
#33784=DIRECTION ( 'NONE',  ( -0.000000000000000000, 1.000000000000000000, -0.000000000000000000 ) ) ;
#33785=DIRECTION ( 'NONE',  ( 1.734723475976806848E-16, -0.000000000000000000, 1.000000000000000000 ) ) ;
#33786=VERTEX_POINT ( 'NONE', #17898 ) ;
#33787=LINE ( 'NONE', #18025, #44401 ) ;
#33788=DIRECTION ( 'NONE',  ( -0.000000000000000000, 1.000000000000000000, -0.000000000000000000 ) ) ;
#33789=EDGE_CURVE ( 'NONE', #17493, #9684, #41148, .T. ) ;
#33795=EDGE_CURVE ( 'NONE', #23374, #3496, #21514, .T. ) ;
#33796=DIRECTION ( 'NONE',  ( -1.000000000000000000, 0.000000000000000000, -0.000000000000000000 ) ) ;
#33797=LINE ( 'NONE', #4504, #30362 ) ;
#33798=DIRECTION ( 'NONE',  ( -1.000000000000000000, 0.000000000000000000, -0.000000000000000000 ) ) ;
#33799=LINE ( 'NONE', #30670, #37641 ) ;
#33800=AXIS2_PLACEMENT_3D ( 'NONE', #46701, #11369, #42848 ) ;
#33801=ORIENTED_EDGE ( 'NONE', *, *, #33628, .T. ) ;
#33805=LINE ( 'NONE', #24571, #30361 ) ;
#33807=CARTESIAN_POINT ( 'NONE',  ( -0.8182917201112814842, 3.346456692913386100, 0.9055118110236167750 ) ) ;
#33808=DIRECTION ( 'NONE',  ( 1.734723475976806848E-16, 0.000000000000000000, 1.000000000000000000 ) ) ;
#33809=EDGE_LOOP ( 'NONE', ( #1258, #45445, #21272, #29501 ) ) ;
#33810=VECTOR ( 'NONE', #31015, 39.37007874015748143 ) ;
#33813=LINE ( 'NONE', #45894, #40572 ) ;
#33814=DIRECTION ( 'NONE',  ( 1.000000000000000000, 0.000000000000000000, 0.000000000000000000 ) ) ;
#33815=ORIENTED_EDGE ( 'NONE', *, *, #30942, .F. ) ;
#33816=ORIENTED_EDGE ( 'NONE', *, *, #7315, .F. ) ;
#33817=ADVANCED_FACE ( 'NONE', ( #5513 ), #9646, .F. ) ;
#33819=FACE_BOUND ( 'NONE', #3896, .T. ) ;
#33820=ORIENTED_EDGE ( 'NONE', *, *, #37018, .F. ) ;
#33823=CARTESIAN_POINT ( 'NONE',  ( -1.091055626815042867, 3.267716535433071279, 1.892679809432645129E-16 ) ) ;
#33826=DIRECTION ( 'NONE',  ( -0.000000000000000000, 1.000000000000000000, -0.000000000000000000 ) ) ;
#33828=ORIENTED_EDGE ( 'NONE', *, *, #32208, .F. ) ;
#33831=PLANE ( 'NONE',  #20253 ) ;
#33832=PLANE ( 'NONE',  #5191 ) ;
#33834=DIRECTION ( 'NONE',  ( -0.000000000000000000, 1.000000000000000000, -0.000000000000000000 ) ) ;
#33837=ORIENTED_EDGE ( 'NONE', *, *, #13702, .T. ) ;
#33838=CARTESIAN_POINT ( 'NONE',  ( -1.091055626815042201, 0.000000000000000000, 0.1181102362204705658 ) ) ;
#33840=CARTESIAN_POINT ( 'NONE',  ( -1.091055626815042645, 0.000000000000000000, 2.007874015748021268 ) ) ;
#33842=DIRECTION ( 'NONE',  ( -0.000000000000000000, 1.000000000000000000, -0.000000000000000000 ) ) ;
#33843=VECTOR ( 'NONE', #10260, 39.37007874015748143 ) ;
#33844=AXIS2_PLACEMENT_3D ( 'NONE', #23322, #39330, #31084 ) ;
#33845=DIRECTION ( 'NONE',  ( -0.000000000000000000, 1.000000000000000000, -0.000000000000000000 ) ) ;
#33847=ADVANCED_FACE ( 'NONE', ( #40886 ), #8874, .F. ) ;
#33848=ORIENTED_EDGE ( 'NONE', *, *, #12198, .F. ) ;
#33849=DIRECTION ( 'NONE',  ( -0.000000000000000000, 1.000000000000000000, -0.000000000000000000 ) ) ;
#33850=LINE ( 'NONE', #13964, #48262 ) ;
#33851=EDGE_CURVE ( 'NONE', #29709, #37961, #33660, .T. ) ;
#33852=VECTOR ( 'NONE', #24263, 39.37007874015748143 ) ;
#33854=EDGE_CURVE ( 'NONE', #28852, #15326, #5252, .T. ) ;
#33855=VERTEX_POINT ( 'NONE', #44235 ) ;
#33857=ORIENTED_EDGE ( 'NONE', *, *, #47394, .F. ) ;
#33858=ADVANCED_FACE ( 'NONE', ( #1382 ), #37531, .F. ) ;
#33860=ORIENTED_EDGE ( 'NONE', *, *, #32499, .F. ) ;
#33861=LINE ( 'NONE', #41846, #35303 ) ;
#33862=VERTEX_POINT ( 'NONE', #33153 ) ;
#33863=DIRECTION ( 'NONE',  ( -1.000000000000000000, -0.000000000000000000, -0.000000000000000000 ) ) ;
#33864=DIRECTION ( 'NONE',  ( -1.000000000000000000, -0.000000000000000000, -0.000000000000000000 ) ) ;
#33865=EDGE_CURVE ( 'NONE', #18980, #39410, #45236, .T. ) ;
#33868=ORIENTED_EDGE ( 'NONE', *, *, #17227, .T. ) ;
#33869=CARTESIAN_POINT ( 'NONE',  ( 1.363819533518803251, 3.346456692913386100, 1.102362204724403938 ) ) ;
#33871=ORIENTED_EDGE ( 'NONE', *, *, #42836, .T. ) ;
#33872=EDGE_CURVE ( 'NONE', #33855, #30686, #13519, .T. ) ;
#33879=DIRECTION ( 'NONE',  ( -0.000000000000000000, 1.000000000000000000, -0.000000000000000000 ) ) ;
#33881=CARTESIAN_POINT ( 'NONE',  ( 1.909347346926324462, 3.346456692913386100, -0.8893194486674360633 ) ) ;
#33883=PLANE ( 'NONE',  #20778 ) ;
#33884=LINE ( 'NONE', #10379, #30188 ) ;
#33885=FACE_OUTER_BOUND ( 'NONE', #5189, .T. ) ;
#33886=ORIENTED_EDGE ( 'NONE', *, *, #28848, .T. ) ;
#33887=ORIENTED_EDGE ( 'NONE', *, *, #49831, .F. ) ;
#33888=VECTOR ( 'NONE', #48416, 39.37007874015748143 ) ;
#33889=EDGE_CURVE ( 'NONE', #46463, #13286, #29256, .T. ) ;
#33890=DIRECTION ( 'NONE',  ( -0.000000000000000000, 1.000000000000000000, -0.000000000000000000 ) ) ;
#33892=LINE ( 'NONE', #6764, #19699 ) ;
#33893=ORIENTED_EDGE ( 'NONE', *, *, #1603, .F. ) ;
#33894=EDGE_LOOP ( 'NONE', ( #46267, #2548, #16454, #20439 ) ) ;
#33895=DIRECTION ( 'NONE',  ( 0.000000000000000000, 0.000000000000000000, -1.000000000000000000 ) ) ;
#33897=CARTESIAN_POINT ( 'NONE',  ( 0.5455278134075216556, 3.346456692913386100, 1.062992125984246083 ) ) ;
#33898=DIRECTION ( 'NONE',  ( 0.000000000000000000, 0.000000000000000000, -1.000000000000000000 ) ) ;
#33901=CARTESIAN_POINT ( 'NONE',  ( -0.07591351300297277671, 3.267716535433071279, 1.417322834645662777 ) ) ;
#33905=DIRECTION ( 'NONE',  ( -0.000000000000000000, 1.000000000000000000, -0.000000000000000000 ) ) ;
#33906=EDGE_CURVE ( 'NONE', #42620, #4245, #21773, .T. ) ;
#33908=ORIENTED_EDGE ( 'NONE', *, *, #32270, .T. ) ;
#33909=CARTESIAN_POINT ( 'NONE',  ( 0.000000000000000000, 3.346456692913386100, 0.000000000000000000 ) ) ;
#33912=CARTESIAN_POINT ( 'NONE',  ( -2.182111253630085290, 0.000000000000000000, -6.146657985744592735E-16 ) ) ;
#33913=EDGE_CURVE ( 'NONE', #28182, #50367, #28743, .T. ) ;
#33914=VERTEX_POINT ( 'NONE', #1122 ) ;
#33917=ORIENTED_EDGE ( 'NONE', *, *, #33789, .F. ) ;
#33918=DIRECTION ( 'NONE',  ( -1.000000000000000000, -0.000000000000000000, -0.000000000000000000 ) ) ;
#33920=CARTESIAN_POINT ( 'NONE',  ( -0.8182917201112819283, 0.000000000000000000, 0.1574803149606285035 ) ) ;
#33922=DIRECTION ( 'NONE',  ( -3.469446951953613696E-16, 0.000000000000000000, -1.000000000000000000 ) ) ;
#33923=VECTOR ( 'NONE', #7663, 39.37007874015748143 ) ;
#33925=DIRECTION ( 'NONE',  ( -1.000000000000000000, -0.000000000000000000, -0.000000000000000000 ) ) ;
#33926=DIRECTION ( 'NONE',  ( -1.000000000000000000, 0.000000000000000000, -0.000000000000000000 ) ) ;
#33927=VERTEX_POINT ( 'NONE', #22529 ) ;
#33928=ORIENTED_EDGE ( 'NONE', *, *, #42702, .T. ) ;
#33931=VERTEX_POINT ( 'NONE', #14275 ) ;
#33932=DIRECTION ( 'NONE',  ( 0.000000000000000000, 0.000000000000000000, -1.000000000000000000 ) ) ;
#33933=CARTESIAN_POINT ( 'NONE',  ( -0.9302092402134520821, 3.346456692913386100, -1.889763779527552146 ) ) ;
#33934=LINE ( 'NONE', #37557, #36836 ) ;
#33937=DIRECTION ( 'NONE',  ( -1.000000000000000000, 0.000000000000000000, 1.734723475976806848E-16 ) ) ;
#33939=ADVANCED_FACE ( 'NONE', ( #49848 ), #18154, .F. ) ;
#33940=DIRECTION ( 'NONE',  ( 1.734723475976806848E-16, -0.000000000000000000, 1.000000000000000000 ) ) ;
#33941=ORIENTED_EDGE ( 'NONE', *, *, #39602, .F. ) ;
#33943=FACE_BOUND ( 'NONE', #17688, .T. ) ;
#33945=DIRECTION ( 'NONE',  ( 1.000000000000000000, -0.000000000000000000, 0.000000000000000000 ) ) ;
#33946=VERTEX_POINT ( 'NONE', #38292 ) ;
#33947=ORIENTED_EDGE ( 'NONE', *, *, #21611, .T. ) ;
#33948=DIRECTION ( 'NONE',  ( 1.734723475976806848E-16, -0.000000000000000000, 1.000000000000000000 ) ) ;
#33950=ADVANCED_FACE ( 'NONE', ( #14024 ), #14535, .F. ) ;
#33951=VECTOR ( 'NONE', #9709, 39.37007874015748143 ) ;
#33953=VECTOR ( 'NONE', #44009, 39.37007874015748143 ) ;
#33954=ORIENTED_EDGE ( 'NONE', *, *, #22914, .T. ) ;
#33957=ORIENTED_EDGE ( 'NONE', *, *, #1374, .T. ) ;
#33961=ORIENTED_EDGE ( 'NONE', *, *, #9337, .T. ) ;
#33963=DIRECTION ( 'NONE',  ( 0.000000000000000000, 1.000000000000000000, 0.000000000000000000 ) ) ;
#33964=EDGE_CURVE ( 'NONE', #3242, #26125, #46000, .T. ) ;
#33965=VECTOR ( 'NONE', #12755, 39.37007874015748143 ) ;
#33966=CARTESIAN_POINT ( 'NONE',  ( 1.015142113812069313, 3.267716535433071279, 0.5905511811023579360 ) ) ;
#33968=DIRECTION ( 'NONE',  ( 1.734723475976806848E-16, 0.000000000000000000, 1.000000000000000000 ) ) ;
#33969=ORIENTED_EDGE ( 'NONE', *, *, #45874, .F. ) ;
#33971=DIRECTION ( 'NONE',  ( -0.000000000000000000, 0.000000000000000000, 1.000000000000000000 ) ) ;
#33972=ADVANCED_FACE ( 'NONE', ( #7293 ), #42144, .F. ) ;
#33973=ORIENTED_EDGE ( 'NONE', *, *, #29220, .F. ) ;
#33974=CARTESIAN_POINT ( 'NONE',  ( 1.636583440222563635, 0.000000000000000000, -1.259842519685035800 ) ) ;
#33975=LINE ( 'NONE', #17712, #47478 ) ;
#33977=DIRECTION ( 'NONE',  ( -1.000000000000000000, 0.000000000000000000, 0.000000000000000000 ) ) ;
#33978=EDGE_CURVE ( 'NONE', #16368, #15591, #41648, .T. ) ;
#33979=CARTESIAN_POINT ( 'NONE',  ( 0.8455406139730251569, 3.346456692913386100, -1.929133858267711110 ) ) ;
#33980=EDGE_CURVE ( 'NONE', #21949, #26003, #38092, .T. ) ;
#33982=ORIENTED_EDGE ( 'NONE', *, *, #28395, .T. ) ;
#33983=CARTESIAN_POINT ( 'NONE',  ( 0.2727639067037602172, 3.346456692913386100, -2.047244094488182231 ) ) ;
#33985=FACE_BOUND ( 'NONE', #46349, .T. ) ;
#33988=AXIS2_PLACEMENT_3D ( 'NONE', #18374, #37246, #29740 ) ;
#33989=DIRECTION ( 'NONE',  ( -0.000000000000000000, 1.000000000000000000, -0.000000000000000000 ) ) ;
#33992=VERTEX_POINT ( 'NONE', #45743 ) ;
#33994=FACE_OUTER_BOUND ( 'NONE', #10935, .T. ) ;
#33995=VECTOR ( 'NONE', #26435, 39.37007874015748143 ) ;
#33996=DIRECTION ( 'NONE',  ( -0.000000000000000000, 1.000000000000000000, -0.000000000000000000 ) ) ;
#34000=ORIENTED_EDGE ( 'NONE', *, *, #11960, .T. ) ;
#34001=LINE ( 'NONE', #17482, #35662 ) ;
#34002=EDGE_CURVE ( 'NONE', #33327, #7706, #10407, .T. ) ;
#34003=LINE ( 'NONE', #22623, #1726 ) ;
#34006=VERTEX_POINT ( 'NONE', #29770 ) ;
#34007=ORIENTED_EDGE ( 'NONE', *, *, #23002, .T. ) ;
#34009=ADVANCED_FACE ( 'NONE', ( #10149 ), #46247, .F. ) ;
#34011=ORIENTED_EDGE ( 'NONE', *, *, #1367, .F. ) ;
#34012=ORIENTED_EDGE ( 'NONE', *, *, #34821, .F. ) ;
#34014=EDGE_LOOP ( 'NONE', ( #27905, #47951, #27806, #13730 ) ) ;
#34015=CARTESIAN_POINT ( 'NONE',  ( -1.166969139818015977, 0.000000000000000000, 1.732283464566920950 ) ) ;
#34019=VECTOR ( 'NONE', #49187, 39.37007874015748143 ) ;
#34020=LINE ( 'NONE', #41259, #49153 ) ;
#34023=CARTESIAN_POINT ( 'NONE',  ( 1.560669927219590747, 0.000000000000000000, -0.1574803149606304187 ) ) ;
#34024=CARTESIAN_POINT ( 'NONE',  ( 0.000000000000000000, 3.346456692913386100, 0.000000000000000000 ) ) ;
#34026=EDGE_CURVE ( 'NONE', #14063, #39780, #2658, .T. ) ;
#34027=CARTESIAN_POINT ( 'NONE',  ( -1.636583440222564301, 0.000000000000000000, 1.574803149606291530 ) ) ;
#34028=LINE ( 'NONE', #49716, #36372 ) ;
#34029=AXIS2_PLACEMENT_3D ( 'NONE', #28981, #5502, #21248 ) ;
#34030=VECTOR ( 'NONE', #5434, 39.37007874015748143 ) ;
#34031=VERTEX_POINT ( 'NONE', #7040 ) ;
#34032=DIRECTION ( 'NONE',  ( -0.000000000000000000, 1.000000000000000000, -0.000000000000000000 ) ) ;
#34035=LINE ( 'NONE', #41515, #41109 ) ;
#34038=ADVANCED_FACE ( 'NONE', ( #15037 ), #30784, .F. ) ;
#34039=EDGE_LOOP ( 'NONE', ( #36380, #14664, #6412, #45615 ) ) ;
#34041=EDGE_LOOP ( 'NONE', ( #29286, #49359, #2604, #17256 ) ) ;
#34042=FACE_OUTER_BOUND ( 'NONE', #37833, .T. ) ;
#34043=DIRECTION ( 'NONE',  ( -0.000000000000000000, 1.000000000000000000, -0.000000000000000000 ) ) ;
#34044=CARTESIAN_POINT ( 'NONE',  ( 0.4696143004045478797, 3.267716535433071279, -0.9842519685039348154 ) ) ;
#34047=EDGE_LOOP ( 'NONE', ( #20989, #10152, #34169, #20559 ) ) ;
#34048=DIRECTION ( 'NONE',  ( 1.734723475976806848E-16, -0.000000000000000000, 1.000000000000000000 ) ) ;
#34050=ORIENTED_EDGE ( 'NONE', *, *, #43889, .F. ) ;
#34053=FACE_OUTER_BOUND ( 'NONE', #19405, .T. ) ;
#34054=PLANE ( 'NONE',  #9556 ) ;
#34055=ORIENTED_EDGE ( 'NONE', *, *, #17357, .T. ) ;
#34057=DIRECTION ( 'NONE',  ( 0.000000000000000000, 0.000000000000000000, 1.000000000000000000 ) ) ;
#34061=ORIENTED_EDGE ( 'NONE', *, *, #28138, .T. ) ;
#34062=FACE_OUTER_BOUND ( 'NONE', #40312, .T. ) ;
#34063=FACE_BOUND ( 'NONE', #36344, .T. ) ;
#34064=ORIENTED_EDGE ( 'NONE', *, *, #26390, .F. ) ;
#34065=AXIS2_PLACEMENT_3D ( 'NONE', #12151, #20921, #25049 ) ;
#34066=VECTOR ( 'NONE', #48764, 39.37007874015748143 ) ;
#34067=DIRECTION ( 'NONE',  ( 0.000000000000000000, -1.000000000000000000, 0.000000000000000000 ) ) ;
#34070=ORIENTED_EDGE ( 'NONE', *, *, #30981, .F. ) ;
#34071=VERTEX_POINT ( 'NONE', #11417 ) ;
#34072=DIRECTION ( 'NONE',  ( -0.000000000000000000, 1.000000000000000000, -0.000000000000000000 ) ) ;
#34073=EDGE_CURVE ( 'NONE', #30262, #30424, #35420, .T. ) ;
#34079=DIRECTION ( 'NONE',  ( -3.469446951953613696E-16, 0.000000000000000000, -1.000000000000000000 ) ) ;
#34080=CARTESIAN_POINT ( 'NONE',  ( -2.182111253630085290, 3.267716535433071279, -0.3149606299212589500 ) ) ;
#34081=DIRECTION ( 'NONE',  ( 1.000000000000000000, 0.000000000000000000, -3.469446951953613696E-16 ) ) ;
#34082=DIRECTION ( 'NONE',  ( 1.000000000000000000, 0.000000000000000000, -3.469446951953613696E-16 ) ) ;
#34083=ORIENTED_EDGE ( 'NONE', *, *, #1975, .T. ) ;
#34084=ORIENTED_EDGE ( 'NONE', *, *, #31225, .F. ) ;
#34086=DIRECTION ( 'NONE',  ( 1.000000000000000000, 0.000000000000000000, 0.000000000000000000 ) ) ;
#34088=EDGE_CURVE ( 'NONE', #50026, #49624, #35928, .T. ) ;
#34089=CARTESIAN_POINT ( 'NONE',  ( 3.927031490892378253E-16, 3.346456692913386100, 2.007874015748021268 ) ) ;
#34090=CARTESIAN_POINT ( 'NONE',  ( 3.927031490892378253E-16, 0.000000000000000000, 0.7480314960629874665 ) ) ;
#34091=EDGE_CURVE ( 'NONE', #8095, #39490, #31295, .T. ) ;
#34092=PLANE ( 'NONE',  #3672 ) ;
#34093=FACE_OUTER_BOUND ( 'NONE', #30551, .T. ) ;
#34095=CIRCLE ( 'NONE', #48044, 2.165354330708661568 ) ;
#34098=CARTESIAN_POINT ( 'NONE',  ( 2.106197740627111514, 0.000000000000000000, -1.299212598425194320 ) ) ;
#34099=ADVANCED_FACE ( 'NONE', ( #42890 ), #15288, .F. ) ;
#34100=VECTOR ( 'NONE', #32908, 39.37007874015748143 ) ;
#34102=VECTOR ( 'NONE', #13291, 39.37007874015748143 ) ;
#34104=VECTOR ( 'NONE', #29245, 39.37007874015748143 ) ;
#34105=CARTESIAN_POINT ( 'NONE',  ( 0.000000000000000000, 3.267716535433071279, 0.000000000000000000 ) ) ;
#34106=VERTEX_POINT ( 'NONE', #35164 ) ;
#34107=AXIS2_PLACEMENT_3D ( 'NONE', #30532, #42138, #34407 ) ;
#34108=ORIENTED_EDGE ( 'NONE', *, *, #12475, .T. ) ;
#34109=LINE ( 'NONE', #2860, #12230 ) ;
#34110=VERTEX_POINT ( 'NONE', #19901 ) ;
#34112=LINE ( 'NONE', #2863, #22269 ) ;
#34115=LINE ( 'NONE', #37487, #10677 ) ;
#34116=VERTEX_POINT ( 'NONE', #7539 ) ;
#34117=ORIENTED_EDGE ( 'NONE', *, *, #49110, .F. ) ;
#34118=CARTESIAN_POINT ( 'NONE',  ( 0.000000000000000000, 3.267716535433071279, 1.889763779527550369 ) ) ;
#34119=CARTESIAN_POINT ( 'NONE',  ( -1.909347346926324462, 3.267716535433071279, 0.7874015748031456541 ) ) ;
#34121=DIRECTION ( 'NONE',  ( -1.000000000000000000, 0.000000000000000000, 0.000000000000000000 ) ) ;
#34122=EDGE_LOOP ( 'NONE', ( #49003, #50044, #20437, #2650 ) ) ;
#34123=LINE ( 'NONE', #38002, #37866 ) ;
#34124=DIRECTION ( 'NONE',  ( -1.000000000000000000, -0.000000000000000000, -0.000000000000000000 ) ) ;
#34126=ORIENTED_EDGE ( 'NONE', *, *, #43731, .F. ) ;
#34128=VECTOR ( 'NONE', #10193, 39.37007874015748143 ) ;
#34129=LINE ( 'NONE', #2121, #24405 ) ;
#34130=ADVANCED_FACE ( 'NONE', ( #43142 ), #28163, .F. ) ;
#34136=EDGE_CURVE ( 'NONE', #12204, #24976, #4427, .T. ) ;
#34137=AXIS2_PLACEMENT_3D ( 'NONE', #10172, #25922, #41670 ) ;
#34138=VECTOR ( 'NONE', #24038, 39.37007874015748143 ) ;
#34140=LINE ( 'NONE', #41370, #22300 ) ;
#34142=ADVANCED_FACE ( 'NONE', ( #7791 ), #39033, .F. ) ;
#34143=FACE_OUTER_BOUND ( 'NONE', #28171, .T. ) ;
#34144=ORIENTED_EDGE ( 'NONE', *, *, #32305, .T. ) ;
#34145=VERTEX_POINT ( 'NONE', #47501 ) ;
#34147=PLANE ( 'NONE',  #19702 ) ;
#34149=VERTEX_POINT ( 'NONE', #3921 ) ;
#34150=CARTESIAN_POINT ( 'NONE',  ( 1.287906020515829919, 0.000000000000000000, -1.574803149606294417 ) ) ;
#34151=CARTESIAN_POINT ( 'NONE',  ( -0.3486774197067334935, 3.346456692913386100, 0.4330708661417290162 ) ) ;
#34152=EDGE_CURVE ( 'NONE', #50816, #31303, #16045, .T. ) ;
#34156=ORIENTED_EDGE ( 'NONE', *, *, #38686, .F. ) ;
#34158=DIRECTION ( 'NONE',  ( -3.469446951953613696E-16, 0.000000000000000000, -1.000000000000000000 ) ) ;
#34159=EDGE_CURVE ( 'NONE', #36331, #50486, #12571, .T. ) ;
#34160=PLANE ( 'NONE',  #983 ) ;
#34162=CARTESIAN_POINT ( 'NONE',  ( 1.636583440222563635, 0.000000000000000000, -1.259842519685035800 ) ) ;
#34164=FACE_OUTER_BOUND ( 'NONE', #28456, .T. ) ;
#34165=VERTEX_POINT ( 'NONE', #47755 ) ;
#34166=PLANE ( 'NONE',  #22591 ) ;
#34169=ORIENTED_EDGE ( 'NONE', *, *, #5915, .F. ) ;
#34170=CIRCLE ( 'NONE', #11884, 2.106299212598425008 ) ;
#34171=LINE ( 'NONE', #30032, #33774 ) ;
#34174=EDGE_CURVE ( 'NONE', #7950, #3576, #43654, .T. ) ;
#34175=AXIS2_PLACEMENT_3D ( 'NONE', #13149, #9015, #1006 ) ;
#34176=VECTOR ( 'NONE', #32510, 39.37007874015748143 ) ;
#34177=LINE ( 'NONE', #7553, #12832 ) ;
#34182=CARTESIAN_POINT ( 'NONE',  ( 1.833433833923350686, 3.267716535433071279, -6.361001426713997494E-16 ) ) ;
#34184=CARTESIAN_POINT ( 'NONE',  ( 0.5455278134075212115, 3.267716535433071279, -0.9448818897637765168 ) ) ;
#34185=ORIENTED_EDGE ( 'NONE', *, *, #34488, .T. ) ;
#34188=DIRECTION ( 'NONE',  ( -1.000000000000000000, 0.000000000000000000, 0.000000000000000000 ) ) ;
#34189=ORIENTED_EDGE ( 'NONE', *, *, #8007, .T. ) ;
#34190=ORIENTED_EDGE ( 'NONE', *, *, #23102, .F. ) ;
#34192=CARTESIAN_POINT ( 'NONE',  ( 0.5455278134075212115, 0.000000000000000000, -6.146657985744592735E-16 ) ) ;
#34193=DIRECTION ( 'NONE',  ( -1.000000000000000000, 0.000000000000000000, -0.000000000000000000 ) ) ;
#34196=DIRECTION ( 'NONE',  ( 0.000000000000000000, 1.000000000000000000, 0.000000000000000000 ) ) ;
#34197=ORIENTED_EDGE ( 'NONE', *, *, #42017, .T. ) ;
#34198=ADVANCED_FACE ( 'NONE', ( #43909 ), #12170, .F. ) ;
#34199=LINE ( 'NONE', #17683, #993 ) ;
#34200=VERTEX_POINT ( 'NONE', #25582 ) ;
#34201=VERTEX_POINT ( 'NONE', #33093 ) ;
#34202=LINE ( 'NONE', #21816, #19615 ) ;
#34203=CARTESIAN_POINT ( 'NONE',  ( -1.985260859929297572, 3.346456692913386100, 0.3149606299212578953 ) ) ;
#34204=EDGE_CURVE ( 'NONE', #28082, #50303, #21205, .T. ) ;
#34206=EDGE_CURVE ( 'NONE', #36591, #14599, #32578, .T. ) ;
#34207=CARTESIAN_POINT ( 'NONE',  ( 0.000000000000000000, 0.000000000000000000, 0.000000000000000000 ) ) ;
#34208=ADVANCED_FACE ( 'NONE', ( #1582 ), #36189, .F. ) ;
#34209=CARTESIAN_POINT ( 'NONE',  ( -0.8942052331142552601, 3.267716535433071279, -1.771653543307081025 ) ) ;
#34210=ORIENTED_EDGE ( 'NONE', *, *, #39189, .F. ) ;
#34211=VECTOR ( 'NONE', #19454, 39.37007874015748143 ) ;
#34213=ORIENTED_EDGE ( 'NONE', *, *, #47854, .T. ) ;
#34214=LINE ( 'NONE', #34464, #40131 ) ;
#34215=DIRECTION ( 'NONE',  ( 1.734723475976806848E-16, -0.000000000000000000, 1.000000000000000000 ) ) ;
#34216=VECTOR ( 'NONE', #48345, 39.37007874015748143 ) ;
#34217=ADVANCED_FACE ( 'NONE', ( #5714 ), #9841, .F. ) ;
#34218=DIRECTION ( 'NONE',  ( -1.000000000000000000, 0.000000000000000000, -0.000000000000000000 ) ) ;
#34219=CARTESIAN_POINT ( 'NONE',  ( -1.363819533518803029, 3.346456692913386100, 1.417322834645662777 ) ) ;
#34220=LINE ( 'NONE', #41205, #32830 ) ;
#34224=EDGE_CURVE ( 'NONE', #35324, #13112, #4942, .T. ) ;
#34225=LINE ( 'NONE', #38350, #14955 ) ;
#34227=CARTESIAN_POINT ( 'NONE',  ( 0.000000000000000000, 3.267716535433071279, 0.9055118110236167750 ) ) ;
#34228=DIRECTION ( 'NONE',  ( 0.000000000000000000, -1.000000000000000000, 0.000000000000000000 ) ) ;
#34231=EDGE_CURVE ( 'NONE', #31088, #38922, #17335, .T. ) ;
#34233=DIRECTION ( 'NONE',  ( -3.469446951953613696E-16, 0.000000000000000000, -1.000000000000000000 ) ) ;
#34234=ORIENTED_EDGE ( 'NONE', *, *, #35985, .T. ) ;
#34235=CARTESIAN_POINT ( 'NONE',  ( -0.5455278134075211005, 3.267716535433071279, 9.463399047163218249E-17 ) ) ;
#34236=ORIENTED_EDGE ( 'NONE', *, *, #629, .T. ) ;
#34237=FACE_BOUND ( 'NONE', #21619, .T. ) ;
#34238=EDGE_CURVE ( 'NONE', #31389, #19986, #1322, .T. ) ;
#34240=CARTESIAN_POINT ( 'NONE',  ( 0.000000000000000000, 3.267716535433071279, -1.102362204724405492 ) ) ;
#34241=CARTESIAN_POINT ( 'NONE',  ( 1.833433833923351353, 0.000000000000000000, -0.9448818897637765168 ) ) ;
#34242=EDGE_LOOP ( 'NONE', ( #45656, #22458, #1732, #41473 ) ) ;
#34244=DIRECTION ( 'NONE',  ( 1.734723475976806848E-16, -0.000000000000000000, 1.000000000000000000 ) ) ;
#34245=VECTOR ( 'NONE', #22462, 39.37007874015748143 ) ;
#34247=VECTOR ( 'NONE', #4901, 39.37007874015748143 ) ;
#34248=ADVANCED_FACE ( 'NONE', ( #5453 ), #20679, .F. ) ;
#34249=CIRCLE ( 'NONE', #16926, 2.106299212598425008 ) ;
#34250=LINE ( 'NONE', #8766, #8728 ) ;
#34251=FACE_OUTER_BOUND ( 'NONE', #20767, .T. ) ;
#34253=DIRECTION ( 'NONE',  ( -0.000000000000000000, 1.000000000000000000, -0.000000000000000000 ) ) ;
#34255=VERTEX_POINT ( 'NONE', #33350 ) ;
#34256=CARTESIAN_POINT ( 'NONE',  ( -2.182111253630085290, 0.000000000000000000, 0.7480314960629874665 ) ) ;
#34257=LINE ( 'NONE', #17737, #49514 ) ;
#34258=VECTOR ( 'NONE', #49674, 39.37007874015748143 ) ;
#34259=VERTEX_POINT ( 'NONE', #13460 ) ;
#34260=CARTESIAN_POINT ( 'NONE',  ( 1.287906020515830141, 3.346456692913386100, -0.3149606299212596716 ) ) ;
#34264=ORIENTED_EDGE ( 'NONE', *, *, #38565, .F. ) ;
#34266=DIRECTION ( 'NONE',  ( -0.000000000000000000, 1.000000000000000000, -0.000000000000000000 ) ) ;
#34269=CARTESIAN_POINT ( 'NONE',  ( -1.985260859929297572, 0.000000000000000000, 0.6299212598425164567 ) ) ;
#34270=LINE ( 'NONE', #22893, #29365 ) ;
#34271=CARTESIAN_POINT ( 'NONE',  ( -0.8182917201112814842, 3.346456692913386100, 0.4724409448818872592 ) ) ;
#34273=CARTESIAN_POINT ( 'NONE',  ( -0.2727639067037611054, 3.346456692913386100, -2.148105963102950877 ) ) ;
#34274=VECTOR ( 'NONE', #7912, 39.37007874015748143 ) ;
#34275=VERTEX_POINT ( 'NONE', #8812 ) ;
#34276=FACE_OUTER_BOUND ( 'NONE', #30106, .T. ) ;
#34277=DIRECTION ( 'NONE',  ( 0.000000000000000000, -1.000000000000000000, 0.000000000000000000 ) ) ;
#34278=VECTOR ( 'NONE', #29066, 39.37007874015748143 ) ;
#34283=LINE ( 'NONE', #18780, #25654 ) ;
#34284=CARTESIAN_POINT ( 'NONE',  ( -0.8182917201112819283, 3.346456692913386100, 2.004783788421104163 ) ) ;
#34285=ORIENTED_EDGE ( 'NONE', *, *, #36148, .T. ) ;
#34288=EDGE_CURVE ( 'NONE', #33634, #6021, #45177, .T. ) ;
#34290=VECTOR ( 'NONE', #17788, 39.37007874015748143 ) ;
#34291=ORIENTED_EDGE ( 'NONE', *, *, #17652, .T. ) ;
#34293=DIRECTION ( 'NONE',  ( -0.000000000000000000, 1.000000000000000000, -0.000000000000000000 ) ) ;
#34294=EDGE_LOOP ( 'NONE', ( #25368, #7764, #34897, #32276 ) ) ;
#34295=CARTESIAN_POINT ( 'NONE',  ( -1.909347346926324684, 3.267716535433071279, 3.312189666507128175E-16 ) ) ;
#34298=CARTESIAN_POINT ( 'NONE',  ( -0.8182917201112814842, 0.000000000000000000, 0.7874015748031456541 ) ) ;
#34300=LINE ( 'NONE', #35050, #32551 ) ;
#34302=ORIENTED_EDGE ( 'NONE', *, *, #39734, .F. ) ;
#34303=EDGE_CURVE ( 'NONE', #4450, #12364, #48522, .T. ) ;
#34305=ORIENTED_EDGE ( 'NONE', *, *, #24100, .F. ) ;
#34306=ORIENTED_EDGE ( 'NONE', *, *, #8664, .T. ) ;
#34307=CARTESIAN_POINT ( 'NONE',  ( -1.909347346926324684, 3.267716535433071279, 3.312189666507128175E-16 ) ) ;
#34308=ORIENTED_EDGE ( 'NONE', *, *, #49898, .T. ) ;
#34309=EDGE_CURVE ( 'NONE', #28890, #33278, #32841, .T. ) ;
#34310=CARTESIAN_POINT ( 'NONE',  ( 1.833433833923351353, 3.346456692913386100, -0.3149606299212596716 ) ) ;
#34311=DIRECTION ( 'NONE',  ( 0.000000000000000000, 1.000000000000000000, 0.000000000000000000 ) ) ;
#34313=DIRECTION ( 'NONE',  ( 1.734723475976806848E-16, -0.000000000000000000, 1.000000000000000000 ) ) ;
#34314=CARTESIAN_POINT ( 'NONE',  ( 1.363819533518803251, 3.267716535433071279, -2.365849761790805487E-16 ) ) ;
#34315=AXIS2_PLACEMENT_3D ( 'NONE', #25631, #44480, #10141 ) ;
#34316=DIRECTION ( 'NONE',  ( 1.000000000000000000, 0.000000000000000000, 0.000000000000000000 ) ) ;
#34317=VECTOR ( 'NONE', #7788, 39.37007874015748143 ) ;
#34318=EDGE_LOOP ( 'NONE', ( #22848, #35906, #33969, #5553 ) ) ;
#34319=ORIENTED_EDGE ( 'NONE', *, *, #7655, .F. ) ;
#34320=VECTOR ( 'NONE', #6133, 39.37007874015748143 ) ;
#34321=PLANE ( 'NONE',  #24880 ) ;
#34322=FACE_BOUND ( 'NONE', #26124, .T. ) ;
#34323=ORIENTED_EDGE ( 'NONE', *, *, #48266, .F. ) ;
#34324=VECTOR ( 'NONE', #31900, 39.37007874015748143 ) ;
#34325=ADVANCED_FACE ( 'NONE', ( #19532 ), #18789, .F. ) ;
#34327=DIRECTION ( 'NONE',  ( -3.469446951953613696E-16, 0.000000000000000000, -1.000000000000000000 ) ) ;
#34328=VECTOR ( 'NONE', #26372, 39.37007874015748143 ) ;
#34329=ORIENTED_EDGE ( 'NONE', *, *, #32399, .T. ) ;
#34330=EDGE_LOOP ( 'NONE', ( #19088, #50504, #34012, #24637 ) ) ;
#34331=EDGE_CURVE ( 'NONE', #8583, #35716, #6911, .T. ) ;
#34332=LINE ( 'NONE', #50016, #26481 ) ;
#34333=VECTOR ( 'NONE', #9477, 39.37007874015748143 ) ;
#34334=CARTESIAN_POINT ( 'NONE',  ( 1.091055626815042645, 3.267716535433071279, -1.892679809432644389E-16 ) ) ;
#34335=ORIENTED_EDGE ( 'NONE', *, *, #17058, .F. ) ;
#34336=ORIENTED_EDGE ( 'NONE', *, *, #21580, .T. ) ;
#34338=DIRECTION ( 'NONE',  ( 1.734723475976806848E-16, 0.000000000000000000, 1.000000000000000000 ) ) ;
#34339=CARTESIAN_POINT ( 'NONE',  ( -0.2727639067037605503, 3.267716535433071279, 4.731699523581609741E-17 ) ) ;
#34340=VERTEX_POINT ( 'NONE', #14663 ) ;
#34342=CARTESIAN_POINT ( 'NONE',  ( 0.4696143004045476022, 3.346456692913386100, -2.113816876263008293 ) ) ;
#34343=CARTESIAN_POINT ( 'NONE',  ( 4.200216290258821831E-16, 3.346456692913386100, 2.165354330708661568 ) ) ;
#34345=FACE_OUTER_BOUND ( 'NONE', #34047, .T. ) ;
#34347=CARTESIAN_POINT ( 'NONE',  ( 0.000000000000000000, 3.267716535433071279, 0.000000000000000000 ) ) ;
#34349=DIRECTION ( 'NONE',  ( -0.000000000000000000, 1.000000000000000000, -0.000000000000000000 ) ) ;
#34350=ORIENTED_EDGE ( 'NONE', *, *, #18872, .T. ) ;
#34351=VECTOR ( 'NONE', #33512, 39.37007874015748143 ) ;
#34353=DIRECTION ( 'NONE',  ( -1.000000000000000000, 0.000000000000000000, 0.000000000000000000 ) ) ;
#34354=VECTOR ( 'NONE', #22083, 39.37007874015748143 ) ;
#34356=VECTOR ( 'NONE', #14048, 39.37007874015748143 ) ;
#34357=ORIENTED_EDGE ( 'NONE', *, *, #15377, .T. ) ;
#34358=CARTESIAN_POINT ( 'NONE',  ( -1.166969139818015977, 3.346456692913386100, -0.4724409448818886470 ) ) ;
#34359=DIRECTION ( 'NONE',  ( -0.000000000000000000, 0.000000000000000000, 1.000000000000000000 ) ) ;
#34360=EDGE_CURVE ( 'NONE', #49094, #1746, #6662, .T. ) ;
#34361=ORIENTED_EDGE ( 'NONE', *, *, #9108, .F. ) ;
#34362=EDGE_CURVE ( 'NONE', #11498, #31195, #3287, .T. ) ;
#34364=AXIS2_PLACEMENT_3D ( 'NONE', #42422, #15062, #46768 ) ;
#34365=VERTEX_POINT ( 'NONE', #38416 ) ;
#34366=DIRECTION ( 'NONE',  ( -0.000000000000000000, 1.000000000000000000, -0.000000000000000000 ) ) ;
#34367=VERTEX_POINT ( 'NONE', #38914 ) ;
#34368=DIRECTION ( 'NONE',  ( 0.000000000000000000, -1.000000000000000000, 0.000000000000000000 ) ) ;
#34369=DIRECTION ( 'NONE',  ( 1.000000000000000000, 0.000000000000000000, 0.000000000000000000 ) ) ;
#34373=EDGE_LOOP ( 'NONE', ( #29539, #10382, #21300, #5043 ) ) ;
#34374=CARTESIAN_POINT ( 'NONE',  ( 1.363819533518803251, 3.346456692913386100, 0.2755905511810996522 ) ) ;
#34375=DIRECTION ( 'NONE',  ( 1.734723475976806848E-16, 0.000000000000000000, 1.000000000000000000 ) ) ;
#34376=CARTESIAN_POINT ( 'NONE',  ( 2.182111253630085290, 3.267716535433071279, -3.785359618865289765E-16 ) ) ;
#34377=PLANE ( 'NONE',  #4604 ) ;
#34378=EDGE_CURVE ( 'NONE', #35330, #15755, #3040, .T. ) ;
#34379=ORIENTED_EDGE ( 'NONE', *, *, #34238, .F. ) ;
#34380=EDGE_CURVE ( 'NONE', #43136, #39958, #14915, .T. ) ;
#34381=DIRECTION ( 'NONE',  ( -0.000000000000000000, 0.000000000000000000, 1.000000000000000000 ) ) ;
#34383=DIRECTION ( 'NONE',  ( 0.000000000000000000, -1.000000000000000000, 0.000000000000000000 ) ) ;
#34384=VECTOR ( 'NONE', #21774, 39.37007874015748143 ) ;
#34385=ORIENTED_EDGE ( 'NONE', *, *, #33266, .T. ) ;
#34386=EDGE_CURVE ( 'NONE', #27803, #13111, #42272, .T. ) ;
#34389=EDGE_CURVE ( 'NONE', #20810, #35404, #46626, .T. ) ;
#34390=ORIENTED_EDGE ( 'NONE', *, *, #45852, .F. ) ;
#34391=ORIENTED_EDGE ( 'NONE', *, *, #22658, .T. ) ;
#34392=DIRECTION ( 'NONE',  ( 1.734723475976806848E-16, -0.000000000000000000, 1.000000000000000000 ) ) ;
#34393=VECTOR ( 'NONE', #12152, 39.37007874015748143 ) ;
#34394=CARTESIAN_POINT ( 'NONE',  ( 1.363819533518803251, 3.346456692913386100, 1.417322834645662777 ) ) ;
#34396=VERTEX_POINT ( 'NONE', #38668 ) ;
#34397=ORIENTED_EDGE ( 'NONE', *, *, #16722, .F. ) ;
#34400=ORIENTED_EDGE ( 'NONE', *, *, #104, .T. ) ;
#34401=CARTESIAN_POINT ( 'NONE',  ( 0.000000000000000000, 3.267716535433071279, 0.000000000000000000 ) ) ;
#34402=CARTESIAN_POINT ( 'NONE',  ( -0.8182917201112814842, 3.346456692913386100, 1.417322834645662777 ) ) ;
#34404=CARTESIAN_POINT ( 'NONE',  ( -2.454875160333845674, 3.346456692913386100, -0.03937007874015881204 ) ) ;
#34407=DIRECTION ( 'NONE',  ( 1.734723475976806848E-16, 0.000000000000000000, 1.000000000000000000 ) ) ;
#34408=DIRECTION ( 'NONE',  ( 1.734723475976806848E-16, -0.000000000000000000, 1.000000000000000000 ) ) ;
#34409=CARTESIAN_POINT ( 'NONE',  ( 0.2727639067037604392, 3.267716535433071279, -1.299212598425193210 ) ) ;
#34412=LINE ( 'NONE', #46249, #34457 ) ;
#34413=LINE ( 'NONE', #23283, #4871 ) ;
#34416=VECTOR ( 'NONE', #3415, 39.37007874015748143 ) ;
#34417=CARTESIAN_POINT ( 'NONE',  ( -1.195183497228115035E-16, 0.000000000000000000, 0.3149606299212576177 ) ) ;
#34418=EDGE_CURVE ( 'NONE', #47614, #35680, #39164, .T. ) ;
#34421=EDGE_LOOP ( 'NONE', ( #12000, #5733, #36597, #23047 ) ) ;
#34424=CARTESIAN_POINT ( 'NONE',  ( -0.8182917201112819283, 3.346456692913386100, 0.1574803149606285035 ) ) ;
#34426=CARTESIAN_POINT ( 'NONE',  ( -0.5455278134075214336, 3.346456692913386100, -0.9448818897637762948 ) ) ;
#34427=DIRECTION ( 'NONE',  ( 1.734723475976806848E-16, 0.000000000000000000, 1.000000000000000000 ) ) ;
#34428=DIRECTION ( 'NONE',  ( -3.469446951953613696E-16, 0.000000000000000000, -1.000000000000000000 ) ) ;
#34431=VERTEX_POINT ( 'NONE', #27534 ) ;
#34433=PLANE ( 'NONE',  #25722 ) ;
#34434=LINE ( 'NONE', #50123, #49365 ) ;
#34436=CARTESIAN_POINT ( 'NONE',  ( -0.5455278134075214336, 0.000000000000000000, -8.878505979408855953E-16 ) ) ;
#34437=CARTESIAN_POINT ( 'NONE',  ( 1.636583440222563857, 3.346456692913386100, -0.6299212598425181220 ) ) ;
#34438=LINE ( 'NONE', #41174, #38487 ) ;
#34443=CARTESIAN_POINT ( 'NONE',  ( 1.015142113812069979, 3.346456692913386100, 1.535433070866133898 ) ) ;
#34445=DIRECTION ( 'NONE',  ( -0.000000000000000000, 1.000000000000000000, -0.000000000000000000 ) ) ;
#34446=VERTEX_POINT ( 'NONE', #30413 ) ;
#34447=FACE_BOUND ( 'NONE', #22188, .T. ) ;
#34449=EDGE_CURVE ( 'NONE', #38883, #39559, #43021, .T. ) ;
#34451=ORIENTED_EDGE ( 'NONE', *, *, #32305, .F. ) ;
#34452=VERTEX_POINT ( 'NONE', #11792 ) ;
#34453=FACE_OUTER_BOUND ( 'NONE', #23420, .T. ) ;
#34454=CARTESIAN_POINT ( 'NONE',  ( 0.2727639067037610499, 3.346456692913386100, 2.047244094488179567 ) ) ;
#34456=VECTOR ( 'NONE', #302, 39.37007874015748143 ) ;
#34457=VECTOR ( 'NONE', #39034, 39.37007874015748143 ) ;
#34460=DIRECTION ( 'NONE',  ( -0.000000000000000000, 1.000000000000000000, -0.000000000000000000 ) ) ;
#34461=ORIENTED_EDGE ( 'NONE', *, *, #11265, .F. ) ;
#34463=EDGE_LOOP ( 'NONE', ( #21312, #9204, #32084, #3945 ) ) ;
#34464=CARTESIAN_POINT ( 'NONE',  ( -1.536664496436148184E-16, 0.000000000000000000, -1.141732283464564013 ) ) ;
#34467=CARTESIAN_POINT ( 'NONE',  ( 0.1968503937007877735, 3.267716535433071279, 2.007874015748021268 ) ) ;
#34468=AXIS2_PLACEMENT_3D ( 'NONE', #44644, #48746, #5424 ) ;
#34469=PLANE ( 'NONE',  #614 ) ;
#34470=LINE ( 'NONE', #42705, #24546 ) ;
#34474=DIRECTION ( 'NONE',  ( -0.000000000000000000, 1.000000000000000000, -0.000000000000000000 ) ) ;
#34475=ORIENTED_EDGE ( 'NONE', *, *, #2533, .T. ) ;
#34476=CARTESIAN_POINT ( 'NONE',  ( 0.7423782071083087075, 0.000000000000000000, 0.3149606299212576177 ) ) ;
#34477=CARTESIAN_POINT ( 'NONE',  ( 0.5455278134075217666, 0.000000000000000000, 1.574803149606291974 ) ) ;
#34480=DIRECTION ( 'NONE',  ( -0.000000000000000000, 1.000000000000000000, -0.000000000000000000 ) ) ;
#34481=PLANE ( 'NONE',  #39197 ) ;
#34484=ORIENTED_EDGE ( 'NONE', *, *, #33166, .F. ) ;
#34486=VERTEX_POINT ( 'NONE', #20571 ) ;
#34487=FACE_BOUND ( 'NONE', #50299, .T. ) ;
#34488=EDGE_CURVE ( 'NONE', #33365, #45283, #35550, .T. ) ;
#34489=DIRECTION ( 'NONE',  ( -1.000000000000000000, -0.000000000000000000, -0.000000000000000000 ) ) ;
#34491=EDGE_CURVE ( 'NONE', #33914, #4458, #12829, .T. ) ;
#34492=VECTOR ( 'NONE', #14164, 39.37007874015748143 ) ;
#34493=ADVANCED_FACE ( 'NONE', ( #36067 ), #28562, .F. ) ;
#34494=ORIENTED_EDGE ( 'NONE', *, *, #28837, .F. ) ;
#34495=ORIENTED_EDGE ( 'NONE', *, *, #37582, .F. ) ;
#34496=LINE ( 'NONE', #49931, #19076 ) ;
#34499=DIRECTION ( 'NONE',  ( -3.469446951953613696E-16, 0.000000000000000000, -1.000000000000000000 ) ) ;
#34502=VECTOR ( 'NONE', #32416, 39.37007874015748143 ) ;
#34504=ORIENTED_EDGE ( 'NONE', *, *, #46557, .T. ) ;
#34506=ORIENTED_EDGE ( 'NONE', *, *, #23901, .T. ) ;
#34507=CARTESIAN_POINT ( 'NONE',  ( -0.8942052331142551491, 3.267716535433071279, 3.102397620449222974E-16 ) ) ;
#34508=AXIS2_PLACEMENT_3D ( 'NONE', #13369, #2258, #2763 ) ;
#34510=EDGE_LOOP ( 'NONE', ( #36588, #29463, #43687, #14160 ) ) ;
#34511=EDGE_CURVE ( 'NONE', #46791, #49048, #13088, .T. ) ;
#34512=CARTESIAN_POINT ( 'NONE',  ( -1.363819533518803473, 0.000000000000000000, -1.614173228346451605 ) ) ;
#34513=ORIENTED_EDGE ( 'NONE', *, *, #6581, .F. ) ;
#34514=ORIENTED_EDGE ( 'NONE', *, *, #1412, .T. ) ;
#34516=EDGE_CURVE ( 'NONE', #20168, #35311, #16706, .T. ) ;
#34517=ORIENTED_EDGE ( 'NONE', *, *, #48681, .F. ) ;
#34519=FACE_OUTER_BOUND ( 'NONE', #43238, .T. ) ;
#34520=DIRECTION ( 'NONE',  ( 1.000000000000000000, -0.000000000000000000, 0.000000000000000000 ) ) ;
#34523=AXIS2_PLACEMENT_3D ( 'NONE', #45321, #17982, #21351 ) ;
#34524=CARTESIAN_POINT ( 'NONE',  ( 1.909347346926324684, 3.346456692913386100, 0.4724409448818868706 ) ) ;
#34527=ORIENTED_EDGE ( 'NONE', *, *, #12567, .T. ) ;
#34528=CARTESIAN_POINT ( 'NONE',  ( -1.486187880958815377, 3.346456692913386100, -1.574803149606293307 ) ) ;
#34530=CARTESIAN_POINT ( 'NONE',  ( 0.1968503937007878568, 3.346456692913386100, 2.204724409448808764 ) ) ;
#34532=VECTOR ( 'NONE', #29736, 39.37007874015748143 ) ;
#34533=VECTOR ( 'NONE', #49738, 39.37007874015748143 ) ;
#34534=ORIENTED_EDGE ( 'NONE', *, *, #9843, .F. ) ;
#34535=LINE ( 'NONE', #14654, #28959 ) ;
#34536=FACE_OUTER_BOUND ( 'NONE', #760, .T. ) ;
#34537=ORIENTED_EDGE ( 'NONE', *, *, #12392, .T. ) ;
#34539=DIRECTION ( 'NONE',  ( 1.000000000000000000, 0.000000000000000000, 0.000000000000000000 ) ) ;
#34541=CARTESIAN_POINT ( 'NONE',  ( -3.414809992080329023E-17, 3.346456692913386100, -0.1968503937007874405 ) ) ;
#34543=EDGE_LOOP ( 'NONE', ( #5302, #16871, #15593, #41237 ) ) ;
#34545=EDGE_CURVE ( 'NONE', #32403, #23735, #4061, .T. ) ;
#34549=CARTESIAN_POINT ( 'NONE',  ( 0.7423782071083090406, 3.267716535433071279, -2.575641807848711180E-16 ) ) ;
#34550=ORIENTED_EDGE ( 'NONE', *, *, #12126, .T. ) ;
#34551=EDGE_CURVE ( 'NONE', #31670, #421, #7924, .T. ) ;
#34553=ORIENTED_EDGE ( 'NONE', *, *, #41226, .T. ) ;
#34554=ORIENTED_EDGE ( 'NONE', *, *, #20344, .T. ) ;
#34555=DIRECTION ( 'NONE',  ( 1.734723475976806848E-16, -0.000000000000000000, 1.000000000000000000 ) ) ;
#34557=DIRECTION ( 'NONE',  ( -1.000000000000000000, 0.000000000000000000, 0.000000000000000000 ) ) ;
#34559=ORIENTED_EDGE ( 'NONE', *, *, #19501, .T. ) ;
#34560=PLANE ( 'NONE',  #23 ) ;
#34561=AXIS2_PLACEMENT_3D ( 'NONE', #42667, #31058, #15308 ) ;
#34562=FACE_OUTER_BOUND ( 'NONE', #3554, .T. ) ;
#34563=DIRECTION ( 'NONE',  ( -0.000000000000000000, 1.000000000000000000, -0.000000000000000000 ) ) ;
#34567=FACE_BOUND ( 'NONE', #30783, .T. ) ;
#34568=ORIENTED_EDGE ( 'NONE', *, *, #34449, .T. ) ;
#34569=VECTOR ( 'NONE', #9110, 39.37007874015748143 ) ;
#34570=DIRECTION ( 'NONE',  ( 1.000000000000000000, -0.000000000000000000, 0.000000000000000000 ) ) ;
#34571=EDGE_CURVE ( 'NONE', #16142, #5543, #31944, .T. ) ;
#34574=VECTOR ( 'NONE', #27474, 39.37007874015748143 ) ;
#34575=CARTESIAN_POINT ( 'NONE',  ( -0.3486774197067337711, 3.267716535433071279, 1.209717811016578338E-16 ) ) ;
#34577=EDGE_LOOP ( 'NONE', ( #20277, #25768, #14436, #17056 ) ) ;
#34578=AXIS2_PLACEMENT_3D ( 'NONE', #25399, #44749, #5784 ) ;
#34579=LINE ( 'NONE', #46413, #702 ) ;
#34581=ORIENTED_EDGE ( 'NONE', *, *, #37760, .T. ) ;
#34583=DIRECTION ( 'NONE',  ( 0.000000000000000000, 0.000000000000000000, -1.000000000000000000 ) ) ;
#34585=CARTESIAN_POINT ( 'NONE',  ( -0.8942052331142552601, 0.000000000000000000, -1.259842519685034690 ) ) ;
#34586=ORIENTED_EDGE ( 'NONE', *, *, #17268, .F. ) ;
#34589=FACE_OUTER_BOUND ( 'NONE', #18773, .T. ) ;
#34591=EDGE_CURVE ( 'NONE', #8821, #3678, #48152, .T. ) ;
#34593=EDGE_CURVE ( 'NONE', #41617, #4117, #16447, .T. ) ;
#34594=FACE_OUTER_BOUND ( 'NONE', #13227, .T. ) ;
#34596=AXIS2_PLACEMENT_3D ( 'NONE', #17539, #49247, #2558 ) ;
#34598=ORIENTED_EDGE ( 'NONE', *, *, #42116, .T. ) ;
#34599=DIRECTION ( 'NONE',  ( -3.469446951953613696E-16, 0.000000000000000000, -1.000000000000000000 ) ) ;
#34601=ORIENTED_EDGE ( 'NONE', *, *, #33889, .T. ) ;
#34602=ORIENTED_EDGE ( 'NONE', *, *, #42900, .F. ) ;
#34604=DIRECTION ( 'NONE',  ( -1.000000000000000000, 0.000000000000000000, -0.000000000000000000 ) ) ;
#34607=VERTEX_POINT ( 'NONE', #4827 ) ;
#34608=EDGE_CURVE ( 'NONE', #50705, #42620, #20824, .T. ) ;
#34609=ADVANCED_FACE ( 'NONE', ( #9462 ), #29331, .F. ) ;
#34612=CARTESIAN_POINT ( 'NONE',  ( -0.2727639067037602727, 3.267716535433071279, 0.5905511811023582691 ) ) ;
#34614=ORIENTED_EDGE ( 'NONE', *, *, #50334, .T. ) ;
#34616=CARTESIAN_POINT ( 'NONE',  ( 0.000000000000000000, 3.267716535433071279, -0.03937007874015908959 ) ) ;
#34618=CARTESIAN_POINT ( 'NONE',  ( -1.985260859929297572, 3.346456692913386100, -6.146657985744592735E-16 ) ) ;
#34619=ORIENTED_EDGE ( 'NONE', *, *, #19814, .T. ) ;
#34620=ORIENTED_EDGE ( 'NONE', *, *, #18084, .F. ) ;
#34622=LINE ( 'NONE', #46210, #15291 ) ;
#34623=VERTEX_POINT ( 'NONE', #49667 ) ;
#34624=CARTESIAN_POINT ( 'NONE',  ( -0.8942052331142552601, 3.267716535433071279, -1.574803149606293529 ) ) ;
#34625=LINE ( 'NONE', #18631, #11014 ) ;
#34626=VECTOR ( 'NONE', #25415, 39.37007874015748143 ) ;
#34627=EDGE_CURVE ( 'NONE', #40529, #21172, #45064, .T. ) ;
#34628=VERTEX_POINT ( 'NONE', #37091 ) ;
#34631=ORIENTED_EDGE ( 'NONE', *, *, #41745, .T. ) ;
#34634=EDGE_CURVE ( 'NONE', #2922, #43170, #25458, .T. ) ;
#34637=CARTESIAN_POINT ( 'NONE',  ( 1.287906020515830141, 0.000000000000000000, 0.4330708661417287386 ) ) ;
#34638=VECTOR ( 'NONE', #15331, 39.37007874015748143 ) ;
#34639=EDGE_CURVE ( 'NONE', #47515, #11356, #29844, .T. ) ;
#34640=EDGE_CURVE ( 'NONE', #31327, #28604, #40967, .T. ) ;
#34642=LINE ( 'NONE', #35397, #40401 ) ;
#34645=EDGE_CURVE ( 'NONE', #15165, #34963, #41219, .T. ) ;
#34646=LINE ( 'NONE', #22769, #31250 ) ;
#34647=DIRECTION ( 'NONE',  ( 1.734723475976806848E-16, -0.000000000000000000, 1.000000000000000000 ) ) ;
#34648=AXIS2_PLACEMENT_3D ( 'NONE', #5723, #44183, #21467 ) ;
#34652=CARTESIAN_POINT ( 'NONE',  ( -1.195183497228115035E-16, 0.000000000000000000, -0.9448818897637765168 ) ) ;
#34659=DIRECTION ( 'NONE',  ( 1.000000000000000000, 0.000000000000000000, 0.000000000000000000 ) ) ;
#34660=VERTEX_POINT ( 'NONE', #21590 ) ;
#34661=DIRECTION ( 'NONE',  ( 1.000000000000000000, 0.000000000000000000, 0.000000000000000000 ) ) ;
#34662=EDGE_CURVE ( 'NONE', #27595, #14000, #9845, .T. ) ;
#34663=CARTESIAN_POINT ( 'NONE',  ( -1.166969139818015977, 0.000000000000000000, -0.4724409448818886470 ) ) ;
#34664=DIRECTION ( 'NONE',  ( 1.000000000000000000, -0.000000000000000000, 0.000000000000000000 ) ) ;
#34665=VERTEX_POINT ( 'NONE', #24953 ) ;
#34666=EDGE_CURVE ( 'NONE', #38782, #1604, #1711, .T. ) ;
#34667=LINE ( 'NONE', #50350, #35786 ) ;
#34668=EDGE_CURVE ( 'NONE', #13594, #24976, #21848, .T. ) ;
#34669=ORIENTED_EDGE ( 'NONE', *, *, #23041, .T. ) ;
#34670=DIRECTION ( 'NONE',  ( -0.000000000000000000, 1.000000000000000000, -0.000000000000000000 ) ) ;
#34671=EDGE_LOOP ( 'NONE', ( #50694, #40937, #6037, #31236 ) ) ;
#34673=ORIENTED_EDGE ( 'NONE', *, *, #27872, .F. ) ;
#34674=AXIS2_PLACEMENT_3D ( 'NONE', #25064, #40816, #5438 ) ;
#34676=CARTESIAN_POINT ( 'NONE',  ( 1.287906020515830363, 3.267716535433071279, -4.468321617281356063E-16 ) ) ;
#34677=DIRECTION ( 'NONE',  ( -0.000000000000000000, 1.000000000000000000, -0.000000000000000000 ) ) ;
#34681=ORIENTED_EDGE ( 'NONE', *, *, #16659, .T. ) ;
#34682=DIRECTION ( 'NONE',  ( 0.000000000000000000, 1.000000000000000000, 0.000000000000000000 ) ) ;
#34684=ORIENTED_EDGE ( 'NONE', *, *, #9473, .F. ) ;
#34685=DIRECTION ( 'NONE',  ( -1.000000000000000000, 0.000000000000000000, -0.000000000000000000 ) ) ;
#34686=DIRECTION ( 'NONE',  ( 1.000000000000000000, 0.000000000000000000, 0.000000000000000000 ) ) ;
#34687=CIRCLE ( 'NONE', #12413, 2.165354330708661568 ) ;
#34688=CARTESIAN_POINT ( 'NONE',  ( 0.000000000000000000, 3.267716535433071279, 0.5905511811023582691 ) ) ;
#34689=ORIENTED_EDGE ( 'NONE', *, *, #7765, .F. ) ;
#34691=DIRECTION ( 'NONE',  ( -0.000000000000000000, 1.000000000000000000, -0.000000000000000000 ) ) ;
#34692=CARTESIAN_POINT ( 'NONE',  ( 0.000000000000000000, 3.267716535433071279, -0.9842519685039348154 ) ) ;
#34694=ORIENTED_EDGE ( 'NONE', *, *, #7404, .T. ) ;
#34698=VERTEX_POINT ( 'NONE', #13846 ) ;
#34702=DIRECTION ( 'NONE',  ( -1.000000000000000000, -0.000000000000000000, -0.000000000000000000 ) ) ;
#34703=ADVANCED_FACE ( 'NONE', ( #25209 ), #17459, .F. ) ;
#34706=VERTEX_POINT ( 'NONE', #25713 ) ;
#34707=EDGE_CURVE ( 'NONE', #17342, #39701, #41466, .T. ) ;
#34708=ADVANCED_FACE ( 'NONE', ( #25970 ), #6093, .F. ) ;
#34710=ORIENTED_EDGE ( 'NONE', *, *, #11384, .F. ) ;
#34711=CARTESIAN_POINT ( 'NONE',  ( -2.071704270381554913, 3.267716535433071279, 0.6299212598425164567 ) ) ;
#34713=VECTOR ( 'NONE', #35604, 39.37007874015748143 ) ;
#34715=CARTESIAN_POINT ( 'NONE',  ( -1.712496953225537188, 0.000000000000000000, 0.1574803149606286423 ) ) ;
#34717=VERTEX_POINT ( 'NONE', #32976 ) ;
#34719=VECTOR ( 'NONE', #8711, 39.37007874015748143 ) ;
#34720=ADVANCED_FACE ( 'NONE', ( #37604 ), #2229, .F. ) ;
#34721=CARTESIAN_POINT ( 'NONE',  ( 1.287906020515830141, 3.346456692913386100, 0.6299212598425161236 ) ) ;
#34722=ORIENTED_EDGE ( 'NONE', *, *, #9664, .F. ) ;
#34723=VECTOR ( 'NONE', #46809, 39.37007874015748143 ) ;
#34724=CARTESIAN_POINT ( 'NONE',  ( -0.07591351300297340121, 0.000000000000000000, -0.3543307086614175816 ) ) ;
#34725=EDGE_CURVE ( 'NONE', #50319, #4205, #15107, .T. ) ;
#34729=DIRECTION ( 'NONE',  ( 1.000000000000000000, -0.000000000000000000, 0.000000000000000000 ) ) ;
#34731=CARTESIAN_POINT ( 'NONE',  ( 1.363819533518803251, 0.000000000000000000, -0.03937007874015908959 ) ) ;
#34732=B_SPLINE_CURVE_WITH_KNOTS ( 'NONE', 3,
 ( #43248, #7898, #9691, #32952 ),
 .UNSPECIFIED., .F., .F.,
 ( 4, 4 ),
 ( 0.000000000000000000, 1.000000000000000000 ),
 .UNSPECIFIED. ) ;
#34733=ADVANCED_FACE ( 'NONE', ( #50171 ), #30863, .F. ) ;
#34734=ORIENTED_EDGE ( 'NONE', *, *, #25806, .T. ) ;
#34735=DIRECTION ( 'NONE',  ( 1.734723475976806848E-16, 0.000000000000000000, 1.000000000000000000 ) ) ;
#34737=FACE_BOUND ( 'NONE', #22425, .T. ) ;
#34739=CARTESIAN_POINT ( 'NONE',  ( 1.363819533518803251, 3.346456692913386100, -0.9842519685039348154 ) ) ;
#34740=ORIENTED_EDGE ( 'NONE', *, *, #4988, .F. ) ;
#34741=ORIENTED_EDGE ( 'NONE', *, *, #16474, .F. ) ;
#34743=DIRECTION ( 'NONE',  ( 1.734723475976806848E-16, -0.000000000000000000, 1.000000000000000000 ) ) ;
#34744=FACE_OUTER_BOUND ( 'NONE', #8976, .T. ) ;
#34745=DIRECTION ( 'NONE',  ( 1.734723475976806848E-16, -0.000000000000000000, 1.000000000000000000 ) ) ;
#34746=DIRECTION ( 'NONE',  ( -0.000000000000000000, 1.000000000000000000, -0.000000000000000000 ) ) ;
#34747=AXIS2_PLACEMENT_3D ( 'NONE', #11286, #22649, #14652 ) ;
#34748=CARTESIAN_POINT ( 'NONE',  ( -0.2727639067037602172, 0.000000000000000000, 2.047244094488179567 ) ) ;
#34749=VECTOR ( 'NONE', #26184, 39.37007874015748143 ) ;
#34751=ORIENTED_EDGE ( 'NONE', *, *, #7425, .F. ) ;
#34753=PLANE ( 'NONE',  #40535 ) ;
#34754=VECTOR ( 'NONE', #50927, 39.37007874015748143 ) ;
#34756=CARTESIAN_POINT ( 'NONE',  ( 0.2727639067037605503, 3.267716535433071279, -4.731699523581609125E-17 ) ) ;
#34757=ORIENTED_EDGE ( 'NONE', *, *, #47253, .F. ) ;
#34760=VECTOR ( 'NONE', #48834, 39.37007874015748143 ) ;
#34761=ORIENTED_EDGE ( 'NONE', *, *, #47322, .T. ) ;
#34762=ORIENTED_EDGE ( 'NONE', *, *, #8723, .F. ) ;
#34763=CARTESIAN_POINT ( 'NONE',  ( 1.015142113812069091, 0.000000000000000000, -1.417322834645664331 ) ) ;
#34764=EDGE_CURVE ( 'NONE', #43265, #35577, #46568, .T. ) ;
#34766=CARTESIAN_POINT ( 'NONE',  ( -1.712496953225537855, 3.346456692913386100, -1.226315847645294221 ) ) ;
#34770=EDGE_CURVE ( 'NONE', #35609, #31365, #7114, .T. ) ;
#34773=DIRECTION ( 'NONE',  ( 1.734723475976806848E-16, -0.000000000000000000, 1.000000000000000000 ) ) ;
#34775=CARTESIAN_POINT ( 'NONE',  ( -0.2727639067037602172, 3.346456692913386100, 2.047244094488179567 ) ) ;
#34779=VECTOR ( 'NONE', #44485, 39.37007874015748143 ) ;
#34780=ORIENTED_EDGE ( 'NONE', *, *, #32740, .T. ) ;
#34783=EDGE_CURVE ( 'NONE', #46441, #37232, #11239, .T. ) ;
#34785=ORIENTED_EDGE ( 'NONE', *, *, #31728, .T. ) ;
#34788=VECTOR ( 'NONE', #49745, 39.37007874015748143 ) ;
#34789=EDGE_CURVE ( 'NONE', #18884, #18853, #22858, .T. ) ;
#34790=VECTOR ( 'NONE', #24728, 39.37007874015748143 ) ;
#34792=VERTEX_POINT ( 'NONE', #26968 ) ;
#34793=PLANE ( 'NONE',  #23131 ) ;
#34796=PLANE ( 'NONE',  #27021 ) ;
#34798=DIRECTION ( 'NONE',  ( 1.000000000000000000, 0.000000000000000000, 0.000000000000000000 ) ) ;
#34801=EDGE_LOOP ( 'NONE', ( #30034, #26814, #9300, #38510 ) ) ;
#34802=DIRECTION ( 'NONE',  ( -1.000000000000000000, 0.000000000000000000, 0.000000000000000000 ) ) ;
#34803=ORIENTED_EDGE ( 'NONE', *, *, #30525, .F. ) ;
#34804=CARTESIAN_POINT ( 'NONE',  ( 3.616083068348484413E-16, 2.362204724409439294, 2.952755905511811552 ) ) ;
#34805=CARTESIAN_POINT ( 'NONE',  ( 0.000000000000000000, 3.267716535433071279, 0.000000000000000000 ) ) ;
#34806=ADVANCED_FACE ( 'NONE', ( #15364 ), #19476, .F. ) ;
#34808=CARTESIAN_POINT ( 'NONE',  ( 0.4696143004045479352, 3.346456692913386100, 0.1574803149606283648 ) ) ;
#34809=CARTESIAN_POINT ( 'NONE',  ( -1.636583440222564301, 0.000000000000000000, -1.456692913385822186 ) ) ;
#34810=ORIENTED_EDGE ( 'NONE', *, *, #8466, .T. ) ;
#34812=LINE ( 'NONE', #45392, #10068 ) ;
#34813=FACE_BOUND ( 'NONE', #17474, .T. ) ;
#34814=VERTEX_POINT ( 'NONE', #31113 ) ;
#34816=LINE ( 'NONE', #50258, #17983 ) ;
#34817=ORIENTED_EDGE ( 'NONE', *, *, #43598, .T. ) ;
#34819=PLANE ( 'NONE',  #21624 ) ;
#34820=VECTOR ( 'NONE', #24724, 39.37007874015748143 ) ;
#34821=EDGE_CURVE ( 'NONE', #44668, #23557, #23105, .T. ) ;
#34823=ORIENTED_EDGE ( 'NONE', *, *, #25610, .T. ) ;
#34827=CARTESIAN_POINT ( 'NONE',  ( 0.7423782071083092626, 3.346456692913386100, 1.889763779527550369 ) ) ;
#34829=VECTOR ( 'NONE', #12426, 39.37007874015748143 ) ;
#34830=FACE_OUTER_BOUND ( 'NONE', #46361, .T. ) ;
#34831=EDGE_CURVE ( 'NONE', #42424, #24628, #42720, .T. ) ;
#34834=ORIENTED_EDGE ( 'NONE', *, *, #39435, .T. ) ;
#34835=ORIENTED_EDGE ( 'NONE', *, *, #38218, .F. ) ;
#34836=DIRECTION ( 'NONE',  ( -0.000000000000000000, 1.000000000000000000, -0.000000000000000000 ) ) ;
#34837=CARTESIAN_POINT ( 'NONE',  ( -1.091055626815042645, 0.000000000000000000, -0.9448818897637760728 ) ) ;
#34840=LINE ( 'NONE', #38962, #17385 ) ;
#34842=ADVANCED_FACE ( 'NONE', ( #3231 ), #26224, .F. ) ;
#34843=FACE_OUTER_BOUND ( 'NONE', #14191, .T. ) ;
#34844=EDGE_LOOP ( 'NONE', ( #30655, #38817, #47236, #33868 ) ) ;
#34845=CARTESIAN_POINT ( 'NONE',  ( 1.833433833923350909, 3.267716535433071279, -1.456692913385823296 ) ) ;
#34846=CARTESIAN_POINT ( 'NONE',  ( 0.000000000000000000, 3.267716535433071279, 0.4724409448818869817 ) ) ;
#34849=ORIENTED_EDGE ( 'NONE', *, *, #22914, .F. ) ;
#34854=EDGE_CURVE ( 'NONE', #24511, #14359, #42962, .T. ) ;
#34855=AXIS2_PLACEMENT_3D ( 'NONE', #21807, #45267, #17169 ) ;
#34857=ORIENTED_EDGE ( 'NONE', *, *, #37760, .F. ) ;
#34858=DIRECTION ( 'NONE',  ( -0.000000000000000000, 1.000000000000000000, -0.000000000000000000 ) ) ;
#34859=VECTOR ( 'NONE', #18947, 39.37007874015748143 ) ;
#34860=EDGE_CURVE ( 'NONE', #4117, #33862, #19729, .T. ) ;
#34861=EDGE_LOOP ( 'NONE', ( #37318, #50111, #10564, #18599 ) ) ;
#34862=VECTOR ( 'NONE', #37261, 39.37007874015748143 ) ;
#34863=VECTOR ( 'NONE', #24892, 39.37007874015748143 ) ;
#34871=EDGE_CURVE ( 'NONE', #44433, #35684, #43219, .T. ) ;
#34872=CARTESIAN_POINT ( 'NONE',  ( 3.519654186525858491E-16, 2.344748451760389596, 2.874015748031496731 ) ) ;
#34874=DIRECTION ( 'NONE',  ( 0.000000000000000000, 0.000000000000000000, -1.000000000000000000 ) ) ;
#34875=EDGE_CURVE ( 'NONE', #41125, #1816, #27730, .T. ) ;
#34876=ORIENTED_EDGE ( 'NONE', *, *, #11756, .T. ) ;
#34879=ORIENTED_EDGE ( 'NONE', *, *, #40059, .F. ) ;
#34881=ORIENTED_EDGE ( 'NONE', *, *, #30819, .F. ) ;
#34885=DIRECTION ( 'NONE',  ( 0.000000000000000000, 1.000000000000000000, 0.000000000000000000 ) ) ;
#34886=ADVANCED_FACE ( 'NONE', ( #631 ), #35490, .F. ) ;
#34889=ADVANCED_FACE ( 'NONE', ( #31616 ), #23866, .F. ) ;
#34890=DIRECTION ( 'NONE',  ( -3.469446951953613696E-16, 0.000000000000000000, -1.000000000000000000 ) ) ;
#34891=ORIENTED_EDGE ( 'NONE', *, *, #38383, .F. ) ;
#34894=LINE ( 'NONE', #20148, #50147 ) ;
#34895=LINE ( 'NONE', #30768, #21862 ) ;
#34896=VECTOR ( 'NONE', #47314, 39.37007874015748143 ) ;
#34897=ORIENTED_EDGE ( 'NONE', *, *, #22195, .F. ) ;
#34899=LINE ( 'NONE', #41887, #15213 ) ;
#34900=VECTOR ( 'NONE', #50323, 39.37007874015748143 ) ;
#34901=VECTOR ( 'NONE', #36623, 39.37007874015748143 ) ;
#34902=CARTESIAN_POINT ( 'NONE',  ( 0.000000000000000000, 3.346456692913386100, 0.000000000000000000 ) ) ;
#34903=LINE ( 'NONE', #42383, #17027 ) ;
#34904=CARTESIAN_POINT ( 'NONE',  ( -2.454875160333845674, 0.000000000000000000, -0.03937007874015881204 ) ) ;
#34905=VECTOR ( 'NONE', #14270, 39.37007874015748143 ) ;
#34909=EDGE_LOOP ( 'NONE', ( #20345, #36736, #21814, #50371 ) ) ;
#34911=CARTESIAN_POINT ( 'NONE',  ( 0.4696143004045479907, 3.267716535433071279, -1.629301903132387999E-16 ) ) ;
#34913=EDGE_LOOP ( 'NONE', ( #5488, #31823, #12963, #30449 ) ) ;
#34914=EDGE_CURVE ( 'NONE', #25659, #46790, #36262, .T. ) ;
#34915=EDGE_LOOP ( 'NONE', ( #37576, #25883, #12246, #8980 ) ) ;
#34916=CARTESIAN_POINT ( 'NONE',  ( -2.071704270381554913, 3.346456692913386100, -0.6299212598425177889 ) ) ;
#34917=ORIENTED_EDGE ( 'NONE', *, *, #49254, .F. ) ;
#34918=LINE ( 'NONE', #31554, #23710 ) ;
#34919=EDGE_CURVE ( 'NONE', #3939, #41046, #5012, .T. ) ;
#34922=CARTESIAN_POINT ( 'NONE',  ( -1.439733046521776361, 3.267716535433071279, 4.995077429881866871E-16 ) ) ;
#34923=CARTESIAN_POINT ( 'NONE',  ( 2.182111253630085290, 3.346456692913386100, 0.6299212598425161236 ) ) ;
#34924=EDGE_CURVE ( 'NONE', #919, #15390, #32136, .T. ) ;
#34925=EDGE_CURVE ( 'NONE', #10877, #22183, #110, .T. ) ;
#34926=ORIENTED_EDGE ( 'NONE', *, *, #7355, .T. ) ;
#34927=VECTOR ( 'NONE', #45710, 39.37007874015748143 ) ;
#34928=ORIENTED_EDGE ( 'NONE', *, *, #49872, .F. ) ;
#34929=ORIENTED_EDGE ( 'NONE', *, *, #38216, .T. ) ;
#34930=LINE ( 'NONE', #34182, #47898 ) ;
#34932=ORIENTED_EDGE ( 'NONE', *, *, #32360, .T. ) ;
#34933=ORIENTED_EDGE ( 'NONE', *, *, #13789, .F. ) ;
#34936=LINE ( 'NONE', #34437, #12082 ) ;
#34937=DIRECTION ( 'NONE',  ( -1.000000000000000000, 0.000000000000000000, 1.734723475976806848E-16 ) ) ;
#34938=VECTOR ( 'NONE', #4349, 39.37007874015748143 ) ;
#34940=ORIENTED_EDGE ( 'NONE', *, *, #25507, .F. ) ;
#34942=DIRECTION ( 'NONE',  ( 1.000000000000000000, 0.000000000000000000, -3.469446951953613696E-16 ) ) ;
#34943=CARTESIAN_POINT ( 'NONE',  ( 4.268512490100411402E-16, 0.000000000000000000, 0.9448818897637749625 ) ) ;
#34945=EDGE_CURVE ( 'NONE', #43549, #45835, #7865, .T. ) ;
#34948=CARTESIAN_POINT ( 'NONE',  ( -0.07591351300297333182, 3.267716535433071279, -0.1574803149606301411 ) ) ;
#34950=ORIENTED_EDGE ( 'NONE', *, *, #21768, .T. ) ;
#34954=LINE ( 'NONE', #31585, #21307 ) ;
#34955=DIRECTION ( 'NONE',  ( -0.000000000000000000, 1.000000000000000000, -0.000000000000000000 ) ) ;
#34956=EDGE_CURVE ( 'NONE', #42980, #29226, #39359, .T. ) ;
#34957=LINE ( 'NONE', #8088, #39571 ) ;
#34958=CYLINDRICAL_SURFACE ( 'NONE', #17038, 2.106299212598425008 ) ;
#34959=ADVANCED_FACE ( 'NONE', ( #31366 ), #28237, .F. ) ;
#34960=ADVANCED_FACE ( 'NONE', ( #43469 ), #32391, .F. ) ;
#34961=LINE ( 'NONE', #50638, #21377 ) ;
#34962=ORIENTED_EDGE ( 'NONE', *, *, #33712, .T. ) ;
#34963=VERTEX_POINT ( 'NONE', #4243 ) ;
#34964=DIRECTION ( 'NONE',  ( -1.000000000000000000, -0.000000000000000000, -0.000000000000000000 ) ) ;
#34965=CARTESIAN_POINT ( 'NONE',  ( 0.000000000000000000, 3.267716535433071279, -0.4724409448818884805 ) ) ;
#34966=DIRECTION ( 'NONE',  ( -0.000000000000000000, 1.000000000000000000, -0.000000000000000000 ) ) ;
#34967=VECTOR ( 'NONE', #34327, 39.37007874015748143 ) ;
#34968=FACE_OUTER_BOUND ( 'NONE', #31626, .T. ) ;
#34969=CARTESIAN_POINT ( 'NONE',  ( -0.8942052331142545940, 3.267716535433071279, 3.102397620449221495E-16 ) ) ;
#34970=ORIENTED_EDGE ( 'NONE', *, *, #22978, .T. ) ;
#34974=DIRECTION ( 'NONE',  ( -3.469446951953613696E-16, 0.000000000000000000, -1.000000000000000000 ) ) ;
#34977=ORIENTED_EDGE ( 'NONE', *, *, #4647, .T. ) ;
#34978=DIRECTION ( 'NONE',  ( -0.000000000000000000, 0.000000000000000000, 1.000000000000000000 ) ) ;
#34981=CARTESIAN_POINT ( 'NONE',  ( 0.2727639067037610499, 0.000000000000000000, 1.417322834645662777 ) ) ;
#34982=DIRECTION ( 'NONE',  ( 0.000000000000000000, 0.000000000000000000, -1.000000000000000000 ) ) ;
#34983=LINE ( 'NONE', #42468, #24392 ) ;
#34985=ORIENTED_EDGE ( 'NONE', *, *, #1893, .T. ) ;
#34988=DIRECTION ( 'NONE',  ( 1.734723475976806848E-16, 0.000000000000000000, 1.000000000000000000 ) ) ;
#34989=DIRECTION ( 'NONE',  ( -1.000000000000000000, -0.000000000000000000, -0.000000000000000000 ) ) ;
#34990=CARTESIAN_POINT ( 'NONE',  ( 0.000000000000000000, 3.267716535433071279, 0.3149606299212576177 ) ) ;
#34991=EDGE_CURVE ( 'NONE', #45413, #15688, #12766, .T. ) ;
#34992=EDGE_CURVE ( 'NONE', #17453, #18200, #20506, .T. ) ;
#34993=ADVANCED_FACE ( 'NONE', ( #12247, #40133, #31884, #4759, #43722, #24121, #20239, #1132 ), #29528, .F. ) ;
#34994=ORIENTED_EDGE ( 'NONE', *, *, #35217, .F. ) ;
#34995=ORIENTED_EDGE ( 'NONE', *, *, #7786, .F. ) ;
#34998=CARTESIAN_POINT ( 'NONE',  ( -0.3486774197067339376, 0.000000000000000000, -0.6299212598425175669 ) ) ;
#34999=DIRECTION ( 'NONE',  ( 0.000000000000000000, 0.000000000000000000, -1.000000000000000000 ) ) ;
#35000=CARTESIAN_POINT ( 'NONE',  ( 0.5455278134075212115, 3.267716535433071279, -9.463399047163220715E-17 ) ) ;
#35001=ADVANCED_FACE ( 'NONE', ( #25905 ), #41655, .F. ) ;
#35002=CARTESIAN_POINT ( 'NONE',  ( 1.636583440222563857, 3.267716535433071279, 0.7480314960629872445 ) ) ;
#35003=ORIENTED_EDGE ( 'NONE', *, *, #39996, .F. ) ;
#35007=CARTESIAN_POINT ( 'NONE',  ( -1.166969139818015977, 3.346456692913386100, -0.7874015748031470974 ) ) ;
#35011=VECTOR ( 'NONE', #3398, 39.37007874015748143 ) ;
#35012=ORIENTED_EDGE ( 'NONE', *, *, #27302, .F. ) ;
#35013=EDGE_LOOP ( 'NONE', ( #35380, #17985, #19233, #32093 ) ) ;
#35014=EDGE_CURVE ( 'NONE', #36931, #24770, #36769, .T. ) ;
#35015=VECTOR ( 'NONE', #19791, 39.37007874015748143 ) ;
#35016=AXIS2_PLACEMENT_3D ( 'NONE', #36629, #21138, #33026 ) ;
#35017=ADVANCED_FACE ( 'NONE', ( #13019 ), #45496, .F. ) ;
#35018=VERTEX_POINT ( 'NONE', #45245 ) ;
#35020=LINE ( 'NONE', #50696, #26875 ) ;
#35023=CIRCLE ( 'NONE', #16067, 2.443628662382284489 ) ;
#35024=EDGE_CURVE ( 'NONE', #19298, #30179, #37028, .T. ) ;
#35025=LINE ( 'NONE', #15400, #35343 ) ;
#35030=DIRECTION ( 'NONE',  ( 1.000000000000000000, -0.000000000000000000, 0.000000000000000000 ) ) ;
#35031=CARTESIAN_POINT ( 'NONE',  ( 1.560669927219590525, 3.346456692913386100, 0.9055118110236164419 ) ) ;
#35032=VERTEX_POINT ( 'NONE', #9140 ) ;
#35033=DIRECTION ( 'NONE',  ( 1.734723475976806848E-16, -0.000000000000000000, 1.000000000000000000 ) ) ;
#35034=LINE ( 'NONE', #7410, #25875 ) ;
#35035=DIRECTION ( 'NONE',  ( -0.000000000000000000, 0.000000000000000000, 1.000000000000000000 ) ) ;
#35036=CARTESIAN_POINT ( 'NONE',  ( 0.000000000000000000, 3.267716535433071279, 0.1181102362204704270 ) ) ;
#35037=VERTEX_POINT ( 'NONE', #32653 ) ;
#35038=CARTESIAN_POINT ( 'NONE',  ( 4.200216290258821831E-16, 3.346456692913386100, 2.165354330708661568 ) ) ;
#35043=VECTOR ( 'NONE', #46978, 39.37007874015748143 ) ;
#35044=VECTOR ( 'NONE', #25762, 39.37007874015748143 ) ;
#35045=DIRECTION ( 'NONE',  ( -1.000000000000000000, -0.000000000000000000, -0.000000000000000000 ) ) ;
#35046=ORIENTED_EDGE ( 'NONE', *, *, #22933, .T. ) ;
#35047=LINE ( 'NONE', #4309, #44572 ) ;
#35048=VECTOR ( 'NONE', #15617, 39.37007874015748143 ) ;
#35050=CARTESIAN_POINT ( 'NONE',  ( 0.8182917201112817063, 3.346456692913386100, -1.732283464566923614 ) ) ;
#35051=CARTESIAN_POINT ( 'NONE',  ( -1.439733046521776583, 3.346456692913386100, -1.617383112398506295 ) ) ;
#35054=AXIS2_PLACEMENT_3D ( 'NONE', #44504, #12253, #9148 ) ;
#35055=ORIENTED_EDGE ( 'NONE', *, *, #7195, .F. ) ;
#35059=ORIENTED_EDGE ( 'NONE', *, *, #12182, .T. ) ;
#35060=DIRECTION ( 'NONE',  ( 1.000000000000000000, 0.000000000000000000, 0.000000000000000000 ) ) ;
#35063=EDGE_CURVE ( 'NONE', #22677, #44810, #13275, .T. ) ;
#35065=VERTEX_POINT ( 'NONE', #25393 ) ;
#35067=VERTEX_POINT ( 'NONE', #5524 ) ;
#35069=LINE ( 'NONE', #28071, #36415 ) ;
#35070=VERTEX_POINT ( 'NONE', #37541 ) ;
#35071=CARTESIAN_POINT ( 'NONE',  ( -0.8942052331142547050, 0.000000000000000000, 0.6299212598425164567 ) ) ;
#35073=ORIENTED_EDGE ( 'NONE', *, *, #25653, .F. ) ;
#35075=DIRECTION ( 'NONE',  ( 0.000000000000000000, 1.000000000000000000, 0.000000000000000000 ) ) ;
#35076=VECTOR ( 'NONE', #45104, 39.37007874015748143 ) ;
#35078=CARTESIAN_POINT ( 'NONE',  ( -1.195183497228115035E-16, 3.346456692913386100, -1.574803149606293529 ) ) ;
#35081=VERTEX_POINT ( 'NONE', #9654 ) ;
#35082=DIRECTION ( 'NONE',  ( -3.469446951953613696E-16, 0.000000000000000000, -1.000000000000000000 ) ) ;
#35084=EDGE_LOOP ( 'NONE', ( #6630, #25639, #33452, #36858 ) ) ;
#35086=DIRECTION ( 'NONE',  ( 0.000000000000000000, 1.000000000000000000, 0.000000000000000000 ) ) ;
#35087=VECTOR ( 'NONE', #24005, 39.37007874015748143 ) ;
#35088=CARTESIAN_POINT ( 'NONE',  ( 2.378961647330872786, 3.346456692913386100, 0.6299212598425161236 ) ) ;
#35091=AXIS2_PLACEMENT_3D ( 'NONE', #45385, #18047, #33808 ) ;
#35093=FACE_OUTER_BOUND ( 'NONE', #24592, .T. ) ;
#35094=DIRECTION ( 'NONE',  ( -3.469446951953613696E-16, 0.000000000000000000, -1.000000000000000000 ) ) ;
#35095=CARTESIAN_POINT ( 'NONE',  ( -0.5455278134075213226, 3.267716535433071279, 9.463399047163221947E-17 ) ) ;
#35096=DIRECTION ( 'NONE',  ( -0.000000000000000000, 0.000000000000000000, 1.000000000000000000 ) ) ;
#35097=LINE ( 'NONE', #26580, #7841 ) ;
#35098=LINE ( 'NONE', #35862, #7732 ) ;
#35099=ORIENTED_EDGE ( 'NONE', *, *, #46492, .T. ) ;
#35100=CARTESIAN_POINT ( 'NONE',  ( 2.182111253630085290, 0.000000000000000000, -1.161035397307311917E-15 ) ) ;
#35101=ORIENTED_EDGE ( 'NONE', *, *, #3780, .F. ) ;
#35102=ORIENTED_EDGE ( 'NONE', *, *, #16410, .F. ) ;
#35104=LINE ( 'NONE', #496, #36075 ) ;
#35105=ORIENTED_EDGE ( 'NONE', *, *, #10238, .F. ) ;
#35107=CARTESIAN_POINT ( 'NONE',  ( 0.000000000000000000, 3.267716535433071279, -0.1574803149606298636 ) ) ;
#35108=EDGE_CURVE ( 'NONE', #17272, #42090, #49099, .T. ) ;
#35111=CARTESIAN_POINT ( 'NONE',  ( -0.07591351300297277671, 3.346456692913386100, 0.7874015748031456541 ) ) ;
#35112=AXIS2_PLACEMENT_3D ( 'NONE', #24905, #44000, #16137 ) ;
#35116=CARTESIAN_POINT ( 'NONE',  ( 0.000000000000000000, 3.267716535433071279, 2.204724409448808764 ) ) ;
#35117=EDGE_CURVE ( 'NONE', #28628, #3517, #22292, .T. ) ;
#35118=VECTOR ( 'NONE', #1611, 39.37007874015748143 ) ;
#35119=EDGE_CURVE ( 'NONE', #29278, #20848, #31044, .T. ) ;
#35120=ORIENTED_EDGE ( 'NONE', *, *, #34645, .T. ) ;
#35121=VECTOR ( 'NONE', #49364, 39.37007874015748143 ) ;
#35123=LINE ( 'NONE', #50800, #42035 ) ;
#35124=EDGE_LOOP ( 'NONE', ( #20543, #29714, #13865, #19066 ) ) ;
#35126=LINE ( 'NONE', #41858, #10318 ) ;
#35127=CARTESIAN_POINT ( 'NONE',  ( 0.1968503937007875237, 3.267716535433071279, -6.829619984160660511E-17 ) ) ;
#35129=ORIENTED_EDGE ( 'NONE', *, *, #13289, .F. ) ;
#35133=ORIENTED_EDGE ( 'NONE', *, *, #21209, .T. ) ;
#35134=CARTESIAN_POINT ( 'NONE',  ( -1.636583440222564301, 3.346456692913386100, -1.456692913385822186 ) ) ;
#35136=ORIENTED_EDGE ( 'NONE', *, *, #28824, .T. ) ;
#35137=ORIENTED_EDGE ( 'NONE', *, *, #38847, .F. ) ;
#35141=CARTESIAN_POINT ( 'NONE',  ( 1.287906020515830141, 3.346456692913386100, -0.9448818897637765168 ) ) ;
#35142=EDGE_CURVE ( 'NONE', #10888, #11679, #34171, .T. ) ;
#35143=AXIS2_PLACEMENT_3D ( 'NONE', #46487, #38285, #30528 ) ;
#35144=PLANE ( 'NONE',  #44023 ) ;
#35147=VERTEX_POINT ( 'NONE', #49605 ) ;
#35148=VECTOR ( 'NONE', #26584, 39.37007874015748143 ) ;
#35149=VECTOR ( 'NONE', #12866, 39.37007874015748143 ) ;
#35151=ORIENTED_EDGE ( 'NONE', *, *, #8597, .T. ) ;
#35152=DIRECTION ( 'NONE',  ( -1.000000000000000000, -0.000000000000000000, -0.000000000000000000 ) ) ;
#35153=ADVANCED_FACE ( 'NONE', ( #42153 ), #10413, .F. ) ;
#35154=DIRECTION ( 'NONE',  ( 0.000000000000000000, 1.000000000000000000, 0.000000000000000000 ) ) ;
#35155=AXIS2_PLACEMENT_3D ( 'NONE', #17858, #9089, #29479 ) ;
#35156=AXIS2_PLACEMENT_3D ( 'NONE', #10197, #45038, #13062 ) ;
#35157=CARTESIAN_POINT ( 'NONE',  ( 0.000000000000000000, 3.267716535433071279, 0.000000000000000000 ) ) ;
#35161=EDGE_LOOP ( 'NONE', ( #33280, #17919, #25712, #33510 ) ) ;
#35162=CARTESIAN_POINT ( 'NONE',  ( 1.636583440222563635, 3.346456692913386100, -0.9448818897637765168 ) ) ;
#35163=ORIENTED_EDGE ( 'NONE', *, *, #31777, .F. ) ;
#35164=CARTESIAN_POINT ( 'NONE',  ( 1.909347346926324684, 3.346456692913386100, 0.1574803149606280872 ) ) ;
#35166=CARTESIAN_POINT ( 'NONE',  ( 0.000000000000000000, 3.267716535433071279, 2.204724409448808764 ) ) ;
#35167=ORIENTED_EDGE ( 'NONE', *, *, #12503, .F. ) ;
#35170=EDGE_LOOP ( 'NONE', ( #36423, #43032, #23194, #38296 ) ) ;
#35172=ORIENTED_EDGE ( 'NONE', *, *, #24402, .T. ) ;
#35173=ADVANCED_FACE ( 'NONE', ( #38303 ), #7300, .F. ) ;
#35174=DIRECTION ( 'NONE',  ( -0.000000000000000000, 1.000000000000000000, -0.000000000000000000 ) ) ;
#35176=CARTESIAN_POINT ( 'NONE',  ( 1.091055626815042645, 0.000000000000000000, -0.9448818897637765168 ) ) ;
#35177=AXIS2_PLACEMENT_3D ( 'NONE', #45867, #13644, #29385 ) ;
#35178=EDGE_CURVE ( 'NONE', #47345, #903, #7049, .T. ) ;
#35180=VERTEX_POINT ( 'NONE', #26406 ) ;
#35181=EDGE_LOOP ( 'NONE', ( #30255, #28419, #17309, #9621 ) ) ;
#35182=FACE_OUTER_BOUND ( 'NONE', #29689, .T. ) ;
#35183=CIRCLE ( 'NONE', #30254, 2.165354330708661568 ) ;
#35185=AXIS2_PLACEMENT_3D ( 'NONE', #18715, #31091, #22334 ) ;
#35186=ORIENTED_EDGE ( 'NONE', *, *, #18648, .F. ) ;
#35187=ORIENTED_EDGE ( 'NONE', *, *, #49042, .F. ) ;
#35188=LINE ( 'NONE', #34436, #21482 ) ;
#35189=DIRECTION ( 'NONE',  ( 1.000000000000000000, -0.000000000000000000, 0.000000000000000000 ) ) ;
#35190=DIRECTION ( 'NONE',  ( 1.734723475976806848E-16, -0.000000000000000000, 1.000000000000000000 ) ) ;
#35191=EDGE_LOOP ( 'NONE', ( #5409, #18565, #31154, #1595 ) ) ;
#35195=VECTOR ( 'NONE', #28974, 39.37007874015748143 ) ;
#35197=ORIENTED_EDGE ( 'NONE', *, *, #44665, .F. ) ;
#35198=CARTESIAN_POINT ( 'NONE',  ( 1.363819533518803251, 3.346456692913386100, 0.1574803149606283648 ) ) ;
#35199=DIRECTION ( 'NONE',  ( -0.000000000000000000, 1.000000000000000000, -0.000000000000000000 ) ) ;
#35200=VECTOR ( 'NONE', #37301, 39.37007874015748143 ) ;
#35201=ORIENTED_EDGE ( 'NONE', *, *, #44442, .T. ) ;
#35202=CARTESIAN_POINT ( 'NONE',  ( -0.8942052331142547050, 0.000000000000000000, 0.4330708661417290162 ) ) ;
#35204=EDGE_LOOP ( 'NONE', ( #17146, #50871, #11422, #46429 ) ) ;
#35209=DIRECTION ( 'NONE',  ( -3.469446951953613696E-16, 0.000000000000000000, -1.000000000000000000 ) ) ;
#35210=CARTESIAN_POINT ( 'NONE',  ( -1.166969139818015755, 3.267716535433071279, 1.220472440944875281 ) ) ;
#35212=ORIENTED_EDGE ( 'NONE', *, *, #15432, .F. ) ;
#35213=ORIENTED_EDGE ( 'NONE', *, *, #46050, .F. ) ;
#35214=CARTESIAN_POINT ( 'NONE',  ( 0.7423782071083087075, 0.000000000000000000, -1.259842519685035134 ) ) ;
#35215=EDGE_CURVE ( 'NONE', #8198, #47008, #46011, .T. ) ;
#35216=LINE ( 'NONE', #38592, #39128 ) ;
#35217=EDGE_CURVE ( 'NONE', #39696, #46790, #50109, .T. ) ;
#35222=CARTESIAN_POINT ( 'NONE',  ( 0.8182917201112819283, 3.346456692913386100, -1.102362204724405714 ) ) ;
#35223=VECTOR ( 'NONE', #13322, 39.37007874015748143 ) ;
#35224=EDGE_LOOP ( 'NONE', ( #50423, #16196, #9079, #24993 ) ) ;
#35225=CARTESIAN_POINT ( 'NONE',  ( 1.091055626815042645, 3.346456692913386100, 0.1181102362204704270 ) ) ;
#35227=LINE ( 'NONE', #39601, #13341 ) ;
#35230=LINE ( 'NONE', #31356, #18284 ) ;
#35231=CARTESIAN_POINT ( 'NONE',  ( 2.088192093915797631, 3.346456692913386100, 0.2755905511810994302 ) ) ;
#35232=CARTESIAN_POINT ( 'NONE',  ( -1.363819533518803473, 3.346456692913386100, -0.3543307086614174151 ) ) ;
#35233=ORIENTED_EDGE ( 'NONE', *, *, #41235, .T. ) ;
#35241=FACE_OUTER_BOUND ( 'NONE', #4276, .T. ) ;
#35243=DIRECTION ( 'NONE',  ( -1.000000000000000000, -0.000000000000000000, -0.000000000000000000 ) ) ;
#35244=CARTESIAN_POINT ( 'NONE',  ( -0.2727639067037608278, 3.346456692913386100, 2.165354330708650465 ) ) ;
#35245=EDGE_CURVE ( 'NONE', #4010, #49945, #26904, .T. ) ;
#35246=ORIENTED_EDGE ( 'NONE', *, *, #34831, .F. ) ;
#35247=ORIENTED_EDGE ( 'NONE', *, *, #9043, .T. ) ;
#35248=CARTESIAN_POINT ( 'NONE',  ( 1.363819533518803029, 3.346456692913386100, -1.417322834645665219 ) ) ;
#35249=EDGE_CURVE ( 'NONE', #22612, #35273, #11423, .T. ) ;
#35251=ORIENTED_EDGE ( 'NONE', *, *, #45368, .F. ) ;
#35254=FACE_OUTER_BOUND ( 'NONE', #44464, .T. ) ;
#35255=LINE ( 'NONE', #50934, #50320 ) ;
#35256=ORIENTED_EDGE ( 'NONE', *, *, #31508, .F. ) ;
#35258=LINE ( 'NONE', #50939, #48818 ) ;
#35260=VECTOR ( 'NONE', #7541, 39.37007874015748143 ) ;
#35262=CARTESIAN_POINT ( 'NONE',  ( -0.2727639067037607723, 3.346456692913386100, 0.4724409448818869817 ) ) ;
#35263=ORIENTED_EDGE ( 'NONE', *, *, #46061, .F. ) ;
#35265=ORIENTED_EDGE ( 'NONE', *, *, #12345, .F. ) ;
#35266=VECTOR ( 'NONE', #256, 39.37007874015748143 ) ;
#35267=EDGE_LOOP ( 'NONE', ( #27072, #39767, #5063, #36007 ) ) ;
#35268=FACE_OUTER_BOUND ( 'NONE', #401, .T. ) ;
#35269=ORIENTED_EDGE ( 'NONE', *, *, #12320, .F. ) ;
#35270=EDGE_LOOP ( 'NONE', ( #15227, #5364, #40561, #18686 ) ) ;
#35272=VECTOR ( 'NONE', #15203, 39.37007874015748143 ) ;
#35273=VERTEX_POINT ( 'NONE', #8050 ) ;
#35275=DIRECTION ( 'NONE',  ( 1.000000000000000000, -0.000000000000000000, 0.000000000000000000 ) ) ;
#35276=CARTESIAN_POINT ( 'NONE',  ( -0.6214413264104945434, 3.267716535433071279, 2.156057715732901026E-16 ) ) ;
#35280=LINE ( 'NONE', #43518, #7471 ) ;
#35281=ADVANCED_FACE ( 'NONE', ( #43 ), #8305, .F. ) ;
#35284=ORIENTED_EDGE ( 'NONE', *, *, #20631, .T. ) ;
#35287=FACE_OUTER_BOUND ( 'NONE', #37218, .T. ) ;
#35288=ORIENTED_EDGE ( 'NONE', *, *, #22253, .T. ) ;
#35289=CARTESIAN_POINT ( 'NONE',  ( 1.015142113812069979, 0.000000000000000000, 1.417322834645662777 ) ) ;
#35290=DIRECTION ( 'NONE',  ( -1.000000000000000000, 0.000000000000000000, -0.000000000000000000 ) ) ;
#35291=ORIENTED_EDGE ( 'NONE', *, *, #1243, .T. ) ;
#35293=AXIS2_PLACEMENT_3D ( 'NONE', #13023, #5016, #17151 ) ;
#35294=VECTOR ( 'NONE', #43983, 39.37007874015748143 ) ;
#35298=DIRECTION ( 'NONE',  ( 1.000000000000000000, -0.000000000000000000, 0.000000000000000000 ) ) ;
#35299=ADVANCED_FACE ( 'NONE', ( #16052 ), #43917, .F. ) ;
#35302=FACE_OUTER_BOUND ( 'NONE', #28795, .T. ) ;
#35303=VECTOR ( 'NONE', #46445, 39.37007874015748143 ) ;
#35304=EDGE_CURVE ( 'NONE', #44668, #7558, #19908, .T. ) ;
#35306=FACE_OUTER_BOUND ( 'NONE', #16615, .T. ) ;
#35307=EDGE_LOOP ( 'NONE', ( #8239, #48682, #28597, #46340 ) ) ;
#35309=VECTOR ( 'NONE', #10513, 39.37007874015748143 ) ;
#35311=VERTEX_POINT ( 'NONE', #50849 ) ;
#35313=EDGE_CURVE ( 'NONE', #39732, #41937, #16312, .T. ) ;
#35314=ORIENTED_EDGE ( 'NONE', *, *, #33872, .F. ) ;
#35315=LINE ( 'NONE', #7935, #20526 ) ;
#35316=VECTOR ( 'NONE', #27391, 39.37007874015748143 ) ;
#35317=DIRECTION ( 'NONE',  ( 1.000000000000000000, 0.000000000000000000, 0.000000000000000000 ) ) ;
#35319=PLANE ( 'NONE',  #47012 ) ;
#35320=ORIENTED_EDGE ( 'NONE', *, *, #14546, .T. ) ;
#35321=CARTESIAN_POINT ( 'NONE',  ( -1.091055626815042201, 3.346456692913386100, 1.259842519685033357 ) ) ;
#35322=FACE_OUTER_BOUND ( 'NONE', #6986, .T. ) ;
#35323=EDGE_LOOP ( 'NONE', ( #2694, #43083, #13996, #5975 ) ) ;
#35324=VERTEX_POINT ( 'NONE', #24315 ) ;
#35326=ORIENTED_EDGE ( 'NONE', *, *, #2347, .F. ) ;
#35328=LINE ( 'NONE', #11821, #20478 ) ;
#35329=VECTOR ( 'NONE', #34802, 39.37007874015748143 ) ;
#35330=VERTEX_POINT ( 'NONE', #23798 ) ;
#35333=FACE_OUTER_BOUND ( 'NONE', #8839, .T. ) ;
#35334=ORIENTED_EDGE ( 'NONE', *, *, #28681, .T. ) ;
#35335=AXIS2_PLACEMENT_3D ( 'NONE', #20205, #24347, #48051 ) ;
#35337=EDGE_LOOP ( 'NONE', ( #15339, #28332, #20709, #49553 ) ) ;
#35339=CARTESIAN_POINT ( 'NONE',  ( -2.258024766633058622, 0.000000000000000000, -0.1574803149606298636 ) ) ;
#35340=VECTOR ( 'NONE', #28517, 39.37007874015748143 ) ;
#35342=CARTESIAN_POINT ( 'NONE',  ( 0.000000000000000000, 3.267716535433071279, -0.9842519685039344823 ) ) ;
#35343=VECTOR ( 'NONE', #46853, 39.37007874015748143 ) ;
#35344=EDGE_LOOP ( 'NONE', ( #5879, #12109, #26841, #19636 ) ) ;
#35345=ORIENTED_EDGE ( 'NONE', *, *, #44190, .F. ) ;
#35347=CARTESIAN_POINT ( 'NONE',  ( -0.5455278134075214336, 0.000000000000000000, -0.6299212598425175669 ) ) ;
#35348=LINE ( 'NONE', #46421, #40184 ) ;
#35349=EDGE_CURVE ( 'NONE', #24866, #47349, #12694, .T. ) ;
#35351=CIRCLE ( 'NONE', #19663, 2.106299212598425008 ) ;
#35352=CARTESIAN_POINT ( 'NONE',  ( -2.182111253630085734, 0.000000000000000000, -1.141732283464563791 ) ) ;
#35353=ADVANCED_FACE ( 'NONE', ( #7546 ), #48019, .F. ) ;
#35357=ORIENTED_EDGE ( 'NONE', *, *, #20046, .F. ) ;
#35358=CARTESIAN_POINT ( 'NONE',  ( -1.536664496436148184E-16, 3.267716535433071279, -1.771653543307081025 ) ) ;
#35359=EDGE_LOOP ( 'NONE', ( #42152, #31269, #49829, #42697 ) ) ;
#35360=CARTESIAN_POINT ( 'NONE',  ( -1.636583440222564301, 3.267716535433071279, 2.839019714148967077E-16 ) ) ;
#35361=VERTEX_POINT ( 'NONE', #566 ) ;
#35363=PLANE ( 'NONE',  #41850 ) ;
#35365=VECTOR ( 'NONE', #45258, 39.37007874015748143 ) ;
#35366=ORIENTED_EDGE ( 'NONE', *, *, #18152, .F. ) ;
#35369=ORIENTED_EDGE ( 'NONE', *, *, #35472, .F. ) ;
#35373=VECTOR ( 'NONE', #33714, 39.37007874015748143 ) ;
#35374=CARTESIAN_POINT ( 'NONE',  ( -0.6214413264104945434, 3.346456692913386100, -0.1574803149606301411 ) ) ;
#35375=CARTESIAN_POINT ( 'NONE',  ( 1.287906020515829919, 3.267716535433071279, -1.666671669919371102 ) ) ;
#35376=AXIS2_PLACEMENT_3D ( 'NONE', #25057, #36171, #1047 ) ;
#35377=ORIENTED_EDGE ( 'NONE', *, *, #14474, .F. ) ;
#35379=ORIENTED_EDGE ( 'NONE', *, *, #25425, .T. ) ;
#35380=ORIENTED_EDGE ( 'NONE', *, *, #38783, .F. ) ;
#35381=PLANE ( 'NONE',  #48229 ) ;
#35384=VECTOR ( 'NONE', #45745, 39.37007874015748143 ) ;
#35385=ORIENTED_EDGE ( 'NONE', *, *, #25136, .F. ) ;
#35386=DIRECTION ( 'NONE',  ( 0.000000000000000000, 0.000000000000000000, -1.000000000000000000 ) ) ;
#35389=LINE ( 'NONE', #27369, #4298 ) ;
#35391=VERTEX_POINT ( 'NONE', #3673 ) ;
#35392=VERTEX_POINT ( 'NONE', #19404 ) ;
#35394=CARTESIAN_POINT ( 'NONE',  ( 0.000000000000000000, 3.267716535433071279, -0.1574803149606301411 ) ) ;
#35395=AXIS2_PLACEMENT_3D ( 'NONE', #1850, #16585, #29209 ) ;
#35396=FACE_OUTER_BOUND ( 'NONE', #7447, .T. ) ;
#35397=CARTESIAN_POINT ( 'NONE',  ( -1.166969139818015533, 3.267716535433071279, 4.048737525165544183E-16 ) ) ;
#35398=ORIENTED_EDGE ( 'NONE', *, *, #33374, .F. ) ;
#35399=ORIENTED_EDGE ( 'NONE', *, *, #37283, .T. ) ;
#35401=CARTESIAN_POINT ( 'NONE',  ( 0.000000000000000000, 3.267716535433071279, -0.8267716535433055070 ) ) ;
#35402=ADVANCED_FACE ( 'NONE', ( #29199 ), #17845, .F. ) ;
#35403=FACE_OUTER_BOUND ( 'NONE', #32935, .T. ) ;
#35404=VERTEX_POINT ( 'NONE', #45183 ) ;
#35405=CARTESIAN_POINT ( 'NONE',  ( 0.000000000000000000, 3.267716535433071279, -1.141732283464563791 ) ) ;
#35406=LINE ( 'NONE', #544, #44095 ) ;
#35407=EDGE_CURVE ( 'NONE', #39871, #2241, #5964, .T. ) ;
#35408=LINE ( 'NONE', #18460, #24795 ) ;
#35410=VECTOR ( 'NONE', #29071, 39.37007874015748143 ) ;
#35412=DIRECTION ( 'NONE',  ( -0.000000000000000000, 0.000000000000000000, 1.000000000000000000 ) ) ;
#35417=VECTOR ( 'NONE', #28422, 39.37007874015748143 ) ;
#35418=ORIENTED_EDGE ( 'NONE', *, *, #3676, .F. ) ;
#35419=ORIENTED_EDGE ( 'NONE', *, *, #22376, .F. ) ;
#35420=LINE ( 'NONE', #15543, #1810 ) ;
#35422=EDGE_CURVE ( 'NONE', #15256, #11390, #29462, .T. ) ;
#35423=CARTESIAN_POINT ( 'NONE',  ( -2.097080421798980687, 3.267716535433071279, -0.1968503937007880511 ) ) ;
#35424=EDGE_LOOP ( 'NONE', ( #39735, #25432, #105, #27963 ) ) ;
#35427=DIRECTION ( 'NONE',  ( 1.000000000000000000, -0.000000000000000000, 0.000000000000000000 ) ) ;
#35429=CARTESIAN_POINT ( 'NONE',  ( -1.091055626815042201, 3.267716535433071279, 0.1181102362204705658 ) ) ;
#35430=VERTEX_POINT ( 'NONE', #44434 ) ;
#35431=LINE ( 'NONE', #3934, #35891 ) ;
#35432=FACE_OUTER_BOUND ( 'NONE', #34510, .T. ) ;
#35433=DIRECTION ( 'NONE',  ( -3.469446951953613696E-16, 0.000000000000000000, -1.000000000000000000 ) ) ;
#35437=ORIENTED_EDGE ( 'NONE', *, *, #33676, .T. ) ;
#35440=ORIENTED_EDGE ( 'NONE', *, *, #735, .F. ) ;
#35441=VERTEX_POINT ( 'NONE', #36707 ) ;
#35442=LINE ( 'NONE', #60, #30549 ) ;
#35443=DIRECTION ( 'NONE',  ( 1.000000000000000000, 0.000000000000000000, -3.469446951953613696E-16 ) ) ;
#35445=EDGE_CURVE ( 'NONE', #50136, #14952, #37480, .T. ) ;
#35447=VERTEX_POINT ( 'NONE', #44679 ) ;
#35448=VERTEX_POINT ( 'NONE', #1330 ) ;
#35449=DIRECTION ( 'NONE',  ( 0.000000000000000000, 0.000000000000000000, 1.000000000000000000 ) ) ;
#35450=DIRECTION ( 'NONE',  ( -1.000000000000000000, 0.000000000000000000, 1.734723475976806848E-16 ) ) ;
#35451=DIRECTION ( 'NONE',  ( 1.734723475976806848E-16, -0.000000000000000000, 1.000000000000000000 ) ) ;
#35452=ORIENTED_EDGE ( 'NONE', *, *, #14272, .F. ) ;
#35453=CARTESIAN_POINT ( 'NONE',  ( -1.439733046521776583, 3.346456692913386100, -0.9448818897637762948 ) ) ;
#35454=CARTESIAN_POINT ( 'NONE',  ( -1.166969139818016199, 0.000000000000000000, 1.850393700787392293 ) ) ;
#35456=CARTESIAN_POINT ( 'NONE',  ( 0.2727639067037604947, 0.000000000000000000, 0.7874015748031454320 ) ) ;
#35458=ORIENTED_EDGE ( 'NONE', *, *, #32880, .F. ) ;
#35459=VECTOR ( 'NONE', #2101, 39.37007874015748143 ) ;
#35460=DIRECTION ( 'NONE',  ( -3.469446951953613696E-16, 0.000000000000000000, -1.000000000000000000 ) ) ;
#35463=CARTESIAN_POINT ( 'NONE',  ( 0.1968503937007873017, 3.267716535433071279, -1.574803149606293529 ) ) ;
#35464=DIRECTION ( 'NONE',  ( -1.000000000000000000, 0.000000000000000000, 1.734723475976806848E-16 ) ) ;
#35470=ADVANCED_FACE ( 'NONE', ( #44178 ), #16830, .F. ) ;
#35472=EDGE_CURVE ( 'NONE', #13662, #44152, #32847, .T. ) ;
#35473=CARTESIAN_POINT ( 'NONE',  ( 1.363819533518803029, 0.000000000000000000, -1.417322834645665219 ) ) ;
#35475=EDGE_LOOP ( 'NONE', ( #1969, #9675, #48027, #7686 ) ) ;
#35476=DIRECTION ( 'NONE',  ( 0.000000000000000000, 0.000000000000000000, 1.000000000000000000 ) ) ;
#35477=LINE ( 'NONE', #19716, #14988 ) ;
#35478=AXIS2_PLACEMENT_3D ( 'NONE', #19889, #35658, #41701 ) ;
#35479=ORIENTED_EDGE ( 'NONE', *, *, #3239, .T. ) ;
#35481=AXIS2_PLACEMENT_3D ( 'NONE', #22506, #30002, #37761 ) ;
#35482=CARTESIAN_POINT ( 'NONE',  ( -0.2727639067037608278, 3.346456692913386100, -0.6692913385826758654 ) ) ;
#35483=EDGE_CURVE ( 'NONE', #1405, #46941, #36965, .T. ) ;
#35487=LINE ( 'NONE', #107, #34896 ) ;
#35489=ORIENTED_EDGE ( 'NONE', *, *, #10631, .T. ) ;
#35490=PLANE ( 'NONE',  #29632 ) ;
#35491=VECTOR ( 'NONE', #37169, 39.37007874015748143 ) ;
#35492=ORIENTED_EDGE ( 'NONE', *, *, #15114, .T. ) ;
#35496=LINE ( 'NONE', #7370, #9517 ) ;
#35497=ADVANCED_FACE ( 'NONE', ( #5461 ), #44937, .F. ) ;
#35498=EDGE_LOOP ( 'NONE', ( #45806, #42889, #4397, #47507 ) ) ;
#35499=ORIENTED_EDGE ( 'NONE', *, *, #5250, .T. ) ;
#35500=DIRECTION ( 'NONE',  ( 0.000000000000000000, 0.000000000000000000, 1.000000000000000000 ) ) ;
#35501=PLANE ( 'NONE',  #3192 ) ;
#35503=PLANE ( 'NONE',  #12673 ) ;
#35506=EDGE_CURVE ( 'NONE', #39358, #10544, #13213, .T. ) ;
#35508=ORIENTED_EDGE ( 'NONE', *, *, #18903, .T. ) ;
#35510=LINE ( 'NONE', #12523, #14257 ) ;
#35512=CARTESIAN_POINT ( 'NONE',  ( 0.7423782071083085965, 3.267716535433071279, 0.7480314960629872445 ) ) ;
#35513=ORIENTED_EDGE ( 'NONE', *, *, #26380, .F. ) ;
#35514=EDGE_CURVE ( 'NONE', #33042, #26820, #37219, .T. ) ;
#35515=LINE ( 'NONE', #20004, #3500 ) ;
#35516=ORIENTED_EDGE ( 'NONE', *, *, #34231, .F. ) ;
#35517=EDGE_LOOP ( 'NONE', ( #8734, #17918, #22759, #5085, #4396 ) ) ;
#35520=ADVANCED_FACE ( 'NONE', ( #40574 ), #12956, .F. ) ;
#35522=VECTOR ( 'NONE', #3803, 39.37007874015748143 ) ;
#35523=EDGE_LOOP ( 'NONE', ( #39557, #46649, #47080, #44563 ) ) ;
#35525=LINE ( 'NONE', #15646, #1361 ) ;
#35527=VERTEX_POINT ( 'NONE', #48277 ) ;
#35529=DIRECTION ( 'NONE',  ( -1.000000000000000000, -0.000000000000000000, -0.000000000000000000 ) ) ;
#35530=DIRECTION ( 'NONE',  ( 1.000000000000000000, 0.000000000000000000, 0.000000000000000000 ) ) ;
#35532=EDGE_CURVE ( 'NONE', #11836, #31518, #28688, .T. ) ;
#35533=CARTESIAN_POINT ( 'NONE',  ( 1.287906020515830141, 3.267716535433071279, -4.468321617281355077E-16 ) ) ;
#35534=EDGE_CURVE ( 'NONE', #14773, #26179, #10607, .T. ) ;
#35535=EDGE_CURVE ( 'NONE', #41248, #40553, #50294, .T. ) ;
#35536=LINE ( 'NONE', #16686, #4707 ) ;
#35538=VERTEX_POINT ( 'NONE', #29972 ) ;
#35540=CARTESIAN_POINT ( 'NONE',  ( -2.258024766633058622, 3.346456692913386100, -0.1574803149606298636 ) ) ;
#35541=LINE ( 'NONE', #20812, #7536 ) ;
#35542=VERTEX_POINT ( 'NONE', #34612 ) ;
#35543=CARTESIAN_POINT ( 'NONE',  ( -0.8182917201112819283, 3.346456692913386100, -1.299212598425193210 ) ) ;
#35544=FACE_OUTER_BOUND ( 'NONE', #13439, .T. ) ;
#35545=VERTEX_POINT ( 'NONE', #26845 ) ;
#35546=LINE ( 'NONE', #9458, #14752 ) ;
#35547=DIRECTION ( 'NONE',  ( 1.000000000000000000, 0.000000000000000000, 0.000000000000000000 ) ) ;
#35550=LINE ( 'NONE', #1203, #33196 ) ;
#35551=VERTEX_POINT ( 'NONE', #30733 ) ;
#35553=PLANE ( 'NONE',  #30846 ) ;
#35554=VECTOR ( 'NONE', #21735, 39.37007874015748143 ) ;
#35555=LINE ( 'NONE', #24193, #6157 ) ;
#35556=CARTESIAN_POINT ( 'NONE',  ( -1.166969139818015533, 0.000000000000000000, 1.417322834645662777 ) ) ;
#35558=EDGE_CURVE ( 'NONE', #37873, #48466, #10853, .T. ) ;
#35559=VERTEX_POINT ( 'NONE', #45434 ) ;
#35560=ORIENTED_EDGE ( 'NONE', *, *, #31943, .F. ) ;
#35563=DIRECTION ( 'NONE',  ( 0.000000000000000000, 0.000000000000000000, 1.000000000000000000 ) ) ;
#35565=DIRECTION ( 'NONE',  ( 1.000000000000000000, 0.000000000000000000, 0.000000000000000000 ) ) ;
#35566=ORIENTED_EDGE ( 'NONE', *, *, #48840, .T. ) ;
#35568=DIRECTION ( 'NONE',  ( -0.000000000000000000, 1.000000000000000000, -0.000000000000000000 ) ) ;
#35573=EDGE_CURVE ( 'NONE', #10030, #15453, #34109, .T. ) ;
#35574=LINE ( 'NONE', #10620, #28948 ) ;
#35576=ORIENTED_EDGE ( 'NONE', *, *, #21292, .T. ) ;
#35577=VERTEX_POINT ( 'NONE', #3108 ) ;
#35578=CARTESIAN_POINT ( 'NONE',  ( 0.000000000000000000, 3.267716535433071279, 0.7480314960629874665 ) ) ;
#35581=ORIENTED_EDGE ( 'NONE', *, *, #48394, .T. ) ;
#35584=LINE ( 'NONE', #37068, #7263 ) ;
#35585=ORIENTED_EDGE ( 'NONE', *, *, #263, .F. ) ;
#35586=CARTESIAN_POINT ( 'NONE',  ( -1.901721518280075296, 3.346456692913386100, 0.9055118110236167750 ) ) ;
#35589=VECTOR ( 'NONE', #41898, 39.37007874015748143 ) ;
#35590=EDGE_CURVE ( 'NONE', #46985, #15789, #6228, .T. ) ;
#35592=DIRECTION ( 'NONE',  ( -3.469446951953613696E-16, 0.000000000000000000, -1.000000000000000000 ) ) ;
#35593=EDGE_CURVE ( 'NONE', #47342, #6449, #33861, .T. ) ;
#35594=EDGE_CURVE ( 'NONE', #3086, #15117, #14220, .T. ) ;
#35595=VERTEX_POINT ( 'NONE', #18610 ) ;
#35598=LINE ( 'NONE', #26574, #31057 ) ;
#35599=DIRECTION ( 'NONE',  ( -0.000000000000000000, 1.000000000000000000, -0.000000000000000000 ) ) ;
#35601=CARTESIAN_POINT ( 'NONE',  ( 1.244991204790707684, 3.346456692913386100, -1.771653543307081691 ) ) ;
#35604=DIRECTION ( 'NONE',  ( -0.000000000000000000, 1.000000000000000000, -0.000000000000000000 ) ) ;
#35605=VECTOR ( 'NONE', #25384, 39.37007874015748143 ) ;
#35606=DIRECTION ( 'NONE',  ( -0.000000000000000000, 1.000000000000000000, -0.000000000000000000 ) ) ;
#35607=ORIENTED_EDGE ( 'NONE', *, *, #22281, .F. ) ;
#35608=CARTESIAN_POINT ( 'NONE',  ( 0.4696143004045479352, 0.000000000000000000, -1.102362204724405714 ) ) ;
#35609=VERTEX_POINT ( 'NONE', #38736 ) ;
#35610=CARTESIAN_POINT ( 'NONE',  ( 1.909347346926324018, 3.267716535433071279, -0.8893194486674360633 ) ) ;
#35613=DIRECTION ( 'NONE',  ( -3.469446951953613696E-16, 0.000000000000000000, -1.000000000000000000 ) ) ;
#35614=PLANE ( 'NONE',  #16269 ) ;
#35616=VERTEX_POINT ( 'NONE', #6732 ) ;
#35617=DIRECTION ( 'NONE',  ( -0.000000000000000000, 1.000000000000000000, -0.000000000000000000 ) ) ;
#35618=ORIENTED_EDGE ( 'NONE', *, *, #17627, .F. ) ;
#35619=DIRECTION ( 'NONE',  ( -3.469446951953613696E-16, 0.000000000000000000, -1.000000000000000000 ) ) ;
#35625=ORIENTED_EDGE ( 'NONE', *, *, #14707, .T. ) ;
#35626=EDGE_CURVE ( 'NONE', #12397, #27247, #22234, .T. ) ;
#35627=VECTOR ( 'NONE', #31311, 39.37007874015748143 ) ;
#35629=VERTEX_POINT ( 'NONE', #42343 ) ;
#35631=PLANE ( 'NONE',  #22698 ) ;
#35632=DIRECTION ( 'NONE',  ( -3.469446951953613696E-16, 0.000000000000000000, -1.000000000000000000 ) ) ;
#35634=AXIS2_PLACEMENT_3D ( 'NONE', #47241, #23792, #4172 ) ;
#35635=EDGE_LOOP ( 'NONE', ( #48410, #26656, #26559, #20610 ) ) ;
#35637=CARTESIAN_POINT ( 'NONE',  ( -1.091055626815042645, 3.267716535433071279, 1.870389530743259199 ) ) ;
#35640=ORIENTED_EDGE ( 'NONE', *, *, #18005, .T. ) ;
#35642=EDGE_CURVE ( 'NONE', #45218, #25764, #19098, .T. ) ;
#35644=VERTEX_POINT ( 'NONE', #6987 ) ;
#35645=CARTESIAN_POINT ( 'NONE',  ( 0.1968503937007873017, 0.000000000000000000, -0.9448818897637765168 ) ) ;
#35646=LINE ( 'NONE', #22762, #38199 ) ;
#35647=EDGE_CURVE ( 'NONE', #23969, #34396, #2603, .T. ) ;
#35648=CARTESIAN_POINT ( 'NONE',  ( 0.5455278134075212115, 0.000000000000000000, 0.9448818897637746295 ) ) ;
#35649=DIRECTION ( 'NONE',  ( 0.000000000000000000, -1.000000000000000000, 0.000000000000000000 ) ) ;
#35650=EDGE_CURVE ( 'NONE', #38168, #39348, #29720, .T. ) ;
#35651=ORIENTED_EDGE ( 'NONE', *, *, #6839, .T. ) ;
#35653=CARTESIAN_POINT ( 'NONE',  ( 0.7423782071083084855, 0.000000000000000000, -1.574803149606293529 ) ) ;
#35654=EDGE_CURVE ( 'NONE', #43157, #30486, #43539, .T. ) ;
#35655=DIRECTION ( 'NONE',  ( -3.469446951953613696E-16, 0.000000000000000000, -1.000000000000000000 ) ) ;
#35656=EDGE_LOOP ( 'NONE', ( #15442, #16973, #42425, #43359 ) ) ;
#35658=DIRECTION ( 'NONE',  ( 0.000000000000000000, 0.000000000000000000, -1.000000000000000000 ) ) ;
#35659=VECTOR ( 'NONE', #48744, 39.37007874015748143 ) ;
#35660=CARTESIAN_POINT ( 'NONE',  ( -1.198202975868768005, 3.346456692913386100, 1.732283464566920950 ) ) ;
#35662=VECTOR ( 'NONE', #5859, 39.37007874015748143 ) ;
#35663=LINE ( 'NONE', #23521, #16331 ) ;
#35666=CARTESIAN_POINT ( 'NONE',  ( 1.091055626815042645, 3.346456692913386100, 0.9448818897637746295 ) ) ;
#35667=AXIS2_PLACEMENT_3D ( 'NONE', #26938, #15580, #10947 ) ;
#35668=VERTEX_POINT ( 'NONE', #47189 ) ;
#35669=VECTOR ( 'NONE', #47938, 39.37007874015748143 ) ;
#35670=ORIENTED_EDGE ( 'NONE', *, *, #19626, .T. ) ;
#35672=DIRECTION ( 'NONE',  ( -3.469446951953613696E-16, 0.000000000000000000, -1.000000000000000000 ) ) ;
#35673=CARTESIAN_POINT ( 'NONE',  ( -1.195183497228115035E-16, 3.346456692913386100, 0.6299212598425161236 ) ) ;
#35675=ORIENTED_EDGE ( 'NONE', *, *, #48117, .F. ) ;
#35680=VERTEX_POINT ( 'NONE', #24260 ) ;
#35681=CARTESIAN_POINT ( 'NONE',  ( 0.4696143004045479352, 0.000000000000000000, -0.4724409448818886470 ) ) ;
#35684=VERTEX_POINT ( 'NONE', #7489 ) ;
#35685=EDGE_CURVE ( 'NONE', #15117, #35815, #8508, .T. ) ;
#35686=ORIENTED_EDGE ( 'NONE', *, *, #37283, .F. ) ;
#35687=ORIENTED_EDGE ( 'NONE', *, *, #27422, .T. ) ;
#35688=PLANE ( 'NONE',  #44677 ) ;
#35690=EDGE_CURVE ( 'NONE', #11338, #681, #27858, .T. ) ;
#35693=LINE ( 'NONE', #40591, #10788 ) ;
#35695=CARTESIAN_POINT ( 'NONE',  ( -1.091055626815042645, 3.346456692913386100, -0.5118110236220467790 ) ) ;
#35697=EDGE_LOOP ( 'NONE', ( #27857, #4585, #37670, #23997 ) ) ;
#35702=CARTESIAN_POINT ( 'NONE',  ( 0.2727639067037604947, 0.000000000000000000, 0.4724409448818868706 ) ) ;
#35703=VECTOR ( 'NONE', #33440, 39.37007874015748143 ) ;
#35704=DIRECTION ( 'NONE',  ( -0.000000000000000000, 0.000000000000000000, 1.000000000000000000 ) ) ;
#35705=ORIENTED_EDGE ( 'NONE', *, *, #16294, .F. ) ;
#35706=LINE ( 'NONE', #22825, #38156 ) ;
#35708=EDGE_LOOP ( 'NONE', ( #9690, #831, #40342, #10429 ) ) ;
#35709=CARTESIAN_POINT ( 'NONE',  ( 1.560669927219590303, 3.346456692913386100, -1.102362204724405714 ) ) ;
#35710=VECTOR ( 'NONE', #46964, 39.37007874015748143 ) ;
#35711=VECTOR ( 'NONE', #22964, 39.37007874015748143 ) ;
#35712=CARTESIAN_POINT ( 'NONE',  ( 4.268512490100411402E-16, 3.267716535433071279, 1.889763779527550369 ) ) ;
#35715=CARTESIAN_POINT ( 'NONE',  ( 0.2727639067037604947, 3.267716535433071279, 0.1574803149606283648 ) ) ;
#35716=VERTEX_POINT ( 'NONE', #3616 ) ;
#35717=VERTEX_POINT ( 'NONE', #11611 ) ;
#35719=EDGE_CURVE ( 'NONE', #30154, #216, #15733, .T. ) ;
#35720=ORIENTED_EDGE ( 'NONE', *, *, #18396, .F. ) ;
#35721=CARTESIAN_POINT ( 'NONE',  ( -1.091055626815042645, 3.267716535433071279, 1.892679809432644389E-16 ) ) ;
#35723=DIRECTION ( 'NONE',  ( -3.469446951953613696E-16, 0.000000000000000000, -1.000000000000000000 ) ) ;
#35724=LINE ( 'NONE', #36499, #43472 ) ;
#35725=EDGE_LOOP ( 'NONE', ( #44580, #34559, #9862, #47920 ) ) ;
#35726=CARTESIAN_POINT ( 'NONE',  ( 1.287906020515830141, 0.000000000000000000, -8.878505979408855953E-16 ) ) ;
#35727=ADVANCED_FACE ( 'NONE', ( #19347 ), #506, .F. ) ;
#35729=ORIENTED_EDGE ( 'NONE', *, *, #15757, .T. ) ;
#35734=DIRECTION ( 'NONE',  ( -1.000000000000000000, 0.000000000000000000, 0.000000000000000000 ) ) ;
#35735=DIRECTION ( 'NONE',  ( 1.734723475976806848E-16, -0.000000000000000000, 1.000000000000000000 ) ) ;
#35736=CARTESIAN_POINT ( 'NONE',  ( 1.015142113812069313, 0.000000000000000000, -0.03937007874015881204 ) ) ;
#35737=VECTOR ( 'NONE', #49255, 39.37007874015748143 ) ;
#35738=ORIENTED_EDGE ( 'NONE', *, *, #17875, .T. ) ;
#35740=DIRECTION ( 'NONE',  ( -0.000000000000000000, 1.000000000000000000, -0.000000000000000000 ) ) ;
#35745=PLANE ( 'NONE',  #39167 ) ;
#35746=FACE_OUTER_BOUND ( 'NONE', #31314, .T. ) ;
#35747=DIRECTION ( 'NONE',  ( 1.000000000000000000, 0.000000000000000000, 0.000000000000000000 ) ) ;
#35751=AXIS2_PLACEMENT_3D ( 'NONE', #35726, #8363, #4488 ) ;
#35752=LINE ( 'NONE', #15866, #28761 ) ;
#35753=ADVANCED_FACE ( 'NONE', ( #43089 ), #7738, .F. ) ;
#35754=EDGE_LOOP ( 'NONE', ( #27121, #3810, #37544, #12727 ) ) ;
#35756=CARTESIAN_POINT ( 'NONE',  ( -1.166969139818015977, 3.346456692913386100, -0.1574803149606300023 ) ) ;
#35757=CARTESIAN_POINT ( 'NONE',  ( 2.378961647330872786, 0.000000000000000000, 0.4330708661417287386 ) ) ;
#35758=EDGE_CURVE ( 'NONE', #51008, #17239, #19851, .T. ) ;
#35763=DIRECTION ( 'NONE',  ( -0.000000000000000000, 1.000000000000000000, -0.000000000000000000 ) ) ;
#35764=DIRECTION ( 'NONE',  ( -0.000000000000000000, 1.000000000000000000, -0.000000000000000000 ) ) ;
#35766=ADVANCED_FACE ( 'NONE', ( #28113 ), #39231, .F. ) ;
#35767=DIRECTION ( 'NONE',  ( 1.000000000000000000, 0.000000000000000000, 0.000000000000000000 ) ) ;
#35768=FACE_BOUND ( 'NONE', #45229, .T. ) ;
#35770=DIRECTION ( 'NONE',  ( -1.000000000000000000, 0.000000000000000000, -0.000000000000000000 ) ) ;
#35771=ORIENTED_EDGE ( 'NONE', *, *, #21433, .F. ) ;
#35772=EDGE_LOOP ( 'NONE', ( #43423, #39506, #39862, #31482, #21424 ) ) ;
#35775=ORIENTED_EDGE ( 'NONE', *, *, #3418, .F. ) ;
#35776=VERTEX_POINT ( 'NONE', #36135 ) ;
#35777=DIRECTION ( 'NONE',  ( 0.000000000000000000, 0.000000000000000000, 1.000000000000000000 ) ) ;
#35778=ORIENTED_EDGE ( 'NONE', *, *, #766, .F. ) ;
#35779=AXIS2_PLACEMENT_3D ( 'NONE', #47861, #28021, #12533 ) ;
#35781=ADVANCED_FACE ( 'NONE', ( #51047 ), #47448, .F. ) ;
#35782=AXIS2_PLACEMENT_3D ( 'NONE', #13395, #25011, #16506 ) ;
#35784=LINE ( 'NONE', #16425, #50746 ) ;
#35785=LINE ( 'NONE', #36047, #11052 ) ;
#35786=VECTOR ( 'NONE', #2416, 39.37007874015748143 ) ;
#35787=VECTOR ( 'NONE', #6720, 39.37007874015748143 ) ;
#35788=EDGE_CURVE ( 'NONE', #30730, #14887, #23736, .T. ) ;
#35789=DIRECTION ( 'NONE',  ( -1.000000000000000000, 0.000000000000000000, 1.734723475976806848E-16 ) ) ;
#35790=LINE ( 'NONE', #16166, #14631 ) ;
#35791=CARTESIAN_POINT ( 'NONE',  ( 1.287906020515830141, 3.267716535433071279, -0.6299212598425181220 ) ) ;
#35792=VECTOR ( 'NONE', #45171, 39.37007874015748143 ) ;
#35793=ORIENTED_EDGE ( 'NONE', *, *, #26415, .T. ) ;
#35795=FACE_OUTER_BOUND ( 'NONE', #3802, .T. ) ;
#35796=ADVANCED_FACE ( 'NONE', ( #12125 ), #30985, .F. ) ;
#35799=PLANE ( 'NONE',  #19880 ) ;
#35801=ORIENTED_EDGE ( 'NONE', *, *, #30368, .T. ) ;
#35802=LINE ( 'NONE', #38909, #13100 ) ;
#35808=CARTESIAN_POINT ( 'NONE',  ( -2.182111253630085290, 3.346456692913386100, 0.7480314960629874665 ) ) ;
#35809=EDGE_CURVE ( 'NONE', #26431, #36543, #17532, .T. ) ;
#35810=DIRECTION ( 'NONE',  ( 1.000000000000000000, 0.000000000000000000, -3.469446951953613696E-16 ) ) ;
#35812=CARTESIAN_POINT ( 'NONE',  ( 1.636583440222563857, 3.267716535433071279, -2.839019714148966584E-16 ) ) ;
#35815=VERTEX_POINT ( 'NONE', #33294 ) ;
#35816=ORIENTED_EDGE ( 'NONE', *, *, #9955, .F. ) ;
#35817=AXIS2_PLACEMENT_3D ( 'NONE', #10204, #41200, #37071 ) ;
#35818=LINE ( 'NONE', #705, #45179 ) ;
#35819=EDGE_LOOP ( 'NONE', ( #19601, #31642, #27118, #32675 ) ) ;
#35820=DIRECTION ( 'NONE',  ( 1.734723475976806848E-16, 0.000000000000000000, 1.000000000000000000 ) ) ;
#35822=AXIS2_PLACEMENT_3D ( 'NONE', #44615, #16765, #40769 ) ;
#35823=EDGE_CURVE ( 'NONE', #49048, #19022, #36651, .T. ) ;
#35826=ORIENTED_EDGE ( 'NONE', *, *, #17426, .F. ) ;
#35830=AXIS2_PLACEMENT_3D ( 'NONE', #625, #36258, #879 ) ;
#35832=ORIENTED_EDGE ( 'NONE', *, *, #33582, .F. ) ;
#35835=LINE ( 'NONE', #28075, #9764 ) ;
#35840=ORIENTED_EDGE ( 'NONE', *, *, #6894, .F. ) ;
#35841=CARTESIAN_POINT ( 'NONE',  ( 1.636583440222563857, 3.346456692913386100, -0.6299212598425181220 ) ) ;
#35842=ORIENTED_EDGE ( 'NONE', *, *, #28751, .T. ) ;
#35843=DIRECTION ( 'NONE',  ( -3.469446951953613696E-16, 0.000000000000000000, -1.000000000000000000 ) ) ;
#35844=DIRECTION ( 'NONE',  ( -0.000000000000000000, 1.000000000000000000, -0.000000000000000000 ) ) ;
#35845=EDGE_CURVE ( 'NONE', #34706, #13220, #9793, .T. ) ;
#35849=DIRECTION ( 'NONE',  ( 0.000000000000000000, 0.000000000000000000, 1.000000000000000000 ) ) ;
#35852=LINE ( 'NONE', #743, #4379 ) ;
#35853=AXIS2_PLACEMENT_3D ( 'NONE', #11398, #7279, #26878 ) ;
#35855=EDGE_CURVE ( 'NONE', #27411, #46657, #20892, .T. ) ;
#35856=VECTOR ( 'NONE', #19480, 39.37007874015748143 ) ;
#35857=CARTESIAN_POINT ( 'NONE',  ( 0.000000000000000000, 3.267716535433071279, -0.6299212598425177889 ) ) ;
#35861=ADVANCED_FACE ( 'NONE', ( #24515 ), #48221, .F. ) ;
#35862=CARTESIAN_POINT ( 'NONE',  ( 0.1968503937007873017, 3.267716535433071279, -6.829619984160653116E-17 ) ) ;
#35864=VERTEX_POINT ( 'NONE', #41287 ) ;
#35865=DIRECTION ( 'NONE',  ( -3.469446951953613696E-16, 0.000000000000000000, -1.000000000000000000 ) ) ;
#35866=EDGE_CURVE ( 'NONE', #39604, #12011, #36330, .T. ) ;
#35867=ORIENTED_EDGE ( 'NONE', *, *, #45329, .T. ) ;
#35869=LINE ( 'NONE', #43849, #15463 ) ;
#35870=DIRECTION ( 'NONE',  ( 1.734723475976806848E-16, -0.000000000000000000, 1.000000000000000000 ) ) ;
#35872=CARTESIAN_POINT ( 'NONE',  ( 0.000000000000000000, 3.267716535433071279, 0.6299212598425164567 ) ) ;
#35876=ADVANCED_FACE ( 'NONE', ( #40267 ), #44622, .F. ) ;
#35877=CARTESIAN_POINT ( 'NONE',  ( 1.091055626815043311, 3.267716535433071279, 1.574803149606291974 ) ) ;
#35883=ORIENTED_EDGE ( 'NONE', *, *, #40550, .T. ) ;
#35885=VECTOR ( 'NONE', #5671, 39.37007874015748143 ) ;
#35886=VECTOR ( 'NONE', #4617, 39.37007874015748143 ) ;
#35889=FACE_BOUND ( 'NONE', #18389, .T. ) ;
#35891=VECTOR ( 'NONE', #15555, 39.37007874015748143 ) ;
#35893=CARTESIAN_POINT ( 'NONE',  ( -1.536664496436148184E-16, 0.000000000000000000, 0.1181102362204701633 ) ) ;
#35894=LINE ( 'NONE', #520, #1092 ) ;
#35895=EDGE_LOOP ( 'NONE', ( #33534, #33908, #24699, #5482 ) ) ;
#35896=DIRECTION ( 'NONE',  ( -0.000000000000000000, 1.000000000000000000, -0.000000000000000000 ) ) ;
#35897=CIRCLE ( 'NONE', #15293, 2.106299212598425008 ) ;
#35898=ORIENTED_EDGE ( 'NONE', *, *, #27335, .F. ) ;
#35899=VERTEX_POINT ( 'NONE', #32268 ) ;
#35901=ORIENTED_EDGE ( 'NONE', *, *, #3873, .T. ) ;
#35903=LINE ( 'NONE', #28913, #31587 ) ;
#35905=LINE ( 'NONE', #8535, #22229 ) ;
#35906=ORIENTED_EDGE ( 'NONE', *, *, #18833, .T. ) ;
#35907=VERTEX_POINT ( 'NONE', #765 ) ;
#35914=CARTESIAN_POINT ( 'NONE',  ( -1.091055626815042201, 0.000000000000000000, 0.9448818897637749625 ) ) ;
#35918=DIRECTION ( 'NONE',  ( -0.000000000000000000, 1.000000000000000000, -0.000000000000000000 ) ) ;
#35920=FACE_OUTER_BOUND ( 'NONE', #8509, .T. ) ;
#35921=ORIENTED_EDGE ( 'NONE', *, *, #8749, .F. ) ;
#35923=DIRECTION ( 'NONE',  ( 1.734723475976806848E-16, -0.000000000000000000, 1.000000000000000000 ) ) ;
#35924=VECTOR ( 'NONE', #21951, 39.37007874015748143 ) ;
#35925=ORIENTED_EDGE ( 'NONE', *, *, #46859, .T. ) ;
#35926=VECTOR ( 'NONE', #34745, 39.37007874015748143 ) ;
#35927=VERTEX_POINT ( 'NONE', #36392 ) ;
#35928=LINE ( 'NONE', #16304, #15003 ) ;
#35929=PLANE ( 'NONE',  #30325 ) ;
#35934=CIRCLE ( 'NONE', #3765, 2.443628662382284489 ) ;
#35935=ORIENTED_EDGE ( 'NONE', *, *, #50886, .T. ) ;
#35937=EDGE_CURVE ( 'NONE', #40469, #39732, #42544, .T. ) ;
#35940=ORIENTED_EDGE ( 'NONE', *, *, #35249, .T. ) ;
#35942=EDGE_CURVE ( 'NONE', #21463, #22677, #29915, .T. ) ;
#35944=FACE_OUTER_BOUND ( 'NONE', #41845, .T. ) ;
#35945=EDGE_CURVE ( 'NONE', #37143, #50043, #3205, .T. ) ;
#35947=VERTEX_POINT ( 'NONE', #34310 ) ;
#35948=EDGE_LOOP ( 'NONE', ( #25778, #26862, #43297, #4425 ) ) ;
#35949=CARTESIAN_POINT ( 'NONE',  ( -1.166969139818015533, 0.000000000000000000, 0.4724409448818871482 ) ) ;
#35950=CARTESIAN_POINT ( 'NONE',  ( 2.182111253630085290, 0.000000000000000000, 0.4330708661417287386 ) ) ;
#35953=ORIENTED_EDGE ( 'NONE', *, *, #3682, .F. ) ;
#35955=CARTESIAN_POINT ( 'NONE',  ( 1.015142113812069091, 3.346456692913386100, -1.845530509571139399 ) ) ;
#35956=DIRECTION ( 'NONE',  ( 0.000000000000000000, -1.000000000000000000, 0.000000000000000000 ) ) ;
#35957=ORIENTED_EDGE ( 'NONE', *, *, #36990, .T. ) ;
#35958=LINE ( 'NONE', #43936, #31246 ) ;
#35959=CARTESIAN_POINT ( 'NONE',  ( -1.299212598425207865, 3.346456692913386100, 1.732283464566920950 ) ) ;
#35960=LINE ( 'NONE', #43682, #33613 ) ;
#35961=AXIS2_PLACEMENT_3D ( 'NONE', #43454, #28478, #44229 ) ;
#35962=VERTEX_POINT ( 'NONE', #33807 ) ;
#35966=EDGE_LOOP ( 'NONE', ( #38970, #14222, #47210, #14274 ) ) ;
#35967=VECTOR ( 'NONE', #210, 39.37007874015748143 ) ;
#35968=DIRECTION ( 'NONE',  ( 0.000000000000000000, 0.000000000000000000, 1.000000000000000000 ) ) ;
#35969=EDGE_LOOP ( 'NONE', ( #38109, #24044, #12471, #33000 ) ) ;
#35970=ORIENTED_EDGE ( 'NONE', *, *, #43608, .T. ) ;
#35972=VECTOR ( 'NONE', #49374, 39.37007874015748143 ) ;
#35974=VECTOR ( 'NONE', #9870, 39.37007874015748143 ) ;
#35977=EDGE_LOOP ( 'NONE', ( #36987, #10745, #6421, #3988 ) ) ;
#35978=ORIENTED_EDGE ( 'NONE', *, *, #22942, .T. ) ;
#35979=VECTOR ( 'NONE', #16976, 39.37007874015748143 ) ;
#35980=PRODUCT ( 'Back Cover', 'Back Cover', '', ( #20399 ) ) ;
#35982=FACE_OUTER_BOUND ( 'NONE', #32857, .T. ) ;
#35983=LINE ( 'NONE', #43959, #21000 ) ;
#35985=EDGE_CURVE ( 'NONE', #26538, #6620, #45631, .T. ) ;
#35986=PLANE ( 'NONE',  #49914 ) ;
#35989=EDGE_CURVE ( 'NONE', #19986, #45868, #38186, .T. ) ;
#35993=VERTEX_POINT ( 'NONE', #18805 ) ;
#35994=DIRECTION ( 'NONE',  ( -0.000000000000000000, 1.000000000000000000, -0.000000000000000000 ) ) ;
#35996=LINE ( 'NONE', #623, #744 ) ;
#35997=ORIENTED_EDGE ( 'NONE', *, *, #23616, .T. ) ;
#35998=AXIS2_PLACEMENT_3D ( 'NONE', #22404, #30406, #49465 ) ;
#35999=PLANE ( 'NONE',  #19301 ) ;
#36001=CARTESIAN_POINT ( 'NONE',  ( 1.363819533518803251, 3.267716535433071279, 1.102362204724403938 ) ) ;
#36002=AXIS2_PLACEMENT_3D ( 'NONE', #47166, #7223, #23204 ) ;
#36003=VECTOR ( 'NONE', #25436, 39.37007874015748143 ) ;
#36004=ORIENTED_EDGE ( 'NONE', *, *, #19366, .T. ) ;
#36005=DIRECTION ( 'NONE',  ( -1.000000000000000000, -0.000000000000000000, -0.000000000000000000 ) ) ;
#36007=ORIENTED_EDGE ( 'NONE', *, *, #19059, .F. ) ;
#36010=EDGE_CURVE ( 'NONE', #48217, #47654, #26041, .T. ) ;
#36011=CARTESIAN_POINT ( 'NONE',  ( 0.2727639067037604392, 0.000000000000000000, 0.5905511811023579360 ) ) ;
#36012=DIRECTION ( 'NONE',  ( -0.000000000000000000, 1.000000000000000000, -0.000000000000000000 ) ) ;
#36017=CARTESIAN_POINT ( 'NONE',  ( 0.000000000000000000, 3.267716535433071279, 0.000000000000000000 ) ) ;
#36018=DIRECTION ( 'NONE',  ( 0.000000000000000000, -1.000000000000000000, 0.000000000000000000 ) ) ;
#36020=EDGE_CURVE ( 'NONE', #48211, #47774, #10043, .T. ) ;
#36021=ORIENTED_EDGE ( 'NONE', *, *, #45651, .F. ) ;
#36022=DIRECTION ( 'NONE',  ( 1.734723475976806848E-16, 0.000000000000000000, 1.000000000000000000 ) ) ;
#36026=ORIENTED_EDGE ( 'NONE', *, *, #5703, .F. ) ;
#36027=ORIENTED_EDGE ( 'NONE', *, *, #40368, .F. ) ;
#36028=DIRECTION ( 'NONE',  ( -3.469446951953613696E-16, 0.000000000000000000, -1.000000000000000000 ) ) ;
#36030=LINE ( 'NONE', #16407, #7394 ) ;
#36032=FACE_BOUND ( 'NONE', #10636, .T. ) ;
#36033=VERTEX_POINT ( 'NONE', #30429 ) ;
#36034=DIRECTION ( 'NONE',  ( -0.000000000000000000, 1.000000000000000000, -0.000000000000000000 ) ) ;
#36039=ORIENTED_EDGE ( 'NONE', *, *, #34668, .T. ) ;
#36041=FACE_OUTER_BOUND ( 'NONE', #2463, .T. ) ;
#36043=ORIENTED_EDGE ( 'NONE', *, *, #8400, .T. ) ;
#36045=LINE ( 'NONE', #15897, #32032 ) ;
#36046=DIRECTION ( 'NONE',  ( -0.000000000000000000, 1.000000000000000000, -0.000000000000000000 ) ) ;
#36047=CARTESIAN_POINT ( 'NONE',  ( 1.287906020515830141, 0.000000000000000000, 0.6299212598425161236 ) ) ;
#36048=CARTESIAN_POINT ( 'NONE',  ( 0.2727639067037610499, 0.000000000000000000, 1.102362204724404160 ) ) ;
#36049=EDGE_CURVE ( 'NONE', #4521, #1056, #14680, .T. ) ;
#36050=DIRECTION ( 'NONE',  ( 0.000000000000000000, 0.000000000000000000, -1.000000000000000000 ) ) ;
#36051=DIRECTION ( 'NONE',  ( 1.734723475976806848E-16, 0.000000000000000000, 1.000000000000000000 ) ) ;
#36052=VERTEX_POINT ( 'NONE', #14930 ) ;
#36053=EDGE_CURVE ( 'NONE', #5972, #47752, #11055, .T. ) ;
#36054=DIRECTION ( 'NONE',  ( -0.000000000000000000, 1.000000000000000000, -0.000000000000000000 ) ) ;
#36055=FACE_OUTER_BOUND ( 'NONE', #22324, .T. ) ;
#36056=DIRECTION ( 'NONE',  ( -1.000000000000000000, 0.000000000000000000, -0.000000000000000000 ) ) ;
#36057=EDGE_CURVE ( 'NONE', #24438, #10605, #10295, .T. ) ;
#36058=ORIENTED_EDGE ( 'NONE', *, *, #14496, .F. ) ;
#36059=LINE ( 'NONE', #35543, #38849 ) ;
#36060=DIRECTION ( 'NONE',  ( -3.469446951953613696E-16, 0.000000000000000000, -1.000000000000000000 ) ) ;
#36063=ADVANCED_FACE ( 'NONE', ( #26795 ), #37420, .F. ) ;
#36064=DIRECTION ( 'NONE',  ( -1.000000000000000000, 0.000000000000000000, 0.000000000000000000 ) ) ;
#36065=DIRECTION ( 'NONE',  ( -0.000000000000000000, 1.000000000000000000, -0.000000000000000000 ) ) ;
#36067=FACE_OUTER_BOUND ( 'NONE', #9792, .T. ) ;
#36069=LINE ( 'NONE', #27173, #19005 ) ;
#36071=LINE ( 'NONE', #24454, #21827 ) ;
#36073=DIRECTION ( 'NONE',  ( 1.734723475976806848E-16, -0.000000000000000000, 1.000000000000000000 ) ) ;
#36074=AXIS2_PLACEMENT_3D ( 'NONE', #27684, #47786, #4719 ) ;
#36075=VECTOR ( 'NONE', #8501, 39.37007874015748143 ) ;
#36076=ORIENTED_EDGE ( 'NONE', *, *, #45268, .F. ) ;
#36077=ORIENTED_EDGE ( 'NONE', *, *, #50594, .F. ) ;
#36079=ORIENTED_EDGE ( 'NONE', *, *, #27108, .F. ) ;
#36080=ADVANCED_FACE ( 'NONE', ( #34053 ), #49239, .F. ) ;
#36081=CARTESIAN_POINT ( 'NONE',  ( 0.000000000000000000, 3.267716535433071279, -6.146657985744592735E-16 ) ) ;
#36083=CARTESIAN_POINT ( 'NONE',  ( 1.909347346926324684, 3.267716535433071279, 0.1574803149606280872 ) ) ;
#36084=EDGE_LOOP ( 'NONE', ( #28114, #44358, #40599, #41595 ) ) ;
#36085=EDGE_CURVE ( 'NONE', #2922, #42532, #21922, .T. ) ;
#36087=CARTESIAN_POINT ( 'NONE',  ( -1.091055626815042645, 0.000000000000000000, -1.259842519685034690 ) ) ;
#36088=ORIENTED_EDGE ( 'NONE', *, *, #49323, .T. ) ;
#36089=PRODUCT_DEFINITION_CONTEXT ( 'detailed design', #7464, 'design' ) ;
#36090=DIRECTION ( 'NONE',  ( -0.000000000000000000, 0.000000000000000000, 1.000000000000000000 ) ) ;
#36092=AXIS2_PLACEMENT_3D ( 'NONE', #5825, #18210, #2211 ) ;
#36094=LINE ( 'NONE', #28329, #36147 ) ;
#36095=VERTEX_POINT ( 'NONE', #50484 ) ;
#36096=VERTEX_POINT ( 'NONE', #42792 ) ;
#36102=DIRECTION ( 'NONE',  ( -0.000000000000000000, 1.000000000000000000, -0.000000000000000000 ) ) ;
#36103=LINE ( 'NONE', #36361, #32484 ) ;
#36104=VECTOR ( 'NONE', #19978, 39.37007874015748143 ) ;
#36105=VECTOR ( 'NONE', #15988, 39.37007874015748143 ) ;
#36106=LINE ( 'NONE', #27833, #36303 ) ;
#36109=FACE_OUTER_BOUND ( 'NONE', #1871, .T. ) ;
#36112=AXIS2_PLACEMENT_3D ( 'NONE', #29159, #44893, #18310 ) ;
#36115=EDGE_CURVE ( 'NONE', #13057, #47970, #15440, .T. ) ;
#36116=DIRECTION ( 'NONE',  ( 1.000000000000000000, 0.000000000000000000, 0.000000000000000000 ) ) ;
#36117=EDGE_CURVE ( 'NONE', #16479, #44707, #35315, .T. ) ;
#36121=VECTOR ( 'NONE', #19313, 39.37007874015748143 ) ;
#36122=EDGE_LOOP ( 'NONE', ( #37389, #7301, #21602, #48009 ) ) ;
#36123=CARTESIAN_POINT ( 'NONE',  ( 1.909347346926324462, 0.000000000000000000, -1.299212598425194320 ) ) ;
#36124=VECTOR ( 'NONE', #1760, 39.37007874015748143 ) ;
#36126=CARTESIAN_POINT ( 'NONE',  ( -0.8942052331142547050, 3.267716535433071279, 0.9448818897637749625 ) ) ;
#36129=CARTESIAN_POINT ( 'NONE',  ( 0.5455278134075212115, 3.346456692913386100, 0.6299212598425161236 ) ) ;
#36130=DIRECTION ( 'NONE',  ( 0.000000000000000000, 1.000000000000000000, 0.000000000000000000 ) ) ;
#36131=ORIENTED_EDGE ( 'NONE', *, *, #15710, .T. ) ;
#36133=FACE_BOUND ( 'NONE', #41269, .T. ) ;
#36135=CARTESIAN_POINT ( 'NONE',  ( 1.833433833923351353, 3.267716535433071279, 1.574803149606291974 ) ) ;
#36137=DIRECTION ( 'NONE',  ( 1.000000000000000000, 0.000000000000000000, 0.000000000000000000 ) ) ;
#36142=ORIENTED_EDGE ( 'NONE', *, *, #5327, .F. ) ;
#36144=LINE ( 'NONE', #776, #29295 ) ;
#36146=DIRECTION ( 'NONE',  ( 1.734723475976806848E-16, 0.000000000000000000, 1.000000000000000000 ) ) ;
#36147=VECTOR ( 'NONE', #973, 39.37007874015748143 ) ;
#36148=EDGE_CURVE ( 'NONE', #34660, #18225, #11806, .T. ) ;
#36150=DIRECTION ( 'NONE',  ( 0.000000000000000000, 0.000000000000000000, -1.000000000000000000 ) ) ;
#36151=CARTESIAN_POINT ( 'NONE',  ( -1.712496953225537855, 3.267716535433071279, -1.226315847645294221 ) ) ;
#36154=VECTOR ( 'NONE', #35275, 39.37007874015748143 ) ;
#36156=EDGE_CURVE ( 'NONE', #5661, #34145, #18020, .T. ) ;
#36157=VERTEX_POINT ( 'NONE', #32661 ) ;
#36158=ORIENTED_EDGE ( 'NONE', *, *, #45054, .T. ) ;
#36161=ORIENTED_EDGE ( 'NONE', *, *, #5684, .T. ) ;
#36162=EDGE_CURVE ( 'NONE', #15505, #10535, #46885, .T. ) ;
#36164=DIRECTION ( 'NONE',  ( -3.469446951953613696E-16, 0.000000000000000000, -1.000000000000000000 ) ) ;
#36165=VECTOR ( 'NONE', #49456, 39.37007874015748143 ) ;
#36166=DIRECTION ( 'NONE',  ( -3.469446951953613696E-16, 0.000000000000000000, -1.000000000000000000 ) ) ;
#36167=CARTESIAN_POINT ( 'NONE',  ( 1.091055626815043311, 3.346456692913386100, 1.377952755905504256 ) ) ;
#36168=ORIENTED_EDGE ( 'NONE', *, *, #22634, .T. ) ;
#36170=LINE ( 'NONE', #17067, #34030 ) ;
#36171=DIRECTION ( 'NONE',  ( 1.000000000000000000, 0.000000000000000000, -3.469446951953613696E-16 ) ) ;
#36172=FACE_OUTER_BOUND ( 'NONE', #9139, .T. ) ;
#36173=LINE ( 'NONE', #8800, #50640 ) ;
#36175=EDGE_CURVE ( 'NONE', #11955, #35311, #11558, .T. ) ;
#36177=VECTOR ( 'NONE', #27741, 39.37007874015748143 ) ;
#36179=EDGE_CURVE ( 'NONE', #10330, #13544, #12067, .T. ) ;
#36181=DIRECTION ( 'NONE',  ( 1.000000000000000000, 0.000000000000000000, -3.469446951953613696E-16 ) ) ;
#36182=VERTEX_POINT ( 'NONE', #50991 ) ;
#36183=DIRECTION ( 'NONE',  ( 1.734723475976806848E-16, -0.000000000000000000, 1.000000000000000000 ) ) ;
#36185=EDGE_LOOP ( 'NONE', ( #40211, #43559, #36027, #24665 ) ) ;
#36186=VERTEX_POINT ( 'NONE', #20766 ) ;
#36187=VECTOR ( 'NONE', #46773, 39.37007874015748143 ) ;
#36188=VECTOR ( 'NONE', #32788, 39.37007874015748143 ) ;
#36189=PLANE ( 'NONE',  #1843 ) ;
#36190=CARTESIAN_POINT ( 'NONE',  ( 0.8182917201112819283, 3.267716535433071279, 0.7874015748031454320 ) ) ;
#36193=VECTOR ( 'NONE', #15020, 39.37007874015748143 ) ;
#36196=EDGE_LOOP ( 'NONE', ( #20783, #46969, #10644, #26995 ) ) ;
#36200=LINE ( 'NONE', #35681, #13641 ) ;
#36202=DIRECTION ( 'NONE',  ( 0.000000000000000000, 0.000000000000000000, 1.000000000000000000 ) ) ;
#36203=EDGE_CURVE ( 'NONE', #6756, #1365, #27804, .T. ) ;
#36204=ORIENTED_EDGE ( 'NONE', *, *, #38413, .F. ) ;
#36206=ORIENTED_EDGE ( 'NONE', *, *, #20900, .T. ) ;
#36207=CARTESIAN_POINT ( 'NONE',  ( -1.091055626815042645, 3.267716535433071279, 2.186531193194249045 ) ) ;
#36211=DIRECTION ( 'NONE',  ( -3.469446951953613696E-16, 0.000000000000000000, -1.000000000000000000 ) ) ;
#36212=CARTESIAN_POINT ( 'NONE',  ( -1.363819533518803473, 3.346456692913386100, -1.417322834645664109 ) ) ;
#36214=ORIENTED_EDGE ( 'NONE', *, *, #20502, .F. ) ;
#36215=EDGE_CURVE ( 'NONE', #25499, #24416, #19045, .T. ) ;
#36218=VECTOR ( 'NONE', #6562, 39.37007874015748143 ) ;
#36219=CARTESIAN_POINT ( 'NONE',  ( 0.5455278134075213226, 3.267716535433071279, -9.463399047163224412E-17 ) ) ;
#36220=EDGE_CURVE ( 'NONE', #36221, #44686, #4017, .T. ) ;
#36221=VERTEX_POINT ( 'NONE', #34804 ) ;
#36222=DIRECTION ( 'NONE',  ( -0.000000000000000000, 1.000000000000000000, -0.000000000000000000 ) ) ;
#36223=LINE ( 'NONE', #32099, #39236 ) ;
#36226=ORIENTED_EDGE ( 'NONE', *, *, #22834, .F. ) ;
#36229=DIRECTION ( 'NONE',  ( 1.000000000000000000, 0.000000000000000000, 0.000000000000000000 ) ) ;
#36230=VECTOR ( 'NONE', #36776, 39.37007874015748143 ) ;
#36233=LINE ( 'NONE', #36485, #4052 ) ;
#36234=VECTOR ( 'NONE', #21018, 39.37007874015748143 ) ;
#36235=ORIENTED_EDGE ( 'NONE', *, *, #25184, .T. ) ;
#36236=ORIENTED_EDGE ( 'NONE', *, *, #2481, .T. ) ;
#36240=ORIENTED_EDGE ( 'NONE', *, *, #34608, .T. ) ;
#36241=LINE ( 'NONE', #12227, #18685 ) ;
#36242=CARTESIAN_POINT ( 'NONE',  ( -1.439733046521776139, 3.346456692913386100, 1.259842519685033357 ) ) ;
#36245=LINE ( 'NONE', #1114, #499 ) ;
#36247=ORIENTED_EDGE ( 'NONE', *, *, #25570, .T. ) ;
#36250=EDGE_CURVE ( 'NONE', #36296, #12695, #1654, .T. ) ;
#36251=FACE_OUTER_BOUND ( 'NONE', #33145, .T. ) ;
#36252=EDGE_LOOP ( 'NONE', ( #10070, #31103, #34108, #5612 ) ) ;
#36256=VECTOR ( 'NONE', #48478, 39.37007874015748143 ) ;
#36257=EDGE_LOOP ( 'NONE', ( #46575, #12180, #19316, #20203 ) ) ;
#36258=DIRECTION ( 'NONE',  ( -1.000000000000000000, 0.000000000000000000, 1.734723475976806848E-16 ) ) ;
#36259=DIRECTION ( 'NONE',  ( -1.000000000000000000, 0.000000000000000000, 1.734723475976806848E-16 ) ) ;
#36260=CARTESIAN_POINT ( 'NONE',  ( -1.299212598425207865, 3.346456692913386100, 1.732283464566920950 ) ) ;
#36262=LINE ( 'NONE', #39869, #24703 ) ;
#36263=DIRECTION ( 'NONE',  ( 1.734723475976806848E-16, 0.000000000000000000, 1.000000000000000000 ) ) ;
#36264=ORIENTED_EDGE ( 'NONE', *, *, #20695, .F. ) ;
#36265=FACE_OUTER_BOUND ( 'NONE', #25248, .T. ) ;
#36266=VECTOR ( 'NONE', #29750, 39.37007874015748143 ) ;
#36267=DIRECTION ( 'NONE',  ( -1.000000000000000000, 0.000000000000000000, -0.000000000000000000 ) ) ;
#36268=PLANE ( 'NONE',  #24707 ) ;
#36273=PLANE ( 'NONE',  #36999 ) ;
#36275=CARTESIAN_POINT ( 'NONE',  ( -1.091055626815042645, 3.346456692913386100, 1.889763779527550147 ) ) ;
#36277=VECTOR ( 'NONE', #43665, 39.37007874015748143 ) ;
#36279=PLANE ( 'NONE',  #47903 ) ;
#36281=ORIENTED_EDGE ( 'NONE', *, *, #12383, .F. ) ;
#36282=ADVANCED_FACE ( 'NONE', ( #25658 ), #21793, .F. ) ;
#36283=CARTESIAN_POINT ( 'NONE',  ( 0.5455278134075208785, 3.267716535433071279, -1.889763779527552812 ) ) ;
#36284=CARTESIAN_POINT ( 'NONE',  ( 1.636583440222563635, 0.000000000000000000, -1.456692913385823296 ) ) ;
#36286=CARTESIAN_POINT ( 'NONE',  ( -0.2727639067037608278, 0.000000000000000000, 2.165354330708650465 ) ) ;
#36287=EDGE_CURVE ( 'NONE', #7564, #41617, #48602, .T. ) ;
#36288=FACE_BOUND ( 'NONE', #25487, .T. ) ;
#36289=ORIENTED_EDGE ( 'NONE', *, *, #14272, .T. ) ;
#36293=ORIENTED_EDGE ( 'NONE', *, *, #36794, .F. ) ;
#36295=ORIENTED_EDGE ( 'NONE', *, *, #34545, .T. ) ;
#36296=VERTEX_POINT ( 'NONE', #37293 ) ;
#36298=ORIENTED_EDGE ( 'NONE', *, *, #18064, .T. ) ;
#36299=EDGE_CURVE ( 'NONE', #15323, #8660, #5532, .T. ) ;
#36300=DIRECTION ( 'NONE',  ( 1.000000000000000000, 0.000000000000000000, 0.000000000000000000 ) ) ;
#36301=CARTESIAN_POINT ( 'NONE',  ( 1.636583440222563857, 3.346456692913386100, 1.259842519685033135 ) ) ;
#36302=FACE_OUTER_BOUND ( 'NONE', #15752, .T. ) ;
#36303=VECTOR ( 'NONE', #40490, 39.37007874015748143 ) ;
#36307=CARTESIAN_POINT ( 'NONE',  ( 1.833433833923351353, 3.346456692913386100, 1.152076279655074087 ) ) ;
#36308=LINE ( 'NONE', #8425, #41038 ) ;
#36310=LINE ( 'NONE', #5064, #33264 ) ;
#36311=EDGE_CURVE ( 'NONE', #42995, #47754, #40904, .T. ) ;
#36312=VECTOR ( 'NONE', #40270, 39.37007874015748143 ) ;
#36313=DIRECTION ( 'NONE',  ( 1.000000000000000000, 0.000000000000000000, 0.000000000000000000 ) ) ;
#36314=EDGE_CURVE ( 'NONE', #25804, #29354, #29538, .T. ) ;
#36317=LINE ( 'NONE', #16178, #7516 ) ;
#36318=CARTESIAN_POINT ( 'NONE',  ( 0.8182917201112819283, 3.267716535433071279, -1.102362204724405714 ) ) ;
#36320=CARTESIAN_POINT ( 'NONE',  ( -0.3486774197067339376, 0.000000000000000000, 0.3149606299212577287 ) ) ;
#36321=DIRECTION ( 'NONE',  ( 1.734723475976806848E-16, -0.000000000000000000, 1.000000000000000000 ) ) ;
#36324=CARTESIAN_POINT ( 'NONE',  ( -0.6214413264104939882, 0.000000000000000000, 0.5905511811023582691 ) ) ;
#36326=FACE_BOUND ( 'NONE', #49259, .T. ) ;
#36330=B_SPLINE_CURVE_WITH_KNOTS ( 'NONE', 3,
 ( #48471, #44879, #25280, #13157 ),
 .UNSPECIFIED., .F., .F.,
 ( 4, 4 ),
 ( 7.902280897695455319E-07, 0.002031616469162080257 ),
 .UNSPECIFIED. ) ;
#36331=VERTEX_POINT ( 'NONE', #17406 ) ;
#36332=ORIENTED_EDGE ( 'NONE', *, *, #1783, .F. ) ;
#36333=DIRECTION ( 'NONE',  ( -3.469446951953613696E-16, 0.000000000000000000, -1.000000000000000000 ) ) ;
#36335=PLANE ( 'NONE',  #26062 ) ;
#36336=VERTEX_POINT ( 'NONE', #48851 ) ;
#36339=AXIS2_PLACEMENT_3D ( 'NONE', #8578, #20703, #19924 ) ;
#36340=ORIENTED_EDGE ( 'NONE', *, *, #46694, .F. ) ;
#36341=CARTESIAN_POINT ( 'NONE',  ( -0.2727639067037602172, 3.267716535433071279, 1.732283464566921172 ) ) ;
#36342=DIRECTION ( 'NONE',  ( 1.734723475976806848E-16, 0.000000000000000000, 1.000000000000000000 ) ) ;
#36343=EDGE_CURVE ( 'NONE', #41040, #21385, #25915, .T. ) ;
#36344=EDGE_LOOP ( 'NONE', ( #15088, #27105, #2674 ) ) ;
#36345=ADVANCED_FACE ( 'NONE', ( #45009 ), #49367, .F. ) ;
#36346=CARTESIAN_POINT ( 'NONE',  ( -0.5455278134075214336, 3.346456692913386100, -2.034427629037601104 ) ) ;
#36347=ORIENTED_EDGE ( 'NONE', *, *, #37981, .T. ) ;
#36348=AXIS2_PLACEMENT_3D ( 'NONE', #5603, #21357, #24203 ) ;
#36350=EDGE_CURVE ( 'NONE', #48914, #15499, #40648, .T. ) ;
#36351=EDGE_CURVE ( 'NONE', #7776, #31368, #22575, .T. ) ;
#36352=CARTESIAN_POINT ( 'NONE',  ( 1.560669927219590303, 3.240767787252049281, -1.896658215779326362 ) ) ;
#36353=EDGE_CURVE ( 'NONE', #30078, #36589, #37578, .T. ) ;
#36355=ORIENTED_EDGE ( 'NONE', *, *, #46908, .T. ) ;
#36357=EDGE_LOOP ( 'NONE', ( #15576, #38490, #46759, #15868 ) ) ;
#36358=CARTESIAN_POINT ( 'NONE',  ( -1.363819533518803029, 0.000000000000000000, 0.1574803149606287811 ) ) ;
#36361=CARTESIAN_POINT ( 'NONE',  ( 1.636583440222563857, 0.000000000000000000, -0.5118110236220471121 ) ) ;
#36362=EDGE_CURVE ( 'NONE', #16605, #19346, #45791, .T. ) ;
#36364=ORIENTED_EDGE ( 'NONE', *, *, #11911, .T. ) ;
#36365=CARTESIAN_POINT ( 'NONE',  ( 0.000000000000000000, 3.267716535433071279, 0.000000000000000000 ) ) ;
#36367=CARTESIAN_POINT ( 'NONE',  ( -1.198202975868765119, 3.267716535433071279, -1.732283464566922726 ) ) ;
#36368=CARTESIAN_POINT ( 'NONE',  ( 0.2727639067037610499, 3.346456692913386100, 1.732283464566921172 ) ) ;
#36369=EDGE_CURVE ( 'NONE', #40420, #47614, #29819, .T. ) ;
#36372=VECTOR ( 'NONE', #29120, 39.37007874015748143 ) ;
#36373=VECTOR ( 'NONE', #29215, 39.37007874015748143 ) ;
#36374=CARTESIAN_POINT ( 'NONE',  ( 0.000000000000000000, 3.346456692913386100, 0.000000000000000000 ) ) ;
#36375=ORIENTED_EDGE ( 'NONE', *, *, #46822, .T. ) ;
#36376=CARTESIAN_POINT ( 'NONE',  ( 0.7423782071083085965, 3.267716535433071279, -1.141732283464564013 ) ) ;
#36377=VERTEX_POINT ( 'NONE', #25688 ) ;
#36379=VECTOR ( 'NONE', #2620, 39.37007874015748143 ) ;
#36380=ORIENTED_EDGE ( 'NONE', *, *, #27564, .F. ) ;
#36381=ADVANCED_FACE ( 'NONE', ( #38336 ), #41441, .F. ) ;
#36382=CARTESIAN_POINT ( 'NONE',  ( -1.091055626815042645, 0.000000000000000000, -0.6299212598425177889 ) ) ;
#36383=LINE ( 'NONE', #5136, #13854 ) ;
#36384=DIRECTION ( 'NONE',  ( 1.734723475976806848E-16, -0.000000000000000000, 1.000000000000000000 ) ) ;
#36390=FACE_BOUND ( 'NONE', #7756, .T. ) ;
#36391=ORIENTED_EDGE ( 'NONE', *, *, #40257, .F. ) ;
#36392=CARTESIAN_POINT ( 'NONE',  ( 1.560669927219590747, 3.346456692913386100, -0.4724409448818889246 ) ) ;
#36393=ORIENTED_EDGE ( 'NONE', *, *, #22295, .T. ) ;
#36394=LINE ( 'NONE', #5664, #31801 ) ;
#36395=LINE ( 'NONE', #4642, #35491 ) ;
#36397=ORIENTED_EDGE ( 'NONE', *, *, #46467, .T. ) ;
#36398=VERTEX_POINT ( 'NONE', #34209 ) ;
#36402=FACE_BOUND ( 'NONE', #39225, .T. ) ;
#36403=EDGE_CURVE ( 'NONE', #22175, #13982, #2703, .T. ) ;
#36407=FACE_OUTER_BOUND ( 'NONE', #33321, .T. ) ;
#36408=EDGE_CURVE ( 'NONE', #14441, #41776, #5816, .T. ) ;
#36410=ORIENTED_EDGE ( 'NONE', *, *, #26403, .F. ) ;
#36413=EDGE_LOOP ( 'NONE', ( #6260, #4502, #6285, #24801 ) ) ;
#36414=ORIENTED_EDGE ( 'NONE', *, *, #11461, .F. ) ;
#36415=VECTOR ( 'NONE', #46897, 39.37007874015748143 ) ;
#36416=ORIENTED_EDGE ( 'NONE', *, *, #617, .T. ) ;
#36419=CARTESIAN_POINT ( 'NONE',  ( 0.000000000000000000, 3.267716535433071279, 0.000000000000000000 ) ) ;
#36420=EDGE_CURVE ( 'NONE', #49288, #46953, #9947, .T. ) ;
#36423=ORIENTED_EDGE ( 'NONE', *, *, #11354, .T. ) ;
#36426=FACE_OUTER_BOUND ( 'NONE', #59, .T. ) ;
#36427=PLANE ( 'NONE',  #15876 ) ;
#36428=EDGE_CURVE ( 'NONE', #20741, #34340, #45039, .T. ) ;
#36429=DIRECTION ( 'NONE',  ( 1.000000000000000000, 0.000000000000000000, -3.469446951953613696E-16 ) ) ;
#36430=LINE ( 'NONE', #5181, #45408 ) ;
#36432=DIRECTION ( 'NONE',  ( 1.000000000000000000, 0.000000000000000000, 0.000000000000000000 ) ) ;
#36434=DIRECTION ( 'NONE',  ( -1.000000000000000000, 0.000000000000000000, -0.000000000000000000 ) ) ;
#36435=CARTESIAN_POINT ( 'NONE',  ( 0.000000000000000000, 3.267716535433071279, 0.000000000000000000 ) ) ;
#36436=ORIENTED_EDGE ( 'NONE', *, *, #38847, .T. ) ;
#36437=DIRECTION ( 'NONE',  ( -0.000000000000000000, 1.000000000000000000, -0.000000000000000000 ) ) ;
#36440=ADVANCED_FACE ( 'NONE', ( #41695 ), #29308, .F. ) ;
#36442=DIRECTION ( 'NONE',  ( -1.000000000000000000, 0.000000000000000000, 0.000000000000000000 ) ) ;
#36443=AXIS2_PLACEMENT_3D ( 'NONE', #5483, #21234, #36988 ) ;
#36444=PLANE ( 'NONE',  #38543 ) ;
#36446=ORIENTED_EDGE ( 'NONE', *, *, #2788, .T. ) ;
#36448=EDGE_CURVE ( 'NONE', #44346, #15612, #14324, .T. ) ;
#36449=ORIENTED_EDGE ( 'NONE', *, *, #38743, .F. ) ;
#36450=CARTESIAN_POINT ( 'NONE',  ( -1.091055626815042645, 0.000000000000000000, -7.512581982576723358E-16 ) ) ;
#36452=ORIENTED_EDGE ( 'NONE', *, *, #32699, .F. ) ;
#36453=ORIENTED_EDGE ( 'NONE', *, *, #16002, .T. ) ;
#36456=PLANE ( 'NONE',  #43314 ) ;
#36457=LINE ( 'NONE', #13218, #17331 ) ;
#36458=DIRECTION ( 'NONE',  ( -0.000000000000000000, 0.000000000000000000, 1.000000000000000000 ) ) ;
#36459=ORIENTED_EDGE ( 'NONE', *, *, #7780, .T. ) ;
#36460=VERTEX_POINT ( 'NONE', #17948 ) ;
#36463=ORIENTED_EDGE ( 'NONE', *, *, #24850, .F. ) ;
#36468=EDGE_CURVE ( 'NONE', #11950, #14008, #22078, .T. ) ;
#36469=ORIENTED_EDGE ( 'NONE', *, *, #30395, .T. ) ;
#36472=CARTESIAN_POINT ( 'NONE',  ( 1.287906020515829919, 0.000000000000000000, -1.889763779527552368 ) ) ;
#36473=EDGE_CURVE ( 'NONE', #4073, #33562, #37838, .T. ) ;
#36475=DIRECTION ( 'NONE',  ( -0.000000000000000000, 1.000000000000000000, -0.000000000000000000 ) ) ;
#36476=LINE ( 'NONE', #33125, #29372 ) ;
#36477=CARTESIAN_POINT ( 'NONE',  ( -1.909347346926324462, 3.346456692913386100, 0.4724409448818871482 ) ) ;
#36479=EDGE_LOOP ( 'NONE', ( #29565, #32364, #30541, #35778 ) ) ;
#36480=DIRECTION ( 'NONE',  ( -0.000000000000000000, 1.000000000000000000, -0.000000000000000000 ) ) ;
#36482=DIRECTION ( 'NONE',  ( -1.000000000000000000, 0.000000000000000000, 1.734723475976806848E-16 ) ) ;
#36483=VECTOR ( 'NONE', #23438, 39.37007874015748143 ) ;
#36484=CARTESIAN_POINT ( 'NONE',  ( -0.3486774197067339376, 3.267716535433071279, 1.209717811016579078E-16 ) ) ;
#36485=CARTESIAN_POINT ( 'NONE',  ( 0.000000000000000000, 3.267716535433071279, -0.8267716535433052849 ) ) ;
#36486=ORIENTED_EDGE ( 'NONE', *, *, #10047, .F. ) ;
#36487=ORIENTED_EDGE ( 'NONE', *, *, #4062, .T. ) ;
#36488=AXIS2_PLACEMENT_3D ( 'NONE', #8399, #23890, #43746 ) ;
#36490=AXIS2_PLACEMENT_3D ( 'NONE', #7333, #19938, #19436 ) ;
#36491=VERTEX_POINT ( 'NONE', #38084 ) ;
#36493=LINE ( 'NONE', #47805, #2026 ) ;
#36494=VECTOR ( 'NONE', #49077, 39.37007874015748143 ) ;
#36498=FACE_OUTER_BOUND ( 'NONE', #27256, .T. ) ;
#36499=CARTESIAN_POINT ( 'NONE',  ( 3.927031490892378253E-16, 3.346456692913386100, 1.062992125984246083 ) ) ;
#36501=PLANE ( 'NONE',  #11023 ) ;
#36503=EDGE_CURVE ( 'NONE', #47345, #10658, #8091, .T. ) ;
#36504=ORIENTED_EDGE ( 'NONE', *, *, #6118, .T. ) ;
#36505=CARTESIAN_POINT ( 'NONE',  ( -0.07591351300297294324, 3.267716535433071279, 2.633779063002555273E-17 ) ) ;
#36506=ADVANCED_FACE ( 'NONE', ( #22835 ), #42936, .F. ) ;
#36508=CARTESIAN_POINT ( 'NONE',  ( 1.833433833923351353, 3.267716535433071279, -0.3149606299212596716 ) ) ;
#36509=ORIENTED_EDGE ( 'NONE', *, *, #31370, .T. ) ;
#36510=EDGE_CURVE ( 'NONE', #14009, #8562, #42443, .T. ) ;
#36512=CARTESIAN_POINT ( 'NONE',  ( 0.2727639067037602172, 3.346456692913386100, -1.732283464566922726 ) ) ;
#36514=ORIENTED_EDGE ( 'NONE', *, *, #28750, .T. ) ;
#36516=CARTESIAN_POINT ( 'NONE',  ( 1.560669927219590525, 3.267716535433071279, -5.414661521997676285E-16 ) ) ;
#36517=VERTEX_POINT ( 'NONE', #19949 ) ;
#36518=DIRECTION ( 'NONE',  ( 0.000000000000000000, 0.000000000000000000, -1.000000000000000000 ) ) ;
#36519=CARTESIAN_POINT ( 'NONE',  ( 1.091055626815042423, 3.346456692913386100, -1.889763779527552368 ) ) ;
#36520=CARTESIAN_POINT ( 'NONE',  ( 0.7423782071083084855, 3.267716535433071279, -1.574803149606293529 ) ) ;
#36521=CARTESIAN_POINT ( 'NONE',  ( 0.5455278134075211005, 0.000000000000000000, -0.8267716535433055070 ) ) ;
#36523=DIRECTION ( 'NONE',  ( -0.000000000000000000, 1.000000000000000000, -0.000000000000000000 ) ) ;
#36525=VERTEX_POINT ( 'NONE', #35715 ) ;
#36526=VERTEX_POINT ( 'NONE', #11213 ) ;
#36527=CARTESIAN_POINT ( 'NONE',  ( 0.000000000000000000, 3.267716535433071279, 1.259842519685033135 ) ) ;
#36528=DIRECTION ( 'NONE',  ( 0.000000000000000000, 0.000000000000000000, -1.000000000000000000 ) ) ;
#36529=ORIENTED_EDGE ( 'NONE', *, *, #50437, .F. ) ;
#36530=PLANE ( 'NONE',  #45634 ) ;
#36531=LINE ( 'NONE', #385, #50710 ) ;
#36533=VECTOR ( 'NONE', #49269, 39.37007874015748143 ) ;
#36535=DIRECTION ( 'NONE',  ( -0.000000000000000000, 1.000000000000000000, -0.000000000000000000 ) ) ;
#36537=VERTEX_POINT ( 'NONE', #7837 ) ;
#36538=VERTEX_POINT ( 'NONE', #11962 ) ;
#36539=DIRECTION ( 'NONE',  ( -1.000000000000000000, 0.000000000000000000, 0.000000000000000000 ) ) ;
#36540=DIRECTION ( 'NONE',  ( -1.000000000000000000, 0.000000000000000000, 0.000000000000000000 ) ) ;
#36542=EDGE_CURVE ( 'NONE', #40300, #5052, #15335, .T. ) ;
#36543=VERTEX_POINT ( 'NONE', #31341 ) ;
#36544=CARTESIAN_POINT ( 'NONE',  ( 1.636583440222563635, 3.267716535433071279, -1.141732283464564013 ) ) ;
#36545=FACE_BOUND ( 'NONE', #32606, .T. ) ;
#36546=VECTOR ( 'NONE', #28546, 39.37007874015748143 ) ;
#36547=VERTEX_POINT ( 'NONE', #50391 ) ;
#36548=CARTESIAN_POINT ( 'NONE',  ( 0.000000000000000000, 3.267716535433071279, 0.4724409448818872592 ) ) ;
#36549=ORIENTED_EDGE ( 'NONE', *, *, #19319, .T. ) ;
#36550=EDGE_LOOP ( 'NONE', ( #42807, #41746, #42502, #44335 ) ) ;
#36551=CARTESIAN_POINT ( 'NONE',  ( -0.5455278134075214336, 3.346456692913386100, 2.034427629037600660 ) ) ;
#36552=ORIENTED_EDGE ( 'NONE', *, *, #27629, .F. ) ;
#36556=DIRECTION ( 'NONE',  ( -0.000000000000000000, 1.000000000000000000, -0.000000000000000000 ) ) ;
#36562=LINE ( 'NONE', #20021, #30343 ) ;
#36563=ORIENTED_EDGE ( 'NONE', *, *, #20107, .F. ) ;
#36564=DIRECTION ( 'NONE',  ( -1.000000000000000000, 0.000000000000000000, 0.000000000000000000 ) ) ;
#36565=VECTOR ( 'NONE', #42717, 39.37007874015748143 ) ;
#36567=AXIS2_PLACEMENT_3D ( 'NONE', #47072, #11749, #7877 ) ;
#36568=VECTOR ( 'NONE', #50335, 39.37007874015748143 ) ;
#36570=DIRECTION ( 'NONE',  ( -0.000000000000000000, 1.000000000000000000, -0.000000000000000000 ) ) ;
#36571=ADVANCED_FACE ( 'NONE', ( #15589 ), #18955, .F. ) ;
#36572=DIRECTION ( 'NONE',  ( -1.000000000000000000, -0.000000000000000000, -0.000000000000000000 ) ) ;
#36575=EDGE_CURVE ( 'NONE', #26074, #27975, #27449, .T. ) ;
#36578=CARTESIAN_POINT ( 'NONE',  ( -1.363819533518803473, 3.346456692913386100, -0.3543307086614174151 ) ) ;
#36579=VECTOR ( 'NONE', #44484, 39.37007874015748143 ) ;
#36580=ORIENTED_EDGE ( 'NONE', *, *, #27647, .F. ) ;
#36583=FACE_BOUND ( 'NONE', #27043, .T. ) ;
#36585=EDGE_CURVE ( 'NONE', #35962, #15224, #43188, .T. ) ;
#36586=CARTESIAN_POINT ( 'NONE',  ( 0.000000000000000000, 3.267716535433071279, -0.7874015748031470974 ) ) ;
#36588=ORIENTED_EDGE ( 'NONE', *, *, #46550, .T. ) ;
#36589=VERTEX_POINT ( 'NONE', #4215 ) ;
#36591=VERTEX_POINT ( 'NONE', #30580 ) ;
#36596=EDGE_CURVE ( 'NONE', #18552, #25411, #34961, .T. ) ;
#36597=ORIENTED_EDGE ( 'NONE', *, *, #44732, .F. ) ;
#36598=CARTESIAN_POINT ( 'NONE',  ( 0.000000000000000000, 3.346456692913386100, 0.000000000000000000 ) ) ;
#36603=EDGE_CURVE ( 'NONE', #23957, #1644, #46789, .T. ) ;
#36605=VECTOR ( 'NONE', #10283, 39.37007874015748143 ) ;
#36606=VERTEX_POINT ( 'NONE', #35210 ) ;
#36607=EDGE_CURVE ( 'NONE', #13403, #28656, #1363, .T. ) ;
#36609=VECTOR ( 'NONE', #16240, 39.37007874015748143 ) ;
#36610=ORIENTED_EDGE ( 'NONE', *, *, #4993, .F. ) ;
#36612=CARTESIAN_POINT ( 'NONE',  ( 0.000000000000000000, 3.267716535433071279, 0.000000000000000000 ) ) ;
#36614=VERTEX_POINT ( 'NONE', #27960 ) ;
#36615=CARTESIAN_POINT ( 'NONE',  ( -0.8942052331142552601, 3.346456692913386100, -0.9448818897637760728 ) ) ;
#36616=EDGE_LOOP ( 'NONE', ( #20211, #5471, #40586, #38771 ) ) ;
#36617=DIRECTION ( 'NONE',  ( 1.000000000000000000, -0.000000000000000000, 0.000000000000000000 ) ) ;
#36618=LINE ( 'NONE', #8226, #28030 ) ;
#36621=CARTESIAN_POINT ( 'NONE',  ( -0.3486774197067334935, 0.000000000000000000, 0.7480314960629874665 ) ) ;
#36622=CARTESIAN_POINT ( 'NONE',  ( -0.2727639067037602727, 3.346456692913386100, 0.9055118110236167750 ) ) ;
#36623=DIRECTION ( 'NONE',  ( 1.000000000000000000, 0.000000000000000000, 0.000000000000000000 ) ) ;
#36626=LINE ( 'NONE', #7976, #44936 ) ;
#36627=ORIENTED_EDGE ( 'NONE', *, *, #33276, .F. ) ;
#36629=CARTESIAN_POINT ( 'NONE',  ( 0.000000000000000000, 3.346456692913386100, 0.000000000000000000 ) ) ;
#36631=EDGE_CURVE ( 'NONE', #49445, #12012, #43695, .T. ) ;
#36632=ORIENTED_EDGE ( 'NONE', *, *, #6288, .F. ) ;
#36634=VECTOR ( 'NONE', #7518, 39.37007874015748143 ) ;
#36636=VECTOR ( 'NONE', #5500, 39.37007874015748143 ) ;
#36639=EDGE_CURVE ( 'NONE', #187, #32403, #36233, .T. ) ;
#36641=DIRECTION ( 'NONE',  ( 1.734723475976806848E-16, 0.000000000000000000, 1.000000000000000000 ) ) ;
#36643=CARTESIAN_POINT ( 'NONE',  ( 1.833433833923351353, 3.267716535433071279, -1.161035397307311917E-15 ) ) ;
#36644=DIRECTION ( 'NONE',  ( 1.000000000000000000, 0.000000000000000000, 0.000000000000000000 ) ) ;
#36645=CARTESIAN_POINT ( 'NONE',  ( 1.833433833923351353, 3.267716535433071279, -1.036830145017913596 ) ) ;
#36646=ORIENTED_EDGE ( 'NONE', *, *, #18071, .T. ) ;
#36647=LINE ( 'NONE', #1269, #4342 ) ;
#36648=VECTOR ( 'NONE', #20366, 39.37007874015748143 ) ;
#36649=FACE_OUTER_BOUND ( 'NONE', #39509, .T. ) ;
#36650=ORIENTED_EDGE ( 'NONE', *, *, #48426, .T. ) ;
#36651=LINE ( 'NONE', #9532, #47675 ) ;
#36653=CARTESIAN_POINT ( 'NONE',  ( -1.091055626815042645, 3.346456692913386100, -0.3149606299212593941 ) ) ;
#36654=DIRECTION ( 'NONE',  ( 1.734723475976806848E-16, -0.000000000000000000, 1.000000000000000000 ) ) ;
#36655=EDGE_CURVE ( 'NONE', #47504, #1038, #32111, .T. ) ;
#36657=ADVANCED_FACE ( 'NONE', ( #16869 ), #39842, .F. ) ;
#36659=ORIENTED_EDGE ( 'NONE', *, *, #4619, .F. ) ;
#36660=EDGE_CURVE ( 'NONE', #22006, #21605, #25116, .T. ) ;
#36661=DIRECTION ( 'NONE',  ( -3.469446951953613696E-16, 0.000000000000000000, -1.000000000000000000 ) ) ;
#36662=DIRECTION ( 'NONE',  ( -0.000000000000000000, 1.000000000000000000, -0.000000000000000000 ) ) ;
#36663=CARTESIAN_POINT ( 'NONE',  ( 0.5455278134075217666, 0.000000000000000000, 1.259842519685033357 ) ) ;
#36664=ORIENTED_EDGE ( 'NONE', *, *, #7895, .T. ) ;
#36665=LINE ( 'NONE', #47465, #17136 ) ;
#36667=ORIENTED_EDGE ( 'NONE', *, *, #42530, .F. ) ;
#36668=LINE ( 'NONE', #8782, #46356 ) ;
#36669=VECTOR ( 'NONE', #22272, 39.37007874015748143 ) ;
#36671=ORIENTED_EDGE ( 'NONE', *, *, #26693, .T. ) ;
#36672=VECTOR ( 'NONE', #2133, 39.37007874015748143 ) ;
#36674=VECTOR ( 'NONE', #17779, 39.37007874015748143 ) ;
#36675=VERTEX_POINT ( 'NONE', #40364 ) ;
#36676=CARTESIAN_POINT ( 'NONE',  ( 0.7423782071083087075, 3.346456692913386100, 0.6299212598425161236 ) ) ;
#36679=DIRECTION ( 'NONE',  ( 0.000000000000000000, 0.000000000000000000, 1.000000000000000000 ) ) ;
#36680=DIRECTION ( 'NONE',  ( 1.734723475976806848E-16, -0.000000000000000000, 1.000000000000000000 ) ) ;
#36682=ORIENTED_EDGE ( 'NONE', *, *, #15115, .F. ) ;
#36683=VECTOR ( 'NONE', #36844, 39.37007874015748143 ) ;
#36687=DIRECTION ( 'NONE',  ( -1.000000000000000000, -0.000000000000000000, -0.000000000000000000 ) ) ;
#36688=DIRECTION ( 'NONE',  ( -0.000000000000000000, 1.000000000000000000, -0.000000000000000000 ) ) ;
#36690=PLANE ( 'NONE',  #11061 ) ;
#36693=FACE_OUTER_BOUND ( 'NONE', #7721, .T. ) ;
#36694=CARTESIAN_POINT ( 'NONE',  ( 0.000000000000000000, 3.267716535433071279, 1.574803149606291530 ) ) ;
#36696=ORIENTED_EDGE ( 'NONE', *, *, #617, .F. ) ;
#36700=DIRECTION ( 'NONE',  ( 1.000000000000000000, 0.000000000000000000, -3.469446951953613696E-16 ) ) ;
#36701=ORIENTED_EDGE ( 'NONE', *, *, #8999, .T. ) ;
#36707=CARTESIAN_POINT ( 'NONE',  ( -0.5455278134075208785, 3.267716535433071279, 1.574803149606291974 ) ) ;
#36708=ORIENTED_EDGE ( 'NONE', *, *, #25284, .F. ) ;
#36709=VECTOR ( 'NONE', #26972, 39.37007874015748143 ) ;
#36712=CARTESIAN_POINT ( 'NONE',  ( -1.712496953225537633, 0.000000000000000000, 1.417322834645662333 ) ) ;
#36713=ADVANCED_FACE ( 'NONE', ( #28975 ), #32619, .F. ) ;
#36715=DIMENSIONAL_EXPONENTS ( 1.000000000000000000, 0.000000000000000000, 0.000000000000000000, 0.000000000000000000, 0.000000000000000000, 0.000000000000000000, 0.000000000000000000 ) ;
#36717=VERTEX_POINT ( 'NONE', #48058 ) ;
#36718=VECTOR ( 'NONE', #15618, 39.37007874015748143 ) ;
#36719=DIRECTION ( 'NONE',  ( 1.734723475976806848E-16, -0.000000000000000000, 1.000000000000000000 ) ) ;
#36722=EDGE_CURVE ( 'NONE', #43398, #1008, #12731, .T. ) ;
#36723=CARTESIAN_POINT ( 'NONE',  ( -0.2727639067037604392, 3.267716535433071279, 4.731699523581607892E-17 ) ) ;
#36724=DIRECTION ( 'NONE',  ( 1.734723475976806848E-16, 0.000000000000000000, 1.000000000000000000 ) ) ;
#36726=VERTEX_POINT ( 'NONE', #12992 ) ;
#36728=DIRECTION ( 'NONE',  ( -0.000000000000000000, 1.000000000000000000, -0.000000000000000000 ) ) ;
#36729=EDGE_CURVE ( 'NONE', #33278, #46567, #12469, .T. ) ;
#36730=LINE ( 'NONE', #844, #7216 ) ;
#36732=CARTESIAN_POINT ( 'NONE',  ( 1.363819533518803695, 3.346456692913386100, 1.732283464566921172 ) ) ;
#36733=CARTESIAN_POINT ( 'NONE',  ( 0.5455278134075211005, 3.346456692913386100, -1.141732283464564013 ) ) ;
#36734=DIRECTION ( 'NONE',  ( 1.000000000000000000, 0.000000000000000000, -3.469446951953613696E-16 ) ) ;
#36735=ORIENTED_EDGE ( 'NONE', *, *, #17510, .F. ) ;
#36736=ORIENTED_EDGE ( 'NONE', *, *, #29260, .F. ) ;
#36739=CARTESIAN_POINT ( 'NONE',  ( 1.015142113812069313, 0.000000000000000000, -0.9842519685039348154 ) ) ;
#36740=CARTESIAN_POINT ( 'NONE',  ( 1.091055626815042423, 3.267716535433071279, -2.086614173228339641 ) ) ;
#36743=ORIENTED_EDGE ( 'NONE', *, *, #9754, .T. ) ;
#36746=CARTESIAN_POINT ( 'NONE',  ( 0.000000000000000000, 3.346456692913386100, 0.000000000000000000 ) ) ;
#36747=ORIENTED_EDGE ( 'NONE', *, *, #1111, .T. ) ;
#36749=CARTESIAN_POINT ( 'NONE',  ( 0.000000000000000000, 3.267716535433071279, 0.000000000000000000 ) ) ;
#36750=VECTOR ( 'NONE', #11930, 39.37007874015748143 ) ;
#36751=AXIS2_PLACEMENT_3D ( 'NONE', #13736, #42107, #29480 ) ;
#36752=DIRECTION ( 'NONE',  ( 1.734723475976806848E-16, 0.000000000000000000, 1.000000000000000000 ) ) ;
#36753=CARTESIAN_POINT ( 'NONE',  ( -0.2727639067037607723, 0.000000000000000000, -0.4724409448818883694 ) ) ;
#36754=CARTESIAN_POINT ( 'NONE',  ( -1.636583440222563635, 3.346456692913386100, 0.9448818897637749625 ) ) ;
#36755=VECTOR ( 'NONE', #47255, 39.37007874015748143 ) ;
#36756=ORIENTED_EDGE ( 'NONE', *, *, #47852, .T. ) ;
#36757=CARTESIAN_POINT ( 'NONE',  ( 4.268512490100411402E-16, 3.267716535433071279, 0.9448818897637749625 ) ) ;
#36758=PLANE ( 'NONE',  #4260 ) ;
#36759=EDGE_CURVE ( 'NONE', #28099, #3513, #24351, .T. ) ;
#36761=DIRECTION ( 'NONE',  ( -1.000000000000000000, 0.000000000000000000, 0.000000000000000000 ) ) ;
#36762=CARTESIAN_POINT ( 'NONE',  ( 1.636583440222563857, 0.000000000000000000, 1.574803149606291974 ) ) ;
#36763=LINE ( 'NONE', #48077, #15592 ) ;
#36765=CARTESIAN_POINT ( 'NONE',  ( -1.909347346926324462, 3.346456692913386100, 0.7874015748031456541 ) ) ;
#36769=LINE ( 'NONE', #1902, #36234 ) ;
#36771=VERTEX_POINT ( 'NONE', #13499 ) ;
#36772=DIRECTION ( 'NONE',  ( -1.000000000000000000, 0.000000000000000000, 1.734723475976806848E-16 ) ) ;
#36773=CARTESIAN_POINT ( 'NONE',  ( -0.07591351300297333182, 0.000000000000000000, -1.102362204724405714 ) ) ;
#36775=LINE ( 'NONE', #32143, #10331 ) ;
#36776=DIRECTION ( 'NONE',  ( 1.000000000000000000, 0.000000000000000000, 0.000000000000000000 ) ) ;
#36777=ORIENTED_EDGE ( 'NONE', *, *, #20193, .F. ) ;
#36778=ORIENTED_EDGE ( 'NONE', *, *, #20656, .F. ) ;
#36779=CARTESIAN_POINT ( 'NONE',  ( -1.636583440222564301, 3.346456692913386100, -1.325930245594398871 ) ) ;
#36780=AXIS2_PLACEMENT_3D ( 'NONE', #45484, #16690, #37271 ) ;
#36781=CARTESIAN_POINT ( 'NONE',  ( 0.7423782071083085965, 3.346456692913386100, -0.1968503937007880511 ) ) ;
#36783=EDGE_LOOP ( 'NONE', ( #10667, #39353, #47526, #45495 ) ) ;
#36784=CARTESIAN_POINT ( 'NONE',  ( -1.091055626815042645, 3.346456692913386100, -1.771653543307081025 ) ) ;
#36785=CARTESIAN_POINT ( 'NONE',  ( 0.7423782071083092626, 0.000000000000000000, 2.204724409448808764 ) ) ;
#36786=CARTESIAN_POINT ( 'NONE',  ( -1.166969139818015977, 3.346456692913386100, -1.417322834645664109 ) ) ;
#36787=VECTOR ( 'NONE', #15380, 39.37007874015748143 ) ;
#36789=ORIENTED_EDGE ( 'NONE', *, *, #325, .F. ) ;
#36790=ORIENTED_EDGE ( 'NONE', *, *, #50163, .F. ) ;
#36791=CARTESIAN_POINT ( 'NONE',  ( 0.1968503937007878568, 3.346456692913386100, 1.889763779527550369 ) ) ;
#36792=CARTESIAN_POINT ( 'NONE',  ( -1.195183497228115035E-16, 3.346456692913386100, 0.6299212598425161236 ) ) ;
#36794=EDGE_CURVE ( 'NONE', #2180, #46194, #33892, .T. ) ;
#36795=CARTESIAN_POINT ( 'NONE',  ( 1.909347346926324684, 0.000000000000000000, 0.2755905511810994302 ) ) ;
#36797=CARTESIAN_POINT ( 'NONE',  ( 0.5455278134075212115, 0.000000000000000000, -0.3149606299212593941 ) ) ;
#36798=FACE_BOUND ( 'NONE', #45694, .T. ) ;
#36799=AXIS2_PLACEMENT_3D ( 'NONE', #31438, #15934, #4321 ) ;
#36801=LINE ( 'NONE', #5552, #23276 ) ;
#36803=ORIENTED_EDGE ( 'NONE', *, *, #29423, .T. ) ;
#36804=CARTESIAN_POINT ( 'NONE',  ( -1.636583440222563635, 0.000000000000000000, 0.6299212598425164567 ) ) ;
#36805=EDGE_CURVE ( 'NONE', #27975, #9992, #10642, .T. ) ;
#36807=EDGE_CURVE ( 'NONE', #11701, #18566, #21754, .T. ) ;
#36811=EDGE_CURVE ( 'NONE', #40680, #25916, #9878, .T. ) ;
#36812=LINE ( 'NONE', #42876, #16408 ) ;
#36814=LINE ( 'NONE', #25189, #37458 ) ;
#36816=AXIS2_PLACEMENT_3D ( 'NONE', #47999, #15534, #24303 ) ;
#36818=CARTESIAN_POINT ( 'NONE',  ( 0.5455278134075216556, 0.000000000000000000, 1.692913385826762873 ) ) ;
#36819=LINE ( 'NONE', #20288, #25363 ) ;
#36821=ORIENTED_EDGE ( 'NONE', *, *, #47256, .F. ) ;
#36822=FACE_OUTER_BOUND ( 'NONE', #12911, .T. ) ;
#36823=AXIS2_PLACEMENT_3D ( 'NONE', #30584, #10711, #10457 ) ;
#36824=AXIS2_PLACEMENT_3D ( 'NONE', #19925, #35443, #36211 ) ;
#36825=CARTESIAN_POINT ( 'NONE',  ( -0.5455278134075216556, 0.000000000000000000, -2.204724409448810540 ) ) ;
#36826=EDGE_CURVE ( 'NONE', #21641, #44588, #29237, .T. ) ;
#36827=ORIENTED_EDGE ( 'NONE', *, *, #22650, .F. ) ;
#36828=DIRECTION ( 'NONE',  ( 1.734723475976806848E-16, 0.000000000000000000, 1.000000000000000000 ) ) ;
#36829=CARTESIAN_POINT ( 'NONE',  ( -1.712496953225537188, 3.346456692913386100, 0.7874015748031456541 ) ) ;
#36830=ORIENTED_EDGE ( 'NONE', *, *, #5054, .T. ) ;
#36832=VECTOR ( 'NONE', #23903, 39.37007874015748143 ) ;
#36833=DIRECTION ( 'NONE',  ( 0.000000000000000000, 0.000000000000000000, -1.000000000000000000 ) ) ;
#36834=EDGE_CURVE ( 'NONE', #8104, #8660, #21496, .T. ) ;
#36836=VECTOR ( 'NONE', #45019, 39.37007874015748143 ) ;
#36837=ADVANCED_FACE ( 'NONE', ( #18381 ), #49069, .F. ) ;
#36838=ORIENTED_EDGE ( 'NONE', *, *, #9043, .F. ) ;
#36839=DIRECTION ( 'NONE',  ( -3.469446951953613696E-16, 0.000000000000000000, -1.000000000000000000 ) ) ;
#36840=ORIENTED_EDGE ( 'NONE', *, *, #34821, .T. ) ;
#36841=FACE_BOUND ( 'NONE', #24261, .T. ) ;
#36843=CARTESIAN_POINT ( 'NONE',  ( -1.712496953225537188, 0.000000000000000000, 0.9055118110236167750 ) ) ;
#36844=DIRECTION ( 'NONE',  ( 1.734723475976806848E-16, -0.000000000000000000, 1.000000000000000000 ) ) ;
#36845=ORIENTED_EDGE ( 'NONE', *, *, #26152, .F. ) ;
#36847=CARTESIAN_POINT ( 'NONE',  ( 1.560669927219590525, 3.267716535433071279, 0.2755905511810996522 ) ) ;
#36848=EDGE_LOOP ( 'NONE', ( #25889, #26686, #5674, #38967 ) ) ;
#36849=LINE ( 'NONE', #28574, #21127 ) ;
#36853=DIRECTION ( 'NONE',  ( -3.469446951953613696E-16, 0.000000000000000000, -1.000000000000000000 ) ) ;
#36854=VECTOR ( 'NONE', #48144, 39.37007874015748143 ) ;
#36857=VECTOR ( 'NONE', #34836, 39.37007874015748143 ) ;
#36858=ORIENTED_EDGE ( 'NONE', *, *, #10803, .F. ) ;
#36862=EDGE_LOOP ( 'NONE', ( #42327, #33764, #28813, #20879 ) ) ;
#36864=VECTOR ( 'NONE', #5495, 39.37007874015748143 ) ;
#36866=ORIENTED_EDGE ( 'NONE', *, *, #9998, .T. ) ;
#36868=CARTESIAN_POINT ( 'NONE',  ( 1.015142113812069979, 0.000000000000000000, 1.732283464566921172 ) ) ;
#36873=ORIENTED_EDGE ( 'NONE', *, *, #40851, .T. ) ;
#36874=CARTESIAN_POINT ( 'NONE',  ( -0.07591351300297333182, 0.000000000000000000, -1.732283464566922726 ) ) ;
#36875=CARTESIAN_POINT ( 'NONE',  ( 2.966619746092224783E-16, 3.313179664429866556, 2.422428857167389982 ) ) ;
#36878=LINE ( 'NONE', #28088, #17068 ) ;
#36879=CARTESIAN_POINT ( 'NONE',  ( 0.7423782071083087075, 3.346456692913386100, 0.3149606299212576177 ) ) ;
#36881=CARTESIAN_POINT ( 'NONE',  ( -0.6214413264104939882, 0.000000000000000000, 1.102362204724404160 ) ) ;
#36882=CARTESIAN_POINT ( 'NONE',  ( 0.000000000000000000, 3.267716535433071279, -1.299212598425193210 ) ) ;
#36885=DIRECTION ( 'NONE',  ( -1.000000000000000000, -0.000000000000000000, -0.000000000000000000 ) ) ;
#36889=DIRECTION ( 'NONE',  ( 0.000000000000000000, 0.000000000000000000, -1.000000000000000000 ) ) ;
#36890=VECTOR ( 'NONE', #34383, 39.37007874015748143 ) ;
#36892=CARTESIAN_POINT ( 'NONE',  ( -1.195183497228115035E-16, 3.267716535433071279, -0.9448818897637765168 ) ) ;
#36893=EDGE_CURVE ( 'NONE', #31173, #27651, #48814, .T. ) ;
#36895=VECTOR ( 'NONE', #13829, 39.37007874015748143 ) ;
#36898=ADVANCED_FACE ( 'NONE', ( #34143 ), #14513, .F. ) ;
#36901=DIRECTION ( 'NONE',  ( -0.000000000000000000, 0.000000000000000000, 1.000000000000000000 ) ) ;
#36903=CARTESIAN_POINT ( 'NONE',  ( -0.5455278134075214336, 0.000000000000000000, 0.3149606299212577287 ) ) ;
#36904=CARTESIAN_POINT ( 'NONE',  ( 0.000000000000000000, 3.267716535433071279, 0.000000000000000000 ) ) ;
#36908=VERTEX_POINT ( 'NONE', #26871 ) ;
#36911=ORIENTED_EDGE ( 'NONE', *, *, #11069, .T. ) ;
#36912=DIRECTION ( 'NONE',  ( -0.000000000000000000, 0.000000000000000000, 1.000000000000000000 ) ) ;
#36916=ORIENTED_EDGE ( 'NONE', *, *, #6618, .F. ) ;
#36917=VERTEX_POINT ( 'NONE', #19377 ) ;
#36920=FACE_BOUND ( 'NONE', #26790, .T. ) ;
#36921=ORIENTED_EDGE ( 'NONE', *, *, #48938, .T. ) ;
#36922=CARTESIAN_POINT ( 'NONE',  ( -2.454875160333845674, 0.000000000000000000, -0.03937007874015881204 ) ) ;
#36923=LINE ( 'NONE', #37436, #20058 ) ;
#36924=EDGE_CURVE ( 'NONE', #50043, #15158, #34642, .T. ) ;
#36925=AXIS2_PLACEMENT_3D ( 'NONE', #33094, #41337, #29195 ) ;
#36926=EDGE_LOOP ( 'NONE', ( #32508, #28690, #29633, #48115 ) ) ;
#36927=DIRECTION ( 'NONE',  ( -1.000000000000000000, 0.000000000000000000, 0.000000000000000000 ) ) ;
#36928=EDGE_CURVE ( 'NONE', #29512, #42332, #15519, .T. ) ;
#36929=EDGE_CURVE ( 'NONE', #43136, #33404, #23510, .T. ) ;
#36931=VERTEX_POINT ( 'NONE', #27130 ) ;
#36932=VERTEX_POINT ( 'NONE', #46968 ) ;
#36933=VECTOR ( 'NONE', #29932, 39.37007874015748143 ) ;
#36934=ADVANCED_FACE ( 'NONE', ( #7770 ), #50325, .F. ) ;
#36937=LINE ( 'NONE', #43630, #48861 ) ;
#36939=DIRECTION ( 'NONE',  ( 1.000000000000000000, 0.000000000000000000, -3.469446951953613696E-16 ) ) ;
#36940=AXIS2_PLACEMENT_3D ( 'NONE', #33576, #9298, #41307 ) ;
#36943=ORIENTED_EDGE ( 'NONE', *, *, #25868, .F. ) ;
#36944=LINE ( 'NONE', #538, #20829 ) ;
#36945=LINE ( 'NONE', #12666, #41137 ) ;
#36946=FACE_BOUND ( 'NONE', #7864, .T. ) ;
#36947=EDGE_CURVE ( 'NONE', #23628, #39512, #31524, .T. ) ;
#36949=DIRECTION ( 'NONE',  ( 1.734723475976806848E-16, -0.000000000000000000, 1.000000000000000000 ) ) ;
#36954=ORIENTED_EDGE ( 'NONE', *, *, #28843, .T. ) ;
#36958=EDGE_LOOP ( 'NONE', ( #45016, #38321, #194, #21657 ) ) ;
#36960=CARTESIAN_POINT ( 'NONE',  ( -1.636583440222564301, 3.346456692913386100, -1.456692913385822186 ) ) ;
#36961=DIRECTION ( 'NONE',  ( -3.469446951953613696E-16, 0.000000000000000000, -1.000000000000000000 ) ) ;
#36963=ORIENTED_EDGE ( 'NONE', *, *, #2888, .T. ) ;
#36965=LINE ( 'NONE', #13725, #41900 ) ;
#36966=CIRCLE ( 'NONE', #14701, 2.493791675044291445 ) ;
#36967=EDGE_LOOP ( 'NONE', ( #27159, #23135, #28050, #9228 ) ) ;
#36968=VECTOR ( 'NONE', #47593, 39.37007874015748143 ) ;
#36969=VECTOR ( 'NONE', #22734, 39.37007874015748143 ) ;
#36970=CARTESIAN_POINT ( 'NONE',  ( 1.363819533518803251, 3.346456692913386100, -0.1574803149606304187 ) ) ;
#36971=DIRECTION ( 'NONE',  ( 0.000000000000000000, -1.000000000000000000, 0.000000000000000000 ) ) ;
#36973=ORIENTED_EDGE ( 'NONE', *, *, #49302, .T. ) ;
#36974=ORIENTED_EDGE ( 'NONE', *, *, #34378, .T. ) ;
#36977=ORIENTED_EDGE ( 'NONE', *, *, #47720, .T. ) ;
#36979=LINE ( 'NONE', #13476, #36373 ) ;
#36980=CARTESIAN_POINT ( 'NONE',  ( -0.5455278134075208785, 0.000000000000000000, 1.574803149606291974 ) ) ;
#36982=AXIS2_PLACEMENT_3D ( 'NONE', #3152, #27144, #3659 ) ;
#36984=CARTESIAN_POINT ( 'NONE',  ( 1.015142113812069313, 3.267716535433071279, -3.521981712565032389E-16 ) ) ;
#36985=CARTESIAN_POINT ( 'NONE',  ( 0.8182917201112819283, 3.346456692913386100, -0.3543307086614175816 ) ) ;
#36986=DIRECTION ( 'NONE',  ( -0.000000000000000000, 1.000000000000000000, -0.000000000000000000 ) ) ;
#36987=ORIENTED_EDGE ( 'NONE', *, *, #50581, .F. ) ;
#36988=DIRECTION ( 'NONE',  ( 1.734723475976806848E-16, 0.000000000000000000, 1.000000000000000000 ) ) ;
#36989=LINE ( 'NONE', #43942, #40057 ) ;
#36990=EDGE_CURVE ( 'NONE', #10750, #37269, #14767, .T. ) ;
#36991=ADVANCED_FACE ( 'NONE', ( #42373 ), #23017, .F. ) ;
#36992=CARTESIAN_POINT ( 'NONE',  ( 2.076281802138679300, 3.346456692913386100, -0.3543307086614178592 ) ) ;
#36993=ORIENTED_EDGE ( 'NONE', *, *, #10625, .T. ) ;
#36994=VERTEX_POINT ( 'NONE', #50823 ) ;
#36996=EDGE_CURVE ( 'NONE', #46747, #49534, #10886, .T. ) ;
#36999=AXIS2_PLACEMENT_3D ( 'NONE', #32924, #17669, #32666 ) ;
#37001=EDGE_CURVE ( 'NONE', #5174, #49411, #4930, .T. ) ;
#37002=DIRECTION ( 'NONE',  ( 0.000000000000000000, -1.000000000000000000, 0.000000000000000000 ) ) ;
#37004=ORIENTED_EDGE ( 'NONE', *, *, #47248, .T. ) ;
#37007=EDGE_LOOP ( 'NONE', ( #11579, #25088, #18802, #45132 ) ) ;
#37008=CARTESIAN_POINT ( 'NONE',  ( 0.000000000000000000, 3.267716535433071279, -0.3543307086614171930 ) ) ;
#37009=CARTESIAN_POINT ( 'NONE',  ( -0.6214413264104939882, 3.346456692913386100, 1.102362204724404160 ) ) ;
#37011=VECTOR ( 'NONE', #29015, 39.37007874015748143 ) ;
#37012=EDGE_CURVE ( 'NONE', #49445, #30308, #2891, .T. ) ;
#37013=LINE ( 'NONE', #21255, #46438 ) ;
#37014=LINE ( 'NONE', #49341, #48295 ) ;
#37015=CARTESIAN_POINT ( 'NONE',  ( -1.166969139818015977, 3.346456692913386100, -1.102362204724405270 ) ) ;
#37016=EDGE_LOOP ( 'NONE', ( #960, #18122, #6280, #15459 ) ) ;
#37017=DIRECTION ( 'NONE',  ( 0.000000000000000000, 0.000000000000000000, -1.000000000000000000 ) ) ;
#37018=EDGE_CURVE ( 'NONE', #10535, #18938, #50572, .T. ) ;
#37019=CARTESIAN_POINT ( 'NONE',  ( 1.015142113812069313, 3.267716535433071279, 0.4724409448818868706 ) ) ;
#37021=DIRECTION ( 'NONE',  ( -3.469446951953613696E-16, 0.000000000000000000, -1.000000000000000000 ) ) ;
#37022=CARTESIAN_POINT ( 'NONE',  ( 1.558105373646060388, 3.267716535433071279, 1.417322834645662777 ) ) ;
#37025=CARTESIAN_POINT ( 'NONE',  ( 0.1968503937007873017, 0.000000000000000000, -0.3149606299212591165 ) ) ;
#37027=ORIENTED_EDGE ( 'NONE', *, *, #14839, .T. ) ;
#37028=LINE ( 'NONE', #44496, #26314 ) ;
#37029=DIRECTION ( 'NONE',  ( 1.000000000000000000, -0.000000000000000000, 0.000000000000000000 ) ) ;
#37030=ORIENTED_EDGE ( 'NONE', *, *, #7943, .T. ) ;
#37031=DIRECTION ( 'NONE',  ( -0.000000000000000000, 1.000000000000000000, -0.000000000000000000 ) ) ;
#37032=EDGE_CURVE ( 'NONE', #2471, #21641, #31274, .T. ) ;
#37033=FACE_OUTER_BOUND ( 'NONE', #45641, .T. ) ;
#37034=DIRECTION ( 'NONE',  ( -3.469446951953613696E-16, 0.000000000000000000, -1.000000000000000000 ) ) ;
#37035=LINE ( 'NONE', #14549, #7090 ) ;
#37036=AXIS2_PLACEMENT_3D ( 'NONE', #10107, #42101, #9855 ) ;
#37037=DIRECTION ( 'NONE',  ( -1.000000000000000000, 0.000000000000000000, 0.000000000000000000 ) ) ;
#37039=ORIENTED_EDGE ( 'NONE', *, *, #29945, .F. ) ;
#37041=PLANE ( 'NONE',  #22180 ) ;
#37042=ORIENTED_EDGE ( 'NONE', *, *, #14094, .T. ) ;
#37043=DIRECTION ( 'NONE',  ( -3.469446951953613696E-16, 0.000000000000000000, -1.000000000000000000 ) ) ;
#37044=DIRECTION ( 'NONE',  ( -1.000000000000000000, 0.000000000000000000, 0.000000000000000000 ) ) ;
#37045=CARTESIAN_POINT ( 'NONE',  ( 1.687984952120845428, 3.267716535433071279, 1.259842519685033135 ) ) ;
#37046=CARTESIAN_POINT ( 'NONE',  ( 2.378961647330872786, 0.000000000000000000, -0.5118110236220471121 ) ) ;
#37047=VECTOR ( 'NONE', #47034, 39.37007874015748143 ) ;
#37048=VERTEX_POINT ( 'NONE', #7014 ) ;
#37050=LINE ( 'NONE', #13044, #4016 ) ;
#37052=DIRECTION ( 'NONE',  ( 0.000000000000000000, 0.000000000000000000, -1.000000000000000000 ) ) ;
#37054=VECTOR ( 'NONE', #46320, 39.37007874015748143 ) ;
#37055=DIRECTION ( 'NONE',  ( -1.000000000000000000, 0.000000000000000000, 0.000000000000000000 ) ) ;
#37056=FACE_BOUND ( 'NONE', #47317, .T. ) ;
#37058=DIRECTION ( 'NONE',  ( -0.000000000000000000, 1.000000000000000000, -0.000000000000000000 ) ) ;
#37059=ORIENTED_EDGE ( 'NONE', *, *, #19422, .T. ) ;
#37061=VECTOR ( 'NONE', #17964, 39.37007874015748143 ) ;
#37067=EDGE_CURVE ( 'NONE', #50364, #47890, #28809, .T. ) ;
#37068=CARTESIAN_POINT ( 'NONE',  ( 1.287906020515830141, 3.267716535433071279, -4.468321617281355077E-16 ) ) ;
#37071=DIRECTION ( 'NONE',  ( -3.469446951953613696E-16, 0.000000000000000000, -1.000000000000000000 ) ) ;
#37072=EDGE_CURVE ( 'NONE', #31903, #26214, #32557, .T. ) ;
#37074=DIRECTION ( 'NONE',  ( 1.000000000000000000, 0.000000000000000000, 0.000000000000000000 ) ) ;
#37075=DIRECTION ( 'NONE',  ( -1.000000000000000000, 0.000000000000000000, -0.000000000000000000 ) ) ;
#37077=ORIENTED_EDGE ( 'NONE', *, *, #38133, .F. ) ;
#37079=ADVANCED_FACE ( 'NONE', ( #24024 ), #48249, .F. ) ;
#37080=DIRECTION ( 'NONE',  ( 1.734723475976806848E-16, -0.000000000000000000, 1.000000000000000000 ) ) ;
#37081=AXIS2_PLACEMENT_3D ( 'NONE', #28402, #43634, #47733 ) ;
#37082=EDGE_LOOP ( 'NONE', ( #6751, #9343, #37626, #34011, #37977 ) ) ;
#37086=DIRECTION ( 'NONE',  ( -3.469446951953613696E-16, 0.000000000000000000, -1.000000000000000000 ) ) ;
#37088=CARTESIAN_POINT ( 'NONE',  ( -1.439733046521776139, 0.000000000000000000, 0.3149606299212578953 ) ) ;
#37089=CARTESIAN_POINT ( 'NONE',  ( -1.166969139818015533, 3.346456692913386100, 0.4724409448818871482 ) ) ;
#37090=ORIENTED_EDGE ( 'NONE', *, *, #25202, .F. ) ;
#37091=CARTESIAN_POINT ( 'NONE',  ( 1.636583440222563857, 3.346456692913386100, 0.1181102362204701633 ) ) ;
#37092=VECTOR ( 'NONE', #16047, 39.37007874015748143 ) ;
#37093=ORIENTED_EDGE ( 'NONE', *, *, #5355, .T. ) ;
#37094=FACE_BOUND ( 'NONE', #25158, .T. ) ;
#37095=EDGE_CURVE ( 'NONE', #5048, #20757, #35905, .T. ) ;
#37097=CARTESIAN_POINT ( 'NONE',  ( -1.439733046521776139, 0.000000000000000000, 1.259842519685033357 ) ) ;
#37100=VERTEX_POINT ( 'NONE', #40551 ) ;
#37101=PLANE ( 'NONE',  #30390 ) ;
#37103=ADVANCED_FACE ( 'NONE', ( #24540 ), #47989, .F. ) ;
#37104=CARTESIAN_POINT ( 'NONE',  ( 2.106197740627112402, 0.000000000000000000, 0.1574803149606280872 ) ) ;
#37105=ORIENTED_EDGE ( 'NONE', *, *, #50373, .T. ) ;
#37106=EDGE_CURVE ( 'NONE', #10548, #49624, #20923, .T. ) ;
#37107=LINE ( 'NONE', #43807, #4197 ) ;
#37108=AXIS2_PLACEMENT_3D ( 'NONE', #18942, #18439, #34193 ) ;
#37109=ORIENTED_EDGE ( 'NONE', *, *, #2056, .F. ) ;
#37110=DIRECTION ( 'NONE',  ( 1.000000000000000000, 0.000000000000000000, 0.000000000000000000 ) ) ;
#37112=DIRECTION ( 'NONE',  ( -1.000000000000000000, 0.000000000000000000, -0.000000000000000000 ) ) ;
#37113=EDGE_LOOP ( 'NONE', ( #9930, #13944, #34881, #12168 ) ) ;
#37115=FACE_OUTER_BOUND ( 'NONE', #31746, .T. ) ;
#37116=ORIENTED_EDGE ( 'NONE', *, *, #7485, .F. ) ;
#37117=EDGE_LOOP ( 'NONE', ( #16119, #42829, #49265, #44833 ) ) ;
#37118=EDGE_CURVE ( 'NONE', #1350, #34628, #16282, .T. ) ;
#37119=VECTOR ( 'NONE', #50515, 39.37007874015748143 ) ;
#37122=ORIENTED_EDGE ( 'NONE', *, *, #24585, .F. ) ;
#37123=EDGE_CURVE ( 'NONE', #31137, #6824, #27891, .T. ) ;
#37124=CARTESIAN_POINT ( 'NONE',  ( 1.560669927219590747, 3.267716535433071279, -0.1574803149606304187 ) ) ;
#37125=EDGE_CURVE ( 'NONE', #3769, #47245, #19883, .T. ) ;
#37127=AXIS2_PLACEMENT_3D ( 'NONE', #17344, #33104, #20691 ) ;
#37129=VERTEX_POINT ( 'NONE', #16025 ) ;
#37132=ORIENTED_EDGE ( 'NONE', *, *, #10469, .T. ) ;
#37135=FACE_OUTER_BOUND ( 'NONE', #14364, .T. ) ;
#37136=LINE ( 'NONE', #14134, #26970 ) ;
#37138=DIRECTION ( 'NONE',  ( -0.000000000000000000, 1.000000000000000000, -0.000000000000000000 ) ) ;
#37139=DIRECTION ( 'NONE',  ( -3.469446951953613696E-16, 0.000000000000000000, -1.000000000000000000 ) ) ;
#37140=FACE_OUTER_BOUND ( 'NONE', #10088, .T. ) ;
#37141=FACE_OUTER_BOUND ( 'NONE', #22501, .T. ) ;
#37143=VERTEX_POINT ( 'NONE', #8022 ) ;
#37144=CARTESIAN_POINT ( 'NONE',  ( 1.363819533518803251, 3.346456692913386100, -0.9842519685039348154 ) ) ;
#37145=EDGE_CURVE ( 'NONE', #40318, #40457, #28144, .T. ) ;
#37147=VERTEX_POINT ( 'NONE', #43883 ) ;
#37148=CARTESIAN_POINT ( 'NONE',  ( 0.000000000000000000, 3.267716535433071279, 0.9448818897637746295 ) ) ;
#37149=ORIENTED_EDGE ( 'NONE', *, *, #12794, .T. ) ;
#37150=DIRECTION ( 'NONE',  ( 0.000000000000000000, 0.000000000000000000, -1.000000000000000000 ) ) ;
#37151=EDGE_CURVE ( 'NONE', #180, #30647, #4153, .T. ) ;
#37161=FACE_OUTER_BOUND ( 'NONE', #34463, .T. ) ;
#37163=DIRECTION ( 'NONE',  ( 0.000000000000000000, 1.000000000000000000, 0.000000000000000000 ) ) ;
#37164=ORIENTED_EDGE ( 'NONE', *, *, #45981, .F. ) ;
#37166=VECTOR ( 'NONE', #39694, 39.37007874015748143 ) ;
#37167=ORIENTED_EDGE ( 'NONE', *, *, #50056, .F. ) ;
#37169=DIRECTION ( 'NONE',  ( -0.000000000000000000, 1.000000000000000000, -0.000000000000000000 ) ) ;
#37170=DIRECTION ( 'NONE',  ( 1.000000000000000000, -0.000000000000000000, 0.000000000000000000 ) ) ;
#37172=LINE ( 'NONE', #13668, #6596 ) ;
#37174=ORIENTED_EDGE ( 'NONE', *, *, #22999, .T. ) ;
#37175=DIRECTION ( 'NONE',  ( 1.000000000000000000, -0.000000000000000000, 0.000000000000000000 ) ) ;
#37177=FACE_BOUND ( 'NONE', #16303, .T. ) ;
#37178=VERTEX_POINT ( 'NONE', #36167 ) ;
#37180=DIRECTION ( 'NONE',  ( 1.000000000000000000, 0.000000000000000000, 0.000000000000000000 ) ) ;
#37181=DIRECTION ( 'NONE',  ( 1.000000000000000000, -0.000000000000000000, 0.000000000000000000 ) ) ;
#37184=EDGE_CURVE ( 'NONE', #39803, #24019, #49768, .T. ) ;
#37185=EDGE_CURVE ( 'NONE', #25804, #6833, #13438, .T. ) ;
#37186=CARTESIAN_POINT ( 'NONE',  ( -1.909347346926324462, 3.267716535433071279, -0.3543307086614171930 ) ) ;
#37187=EDGE_CURVE ( 'NONE', #43058, #50549, #18937, .T. ) ;
#37191=ORIENTED_EDGE ( 'NONE', *, *, #18412, .F. ) ;
#37195=VECTOR ( 'NONE', #2504, 39.37007874015748143 ) ;
#37198=VERTEX_POINT ( 'NONE', #29694 ) ;
#37199=ORIENTED_EDGE ( 'NONE', *, *, #18459, .F. ) ;
#37200=PLANE ( 'NONE',  #7633 ) ;
#37202=LINE ( 'NONE', #24297, #45566 ) ;
#37203=VECTOR ( 'NONE', #31127, 39.37007874015748143 ) ;
#37204=CARTESIAN_POINT ( 'NONE',  ( 1.363819533518803251, 0.000000000000000000, 0.1574803149606283648 ) ) ;
#37205=LINE ( 'NONE', #5949, #23978 ) ;
#37207=DIRECTION ( 'NONE',  ( 1.734723475976806848E-16, 0.000000000000000000, 1.000000000000000000 ) ) ;
#37208=VERTEX_POINT ( 'NONE', #13696 ) ;
#37209=DIRECTION ( 'NONE',  ( -1.000000000000000000, 0.000000000000000000, -0.000000000000000000 ) ) ;
#37210=DIRECTION ( 'NONE',  ( -3.469446951953613696E-16, 0.000000000000000000, -1.000000000000000000 ) ) ;
#37213=DIRECTION ( 'NONE',  ( -0.000000000000000000, 0.000000000000000000, 1.000000000000000000 ) ) ;
#37214=LINE ( 'NONE', #25328, #28649 ) ;
#37215=ADVANCED_FACE ( 'NONE', ( #17316 ), #33585, .F. ) ;
#37216=EDGE_LOOP ( 'NONE', ( #8372, #21567, #12226, #31833 ) ) ;
#37218=EDGE_LOOP ( 'NONE', ( #35957, #29556, #40022, #18475 ) ) ;
#37219=LINE ( 'NONE', #21721, #4832 ) ;
#37221=ORIENTED_EDGE ( 'NONE', *, *, #8146, .F. ) ;
#37222=VECTOR ( 'NONE', #21838, 39.37007874015748143 ) ;
#37223=PLANE ( 'NONE',  #21893 ) ;
#37224=CARTESIAN_POINT ( 'NONE',  ( -1.439733046521776583, 3.346456692913386100, -0.9448818897637762948 ) ) ;
#37226=ORIENTED_EDGE ( 'NONE', *, *, #7215, .F. ) ;
#37227=ORIENTED_EDGE ( 'NONE', *, *, #35647, .F. ) ;
#37229=VECTOR ( 'NONE', #2998, 39.37007874015748143 ) ;
#37230=DIRECTION ( 'NONE',  ( -1.000000000000000000, -0.000000000000000000, -0.000000000000000000 ) ) ;
#37232=VERTEX_POINT ( 'NONE', #25817 ) ;
#37233=CARTESIAN_POINT ( 'NONE',  ( 0.7423782071083084855, 3.346456692913386100, -1.971134437475891454 ) ) ;
#37234=CARTESIAN_POINT ( 'NONE',  ( 0.000000000000000000, 3.267716535433071279, 0.000000000000000000 ) ) ;
#37238=VECTOR ( 'NONE', #24944, 39.37007874015748143 ) ;
#37239=EDGE_LOOP ( 'NONE', ( #10626, #2501, #35212, #34213 ) ) ;
#37240=EDGE_CURVE ( 'NONE', #38782, #2547, #33073, .T. ) ;
#37241=CARTESIAN_POINT ( 'NONE',  ( 2.106197740627112402, 0.000000000000000000, 1.102362204724403938 ) ) ;
#37242=CARTESIAN_POINT ( 'NONE',  ( -1.166969139818016199, 3.267716535433071279, -1.823990790610291013 ) ) ;
#37243=CARTESIAN_POINT ( 'NONE',  ( -2.182111253630085290, 3.267716535433071279, 3.785359618865288779E-16 ) ) ;
#37244=ORIENTED_EDGE ( 'NONE', *, *, #29977, .F. ) ;
#37245=EDGE_CURVE ( 'NONE', #37726, #27355, #17288, .T. ) ;
#37246=DIRECTION ( 'NONE',  ( 0.000000000000000000, 0.000000000000000000, -1.000000000000000000 ) ) ;
#37247=LINE ( 'NONE', #13746, #16999 ) ;
#37249=FACE_OUTER_BOUND ( 'NONE', #30726, .T. ) ;
#37250=ORIENTED_EDGE ( 'NONE', *, *, #42928, .T. ) ;
#37251=EDGE_LOOP ( 'NONE', ( #46142, #3618, #8271 ) ) ;
#37252=EDGE_CURVE ( 'NONE', #31232, #22619, #6203, .T. ) ;
#37254=CARTESIAN_POINT ( 'NONE',  ( 0.7423782071083085965, 3.346456692913386100, -0.5118110236220467790 ) ) ;
#37256=DIRECTION ( 'NONE',  ( 1.734723475976806848E-16, 0.000000000000000000, 1.000000000000000000 ) ) ;
#37257=ORIENTED_EDGE ( 'NONE', *, *, #47256, .T. ) ;
#37258=ORIENTED_EDGE ( 'NONE', *, *, #22928, .T. ) ;
#37260=ORIENTED_EDGE ( 'NONE', *, *, #30752, .F. ) ;
#37261=DIRECTION ( 'NONE',  ( 1.000000000000000000, -0.000000000000000000, 0.000000000000000000 ) ) ;
#37263=AXIS2_PLACEMENT_3D ( 'NONE', #22847, #7356, #34974 ) ;
#37264=VECTOR ( 'NONE', #18186, 39.37007874015748143 ) ;
#37267=VECTOR ( 'NONE', #12001, 39.37007874015748143 ) ;
#37268=DIRECTION ( 'NONE',  ( 0.000000000000000000, -1.000000000000000000, 0.000000000000000000 ) ) ;
#37269=VERTEX_POINT ( 'NONE', #41067 ) ;
#37270=CARTESIAN_POINT ( 'NONE',  ( -1.909347346926324906, 3.346456692913386100, -1.102362204724405492 ) ) ;
#37271=DIRECTION ( 'NONE',  ( 0.000000000000000000, 0.000000000000000000, 1.000000000000000000 ) ) ;
#37272=AXIS2_PLACEMENT_3D ( 'NONE', #4087, #7694, #11816 ) ;
#37273=FACE_OUTER_BOUND ( 'NONE', #37401, .T. ) ;
#37274=VERTEX_POINT ( 'NONE', #14455 ) ;
#37276=CARTESIAN_POINT ( 'NONE',  ( -0.8182917201112814842, 3.346456692913386100, 0.5905511811023582691 ) ) ;
#37277=DIRECTION ( 'NONE',  ( -1.000000000000000000, 0.000000000000000000, -0.000000000000000000 ) ) ;
#37278=LINE ( 'NONE', #21266, #5689 ) ;
#37279=ORIENTED_EDGE ( 'NONE', *, *, #38300, .F. ) ;
#37283=EDGE_CURVE ( 'NONE', #12857, #2160, #2579, .T. ) ;
#37284=ORIENTED_EDGE ( 'NONE', *, *, #48062, .T. ) ;
#37289=ADVANCED_FACE ( 'NONE', ( #21440 ), #17565, .F. ) ;
#37290=LINE ( 'NONE', #41660, #21055 ) ;
#37292=FACE_OUTER_BOUND ( 'NONE', #11684, .T. ) ;
#37293=CARTESIAN_POINT ( 'NONE',  ( -1.363819533518803473, 3.346456692913386100, 1.535433070866133232 ) ) ;
#37296=DIRECTION ( 'NONE',  ( -1.000000000000000000, 0.000000000000000000, 0.000000000000000000 ) ) ;
#37297=DIRECTION ( 'NONE',  ( -0.000000000000000000, 1.000000000000000000, -0.000000000000000000 ) ) ;
#37298=ORIENTED_EDGE ( 'NONE', *, *, #12217, .F. ) ;
#37299=FACE_OUTER_BOUND ( 'NONE', #4658, .T. ) ;
#37300=DIRECTION ( 'NONE',  ( 1.000000000000000000, 0.000000000000000000, -3.469446951953613696E-16 ) ) ;
#37301=DIRECTION ( 'NONE',  ( 1.734723475976806848E-16, -0.000000000000000000, 1.000000000000000000 ) ) ;
#37304=ORIENTED_EDGE ( 'NONE', *, *, #25264, .F. ) ;
#37309=LINE ( 'NONE', #37562, #12361 ) ;
#37310=ORIENTED_EDGE ( 'NONE', *, *, #3519, .T. ) ;
#37311=CARTESIAN_POINT ( 'NONE',  ( -0.8182917201112814842, 3.346456692913386100, 0.7874015748031456541 ) ) ;
#37313=FACE_BOUND ( 'NONE', #16935, .T. ) ;
#37314=EDGE_LOOP ( 'NONE', ( #24175, #40219, #28995, #12214 ) ) ;
#37316=ADVANCED_FACE ( 'NONE', ( #9821 ), #5942, .F. ) ;
#37317=LINE ( 'NONE', #10189, #19953 ) ;
#37318=ORIENTED_EDGE ( 'NONE', *, *, #14770, .T. ) ;
#37319=VECTOR ( 'NONE', #18245, 39.37007874015748143 ) ;
#37320=EDGE_LOOP ( 'NONE', ( #37430, #1286, #39392, #40171 ) ) ;
#37321=CARTESIAN_POINT ( 'NONE',  ( -2.182111253630085290, 3.346456692913386100, 0.3149606299212578953 ) ) ;
#37322=CARTESIAN_POINT ( 'NONE',  ( -1.909347346926324906, 3.346456692913386100, -0.8893194486674343979 ) ) ;
#37323=VECTOR ( 'NONE', #28820, 39.37007874015748143 ) ;
#37324=ORIENTED_EDGE ( 'NONE', *, *, #38188, .F. ) ;
#37325=LINE ( 'NONE', #33198, #45058 ) ;
#37326=DIRECTION ( 'NONE',  ( 0.000000000000000000, 0.000000000000000000, -1.000000000000000000 ) ) ;
#37328=EDGE_CURVE ( 'NONE', #18704, #36771, #17819, .T. ) ;
#37330=LINE ( 'NONE', #17699, #14405 ) ;
#37331=DIRECTION ( 'NONE',  ( -3.469446951953613696E-16, 0.000000000000000000, -1.000000000000000000 ) ) ;
#37332=CARTESIAN_POINT ( 'NONE',  ( -1.091055626815042645, 0.000000000000000000, -1.141732283464563569 ) ) ;
#37334=ORIENTED_EDGE ( 'NONE', *, *, #21545, .T. ) ;
#37335=DIRECTION ( 'NONE',  ( -3.469446951953613696E-16, 0.000000000000000000, -1.000000000000000000 ) ) ;
#37337=VERTEX_POINT ( 'NONE', #42573 ) ;
#37338=AXIS2_PLACEMENT_3D ( 'NONE', #15454, #10572, #7207 ) ;
#37339=CARTESIAN_POINT ( 'NONE',  ( -1.985260859929297572, 0.000000000000000000, -0.3149606299212589500 ) ) ;
#37340=DIRECTION ( 'NONE',  ( 1.000000000000000000, 0.000000000000000000, 0.000000000000000000 ) ) ;
#37341=ORIENTED_EDGE ( 'NONE', *, *, #24554, .F. ) ;
#37342=DIRECTION ( 'NONE',  ( -0.000000000000000000, 1.000000000000000000, -0.000000000000000000 ) ) ;
#37347=ORIENTED_EDGE ( 'NONE', *, *, #35573, .T. ) ;
#37348=VECTOR ( 'NONE', #15821, 39.37007874015748143 ) ;
#37349=DIRECTION ( 'NONE',  ( -0.000000000000000000, 1.000000000000000000, -0.000000000000000000 ) ) ;
#37350=VERTEX_POINT ( 'NONE', #11337 ) ;
#37351=FACE_BOUND ( 'NONE', #15536, .T. ) ;
#37353=CARTESIAN_POINT ( 'NONE',  ( 1.015142113812069313, 3.346456692913386100, 0.4724409448818868706 ) ) ;
#37354=VECTOR ( 'NONE', #37029, 39.37007874015748143 ) ;
#37355=CARTESIAN_POINT ( 'NONE',  ( -1.439733046521776583, 3.346456692913386100, -0.3149606299212592275 ) ) ;
#37356=CARTESIAN_POINT ( 'NONE',  ( 0.000000000000000000, 3.267716535433071279, 0.1574803149606283648 ) ) ;
#37357=EDGE_CURVE ( 'NONE', #47624, #3690, #46417, .T. ) ;
#37359=EDGE_LOOP ( 'NONE', ( #18569, #11617, #48760, #2366 ) ) ;
#37360=VERTEX_POINT ( 'NONE', #23449 ) ;
#37364=PLANE ( 'NONE',  #8770 ) ;
#37368=EDGE_CURVE ( 'NONE', #13971, #14497, #26571, .T. ) ;
#37370=LINE ( 'NONE', #13612, #22478 ) ;
#37372=ORIENTED_EDGE ( 'NONE', *, *, #8243, .F. ) ;
#37373=EDGE_CURVE ( 'NONE', #24661, #14486, #6956, .T. ) ;
#37375=ORIENTED_EDGE ( 'NONE', *, *, #8273, .T. ) ;
#37376=VERTEX_POINT ( 'NONE', #11083 ) ;
#37377=ADVANCED_FACE ( 'NONE', ( #6708 ), #51020, .F. ) ;
#37378=VERTEX_POINT ( 'NONE', #23200 ) ;
#37379=VERTEX_POINT ( 'NONE', #22706 ) ;
#37380=CARTESIAN_POINT ( 'NONE',  ( -1.091055626815042645, 3.346456692913386100, -0.9448818897637760728 ) ) ;
#37381=VECTOR ( 'NONE', #20457, 39.37007874015748143 ) ;
#37382=VERTEX_POINT ( 'NONE', #3085 ) ;
#37383=LINE ( 'NONE', #10257, #13899 ) ;
#37384=ADVANCED_FACE ( 'NONE', ( #18586 ), #18834, .F. ) ;
#37385=LINE ( 'NONE', #18255, #34320 ) ;
#37386=AXIS2_PLACEMENT_3D ( 'NONE', #27631, #7012, #43375 ) ;
#37387=AXIS2_PLACEMENT_3D ( 'NONE', #13890, #34277, #21890 ) ;
#37389=ORIENTED_EDGE ( 'NONE', *, *, #30970, .T. ) ;
#37391=LINE ( 'NONE', #45859, #22967 ) ;
#37394=CARTESIAN_POINT ( 'NONE',  ( -0.5455278134075216556, 3.346456692913386100, -2.204724409448810540 ) ) ;
#37396=EDGE_CURVE ( 'NONE', #32922, #9737, #30200, .T. ) ;
#37397=CARTESIAN_POINT ( 'NONE',  ( -1.195183497228115035E-16, 3.346456692913386100, 0.3149606299212576177 ) ) ;
#37398=CARTESIAN_POINT ( 'NONE',  ( -0.8182917201112819283, 0.000000000000000000, -0.7874015748031467643 ) ) ;
#37399=LINE ( 'NONE', #28868, #2909 ) ;
#37400=CARTESIAN_POINT ( 'NONE',  ( -2.001301579076982584, 3.346456692913386100, -0.8267716535433052849 ) ) ;
#37401=EDGE_LOOP ( 'NONE', ( #21349, #32749, #48006, #34070 ) ) ;
#37402=DIRECTION ( 'NONE',  ( 0.000000000000000000, 0.000000000000000000, 1.000000000000000000 ) ) ;
#37405=DIRECTION ( 'NONE',  ( -1.000000000000000000, 0.000000000000000000, 1.734723475976806848E-16 ) ) ;
#37406=ORIENTED_EDGE ( 'NONE', *, *, #10594, .T. ) ;
#37407=CARTESIAN_POINT ( 'NONE',  ( -1.636583440222563635, 3.346456692913386100, 1.259842519685033357 ) ) ;
#37410=CARTESIAN_POINT ( 'NONE',  ( -2.182111253630085290, 3.346456692913386100, 0.1181102362204704270 ) ) ;
#37411=DIRECTION ( 'NONE',  ( 1.734723475976806848E-16, -0.000000000000000000, 1.000000000000000000 ) ) ;
#37412=FACE_OUTER_BOUND ( 'NONE', #26434, .T. ) ;
#37414=EDGE_CURVE ( 'NONE', #48104, #2922, #3332, .T. ) ;
#37416=VECTOR ( 'NONE', #24848, 39.37007874015748143 ) ;
#37417=ORIENTED_EDGE ( 'NONE', *, *, #4039, .F. ) ;
#37419=ORIENTED_EDGE ( 'NONE', *, *, #27170, .F. ) ;
#37420=PLANE ( 'NONE',  #39462 ) ;
#37421=VECTOR ( 'NONE', #3862, 39.37007874015748143 ) ;
#37424=VECTOR ( 'NONE', #47161, 39.37007874015748143 ) ;
#37427=LINE ( 'NONE', #45388, #22447 ) ;
#37428=VECTOR ( 'NONE', #38478, 39.37007874015748143 ) ;
#37430=ORIENTED_EDGE ( 'NONE', *, *, #41315, .T. ) ;
#37431=VERTEX_POINT ( 'NONE', #38955 ) ;
#37432=DIRECTION ( 'NONE',  ( -1.000000000000000000, 0.000000000000000000, 1.734723475976806848E-16 ) ) ;
#37433=FACE_BOUND ( 'NONE', #20682, .T. ) ;
#37436=CARTESIAN_POINT ( 'NONE',  ( 1.015142113812069979, 3.346456692913386100, 2.047244094488179567 ) ) ;
#37437=EDGE_CURVE ( 'NONE', #48050, #39080, #42072, .T. ) ;
#37438=EDGE_LOOP ( 'NONE', ( #39582, #17369, #46611, #14687 ) ) ;
#37439=VERTEX_POINT ( 'NONE', #22456 ) ;
#37440=DIRECTION ( 'NONE',  ( 1.734723475976806848E-16, -0.000000000000000000, 1.000000000000000000 ) ) ;
#37441=DIRECTION ( 'NONE',  ( 0.000000000000000000, 1.000000000000000000, 0.000000000000000000 ) ) ;
#37442=ORIENTED_EDGE ( 'NONE', *, *, #34152, .F. ) ;
#37443=VERTEX_POINT ( 'NONE', #43063 ) ;
#37446=CARTESIAN_POINT ( 'NONE',  ( -2.043170538425928662, 3.346456692913386100, -0.5118110236220464460 ) ) ;
#37448=DIRECTION ( 'NONE',  ( 1.000000000000000000, 0.000000000000000000, 0.000000000000000000 ) ) ;
#37449=EDGE_CURVE ( 'NONE', #9370, #38459, #46914, .T. ) ;
#37451=CARTESIAN_POINT ( 'NONE',  ( 2.017116292511733633, 3.267716535433071279, 0.7874015748031456541 ) ) ;
#37452=DIRECTION ( 'NONE',  ( 1.000000000000000000, 0.000000000000000000, -3.469446951953613696E-16 ) ) ;
#37453=EDGE_LOOP ( 'NONE', ( #20540, #45842, #21876, #21906 ) ) ;
#37454=ORIENTED_EDGE ( 'NONE', *, *, #20793, .F. ) ;
#37457=CARTESIAN_POINT ( 'NONE',  ( 0.000000000000000000, 3.267716535433071279, -1.771653543307080581 ) ) ;
#37458=VECTOR ( 'NONE', #17952, 39.37007874015748143 ) ;
#37459=CARTESIAN_POINT ( 'NONE',  ( 1.909347346926324462, 0.000000000000000000, -0.7874015748031473194 ) ) ;
#37460=EDGE_CURVE ( 'NONE', #31646, #49607, #8992, .T. ) ;
#37463=VECTOR ( 'NONE', #6564, 39.37007874015748143 ) ;
#37467=DIRECTION ( 'NONE',  ( -3.469446951953613696E-16, 0.000000000000000000, -1.000000000000000000 ) ) ;
#37468=DIRECTION ( 'NONE',  ( 1.000000000000000000, 0.000000000000000000, 0.000000000000000000 ) ) ;
#37472=EDGE_LOOP ( 'NONE', ( #29161, #14246, #13242, #15202 ) ) ;
#37473=ORIENTED_EDGE ( 'NONE', *, *, #2908, .F. ) ;
#37475=CARTESIAN_POINT ( 'NONE',  ( 1.015142113812069091, 3.226129038349118794, -2.244094488188969283 ) ) ;
#37476=ORIENTED_EDGE ( 'NONE', *, *, #37252, .F. ) ;
#37477=EDGE_CURVE ( 'NONE', #8594, #45509, #986, .T. ) ;
#37478=EDGE_CURVE ( 'NONE', #9370, #29512, #31721, .T. ) ;
#37479=ORIENTED_EDGE ( 'NONE', *, *, #26443, .T. ) ;
#37480=LINE ( 'NONE', #1068, #18832 ) ;
#37481=VERTEX_POINT ( 'NONE', #15709 ) ;
#37482=LINE ( 'NONE', #5969, #9510 ) ;
#37483=DIRECTION ( 'NONE',  ( -0.000000000000000000, 1.000000000000000000, -0.000000000000000000 ) ) ;
#37484=EDGE_LOOP ( 'NONE', ( #28216, #201, #22321, #8322 ) ) ;
#37485=VERTEX_POINT ( 'NONE', #598 ) ;
#37486=ORIENTED_EDGE ( 'NONE', *, *, #19428, .F. ) ;
#37487=CARTESIAN_POINT ( 'NONE',  ( -0.8182917201112821504, 3.346456692913386100, 1.940849049717691344 ) ) ;
#37488=VECTOR ( 'NONE', #2898, 39.37007874015748143 ) ;
#37489=ORIENTED_EDGE ( 'NONE', *, *, #74, .T. ) ;
#37490=EDGE_LOOP ( 'NONE', ( #35059, #47115, #7512, #379 ) ) ;
#37491=DIRECTION ( 'NONE',  ( 1.000000000000000000, -0.000000000000000000, 0.000000000000000000 ) ) ;
#37495=AXIS2_PLACEMENT_3D ( 'NONE', #29648, #6660, #13647 ) ;
#37496=VERTEX_POINT ( 'NONE', #12352 ) ;
#37497=CARTESIAN_POINT ( 'NONE',  ( 0.000000000000000000, 3.267716535433071279, 0.000000000000000000 ) ) ;
#37498=LINE ( 'NONE', #29737, #37416 ) ;
#37499=CARTESIAN_POINT ( 'NONE',  ( 1.091055626815042423, 0.000000000000000000, -2.086614173228339641 ) ) ;
#37502=LINE ( 'NONE', #18375, #16183 ) ;
#37503=VECTOR ( 'NONE', #34729, 39.37007874015748143 ) ;
#37504=CARTESIAN_POINT ( 'NONE',  ( -0.6214413264104945434, 3.267716535433071279, -0.7874015748031467643 ) ) ;
#37505=ORIENTED_EDGE ( 'NONE', *, *, #5620, .F. ) ;
#37506=ORIENTED_EDGE ( 'NONE', *, *, #44222, .T. ) ;
#37507=LINE ( 'NONE', #14250, #6637 ) ;
#37508=ADVANCED_FACE ( 'NONE', ( #47932 ), #28085, .F. ) ;
#37509=EDGE_CURVE ( 'NONE', #50129, #29717, #12099, .T. ) ;
#37510=LINE ( 'NONE', #17878, #588 ) ;
#37512=ORIENTED_EDGE ( 'NONE', *, *, #10755, .F. ) ;
#37513=ORIENTED_EDGE ( 'NONE', *, *, #38395, .F. ) ;
#37516=ORIENTED_EDGE ( 'NONE', *, *, #25354, .T. ) ;
#37517=CARTESIAN_POINT ( 'NONE',  ( 1.015142113812069313, 3.267716535433071279, -3.521981712565032389E-16 ) ) ;
#37519=LINE ( 'NONE', #45731, #43131 ) ;
#37521=DIRECTION ( 'NONE',  ( -0.000000000000000000, 1.000000000000000000, -0.000000000000000000 ) ) ;
#37523=VECTOR ( 'NONE', #21194, 39.37007874015748143 ) ;
#37524=LINE ( 'NONE', #10145, #18443 ) ;
#37525=CARTESIAN_POINT ( 'NONE',  ( 1.287906020515830141, 3.267716535433071279, -0.8267716535433055070 ) ) ;
#37528=CARTESIAN_POINT ( 'NONE',  ( 0.1968503937007873017, 3.346456692913386100, -0.6299212598425177889 ) ) ;
#37529=VECTOR ( 'NONE', #23356, 39.37007874015748143 ) ;
#37530=ORIENTED_EDGE ( 'NONE', *, *, #33519, .F. ) ;
#37531=PLANE ( 'NONE',  #19084 ) ;
#37534=CARTESIAN_POINT ( 'NONE',  ( -0.8942052331142552601, 0.000000000000000000, -0.1968503937007881899 ) ) ;
#37535=VERTEX_POINT ( 'NONE', #40237 ) ;
#37536=EDGE_CURVE ( 'NONE', #35361, #43946, #36106, .T. ) ;
#37538=VECTOR ( 'NONE', #12319, 39.37007874015748143 ) ;
#37539=EDGE_CURVE ( 'NONE', #32210, #30461, #43828, .T. ) ;
#37540=ORIENTED_EDGE ( 'NONE', *, *, #3252, .F. ) ;
#37541=CARTESIAN_POINT ( 'NONE',  ( -1.166969139818015977, 3.346456692913386100, -1.417322834645664109 ) ) ;
#37544=ORIENTED_EDGE ( 'NONE', *, *, #43139, .F. ) ;
#37546=LINE ( 'NONE', #29534, #31731 ) ;
#37547=PLANE ( 'NONE',  #5720 ) ;
#37549=CARTESIAN_POINT ( 'NONE',  ( 1.287906020515830141, 0.000000000000000000, -0.9448818897637765168 ) ) ;
#37550=ORIENTED_EDGE ( 'NONE', *, *, #32564, .F. ) ;
#37552=CARTESIAN_POINT ( 'NONE',  ( -0.3486774197067340486, 3.267716535433071279, 2.007874015748021268 ) ) ;
#37553=CARTESIAN_POINT ( 'NONE',  ( -0.5455278134075214336, 3.346456692913386100, 0.3149606299212577287 ) ) ;
#37555=DIRECTION ( 'NONE',  ( -0.000000000000000000, 1.000000000000000000, -0.000000000000000000 ) ) ;
#37556=PLANE ( 'NONE',  #47417 ) ;
#37557=CARTESIAN_POINT ( 'NONE',  ( -2.182111253630085290, 0.000000000000000000, 0.9448818897637749625 ) ) ;
#37558=ORIENTED_EDGE ( 'NONE', *, *, #23509, .F. ) ;
#37559=ORIENTED_EDGE ( 'NONE', *, *, #49346, .F. ) ;
#37560=LINE ( 'NONE', #1927, #7338 ) ;
#37562=CARTESIAN_POINT ( 'NONE',  ( 1.560669927219590747, 0.000000000000000000, 0.4724409448818871482 ) ) ;
#37563=ORIENTED_EDGE ( 'NONE', *, *, #12283, .T. ) ;
#37565=CARTESIAN_POINT ( 'NONE',  ( 0.000000000000000000, 3.267716535433071279, 0.3149606299212573401 ) ) ;
#37566=AXIS2_PLACEMENT_3D ( 'NONE', #11285, #35035, #47109 ) ;
#37570=EDGE_LOOP ( 'NONE', ( #20688, #16688, #14544, #17514 ) ) ;
#37571=VERTEX_POINT ( 'NONE', #44345 ) ;
#37572=FACE_OUTER_BOUND ( 'NONE', #24357, .T. ) ;
#37573=DIRECTION ( 'NONE',  ( 0.000000000000000000, 0.000000000000000000, 1.000000000000000000 ) ) ;
#37574=VECTOR ( 'NONE', #45437, 39.37007874015748143 ) ;
#37576=ORIENTED_EDGE ( 'NONE', *, *, #21251, .F. ) ;
#37578=LINE ( 'NONE', #2461, #25493 ) ;
#37580=EDGE_CURVE ( 'NONE', #24715, #15133, #43578, .T. ) ;
#37581=AXIS2_PLACEMENT_3D ( 'NONE', #39365, #117, #23357 ) ;
#37582=EDGE_CURVE ( 'NONE', #7484, #3114, #36618, .T. ) ;
#37584=ADVANCED_FACE ( 'NONE', ( #31465 ), #20080, .F. ) ;
#37586=CARTESIAN_POINT ( 'NONE',  ( -2.182111253630085290, 3.226699998040846395, -1.141732283464563791 ) ) ;
#37588=CARTESIAN_POINT ( 'NONE',  ( 1.015142113812069979, 0.000000000000000000, 1.220472440944875281 ) ) ;
#37589=ORIENTED_EDGE ( 'NONE', *, *, #20316, .F. ) ;
#37592=ORIENTED_EDGE ( 'NONE', *, *, #40225, .T. ) ;
#37593=DIRECTION ( 'NONE',  ( 1.000000000000000000, 0.000000000000000000, 0.000000000000000000 ) ) ;
#37595=CARTESIAN_POINT ( 'NONE',  ( -2.438548951736694725, 3.267716535433071279, -0.1574803149606298636 ) ) ;
#37596=ORIENTED_EDGE ( 'NONE', *, *, #15241, .T. ) ;
#37597=DIRECTION ( 'NONE',  ( -0.000000000000000000, 1.000000000000000000, -0.000000000000000000 ) ) ;
#37598=DIRECTION ( 'NONE',  ( -3.469446951953613696E-16, 0.000000000000000000, -1.000000000000000000 ) ) ;
#37603=ORIENTED_EDGE ( 'NONE', *, *, #31937, .F. ) ;
#37604=FACE_OUTER_BOUND ( 'NONE', #41321, .T. ) ;
#37605=ORIENTED_EDGE ( 'NONE', *, *, #10433, .T. ) ;
#37606=DIRECTION ( 'NONE',  ( 0.000000000000000000, 1.000000000000000000, 0.000000000000000000 ) ) ;
#37607=AXIS2_PLACEMENT_3D ( 'NONE', #13161, #44881, #9535 ) ;
#37608=CARTESIAN_POINT ( 'NONE',  ( 1.287906020515830585, 3.346456692913386100, 1.889763779527550369 ) ) ;
#37610=CARTESIAN_POINT ( 'NONE',  ( 1.363819533518803251, 0.000000000000000000, 1.102362204724403938 ) ) ;
#37611=VECTOR ( 'NONE', #21148, 39.37007874015748143 ) ;
#37612=AXIS2_PLACEMENT_3D ( 'NONE', #40069, #12439, #36202 ) ;
#37613=VERTEX_POINT ( 'NONE', #27575 ) ;
#37614=EDGE_LOOP ( 'NONE', ( #38767, #6186, #3366, #24928 ) ) ;
#37616=EDGE_LOOP ( 'NONE', ( #27645, #48553, #36077, #25406 ) ) ;
#37617=CARTESIAN_POINT ( 'NONE',  ( 1.636583440222563857, 3.346456692913386100, -0.3149606299212596716 ) ) ;
#37618=ORIENTED_EDGE ( 'NONE', *, *, #44327, .T. ) ;
#37619=CARTESIAN_POINT ( 'NONE',  ( 0.000000000000000000, 3.267716535433071279, 0.000000000000000000 ) ) ;
#37621=CARTESIAN_POINT ( 'NONE',  ( -1.091055626815042645, 0.000000000000000000, -0.1968503937007881899 ) ) ;
#37622=LINE ( 'NONE', #6877, #42145 ) ;
#37623=ORIENTED_EDGE ( 'NONE', *, *, #50380, .F. ) ;
#37625=ORIENTED_EDGE ( 'NONE', *, *, #47196, .T. ) ;
#37626=ORIENTED_EDGE ( 'NONE', *, *, #42291, .F. ) ;
#37628=ORIENTED_EDGE ( 'NONE', *, *, #46206, .T. ) ;
#37630=DIRECTION ( 'NONE',  ( 1.734723475976806848E-16, -0.000000000000000000, 1.000000000000000000 ) ) ;
#37631=ADVANCED_FACE ( 'NONE', ( #45598 ), #2261, .F. ) ;
#37632=AXIS2_PLACEMENT_3D ( 'NONE', #24981, #45093, #33767 ) ;
#37633=EDGE_CURVE ( 'NONE', #15411, #42940, #37643, .T. ) ;
#37635=ORIENTED_EDGE ( 'NONE', *, *, #20165, .F. ) ;
#37639=CARTESIAN_POINT ( 'NONE',  ( -0.07591351300297340121, 3.267716535433071279, -0.9842519685039344823 ) ) ;
#37640=ADVANCED_FACE ( 'NONE', ( #21378 ), #44847, .F. ) ;
#37641=VECTOR ( 'NONE', #10036, 39.37007874015748143 ) ;
#37643=LINE ( 'NONE', #41256, #14036 ) ;
#37644=VERTEX_POINT ( 'NONE', #41501 ) ;
#37645=CIRCLE ( 'NONE', #15373, 2.106299212598425008 ) ;
#37646=CARTESIAN_POINT ( 'NONE',  ( -0.5455278134075208785, 3.346456692913386100, 0.4330708661417290162 ) ) ;
#37647=LINE ( 'NONE', #42253, #37725 ) ;
#37648=VERTEX_POINT ( 'NONE', #40745 ) ;
#37650=DIRECTION ( 'NONE',  ( 1.734723475976806848E-16, 0.000000000000000000, 1.000000000000000000 ) ) ;
#37653=ORIENTED_EDGE ( 'NONE', *, *, #16866, .T. ) ;
#37657=VERTEX_POINT ( 'NONE', #6134 ) ;
#37659=LINE ( 'NONE', #26278, #9446 ) ;
#37660=ORIENTED_EDGE ( 'NONE', *, *, #34002, .T. ) ;
#37664=ORIENTED_EDGE ( 'NONE', *, *, #7952, .T. ) ;
#37666=LINE ( 'NONE', #26529, #42366 ) ;
#37669=DIRECTION ( 'NONE',  ( -0.000000000000000000, 1.000000000000000000, -0.000000000000000000 ) ) ;
#37670=ORIENTED_EDGE ( 'NONE', *, *, #16268, .F. ) ;
#37671=EDGE_CURVE ( 'NONE', #38575, #39739, #13630, .T. ) ;
#37672=VECTOR ( 'NONE', #33785, 39.37007874015748143 ) ;
#37673=PLANE ( 'NONE',  #207 ) ;
#37674=VECTOR ( 'NONE', #1747, 39.37007874015748143 ) ;
#37675=EDGE_LOOP ( 'NONE', ( #8573, #10452, #24524, #30607 ) ) ;
#37676=VERTEX_POINT ( 'NONE', #33012 ) ;
#37678=CARTESIAN_POINT ( 'NONE',  ( -0.2727639067037608278, 3.346456692913386100, -1.929133858267710000 ) ) ;
#37680=ORIENTED_EDGE ( 'NONE', *, *, #24506, .T. ) ;
#37681=DIRECTION ( 'NONE',  ( -0.000000000000000000, 0.000000000000000000, 1.000000000000000000 ) ) ;
#37683=EDGE_CURVE ( 'NONE', #33009, #58, #29631, .T. ) ;
#37684=VERTEX_POINT ( 'NONE', #9245 ) ;
#37685=LINE ( 'NONE', #18810, #21492 ) ;
#37687=CARTESIAN_POINT ( 'NONE',  ( -0.6214413264104945434, 3.346456692913386100, -1.102362204724405492 ) ) ;
#37690=ORIENTED_EDGE ( 'NONE', *, *, #1883, .T. ) ;
#37691=ORIENTED_EDGE ( 'NONE', *, *, #29340, .F. ) ;
#37692=DIRECTION ( 'NONE',  ( 1.000000000000000000, 0.000000000000000000, 0.000000000000000000 ) ) ;
#37693=FACE_BOUND ( 'NONE', #24671, .T. ) ;
#37694=ORIENTED_EDGE ( 'NONE', *, *, #44917, .F. ) ;
#37697=ORIENTED_EDGE ( 'NONE', *, *, #32570, .T. ) ;
#37698=ORIENTED_EDGE ( 'NONE', *, *, #46725, .F. ) ;
#37699=LINE ( 'NONE', #21429, #8463 ) ;
#37704=CARTESIAN_POINT ( 'NONE',  ( 0.1968503937007878568, 3.267716535433071279, -6.829619984160672837E-17 ) ) ;
#37705=EDGE_CURVE ( 'NONE', #32825, #19764, #22141, .T. ) ;
#37706=DIRECTION ( 'NONE',  ( -1.000000000000000000, -0.000000000000000000, -0.000000000000000000 ) ) ;
#37707=ADVANCED_FACE ( 'NONE', ( #21626 ), #25247, .F. ) ;
#37710=EDGE_CURVE ( 'NONE', #50633, #31767, #17000, .T. ) ;
#37711=DIRECTION ( 'NONE',  ( 0.000000000000000000, 1.000000000000000000, 0.000000000000000000 ) ) ;
#37712=ORIENTED_EDGE ( 'NONE', *, *, #30207, .F. ) ;
#37714=CARTESIAN_POINT ( 'NONE',  ( -1.166969139818016199, 0.000000000000000000, -1.299212598425192544 ) ) ;
#37716=LINE ( 'NONE', #37457, #33745 ) ;
#37717=PLANE ( 'NONE',  #20028 ) ;
#37719=DIRECTION ( 'NONE',  ( -1.000000000000000000, 0.000000000000000000, 0.000000000000000000 ) ) ;
#37720=CARTESIAN_POINT ( 'NONE',  ( 2.361042194882304379, 3.267716535433071279, 0.6299212598425161236 ) ) ;
#37721=CARTESIAN_POINT ( 'NONE',  ( 1.560669927219590525, 0.000000000000000000, 0.5905511811023579360 ) ) ;
#37722=EDGE_LOOP ( 'NONE', ( #10415, #25525, #639, #45108 ) ) ;
#37723=LINE ( 'NONE', #18850, #26720 ) ;
#37724=DIRECTION ( 'NONE',  ( -0.000000000000000000, 1.000000000000000000, -0.000000000000000000 ) ) ;
#37725=VECTOR ( 'NONE', #2263, 39.37007874015748143 ) ;
#37726=VERTEX_POINT ( 'NONE', #24992 ) ;
#37727=EDGE_LOOP ( 'NONE', ( #27115, #13649, #36954, #13290 ) ) ;
#37728=DIRECTION ( 'NONE',  ( -3.469446951953613696E-16, 0.000000000000000000, -1.000000000000000000 ) ) ;
#37730=EDGE_CURVE ( 'NONE', #39348, #28725, #32760, .T. ) ;
#37731=ORIENTED_EDGE ( 'NONE', *, *, #37106, .T. ) ;
#37733=EDGE_CURVE ( 'NONE', #19488, #48282, #45097, .T. ) ;
#37736=DIRECTION ( 'NONE',  ( -1.000000000000000000, -0.000000000000000000, -0.000000000000000000 ) ) ;
#37739=ORIENTED_EDGE ( 'NONE', *, *, #3013, .T. ) ;
#37742=ORIENTED_EDGE ( 'NONE', *, *, #16470, .T. ) ;
#37743=VERTEX_POINT ( 'NONE', #17753 ) ;
#37744=EDGE_CURVE ( 'NONE', #47890, #12778, #21124, .T. ) ;
#37745=DIRECTION ( 'NONE',  ( 0.000000000000000000, 0.000000000000000000, 1.000000000000000000 ) ) ;
#37746=CYLINDRICAL_SURFACE ( 'NONE', #31849, 2.952755905511811552 ) ;
#37747=CARTESIAN_POINT ( 'NONE',  ( -1.439733046521776139, 3.267716535433071279, -4.780733988912460139E-16 ) ) ;
#37748=AXIS2_PLACEMENT_3D ( 'NONE', #19060, #42559, #42303 ) ;
#37750=ORIENTED_EDGE ( 'NONE', *, *, #40225, .F. ) ;
#37751=CARTESIAN_POINT ( 'NONE',  ( -1.363819533518803029, 3.346456692913386100, 0.9055118110236167750 ) ) ;
#37753=CARTESIAN_POINT ( 'NONE',  ( -2.258024766633058622, 3.267716535433071279, -0.03937007874015881204 ) ) ;
#37754=VERTEX_POINT ( 'NONE', #30391 ) ;
#37756=DIRECTION ( 'NONE',  ( 1.734723475976806848E-16, -0.000000000000000000, 1.000000000000000000 ) ) ;
#37757=DIRECTION ( 'NONE',  ( 1.000000000000000000, 0.000000000000000000, -3.469446951953613696E-16 ) ) ;
#37758=ORIENTED_EDGE ( 'NONE', *, *, #35590, .F. ) ;
#37759=ORIENTED_EDGE ( 'NONE', *, *, #50874, .T. ) ;
#37760=EDGE_CURVE ( 'NONE', #34814, #23582, #22894, .T. ) ;
#37761=DIRECTION ( 'NONE',  ( -3.469446951953613696E-16, 0.000000000000000000, -1.000000000000000000 ) ) ;
#37762=CARTESIAN_POINT ( 'NONE',  ( 0.000000000000000000, 3.267716535433071279, 1.574803149606291974 ) ) ;
#37763=EDGE_CURVE ( 'NONE', #41844, #45206, #31150, .T. ) ;
#37767=ORIENTED_EDGE ( 'NONE', *, *, #2017, .T. ) ;
#37768=EDGE_CURVE ( 'NONE', #17591, #38922, #19012, .T. ) ;
#37769=CARTESIAN_POINT ( 'NONE',  ( 3.927031490892378253E-16, 0.000000000000000000, 1.377952755905504256 ) ) ;
#37770=EDGE_LOOP ( 'NONE', ( #27095, #49484, #31785, #47816 ) ) ;
#37772=CARTESIAN_POINT ( 'NONE',  ( -0.07591351300297277671, 0.000000000000000000, 2.047244094488179567 ) ) ;
#37773=AXIS2_PLACEMENT_3D ( 'NONE', #39619, #19731, #19478 ) ;
#37776=PLANE ( 'NONE',  #40901 ) ;
#37777=DIRECTION ( 'NONE',  ( 0.000000000000000000, 0.000000000000000000, -1.000000000000000000 ) ) ;
#37778=ORIENTED_EDGE ( 'NONE', *, *, #7887, .T. ) ;
#37781=VECTOR ( 'NONE', #41302, 39.37007874015748143 ) ;
#37782=DIRECTION ( 'NONE',  ( -1.000000000000000000, -0.000000000000000000, -0.000000000000000000 ) ) ;
#37784=VECTOR ( 'NONE', #34670, 39.37007874015748143 ) ;
#37786=CARTESIAN_POINT ( 'NONE',  ( 2.182111253630085290, 0.000000000000000000, 0.3149606299212573401 ) ) ;
#37789=EDGE_CURVE ( 'NONE', #4458, #37754, #38892, .T. ) ;
#37790=VECTOR ( 'NONE', #23192, 39.37007874015748143 ) ;
#37791=DIRECTION ( 'NONE',  ( 0.000000000000000000, 0.000000000000000000, -1.000000000000000000 ) ) ;
#37793=DIRECTION ( 'NONE',  ( -1.000000000000000000, 0.000000000000000000, -0.000000000000000000 ) ) ;
#37795=ORIENTED_EDGE ( 'NONE', *, *, #44980, .T. ) ;
#37797=CARTESIAN_POINT ( 'NONE',  ( 0.2727639067037604392, 3.267716535433071279, 0.2755905511810994302 ) ) ;
#37799=CARTESIAN_POINT ( 'NONE',  ( 1.287906020515829919, 0.000000000000000000, -1.259842519685035134 ) ) ;
#37800=LINE ( 'NONE', #2425, #12378 ) ;
#37801=LINE ( 'NONE', #14039, #16938 ) ;
#37802=EDGE_CURVE ( 'NONE', #31344, #37886, #3024, .T. ) ;
#37804=ORIENTED_EDGE ( 'NONE', *, *, #29170, .T. ) ;
#37806=DIRECTION ( 'NONE',  ( 1.734723475976806848E-16, -0.000000000000000000, 1.000000000000000000 ) ) ;
#37807=DIRECTION ( 'NONE',  ( 1.000000000000000000, 0.000000000000000000, -3.469446951953613696E-16 ) ) ;
#37808=ORIENTED_EDGE ( 'NONE', *, *, #27878, .F. ) ;
#37810=LINE ( 'NONE', #22052, #5492 ) ;
#37812=ORIENTED_EDGE ( 'NONE', *, *, #7138, .F. ) ;
#37813=ORIENTED_EDGE ( 'NONE', *, *, #39675, .F. ) ;
#37814=FACE_OUTER_BOUND ( 'NONE', #39446, .T. ) ;
#37815=CARTESIAN_POINT ( 'NONE',  ( 2.182111253630085290, 3.267716535433071279, -1.161035397307311917E-15 ) ) ;
#37817=DIRECTION ( 'NONE',  ( -3.469446951953613696E-16, 0.000000000000000000, -1.000000000000000000 ) ) ;
#37818=EDGE_CURVE ( 'NONE', #48094, #32722, #46857, .T. ) ;
#37819=ORIENTED_EDGE ( 'NONE', *, *, #27211, .F. ) ;
#37821=CARTESIAN_POINT ( 'NONE',  ( -1.363819533518803473, 3.267716535433071279, -1.732283464566922726 ) ) ;
#37824=ORIENTED_EDGE ( 'NONE', *, *, #12904, .F. ) ;
#37825=VECTOR ( 'NONE', #12083, 39.37007874015748143 ) ;
#37826=ORIENTED_EDGE ( 'NONE', *, *, #9890, .F. ) ;
#37828=DIRECTION ( 'NONE',  ( 1.000000000000000000, 0.000000000000000000, 0.000000000000000000 ) ) ;
#37829=DIRECTION ( 'NONE',  ( 1.000000000000000000, 0.000000000000000000, -3.469446951953613696E-16 ) ) ;
#37831=VECTOR ( 'NONE', #46390, 39.37007874015748143 ) ;
#37833=EDGE_LOOP ( 'NONE', ( #42062, #24610, #32173, #24984 ) ) ;
#37834=CARTESIAN_POINT ( 'NONE',  ( -2.454875160333845674, 3.245198442041970832, 0.02684680494028401573 ) ) ;
#37836=EDGE_CURVE ( 'NONE', #2302, #35717, #46108, .T. ) ;
#37837=VECTOR ( 'NONE', #41253, 39.37007874015748143 ) ;
#37838=LINE ( 'NONE', #41947, #13123 ) ;
#37839=ORIENTED_EDGE ( 'NONE', *, *, #1820, .T. ) ;
#37840=ADVANCED_FACE ( 'NONE', ( #27005 ), #30643, .F. ) ;
#37841=VECTOR ( 'NONE', #6086, 39.37007874015748143 ) ;
#37842=VERTEX_POINT ( 'NONE', #3526 ) ;
#37845=AXIS2_PLACEMENT_3D ( 'NONE', #44593, #9249, #5372 ) ;
#37846=PLANE ( 'NONE',  #2540 ) ;
#37847=CARTESIAN_POINT ( 'NONE',  ( -1.091055626815042201, 0.000000000000000000, 1.259842519685033357 ) ) ;
#37850=CARTESIAN_POINT ( 'NONE',  ( -1.166969139818015533, 3.346456692913386100, 0.7874015748031456541 ) ) ;
#37851=DIRECTION ( 'NONE',  ( -0.000000000000000000, 1.000000000000000000, -0.000000000000000000 ) ) ;
#37852=ORIENTED_EDGE ( 'NONE', *, *, #28463, .F. ) ;
#37853=DIRECTION ( 'NONE',  ( -3.469446951953613696E-16, 0.000000000000000000, -1.000000000000000000 ) ) ;
#37854=DIRECTION ( 'NONE',  ( -3.469446951953613696E-16, 0.000000000000000000, -1.000000000000000000 ) ) ;
#37855=ORIENTED_EDGE ( 'NONE', *, *, #26504, .T. ) ;
#37856=DIRECTION ( 'NONE',  ( -0.000000000000000000, 0.000000000000000000, 1.000000000000000000 ) ) ;
#37857=AXIS2_PLACEMENT_3D ( 'NONE', #21601, #9474, #40979 ) ;
#37858=DIRECTION ( 'NONE',  ( -0.000000000000000000, 1.000000000000000000, -0.000000000000000000 ) ) ;
#37859=LINE ( 'NONE', #49166, #16961 ) ;
#37860=B_SPLINE_CURVE_WITH_KNOTS ( 'NONE', 3,
 ( #46044, #37834, #42442, #42935 ),
 .UNSPECIFIED., .F., .F.,
 ( 4, 4 ),
 ( 0.02645197609580694081, 0.03146547178533463940 ),
 .UNSPECIFIED. ) ;
#37863=EDGE_LOOP ( 'NONE', ( #2937, #29569, #14189 ) ) ;
#37864=FACE_BOUND ( 'NONE', #41272, .T. ) ;
#37865=DIRECTION ( 'NONE',  ( 1.734723475976806848E-16, -0.000000000000000000, 1.000000000000000000 ) ) ;
#37866=VECTOR ( 'NONE', #30247, 39.37007874015748143 ) ;
#37867=VECTOR ( 'NONE', #18198, 39.37007874015748143 ) ;
#37868=DIRECTION ( 'NONE',  ( 1.000000000000000000, 0.000000000000000000, 0.000000000000000000 ) ) ;
#37871=AXIS2_PLACEMENT_3D ( 'NONE', #8539, #797, #48253 ) ;
#37872=EDGE_CURVE ( 'NONE', #13698, #37269, #45856, .T. ) ;
#37873=VERTEX_POINT ( 'NONE', #3272 ) ;
#37874=ORIENTED_EDGE ( 'NONE', *, *, #44543, .F. ) ;
#37875=DIRECTION ( 'NONE',  ( 1.734723475976806848E-16, -0.000000000000000000, 1.000000000000000000 ) ) ;
#37877=CARTESIAN_POINT ( 'NONE',  ( 1.091055626815042645, 0.000000000000000000, -0.8267716535433055070 ) ) ;
#37878=ORIENTED_EDGE ( 'NONE', *, *, #14365, .T. ) ;
#37879=DIRECTION ( 'NONE',  ( 1.000000000000000000, 0.000000000000000000, 0.000000000000000000 ) ) ;
#37880=ORIENTED_EDGE ( 'NONE', *, *, #21830, .T. ) ;
#37881=CARTESIAN_POINT ( 'NONE',  ( 1.909347346926324684, 0.000000000000000000, 0.4724409448818868706 ) ) ;
#37882=DIRECTION ( 'NONE',  ( -3.469446951953613696E-16, 0.000000000000000000, -1.000000000000000000 ) ) ;
#37884=LINE ( 'NONE', #17993, #41433 ) ;
#37886=VERTEX_POINT ( 'NONE', #42009 ) ;
#37889=AXIS2_PLACEMENT_3D ( 'NONE', #35950, #578, #23056 ) ;
#37891=ORIENTED_EDGE ( 'NONE', *, *, #49068, .F. ) ;
#37892=LINE ( 'NONE', #44584, #17029 ) ;
#37893=EDGE_CURVE ( 'NONE', #17882, #14542, #31404, .T. ) ;
#37894=ORIENTED_EDGE ( 'NONE', *, *, #43886, .T. ) ;
#37895=DIRECTION ( 'NONE',  ( -3.469446951953613696E-16, 0.000000000000000000, -1.000000000000000000 ) ) ;
#37897=VECTOR ( 'NONE', #33834, 39.37007874015748143 ) ;
#37899=VECTOR ( 'NONE', #27986, 39.37007874015748143 ) ;
#37902=ORIENTED_EDGE ( 'NONE', *, *, #35483, .T. ) ;
#37903=LINE ( 'NONE', #34023, #7631 ) ;
#37904=CARTESIAN_POINT ( 'NONE',  ( -2.182111253630085290, 3.346456692913386100, 0.3149606299212578953 ) ) ;
#37907=DIRECTION ( 'NONE',  ( -0.000000000000000000, 1.000000000000000000, -0.000000000000000000 ) ) ;
#37909=DIRECTION ( 'NONE',  ( -1.000000000000000000, 0.000000000000000000, 1.734723475976806848E-16 ) ) ;
#37910=CARTESIAN_POINT ( 'NONE',  ( -0.8182917201112814842, 3.346456692913386100, 1.535433070866133898 ) ) ;
#37913=LINE ( 'NONE', #48959, #49782 ) ;
#37914=ORIENTED_EDGE ( 'NONE', *, *, #42839, .F. ) ;
#37915=ORIENTED_EDGE ( 'NONE', *, *, #2705, .F. ) ;
#37918=CARTESIAN_POINT ( 'NONE',  ( 1.636583440222563857, 3.346456692913386100, 1.062992125984245639 ) ) ;
#37919=LINE ( 'NONE', #9784, #18509 ) ;
#37921=VECTOR ( 'NONE', #49496, 39.37007874015748143 ) ;
#37923=CARTESIAN_POINT ( 'NONE',  ( 2.106197740627111514, 3.267716535433071279, -0.7874015748031473194 ) ) ;
#37927=EDGE_CURVE ( 'NONE', #32172, #42867, #40179, .T. ) ;
#37928=CARTESIAN_POINT ( 'NONE',  ( -1.091055626815042645, 3.267716535433071279, -1.456692913385822186 ) ) ;
#37929=ORIENTED_EDGE ( 'NONE', *, *, #26502, .T. ) ;
#37930=CARTESIAN_POINT ( 'NONE',  ( 0.000000000000000000, 3.267716535433071279, -0.6692913385826764205 ) ) ;
#37931=FACE_OUTER_BOUND ( 'NONE', #46525, .T. ) ;
#37932=ORIENTED_EDGE ( 'NONE', *, *, #20802, .F. ) ;
#37936=DIRECTION ( 'NONE',  ( -3.469446951953613696E-16, 0.000000000000000000, -1.000000000000000000 ) ) ;
#37937=EDGE_CURVE ( 'NONE', #47433, #35962, #674, .T. ) ;
#37939=ORIENTED_EDGE ( 'NONE', *, *, #4929, .T. ) ;
#37942=FACE_BOUND ( 'NONE', #16533, .T. ) ;
#37943=ORIENTED_EDGE ( 'NONE', *, *, #8526, .T. ) ;
#37944=VECTOR ( 'NONE', #37483, 39.37007874015748143 ) ;
#37945=PLANE ( 'NONE',  #32814 ) ;
#37946=ADVANCED_FACE ( 'NONE', ( #43769 ), #23912, .F. ) ;
#37947=FACE_OUTER_BOUND ( 'NONE', #15912, .T. ) ;
#37949=EDGE_LOOP ( 'NONE', ( #1806, #45274, #25022, #12146 ) ) ;
#37950=CARTESIAN_POINT ( 'NONE',  ( 0.000000000000000000, 3.267716535433071279, -0.1574803149606298636 ) ) ;
#37951=DIRECTION ( 'NONE',  ( 1.734723475976806848E-16, -0.000000000000000000, 1.000000000000000000 ) ) ;
#37952=EDGE_CURVE ( 'NONE', #14507, #25804, #930, .T. ) ;
#37953=ORIENTED_EDGE ( 'NONE', *, *, #15427, .T. ) ;
#37954=ORIENTED_EDGE ( 'NONE', *, *, #531, .F. ) ;
#37956=FACE_OUTER_BOUND ( 'NONE', #36926, .T. ) ;
#37957=DIRECTION ( 'NONE',  ( 0.000000000000000000, -1.000000000000000000, 0.000000000000000000 ) ) ;
#37959=CARTESIAN_POINT ( 'NONE',  ( 0.8182917201112819283, 0.000000000000000000, 1.102362204724403938 ) ) ;
#37960=ORIENTED_EDGE ( 'NONE', *, *, #29307, .F. ) ;
#37961=VERTEX_POINT ( 'NONE', #19516 ) ;
#37969=AXIS2_PLACEMENT_3D ( 'NONE', #43895, #24300, #40041 ) ;
#37970=VECTOR ( 'NONE', #32358, 39.37007874015748143 ) ;
#37974=CARTESIAN_POINT ( 'NONE',  ( -0.8942052331142552601, 3.346456692913386100, -1.259842519685034690 ) ) ;
#37975=PLANE ( 'NONE',  #43382 ) ;
#37976=VECTOR ( 'NONE', #38190, 39.37007874015748143 ) ;
#37977=ORIENTED_EDGE ( 'NONE', *, *, #20469, .F. ) ;
#37978=ORIENTED_EDGE ( 'NONE', *, *, #22288, .F. ) ;
#37979=DIRECTION ( 'NONE',  ( 1.000000000000000000, -0.000000000000000000, 0.000000000000000000 ) ) ;
#37980=ORIENTED_EDGE ( 'NONE', *, *, #1881, .T. ) ;
#37981=EDGE_CURVE ( 'NONE', #36589, #48375, #31662, .T. ) ;
#37982=ORIENTED_EDGE ( 'NONE', *, *, #6593, .T. ) ;
#37983=DIRECTION ( 'NONE',  ( -0.000000000000000000, 1.000000000000000000, -0.000000000000000000 ) ) ;
#37985=ADVANCED_FACE ( 'NONE', ( #8423 ), #39659, .F. ) ;
#37987=LINE ( 'NONE', #25847, #51048 ) ;
#37989=ADVANCED_FACE ( 'NONE', ( #31928 ), #44292, .F. ) ;
#37993=ORIENTED_EDGE ( 'NONE', *, *, #9754, .F. ) ;
#37994=ORIENTED_EDGE ( 'NONE', *, *, #10749, .F. ) ;
#37996=CARTESIAN_POINT ( 'NONE',  ( 0.8182917201112824834, 0.000000000000000000, 1.850393700787392293 ) ) ;
#37997=LINE ( 'NONE', #10622, #97 ) ;
#37999=VECTOR ( 'NONE', #2710, 39.37007874015748143 ) ;
#38000=ORIENTED_EDGE ( 'NONE', *, *, #12098, .T. ) ;
#38001=VECTOR ( 'NONE', #12569, 39.37007874015748143 ) ;
#38002=CARTESIAN_POINT ( 'NONE',  ( -0.3486774197067335490, 3.267716535433071279, 1.209717811016577599E-16 ) ) ;
#38003=EDGE_CURVE ( 'NONE', #4171, #11553, #35280, .T. ) ;
#38004=LINE ( 'NONE', #38507, #14289 ) ;
#38005=LINE ( 'NONE', #10118, #14628 ) ;
#38007=ORIENTED_EDGE ( 'NONE', *, *, #12286, .F. ) ;
#38010=FACE_OUTER_BOUND ( 'NONE', #7221, .T. ) ;
#38011=ADVANCED_FACE ( 'NONE', ( #15653 ), #8675, .F. ) ;
#38012=VERTEX_POINT ( 'NONE', #4288 ) ;
#38013=ORIENTED_EDGE ( 'NONE', *, *, #20606, .T. ) ;
#38014=CIRCLE ( 'NONE', #33079, 2.106299212598425008 ) ;
#38016=CARTESIAN_POINT ( 'NONE',  ( -1.166969139818015755, 3.267716535433071279, 4.048737525165544676E-16 ) ) ;
#38017=ADVANCED_FACE ( 'NONE', ( #20551 ), #12546, .F. ) ;
#38020=ORIENTED_EDGE ( 'NONE', *, *, #16110, .T. ) ;
#38021=ORIENTED_EDGE ( 'NONE', *, *, #45175, .F. ) ;
#38023=DIRECTION ( 'NONE',  ( -1.000000000000000000, -0.000000000000000000, -0.000000000000000000 ) ) ;
#38025=CARTESIAN_POINT ( 'NONE',  ( -1.195183497228115035E-16, 0.000000000000000000, -1.574803149606293529 ) ) ;
#38027=DIRECTION ( 'NONE',  ( -1.000000000000000000, 0.000000000000000000, -0.000000000000000000 ) ) ;
#38029=DIRECTION ( 'NONE',  ( -3.469446951953613696E-16, 0.000000000000000000, -1.000000000000000000 ) ) ;
#38030=CARTESIAN_POINT ( 'NONE',  ( 1.091055626815042645, 3.267716535433071279, -1.892679809432644882E-16 ) ) ;
#38031=ORIENTED_EDGE ( 'NONE', *, *, #36928, .F. ) ;
#38032=DIRECTION ( 'NONE',  ( -0.000000000000000000, 1.000000000000000000, -0.000000000000000000 ) ) ;
#38034=EDGE_CURVE ( 'NONE', #7688, #46917, #2208, .T. ) ;
#38035=DIRECTION ( 'NONE',  ( 1.000000000000000000, 0.000000000000000000, 0.000000000000000000 ) ) ;
#38037=VECTOR ( 'NONE', #22715, 39.37007874015748143 ) ;
#38038=EDGE_LOOP ( 'NONE', ( #6606, #48242, #12639, #8941 ) ) ;
#38040=CIRCLE ( 'NONE', #17433, 2.165354330708661568 ) ;
#38042=DIRECTION ( 'NONE',  ( -0.000000000000000000, 0.000000000000000000, 1.000000000000000000 ) ) ;
#38043=ORIENTED_EDGE ( 'NONE', *, *, #39094, .T. ) ;
#38044=CARTESIAN_POINT ( 'NONE',  ( 4.268512490100411402E-16, 0.000000000000000000, 2.204724409448808764 ) ) ;
#38045=ORIENTED_EDGE ( 'NONE', *, *, #1260, .T. ) ;
#38047=VECTOR ( 'NONE', #47589, 39.37007874015748143 ) ;
#38048=ORIENTED_EDGE ( 'NONE', *, *, #9241, .F. ) ;
#38049=LINE ( 'NONE', #46259, #41889 ) ;
#38050=EDGE_CURVE ( 'NONE', #46240, #45206, #24934, .T. ) ;
#38051=VECTOR ( 'NONE', #14342, 39.37007874015748143 ) ;
#38053=LINE ( 'NONE', #18923, #27192 ) ;
#38054=CARTESIAN_POINT ( 'NONE',  ( 2.106197740627112402, 3.346456692913386100, 0.02067487291359298637 ) ) ;
#38057=ORIENTED_EDGE ( 'NONE', *, *, #43113, .T. ) ;
#38058=ORIENTED_EDGE ( 'NONE', *, *, #27332, .F. ) ;
#38059=CARTESIAN_POINT ( 'NONE',  ( -0.3486774197067334380, 0.000000000000000000, 1.259842519685033357 ) ) ;
#38060=DIRECTION ( 'NONE',  ( 1.734723475976806848E-16, -0.000000000000000000, 1.000000000000000000 ) ) ;
#38062=FACE_OUTER_BOUND ( 'NONE', #14761, .T. ) ;
#38063=LINE ( 'NONE', #3185, #19479 ) ;
#38064=CARTESIAN_POINT ( 'NONE',  ( 0.2727639067037604947, 3.346456692913386100, -0.1574803149606298636 ) ) ;
#38065=VERTEX_POINT ( 'NONE', #25439 ) ;
#38066=ORIENTED_EDGE ( 'NONE', *, *, #50776, .T. ) ;
#38069=LINE ( 'NONE', #6572, #38754 ) ;
#38072=FACE_BOUND ( 'NONE', #34421, .T. ) ;
#38073=ORIENTED_EDGE ( 'NONE', *, *, #35845, .F. ) ;
#38074=CARTESIAN_POINT ( 'NONE',  ( -1.166969139818015977, 3.346456692913386100, -0.4724409448818886470 ) ) ;
#38076=VERTEX_POINT ( 'NONE', #14079 ) ;
#38077=LINE ( 'NONE', #37321, #41094 ) ;
#38078=LINE ( 'NONE', #5555, #34128 ) ;
#38080=LINE ( 'NONE', #2956, #30514 ) ;
#38081=VECTOR ( 'NONE', #25171, 39.37007874015748143 ) ;
#38082=EDGE_CURVE ( 'NONE', #30055, #24780, #5311, .T. ) ;
#38083=CARTESIAN_POINT ( 'NONE',  ( -0.2727639067037607723, 0.000000000000000000, 2.362204724409437961 ) ) ;
#38084=CARTESIAN_POINT ( 'NONE',  ( 2.182111253630085290, 3.267716535433071279, -0.1968503937007886062 ) ) ;
#38085=VERTEX_POINT ( 'NONE', #29052 ) ;
#38089=LINE ( 'NONE', #15091, #50781 ) ;
#38090=ADVANCED_FACE ( 'NONE', ( #20806 ), #49150, .F. ) ;
#38092=CIRCLE ( 'NONE', #22418, 2.106299212598425008 ) ;
#38093=ADVANCED_FACE ( 'NONE', ( #24684 ), #40440, .F. ) ;
#38095=CARTESIAN_POINT ( 'NONE',  ( 1.636583440222563857, 0.000000000000000000, 0.3149606299212576177 ) ) ;
#38096=DIRECTION ( 'NONE',  ( 1.000000000000000000, 0.000000000000000000, -3.469446951953613696E-16 ) ) ;
#38098=ORIENTED_EDGE ( 'NONE', *, *, #38050, .F. ) ;
#38100=ADVANCED_FACE ( 'NONE', ( #32701 ), #5312, .F. ) ;
#38101=CARTESIAN_POINT ( 'NONE',  ( 1.833433833923350909, 3.267716535433071279, -6.361001426713997494E-16 ) ) ;
#38102=EDGE_LOOP ( 'NONE', ( #5386, #31813, #30386, #28317, #9629 ) ) ;
#38104=DIRECTION ( 'NONE',  ( 1.000000000000000000, 0.000000000000000000, 0.000000000000000000 ) ) ;
#38105=ORIENTED_EDGE ( 'NONE', *, *, #6286, .T. ) ;
#38106=LINE ( 'NONE', #9714, #28791 ) ;
#38109=ORIENTED_EDGE ( 'NONE', *, *, #19589, .F. ) ;
#38110=CARTESIAN_POINT ( 'NONE',  ( 0.000000000000000000, 3.267716535433071279, 0.9055118110236167750 ) ) ;
#38111=ORIENTED_EDGE ( 'NONE', *, *, #24171, .T. ) ;
#38112=DIRECTION ( 'NONE',  ( 0.000000000000000000, 0.000000000000000000, 1.000000000000000000 ) ) ;
#38115=AXIS2_PLACEMENT_3D ( 'NONE', #43684, #12981, #32873 ) ;
#38116=LINE ( 'NONE', #27227, #12800 ) ;
#38117=DIRECTION ( 'NONE',  ( -0.000000000000000000, 1.000000000000000000, -0.000000000000000000 ) ) ;
#38118=ADVANCED_FACE ( 'NONE', ( #13071 ), #21575, .F. ) ;
#38120=ORIENTED_EDGE ( 'NONE', *, *, #30715, .T. ) ;
#38122=CARTESIAN_POINT ( 'NONE',  ( -1.363819533518803473, 3.346456692913386100, -1.299212598425192544 ) ) ;
#38123=EDGE_CURVE ( 'NONE', #40287, #51008, #45292, .T. ) ;
#38124=CARTESIAN_POINT ( 'NONE',  ( -0.5455278134075214336, 3.346456692913386100, -1.889763779527552146 ) ) ;
#38125=AXIS2_PLACEMENT_3D ( 'NONE', #24920, #12529, #40671 ) ;
#38127=DIRECTION ( 'NONE',  ( -0.000000000000000000, 1.000000000000000000, -0.000000000000000000 ) ) ;
#38128=CARTESIAN_POINT ( 'NONE',  ( -1.536664496436148184E-16, 3.346456692913386100, -1.771653543307081025 ) ) ;
#38131=ORIENTED_EDGE ( 'NONE', *, *, #49982, .F. ) ;
#38132=CARTESIAN_POINT ( 'NONE',  ( 1.015142113812069313, 3.346456692913386100, 0.5905511811023579360 ) ) ;
#38133=EDGE_CURVE ( 'NONE', #21081, #33042, #17195, .T. ) ;
#38136=DIRECTION ( 'NONE',  ( -1.000000000000000000, 0.000000000000000000, 0.000000000000000000 ) ) ;
#38137=VERTEX_POINT ( 'NONE', #1694 ) ;
#38138=ORIENTED_EDGE ( 'NONE', *, *, #10169, .T. ) ;
#38139=ORIENTED_EDGE ( 'NONE', *, *, #3937, .F. ) ;
#38142=ORIENTED_EDGE ( 'NONE', *, *, #47684, .F. ) ;
#38144=DIRECTION ( 'NONE',  ( 1.000000000000000000, 0.000000000000000000, 0.000000000000000000 ) ) ;
#38145=VECTOR ( 'NONE', #20396, 39.37007874015748143 ) ;
#38146=ADVANCED_FACE ( 'NONE', ( #48887 ), #29315, .F. ) ;
#38151=CARTESIAN_POINT ( 'NONE',  ( -1.439733046521776361, 3.346456692913386100, -0.1968503937007879123 ) ) ;
#38152=CARTESIAN_POINT ( 'NONE',  ( -0.8182917201112819283, 3.346456692913386100, -1.614173228346451605 ) ) ;
#38153=EDGE_LOOP ( 'NONE', ( #26373, #45174, #38680, #26060 ) ) ;
#38155=FACE_OUTER_BOUND ( 'NONE', #49015, .T. ) ;
#38156=VECTOR ( 'NONE', #11700, 39.37007874015748143 ) ;
#38157=LINE ( 'NONE', #33530, #22696 ) ;
#38158=CARTESIAN_POINT ( 'NONE',  ( 1.091055626815042645, 3.267716535433071279, 0.7480314960629872445 ) ) ;
#38159=VECTOR ( 'NONE', #33396, 39.37007874015748143 ) ;
#38160=AXIS2_PLACEMENT_3D ( 'NONE', #17069, #5700, #8540 ) ;
#38162=DIRECTION ( 'NONE',  ( -0.000000000000000000, 1.000000000000000000, -0.000000000000000000 ) ) ;
#38163=DIRECTION ( 'NONE',  ( -1.000000000000000000, 0.000000000000000000, -0.000000000000000000 ) ) ;
#38166=CARTESIAN_POINT ( 'NONE',  ( 1.363819533518803029, 0.000000000000000000, -1.102362204724405714 ) ) ;
#38168=VERTEX_POINT ( 'NONE', #41955 ) ;
#38171=ORIENTED_EDGE ( 'NONE', *, *, #14123, .T. ) ;
#38173=DIRECTION ( 'NONE',  ( -0.000000000000000000, 0.000000000000000000, 1.000000000000000000 ) ) ;
#38176=CARTESIAN_POINT ( 'NONE',  ( 0.000000000000000000, 3.267716535433071279, 1.535433070866133898 ) ) ;
#38178=ORIENTED_EDGE ( 'NONE', *, *, #44992, .F. ) ;
#38180=DIRECTION ( 'NONE',  ( -1.000000000000000000, -0.000000000000000000, -0.000000000000000000 ) ) ;
#38181=ORIENTED_EDGE ( 'NONE', *, *, #26826, .F. ) ;
#38182=ORIENTED_EDGE ( 'NONE', *, *, #34551, .T. ) ;
#38184=ADVANCED_FACE ( 'NONE', ( #2968 ), #18208, .F. ) ;
#38185=VERTEX_POINT ( 'NONE', #34467 ) ;
#38186=LINE ( 'NONE', #37930, #4864 ) ;
#38187=CARTESIAN_POINT ( 'NONE',  ( -0.6214413264104945434, 3.346456692913386100, -0.3543307086614175816 ) ) ;
#38188=EDGE_CURVE ( 'NONE', #1872, #33170, #43130, .T. ) ;
#38189=ORIENTED_EDGE ( 'NONE', *, *, #30694, .T. ) ;
#38190=DIRECTION ( 'NONE',  ( -0.000000000000000000, 1.000000000000000000, -0.000000000000000000 ) ) ;
#38191=CARTESIAN_POINT ( 'NONE',  ( -1.166969139818015533, 3.267716535433071279, 1.417322834645662777 ) ) ;
#38193=FACE_OUTER_BOUND ( 'NONE', #42540, .T. ) ;
#38195=ORIENTED_EDGE ( 'NONE', *, *, #18524, .T. ) ;
#38196=LINE ( 'NONE', #49751, #18278 ) ;
#38197=FACE_BOUND ( 'NONE', #6275, .T. ) ;
#38198=ORIENTED_EDGE ( 'NONE', *, *, #20952, .F. ) ;
#38199=VECTOR ( 'NONE', #38516, 39.37007874015748143 ) ;
#38201=CARTESIAN_POINT ( 'NONE',  ( 0.000000000000000000, 3.267716535433071279, -1.456692913385822186 ) ) ;
#38202=PLANE ( 'NONE',  #46465 ) ;
#38203=ORIENTED_EDGE ( 'NONE', *, *, #21722, .F. ) ;
#38204=ORIENTED_EDGE ( 'NONE', *, *, #7689, .F. ) ;
#38205=CARTESIAN_POINT ( 'NONE',  ( 1.560669927219590747, 3.346456692913386100, -0.1574803149606304187 ) ) ;
#38209=VERTEX_POINT ( 'NONE', #27383 ) ;
#38210=ORIENTED_EDGE ( 'NONE', *, *, #3808, .T. ) ;
#38211=CARTESIAN_POINT ( 'NONE',  ( 1.015142113812069091, 3.346456692913386100, -1.912654141836395816 ) ) ;
#38212=CARTESIAN_POINT ( 'NONE',  ( 0.000000000000000000, 2.362204724409439294, 0.000000000000000000 ) ) ;
#38214=ORIENTED_EDGE ( 'NONE', *, *, #39673, .F. ) ;
#38216=EDGE_CURVE ( 'NONE', #21605, #2219, #6339, .T. ) ;
#38217=DIRECTION ( 'NONE',  ( -1.000000000000000000, 0.000000000000000000, -0.000000000000000000 ) ) ;
#38218=EDGE_CURVE ( 'NONE', #46986, #18782, #35408, .T. ) ;
#38219=LINE ( 'NONE', #41571, #44763 ) ;
#38221=ADVANCED_FACE ( 'NONE', ( #14842 ), #37846, .F. ) ;
#38222=CARTESIAN_POINT ( 'NONE',  ( -0.3486774197067334935, 3.267716535433071279, 0.7480314960629874665 ) ) ;
#38226=VERTEX_POINT ( 'NONE', #33966 ) ;
#38227=LINE ( 'NONE', #30474, #4465 ) ;
#38228=DIRECTION ( 'NONE',  ( -3.469446951953613696E-16, 0.000000000000000000, -1.000000000000000000 ) ) ;
#38230=ORIENTED_EDGE ( 'NONE', *, *, #12257, .T. ) ;
#38231=VECTOR ( 'NONE', #35844, 39.37007874015748143 ) ;
#38232=ORIENTED_EDGE ( 'NONE', *, *, #44766, .T. ) ;
#38237=ORIENTED_EDGE ( 'NONE', *, *, #13864, .T. ) ;
#38238=AXIS2_PLACEMENT_3D ( 'NONE', #870, #39345, #11978 ) ;
#38239=EDGE_CURVE ( 'NONE', #37842, #35391, #3912, .T. ) ;
#38241=CARTESIAN_POINT ( 'NONE',  ( -0.2727639067037610499, 0.000000000000000000, -2.047244094488181343 ) ) ;
#38243=CARTESIAN_POINT ( 'NONE',  ( 0.8455406139730251569, 3.267716535433071279, -1.929133858267711110 ) ) ;
#38245=EDGE_LOOP ( 'NONE', ( #10618, #33251, #31143, #34751 ) ) ;
#38246=CARTESIAN_POINT ( 'NONE',  ( -1.863748091109392213, 3.346456692913386100, -1.102362204724405492 ) ) ;
#38248=VERTEX_POINT ( 'NONE', #23780 ) ;
#38249=DIRECTION ( 'NONE',  ( 0.000000000000000000, 0.000000000000000000, -1.000000000000000000 ) ) ;
#38250=FACE_OUTER_BOUND ( 'NONE', #28279, .T. ) ;
#38251=CARTESIAN_POINT ( 'NONE',  ( -1.195183497228115035E-16, 3.267716535433071279, -0.3149606299212591165 ) ) ;
#38253=ORIENTED_EDGE ( 'NONE', *, *, #26058, .F. ) ;
#38256=CARTESIAN_POINT ( 'NONE',  ( 4.268512490100411402E-16, 3.346456692913386100, 1.889763779527550369 ) ) ;
#38261=ORIENTED_EDGE ( 'NONE', *, *, #26699, .T. ) ;
#38263=ORIENTED_EDGE ( 'NONE', *, *, #17440, .T. ) ;
#38265=VECTOR ( 'NONE', #30285, 39.37007874015748143 ) ;
#38266=AXIS2_PLACEMENT_3D ( 'NONE', #50037, #45931, #10597 ) ;
#38270=ORIENTED_EDGE ( 'NONE', *, *, #38003, .T. ) ;
#38273=VECTOR ( 'NONE', #46739, 39.37007874015748143 ) ;
#38275=EDGE_CURVE ( 'NONE', #22076, #48087, #22338, .T. ) ;
#38276=PLANE ( 'NONE',  #16881 ) ;
#38278=ORIENTED_EDGE ( 'NONE', *, *, #10050, .F. ) ;
#38279=LINE ( 'NONE', #2392, #12602 ) ;
#38281=EDGE_CURVE ( 'NONE', #25746, #33365, #48256, .T. ) ;
#38282=ADVANCED_FACE ( 'NONE', ( #44159 ), #4417, .F. ) ;
#38283=EDGE_CURVE ( 'NONE', #41994, #23774, #12942, .T. ) ;
#38285=DIRECTION ( 'NONE',  ( -0.000000000000000000, 0.000000000000000000, 1.000000000000000000 ) ) ;
#38286=CARTESIAN_POINT ( 'NONE',  ( 0.8182917201112824834, 0.000000000000000000, 1.535433070866133898 ) ) ;
#38287=VERTEX_POINT ( 'NONE', #21196 ) ;
#38289=CARTESIAN_POINT ( 'NONE',  ( -0.4513972801127658641, 3.267716535433071279, -2.401574803149598036 ) ) ;
#38291=VERTEX_POINT ( 'NONE', #13195 ) ;
#38292=CARTESIAN_POINT ( 'NONE',  ( 0.4696143004045484348, 3.267716535433071279, 2.165354330708650910 ) ) ;
#38293=DIRECTION ( 'NONE',  ( -0.000000000000000000, 1.000000000000000000, -0.000000000000000000 ) ) ;
#38294=EDGE_CURVE ( 'NONE', #17089, #15497, #32052, .T. ) ;
#38295=CARTESIAN_POINT ( 'NONE',  ( 1.441853549388196321, 3.267716535433071279, 1.535433070866133898 ) ) ;
#38296=ORIENTED_EDGE ( 'NONE', *, *, #21790, .F. ) ;
#38297=PLANE ( 'NONE',  #29183 ) ;
#38298=VECTOR ( 'NONE', #28720, 39.37007874015748143 ) ;
#38299=VECTOR ( 'NONE', #41633, 39.37007874015748143 ) ;
#38300=EDGE_CURVE ( 'NONE', #48919, #50319, #20152, .T. ) ;
#38301=ORIENTED_EDGE ( 'NONE', *, *, #25701, .F. ) ;
#38302=AXIS2_PLACEMENT_3D ( 'NONE', #4573, #28309, #8953 ) ;
#38303=FACE_OUTER_BOUND ( 'NONE', #48270, .T. ) ;
#38304=EDGE_LOOP ( 'NONE', ( #34234, #10647, #31649, #4649 ) ) ;
#38306=VECTOR ( 'NONE', #952, 39.37007874015748143 ) ;
#38307=VECTOR ( 'NONE', #11097, 39.37007874015748143 ) ;
#38308=FACE_OUTER_BOUND ( 'NONE', #2632, .T. ) ;
#38309=DIRECTION ( 'NONE',  ( 1.000000000000000000, 0.000000000000000000, 0.000000000000000000 ) ) ;
#38310=DIRECTION ( 'NONE',  ( 1.734723475976806848E-16, 0.000000000000000000, 1.000000000000000000 ) ) ;
#38311=EDGE_CURVE ( 'NONE', #30476, #3517, #9059, .T. ) ;
#38313=ORIENTED_EDGE ( 'NONE', *, *, #50952, .F. ) ;
#38316=ORIENTED_EDGE ( 'NONE', *, *, #37671, .F. ) ;
#38317=CARTESIAN_POINT ( 'NONE',  ( 0.5455278134075214336, 3.267716535433071279, -9.463399047163225645E-17 ) ) ;
#38318=CARTESIAN_POINT ( 'NONE',  ( -0.3486774197067339376, 3.267716535433071279, -0.6299212598425175669 ) ) ;
#38320=ORIENTED_EDGE ( 'NONE', *, *, #40646, .T. ) ;
#38321=ORIENTED_EDGE ( 'NONE', *, *, #34516, .T. ) ;
#38323=PLANE ( 'NONE',  #46396 ) ;
#38326=CARTESIAN_POINT ( 'NONE',  ( -0.6214413264104945434, 3.267716535433071279, 2.012537465693970962 ) ) ;
#38327=CARTESIAN_POINT ( 'NONE',  ( -1.439733046521776139, 0.000000000000000000, -4.780733988912460139E-16 ) ) ;
#38331=VERTEX_POINT ( 'NONE', #48511 ) ;
#38332=CARTESIAN_POINT ( 'NONE',  ( -1.536664496436148184E-16, 0.000000000000000000, -1.456692913385822630 ) ) ;
#38334=CARTESIAN_POINT ( 'NONE',  ( 4.268512490100411402E-16, 3.346456692913386100, 2.204724409448808764 ) ) ;
#38336=FACE_OUTER_BOUND ( 'NONE', #18741, .T. ) ;
#38340=LINE ( 'NONE', #3212, #47485 ) ;
#38342=ADVANCED_FACE ( 'NONE', ( #8545 ), #20935, .F. ) ;
#38347=FACE_OUTER_BOUND ( 'NONE', #25217, .T. ) ;
#38349=DIRECTION ( 'NONE',  ( -0.000000000000000000, 1.000000000000000000, -0.000000000000000000 ) ) ;
#38350=CARTESIAN_POINT ( 'NONE',  ( -1.166969139818015533, 3.346456692913386100, 0.7874015748031456541 ) ) ;
#38351=ORIENTED_EDGE ( 'NONE', *, *, #25040, .F. ) ;
#38352=FACE_OUTER_BOUND ( 'NONE', #14877, .T. ) ;
#38353=CARTESIAN_POINT ( 'NONE',  ( -1.091055626815042645, 3.346456692913386100, -1.456692913385822186 ) ) ;
#38354=ORIENTED_EDGE ( 'NONE', *, *, #2507, .F. ) ;
#38356=CARTESIAN_POINT ( 'NONE',  ( 1.560669927219590303, 3.267716535433071279, -5.414661521997676285E-16 ) ) ;
#38357=FACE_OUTER_BOUND ( 'NONE', #39478, .T. ) ;
#38358=VERTEX_POINT ( 'NONE', #44662 ) ;
#38361=PLANE ( 'NONE',  #18794 ) ;
#38362=CARTESIAN_POINT ( 'NONE',  ( 1.287906020515830141, 3.267716535433071279, 1.259842519685033357 ) ) ;
#38363=DIRECTION ( 'NONE',  ( -1.000000000000000000, 0.000000000000000000, 1.734723475976806848E-16 ) ) ;
#38364=ADVANCED_FACE ( 'NONE', ( #40558 ), #32307, .F. ) ;
#38365=ORIENTED_EDGE ( 'NONE', *, *, #50857, .T. ) ;
#38367=PLANE ( 'NONE',  #8360 ) ;
#38368=VECTOR ( 'NONE', #11028, 39.37007874015748143 ) ;
#38370=VECTOR ( 'NONE', #37175, 39.37007874015748143 ) ;
#38371=CARTESIAN_POINT ( 'NONE',  ( 1.636583440222563857, 3.346456692913386100, 0.7480314960629872445 ) ) ;
#38374=VECTOR ( 'NONE', #38491, 39.37007874015748143 ) ;
#38375=CARTESIAN_POINT ( 'NONE',  ( 0.000000000000000000, 3.346456692913386100, 0.000000000000000000 ) ) ;
#38376=ORIENTED_EDGE ( 'NONE', *, *, #5741, .T. ) ;
#38379=ADVANCED_FACE ( 'NONE', ( #12674 ), #39782, .F. ) ;
#38380=LINE ( 'NONE', #30625, #12440 ) ;
#38381=VECTOR ( 'NONE', #25976, 39.37007874015748143 ) ;
#38383=EDGE_CURVE ( 'NONE', #39867, #20338, #36430, .T. ) ;
#38385=VERTEX_POINT ( 'NONE', #40305 ) ;
#38387=EDGE_CURVE ( 'NONE', #42728, #40166, #1051, .T. ) ;
#38388=ORIENTED_EDGE ( 'NONE', *, *, #14073, .F. ) ;
#38390=CARTESIAN_POINT ( 'NONE',  ( 1.909347346926324684, 3.346456692913386100, -0.03937007874015936021 ) ) ;
#38395=EDGE_CURVE ( 'NONE', #31182, #40680, #31424, .T. ) ;
#38398=VECTOR ( 'NONE', #20615, 39.37007874015748143 ) ;
#38400=ORIENTED_EDGE ( 'NONE', *, *, #39152, .F. ) ;
#38402=LINE ( 'NONE', #40113, #33298 ) ;
#38403=VECTOR ( 'NONE', #11332, 39.37007874015748143 ) ;
#38404=DIRECTION ( 'NONE',  ( -0.000000000000000000, 1.000000000000000000, -0.000000000000000000 ) ) ;
#38406=ORIENTED_EDGE ( 'NONE', *, *, #11063, .F. ) ;
#38407=LINE ( 'NONE', #50218, #19050 ) ;
#38409=VERTEX_POINT ( 'NONE', #25313 ) ;
#38410=DIRECTION ( 'NONE',  ( 1.734723475976806848E-16, -0.000000000000000000, 1.000000000000000000 ) ) ;
#38412=DIRECTION ( 'NONE',  ( 0.000000000000000000, 0.000000000000000000, -1.000000000000000000 ) ) ;
#38413=EDGE_CURVE ( 'NONE', #38226, #49191, #21449, .T. ) ;
#38414=VECTOR ( 'NONE', #41535, 39.37007874015748143 ) ;
#38415=EDGE_LOOP ( 'NONE', ( #39548, #12703, #4949, #46555 ) ) ;
#38416=CARTESIAN_POINT ( 'NONE',  ( 1.636583440222563857, 3.346456692913386100, 1.574803149606291974 ) ) ;
#38419=CARTESIAN_POINT ( 'NONE',  ( -0.3486774197067339376, 3.267716535433071279, -1.889763779527552146 ) ) ;
#38420=CARTESIAN_POINT ( 'NONE',  ( -1.712496953225537188, 3.267716535433071279, -0.3543307086614171930 ) ) ;
#38421=CARTESIAN_POINT ( 'NONE',  ( 1.363819533518803029, 3.267716535433071279, -1.299212598425193210 ) ) ;
#38422=DIRECTION ( 'NONE',  ( -1.000000000000000000, 0.000000000000000000, 0.000000000000000000 ) ) ;
#38423=ORIENTED_EDGE ( 'NONE', *, *, #49477, .F. ) ;
#38426=ORIENTED_EDGE ( 'NONE', *, *, #33461, .T. ) ;
#38427=ORIENTED_EDGE ( 'NONE', *, *, #42352, .T. ) ;
#38429=ORIENTED_EDGE ( 'NONE', *, *, #12503, .T. ) ;
#38430=CARTESIAN_POINT ( 'NONE',  ( -1.166969139818015977, 0.000000000000000000, -0.7874015748031470974 ) ) ;
#38432=ORIENTED_EDGE ( 'NONE', *, *, #1243, .F. ) ;
#38433=EDGE_CURVE ( 'NONE', #23949, #11818, #37205, .T. ) ;
#38434=CARTESIAN_POINT ( 'NONE',  ( 0.000000000000000000, 3.267716535433071279, 0.1574803149606287811 ) ) ;
#38436=DIRECTION ( 'NONE',  ( -0.000000000000000000, 0.000000000000000000, 1.000000000000000000 ) ) ;
#38437=EDGE_CURVE ( 'NONE', #42646, #10879, #45297, .T. ) ;
#38438=AXIS2_PLACEMENT_3D ( 'NONE', #50832, #35412, #31286 ) ;
#38440=PLANE ( 'NONE',  #42827 ) ;
#38442=ORIENTED_EDGE ( 'NONE', *, *, #46054, .F. ) ;
#38446=FACE_BOUND ( 'NONE', #44564, .T. ) ;
#38447=ORIENTED_EDGE ( 'NONE', *, *, #18521, .T. ) ;
#38448=AXIS2_PLACEMENT_3D ( 'NONE', #37234, #40592, #45447 ) ;
#38449=DIRECTION ( 'NONE',  ( -0.000000000000000000, 1.000000000000000000, -0.000000000000000000 ) ) ;
#38450=VECTOR ( 'NONE', #3196, 39.37007874015748143 ) ;
#38451=ORIENTED_EDGE ( 'NONE', *, *, #37328, .T. ) ;
#38453=FACE_OUTER_BOUND ( 'NONE', #24234, .T. ) ;
#38454=VECTOR ( 'NONE', #35565, 39.37007874015748143 ) ;
#38455=CARTESIAN_POINT ( 'NONE',  ( -2.449433152083427156, 3.244423651327855485, -0.1574803149606298636 ) ) ;
#38458=PLANE ( 'NONE',  #14709 ) ;
#38459=VERTEX_POINT ( 'NONE', #38222 ) ;
#38460=DIRECTION ( 'NONE',  ( -3.469446951953613696E-16, 0.000000000000000000, -1.000000000000000000 ) ) ;
#38461=CARTESIAN_POINT ( 'NONE',  ( -0.8182917201112819283, 0.000000000000000000, -1.102362204724405492 ) ) ;
#38462=ADVANCED_FACE ( 'NONE', ( #18336 ), #41328, .F. ) ;
#38465=ORIENTED_EDGE ( 'NONE', *, *, #7527, .F. ) ;
#38467=DIRECTION ( 'NONE',  ( -3.469446951953613696E-16, 0.000000000000000000, -1.000000000000000000 ) ) ;
#38469=EDGE_CURVE ( 'NONE', #29102, #15326, #49281, .T. ) ;
#38470=LINE ( 'NONE', #51025, #17585 ) ;
#38471=DIRECTION ( 'NONE',  ( 1.000000000000000000, 0.000000000000000000, 0.000000000000000000 ) ) ;
#38474=VECTOR ( 'NONE', #10528, 39.37007874015748143 ) ;
#38476=EDGE_LOOP ( 'NONE', ( #39706, #46597, #35213, #42103 ) ) ;
#38477=VECTOR ( 'NONE', #45934, 39.37007874015748143 ) ;
#38478=DIRECTION ( 'NONE',  ( -3.469446951953613696E-16, 0.000000000000000000, -1.000000000000000000 ) ) ;
#38479=LINE ( 'NONE', #46185, #23603 ) ;
#38484=DIRECTION ( 'NONE',  ( -0.000000000000000000, 1.000000000000000000, -0.000000000000000000 ) ) ;
#38487=VECTOR ( 'NONE', #9928, 39.37007874015748143 ) ;
#38488=EDGE_LOOP ( 'NONE', ( #17138, #40426, #6710, #32746, #26247 ) ) ;
#38490=ORIENTED_EDGE ( 'NONE', *, *, #531, .T. ) ;
#38491=DIRECTION ( 'NONE',  ( 1.734723475976806848E-16, -0.000000000000000000, 1.000000000000000000 ) ) ;
#38492=DIRECTION ( 'NONE',  ( 1.734723475976806848E-16, 0.000000000000000000, 1.000000000000000000 ) ) ;
#38495=EDGE_CURVE ( 'NONE', #552, #2219, #45671, .T. ) ;
#38496=CARTESIAN_POINT ( 'NONE',  ( 1.091055626815042645, 3.346456692913386100, 1.062992125984246083 ) ) ;
#38498=ORIENTED_EDGE ( 'NONE', *, *, #19963, .T. ) ;
#38502=LINE ( 'NONE', #50305, #24017 ) ;
#38505=ORIENTED_EDGE ( 'NONE', *, *, #46841, .T. ) ;
#38506=FACE_OUTER_BOUND ( 'NONE', #39745, .T. ) ;
#38507=CARTESIAN_POINT ( 'NONE',  ( 0.8182917201112824834, 3.346456692913386100, 1.850393700787392293 ) ) ;
#38508=DIRECTION ( 'NONE',  ( 1.734723475976806848E-16, -0.000000000000000000, 1.000000000000000000 ) ) ;
#38509=AXIS2_PLACEMENT_3D ( 'NONE', #50911, #30600, #23597 ) ;
#38510=ORIENTED_EDGE ( 'NONE', *, *, #26626, .F. ) ;
#38513=ORIENTED_EDGE ( 'NONE', *, *, #50160, .T. ) ;
#38514=EDGE_CURVE ( 'NONE', #26233, #7688, #22217, .T. ) ;
#38516=DIRECTION ( 'NONE',  ( -0.000000000000000000, 1.000000000000000000, -0.000000000000000000 ) ) ;
#38517=ADVANCED_FACE ( 'NONE', ( #34594 ), #3341, .F. ) ;
#38518=VECTOR ( 'NONE', #33638, 39.37007874015748143 ) ;
#38520=DIRECTION ( 'NONE',  ( 1.734723475976806848E-16, 0.000000000000000000, 1.000000000000000000 ) ) ;
#38521=ORIENTED_EDGE ( 'NONE', *, *, #35178, .F. ) ;
#38523=PLANE ( 'NONE',  #9811 ) ;
#38525=LINE ( 'NONE', #46233, #6154 ) ;
#38526=ORIENTED_EDGE ( 'NONE', *, *, #3239, .F. ) ;
#38529=CARTESIAN_POINT ( 'NONE',  ( -0.3486774197067334380, 3.346456692913386100, 0.6299212598425164567 ) ) ;
#38530=DIRECTION ( 'NONE',  ( 1.734723475976806848E-16, 0.000000000000000000, 1.000000000000000000 ) ) ;
#38531=CARTESIAN_POINT ( 'NONE',  ( -0.6214413264104939882, 3.346456692913386100, 0.5905511811023582691 ) ) ;
#38532=ORIENTED_EDGE ( 'NONE', *, *, #10267, .F. ) ;
#38533=LINE ( 'NONE', #30779, #285 ) ;
#38534=CARTESIAN_POINT ( 'NONE',  ( 0.7423782071083087075, 0.000000000000000000, -6.146657985744592735E-16 ) ) ;
#38537=ORIENTED_EDGE ( 'NONE', *, *, #7384, .T. ) ;
#38539=LINE ( 'NONE', #46496, #13820 ) ;
#38540=DIRECTION ( 'NONE',  ( 1.000000000000000000, 0.000000000000000000, -3.469446951953613696E-16 ) ) ;
#38541=VECTOR ( 'NONE', #47277, 39.37007874015748143 ) ;
#38542=ORIENTED_EDGE ( 'NONE', *, *, #39947, .T. ) ;
#38543=AXIS2_PLACEMENT_3D ( 'NONE', #1063, #16824, #48012 ) ;
#38544=LINE ( 'NONE', #18411, #38265 ) ;
#38546=CARTESIAN_POINT ( 'NONE',  ( 0.000000000000000000, 3.267716535433071279, 1.220472440944875281 ) ) ;
#38548=DIRECTION ( 'NONE',  ( 1.734723475976806848E-16, -0.000000000000000000, 1.000000000000000000 ) ) ;
#38549=ORIENTED_EDGE ( 'NONE', *, *, #22592, .F. ) ;
#38551=DIRECTION ( 'NONE',  ( 0.000000000000000000, 0.000000000000000000, -1.000000000000000000 ) ) ;
#38552=CARTESIAN_POINT ( 'NONE',  ( -1.636583440222563635, 0.000000000000000000, 1.062992125984246083 ) ) ;
#38553=ORIENTED_EDGE ( 'NONE', *, *, #14482, .F. ) ;
#38557=CARTESIAN_POINT ( 'NONE',  ( -1.091055626815042645, 3.232777166330607521, 2.204724409448808764 ) ) ;
#38558=CARTESIAN_POINT ( 'NONE',  ( -0.6214413264104945434, 3.346456692913386100, -1.732283464566922726 ) ) ;
#38560=EDGE_LOOP ( 'NONE', ( #21681, #39395, #7364, #4736 ) ) ;
#38562=LINE ( 'NONE', #46274, #19356 ) ;
#38565=EDGE_CURVE ( 'NONE', #16345, #26927, #50772, .T. ) ;
#38566=ORIENTED_EDGE ( 'NONE', *, *, #25284, .T. ) ;
#38567=ORIENTED_EDGE ( 'NONE', *, *, #5701, .F. ) ;
#38569=CARTESIAN_POINT ( 'NONE',  ( -0.3486774197067334380, 3.346456692913386100, 1.889763779527550369 ) ) ;
#38570=FACE_OUTER_BOUND ( 'NONE', #36122, .T. ) ;
#38572=ORIENTED_EDGE ( 'NONE', *, *, #22832, .F. ) ;
#38573=DIRECTION ( 'NONE',  ( 1.000000000000000000, 0.000000000000000000, 0.000000000000000000 ) ) ;
#38574=LINE ( 'NONE', #31326, #38450 ) ;
#38575=VERTEX_POINT ( 'NONE', #22966 ) ;
#38578=ORIENTED_EDGE ( 'NONE', *, *, #3603, .F. ) ;
#38579=PLANE ( 'NONE',  #18016 ) ;
#38581=LINE ( 'NONE', #16990, #27216 ) ;
#38586=DIRECTION ( 'NONE',  ( 1.734723475976806848E-16, 0.000000000000000000, 1.000000000000000000 ) ) ;
#38588=EDGE_CURVE ( 'NONE', #39237, #27835, #43330, .T. ) ;
#38590=ORIENTED_EDGE ( 'NONE', *, *, #9830, .F. ) ;
#38592=CARTESIAN_POINT ( 'NONE',  ( -1.985260859929297572, 0.000000000000000000, 0.3149606299212578953 ) ) ;
#38594=DIRECTION ( 'NONE',  ( -1.000000000000000000, -0.000000000000000000, -0.000000000000000000 ) ) ;
#38596=ORIENTED_EDGE ( 'NONE', *, *, #10650, .T. ) ;
#38598=AXIS2_PLACEMENT_3D ( 'NONE', #38286, #10899, #14780 ) ;
#38599=EDGE_CURVE ( 'NONE', #44295, #13419, #34840, .T. ) ;
#38600=DIRECTION ( 'NONE',  ( -3.469446951953613696E-16, 0.000000000000000000, -1.000000000000000000 ) ) ;
#38601=ORIENTED_EDGE ( 'NONE', *, *, #7890, .T. ) ;
#38603=DIRECTION ( 'NONE',  ( -3.469446951953613696E-16, 0.000000000000000000, -1.000000000000000000 ) ) ;
#38604=DIRECTION ( 'NONE',  ( -0.000000000000000000, 1.000000000000000000, -0.000000000000000000 ) ) ;
#38605=PLANE ( 'NONE',  #3651 ) ;
#38606=PLANE ( 'NONE',  #1096 ) ;
#38607=DIRECTION ( 'NONE',  ( 1.000000000000000000, 0.000000000000000000, -3.469446951953613696E-16 ) ) ;
#38609=DIRECTION ( 'NONE',  ( 1.734723475976806848E-16, -0.000000000000000000, 1.000000000000000000 ) ) ;
#38610=EDGE_LOOP ( 'NONE', ( #33128, #47278, #10550, #28343 ) ) ;
#38611=FACE_BOUND ( 'NONE', #44555, .T. ) ;
#38612=DIRECTION ( 'NONE',  ( -0.000000000000000000, 1.000000000000000000, -0.000000000000000000 ) ) ;
#38613=LINE ( 'NONE', #15370, #14458 ) ;
#38614=VECTOR ( 'NONE', #10549, 39.37007874015748143 ) ;
#38618=CARTESIAN_POINT ( 'NONE',  ( 1.015142113812069091, 3.346456692913386100, -1.732283464566923614 ) ) ;
#38620=LINE ( 'NONE', #31124, #46434 ) ;
#38621=VECTOR ( 'NONE', #33948, 39.37007874015748143 ) ;
#38622=PLANE ( 'NONE',  #21119 ) ;
#38623=DIRECTION ( 'NONE',  ( 0.000000000000000000, 0.000000000000000000, -1.000000000000000000 ) ) ;
#38626=VECTOR ( 'NONE', #905, 39.37007874015748143 ) ;
#38627=AXIS2_PLACEMENT_3D ( 'NONE', #40063, #4432, #20170 ) ;
#38628=ORIENTED_EDGE ( 'NONE', *, *, #2967, .F. ) ;
#38629=EDGE_CURVE ( 'NONE', #11828, #35927, #50033, .T. ) ;
#38630=CARTESIAN_POINT ( 'NONE',  ( 1.091055626815042645, 0.000000000000000000, 0.9448818897637746295 ) ) ;
#38631=DIRECTION ( 'NONE',  ( -1.000000000000000000, -0.000000000000000000, -0.000000000000000000 ) ) ;
#38632=ADVANCED_FACE ( 'NONE', ( #11592 ), #31474, .F. ) ;
#38633=AXIS2_PLACEMENT_3D ( 'NONE', #48380, #5055, #47354 ) ;
#38634=LINE ( 'NONE', #42743, #45439 ) ;
#38635=VERTEX_POINT ( 'NONE', #18844 ) ;
#38637=VERTEX_POINT ( 'NONE', #15719 ) ;
#38638=ORIENTED_EDGE ( 'NONE', *, *, #17711, .F. ) ;
#38639=VECTOR ( 'NONE', #22655, 39.37007874015748143 ) ;
#38640=ADVANCED_FACE ( 'NONE', ( #7228 ), #31224, .F. ) ;
#38641=VERTEX_POINT ( 'NONE', #11345 ) ;
#38645=LINE ( 'NONE', #7150, #49303 ) ;
#38646=CARTESIAN_POINT ( 'NONE',  ( 1.670330979180827180, 3.346456692913386100, 1.377952755905504256 ) ) ;
#38647=VECTOR ( 'NONE', #29019, 39.37007874015748143 ) ;
#38648=EDGE_CURVE ( 'NONE', #739, #36398, #44597, .T. ) ;
#38649=DIRECTION ( 'NONE',  ( -0.000000000000000000, 1.000000000000000000, -0.000000000000000000 ) ) ;
#38654=CARTESIAN_POINT ( 'NONE',  ( 1.287906020515830141, 3.346456692913386100, -0.1968503937007883287 ) ) ;
#38655=DIRECTION ( 'NONE',  ( -1.000000000000000000, 0.000000000000000000, -0.000000000000000000 ) ) ;
#38657=DIRECTION ( 'NONE',  ( -1.000000000000000000, 0.000000000000000000, 1.734723475976806848E-16 ) ) ;
#38658=VECTOR ( 'NONE', #9932, 39.37007874015748143 ) ;
#38660=ORIENTED_EDGE ( 'NONE', *, *, #39737, .F. ) ;
#38662=FACE_OUTER_BOUND ( 'NONE', #31956, .T. ) ;
#38664=LINE ( 'NONE', #39671, #15552 ) ;
#38666=AXIS2_PLACEMENT_3D ( 'NONE', #21, #4410, #46971 ) ;
#38667=EDGE_CURVE ( 'NONE', #49919, #10750, #39984, .T. ) ;
#38668=CARTESIAN_POINT ( 'NONE',  ( -1.636583440222564301, 3.267716535433071279, -1.574803149606293307 ) ) ;
#38669=AXIS2_PLACEMENT_3D ( 'NONE', #23098, #46315, #19217 ) ;
#38671=DIRECTION ( 'NONE',  ( 1.734723475976806848E-16, -0.000000000000000000, 1.000000000000000000 ) ) ;
#38673=CARTESIAN_POINT ( 'NONE',  ( 1.636583440222563857, 3.346456692913386100, 1.259842519685033135 ) ) ;
#38675=DIRECTION ( 'NONE',  ( 1.000000000000000000, 0.000000000000000000, -3.469446951953613696E-16 ) ) ;
#38676=LINE ( 'NONE', #11550, #3688 ) ;
#38677=ORIENTED_EDGE ( 'NONE', *, *, #24290, .F. ) ;
#38678=CARTESIAN_POINT ( 'NONE',  ( 0.000000000000000000, 3.267716535433071279, 0.9055118110236167750 ) ) ;
#38680=ORIENTED_EDGE ( 'NONE', *, *, #17998, .F. ) ;
#38681=CARTESIAN_POINT ( 'NONE',  ( 2.182111253630085290, 0.000000000000000000, 0.4330708661417287386 ) ) ;
#38682=ORIENTED_EDGE ( 'NONE', *, *, #15739, .F. ) ;
#38683=DIRECTION ( 'NONE',  ( 0.000000000000000000, -1.000000000000000000, 0.000000000000000000 ) ) ;
#38684=DIRECTION ( 'NONE',  ( -0.000000000000000000, 1.000000000000000000, -0.000000000000000000 ) ) ;
#38686=EDGE_CURVE ( 'NONE', #13181, #7908, #43586, .T. ) ;
#38689=CARTESIAN_POINT ( 'NONE',  ( -3.927031490892378253E-16, 0.000000000000000000, -1.889763779527552146 ) ) ;
#38690=ADVANCED_FACE ( 'NONE', ( #12106 ), #48447, .F. ) ;
#38692=EDGE_LOOP ( 'NONE', ( #22767, #44471, #19414, #29621 ) ) ;
#38694=CARTESIAN_POINT ( 'NONE',  ( 0.5455278134075217666, 0.000000000000000000, 2.204724409448808764 ) ) ;
#38695=FACE_BOUND ( 'NONE', #34909, .T. ) ;
#38696=VERTEX_POINT ( 'NONE', #9254 ) ;
#38697=VECTOR ( 'NONE', #46046, 39.37007874015748143 ) ;
#38699=ORIENTED_EDGE ( 'NONE', *, *, #3523, .F. ) ;
#38700=ORIENTED_EDGE ( 'NONE', *, *, #14731, .T. ) ;
#38701=AXIS2_PLACEMENT_3D ( 'NONE', #33737, #6358, #42470 ) ;
#38702=CARTESIAN_POINT ( 'NONE',  ( 0.4696143004045484348, 3.267716535433071279, 1.850393700787392293 ) ) ;
#38703=CARTESIAN_POINT ( 'NONE',  ( -2.438548951736694725, 3.267716535433071279, -0.1574803149606298636 ) ) ;
#38705=AXIS2_PLACEMENT_3D ( 'NONE', #29786, #6032, #5529 ) ;
#38708=DIRECTION ( 'NONE',  ( -0.000000000000000000, 1.000000000000000000, -0.000000000000000000 ) ) ;
#38709=CARTESIAN_POINT ( 'NONE',  ( -1.985260859929297572, 3.346456692913386100, 0.8645800689071783118 ) ) ;
#38710=EDGE_CURVE ( 'NONE', #1008, #49945, #20088, .T. ) ;
#38713=ORIENTED_EDGE ( 'NONE', *, *, #44032, .T. ) ;
#38714=DIRECTION ( 'NONE',  ( 1.734723475976806848E-16, -0.000000000000000000, 1.000000000000000000 ) ) ;
#38715=CARTESIAN_POINT ( 'NONE',  ( -1.909347346926324906, 0.000000000000000000, -1.299212598425193210 ) ) ;
#38716=CARTESIAN_POINT ( 'NONE',  ( -1.363819533518803473, 0.000000000000000000, -1.732283464566922726 ) ) ;
#38718=EDGE_CURVE ( 'NONE', #43660, #36491, #28092, .T. ) ;
#38719=DIRECTION ( 'NONE',  ( 1.734723475976806848E-16, -0.000000000000000000, 1.000000000000000000 ) ) ;
#38720=EDGE_CURVE ( 'NONE', #49994, #35361, #43839, .T. ) ;
#38722=VECTOR ( 'NONE', #34563, 39.37007874015748143 ) ;
#38723=EDGE_CURVE ( 'NONE', #39358, #25903, #19833, .T. ) ;
#38724=DIRECTION ( 'NONE',  ( -0.000000000000000000, 1.000000000000000000, -0.000000000000000000 ) ) ;
#38726=CARTESIAN_POINT ( 'NONE',  ( 0.000000000000000000, 3.267716535433071279, 0.5905511811023579360 ) ) ;
#38727=LINE ( 'NONE', #26341, #9617 ) ;
#38728=ORIENTED_EDGE ( 'NONE', *, *, #26359, .F. ) ;
#38729=VERTEX_POINT ( 'NONE', #995 ) ;
#38730=CARTESIAN_POINT ( 'NONE',  ( -0.6214413264104945434, 3.346456692913386100, 2.012537465693970962 ) ) ;
#38731=DIRECTION ( 'NONE',  ( 0.000000000000000000, 0.000000000000000000, 1.000000000000000000 ) ) ;
#38732=VERTEX_POINT ( 'NONE', #28867 ) ;
#38736=CARTESIAN_POINT ( 'NONE',  ( -0.8942052331142547050, 3.346456692913386100, 0.6299212598425164567 ) ) ;
#38737=VECTOR ( 'NONE', #11115, 39.37007874015748143 ) ;
#38740=LINE ( 'NONE', #15238, #44938 ) ;
#38741=CARTESIAN_POINT ( 'NONE',  ( -1.636583440222564301, 3.346456692913386100, -0.5118110236220466680 ) ) ;
#38743=EDGE_CURVE ( 'NONE', #4494, #46953, #8741, .T. ) ;
#38744=ORIENTED_EDGE ( 'NONE', *, *, #10183, .T. ) ;
#38746=VERTEX_POINT ( 'NONE', #47942 ) ;
#38747=ORIENTED_EDGE ( 'NONE', *, *, #31430, .T. ) ;
#38748=CARTESIAN_POINT ( 'NONE',  ( -0.07591351300297340121, 0.000000000000000000, 0.2755905511810995412 ) ) ;
#38750=DIRECTION ( 'NONE',  ( 1.000000000000000000, 0.000000000000000000, 0.000000000000000000 ) ) ;
#38751=ORIENTED_EDGE ( 'NONE', *, *, #12858, .F. ) ;
#38753=FACE_OUTER_BOUND ( 'NONE', #17386, .T. ) ;
#38754=VECTOR ( 'NONE', #10440, 39.37007874015748143 ) ;
#38756=CARTESIAN_POINT ( 'NONE',  ( 0.1968503937007873017, 3.346456692913386100, -1.574803149606293529 ) ) ;
#38757=ORIENTED_EDGE ( 'NONE', *, *, #6132, .T. ) ;
#38759=ORIENTED_EDGE ( 'NONE', *, *, #3612, .T. ) ;
#38760=CARTESIAN_POINT ( 'NONE',  ( 1.091055626815042645, 3.346456692913386100, 0.3149606299212578953 ) ) ;
#38762=DIRECTION ( 'NONE',  ( 0.000000000000000000, 0.000000000000000000, -1.000000000000000000 ) ) ;
#38763=AXIS2_PLACEMENT_3D ( 'NONE', #32108, #24605, #29234 ) ;
#38765=DIRECTION ( 'NONE',  ( 0.000000000000000000, 1.000000000000000000, 0.000000000000000000 ) ) ;
#38766=ORIENTED_EDGE ( 'NONE', *, *, #20469, .T. ) ;
#38767=ORIENTED_EDGE ( 'NONE', *, *, #40433, .T. ) ;
#38770=VECTOR ( 'NONE', #12129, 39.37007874015748143 ) ;
#38771=ORIENTED_EDGE ( 'NONE', *, *, #44327, .F. ) ;
#38772=PLANE ( 'NONE',  #25799 ) ;
#38773=CARTESIAN_POINT ( 'NONE',  ( -1.985260859929297572, 3.267716535433071279, 0.8645800689071783118 ) ) ;
#38775=CARTESIAN_POINT ( 'NONE',  ( -0.2727639067037608278, 3.267716535433071279, 2.165354330708650465 ) ) ;
#38778=LINE ( 'NONE', #2649, #35316 ) ;
#38779=ORIENTED_EDGE ( 'NONE', *, *, #39861, .F. ) ;
#38780=CARTESIAN_POINT ( 'NONE',  ( -0.3486774197067334935, 0.000000000000000000, 1.692913385826762873 ) ) ;
#38782=VERTEX_POINT ( 'NONE', #26017 ) ;
#38783=EDGE_CURVE ( 'NONE', #49887, #17928, #10268, .T. ) ;
#38784=DIRECTION ( 'NONE',  ( 1.000000000000000000, 0.000000000000000000, 0.000000000000000000 ) ) ;
#38788=ORIENTED_EDGE ( 'NONE', *, *, #50720, .F. ) ;
#38789=DIRECTION ( 'NONE',  ( -3.469446951953613696E-16, 0.000000000000000000, -1.000000000000000000 ) ) ;
#38793=ORIENTED_EDGE ( 'NONE', *, *, #26592, .F. ) ;
#38795=ORIENTED_EDGE ( 'NONE', *, *, #12392, .F. ) ;
#38796=AXIS2_PLACEMENT_3D ( 'NONE', #48133, #47357, #414 ) ;
#38798=ADVANCED_FACE ( 'NONE', ( #37141 ), #10786, .T. ) ;
#38800=LINE ( 'NONE', #38552, #14488 ) ;
#38801=AXIS2_PLACEMENT_3D ( 'NONE', #3946, #19678, #46273 ) ;
#38803=ORIENTED_EDGE ( 'NONE', *, *, #19650, .T. ) ;
#38804=EDGE_LOOP ( 'NONE', ( #48747, #30674, #34741, #11223 ) ) ;
#38806=CARTESIAN_POINT ( 'NONE',  ( -0.5455278134075208785, 0.000000000000000000, 1.259842519685033357 ) ) ;
#38807=CARTESIAN_POINT ( 'NONE',  ( -1.195183497228115035E-16, 3.346456692913386100, -1.259842519685035134 ) ) ;
#38808=EDGE_CURVE ( 'NONE', #18704, #2485, #48702, .T. ) ;
#38809=ORIENTED_EDGE ( 'NONE', *, *, #37710, .F. ) ;
#38811=LINE ( 'NONE', #50368, #8278 ) ;
#38812=CARTESIAN_POINT ( 'NONE',  ( 2.182111253630085290, 3.267716535433071279, -0.5118110236220471121 ) ) ;
#38815=EDGE_CURVE ( 'NONE', #35947, #2241, #17264, .T. ) ;
#38816=ORIENTED_EDGE ( 'NONE', *, *, #21830, .F. ) ;
#38817=ORIENTED_EDGE ( 'NONE', *, *, #33795, .F. ) ;
#38820=LINE ( 'NONE', #45518, #16267 ) ;
#38822=CARTESIAN_POINT ( 'NONE',  ( -1.536664496436148184E-16, 3.346456692913386100, -1.771653543307081025 ) ) ;
#38823=ORIENTED_EDGE ( 'NONE', *, *, #38514, .F. ) ;
#38826=ORIENTED_EDGE ( 'NONE', *, *, #9069, .T. ) ;
#38830=PLANE ( 'NONE',  #3831 ) ;
#38832=ORIENTED_EDGE ( 'NONE', *, *, #38906, .T. ) ;
#38834=ORIENTED_EDGE ( 'NONE', *, *, #48596, .T. ) ;
#38835=DIRECTION ( 'NONE',  ( -3.469446951953613696E-16, 0.000000000000000000, -1.000000000000000000 ) ) ;
#38836=LINE ( 'NONE', #22335, #34211 ) ;
#38837=AXIS2_PLACEMENT_3D ( 'NONE', #30145, #2526, #49461 ) ;
#38838=VECTOR ( 'NONE', #30494, 39.37007874015748143 ) ;
#38841=PLANE ( 'NONE',  #6428 ) ;
#38842=ORIENTED_EDGE ( 'NONE', *, *, #25570, .F. ) ;
#38845=VECTOR ( 'NONE', #15745, 39.37007874015748143 ) ;
#38847=EDGE_CURVE ( 'NONE', #47095, #41290, #33021, .T. ) ;
#38848=ORIENTED_EDGE ( 'NONE', *, *, #43267, .F. ) ;
#38849=VECTOR ( 'NONE', #682, 39.37007874015748143 ) ;
#38850=CARTESIAN_POINT ( 'NONE',  ( 0.8182917201112819283, 3.346456692913386100, -0.4724409448818889246 ) ) ;
#38854=FACE_OUTER_BOUND ( 'NONE', #8286, .T. ) ;
#38855=DIRECTION ( 'NONE',  ( -1.000000000000000000, 0.000000000000000000, -0.000000000000000000 ) ) ;
#38856=ORIENTED_EDGE ( 'NONE', *, *, #27488, .T. ) ;
#38858=ORIENTED_EDGE ( 'NONE', *, *, #32564, .T. ) ;
#38860=CARTESIAN_POINT ( 'NONE',  ( -1.091055626815042645, 3.346456692913386100, 1.889763779527550147 ) ) ;
#38861=EDGE_CURVE ( 'NONE', #37431, #13717, #25638, .T. ) ;
#38864=ORIENTED_EDGE ( 'NONE', *, *, #47270, .F. ) ;
#38865=DIRECTION ( 'NONE',  ( -0.000000000000000000, 0.000000000000000000, 1.000000000000000000 ) ) ;
#38867=EDGE_CURVE ( 'NONE', #814, #5850, #32247, .T. ) ;
#38868=DIRECTION ( 'NONE',  ( -0.000000000000000000, 0.000000000000000000, 1.000000000000000000 ) ) ;
#38869=FACE_OUTER_BOUND ( 'NONE', #41599, .T. ) ;
#38870=FACE_OUTER_BOUND ( 'NONE', #18127, .T. ) ;
#38871=AXIS2_PLACEMENT_3D ( 'NONE', #6654, #22399, #936 ) ;
#38872=CARTESIAN_POINT ( 'NONE',  ( -2.182111253630085290, 0.000000000000000000, 0.6299212598425164567 ) ) ;
#38873=VECTOR ( 'NONE', #46033, 39.37007874015748143 ) ;
#38874=ORIENTED_EDGE ( 'NONE', *, *, #20800, .T. ) ;
#38875=ORIENTED_EDGE ( 'NONE', *, *, #28829, .F. ) ;
#38877=CARTESIAN_POINT ( 'NONE',  ( -0.8942052331142547050, 3.346456692913386100, 0.9448818897637749625 ) ) ;
#38879=ORIENTED_EDGE ( 'NONE', *, *, #41590, .F. ) ;
#38882=AXIS2_PLACEMENT_3D ( 'NONE', #19305, #50748, #23953 ) ;
#38883=VERTEX_POINT ( 'NONE', #14140 ) ;
#38885=VECTOR ( 'NONE', #874, 39.37007874015748143 ) ;
#38886=ORIENTED_EDGE ( 'NONE', *, *, #24977, .F. ) ;
#38887=ORIENTED_EDGE ( 'NONE', *, *, #19963, .F. ) ;
#38889=FACE_OUTER_BOUND ( 'NONE', #6047, .T. ) ;
#38892=LINE ( 'NONE', #34271, #11562 ) ;
#38895=ORIENTED_EDGE ( 'NONE', *, *, #18843, .T. ) ;
#38896=EDGE_CURVE ( 'NONE', #11695, #22651, #34028, .T. ) ;
#38897=LINE ( 'NONE', #50212, #22522 ) ;
#38898=DIRECTION ( 'NONE',  ( 1.000000000000000000, 0.000000000000000000, 0.000000000000000000 ) ) ;
#38903=ORIENTED_EDGE ( 'NONE', *, *, #18349, .T. ) ;
#38904=VECTOR ( 'NONE', #16340, 39.37007874015748143 ) ;
#38905=LINE ( 'NONE', #18531, #33923 ) ;
#38906=EDGE_CURVE ( 'NONE', #49994, #3958, #14395, .T. ) ;
#38907=LINE ( 'NONE', #46870, #28580 ) ;
#38908=ORIENTED_EDGE ( 'NONE', *, *, #17584, .T. ) ;
#38909=CARTESIAN_POINT ( 'NONE',  ( -0.6214413264104945434, 3.346456692913386100, -0.7874015748031467643 ) ) ;
#38910=EDGE_CURVE ( 'NONE', #5972, #27664, #29383, .T. ) ;
#38913=VECTOR ( 'NONE', #40727, 39.37007874015748143 ) ;
#38914=CARTESIAN_POINT ( 'NONE',  ( -1.985260859929297794, 3.346456692913386100, 0.4330708661417290162 ) ) ;
#38916=DIRECTION ( 'NONE',  ( 1.734723475976806848E-16, -0.000000000000000000, 1.000000000000000000 ) ) ;
#38920=EDGE_CURVE ( 'NONE', #24951, #14359, #41013, .T. ) ;
#38921=LINE ( 'NONE', #35812, #9485 ) ;
#38922=VERTEX_POINT ( 'NONE', #5636 ) ;
#38923=EDGE_LOOP ( 'NONE', ( #4972, #38429, #5202, #46534 ) ) ;
#38925=CARTESIAN_POINT ( 'NONE',  ( -3.414809992080329023E-17, 0.000000000000000000, -0.1968503937007874405 ) ) ;
#38930=ORIENTED_EDGE ( 'NONE', *, *, #30409, .T. ) ;
#38931=LINE ( 'NONE', #50487, #3317 ) ;
#38932=ORIENTED_EDGE ( 'NONE', *, *, #21027, .F. ) ;
#38934=PLANE ( 'NONE',  #988 ) ;
#38935=ORIENTED_EDGE ( 'NONE', *, *, #49010, .F. ) ;
#38936=VERTEX_POINT ( 'NONE', #2776 ) ;
#38937=LINE ( 'NONE', #3826, #14999 ) ;
#38940=VECTOR ( 'NONE', #44398, 39.37007874015748143 ) ;
#38941=DIRECTION ( 'NONE',  ( 1.000000000000000000, 0.000000000000000000, 0.000000000000000000 ) ) ;
#38942=EDGE_LOOP ( 'NONE', ( #26947, #38066, #41305, #37932 ) ) ;
#38943=VERTEX_POINT ( 'NONE', #38158 ) ;
#38946=CARTESIAN_POINT ( 'NONE',  ( -1.636583440222563635, 0.000000000000000000, 1.259842519685033357 ) ) ;
#38948=ORIENTED_EDGE ( 'NONE', *, *, #13447, .F. ) ;
#38955=CARTESIAN_POINT ( 'NONE',  ( 0.9834642517162937025, 3.346456692913386100, -1.929133858267711110 ) ) ;
#38958=CARTESIAN_POINT ( 'NONE',  ( 0.8182917201112819283, 0.000000000000000000, -0.03937007874015881204 ) ) ;
#38960=CARTESIAN_POINT ( 'NONE',  ( 0.000000000000000000, 3.267716535433071279, 0.7874015748031454320 ) ) ;
#38962=CARTESIAN_POINT ( 'NONE',  ( 0.4696143004045483793, 3.267716535433071279, -1.629301903132388985E-16 ) ) ;
#38963=ADVANCED_FACE ( 'NONE', ( #42518 ), #3792, .F. ) ;
#38964=CARTESIAN_POINT ( 'NONE',  ( 0.8182917201112824834, 0.000000000000000000, 2.047244094488179567 ) ) ;
#38965=ADVANCED_FACE ( 'NONE', ( #30400 ), #42766, .F. ) ;
#38966=CARTESIAN_POINT ( 'NONE',  ( -1.712496953225537411, 3.267716535433071279, 5.941417334598190051E-16 ) ) ;
#38967=ORIENTED_EDGE ( 'NONE', *, *, #5039, .F. ) ;
#38968=CARTESIAN_POINT ( 'NONE',  ( -0.8942052331142552601, 0.000000000000000000, -0.9448818897637760728 ) ) ;
#38970=ORIENTED_EDGE ( 'NONE', *, *, #17816, .T. ) ;
#38971=DIRECTION ( 'NONE',  ( -0.000000000000000000, 1.000000000000000000, -0.000000000000000000 ) ) ;
#38972=CARTESIAN_POINT ( 'NONE',  ( -1.166969139818015755, 0.000000000000000000, 0.2755905511810996522 ) ) ;
#38973=ORIENTED_EDGE ( 'NONE', *, *, #9642, .F. ) ;
#38974=VECTOR ( 'NONE', #12718, 39.37007874015748143 ) ;
#38975=LINE ( 'NONE', #35107, #4012 ) ;
#38979=ORIENTED_EDGE ( 'NONE', *, *, #45239, .T. ) ;
#38980=VECTOR ( 'NONE', #1110, 39.37007874015748143 ) ;
#38985=ORIENTED_EDGE ( 'NONE', *, *, #33529, .F. ) ;
#38986=AXIS2_PLACEMENT_3D ( 'NONE', #39151, #31155, #15154 ) ;
#38988=EDGE_LOOP ( 'NONE', ( #27602, #31894, #34156, #998 ) ) ;
#38989=EDGE_LOOP ( 'NONE', ( #31645, #41722, #11109, #7852 ) ) ;
#38990=PLANE ( 'NONE',  #31761 ) ;
#38991=CARTESIAN_POINT ( 'NONE',  ( -0.2727639067037607723, 3.346456692913386100, -1.732283464566922726 ) ) ;
#38992=LINE ( 'NONE', #27363, #23532 ) ;
#38993=ADVANCED_FACE ( 'NONE', ( #30907 ), #31410, .F. ) ;
#38998=EDGE_CURVE ( 'NONE', #49634, #40865, #14905, .T. ) ;
#39000=DIRECTION ( 'NONE',  ( 1.734723475976806848E-16, -0.000000000000000000, 1.000000000000000000 ) ) ;
#39001=ADVANCED_FACE ( 'NONE', ( #10774 ), #26767, .F. ) ;
#39002=VERTEX_POINT ( 'NONE', #7658 ) ;
#39005=ORIENTED_EDGE ( 'NONE', *, *, #21663, .T. ) ;
#39008=FACE_OUTER_BOUND ( 'NONE', #28665, .T. ) ;
#39009=DIRECTION ( 'NONE',  ( -1.000000000000000000, 0.000000000000000000, 1.734723475976806848E-16 ) ) ;
#39012=ORIENTED_EDGE ( 'NONE', *, *, #15816, .F. ) ;
#39013=VECTOR ( 'NONE', #33570, 39.37007874015748143 ) ;
#39015=FACE_OUTER_BOUND ( 'NONE', #30251, .T. ) ;
#39016=VECTOR ( 'NONE', #48336, 39.37007874015748143 ) ;
#39018=DIRECTION ( 'NONE',  ( -0.000000000000000000, 0.000000000000000000, 1.000000000000000000 ) ) ;
#39019=CARTESIAN_POINT ( 'NONE',  ( 1.091055626815043311, 0.000000000000000000, 1.692913385826762873 ) ) ;
#39021=EDGE_CURVE ( 'NONE', #14542, #13249, #50462, .T. ) ;
#39023=ADVANCED_FACE ( 'NONE', ( #35287 ), #50968, .F. ) ;
#39024=DIRECTION ( 'NONE',  ( 0.000000000000000000, 1.000000000000000000, 0.000000000000000000 ) ) ;
#39025=DIRECTION ( 'NONE',  ( -0.000000000000000000, 1.000000000000000000, -0.000000000000000000 ) ) ;
#39029=EDGE_CURVE ( 'NONE', #10448, #10406, #1193, .T. ) ;
#39030=LINE ( 'NONE', #10901, #7704 ) ;
#39032=VERTEX_POINT ( 'NONE', #4813 ) ;
#39033=PLANE ( 'NONE',  #996 ) ;
#39034=DIRECTION ( 'NONE',  ( -3.469446951953613696E-16, 0.000000000000000000, -1.000000000000000000 ) ) ;
#39037=ORIENTED_EDGE ( 'NONE', *, *, #9405, .F. ) ;
#39039=ORIENTED_EDGE ( 'NONE', *, *, #15467, .F. ) ;
#39040=CARTESIAN_POINT ( 'NONE',  ( 1.636583440222563857, 3.346456692913386100, -0.5118110236220471121 ) ) ;
#39041=ORIENTED_EDGE ( 'NONE', *, *, #15350, .T. ) ;
#39042=CARTESIAN_POINT ( 'NONE',  ( 0.8182917201112824834, 3.346456692913386100, 1.220472440944875281 ) ) ;
#39043=FACE_OUTER_BOUND ( 'NONE', #23400, .T. ) ;
#39044=DIRECTION ( 'NONE',  ( 0.000000000000000000, 1.000000000000000000, 0.000000000000000000 ) ) ;
#39046=VECTOR ( 'NONE', #26942, 39.37007874015748143 ) ;
#39047=ORIENTED_EDGE ( 'NONE', *, *, #18813, .F. ) ;
#39048=VERTEX_POINT ( 'NONE', #48140 ) ;
#39050=CARTESIAN_POINT ( 'NONE',  ( 1.636583440222563857, 3.346456692913386100, 1.062992125984245639 ) ) ;
#39051=ORIENTED_EDGE ( 'NONE', *, *, #19669, .T. ) ;
#39052=VERTEX_POINT ( 'NONE', #24178 ) ;
#39054=DIRECTION ( 'NONE',  ( -0.000000000000000000, 1.000000000000000000, -0.000000000000000000 ) ) ;
#39055=DIRECTION ( 'NONE',  ( -1.000000000000000000, 0.000000000000000000, -0.000000000000000000 ) ) ;
#39057=CIRCLE ( 'NONE', #30000, 2.106299212598425008 ) ;
#39058=CIRCLE ( 'NONE', #20936, 2.106299212598425008 ) ;
#39059=ORIENTED_EDGE ( 'NONE', *, *, #33232, .T. ) ;
#39060=ORIENTED_EDGE ( 'NONE', *, *, #41891, .F. ) ;
#39064=LINE ( 'NONE', #50875, #3083 ) ;
#39065=ADVANCED_FACE ( 'NONE', ( #15909 ), #44039, .F. ) ;
#39068=EDGE_CURVE ( 'NONE', #29618, #22693, #12818, .T. ) ;
#39069=CARTESIAN_POINT ( 'NONE',  ( -2.454875160333845674, 3.346456692913386100, -0.3543307086614173040 ) ) ;
#39071=ORIENTED_EDGE ( 'NONE', *, *, #22145, .T. ) ;
#39073=VERTEX_POINT ( 'NONE', #40446 ) ;
#39075=CARTESIAN_POINT ( 'NONE',  ( 0.5455278134075212115, 3.267716535433071279, -0.6299212598425181220 ) ) ;
#39077=CARTESIAN_POINT ( 'NONE',  ( -1.636583440222563635, 3.346456692913386100, 1.062992125984246083 ) ) ;
#39080=VERTEX_POINT ( 'NONE', #8681 ) ;
#39081=VERTEX_POINT ( 'NONE', #12553 ) ;
#39083=ORIENTED_EDGE ( 'NONE', *, *, #28070, .F. ) ;
#39084=DIRECTION ( 'NONE',  ( -1.000000000000000000, 0.000000000000000000, 1.734723475976806848E-16 ) ) ;
#39085=LINE ( 'NONE', #23332, #13568 ) ;
#39087=ADVANCED_FACE ( 'NONE', ( #16691 ), #12303, .F. ) ;
#39088=CARTESIAN_POINT ( 'NONE',  ( 1.015142113812069313, 0.000000000000000000, 0.7874015748031454320 ) ) ;
#39091=VECTOR ( 'NONE', #9186, 39.37007874015748143 ) ;
#39093=DIRECTION ( 'NONE',  ( 0.000000000000000000, 0.000000000000000000, 1.000000000000000000 ) ) ;
#39094=EDGE_CURVE ( 'NONE', #30018, #50731, #35541, .T. ) ;
#39096=CARTESIAN_POINT ( 'NONE',  ( -1.166969139818015977, 3.267716535433071279, 4.048737525165546155E-16 ) ) ;
#39100=CARTESIAN_POINT ( 'NONE',  ( 0.000000000000000000, 3.267716535433071279, 1.102362204724403938 ) ) ;
#39101=CARTESIAN_POINT ( 'NONE',  ( -0.8182917201112819283, 0.000000000000000000, -1.732283464566922726 ) ) ;
#39102=DIRECTION ( 'NONE',  ( 1.000000000000000000, -0.000000000000000000, 0.000000000000000000 ) ) ;
#39103=FACE_OUTER_BOUND ( 'NONE', #15171, .T. ) ;
#39105=LINE ( 'NONE', #27470, #26712 ) ;
#39109=ORIENTED_EDGE ( 'NONE', *, *, #4694, .T. ) ;
#39110=CARTESIAN_POINT ( 'NONE',  ( 2.106197740627112402, 3.346456692913386100, 0.02067487291359298290 ) ) ;
#39112=LINE ( 'NONE', #3743, #44946 ) ;
#39113=ORIENTED_EDGE ( 'NONE', *, *, #11989, .T. ) ;
#39116=CARTESIAN_POINT ( 'NONE',  ( 0.2727639067037602172, 3.346456692913386100, -1.929133858267710000 ) ) ;
#39117=ORIENTED_EDGE ( 'NONE', *, *, #50439, .F. ) ;
#39118=LINE ( 'NONE', #46334, #2765 ) ;
#39122=VERTEX_POINT ( 'NONE', #31669 ) ;
#39123=LINE ( 'NONE', #38630, #28732 ) ;
#39124=LINE ( 'NONE', #6876, #12563 ) ;
#39125=LINE ( 'NONE', #3764, #19072 ) ;
#39128=VECTOR ( 'NONE', #46055, 39.37007874015748143 ) ;
#39130=EDGE_CURVE ( 'NONE', #1872, #47459, #8937, .T. ) ;
#39131=LINE ( 'NONE', #4025, #10903 ) ;
#39132=VECTOR ( 'NONE', #13199, 39.37007874015748143 ) ;
#39134=ORIENTED_EDGE ( 'NONE', *, *, #36311, .T. ) ;
#39137=VECTOR ( 'NONE', #24765, 39.37007874015748143 ) ;
#39138=ORIENTED_EDGE ( 'NONE', *, *, #48765, .T. ) ;
#39141=EDGE_LOOP ( 'NONE', ( #44903, #35136, #1613, #49242 ) ) ;
#39142=AXIS2_PLACEMENT_3D ( 'NONE', #12061, #7677, #34798 ) ;
#39146=EDGE_CURVE ( 'NONE', #35538, #4542, #23659, .T. ) ;
#39147=CARTESIAN_POINT ( 'NONE',  ( 0.5455278134075208785, 0.000000000000000000, -1.574803149606293529 ) ) ;
#39148=LINE ( 'NONE', #6896, #26956 ) ;
#39150=ORIENTED_EDGE ( 'NONE', *, *, #25225, .T. ) ;
#39151=CARTESIAN_POINT ( 'NONE',  ( 1.363819533518803251, 0.000000000000000000, 0.5905511811023579360 ) ) ;
#39152=EDGE_CURVE ( 'NONE', #37360, #28099, #4296, .T. ) ;
#39153=DIRECTION ( 'NONE',  ( 1.000000000000000000, -0.000000000000000000, 0.000000000000000000 ) ) ;
#39155=ORIENTED_EDGE ( 'NONE', *, *, #1075, .T. ) ;
#39156=DIRECTION ( 'NONE',  ( 0.000000000000000000, -1.000000000000000000, 0.000000000000000000 ) ) ;
#39157=CARTESIAN_POINT ( 'NONE',  ( -0.6214413264104939882, 3.267716535433071279, 0.7874015748031456541 ) ) ;
#39162=VECTOR ( 'NONE', #32456, 39.37007874015748143 ) ;
#39164=LINE ( 'NONE', #2789, #41393 ) ;
#39167=AXIS2_PLACEMENT_3D ( 'NONE', #24126, #4507, #28500 ) ;
#39169=CARTESIAN_POINT ( 'NONE',  ( 0.000000000000000000, 3.346456692913386100, 0.000000000000000000 ) ) ;
#39171=VERTEX_POINT ( 'NONE', #43776 ) ;
#39172=AXIS2_PLACEMENT_3D ( 'NONE', #10161, #22045, #33926 ) ;
#39173=VERTEX_POINT ( 'NONE', #8429 ) ;
#39174=ORIENTED_EDGE ( 'NONE', *, *, #43604, .T. ) ;
#39175=DIRECTION ( 'NONE',  ( 1.000000000000000000, -0.000000000000000000, 0.000000000000000000 ) ) ;
#39178=PLANE ( 'NONE',  #7122 ) ;
#39179=ORIENTED_EDGE ( 'NONE', *, *, #17622, .F. ) ;
#39180=CARTESIAN_POINT ( 'NONE',  ( -2.009899395340762229, 3.346456692913386100, -0.6299212598425177889 ) ) ;
#39181=ORIENTED_EDGE ( 'NONE', *, *, #9405, .T. ) ;
#39182=DIRECTION ( 'NONE',  ( 1.000000000000000000, -0.000000000000000000, 0.000000000000000000 ) ) ;
#39183=ADVANCED_FACE ( 'NONE', ( #39923 ), #4556, .F. ) ;
#39185=EDGE_CURVE ( 'NONE', #41776, #50744, #6079, .T. ) ;
#39188=VERTEX_POINT ( 'NONE', #1446 ) ;
#39189=EDGE_CURVE ( 'NONE', #1162, #13413, #32710, .T. ) ;
#39190=CARTESIAN_POINT ( 'NONE',  ( 3.335048530465896514E-16, 3.346456692913386100, 2.493791675044291445 ) ) ;
#39195=AXIS2_PLACEMENT_3D ( 'NONE', #156, #15907, #7412 ) ;
#39196=DIRECTION ( 'NONE',  ( 0.000000000000000000, -1.000000000000000000, 0.000000000000000000 ) ) ;
#39197=AXIS2_PLACEMENT_3D ( 'NONE', #34731, #23101, #38855 ) ;
#39198=EDGE_LOOP ( 'NONE', ( #25032, #25403, #28953, #46707 ) ) ;
#39201=ORIENTED_EDGE ( 'NONE', *, *, #2908, .T. ) ;
#39203=CARTESIAN_POINT ( 'NONE',  ( 0.000000000000000000, 0.000000000000000000, 0.000000000000000000 ) ) ;
#39204=EDGE_CURVE ( 'NONE', #24648, #4720, #29320, .T. ) ;
#39208=EDGE_LOOP ( 'NONE', ( #5319, #21366, #49441, #28370 ) ) ;
#39210=CARTESIAN_POINT ( 'NONE',  ( -0.3486774197067340486, 3.267716535433071279, -1.456692913385822630 ) ) ;
#39211=FACE_OUTER_BOUND ( 'NONE', #38304, .T. ) ;
#39212=CARTESIAN_POINT ( 'NONE',  ( 1.441853549388196321, 3.346456692913386100, 1.535433070866133898 ) ) ;
#39213=EDGE_CURVE ( 'NONE', #31389, #24633, #9453, .T. ) ;
#39216=LINE ( 'NONE', #6972, #10320 ) ;
#39217=VERTEX_POINT ( 'NONE', #5830 ) ;
#39218=LINE ( 'NONE', #31736, #15186 ) ;
#39219=ORIENTED_EDGE ( 'NONE', *, *, #5649, .T. ) ;
#39220=DIRECTION ( 'NONE',  ( 1.734723475976806848E-16, 0.000000000000000000, 1.000000000000000000 ) ) ;
#39223=DIRECTION ( 'NONE',  ( -1.000000000000000000, 0.000000000000000000, -0.000000000000000000 ) ) ;
#39224=CARTESIAN_POINT ( 'NONE',  ( -0.8182917201112819283, 3.346456692913386100, 2.047244094488179567 ) ) ;
#39225=EDGE_LOOP ( 'NONE', ( #21125, #23877, #14247, #18440, #6675 ) ) ;
#39228=LINE ( 'NONE', #35872, #23788 ) ;
#39229=VECTOR ( 'NONE', #46912, 39.37007874015748143 ) ;
#39231=PLANE ( 'NONE',  #28733 ) ;
#39234=LINE ( 'NONE', #27603, #19441 ) ;
#39236=VECTOR ( 'NONE', #47790, 39.37007874015748143 ) ;
#39237=VERTEX_POINT ( 'NONE', #17959 ) ;
#39238=AXIS2_PLACEMENT_3D ( 'NONE', #3503, #31380, #47074 ) ;
#39239=DIRECTION ( 'NONE',  ( 1.000000000000000000, -0.000000000000000000, 0.000000000000000000 ) ) ;
#39241=ORIENTED_EDGE ( 'NONE', *, *, #28047, .F. ) ;
#39244=PLANE ( 'NONE',  #13682 ) ;
#39245=EDGE_CURVE ( 'NONE', #8994, #16391, #44798, .T. ) ;
#39246=EDGE_LOOP ( 'NONE', ( #27358, #37479, #18512, #15520 ) ) ;
#39247=FACE_OUTER_BOUND ( 'NONE', #26346, .T. ) ;
#39250=EDGE_CURVE ( 'NONE', #7930, #49632, #2473, .T. ) ;
#39252=CARTESIAN_POINT ( 'NONE',  ( -0.07591351300297366489, 3.346456692913386100, -2.244094488188968395 ) ) ;
#39254=ORIENTED_EDGE ( 'NONE', *, *, #39477, .F. ) ;
#39256=VERTEX_POINT ( 'NONE', #45051 ) ;
#39257=CARTESIAN_POINT ( 'NONE',  ( 0.5455278134075217666, 3.346456692913386100, 1.574803149606291974 ) ) ;
#39258=DIRECTION ( 'NONE',  ( 1.000000000000000000, -0.000000000000000000, 0.000000000000000000 ) ) ;
#39259=AXIS2_PLACEMENT_3D ( 'NONE', #30273, #26888, #38530 ) ;
#39260=DIRECTION ( 'NONE',  ( 1.734723475976806848E-16, 0.000000000000000000, 1.000000000000000000 ) ) ;
#39261=CARTESIAN_POINT ( 'NONE',  ( -1.091055626815042201, 3.267716535433071279, 1.892679809432643650E-16 ) ) ;
#39263=ORIENTED_EDGE ( 'NONE', *, *, #23584, .T. ) ;
#39264=AXIS2_PLACEMENT_3D ( 'NONE', #20942, #21456, #25072 ) ;
#39266=VECTOR ( 'NONE', #8987, 39.37007874015748143 ) ;
#39268=ORIENTED_EDGE ( 'NONE', *, *, #8882, .F. ) ;
#39270=PLANE ( 'NONE',  #23485 ) ;
#39271=AXIS2_PLACEMENT_3D ( 'NONE', #27426, #15567, #26924 ) ;
#39274=ADVANCED_FACE ( 'NONE', ( #48388 ), #41708, .F. ) ;
#39275=LINE ( 'NONE', #39529, #18434 ) ;
#39277=CARTESIAN_POINT ( 'NONE',  ( -1.909347346926324906, 0.000000000000000000, -0.6692913385826758654 ) ) ;
#39279=ORIENTED_EDGE ( 'NONE', *, *, #35642, .F. ) ;
#39281=LINE ( 'NONE', #16562, #41718 ) ;
#39282=ORIENTED_EDGE ( 'NONE', *, *, #43620, .F. ) ;
#39283=EDGE_CURVE ( 'NONE', #38635, #43930, #44546, .T. ) ;
#39285=DIRECTION ( 'NONE',  ( -3.469446951953613696E-16, 0.000000000000000000, -1.000000000000000000 ) ) ;
#39288=VERTEX_POINT ( 'NONE', #5318 ) ;
#39290=ADVANCED_FACE ( 'NONE', ( #14085 ), #1956, .F. ) ;
#39293=ORIENTED_EDGE ( 'NONE', *, *, #9728, .T. ) ;
#39295=ORIENTED_EDGE ( 'NONE', *, *, #25228, .T. ) ;
#39296=EDGE_CURVE ( 'NONE', #11113, #20686, #21071, .T. ) ;
#39297=LINE ( 'NONE', #4184, #20219 ) ;
#39298=CARTESIAN_POINT ( 'NONE',  ( 0.000000000000000000, 3.346456692913386100, 0.000000000000000000 ) ) ;
#39299=PLANE ( 'NONE',  #31811 ) ;
#39300=VECTOR ( 'NONE', #1449, 39.37007874015748143 ) ;
#39303=ORIENTED_EDGE ( 'NONE', *, *, #31984, .F. ) ;
#39304=CARTESIAN_POINT ( 'NONE',  ( -0.2727639067037602727, 0.000000000000000000, 0.5905511811023582691 ) ) ;
#39305=AXIS2_PLACEMENT_3D ( 'NONE', #49209, #13632, #18011 ) ;
#39307=ORIENTED_EDGE ( 'NONE', *, *, #18648, .T. ) ;
#39309=PLANE ( 'NONE',  #38801 ) ;
#39310=CARTESIAN_POINT ( 'NONE',  ( 1.015142113812069313, 0.000000000000000000, -0.1574803149606301411 ) ) ;
#39311=DIRECTION ( 'NONE',  ( -1.000000000000000000, 0.000000000000000000, 1.734723475976806848E-16 ) ) ;
#39312=EDGE_CURVE ( 'NONE', #7739, #43163, #21329, .T. ) ;
#39313=ORIENTED_EDGE ( 'NONE', *, *, #21062, .T. ) ;
#39315=LINE ( 'NONE', #31835, #30766 ) ;
#39317=DIRECTION ( 'NONE',  ( -0.000000000000000000, 1.000000000000000000, -0.000000000000000000 ) ) ;
#39318=EDGE_CURVE ( 'NONE', #35864, #12600, #25702, .T. ) ;
#39320=EDGE_LOOP ( 'NONE', ( #36289, #18963, #49668, #3753 ) ) ;
#39323=ORIENTED_EDGE ( 'NONE', *, *, #37368, .F. ) ;
#39324=EDGE_CURVE ( 'NONE', #1994, #1350, #25444, .T. ) ;
#39325=CARTESIAN_POINT ( 'NONE',  ( -1.363819533518803473, 3.346456692913386100, 1.605145679676863057 ) ) ;
#39326=ORIENTED_EDGE ( 'NONE', *, *, #44447, .T. ) ;
#39328=DIRECTION ( 'NONE',  ( -0.000000000000000000, 1.000000000000000000, -0.000000000000000000 ) ) ;
#39330=DIRECTION ( 'NONE',  ( 0.000000000000000000, -1.000000000000000000, 0.000000000000000000 ) ) ;
#39334=ORIENTED_EDGE ( 'NONE', *, *, #2724, .F. ) ;
#39338=AXIS2_PLACEMENT_3D ( 'NONE', #28621, #13394, #32779 ) ;
#39341=FACE_OUTER_BOUND ( 'NONE', #50084, .T. ) ;
#39344=ORIENTED_EDGE ( 'NONE', *, *, #46406, .F. ) ;
#39345=DIRECTION ( 'NONE',  ( 0.000000000000000000, -1.000000000000000000, 0.000000000000000000 ) ) ;
#39346=DIRECTION ( 'NONE',  ( -3.469446951953613696E-16, 0.000000000000000000, -1.000000000000000000 ) ) ;
#39347=EDGE_CURVE ( 'NONE', #44408, #28725, #10722, .T. ) ;
#39348=VERTEX_POINT ( 'NONE', #50162 ) ;
#39349=DIRECTION ( 'NONE',  ( 0.000000000000000000, -1.000000000000000000, 0.000000000000000000 ) ) ;
#39350=ADVANCED_FACE ( 'NONE', ( #3478 ), #23338, .F. ) ;
#39351=FACE_OUTER_BOUND ( 'NONE', #42665, .T. ) ;
#39353=ORIENTED_EDGE ( 'NONE', *, *, #21433, .T. ) ;
#39354=EDGE_CURVE ( 'NONE', #34110, #11339, #3218, .T. ) ;
#39355=LINE ( 'NONE', #3735, #44073 ) ;
#39356=CARTESIAN_POINT ( 'NONE',  ( -0.3486774197067338266, 3.267716535433071279, 1.209717811016578585E-16 ) ) ;
#39357=DIRECTION ( 'NONE',  ( 0.000000000000000000, 0.000000000000000000, -1.000000000000000000 ) ) ;
#39358=VERTEX_POINT ( 'NONE', #11479 ) ;
#39359=LINE ( 'NONE', #8884, #20566 ) ;
#39361=VERTEX_POINT ( 'NONE', #18966 ) ;
#39362=VECTOR ( 'NONE', #47167, 39.37007874015748143 ) ;
#39364=CARTESIAN_POINT ( 'NONE',  ( 1.015142113812069091, 3.226129038349118794, -2.244094488188969283 ) ) ;
#39365=CARTESIAN_POINT ( 'NONE',  ( -2.182111253630085734, 0.000000000000000000, -0.9448818897637762948 ) ) ;
#39366=EDGE_CURVE ( 'NONE', #15591, #50954, #34225, .T. ) ;
#39367=EDGE_LOOP ( 'NONE', ( #3564, #1800, #20367, #21521 ) ) ;
#39369=DIRECTION ( 'NONE',  ( -1.000000000000000000, 0.000000000000000000, -0.000000000000000000 ) ) ;
#39372=VERTEX_POINT ( 'NONE', #26459 ) ;
#39373=LINE ( 'NONE', #47331, #20896 ) ;
#39374=FACE_OUTER_BOUND ( 'NONE', #8938, .T. ) ;
#39375=EDGE_CURVE ( 'NONE', #46139, #8923, #7602, .T. ) ;
#39376=LINE ( 'NONE', #23885, #24446 ) ;
#39378=PLANE ( 'NONE',  #20668 ) ;
#39379=EDGE_LOOP ( 'NONE', ( #967, #33730, #33088, #30949 ) ) ;
#39380=ORIENTED_EDGE ( 'NONE', *, *, #17841, .T. ) ;
#39381=DIRECTION ( 'NONE',  ( -0.000000000000000000, 1.000000000000000000, -0.000000000000000000 ) ) ;
#39384=ADVANCED_FACE ( 'NONE', ( #49908 ), #14338, .F. ) ;
#39385=EDGE_CURVE ( 'NONE', #21759, #17096, #27212, .T. ) ;
#39386=DIRECTION ( 'NONE',  ( -3.469446951953613696E-16, 0.000000000000000000, -1.000000000000000000 ) ) ;
#39387=ORIENTED_EDGE ( 'NONE', *, *, #27211, .T. ) ;
#39388=EDGE_CURVE ( 'NONE', #22792, #26280, #18214, .T. ) ;
#39389=DIRECTION ( 'NONE',  ( -3.469446951953613696E-16, 0.000000000000000000, -1.000000000000000000 ) ) ;
#39391=AXIS2_PLACEMENT_3D ( 'NONE', #48234, #28646, #44393 ) ;
#39392=ORIENTED_EDGE ( 'NONE', *, *, #10847, .F. ) ;
#39395=ORIENTED_EDGE ( 'NONE', *, *, #15196, .T. ) ;
#39396=LINE ( 'NONE', #20279, #44216 ) ;
#39397=VECTOR ( 'NONE', #45909, 39.37007874015748143 ) ;
#39398=ORIENTED_EDGE ( 'NONE', *, *, #19205, .F. ) ;
#39401=FACE_OUTER_BOUND ( 'NONE', #42592, .T. ) ;
#39403=CARTESIAN_POINT ( 'NONE',  ( 1.287906020515829919, 0.000000000000000000, -1.574803149606294417 ) ) ;
#39404=LINE ( 'NONE', #4807, #5564 ) ;
#39405=CARTESIAN_POINT ( 'NONE',  ( -2.061297163897529483, 3.346456692913386100, 0.4330708661417290162 ) ) ;
#39406=ORIENTED_EDGE ( 'NONE', *, *, #9976, .T. ) ;
#39407=DIRECTION ( 'NONE',  ( -3.469446951953613696E-16, 0.000000000000000000, -1.000000000000000000 ) ) ;
#39410=VERTEX_POINT ( 'NONE', #34721 ) ;
#39413=DIRECTION ( 'NONE',  ( -0.000000000000000000, 1.000000000000000000, -0.000000000000000000 ) ) ;
#39415=DIRECTION ( 'NONE',  ( -0.000000000000000000, 1.000000000000000000, -0.000000000000000000 ) ) ;
#39418=EDGE_CURVE ( 'NONE', #39032, #28119, #22590, .T. ) ;
#39420=VECTOR ( 'NONE', #15078, 39.37007874015748143 ) ;
#39421=DIRECTION ( 'NONE',  ( -0.000000000000000000, 0.000000000000000000, 1.000000000000000000 ) ) ;
#39422=ORIENTED_EDGE ( 'NONE', *, *, #40814, .F. ) ;
#39423=CARTESIAN_POINT ( 'NONE',  ( 2.105931235793975009, 3.267716535433071279, -0.03937007874015936021 ) ) ;
#39427=CARTESIAN_POINT ( 'NONE',  ( -1.636583440222564301, 0.000000000000000000, -1.456692913385822186 ) ) ;
#39428=ORIENTED_EDGE ( 'NONE', *, *, #26663, .F. ) ;
#39429=VECTOR ( 'NONE', #13119, 39.37007874015748143 ) ;
#39430=ORIENTED_EDGE ( 'NONE', *, *, #7322, .T. ) ;
#39431=VERTEX_POINT ( 'NONE', #46807 ) ;
#39432=DIRECTION ( 'NONE',  ( 1.000000000000000000, -0.000000000000000000, 0.000000000000000000 ) ) ;
#39433=EDGE_LOOP ( 'NONE', ( #23894, #34950, #38432, #3685 ) ) ;
#39434=CARTESIAN_POINT ( 'NONE',  ( 0.000000000000000000, 2.362204724409439294, 0.000000000000000000 ) ) ;
#39435=EDGE_CURVE ( 'NONE', #8967, #9639, #26711, .T. ) ;
#39437=CARTESIAN_POINT ( 'NONE',  ( 2.106197740627111514, 0.000000000000000000, -0.9842519685039348154 ) ) ;
#39438=ORIENTED_EDGE ( 'NONE', *, *, #12415, .F. ) ;
#39439=LINE ( 'NONE', #3818, #19009 ) ;
#39440=ADVANCED_FACE ( 'NONE', ( #41963 ), #26213, .F. ) ;
#39441=ORIENTED_EDGE ( 'NONE', *, *, #12904, .T. ) ;
#39442=FACE_OUTER_BOUND ( 'NONE', #16402, .T. ) ;
#39443=EDGE_CURVE ( 'NONE', #16050, #39976, #30090, .T. ) ;
#39446=EDGE_LOOP ( 'NONE', ( #15741, #27504, #47740, #11646 ) ) ;
#39447=EDGE_CURVE ( 'NONE', #1681, #37048, #22344, .T. ) ;
#39448=DIRECTION ( 'NONE',  ( -0.000000000000000000, 1.000000000000000000, -0.000000000000000000 ) ) ;
#39449=EDGE_LOOP ( 'NONE', ( #28497, #19869, #291, #22210 ) ) ;
#39452=ORIENTED_EDGE ( 'NONE', *, *, #48484, .T. ) ;
#39455=ORIENTED_EDGE ( 'NONE', *, *, #72, .F. ) ;
#39457=DIRECTION ( 'NONE',  ( 1.734723475976806848E-16, -0.000000000000000000, 1.000000000000000000 ) ) ;
#39462=AXIS2_PLACEMENT_3D ( 'NONE', #10797, #49489, #13920 ) ;
#39463=DIRECTION ( 'NONE',  ( -0.000000000000000000, 1.000000000000000000, -0.000000000000000000 ) ) ;
#39465=ORIENTED_EDGE ( 'NONE', *, *, #42715, .T. ) ;
#39466=ORIENTED_EDGE ( 'NONE', *, *, #12256, .T. ) ;
#39468=DIRECTION ( 'NONE',  ( 1.000000000000000000, 0.000000000000000000, 0.000000000000000000 ) ) ;
#39470=DIRECTION ( 'NONE',  ( 1.000000000000000000, 0.000000000000000000, 0.000000000000000000 ) ) ;
#39471=AXIS2_PLACEMENT_3D ( 'NONE', #31940, #40452, #16956 ) ;
#39473=DIRECTION ( 'NONE',  ( -1.000000000000000000, 0.000000000000000000, 0.000000000000000000 ) ) ;
#39475=EDGE_LOOP ( 'NONE', ( #29899, #12951, #11442, #18503 ) ) ;
#39476=DIRECTION ( 'NONE',  ( -3.469446951953613696E-16, 0.000000000000000000, -1.000000000000000000 ) ) ;
#39477=EDGE_CURVE ( 'NONE', #15126, #3065, #35227, .T. ) ;
#39478=EDGE_LOOP ( 'NONE', ( #14240, #12362, #43323, #28764 ) ) ;
#39479=FACE_OUTER_BOUND ( 'NONE', #1065, .T. ) ;
#39480=EDGE_CURVE ( 'NONE', #18622, #19884, #35477, .T. ) ;
#39483=CARTESIAN_POINT ( 'NONE',  ( -1.166969139818015755, 0.000000000000000000, 0.9055118110236167750 ) ) ;
#39484=DIRECTION ( 'NONE',  ( 1.734723475976806848E-16, 0.000000000000000000, 1.000000000000000000 ) ) ;
#39487=LINE ( 'NONE', #15488, #14736 ) ;
#39488=EDGE_LOOP ( 'NONE', ( #31453, #47150, #31560, #26922 ) ) ;
#39489=DIRECTION ( 'NONE',  ( 0.000000000000000000, 1.000000000000000000, 0.000000000000000000 ) ) ;
#39490=VERTEX_POINT ( 'NONE', #28225 ) ;
#39492=VECTOR ( 'NONE', #3208, 39.37007874015748143 ) ;
#39494=CARTESIAN_POINT ( 'NONE',  ( -1.166969139818015977, 3.346456692913386100, 1.732283464566920950 ) ) ;
#39495=EDGE_CURVE ( 'NONE', #14359, #24862, #39856, .T. ) ;
#39497=ORIENTED_EDGE ( 'NONE', *, *, #25629, .T. ) ;
#39500=VERTEX_POINT ( 'NONE', #12751 ) ;
#39501=ADVANCED_FACE ( 'NONE', ( #36251 ), #43968, .F. ) ;
#39502=CARTESIAN_POINT ( 'NONE',  ( 0.8182917201112817063, 0.000000000000000000, -2.244094488188969283 ) ) ;
#39505=VECTOR ( 'NONE', #39102, 39.37007874015748143 ) ;
#39506=ORIENTED_EDGE ( 'NONE', *, *, #39873, .T. ) ;
#39507=CARTESIAN_POINT ( 'NONE',  ( 1.909347346926324684, 3.346456692913386100, 0.1574803149606280872 ) ) ;
#39508=DIRECTION ( 'NONE',  ( 0.000000000000000000, 1.000000000000000000, 0.000000000000000000 ) ) ;
#39509=EDGE_LOOP ( 'NONE', ( #34144, #32784, #42391, #38465 ) ) ;
#39510=CARTESIAN_POINT ( 'NONE',  ( -0.5455278134075214336, 0.000000000000000000, 0.1181102362204703021 ) ) ;
#39511=ORIENTED_EDGE ( 'NONE', *, *, #5843, .T. ) ;
#39512=VERTEX_POINT ( 'NONE', #24109 ) ;
#39516=ORIENTED_EDGE ( 'NONE', *, *, #16268, .T. ) ;
#39517=CARTESIAN_POINT ( 'NONE',  ( 0.000000000000000000, 3.267716535433071279, 0.7480314960629874665 ) ) ;
#39519=FACE_OUTER_BOUND ( 'NONE', #245, .T. ) ;
#39520=CARTESIAN_POINT ( 'NONE',  ( -0.3486774197067340486, 0.000000000000000000, 0.1181102362204703021 ) ) ;
#39522=ORIENTED_EDGE ( 'NONE', *, *, #5994, .T. ) ;
#39527=CARTESIAN_POINT ( 'NONE',  ( 0.7423782071083092626, 0.000000000000000000, 1.889763779527550369 ) ) ;
#39528=VECTOR ( 'NONE', #21185, 39.37007874015748143 ) ;
#39529=CARTESIAN_POINT ( 'NONE',  ( -0.07591351300297277671, 3.346456692913386100, 1.732283464566921172 ) ) ;
#39532=ORIENTED_EDGE ( 'NONE', *, *, #43031, .T. ) ;
#39536=AXIS2_PLACEMENT_3D ( 'NONE', #4248, #28501, #11997 ) ;
#39537=VERTEX_POINT ( 'NONE', #16373 ) ;
#39539=ORIENTED_EDGE ( 'NONE', *, *, #36403, .F. ) ;
#39540=DIRECTION ( 'NONE',  ( 1.000000000000000000, 0.000000000000000000, -3.469446951953613696E-16 ) ) ;
#39541=LINE ( 'NONE', #20426, #4740 ) ;
#39543=ADVANCED_FACE ( 'NONE', ( #8872 ), #8618, .F. ) ;
#39544=EDGE_LOOP ( 'NONE', ( #18636, #45056, #44623, #37505 ) ) ;
#39548=ORIENTED_EDGE ( 'NONE', *, *, #29598, .T. ) ;
#39551=PLANE ( 'NONE',  #23527 ) ;
#39553=DIRECTION ( 'NONE',  ( -1.000000000000000000, 0.000000000000000000, -0.000000000000000000 ) ) ;
#39555=AXIS2_PLACEMENT_3D ( 'NONE', #393, #31640, #43495 ) ;
#39557=ORIENTED_EDGE ( 'NONE', *, *, #23402, .T. ) ;
#39558=EDGE_LOOP ( 'NONE', ( #41311, #49851, #50498, #41069 ) ) ;
#39559=VERTEX_POINT ( 'NONE', #15602 ) ;
#39561=CARTESIAN_POINT ( 'NONE',  ( -1.353990537516116754, 3.244463339810032210, 2.047244094488179567 ) ) ;
#39562=VERTEX_POINT ( 'NONE', #23594 ) ;
#39566=PLANE ( 'NONE',  #36824 ) ;
#39567=CARTESIAN_POINT ( 'NONE',  ( -1.091055626815042201, 3.346456692913386100, 0.7480314960629874665 ) ) ;
#39569=EDGE_LOOP ( 'NONE', ( #48250, #12494, #33947, #22047 ) ) ;
#39570=VERTEX_POINT ( 'NONE', #47049 ) ;
#39571=VECTOR ( 'NONE', #46538, 39.37007874015748143 ) ;
#39572=CARTESIAN_POINT ( 'NONE',  ( 0.2727639067037606613, 3.267716535433071279, -4.731699523581610974E-17 ) ) ;
#39573=DIRECTION ( 'NONE',  ( -1.000000000000000000, -0.000000000000000000, -0.000000000000000000 ) ) ;
#39574=ADVANCED_FACE ( 'NONE', ( #47563 ), #11722, .F. ) ;
#39575=CARTESIAN_POINT ( 'NONE',  ( -0.8942052331142547050, 3.267716535433071279, 0.1181102362204705658 ) ) ;
#39576=ORIENTED_EDGE ( 'NONE', *, *, #2216, .T. ) ;
#39578=DIRECTION ( 'NONE',  ( -0.000000000000000000, 1.000000000000000000, -0.000000000000000000 ) ) ;
#39581=ORIENTED_EDGE ( 'NONE', *, *, #49471, .F. ) ;
#39582=ORIENTED_EDGE ( 'NONE', *, *, #13621, .F. ) ;
#39583=AXIS2_PLACEMENT_3D ( 'NONE', #24321, #11677, #40068 ) ;
#39585=CARTESIAN_POINT ( 'NONE',  ( -0.5455278134075208785, 0.000000000000000000, 0.9448818897637749625 ) ) ;
#39587=LINE ( 'NONE', #39077, #23096 ) ;
#39588=CARTESIAN_POINT ( 'NONE',  ( 0.000000000000000000, 3.346456692913386100, -2.952755905511811552 ) ) ;
#39590=ORIENTED_EDGE ( 'NONE', *, *, #38629, .T. ) ;
#39591=ORIENTED_EDGE ( 'NONE', *, *, #32436, .F. ) ;
#39592=EDGE_CURVE ( 'NONE', #9076, #41777, #13517, .T. ) ;
#39594=DIRECTION ( 'NONE',  ( 0.000000000000000000, -1.000000000000000000, 0.000000000000000000 ) ) ;
#39596=ADVANCED_FACE ( 'NONE', ( #5767 ), #21771, .F. ) ;
#39597=DIRECTION ( 'NONE',  ( 1.000000000000000000, -0.000000000000000000, 0.000000000000000000 ) ) ;
#39598=LINE ( 'NONE', #4996, #14641 ) ;
#39600=CARTESIAN_POINT ( 'NONE',  ( -2.182111253630085290, 3.346456692913386100, -0.1968503937007880511 ) ) ;
#39601=CARTESIAN_POINT ( 'NONE',  ( 0.000000000000000000, 3.267716535433071279, 0.3149606299212578953 ) ) ;
#39602=EDGE_CURVE ( 'NONE', #44569, #713, #25131, .T. ) ;
#39603=VECTOR ( 'NONE', #39916, 39.37007874015748143 ) ;
#39604=VERTEX_POINT ( 'NONE', #40883 ) ;
#39605=DIRECTION ( 'NONE',  ( -1.000000000000000000, 0.000000000000000000, -0.000000000000000000 ) ) ;
#39606=VECTOR ( 'NONE', #3964, 39.37007874015748143 ) ;
#39609=EDGE_LOOP ( 'NONE', ( #4954, #49509, #16890, #33361 ) ) ;
#39610=LINE ( 'NONE', #4239, #48979 ) ;
#39611=CARTESIAN_POINT ( 'NONE',  ( 1.091055626815042645, 0.000000000000000000, 0.4330708661417287386 ) ) ;
#39614=EDGE_LOOP ( 'NONE', ( #16518, #9172, #29072, #39960 ) ) ;
#39615=DIRECTION ( 'NONE',  ( 1.000000000000000000, 0.000000000000000000, 0.000000000000000000 ) ) ;
#39616=VECTOR ( 'NONE', #35568, 39.37007874015748143 ) ;
#39618=VERTEX_POINT ( 'NONE', #37528 ) ;
#39619=CARTESIAN_POINT ( 'NONE',  ( 1.363819533518803029, 0.000000000000000000, -1.732283464566923170 ) ) ;
#39620=CARTESIAN_POINT ( 'NONE',  ( -1.166969139818016199, 3.267716535433071279, 1.535433070866133232 ) ) ;
#39621=PLANE ( 'NONE',  #9849 ) ;
#39622=CARTESIAN_POINT ( 'NONE',  ( -0.5455278134075214336, 0.000000000000000000, -0.8267716535433049518 ) ) ;
#39623=ORIENTED_EDGE ( 'NONE', *, *, #44063, .F. ) ;
#39624=VERTEX_POINT ( 'NONE', #17137 ) ;
#39626=DIRECTION ( 'NONE',  ( 1.000000000000000000, 0.000000000000000000, 0.000000000000000000 ) ) ;
#39627=EDGE_LOOP ( 'NONE', ( #1913, #25990, #43658, #2458 ) ) ;
#39628=CARTESIAN_POINT ( 'NONE',  ( 0.2727639067037604392, 3.346456692913386100, -0.9842519685039348154 ) ) ;
#39629=PLANE ( 'NONE',  #23573 ) ;
#39630=LINE ( 'NONE', #4258, #31858 ) ;
#39631=DIRECTION ( 'NONE',  ( 1.000000000000000000, 0.000000000000000000, 0.000000000000000000 ) ) ;
#39636=ADVANCED_FACE ( 'NONE', ( #37273 ), #36758, .F. ) ;
#39637=CARTESIAN_POINT ( 'NONE',  ( 1.091055626815042645, 3.267716535433071279, 1.259842519685033357 ) ) ;
#39638=DIRECTION ( 'NONE',  ( 1.734723475976806848E-16, 0.000000000000000000, 1.000000000000000000 ) ) ;
#39639=FACE_BOUND ( 'NONE', #27429, .T. ) ;
#39640=ORIENTED_EDGE ( 'NONE', *, *, #22020, .T. ) ;
#39645=EDGE_CURVE ( 'NONE', #2869, #25971, #45487, .T. ) ;
#39646=VECTOR ( 'NONE', #39473, 39.37007874015748143 ) ;
#39648=ADVANCED_FACE ( 'NONE', ( #25381 ), #28741, .F. ) ;
#39649=EDGE_CURVE ( 'NONE', #41521, #28822, #5249, .T. ) ;
#39650=ORIENTED_EDGE ( 'NONE', *, *, #12575, .T. ) ;
#39653=ORIENTED_EDGE ( 'NONE', *, *, #47301, .T. ) ;
#39654=ADVANCED_FACE ( 'NONE', ( #33149 ), #29252, .F. ) ;
#39659=PLANE ( 'NONE',  #16541 ) ;
#39660=DIRECTION ( 'NONE',  ( -0.000000000000000000, 1.000000000000000000, -0.000000000000000000 ) ) ;
#39661=DIRECTION ( 'NONE',  ( 0.000000000000000000, -1.000000000000000000, 0.000000000000000000 ) ) ;
#39662=ORIENTED_EDGE ( 'NONE', *, *, #16059, .F. ) ;
#39663=CARTESIAN_POINT ( 'NONE',  ( 0.000000000000000000, 3.267716535433071279, 1.535433070866133898 ) ) ;
#39664=CARTESIAN_POINT ( 'NONE',  ( -1.439733046521776583, 3.346456692913386100, -1.259842519685034468 ) ) ;
#39666=EDGE_CURVE ( 'NONE', #2104, #13220, #48581, .T. ) ;
#39668=CARTESIAN_POINT ( 'NONE',  ( 1.363819533518803029, 0.000000000000000000, -1.299212598425193210 ) ) ;
#39669=LINE ( 'NONE', #47882, #40124 ) ;
#39670=EDGE_LOOP ( 'NONE', ( #45304, #27555, #19607, #19311, #12554 ) ) ;
#39671=CARTESIAN_POINT ( 'NONE',  ( 1.909347346926324018, 3.346456692913386100, -0.8893194486674360633 ) ) ;
#39673=EDGE_CURVE ( 'NONE', #21081, #40619, #1380, .T. ) ;
#39675=EDGE_CURVE ( 'NONE', #10342, #34149, #1119, .T. ) ;
#39677=CIRCLE ( 'NONE', #1752, 2.106299212598425008 ) ;
#39678=ORIENTED_EDGE ( 'NONE', *, *, #22081, .F. ) ;
#39679=LINE ( 'NONE', #28308, #47000 ) ;
#39680=DIRECTION ( 'NONE',  ( 1.000000000000000000, -0.000000000000000000, 0.000000000000000000 ) ) ;
#39681=VECTOR ( 'NONE', #40953, 39.37007874015748143 ) ;
#39682=AXIS2_PLACEMENT_3D ( 'NONE', #45954, #38249, #7942 ) ;
#39684=LINE ( 'NONE', #27795, #46554 ) ;
#39686=VERTEX_POINT ( 'NONE', #9382 ) ;
#39687=ORIENTED_EDGE ( 'NONE', *, *, #20683, .F. ) ;
#39689=ORIENTED_EDGE ( 'NONE', *, *, #24784, .T. ) ;
#39691=VECTOR ( 'NONE', #41299, 39.37007874015748143 ) ;
#39693=VERTEX_POINT ( 'NONE', #21261 ) ;
#39694=DIRECTION ( 'NONE',  ( 0.000000000000000000, -1.000000000000000000, 0.000000000000000000 ) ) ;
#39696=VERTEX_POINT ( 'NONE', #37019 ) ;
#39697=DIRECTION ( 'NONE',  ( -1.000000000000000000, 0.000000000000000000, -0.000000000000000000 ) ) ;
#39700=CARTESIAN_POINT ( 'NONE',  ( 1.091055626815042423, 3.346456692913386100, -1.259842519685035134 ) ) ;
#39701=VERTEX_POINT ( 'NONE', #1634 ) ;
#39703=CARTESIAN_POINT ( 'NONE',  ( 1.015142113812069091, 0.000000000000000000, -1.417322834645664331 ) ) ;
#39706=ORIENTED_EDGE ( 'NONE', *, *, #32283, .T. ) ;
#39708=DIRECTION ( 'NONE',  ( -3.469446951953613696E-16, 0.000000000000000000, -1.000000000000000000 ) ) ;
#39709=EDGE_CURVE ( 'NONE', #9214, #1425, #45233, .T. ) ;
#39711=ORIENTED_EDGE ( 'NONE', *, *, #3413, .F. ) ;
#39712=LINE ( 'NONE', #8475, #39429 ) ;
#39713=ORIENTED_EDGE ( 'NONE', *, *, #39768, .F. ) ;
#39714=DIRECTION ( 'NONE',  ( 1.000000000000000000, 0.000000000000000000, -3.469446951953613696E-16 ) ) ;
#39715=AXIS2_PLACEMENT_3D ( 'NONE', #10065, #9813, #41556 ) ;
#39716=DIRECTION ( 'NONE',  ( 1.000000000000000000, 0.000000000000000000, 0.000000000000000000 ) ) ;
#39717=VECTOR ( 'NONE', #39386, 39.37007874015748143 ) ;
#39718=DIRECTION ( 'NONE',  ( -1.000000000000000000, -0.000000000000000000, -0.000000000000000000 ) ) ;
#39719=ORIENTED_EDGE ( 'NONE', *, *, #26152, .T. ) ;
#39720=ORIENTED_EDGE ( 'NONE', *, *, #21417, .T. ) ;
#39721=VECTOR ( 'NONE', #7872, 39.37007874015748143 ) ;
#39722=LINE ( 'NONE', #43833, #3052 ) ;
#39723=DIRECTION ( 'NONE',  ( -3.469446951953613696E-16, 0.000000000000000000, -1.000000000000000000 ) ) ;
#39724=LINE ( 'NONE', #40242, #42302 ) ;
#39725=VECTOR ( 'NONE', #17237, 39.37007874015748143 ) ;
#39726=EDGE_CURVE ( 'NONE', #2108, #29370, #45997, .T. ) ;
#39728=DIRECTION ( 'NONE',  ( -0.000000000000000000, 1.000000000000000000, -0.000000000000000000 ) ) ;
#39730=EDGE_CURVE ( 'NONE', #46927, #29618, #41645, .T. ) ;
#39731=CARTESIAN_POINT ( 'NONE',  ( -1.439733046521776139, 0.000000000000000000, 1.259842519685033357 ) ) ;
#39732=VERTEX_POINT ( 'NONE', #46493 ) ;
#39734=EDGE_CURVE ( 'NONE', #43301, #48914, #2654, .T. ) ;
#39735=ORIENTED_EDGE ( 'NONE', *, *, #36057, .T. ) ;
#39737=EDGE_CURVE ( 'NONE', #9639, #39686, #25718, .T. ) ;
#39739=VERTEX_POINT ( 'NONE', #6540 ) ;
#39742=CARTESIAN_POINT ( 'NONE',  ( 1.770012363201889594, 3.346456692913386100, -1.141732283464564013 ) ) ;
#39745=EDGE_LOOP ( 'NONE', ( #50097, #13968, #9597, #49182 ) ) ;
#39748=DIRECTION ( 'NONE',  ( -0.000000000000000000, 1.000000000000000000, -0.000000000000000000 ) ) ;
#39749=FACE_OUTER_BOUND ( 'NONE', #7089, .T. ) ;
#39755=LINE ( 'NONE', #4650, #27611 ) ;
#39756=DIRECTION ( 'NONE',  ( -0.000000000000000000, 1.000000000000000000, -0.000000000000000000 ) ) ;
#39757=FACE_BOUND ( 'NONE', #20904, .T. ) ;
#39758=VECTOR ( 'NONE', #8693, 39.37007874015748143 ) ;
#39763=LINE ( 'NONE', #4144, #22475 ) ;
#39764=EDGE_CURVE ( 'NONE', #31670, #36537, #22029, .T. ) ;
#39765=ADVANCED_FACE ( 'NONE', ( #18404 ), #34160, .F. ) ;
#39766=ORIENTED_EDGE ( 'NONE', *, *, #24074, .T. ) ;
#39767=ORIENTED_EDGE ( 'NONE', *, *, #14425, .T. ) ;
#39768=EDGE_CURVE ( 'NONE', #28846, #35081, #3455, .T. ) ;
#39769=ORIENTED_EDGE ( 'NONE', *, *, #4111, .T. ) ;
#39773=CARTESIAN_POINT ( 'NONE',  ( -1.091055626815042645, 3.346456692913386100, 1.692913385826762873 ) ) ;
#39774=DIRECTION ( 'NONE',  ( -0.000000000000000000, 1.000000000000000000, -0.000000000000000000 ) ) ;
#39778=PLANE ( 'NONE',  #38666 ) ;
#39779=DIRECTION ( 'NONE',  ( -0.000000000000000000, 1.000000000000000000, -0.000000000000000000 ) ) ;
#39780=VERTEX_POINT ( 'NONE', #26894 ) ;
#39781=CARTESIAN_POINT ( 'NONE',  ( -1.486187880958815377, 3.346456692913386100, -1.574803149606293307 ) ) ;
#39782=PLANE ( 'NONE',  #20657 ) ;
#39784=ADVANCED_FACE ( 'NONE', ( #46244 ), #26397, .F. ) ;
#39786=LINE ( 'NONE', #43646, #11855 ) ;
#39787=LINE ( 'NONE', #20155, #2166 ) ;
#39789=PLANE ( 'NONE',  #5277 ) ;
#39791=EDGE_CURVE ( 'NONE', #3695, #4193, #6782, .T. ) ;
#39792=VECTOR ( 'NONE', #15074, 39.37007874015748143 ) ;
#39793=ORIENTED_EDGE ( 'NONE', *, *, #20707, .T. ) ;
#39794=VECTOR ( 'NONE', #29756, 39.37007874015748143 ) ;
#39795=ORIENTED_EDGE ( 'NONE', *, *, #44790, .F. ) ;
#39796=VECTOR ( 'NONE', #6207, 39.37007874015748143 ) ;
#39798=CARTESIAN_POINT ( 'NONE',  ( 0.5455278134075213226, 3.267716535433071279, -9.463399047163224412E-17 ) ) ;
#39801=ORIENTED_EDGE ( 'NONE', *, *, #9588, .T. ) ;
#39802=CARTESIAN_POINT ( 'NONE',  ( 0.000000000000000000, 3.267716535433071279, -0.3149606299212596716 ) ) ;
#39803=VERTEX_POINT ( 'NONE', #42645 ) ;
#39804=DIRECTION ( 'NONE',  ( -3.469446951953613696E-16, 0.000000000000000000, -1.000000000000000000 ) ) ;
#39805=EDGE_LOOP ( 'NONE', ( #31208, #2830, #35970, #35479 ) ) ;
#39808=CARTESIAN_POINT ( 'NONE',  ( -1.166969139818015977, 0.000000000000000000, -1.732283464566922726 ) ) ;
#39809=VERTEX_POINT ( 'NONE', #34409 ) ;
#39810=ORIENTED_EDGE ( 'NONE', *, *, #17814, .T. ) ;
#39813=CARTESIAN_POINT ( 'NONE',  ( 0.000000000000000000, 3.267716535433071279, 0.4330708661417287386 ) ) ;
#39815=ORIENTED_EDGE ( 'NONE', *, *, #621, .T. ) ;
#39816=CARTESIAN_POINT ( 'NONE',  ( -0.3486774197067334380, 3.267716535433071279, 1.889763779527550369 ) ) ;
#39817=DIRECTION ( 'NONE',  ( -0.000000000000000000, 1.000000000000000000, -0.000000000000000000 ) ) ;
#39818=CARTESIAN_POINT ( 'NONE',  ( 2.052631463899901920, 3.267716535433071279, -0.4724409448818889246 ) ) ;
#39819=ORIENTED_EDGE ( 'NONE', *, *, #4548, .T. ) ;
#39821=DIRECTION ( 'NONE',  ( 0.000000000000000000, 0.000000000000000000, -1.000000000000000000 ) ) ;
#39827=EDGE_CURVE ( 'NONE', #6728, #49076, #22785, .T. ) ;
#39828=VERTEX_POINT ( 'NONE', #3157 ) ;
#39830=DIRECTION ( 'NONE',  ( -3.469446951953613696E-16, 0.000000000000000000, -1.000000000000000000 ) ) ;
#39832=ORIENTED_EDGE ( 'NONE', *, *, #16059, .T. ) ;
#39833=PLANE ( 'NONE',  #35335 ) ;
#39834=CARTESIAN_POINT ( 'NONE',  ( -1.363819533518803473, 0.000000000000000000, -1.929133858267710000 ) ) ;
#39836=VECTOR ( 'NONE', #15013, 39.37007874015748143 ) ;
#39837=VECTOR ( 'NONE', #6400, 39.37007874015748143 ) ;
#39842=PLANE ( 'NONE',  #50971 ) ;
#39843=EDGE_LOOP ( 'NONE', ( #41051, #35379, #4535, #10200 ) ) ;
#39845=VECTOR ( 'NONE', #7161, 39.37007874015748143 ) ;
#39846=ORIENTED_EDGE ( 'NONE', *, *, #18290, .F. ) ;
#39847=DIRECTION ( 'NONE',  ( 1.000000000000000000, 0.000000000000000000, -3.469446951953613696E-16 ) ) ;
#39848=DIRECTION ( 'NONE',  ( -0.000000000000000000, 1.000000000000000000, -0.000000000000000000 ) ) ;
#39849=ADVANCED_FACE ( 'NONE', ( #17555 ), #26063, .F. ) ;
#39850=DIRECTION ( 'NONE',  ( -3.469446951953613696E-16, 0.000000000000000000, -1.000000000000000000 ) ) ;
#39852=CARTESIAN_POINT ( 'NONE',  ( 0.000000000000000000, 3.267716535433071279, 0.1574803149606286423 ) ) ;
#39855=ADVANCED_FACE ( 'NONE', ( #29163 ), #1293, .F. ) ;
#39856=LINE ( 'NONE', #4748, #33138 ) ;
#39857=ORIENTED_EDGE ( 'NONE', *, *, #2853, .F. ) ;
#39859=CARTESIAN_POINT ( 'NONE',  ( 1.363819533518803251, 0.000000000000000000, -0.3543307086614178592 ) ) ;
#39860=DIRECTION ( 'NONE',  ( 1.000000000000000000, 0.000000000000000000, 0.000000000000000000 ) ) ;
#39861=EDGE_CURVE ( 'NONE', #12697, #42646, #26207, .T. ) ;
#39862=ORIENTED_EDGE ( 'NONE', *, *, #41634, .T. ) ;
#39866=VECTOR ( 'NONE', #19118, 39.37007874015748143 ) ;
#39867=VERTEX_POINT ( 'NONE', #18070 ) ;
#39868=AXIS2_PLACEMENT_3D ( 'NONE', #32196, #24948, #47885 ) ;
#39869=CARTESIAN_POINT ( 'NONE',  ( 0.8182917201112819283, 3.346456692913386100, 0.4724409448818868706 ) ) ;
#39870=DIRECTION ( 'NONE',  ( -1.000000000000000000, 0.000000000000000000, 1.734723475976806848E-16 ) ) ;
#39871=VERTEX_POINT ( 'NONE', #45403 ) ;
#39872=CARTESIAN_POINT ( 'NONE',  ( -0.5455278134075208785, 3.346456692913386100, 1.062992125984246083 ) ) ;
#39873=EDGE_CURVE ( 'NONE', #23012, #15854, #44900, .T. ) ;
#39874=VECTOR ( 'NONE', #31980, 39.37007874015748143 ) ;
#39875=VECTOR ( 'NONE', #28477, 39.37007874015748143 ) ;
#39876=FACE_OUTER_BOUND ( 'NONE', #26293, .T. ) ;
#39878=DIRECTION ( 'NONE',  ( 1.000000000000000000, 0.000000000000000000, -3.469446951953613696E-16 ) ) ;
#39879=ORIENTED_EDGE ( 'NONE', *, *, #15908, .T. ) ;
#39880=ORIENTED_EDGE ( 'NONE', *, *, #16760, .T. ) ;
#39881=DIRECTION ( 'NONE',  ( -3.469446951953613696E-16, 0.000000000000000000, -1.000000000000000000 ) ) ;
#39882=VECTOR ( 'NONE', #42202, 39.37007874015748143 ) ;
#39883=DIRECTION ( 'NONE',  ( -3.469446951953613696E-16, 0.000000000000000000, -1.000000000000000000 ) ) ;
#39885=CARTESIAN_POINT ( 'NONE',  ( 1.091055626815042645, 0.000000000000000000, -0.3149606299212596716 ) ) ;
#39886=LINE ( 'NONE', #27744, #34324 ) ;
#39889=VERTEX_POINT ( 'NONE', #25552 ) ;
#39892=DIRECTION ( 'NONE',  ( -0.000000000000000000, 1.000000000000000000, -0.000000000000000000 ) ) ;
#39893=LINE ( 'NONE', #43747, #18925 ) ;
#39895=FACE_BOUND ( 'NONE', #26697, .T. ) ;
#39899=EDGE_LOOP ( 'NONE', ( #6801, #31735, #46231, #3686 ) ) ;
#39904=ORIENTED_EDGE ( 'NONE', *, *, #36468, .T. ) ;
#39905=DIRECTION ( 'NONE',  ( -1.000000000000000000, 0.000000000000000000, 1.734723475976806848E-16 ) ) ;
#39908=AXIS2_PLACEMENT_3D ( 'NONE', #15641, #41809, #18311 ) ;
#39910=VECTOR ( 'NONE', #34043, 39.37007874015748143 ) ;
#39911=CARTESIAN_POINT ( 'NONE',  ( 0.2727639067037604947, 0.000000000000000000, -0.7874015748031473194 ) ) ;
#39915=CIRCLE ( 'NONE', #1997, 2.165354330708661568 ) ;
#39916=DIRECTION ( 'NONE',  ( -3.469446951953613696E-16, 0.000000000000000000, -1.000000000000000000 ) ) ;
#39920=ORIENTED_EDGE ( 'NONE', *, *, #21141, .F. ) ;
#39921=DIRECTION ( 'NONE',  ( 1.734723475976806848E-16, 0.000000000000000000, 1.000000000000000000 ) ) ;
#39922=LINE ( 'NONE', #19019, #15281 ) ;
#39923=FACE_OUTER_BOUND ( 'NONE', #15600, .T. ) ;
#39924=ORIENTED_EDGE ( 'NONE', *, *, #37414, .F. ) ;
#39925=FACE_OUTER_BOUND ( 'NONE', #23243, .T. ) ;
#39927=ORIENTED_EDGE ( 'NONE', *, *, #49519, .T. ) ;
#39928=CARTESIAN_POINT ( 'NONE',  ( 0.2727639067037604947, 0.000000000000000000, -0.4724409448818886470 ) ) ;
#39934=CARTESIAN_POINT ( 'NONE',  ( 0.8182917201112821504, 3.267716535433071279, -1.419509857074483539E-16 ) ) ;
#39935=ADVANCED_FACE ( 'NONE', ( #2317 ), #9557, .F. ) ;
#39937=LINE ( 'NONE', #1208, #5308 ) ;
#39941=PRODUCT_DEFINITION_FORMATION_WITH_SPECIFIED_SOURCE ( 'ANY', '', #35980, .NOT_KNOWN. ) ;
#39942=ORIENTED_EDGE ( 'NONE', *, *, #49143, .F. ) ;
#39943=VERTEX_POINT ( 'NONE', #33063 ) ;
#39944=AXIS2_PLACEMENT_3D ( 'NONE', #29826, #41700, #6337 ) ;
#39947=EDGE_CURVE ( 'NONE', #30279, #18986, #49262, .T. ) ;
#39949=LINE ( 'NONE', #30935, #38454 ) ;
#39950=ORIENTED_EDGE ( 'NONE', *, *, #5922, .F. ) ;
#39951=EDGE_CURVE ( 'NONE', #46754, #37143, #32811, .T. ) ;
#39953=CARTESIAN_POINT ( 'NONE',  ( 0.7423782071083084855, 3.346456692913386100, -2.034117492951036166 ) ) ;
#39954=ORIENTED_EDGE ( 'NONE', *, *, #2477, .T. ) ;
#39955=DIRECTION ( 'NONE',  ( 0.000000000000000000, 0.000000000000000000, -1.000000000000000000 ) ) ;
#39958=VERTEX_POINT ( 'NONE', #49507 ) ;
#39959=DIRECTION ( 'NONE',  ( -0.000000000000000000, 1.000000000000000000, -0.000000000000000000 ) ) ;
#39960=ORIENTED_EDGE ( 'NONE', *, *, #43118, .F. ) ;
#39962=DIRECTION ( 'NONE',  ( -0.000000000000000000, 1.000000000000000000, -0.000000000000000000 ) ) ;
#39963=EDGE_LOOP ( 'NONE', ( #38832, #33928, #10619, #48680 ) ) ;
#39964=VERTEX_POINT ( 'NONE', #17055 ) ;
#39965=EDGE_CURVE ( 'NONE', #37644, #39618, #17307, .T. ) ;
#39967=LINE ( 'NONE', #4094, #10820 ) ;
#39968=EDGE_CURVE ( 'NONE', #20299, #8395, #22448, .T. ) ;
#39969=PLANE ( 'NONE',  #6461 ) ;
#39970=EDGE_LOOP ( 'NONE', ( #46542, #48424, #29440, #7969 ) ) ;
#39973=DIRECTION ( 'NONE',  ( -0.000000000000000000, 1.000000000000000000, -0.000000000000000000 ) ) ;
#39974=CARTESIAN_POINT ( 'NONE',  ( -0.5455278134075211005, 3.267716535433071279, 9.463399047163218249E-17 ) ) ;
#39976=VERTEX_POINT ( 'NONE', #42065 ) ;
#39977=ORIENTED_EDGE ( 'NONE', *, *, #39068, .T. ) ;
#39979=DIRECTION ( 'NONE',  ( 1.734723475976806848E-16, -0.000000000000000000, 1.000000000000000000 ) ) ;
#39980=FACE_OUTER_BOUND ( 'NONE', #11489, .T. ) ;
#39983=VECTOR ( 'NONE', #35243, 39.37007874015748143 ) ;
#39984=LINE ( 'NONE', #47687, #44599 ) ;
#39987=ADVANCED_FACE ( 'NONE', ( #26562 ), #50017, .F. ) ;
#39988=CARTESIAN_POINT ( 'NONE',  ( 0.000000000000000000, 3.267716535433071279, 0.2755905511810996522 ) ) ;
#39990=ORIENTED_EDGE ( 'NONE', *, *, #12328, .T. ) ;
#39991=DIRECTION ( 'NONE',  ( 1.000000000000000000, 0.000000000000000000, 0.000000000000000000 ) ) ;
#39992=ORIENTED_EDGE ( 'NONE', *, *, #39245, .F. ) ;
#39994=CARTESIAN_POINT ( 'NONE',  ( 1.015142113812069313, 3.267716535433071279, -0.1574803149606301411 ) ) ;
#39995=DIRECTION ( 'NONE',  ( -0.000000000000000000, 1.000000000000000000, -0.000000000000000000 ) ) ;
#39996=EDGE_CURVE ( 'NONE', #9706, #26586, #24281, .T. ) ;
#39997=PLANE ( 'NONE',  #44868 ) ;
#40003=FACE_BOUND ( 'NONE', #46343, .T. ) ;
#40004=ORIENTED_EDGE ( 'NONE', *, *, #26626, .T. ) ;
#40005=DIRECTION ( 'NONE',  ( 1.000000000000000000, 0.000000000000000000, 0.000000000000000000 ) ) ;
#40006=EDGE_LOOP ( 'NONE', ( #10663, #43743, #12279, #36414 ) ) ;
#40008=CARTESIAN_POINT ( 'NONE',  ( -0.5455278134075214336, 0.000000000000000000, -1.771653543307081025 ) ) ;
#40009=CARTESIAN_POINT ( 'NONE',  ( 1.363819533518803251, 3.267716535433071279, 0.7874015748031454320 ) ) ;
#40010=AXIS2_PLACEMENT_3D ( 'NONE', #32767, #48446, #13133 ) ;
#40011=EDGE_LOOP ( 'NONE', ( #50259, #7048, #8721, #46618, #31009 ) ) ;
#40012=ORIENTED_EDGE ( 'NONE', *, *, #5828, .T. ) ;
#40014=CARTESIAN_POINT ( 'NONE',  ( 1.287906020515830141, 3.346456692913386100, 0.7480314960629872445 ) ) ;
#40016=CARTESIAN_POINT ( 'NONE',  ( 0.000000000000000000, 3.267716535433071279, -0.7874015748031470974 ) ) ;
#40019=EDGE_CURVE ( 'NONE', #41514, #272, #18576, .T. ) ;
#40020=DIRECTION ( 'NONE',  ( 1.000000000000000000, -0.000000000000000000, 0.000000000000000000 ) ) ;
#40022=ORIENTED_EDGE ( 'NONE', *, *, #5295, .F. ) ;
#40025=VECTOR ( 'NONE', #2234, 39.37007874015748143 ) ;
#40030=VERTEX_POINT ( 'NONE', #50262 ) ;
#40033=CARTESIAN_POINT ( 'NONE',  ( -0.5455278134075208785, 0.000000000000000000, 0.9448818897637749625 ) ) ;
#40037=DIRECTION ( 'NONE',  ( 1.734723475976806848E-16, 0.000000000000000000, 1.000000000000000000 ) ) ;
#40038=CARTESIAN_POINT ( 'NONE',  ( -0.6214413264104939882, 3.346456692913386100, 1.732283464566921172 ) ) ;
#40039=CARTESIAN_POINT ( 'NONE',  ( -0.2727639067037608278, 0.000000000000000000, -0.6692913385826758654 ) ) ;
#40040=LINE ( 'NONE', #19383, #27608 ) ;
#40041=DIRECTION ( 'NONE',  ( 1.734723475976806848E-16, 0.000000000000000000, 1.000000000000000000 ) ) ;
#40042=DIRECTION ( 'NONE',  ( -0.000000000000000000, 0.000000000000000000, 1.000000000000000000 ) ) ;
#40043=CARTESIAN_POINT ( 'NONE',  ( 0.000000000000000000, 3.267716535433071279, 0.000000000000000000 ) ) ;
#40045=ORIENTED_EDGE ( 'NONE', *, *, #37478, .F. ) ;
#40048=CARTESIAN_POINT ( 'NONE',  ( -0.2727639067037607723, 3.346456692913386100, -1.102362204724405714 ) ) ;
#40050=ORIENTED_EDGE ( 'NONE', *, *, #13134, .T. ) ;
#40052=EDGE_LOOP ( 'NONE', ( #21714, #26864, #22826, #13896, #135, #31045, #16181, #41915, #42316, #7638, #44965, #27032, #29267, #24080, #48665, #43035, #5807, #30149, #13513, #10854, #15030, #25174, #49376, #38834 ) ) ;
#40053=DIRECTION ( 'NONE',  ( 1.000000000000000000, -0.000000000000000000, 0.000000000000000000 ) ) ;
#40056=EDGE_CURVE ( 'NONE', #17956, #18819, #30452, .T. ) ;
#40057=VECTOR ( 'NONE', #17365, 39.37007874015748143 ) ;
#40058=ORIENTED_EDGE ( 'NONE', *, *, #50443, .T. ) ;
#40059=EDGE_CURVE ( 'NONE', #39624, #5523, #22200, .T. ) ;
#40060=AXIS2_PLACEMENT_3D ( 'NONE', #50242, #14427, #25786 ) ;
#40062=ORIENTED_EDGE ( 'NONE', *, *, #34627, .T. ) ;
#40063=CARTESIAN_POINT ( 'NONE',  ( -0.8182917201112814842, 0.000000000000000000, 1.220472440944875281 ) ) ;
#40065=DIRECTION ( 'NONE',  ( 1.734723475976806848E-16, 0.000000000000000000, 1.000000000000000000 ) ) ;
#40066=ORIENTED_EDGE ( 'NONE', *, *, #16524, .T. ) ;
#40067=DIRECTION ( 'NONE',  ( 1.734723475976806848E-16, -0.000000000000000000, 1.000000000000000000 ) ) ;
#40068=DIRECTION ( 'NONE',  ( -1.000000000000000000, 0.000000000000000000, -0.000000000000000000 ) ) ;
#40069=CARTESIAN_POINT ( 'NONE',  ( 0.000000000000000000, 3.267716535433071279, 0.000000000000000000 ) ) ;
#40070=VERTEX_POINT ( 'NONE', #42567 ) ;
#40072=EDGE_LOOP ( 'NONE', ( #44735, #1116, #44117, #1525 ) ) ;
#40077=CARTESIAN_POINT ( 'NONE',  ( 0.000000000000000000, 3.346456692913386100, 0.000000000000000000 ) ) ;
#40079=EDGE_CURVE ( 'NONE', #31299, #48104, #26316, .T. ) ;
#40083=DIRECTION ( 'NONE',  ( 1.734723475976806848E-16, -0.000000000000000000, 1.000000000000000000 ) ) ;
#40086=ORIENTED_EDGE ( 'NONE', *, *, #9406, .T. ) ;
#40087=PLANE ( 'NONE',  #26555 ) ;
#40088=LINE ( 'NONE', #48298, #47453 ) ;
#40090=ORIENTED_EDGE ( 'NONE', *, *, #28302, .T. ) ;
#40094=ORIENTED_EDGE ( 'NONE', *, *, #18103, .T. ) ;
#40097=( NAMED_UNIT ( * ) PLANE_ANGLE_UNIT ( ) SI_UNIT ( $, .RADIAN. ) );
#40098=EDGE_CURVE ( 'NONE', #16054, #46917, #11328, .T. ) ;
#40099=VECTOR ( 'NONE', #13546, 39.37007874015748143 ) ;
#40100=LINE ( 'NONE', #47798, #37970 ) ;
#40101=VECTOR ( 'NONE', #39578, 39.37007874015748143 ) ;
#40105=EDGE_LOOP ( 'NONE', ( #17133, #20395, #26398, #38237 ) ) ;
#40106=AXIS2_PLACEMENT_3D ( 'NONE', #31633, #38623, #19492 ) ;
#40107=CARTESIAN_POINT ( 'NONE',  ( -1.536664496436148184E-16, 0.000000000000000000, -0.8267716535433052849 ) ) ;
#40110=PLANE ( 'NONE',  #27728 ) ;
#40111=CARTESIAN_POINT ( 'NONE',  ( -1.732283464566932052, 3.346456692913386100, -1.299212598425193210 ) ) ;
#40113=CARTESIAN_POINT ( 'NONE',  ( -1.536664496436148184E-16, 0.000000000000000000, -1.456692913385822630 ) ) ;
#40114=PLANE ( 'NONE',  #21111 ) ;
#40115=DIRECTION ( 'NONE',  ( 1.000000000000000000, -0.000000000000000000, 0.000000000000000000 ) ) ;
#40119=ORIENTED_EDGE ( 'NONE', *, *, #7719, .T. ) ;
#40121=LINE ( 'NONE', #4752, #43453 ) ;
#40122=CARTESIAN_POINT ( 'NONE',  ( -0.07591351300297337346, 3.267716535433071279, 2.633779063002570064E-17 ) ) ;
#40123=ORIENTED_EDGE ( 'NONE', *, *, #30176, .T. ) ;
#40124=VECTOR ( 'NONE', #28553, 39.37007874015748143 ) ;
#40126=CARTESIAN_POINT ( 'NONE',  ( -0.5455278134075214336, 0.000000000000000000, -8.878505979408855953E-16 ) ) ;
#40127=LINE ( 'NONE', #27984, #46471 ) ;
#40128=ADVANCED_FACE ( 'NONE', ( #47669 ), #39969, .F. ) ;
#40129=AXIS2_PLACEMENT_3D ( 'NONE', #2262, #21884, #6396 ) ;
#40131=VECTOR ( 'NONE', #15340, 39.37007874015748143 ) ;
#40132=ORIENTED_EDGE ( 'NONE', *, *, #12990, .F. ) ;
#40133=FACE_BOUND ( 'NONE', #3950, .T. ) ;
#40134=DIRECTION ( 'NONE',  ( -0.000000000000000000, 0.000000000000000000, 1.000000000000000000 ) ) ;
#40135=ORIENTED_EDGE ( 'NONE', *, *, #12138, .F. ) ;
#40136=EDGE_CURVE ( 'NONE', #25127, #23961, #9437, .T. ) ;
#40138=EDGE_CURVE ( 'NONE', #12457, #35559, #35584, .T. ) ;
#40139=LINE ( 'NONE', #20759, #17733 ) ;
#40140=CARTESIAN_POINT ( 'NONE',  ( 0.7423782071083091516, 3.346456692913386100, 1.692913385826762873 ) ) ;
#40142=CIRCLE ( 'NONE', #12905, 2.106299212598425008 ) ;
#40147=EDGE_LOOP ( 'NONE', ( #10306, #17568, #40182, #23289 ) ) ;
#40149=LINE ( 'NONE', #20252, #1534 ) ;
#40150=ORIENTED_EDGE ( 'NONE', *, *, #45364, .F. ) ;
#40152=CARTESIAN_POINT ( 'NONE',  ( 1.833433833923351353, 0.000000000000000000, 0.6299212598425164567 ) ) ;
#40154=CARTESIAN_POINT ( 'NONE',  ( 2.100403847690402337, 3.346456692913386100, -0.1574803149606304187 ) ) ;
#40155=VERTEX_POINT ( 'NONE', #31714 ) ;
#40157=ADVANCED_FACE ( 'NONE', ( #35333 ), #27823, .F. ) ;
#40158=CARTESIAN_POINT ( 'NONE',  ( -0.5455278134075214336, 3.346456692913386100, -0.5118110236220467790 ) ) ;
#40160=DIRECTION ( 'NONE',  ( 1.734723475976806848E-16, -0.000000000000000000, 1.000000000000000000 ) ) ;
#40162=FACE_BOUND ( 'NONE', #43038, .T. ) ;
#40164=EDGE_CURVE ( 'NONE', #40553, #31330, #21315, .T. ) ;
#40166=VERTEX_POINT ( 'NONE', #12090 ) ;
#40169=AXIS2_PLACEMENT_3D ( 'NONE', #24112, #44236, #12756 ) ;
#40170=ORIENTED_EDGE ( 'NONE', *, *, #17752, .T. ) ;
#40171=ORIENTED_EDGE ( 'NONE', *, *, #6278, .F. ) ;
#40172=CARTESIAN_POINT ( 'NONE',  ( 0.000000000000000000, 0.000000000000000000, 0.000000000000000000 ) ) ;
#40173=ORIENTED_EDGE ( 'NONE', *, *, #25425, .F. ) ;
#40174=VECTOR ( 'NONE', #2711, 39.37007874015748143 ) ;
#40179=LINE ( 'NONE', #20286, #40470 ) ;
#40180=CARTESIAN_POINT ( 'NONE',  ( 0.000000000000000000, 3.267716535433071279, 0.000000000000000000 ) ) ;
#40181=DIRECTION ( 'NONE',  ( -0.000000000000000000, 1.000000000000000000, -0.000000000000000000 ) ) ;
#40182=ORIENTED_EDGE ( 'NONE', *, *, #11607, .F. ) ;
#40183=CARTESIAN_POINT ( 'NONE',  ( 0.2727639067037604392, 3.267716535433071279, -4.731699523581607892E-17 ) ) ;
#40184=VECTOR ( 'NONE', #27837, 39.37007874015748143 ) ;
#40188=CARTESIAN_POINT ( 'NONE',  ( -0.9302092402134559679, 3.267716535433071279, 1.889763779527550147 ) ) ;
#40191=EDGE_LOOP ( 'NONE', ( #5627, #31601, #5657, #20771 ) ) ;
#40193=FACE_OUTER_BOUND ( 'NONE', #30431, .T. ) ;
#40194=LINE ( 'NONE', #36578, #20214 ) ;
#40197=DIRECTION ( 'NONE',  ( -0.000000000000000000, 1.000000000000000000, -0.000000000000000000 ) ) ;
#40199=ORIENTED_EDGE ( 'NONE', *, *, #11608, .T. ) ;
#40200=FACE_BOUND ( 'NONE', #6594, .T. ) ;
#40202=DIRECTION ( 'NONE',  ( -0.000000000000000000, 1.000000000000000000, -0.000000000000000000 ) ) ;
#40204=CARTESIAN_POINT ( 'NONE',  ( 0.000000000000000000, 3.267716535433071279, -1.161035397307311917E-15 ) ) ;
#40205=EDGE_CURVE ( 'NONE', #45614, #39943, #23960, .T. ) ;
#40206=VECTOR ( 'NONE', #25105, 39.37007874015748143 ) ;
#40207=EDGE_CURVE ( 'NONE', #12462, #35716, #467, .T. ) ;
#40210=LINE ( 'NONE', #31955, #48475 ) ;
#40211=ORIENTED_EDGE ( 'NONE', *, *, #16987, .F. ) ;
#40213=EDGE_LOOP ( 'NONE', ( #26011, #36168, #10441, #39406 ) ) ;
#40214=CARTESIAN_POINT ( 'NONE',  ( 1.015142113812069757, 3.267716535433071279, -3.521981712565033375E-16 ) ) ;
#40215=EDGE_CURVE ( 'NONE', #31646, #31327, #32229, .T. ) ;
#40217=DIRECTION ( 'NONE',  ( 0.000000000000000000, 0.000000000000000000, -1.000000000000000000 ) ) ;
#40218=DIRECTION ( 'NONE',  ( -1.000000000000000000, 0.000000000000000000, 1.734723475976806848E-16 ) ) ;
#40219=ORIENTED_EDGE ( 'NONE', *, *, #33464, .T. ) ;
#40221=DIRECTION ( 'NONE',  ( -1.000000000000000000, 0.000000000000000000, 0.000000000000000000 ) ) ;
#40223=VECTOR ( 'NONE', #9705, 39.37007874015748143 ) ;
#40224=DIRECTION ( 'NONE',  ( 1.000000000000000000, -0.000000000000000000, 0.000000000000000000 ) ) ;
#40225=EDGE_CURVE ( 'NONE', #9041, #22692, #33199, .T. ) ;
#40226=ORIENTED_EDGE ( 'NONE', *, *, #14860, .T. ) ;
#40228=CARTESIAN_POINT ( 'NONE',  ( -0.5455278134075214336, 3.346456692913386100, -0.3149606299212593941 ) ) ;
#40229=ORIENTED_EDGE ( 'NONE', *, *, #27388, .T. ) ;
#40231=EDGE_CURVE ( 'NONE', #28846, #43954, #26566, .T. ) ;
#40234=LINE ( 'NONE', #4862, #17618 ) ;
#40236=VECTOR ( 'NONE', #39995, 39.37007874015748143 ) ;
#40237=CARTESIAN_POINT ( 'NONE',  ( -0.07591351300297277671, 3.267716535433071279, 1.102362204724404160 ) ) ;
#40238=ORIENTED_EDGE ( 'NONE', *, *, #4967, .T. ) ;
#40241=FACE_OUTER_BOUND ( 'NONE', #8304, .T. ) ;
#40242=CARTESIAN_POINT ( 'NONE',  ( 0.5455278134075213226, 3.267716535433071279, -9.463399047163224412E-17 ) ) ;
#40244=AXIS2_PLACEMENT_3D ( 'NONE', #2819, #42058, #11321 ) ;
#40245=PLANE ( 'NONE',  #44126 ) ;
#40247=CARTESIAN_POINT ( 'NONE',  ( -1.166969139818016199, 0.000000000000000000, -0.9842519685039344823 ) ) ;
#40248=VECTOR ( 'NONE', #40005, 39.37007874015748143 ) ;
#40251=CARTESIAN_POINT ( 'NONE',  ( -0.8942052331142552601, 0.000000000000000000, 1.889763779527550147 ) ) ;
#40252=VECTOR ( 'NONE', #29687, 39.37007874015748143 ) ;
#40253=ORIENTED_EDGE ( 'NONE', *, *, #28798, .T. ) ;
#40255=VECTOR ( 'NONE', #50584, 39.37007874015748143 ) ;
#40256=ORIENTED_EDGE ( 'NONE', *, *, #43992, .T. ) ;
#40257=EDGE_CURVE ( 'NONE', #528, #9706, #3249, .T. ) ;
#40263=EDGE_CURVE ( 'NONE', #38696, #8095, #7707, .T. ) ;
#40264=DIRECTION ( 'NONE',  ( -0.000000000000000000, 1.000000000000000000, -0.000000000000000000 ) ) ;
#40265=FACE_BOUND ( 'NONE', #20248, .T. ) ;
#40267=FACE_OUTER_BOUND ( 'NONE', #21454, .T. ) ;
#40268=ORIENTED_EDGE ( 'NONE', *, *, #25184, .F. ) ;
#40270=DIRECTION ( 'NONE',  ( -0.000000000000000000, 1.000000000000000000, -0.000000000000000000 ) ) ;
#40273=ORIENTED_EDGE ( 'NONE', *, *, #49425, .T. ) ;
#40275=DIRECTION ( 'NONE',  ( -1.000000000000000000, 0.000000000000000000, -0.000000000000000000 ) ) ;
#40278=VECTOR ( 'NONE', #35460, 39.37007874015748143 ) ;
#40281=CARTESIAN_POINT ( 'NONE',  ( -0.8182917201112814842, 0.000000000000000000, 1.417322834645662777 ) ) ;
#40282=DIRECTION ( 'NONE',  ( 1.000000000000000000, 0.000000000000000000, 0.000000000000000000 ) ) ;
#40283=EDGE_CURVE ( 'NONE', #38696, #28900, #22953, .T. ) ;
#40284=EDGE_LOOP ( 'NONE', ( #25591, #47722, #50077, #32083 ) ) ;
#40285=AXIS2_PLACEMENT_3D ( 'NONE', #23647, #42246, #11016 ) ;
#40286=LINE ( 'NONE', #20131, #24943 ) ;
#40287=VERTEX_POINT ( 'NONE', #4098 ) ;
#40288=ORIENTED_EDGE ( 'NONE', *, *, #3987, .F. ) ;
#40289=VECTOR ( 'NONE', #18476, 39.37007874015748143 ) ;
#40291=VERTEX_POINT ( 'NONE', #208 ) ;
#40293=LINE ( 'NONE', #2072, #241 ) ;
#40297=CARTESIAN_POINT ( 'NONE',  ( -0.3486774197067339376, 0.000000000000000000, -1.574803149606293529 ) ) ;
#40300=VERTEX_POINT ( 'NONE', #46910 ) ;
#40302=DIRECTION ( 'NONE',  ( -3.469446951953613696E-16, 0.000000000000000000, -1.000000000000000000 ) ) ;
#40303=PLANE ( 'NONE',  #38160 ) ;
#40304=CARTESIAN_POINT ( 'NONE',  ( 1.091055626815043311, 0.000000000000000000, 1.377952755905504256 ) ) ;
#40305=CARTESIAN_POINT ( 'NONE',  ( 1.015142113812069091, 3.346456692913386100, -1.614173228346451605 ) ) ;
#40306=CARTESIAN_POINT ( 'NONE',  ( -0.5455278134075208785, 3.346456692913386100, 1.692913385826762873 ) ) ;
#40308=CONICAL_SURFACE ( 'NONE', #32054, 2.422428857167389982, 0.4363323129985800519 ) ;
#40309=EDGE_CURVE ( 'NONE', #35147, #16704, #30954, .T. ) ;
#40310=PLANE ( 'NONE',  #17660 ) ;
#40311=LINE ( 'NONE', #6657, #29398 ) ;
#40312=EDGE_LOOP ( 'NONE', ( #10288, #9024, #40741, #29671 ) ) ;
#40314=CARTESIAN_POINT ( 'NONE',  ( 0.2727639067037604392, 0.000000000000000000, -0.3543307086614173040 ) ) ;
#40316=ORIENTED_EDGE ( 'NONE', *, *, #44150, .F. ) ;
#40317=EDGE_CURVE ( 'NONE', #15064, #40389, #42814, .T. ) ;
#40318=VERTEX_POINT ( 'NONE', #19821 ) ;
#40319=VECTOR ( 'NONE', #18693, 39.37007874015748143 ) ;
#40321=CARTESIAN_POINT ( 'NONE',  ( 1.928732080931637505, 3.346456692913386100, -0.9842519685039348154 ) ) ;
#40322=PLANE ( 'NONE',  #14659 ) ;
#40326=EDGE_CURVE ( 'NONE', #20192, #6756, #42569, .T. ) ;
#40327=AXIS2_PLACEMENT_3D ( 'NONE', #35653, #46726, #27894 ) ;
#40328=EDGE_LOOP ( 'NONE', ( #7140, #36397, #3053, #35675 ) ) ;
#40329=CARTESIAN_POINT ( 'NONE',  ( -0.5455278134075214336, 0.000000000000000000, -0.9448818897637762948 ) ) ;
#40333=ORIENTED_EDGE ( 'NONE', *, *, #5198, .F. ) ;
#40336=CARTESIAN_POINT ( 'NONE',  ( -2.103998301714549157, 3.346456692913386100, -0.5118110236220464460 ) ) ;
#40337=ORIENTED_EDGE ( 'NONE', *, *, #17507, .T. ) ;
#40338=ORIENTED_EDGE ( 'NONE', *, *, #8332, .T. ) ;
#40339=EDGE_LOOP ( 'NONE', ( #5354, #21840, #31751, #16189 ) ) ;
#40340=CARTESIAN_POINT ( 'NONE',  ( -0.5455278134075214336, 0.000000000000000000, -1.574803149606293529 ) ) ;
#40341=VERTEX_POINT ( 'NONE', #19315 ) ;
#40342=ORIENTED_EDGE ( 'NONE', *, *, #7600, .F. ) ;
#40344=DIRECTION ( 'NONE',  ( 0.000000000000000000, -1.000000000000000000, 0.000000000000000000 ) ) ;
#40345=DIRECTION ( 'NONE',  ( -0.000000000000000000, 1.000000000000000000, -0.000000000000000000 ) ) ;
#40347=DIRECTION ( 'NONE',  ( -3.469446951953613696E-16, 0.000000000000000000, -1.000000000000000000 ) ) ;
#40348=CARTESIAN_POINT ( 'NONE',  ( -1.091055626815042645, 3.346456692913386100, -0.8267716535433052849 ) ) ;
#40350=ORIENTED_EDGE ( 'NONE', *, *, #49477, .T. ) ;
#40351=CARTESIAN_POINT ( 'NONE',  ( -0.3486774197067342151, 0.000000000000000000, -2.204724409448810540 ) ) ;
#40352=DIRECTION ( 'NONE',  ( -3.469446951953613696E-16, 0.000000000000000000, -1.000000000000000000 ) ) ;
#40353=DIRECTION ( 'NONE',  ( -1.000000000000000000, 0.000000000000000000, 1.734723475976806848E-16 ) ) ;
#40361=ADVANCED_FACE ( 'NONE', ( #15458 ), #31207, .F. ) ;
#40362=ADVANCED_FACE ( 'NONE', ( #7962 ), #38458, .F. ) ;
#40364=CARTESIAN_POINT ( 'NONE',  ( -0.2727639067037607723, 3.267716535433071279, -0.1574803149606301411 ) ) ;
#40365=VECTOR ( 'NONE', #37349, 39.37007874015748143 ) ;
#40366=ORIENTED_EDGE ( 'NONE', *, *, #41023, .T. ) ;
#40367=ORIENTED_EDGE ( 'NONE', *, *, #48372, .T. ) ;
#40368=EDGE_CURVE ( 'NONE', #8660, #18633, #34579, .T. ) ;
#40370=AXIS2_PLACEMENT_3D ( 'NONE', #10666, #38540, #50842 ) ;
#40372=PLANE ( 'NONE',  #34029 ) ;
#40374=EDGE_CURVE ( 'NONE', #33705, #23434, #12599, .T. ) ;
#40376=CARTESIAN_POINT ( 'NONE',  ( -0.8942052331142552601, 3.346456692913386100, 1.692913385826762873 ) ) ;
#40377=CARTESIAN_POINT ( 'NONE',  ( 0.8182917201112819283, 3.346456692913386100, 0.4724409448818868706 ) ) ;
#40378=CARTESIAN_POINT ( 'NONE',  ( -0.3486774197067334935, 3.346456692913386100, 0.7480314960629874665 ) ) ;
#40379=ORIENTED_EDGE ( 'NONE', *, *, #17695, .F. ) ;
#40380=PLANE ( 'NONE',  #35751 ) ;
#40382=DIRECTION ( 'NONE',  ( 0.000000000000000000, 0.000000000000000000, -1.000000000000000000 ) ) ;
#40383=ORIENTED_EDGE ( 'NONE', *, *, #27177, .F. ) ;
#40385=EDGE_CURVE ( 'NONE', #25253, #8785, #39712, .T. ) ;
#40387=LINE ( 'NONE', #20749, #17262 ) ;
#40389=VERTEX_POINT ( 'NONE', #47671 ) ;
#40390=DIRECTION ( 'NONE',  ( -3.469446951953613696E-16, 0.000000000000000000, -1.000000000000000000 ) ) ;
#40391=DIRECTION ( 'NONE',  ( 1.734723475976806848E-16, 0.000000000000000000, 1.000000000000000000 ) ) ;
#40392=ADVANCED_FACE ( 'NONE', ( #4599 ), #24481, .F. ) ;
#40393=CARTESIAN_POINT ( 'NONE',  ( 0.000000000000000000, 3.267716535433071279, -1.771653543307081691 ) ) ;
#40394=EDGE_CURVE ( 'NONE', #3256, #20489, #48184, .T. ) ;
#40395=EDGE_LOOP ( 'NONE', ( #28201, #39059, #39155, #8468 ) ) ;
#40396=CARTESIAN_POINT ( 'NONE',  ( -0.2727639067037602727, 0.000000000000000000, 0.9055118110236167750 ) ) ;
#40398=ORIENTED_EDGE ( 'NONE', *, *, #41409, .F. ) ;
#40400=PLANE ( 'NONE',  #13853 ) ;
#40401=VECTOR ( 'NONE', #22765, 39.37007874015748143 ) ;
#40402=DIRECTION ( 'NONE',  ( 0.000000000000000000, 0.000000000000000000, -1.000000000000000000 ) ) ;
#40403=FACE_OUTER_BOUND ( 'NONE', #24152, .T. ) ;
#40405=ORIENTED_EDGE ( 'NONE', *, *, #15372, .F. ) ;
#40408=DIRECTION ( 'NONE',  ( -0.000000000000000000, -1.000000000000000000, -0.000000000000000000 ) ) ;
#40409=ORIENTED_EDGE ( 'NONE', *, *, #43364, .F. ) ;
#40411=PLANE ( 'NONE',  #26846 ) ;
#40412=VECTOR ( 'NONE', #21215, 39.37007874015748143 ) ;
#40415=ORIENTED_EDGE ( 'NONE', *, *, #11960, .F. ) ;
#40416=ORIENTED_EDGE ( 'NONE', *, *, #43202, .T. ) ;
#40417=CARTESIAN_POINT ( 'NONE',  ( -0.8942052331142547050, 3.346456692913386100, 1.574803149606291974 ) ) ;
#40418=LINE ( 'NONE', #31639, #49665 ) ;
#40419=CARTESIAN_POINT ( 'NONE',  ( 0.2727639067037604392, 0.000000000000000000, -1.299212598425193210 ) ) ;
#40420=VERTEX_POINT ( 'NONE', #35841 ) ;
#40422=FACE_BOUND ( 'NONE', #37438, .T. ) ;
#40424=DIRECTION ( 'NONE',  ( 0.000000000000000000, 1.000000000000000000, 0.000000000000000000 ) ) ;
#40425=ORIENTED_EDGE ( 'NONE', *, *, #19206, .T. ) ;
#40426=ORIENTED_EDGE ( 'NONE', *, *, #46266, .T. ) ;
#40428=ORIENTED_EDGE ( 'NONE', *, *, #6024, .F. ) ;
#40429=EDGE_LOOP ( 'NONE', ( #35576, #7551, #8228, #46478 ) ) ;
#40433=EDGE_CURVE ( 'NONE', #65, #23861, #32492, .T. ) ;
#40434=CARTESIAN_POINT ( 'NONE',  ( 1.636583440222563857, 0.000000000000000000, 0.6299212598425164567 ) ) ;
#40435=LINE ( 'NONE', #928, #43345 ) ;
#40440=PLANE ( 'NONE',  #32214 ) ;
#40442=PLANE ( 'NONE',  #31967 ) ;
#40443=EDGE_LOOP ( 'NONE', ( #36375, #5526, #6082, #42727, #7575 ) ) ;
#40444=CARTESIAN_POINT ( 'NONE',  ( 0.4696143004045478797, 3.346456692913386100, 0.2755905511810994302 ) ) ;
#40445=VECTOR ( 'NONE', #43352, 39.37007874015748143 ) ;
#40446=CARTESIAN_POINT ( 'NONE',  ( -0.07591351300297277671, 3.267716535433071279, 1.732283464566921172 ) ) ;
#40448=CARTESIAN_POINT ( 'NONE',  ( 1.560669927219590747, 3.346456692913386100, -0.4724409448818889246 ) ) ;
#40449=EDGE_CURVE ( 'NONE', #2298, #28697, #21118, .T. ) ;
#40451=VERTEX_POINT ( 'NONE', #5107 ) ;
#40452=DIRECTION ( 'NONE',  ( -0.000000000000000000, 0.000000000000000000, 1.000000000000000000 ) ) ;
#40453=DIRECTION ( 'NONE',  ( 1.000000000000000000, 0.000000000000000000, -3.469446951953613696E-16 ) ) ;
#40454=DIRECTION ( 'NONE',  ( 1.000000000000000000, 0.000000000000000000, 0.000000000000000000 ) ) ;
#40457=VERTEX_POINT ( 'NONE', #470 ) ;
#40458=CARTESIAN_POINT ( 'NONE',  ( -0.8182917201112814842, 0.000000000000000000, 0.4724409448818872592 ) ) ;
#40460=FACE_BOUND ( 'NONE', #2002, .T. ) ;
#40461=PLANE ( 'NONE',  #38302 ) ;
#40463=LINE ( 'NONE', #21347, #14420 ) ;
#40464=ORIENTED_EDGE ( 'NONE', *, *, #32360, .F. ) ;
#40465=EDGE_LOOP ( 'NONE', ( #34083, #22937, #42924, #15944 ) ) ;
#40466=CARTESIAN_POINT ( 'NONE',  ( -0.8182917201112819283, 3.346456692913386100, -1.614173228346451605 ) ) ;
#40467=EDGE_LOOP ( 'NONE', ( #27171, #5337, #41297, #15434 ) ) ;
#40468=CARTESIAN_POINT ( 'NONE',  ( -0.5455278134075208785, 3.267716535433071279, 1.377952755905504256 ) ) ;
#40469=VERTEX_POINT ( 'NONE', #36615 ) ;
#40470=VECTOR ( 'NONE', #8167, 39.37007874015748143 ) ;
#40471=DIRECTION ( 'NONE',  ( -0.000000000000000000, 1.000000000000000000, -0.000000000000000000 ) ) ;
#40472=VECTOR ( 'NONE', #13907, 39.37007874015748143 ) ;
#40473=ORIENTED_EDGE ( 'NONE', *, *, #11799, .T. ) ;
#40474=DIRECTION ( 'NONE',  ( 1.000000000000000000, 0.000000000000000000, 0.000000000000000000 ) ) ;
#40477=LINE ( 'NONE', #44330, #34790 ) ;
#40480=ORIENTED_EDGE ( 'NONE', *, *, #36928, .T. ) ;
#40482=EDGE_CURVE ( 'NONE', #29354, #47979, #31976, .T. ) ;
#40483=ORIENTED_EDGE ( 'NONE', *, *, #10126, .F. ) ;
#40485=ORIENTED_EDGE ( 'NONE', *, *, #1071, .T. ) ;
#40487=EDGE_CURVE ( 'NONE', #19354, #47308, #1236, .T. ) ;
#40490=DIRECTION ( 'NONE',  ( -1.000000000000000000, 0.000000000000000000, 0.000000000000000000 ) ) ;
#40491=ORIENTED_EDGE ( 'NONE', *, *, #40394, .F. ) ;
#40492=DIRECTION ( 'NONE',  ( 0.000000000000000000, 1.000000000000000000, 0.000000000000000000 ) ) ;
#40496=FACE_OUTER_BOUND ( 'NONE', #23052, .T. ) ;
#40500=CARTESIAN_POINT ( 'NONE',  ( 0.7423782071083087075, 0.000000000000000000, 0.6299212598425161236 ) ) ;
#40501=ADVANCED_FACE ( 'NONE', ( #43572 ), #8222, .F. ) ;
#40502=ORIENTED_EDGE ( 'NONE', *, *, #36203, .F. ) ;
#40505=ORIENTED_EDGE ( 'NONE', *, *, #22691, .T. ) ;
#40506=CARTESIAN_POINT ( 'NONE',  ( -0.8182917201112819283, 3.346456692913386100, -0.9842519685039342603 ) ) ;
#40507=EDGE_CURVE ( 'NONE', #34452, #49288, #4859, .T. ) ;
#40508=VECTOR ( 'NONE', #50067, 39.37007874015748143 ) ;
#40510=LINE ( 'NONE', #17273, #5821 ) ;
#40514=CARTESIAN_POINT ( 'NONE',  ( 1.091055626815042645, 3.267716535433071279, -1.892679809432644389E-16 ) ) ;
#40516=ORIENTED_EDGE ( 'NONE', *, *, #34288, .F. ) ;
#40518=DIRECTION ( 'NONE',  ( 1.734723475976806848E-16, -0.000000000000000000, 1.000000000000000000 ) ) ;
#40520=FACE_BOUND ( 'NONE', #31429, .T. ) ;
#40521=ORIENTED_EDGE ( 'NONE', *, *, #19706, .T. ) ;
#40523=EDGE_CURVE ( 'NONE', #383, #31088, #42005, .T. ) ;
#40524=ORIENTED_EDGE ( 'NONE', *, *, #29340, .T. ) ;
#40525=DIRECTION ( 'NONE',  ( -0.000000000000000000, 1.000000000000000000, -0.000000000000000000 ) ) ;
#40526=CARTESIAN_POINT ( 'NONE',  ( 0.000000000000000000, 3.346456692913386100, 0.000000000000000000 ) ) ;
#40528=VERTEX_POINT ( 'NONE', #5873 ) ;
#40529=VERTEX_POINT ( 'NONE', #41752 ) ;
#40531=CARTESIAN_POINT ( 'NONE',  ( 0.5455278134075211005, 0.000000000000000000, 0.4330708661417287386 ) ) ;
#40532=FACE_BOUND ( 'NONE', #39379, .T. ) ;
#40533=ORIENTED_EDGE ( 'NONE', *, *, #6457, .T. ) ;
#40535=AXIS2_PLACEMENT_3D ( 'NONE', #31386, #4268, #35767 ) ;
#40540=VECTOR ( 'NONE', #45507, 39.37007874015748143 ) ;
#40542=EDGE_LOOP ( 'NONE', ( #3847, #1097, #13211, #3452 ) ) ;
#40544=ORIENTED_EDGE ( 'NONE', *, *, #1171, .F. ) ;
#40548=FACE_OUTER_BOUND ( 'NONE', #31355, .T. ) ;
#40549=PLANE ( 'NONE',  #5303 ) ;
#40550=EDGE_CURVE ( 'NONE', #42097, #17453, #21373, .T. ) ;
#40551=CARTESIAN_POINT ( 'NONE',  ( 1.287906020515830585, 3.267716535433071279, 1.889763779527550369 ) ) ;
#40552=ORIENTED_EDGE ( 'NONE', *, *, #35142, .T. ) ;
#40553=VERTEX_POINT ( 'NONE', #45095 ) ;
#40555=FACE_OUTER_BOUND ( 'NONE', #35948, .T. ) ;
#40556=CARTESIAN_POINT ( 'NONE',  ( -1.636583440222564301, 0.000000000000000000, -0.9448818897637762948 ) ) ;
#40558=FACE_OUTER_BOUND ( 'NONE', #43590, .T. ) ;
#40559=DIRECTION ( 'NONE',  ( 1.000000000000000000, 0.000000000000000000, 0.000000000000000000 ) ) ;
#40560=DIRECTION ( 'NONE',  ( -0.000000000000000000, 1.000000000000000000, -0.000000000000000000 ) ) ;
#40561=ORIENTED_EDGE ( 'NONE', *, *, #42894, .F. ) ;
#40562=LINE ( 'NONE', #5708, #35792 ) ;
#40563=CARTESIAN_POINT ( 'NONE',  ( -1.712496953225537188, 3.346456692913386100, 0.1574803149606286423 ) ) ;
#40564=VERTEX_POINT ( 'NONE', #49203 ) ;
#40566=ORIENTED_EDGE ( 'NONE', *, *, #9728, .F. ) ;
#40567=DIRECTION ( 'NONE',  ( 0.000000000000000000, -1.000000000000000000, 0.000000000000000000 ) ) ;
#40569=PLANE ( 'NONE',  #8047 ) ;
#40570=EDGE_LOOP ( 'NONE', ( #4190, #39041, #25986, #4923 ) ) ;
#40572=VECTOR ( 'NONE', #41541, 39.37007874015748143 ) ;
#40573=ORIENTED_EDGE ( 'NONE', *, *, #17563, .T. ) ;
#40574=FACE_OUTER_BOUND ( 'NONE', #44566, .T. ) ;
#40575=AXIS2_PLACEMENT_3D ( 'NONE', #8916, #40424, #21050 ) ;
#40576=ORIENTED_EDGE ( 'NONE', *, *, #22184, .T. ) ;
#40577=ADVANCED_FACE ( 'NONE', ( #10005 ), #6645, .F. ) ;
#40578=ORIENTED_EDGE ( 'NONE', *, *, #33087, .F. ) ;
#40580=CARTESIAN_POINT ( 'NONE',  ( -0.8942052331142547050, 3.267716535433071279, 1.574803149606291974 ) ) ;
#40581=DIRECTION ( 'NONE',  ( 1.734723475976806848E-16, -0.000000000000000000, 1.000000000000000000 ) ) ;
#40582=ADVANCED_FACE ( 'NONE', ( #21880 ), #29627, .F. ) ;
#40584=ORIENTED_EDGE ( 'NONE', *, *, #34666, .T. ) ;
#40585=ORIENTED_EDGE ( 'NONE', *, *, #43348, .F. ) ;
#40586=ORIENTED_EDGE ( 'NONE', *, *, #11731, .F. ) ;
#40588=ORIENTED_EDGE ( 'NONE', *, *, #32000, .T. ) ;
#40589=ORIENTED_EDGE ( 'NONE', *, *, #4043, .T. ) ;
#40590=EDGE_CURVE ( 'NONE', #24946, #10781, #37383, .T. ) ;
#40591=CARTESIAN_POINT ( 'NONE',  ( 0.8182917201112817063, 3.346456692913386100, -2.047244094488181343 ) ) ;
#40592=DIRECTION ( 'NONE',  ( 0.000000000000000000, 1.000000000000000000, 0.000000000000000000 ) ) ;
#40594=EDGE_CURVE ( 'NONE', #37232, #15892, #44843, .T. ) ;
#40596=CARTESIAN_POINT ( 'NONE',  ( 0.7423782071083087075, 3.267716535433071279, 0.3149606299212576177 ) ) ;
#40597=LINE ( 'NONE', #21231, #22544 ) ;
#40598=LINE ( 'NONE', #44458, #49220 ) ;
#40599=ORIENTED_EDGE ( 'NONE', *, *, #18621, .F. ) ;
#40603=ORIENTED_EDGE ( 'NONE', *, *, #50003, .F. ) ;
#40604=ORIENTED_EDGE ( 'NONE', *, *, #18621, .T. ) ;
#40606=( CONVERSION_BASED_UNIT ( 'INCH', #24088 ) LENGTH_UNIT ( ) NAMED_UNIT ( #36715 ) );
#40607=EDGE_CURVE ( 'NONE', #7571, #43175, #22390, .T. ) ;
#40609=VECTOR ( 'NONE', #36927, 39.37007874015748143 ) ;
#40611=EDGE_CURVE ( 'NONE', #35864, #43265, #22137, .T. ) ;
#40613=ORIENTED_EDGE ( 'NONE', *, *, #48650, .F. ) ;
#40617=LINE ( 'NONE', #17123, #50564 ) ;
#40618=AXIS2_PLACEMENT_3D ( 'NONE', #41873, #9619, #6512 ) ;
#40619=VERTEX_POINT ( 'NONE', #33255 ) ;
#40621=LINE ( 'NONE', #1371, #44864 ) ;
#40623=DIRECTION ( 'NONE',  ( -1.000000000000000000, 0.000000000000000000, 0.000000000000000000 ) ) ;
#40625=CARTESIAN_POINT ( 'NONE',  ( -0.5455278134075214336, 3.267716535433071279, -0.9448818897637762948 ) ) ;
#40627=CARTESIAN_POINT ( 'NONE',  ( -0.07591351300297327631, 3.267716535433071279, 2.633779063002566366E-17 ) ) ;
#40628=DIRECTION ( 'NONE',  ( -1.000000000000000000, -0.000000000000000000, -0.000000000000000000 ) ) ;
#40629=VERTEX_POINT ( 'NONE', #48940 ) ;
#40630=CARTESIAN_POINT ( 'NONE',  ( 1.287906020515830585, 0.000000000000000000, 1.889763779527550369 ) ) ;
#40632=CARTESIAN_POINT ( 'NONE',  ( 0.1968503937007873017, 3.346456692913386100, -1.574803149606293529 ) ) ;
#40633=ORIENTED_EDGE ( 'NONE', *, *, #3625, .F. ) ;
#40634=EDGE_CURVE ( 'NONE', #27835, #37100, #2517, .T. ) ;
#40640=VERTEX_POINT ( 'NONE', #13626 ) ;
#40641=DIRECTION ( 'NONE',  ( 0.000000000000000000, -1.000000000000000000, 0.000000000000000000 ) ) ;
#40642=LINE ( 'NONE', #5783, #17762 ) ;
#40643=DIRECTION ( 'NONE',  ( -1.000000000000000000, 0.000000000000000000, -0.000000000000000000 ) ) ;
#40646=EDGE_CURVE ( 'NONE', #32098, #3695, #40999, .T. ) ;
#40647=EDGE_CURVE ( 'NONE', #27463, #21275, #7400, .T. ) ;
#40648=LINE ( 'NONE', #5273, #36230 ) ;
#40649=CIRCLE ( 'NONE', #18384, 2.106299212598425008 ) ;
#40651=ORIENTED_EDGE ( 'NONE', *, *, #9306, .T. ) ;
#40652=DIRECTION ( 'NONE',  ( 1.000000000000000000, 0.000000000000000000, -3.469446951953613696E-16 ) ) ;
#40653=DIRECTION ( 'NONE',  ( -0.000000000000000000, 1.000000000000000000, -0.000000000000000000 ) ) ;
#40655=CARTESIAN_POINT ( 'NONE',  ( 1.636583440222563635, 0.000000000000000000, -0.9448818897637765168 ) ) ;
#40656=LINE ( 'NONE', #20256, #44169 ) ;
#40657=CARTESIAN_POINT ( 'NONE',  ( -1.195183497228115035E-16, 0.000000000000000000, -0.6299212598425177889 ) ) ;
#40658=VECTOR ( 'NONE', #36164, 39.37007874015748143 ) ;
#40659=DIRECTION ( 'NONE',  ( 0.000000000000000000, 1.000000000000000000, 0.000000000000000000 ) ) ;
#40660=VECTOR ( 'NONE', #49278, 39.37007874015748143 ) ;
#40662=ORIENTED_EDGE ( 'NONE', *, *, #19246, .F. ) ;
#40663=DIRECTION ( 'NONE',  ( -3.469446951953613696E-16, 0.000000000000000000, -1.000000000000000000 ) ) ;
#40664=CARTESIAN_POINT ( 'NONE',  ( 0.000000000000000000, 3.267716535433071279, 1.732283464566921172 ) ) ;
#40665=CARTESIAN_POINT ( 'NONE',  ( 1.363819533518803695, 3.346456692913386100, 1.732283464566921172 ) ) ;
#40667=DIRECTION ( 'NONE',  ( 1.734723475976806848E-16, 0.000000000000000000, 1.000000000000000000 ) ) ;
#40668=FACE_BOUND ( 'NONE', #18822, .T. ) ;
#40669=VECTOR ( 'NONE', #36054, 39.37007874015748143 ) ;
#40670=ORIENTED_EDGE ( 'NONE', *, *, #31937, .T. ) ;
#40671=DIRECTION ( 'NONE',  ( 0.000000000000000000, 0.000000000000000000, 1.000000000000000000 ) ) ;
#40672=ORIENTED_EDGE ( 'NONE', *, *, #8178, .F. ) ;
#40674=ADVANCED_FACE ( 'NONE', ( #38889 ), #27001, .F. ) ;
#40675=DIRECTION ( 'NONE',  ( -1.000000000000000000, 0.000000000000000000, 1.734723475976806848E-16 ) ) ;
#40676=ADVANCED_FACE ( 'NONE', ( #7900 ), #50203, .F. ) ;
#40678=DIRECTION ( 'NONE',  ( -0.000000000000000000, 1.000000000000000000, -0.000000000000000000 ) ) ;
#40679=EDGE_CURVE ( 'NONE', #26214, #39217, #3021, .T. ) ;
#40680=VERTEX_POINT ( 'NONE', #27509 ) ;
#40681=EDGE_CURVE ( 'NONE', #13726, #21920, #50448, .T. ) ;
#40682=DIRECTION ( 'NONE',  ( -1.000000000000000000, 0.000000000000000000, 0.000000000000000000 ) ) ;
#40684=CARTESIAN_POINT ( 'NONE',  ( 1.287906020515829919, 3.346456692913386100, -1.889763779527552368 ) ) ;
#40685=CARTESIAN_POINT ( 'NONE',  ( -0.8182917201112819283, 0.000000000000000000, -0.3543307086614175816 ) ) ;
#40688=PLANE ( 'NONE',  #20365 ) ;
#40689=CARTESIAN_POINT ( 'NONE',  ( -4.268512490100411402E-16, 3.346456692913386100, -2.401574803149598480 ) ) ;
#40690=ORIENTED_EDGE ( 'NONE', *, *, #20163, .F. ) ;
#40691=DIRECTION ( 'NONE',  ( -3.469446951953613696E-16, 0.000000000000000000, -1.000000000000000000 ) ) ;
#40692=VECTOR ( 'NONE', #29002, 39.37007874015748143 ) ;
#40693=DIRECTION ( 'NONE',  ( -0.000000000000000000, 1.000000000000000000, -0.000000000000000000 ) ) ;
#40694=VECTOR ( 'NONE', #26640, 39.37007874015748143 ) ;
#40697=LINE ( 'NONE', #685, #36854 ) ;
#40698=ORIENTED_EDGE ( 'NONE', *, *, #19749, .F. ) ;
#40699=DIRECTION ( 'NONE',  ( 1.000000000000000000, 0.000000000000000000, -3.469446951953613696E-16 ) ) ;
#40702=VECTOR ( 'NONE', #25379, 39.37007874015748143 ) ;
#40704=DIRECTION ( 'NONE',  ( 1.000000000000000000, 0.000000000000000000, -3.469446951953613696E-16 ) ) ;
#40707=FACE_BOUND ( 'NONE', #22680, .T. ) ;
#40708=DIRECTION ( 'NONE',  ( 1.000000000000000000, 0.000000000000000000, 0.000000000000000000 ) ) ;
#40709=DIRECTION ( 'NONE',  ( -0.000000000000000000, 1.000000000000000000, -0.000000000000000000 ) ) ;
#40710=DIRECTION ( 'NONE',  ( 1.734723475976806848E-16, -0.000000000000000000, 1.000000000000000000 ) ) ;
#40711=EDGE_CURVE ( 'NONE', #38291, #18200, #38645, .T. ) ;
#40712=EDGE_LOOP ( 'NONE', ( #34835, #19, #13873 ) ) ;
#40714=EDGE_CURVE ( 'NONE', #30930, #14507, #46354, .T. ) ;
#40715=CARTESIAN_POINT ( 'NONE',  ( -1.091055626815042201, 0.000000000000000000, 0.3149606299212580063 ) ) ;
#40719=EDGE_CURVE ( 'NONE', #50260, #35018, #14642, .T. ) ;
#40720=CARTESIAN_POINT ( 'NONE',  ( -0.5455278134075214336, 0.000000000000000000, 2.204724409448808764 ) ) ;
#40723=DIRECTION ( 'NONE',  ( -0.000000000000000000, 1.000000000000000000, -0.000000000000000000 ) ) ;
#40725=LINE ( 'NONE', #20845, #47042 ) ;
#40726=ORIENTED_EDGE ( 'NONE', *, *, #12221, .T. ) ;
#40727=DIRECTION ( 'NONE',  ( -1.000000000000000000, 0.000000000000000000, 0.000000000000000000 ) ) ;
#40728=VECTOR ( 'NONE', #39680, 39.37007874015748143 ) ;
#40729=ORIENTED_EDGE ( 'NONE', *, *, #34640, .F. ) ;
#40730=ORIENTED_EDGE ( 'NONE', *, *, #9303, .T. ) ;
#40731=VECTOR ( 'NONE', #21777, 39.37007874015748143 ) ;
#40732=VECTOR ( 'NONE', #40560, 39.37007874015748143 ) ;
#40735=ORIENTED_EDGE ( 'NONE', *, *, #22380, .F. ) ;
#40738=DIRECTION ( 'NONE',  ( 1.000000000000000000, 0.000000000000000000, 0.000000000000000000 ) ) ;
#40739=AXIS2_PLACEMENT_3D ( 'NONE', #1576, #21455, #37209 ) ;
#40740=ADVANCED_FACE ( 'NONE', ( #15143 ), #31400, .F. ) ;
#40741=ORIENTED_EDGE ( 'NONE', *, *, #36343, .F. ) ;
#40742=CARTESIAN_POINT ( 'NONE',  ( 1.091055626815042645, 3.346456692913386100, -0.1968503937007883287 ) ) ;
#40743=ORIENTED_EDGE ( 'NONE', *, *, #36117, .F. ) ;
#40744=DIRECTION ( 'NONE',  ( -0.000000000000000000, 1.000000000000000000, -0.000000000000000000 ) ) ;
#40745=CARTESIAN_POINT ( 'NONE',  ( 1.909347346926324684, 3.267716535433071279, -0.1574803149606304187 ) ) ;
#40748=PLANE ( 'NONE',  #37845 ) ;
#40749=ORIENTED_EDGE ( 'NONE', *, *, #43139, .T. ) ;
#40750=FACE_OUTER_BOUND ( 'NONE', #15766, .T. ) ;
#40751=FACE_OUTER_BOUND ( 'NONE', #18191, .T. ) ;
#40753=DIRECTION ( 'NONE',  ( -0.000000000000000000, 1.000000000000000000, -0.000000000000000000 ) ) ;
#40754=DIRECTION ( 'NONE',  ( 1.734723475976806848E-16, 0.000000000000000000, 1.000000000000000000 ) ) ;
#40755=ORIENTED_EDGE ( 'NONE', *, *, #37095, .T. ) ;
#40757=DIRECTION ( 'NONE',  ( 1.734723475976806848E-16, -0.000000000000000000, 1.000000000000000000 ) ) ;
#40759=ORIENTED_EDGE ( 'NONE', *, *, #32936, .T. ) ;
#40760=CARTESIAN_POINT ( 'NONE',  ( 0.8182917201112824834, 0.000000000000000000, 1.732283464566921172 ) ) ;
#40761=VECTOR ( 'NONE', #25051, 39.37007874015748143 ) ;
#40769=DIRECTION ( 'NONE',  ( -1.000000000000000000, 0.000000000000000000, -0.000000000000000000 ) ) ;
#40771=ORIENTED_EDGE ( 'NONE', *, *, #10533, .F. ) ;
#40773=EDGE_CURVE ( 'NONE', #35361, #11368, #50698, .T. ) ;
#40774=AXIS2_PLACEMENT_3D ( 'NONE', #30857, #45366, #10028 ) ;
#40775=CARTESIAN_POINT ( 'NONE',  ( 0.4696143004045484903, 0.000000000000000000, 1.102362204724404160 ) ) ;
#40779=VERTEX_POINT ( 'NONE', #7647 ) ;
#40783=LINE ( 'NONE', #5405, #13375 ) ;
#40786=ORIENTED_EDGE ( 'NONE', *, *, #23616, .F. ) ;
#40789=FACE_BOUND ( 'NONE', #4211, .T. ) ;
#40790=LINE ( 'NONE', #21173, #33655 ) ;
#40791=EDGE_CURVE ( 'NONE', #6075, #46791, #14893, .T. ) ;
#40793=EDGE_LOOP ( 'NONE', ( #11912, #50039, #8709, #4715 ) ) ;
#40795=APPLICATION_CONTEXT ( 'automotive_design' ) ;
#40796=VECTOR ( 'NONE', #43701, 39.37007874015748143 ) ;
#40798=ADVANCED_FACE ( 'NONE', ( #30640 ), #49955, .F. ) ;
#40800=AXIS2_PLACEMENT_3D ( 'NONE', #20671, #40042, #36432 ) ;
#40801=ORIENTED_EDGE ( 'NONE', *, *, #430, .T. ) ;
#40802=CIRCLE ( 'NONE', #18542, 2.443628662382284489 ) ;
#40803=ORIENTED_EDGE ( 'NONE', *, *, #1568, .F. ) ;
#40804=DIRECTION ( 'NONE',  ( -3.469446951953613696E-16, 0.000000000000000000, -1.000000000000000000 ) ) ;
#40806=PLANE ( 'NONE',  #48925 ) ;
#40807=DIRECTION ( 'NONE',  ( -0.000000000000000000, 1.000000000000000000, -0.000000000000000000 ) ) ;
#40808=EDGE_LOOP ( 'NONE', ( #35151, #30820, #498, #31548 ) ) ;
#40810=VECTOR ( 'NONE', #4917, 39.37007874015748143 ) ;
#40811=LINE ( 'NONE', #13441, #30737 ) ;
#40813=CARTESIAN_POINT ( 'NONE',  ( 0.000000000000000000, 3.267716535433071279, -1.771653543307081025 ) ) ;
#40814=EDGE_CURVE ( 'NONE', #25289, #1960, #35025, .T. ) ;
#40815=LINE ( 'NONE', #1050, #12792 ) ;
#40816=DIRECTION ( 'NONE',  ( 1.000000000000000000, 0.000000000000000000, -3.469446951953613696E-16 ) ) ;
#40817=DIRECTION ( 'NONE',  ( -1.000000000000000000, -0.000000000000000000, -0.000000000000000000 ) ) ;
#40818=LINE ( 'NONE', #24553, #33339 ) ;
#40820=CARTESIAN_POINT ( 'NONE',  ( -1.166969139818015977, 3.346456692913386100, -1.823990790610291013 ) ) ;
#40821=LINE ( 'NONE', #29191, #42551 ) ;
#40822=EDGE_LOOP ( 'NONE', ( #233, #29606, #5228, #39254 ) ) ;
#40824=CARTESIAN_POINT ( 'NONE',  ( 1.363819533518803251, 3.346456692913386100, -0.7874015748031473194 ) ) ;
#40825=FACE_OUTER_BOUND ( 'NONE', #45698, .T. ) ;
#40826=ORIENTED_EDGE ( 'NONE', *, *, #7528, .F. ) ;
#40827=AXIS2_PLACEMENT_3D ( 'NONE', #23517, #35154, #27382 ) ;
#40828=AXIS2_PLACEMENT_3D ( 'NONE', #19612, #20645, #24525 ) ;
#40829=ORIENTED_EDGE ( 'NONE', *, *, #3465, .T. ) ;
#40831=DIRECTION ( 'NONE',  ( -3.469446951953613696E-16, 0.000000000000000000, -1.000000000000000000 ) ) ;
#40832=VECTOR ( 'NONE', #50359, 39.37007874015748143 ) ;
#40834=ADVANCED_FACE ( 'NONE', ( #28537 ), #24421, .F. ) ;
#40835=CARTESIAN_POINT ( 'NONE',  ( -1.985260859929298016, 3.346456692913386100, -0.7037298423582233342 ) ) ;
#40836=LINE ( 'NONE', #44441, #46157 ) ;
#40837=ADVANCED_FACE ( 'NONE', ( #16160 ), #47617, .F. ) ;
#40839=EDGE_LOOP ( 'NONE', ( #28687, #34761, #43449, #32693 ) ) ;
#40842=VECTOR ( 'NONE', #49611, 39.37007874015748143 ) ;
#40843=LINE ( 'NONE', #24328, #10640 ) ;
#40844=EDGE_LOOP ( 'NONE', ( #12537, #19170, #16327, #31638 ) ) ;
#40846=LINE ( 'NONE', #5473, #9175 ) ;
#40847=CARTESIAN_POINT ( 'NONE',  ( 1.833433833923351353, 3.267716535433071279, -0.1968503937007886062 ) ) ;
#40849=VERTEX_POINT ( 'NONE', #27770 ) ;
#40851=EDGE_CURVE ( 'NONE', #31303, #3180, #24930, .T. ) ;
#40852=LINE ( 'NONE', #25605, #43123 ) ;
#40853=LINE ( 'NONE', #17608, #2276 ) ;
#40856=CARTESIAN_POINT ( 'NONE',  ( 0.1968503937007873017, 0.000000000000000000, -1.574803149606293529 ) ) ;
#40859=ORIENTED_EDGE ( 'NONE', *, *, #9243, .T. ) ;
#40860=ORIENTED_EDGE ( 'NONE', *, *, #5183, .T. ) ;
#40861=LINE ( 'NONE', #36739, #49444 ) ;
#40863=FACE_OUTER_BOUND ( 'NONE', #29775, .T. ) ;
#40864=CARTESIAN_POINT ( 'NONE',  ( -0.2727639067037608278, 0.000000000000000000, -1.929133858267710000 ) ) ;
#40865=VERTEX_POINT ( 'NONE', #44025 ) ;
#40866=EDGE_LOOP ( 'NONE', ( #41589, #29949, #16829, #13952 ) ) ;
#40869=DIRECTION ( 'NONE',  ( -0.000000000000000000, 1.000000000000000000, -0.000000000000000000 ) ) ;
#40870=ORIENTED_EDGE ( 'NONE', *, *, #32585, .T. ) ;
#40871=LINE ( 'NONE', #41130, #47159 ) ;
#40873=LINE ( 'NONE', #37772, #352 ) ;
#40874=AXIS2_PLACEMENT_3D ( 'NONE', #21466, #20690, #17343 ) ;
#40875=VECTOR ( 'NONE', #7075, 39.37007874015748143 ) ;
#40876=FACE_OUTER_BOUND ( 'NONE', #3060, .T. ) ;
#40877=CARTESIAN_POINT ( 'NONE',  ( 0.1968503937007869686, 0.000000000000000000, -2.401574803149598480 ) ) ;
#40879=VECTOR ( 'NONE', #12700, 39.37007874015748143 ) ;
#40881=CARTESIAN_POINT ( 'NONE',  ( 1.091055626815042423, 0.000000000000000000, -1.889763779527552368 ) ) ;
#40882=EDGE_CURVE ( 'NONE', #13286, #36052, #20281, .T. ) ;
#40883=CARTESIAN_POINT ( 'NONE',  ( 2.378961647330872342, 3.230577599468342775, 0.6299212598425161236 ) ) ;
#40884=EDGE_CURVE ( 'NONE', #25226, #28296, #36045, .T. ) ;
#40886=FACE_OUTER_BOUND ( 'NONE', #31053, .T. ) ;
#40887=CARTESIAN_POINT ( 'NONE',  ( -0.07591351300297284610, 3.346456692913386100, 1.850393700787392293 ) ) ;
#40891=DIRECTION ( 'NONE',  ( 1.000000000000000000, 0.000000000000000000, -3.469446951953613696E-16 ) ) ;
#40892=EDGE_LOOP ( 'NONE', ( #34306, #24366, #47330, #33604 ) ) ;
#40893=DIRECTION ( 'NONE',  ( 1.000000000000000000, -0.000000000000000000, 0.000000000000000000 ) ) ;
#40894=DIRECTION ( 'NONE',  ( -0.000000000000000000, 1.000000000000000000, -0.000000000000000000 ) ) ;
#40895=ORIENTED_EDGE ( 'NONE', *, *, #8261, .T. ) ;
#40897=EDGE_CURVE ( 'NONE', #24770, #42837, #13067, .T. ) ;
#40898=CARTESIAN_POINT ( 'NONE',  ( 1.091055626815042423, 0.000000000000000000, -1.259842519685035134 ) ) ;
#40899=DIRECTION ( 'NONE',  ( 1.000000000000000000, 0.000000000000000000, 0.000000000000000000 ) ) ;
#40901=AXIS2_PLACEMENT_3D ( 'NONE', #41637, #25887, #24874 ) ;
#40902=EDGE_CURVE ( 'NONE', #8821, #28712, #32178, .T. ) ;
#40903=EDGE_CURVE ( 'NONE', #6366, #8029, #12540, .T. ) ;
#40904=LINE ( 'NONE', #21531, #27957 ) ;
#40905=ORIENTED_EDGE ( 'NONE', *, *, #12095, .T. ) ;
#40906=ORIENTED_EDGE ( 'NONE', *, *, #1683, .T. ) ;
#40907=CARTESIAN_POINT ( 'NONE',  ( -2.182111253630085290, 3.346456692913386100, 0.4330708661417290162 ) ) ;
#40908=VECTOR ( 'NONE', #2089, 39.37007874015748143 ) ;
#40910=CARTESIAN_POINT ( 'NONE',  ( 2.106197740627112402, 3.267716535433071279, -0.5026832550384014997 ) ) ;
#40912=ORIENTED_EDGE ( 'NONE', *, *, #44147, .T. ) ;
#40915=CARTESIAN_POINT ( 'NONE',  ( -1.363819533518803029, 0.000000000000000000, 0.1574803149606287811 ) ) ;
#40916=VECTOR ( 'NONE', #28115, 39.37007874015748143 ) ;
#40917=DIRECTION ( 'NONE',  ( -0.000000000000000000, 1.000000000000000000, -0.000000000000000000 ) ) ;
#40918=ORIENTED_EDGE ( 'NONE', *, *, #17207, .T. ) ;
#40919=ORIENTED_EDGE ( 'NONE', *, *, #17418, .T. ) ;
#40920=FACE_OUTER_BOUND ( 'NONE', #35635, .T. ) ;
#40921=FACE_OUTER_BOUND ( 'NONE', #23191, .T. ) ;
#40922=VECTOR ( 'NONE', #9525, 39.37007874015748143 ) ;
#40923=CARTESIAN_POINT ( 'NONE',  ( -1.091055626815042201, 0.000000000000000000, 0.4330708661417290162 ) ) ;
#40924=ORIENTED_EDGE ( 'NONE', *, *, #30811, .T. ) ;
#40925=CARTESIAN_POINT ( 'NONE',  ( 1.833433833923351353, 3.346456692913386100, -0.9448818897637765168 ) ) ;
#40926=FACE_BOUND ( 'NONE', #14653, .T. ) ;
#40927=AXIS2_PLACEMENT_3D ( 'NONE', #22616, #22116, #17731 ) ;
#40928=EDGE_LOOP ( 'NONE', ( #29058, #41939, #29871, #296 ) ) ;
#40929=CARTESIAN_POINT ( 'NONE',  ( -1.636583440222563635, 0.000000000000000000, 0.1181102362204704270 ) ) ;
#40931=EDGE_LOOP ( 'NONE', ( #36650, #29378, #16259, #36391 ) ) ;
#40933=EDGE_CURVE ( 'NONE', #46112, #22897, #8672, .T. ) ;
#40934=ORIENTED_EDGE ( 'NONE', *, *, #15135, .T. ) ;
#40935=DIRECTION ( 'NONE',  ( 0.000000000000000000, 1.000000000000000000, 0.000000000000000000 ) ) ;
#40937=ORIENTED_EDGE ( 'NONE', *, *, #22982, .F. ) ;
#40938=CARTESIAN_POINT ( 'NONE',  ( -1.439733046521776361, 3.267716535433071279, 4.995077429881866871E-16 ) ) ;
#40940=ADVANCED_FACE ( 'NONE', ( #24680 ), #31655, .F. ) ;
#40941=LINE ( 'NONE', #21063, #47262 ) ;
#40942=EDGE_CURVE ( 'NONE', #49645, #29198, #8163, .T. ) ;
#40944=VECTOR ( 'NONE', #49660, 39.37007874015748143 ) ;
#40945=CARTESIAN_POINT ( 'NONE',  ( -2.182111253630085734, 3.267716535433070391, -1.099868863272876141 ) ) ;
#40946=CARTESIAN_POINT ( 'NONE',  ( 1.636583440222563635, 3.346456692913386100, -1.417869535855832419 ) ) ;
#40948=VECTOR ( 'NONE', #2759, 39.37007874015748143 ) ;
#40949=EDGE_LOOP ( 'NONE', ( #43535, #50987, #35345, #7945 ) ) ;
#40951=VECTOR ( 'NONE', #38835, 39.37007874015748143 ) ;
#40952=VECTOR ( 'NONE', #48609, 39.37007874015748143 ) ;
#40953=DIRECTION ( 'NONE',  ( 1.734723475976806848E-16, -0.000000000000000000, 1.000000000000000000 ) ) ;
#40954=VERTEX_POINT ( 'NONE', #23905 ) ;
#40955=CARTESIAN_POINT ( 'NONE',  ( 0.4696143004045484903, 3.346456692913386100, 2.362204724409437961 ) ) ;
#40956=CARTESIAN_POINT ( 'NONE',  ( -0.5455278134075208785, 0.000000000000000000, 1.377952755905504256 ) ) ;
#40957=ORIENTED_EDGE ( 'NONE', *, *, #18510, .T. ) ;
#40958=CARTESIAN_POINT ( 'NONE',  ( 1.363819533518803251, 3.346456692913386100, 1.102362204724403938 ) ) ;
#40960=ADVANCED_FACE ( 'NONE', ( #33201 ), #38523, .F. ) ;
#40962=DIRECTION ( 'NONE',  ( -1.000000000000000000, 0.000000000000000000, 0.000000000000000000 ) ) ;
#40964=VECTOR ( 'NONE', #31569, 39.37007874015748143 ) ;
#40965=B_SPLINE_CURVE_WITH_KNOTS ( 'NONE', 3,
 ( #14971, #27083, #14719, #7474 ),
 .UNSPECIFIED., .F., .F.,
 ( 4, 4 ),
 ( 0.02651100088651920511, 0.02872006419308328895 ),
 .UNSPECIFIED. ) ;
#40966=ORIENTED_EDGE ( 'NONE', *, *, #34634, .T. ) ;
#40967=LINE ( 'NONE', #9720, #15036 ) ;
#40968=VERTEX_POINT ( 'NONE', #26384 ) ;
#40969=FACE_BOUND ( 'NONE', #20159, .T. ) ;
#40970=LINE ( 'NONE', #48911, #13569 ) ;
#40972=LINE ( 'NONE', #2491, #30922 ) ;
#40973=LINE ( 'NONE', #12574, #36683 ) ;
#40974=EDGE_CURVE ( 'NONE', #31767, #20580, #14771, .T. ) ;
#40975=EDGE_CURVE ( 'NONE', #1319, #5048, #30767, .T. ) ;
#40976=ORIENTED_EDGE ( 'NONE', *, *, #21271, .T. ) ;
#40978=EDGE_CURVE ( 'NONE', #13286, #31414, #25435, .T. ) ;
#40979=DIRECTION ( 'NONE',  ( -1.000000000000000000, 0.000000000000000000, -0.000000000000000000 ) ) ;
#40980=EDGE_CURVE ( 'NONE', #50863, #17115, #18386, .T. ) ;
#40981=EDGE_LOOP ( 'NONE', ( #43753, #30364, #14165, #37116 ) ) ;
#40982=LINE ( 'NONE', #48413, #19449 ) ;
#40984=PLANE ( 'NONE',  #36348 ) ;
#40986=DIRECTION ( 'NONE',  ( 0.000000000000000000, -1.000000000000000000, 0.000000000000000000 ) ) ;
#40990=ORIENTED_EDGE ( 'NONE', *, *, #20694, .F. ) ;
#40991=CARTESIAN_POINT ( 'NONE',  ( -0.8182917201112814842, 0.000000000000000000, 0.2755905511810998187 ) ) ;
#40992=ORIENTED_EDGE ( 'NONE', *, *, #15762, .T. ) ;
#40994=VECTOR ( 'NONE', #36166, 39.37007874015748143 ) ;
#40995=ORIENTED_EDGE ( 'NONE', *, *, #7887, .F. ) ;
#40996=VERTEX_POINT ( 'NONE', #46480 ) ;
#40997=LINE ( 'NONE', #13367, #18682 ) ;
#40999=LINE ( 'NONE', #5622, #18835 ) ;
#41003=ADVANCED_FACE ( 'NONE', ( #10889 ), #34147, .F. ) ;
#41004=DIRECTION ( 'NONE',  ( 5.175581015019631661E-17, -0.9063077870366510469, 0.4226182617406972208 ) ) ;
#41005=EDGE_LOOP ( 'NONE', ( #25934, #24224, #14051, #38567 ) ) ;
#41006=EDGE_CURVE ( 'NONE', #14697, #28392, #5305, .T. ) ;
#41008=DIRECTION ( 'NONE',  ( 1.000000000000000000, 0.000000000000000000, 0.000000000000000000 ) ) ;
#41013=LINE ( 'NONE', #5379, #23196 ) ;
#41014=FACE_OUTER_BOUND ( 'NONE', #39488, .T. ) ;
#41017=AXIS2_PLACEMENT_3D ( 'NONE', #21909, #37150, #41025 ) ;
#41020=EDGE_LOOP ( 'NONE', ( #24487, #17012, #34994, #34689 ) ) ;
#41021=VECTOR ( 'NONE', #33468, 39.37007874015748143 ) ;
#41022=CARTESIAN_POINT ( 'NONE',  ( 1.636583440222563635, 3.346456692913386100, -1.325930245594399537 ) ) ;
#41023=EDGE_CURVE ( 'NONE', #2513, #5755, #34646, .T. ) ;
#41024=ORIENTED_EDGE ( 'NONE', *, *, #40136, .F. ) ;
#41025=DIRECTION ( 'NONE',  ( -1.000000000000000000, 0.000000000000000000, -0.000000000000000000 ) ) ;
#41026=PLANE ( 'NONE',  #35782 ) ;
#41030=CARTESIAN_POINT ( 'NONE',  ( 2.106197740627111514, 0.000000000000000000, -0.7874015748031473194 ) ) ;
#41031=ORIENTED_EDGE ( 'NONE', *, *, #9642, .T. ) ;
#41032=EDGE_CURVE ( 'NONE', #36221, #29961, #36812, .T. ) ;
#41033=CARTESIAN_POINT ( 'NONE',  ( 0.000000000000000000, 3.267716535433071279, -1.614173228346451605 ) ) ;
#41034=FACE_BOUND ( 'NONE', #36252, .T. ) ;
#41037=CARTESIAN_POINT ( 'NONE',  ( 0.8182917201112819283, 0.000000000000000000, -1.102362204724405714 ) ) ;
#41038=VECTOR ( 'NONE', #28804, 39.37007874015748143 ) ;
#41040=VERTEX_POINT ( 'NONE', #7522 ) ;
#41041=CARTESIAN_POINT ( 'NONE',  ( -1.363819533518803473, 0.000000000000000000, -0.7874015748031470974 ) ) ;
#41042=FACE_OUTER_BOUND ( 'NONE', #45098, .T. ) ;
#41043=DIRECTION ( 'NONE',  ( 0.000000000000000000, 0.000000000000000000, -1.000000000000000000 ) ) ;
#41046=VERTEX_POINT ( 'NONE', #19634 ) ;
#41047=EDGE_LOOP ( 'NONE', ( #41747, #7796, #36058, #32884 ) ) ;
#41050=FACE_BOUND ( 'NONE', #21392, .T. ) ;
#41051=ORIENTED_EDGE ( 'NONE', *, *, #1211, .T. ) ;
#41052=CARTESIAN_POINT ( 'NONE',  ( 1.636583440222563857, 3.267716535433071279, 0.6299212598425164567 ) ) ;
#41053=DIRECTION ( 'NONE',  ( 1.000000000000000000, -0.000000000000000000, 0.000000000000000000 ) ) ;
#41055=VECTOR ( 'NONE', #2857, 39.37007874015748143 ) ;
#41057=ORIENTED_EDGE ( 'NONE', *, *, #47094, .T. ) ;
#41058=DIRECTION ( 'NONE',  ( 1.000000000000000000, 0.000000000000000000, -3.469446951953613696E-16 ) ) ;
#41059=CARTESIAN_POINT ( 'NONE',  ( -1.057143431661237143, 3.346456692913386100, -1.889763779527552146 ) ) ;
#41062=VECTOR ( 'NONE', #23185, 39.37007874015748143 ) ;
#41063=ORIENTED_EDGE ( 'NONE', *, *, #26497, .F. ) ;
#41065=CARTESIAN_POINT ( 'NONE',  ( 1.015142113812069313, 3.346456692913386100, 1.102362204724403938 ) ) ;
#41066=CARTESIAN_POINT ( 'NONE',  ( 0.000000000000000000, 3.267716535433071279, 0.000000000000000000 ) ) ;
#41067=CARTESIAN_POINT ( 'NONE',  ( 1.287906020515830141, 3.346456692913386100, 0.9448818897637746295 ) ) ;
#41069=ORIENTED_EDGE ( 'NONE', *, *, #20762, .T. ) ;
#41070=ORIENTED_EDGE ( 'NONE', *, *, #29987, .F. ) ;
#41071=ADVANCED_FACE ( 'NONE', ( #4157 ), #39778, .F. ) ;
#41075=CARTESIAN_POINT ( 'NONE',  ( -0.5455278134075208785, 3.346456692913386100, 1.259842519685033357 ) ) ;
#41076=CARTESIAN_POINT ( 'NONE',  ( -0.3486774197067340486, 0.000000000000000000, -1.771653543307081025 ) ) ;
#41077=EDGE_CURVE ( 'NONE', #49909, #36932, #34894, .T. ) ;
#41078=DIRECTION ( 'NONE',  ( 0.000000000000000000, 0.000000000000000000, 1.000000000000000000 ) ) ;
#41080=CARTESIAN_POINT ( 'NONE',  ( 1.636583440222563635, 3.346456692913386100, -0.9448818897637765168 ) ) ;
#41081=VERTEX_POINT ( 'NONE', #15768 ) ;
#41082=CARTESIAN_POINT ( 'NONE',  ( -1.091055626815042645, 0.000000000000000000, -1.771653543307081025 ) ) ;
#41084=VERTEX_POINT ( 'NONE', #31019 ) ;
#41085=ORIENTED_EDGE ( 'NONE', *, *, #10074, .T. ) ;
#41086=DIRECTION ( 'NONE',  ( 1.000000000000000000, 0.000000000000000000, 0.000000000000000000 ) ) ;
#41087=DIRECTION ( 'NONE',  ( -1.000000000000000000, 0.000000000000000000, 1.734723475976806848E-16 ) ) ;
#41089=VECTOR ( 'NONE', #10293, 39.37007874015748143 ) ;
#41091=EDGE_CURVE ( 'NONE', #48217, #4317, #23775, .T. ) ;
#41092=ORIENTED_EDGE ( 'NONE', *, *, #548, .F. ) ;
#41094=VECTOR ( 'NONE', #37828, 39.37007874015748143 ) ;
#41096=VECTOR ( 'NONE', #22039, 39.37007874015748143 ) ;
#41097=DIRECTION ( 'NONE',  ( -1.000000000000000000, 0.000000000000000000, 1.734723475976806848E-16 ) ) ;
#41098=DIRECTION ( 'NONE',  ( -1.000000000000000000, 0.000000000000000000, 0.000000000000000000 ) ) ;
#41100=ORIENTED_EDGE ( 'NONE', *, *, #27297, .F. ) ;
#41101=ORIENTED_EDGE ( 'NONE', *, *, #28978, .F. ) ;
#41102=EDGE_LOOP ( 'NONE', ( #15725, #12443, #23273, #20638 ) ) ;
#41103=CARTESIAN_POINT ( 'NONE',  ( -1.909347346926324906, 3.346456692913386100, 1.220472440944875059 ) ) ;
#41104=ORIENTED_EDGE ( 'NONE', *, *, #3043, .T. ) ;
#41108=DIRECTION ( 'NONE',  ( 1.000000000000000000, 0.000000000000000000, 0.000000000000000000 ) ) ;
#41109=VECTOR ( 'NONE', #29900, 39.37007874015748143 ) ;
#41110=ADVANCED_FACE ( 'NONE', ( #31527 ), #12157, .F. ) ;
#41112=CARTESIAN_POINT ( 'NONE',  ( 0.7423782071083085965, 3.346456692913386100, -1.456692913385822630 ) ) ;
#41113=CARTESIAN_POINT ( 'NONE',  ( -0.9302092402134520821, 3.267716535433071279, -1.889763779527552146 ) ) ;
#41116=DIRECTION ( 'NONE',  ( 0.000000000000000000, -1.000000000000000000, 0.000000000000000000 ) ) ;
#41120=EDGE_LOOP ( 'NONE', ( #7968, #40755, #34586, #30757 ) ) ;
#41121=CARTESIAN_POINT ( 'NONE',  ( -0.2727639067037608278, 0.000000000000000000, -0.9842519685039344823 ) ) ;
#41122=VECTOR ( 'NONE', #22365, 39.37007874015748143 ) ;
#41123=DIRECTION ( 'NONE',  ( 1.000000000000000000, -0.000000000000000000, 0.000000000000000000 ) ) ;
#41124=DIRECTION ( 'NONE',  ( 1.000000000000000000, 0.000000000000000000, 0.000000000000000000 ) ) ;
#41125=VERTEX_POINT ( 'NONE', #5435 ) ;
#41126=ORIENTED_EDGE ( 'NONE', *, *, #8999, .F. ) ;
#41128=PLANE ( 'NONE',  #3638 ) ;
#41129=EDGE_LOOP ( 'NONE', ( #33893, #7963, #40771, #21947 ) ) ;
#41130=CARTESIAN_POINT ( 'NONE',  ( 0.000000000000000000, 3.267716535433071279, 1.062992125984246083 ) ) ;
#41131=LINE ( 'NONE', #21249, #30884 ) ;
#41132=ADVANCED_FACE ( 'NONE', ( #24544 ), #20411, .F. ) ;
#41133=AXIS2_PLACEMENT_3D ( 'NONE', #29223, #25352, #5734 ) ;
#41134=VECTOR ( 'NONE', #41534, 39.37007874015748143 ) ;
#41135=EDGE_CURVE ( 'NONE', #32722, #50026, #36945, .T. ) ;
#41136=ADVANCED_FACE ( 'NONE', ( #36426 ), #20666, .F. ) ;
#41137=VECTOR ( 'NONE', #16804, 39.37007874015748143 ) ;
#41138=CARTESIAN_POINT ( 'NONE',  ( 0.2727639067037610499, 0.000000000000000000, 2.362204724409437961 ) ) ;
#41140=DIRECTION ( 'NONE',  ( 1.000000000000000000, 0.000000000000000000, 0.000000000000000000 ) ) ;
#41141=CARTESIAN_POINT ( 'NONE',  ( 0.000000000000000000, 3.346456692913386100, 0.000000000000000000 ) ) ;
#41142=ORIENTED_EDGE ( 'NONE', *, *, #9538, .F. ) ;
#41144=DIRECTION ( 'NONE',  ( -1.000000000000000000, -0.000000000000000000, -0.000000000000000000 ) ) ;
#41145=VECTOR ( 'NONE', #47054, 39.37007874015748143 ) ;
#41148=LINE ( 'NONE', #2152, #3428 ) ;
#41149=PLANE ( 'NONE',  #13779 ) ;
#41151=LINE ( 'NONE', #9386, #44437 ) ;
#41154=CARTESIAN_POINT ( 'NONE',  ( 1.363819533518803251, 3.267716535433071279, -0.03937007874015908959 ) ) ;
#41155=ADVANCED_FACE ( 'NONE', ( #44659 ), #28148, .F. ) ;
#41156=ORIENTED_EDGE ( 'NONE', *, *, #24195, .T. ) ;
#41159=ORIENTED_EDGE ( 'NONE', *, *, #30525, .T. ) ;
#41160=DIRECTION ( 'NONE',  ( -1.000000000000000000, 0.000000000000000000, 0.000000000000000000 ) ) ;
#41162=LINE ( 'NONE', #21791, #8221 ) ;
#41164=AXIS2_PLACEMENT_3D ( 'NONE', #22049, #37807, #21798 ) ;
#41167=ORIENTED_EDGE ( 'NONE', *, *, #2840, .T. ) ;
#41171=EDGE_LOOP ( 'NONE', ( #20254, #24855, #17484, #43829 ) ) ;
#41172=DIRECTION ( 'NONE',  ( -3.469446951953613696E-16, 0.000000000000000000, -1.000000000000000000 ) ) ;
#41173=LINE ( 'NONE', #5794, #35972 ) ;
#41174=CARTESIAN_POINT ( 'NONE',  ( 1.015142113812069091, 3.346456692913386100, -1.912654141836395816 ) ) ;
#41175=EDGE_CURVE ( 'NONE', #36717, #31407, #12936, .T. ) ;
#41177=ORIENTED_EDGE ( 'NONE', *, *, #11699, .F. ) ;
#41178=ORIENTED_EDGE ( 'NONE', *, *, #2973, .F. ) ;
#41179=LINE ( 'NONE', #17929, #4863 ) ;
#41180=CARTESIAN_POINT ( 'NONE',  ( 0.5455278134075212115, 0.000000000000000000, 0.6299212598425161236 ) ) ;
#41181=CARTESIAN_POINT ( 'NONE',  ( -2.449433152083427601, 3.244423651327855485, 0.1574803149606286423 ) ) ;
#41182=ORIENTED_EDGE ( 'NONE', *, *, #18329, .T. ) ;
#41183=VECTOR ( 'NONE', #23606, 39.37007874015748143 ) ;
#41184=FACE_BOUND ( 'NONE', #35359, .T. ) ;
#41185=ORIENTED_EDGE ( 'NONE', *, *, #50211, .T. ) ;
#41186=EDGE_CURVE ( 'NONE', #22883, #20959, #44411, .T. ) ;
#41187=DIRECTION ( 'NONE',  ( 0.000000000000000000, -1.000000000000000000, 0.000000000000000000 ) ) ;
#41189=ORIENTED_EDGE ( 'NONE', *, *, #45839, .F. ) ;
#41190=VECTOR ( 'NONE', #45250, 39.37007874015748143 ) ;
#41191=FACE_OUTER_BOUND ( 'NONE', #43884, .T. ) ;
#41193=EDGE_CURVE ( 'NONE', #31407, #44897, #21445, .T. ) ;
#41195=DIRECTION ( 'NONE',  ( 1.734723475976806848E-16, 0.000000000000000000, 1.000000000000000000 ) ) ;
#41196=CARTESIAN_POINT ( 'NONE',  ( 0.000000000000000000, 3.267716535433071279, 1.732283464566921172 ) ) ;
#41198=CARTESIAN_POINT ( 'NONE',  ( 0.000000000000000000, 3.267716535433071279, 2.007874015748021268 ) ) ;
#41200=DIRECTION ( 'NONE',  ( 1.000000000000000000, 0.000000000000000000, -3.469446951953613696E-16 ) ) ;
#41201=ADVANCED_FACE ( 'NONE', ( #40555 ), #21191, .F. ) ;
#41202=CARTESIAN_POINT ( 'NONE',  ( -2.182111253630085734, 3.254137321050718956, -1.113937159217551764 ) ) ;
#41204=FACE_OUTER_BOUND ( 'NONE', #50266, .T. ) ;
#41205=CARTESIAN_POINT ( 'NONE',  ( -1.636583440222563635, 3.346456692913386100, 0.4330708661417290162 ) ) ;
#41208=CARTESIAN_POINT ( 'NONE',  ( 0.000000000000000000, 3.267716535433071279, 0.1181102362204701633 ) ) ;
#41209=VECTOR ( 'NONE', #18326, 39.37007874015748143 ) ;
#41210=ORIENTED_EDGE ( 'NONE', *, *, #34551, .F. ) ;
#41211=PLANE ( 'NONE',  #24021 ) ;
#41212=CARTESIAN_POINT ( 'NONE',  ( -1.166969139818015977, 3.267716535433071279, -0.7874015748031470974 ) ) ;
#41213=EDGE_LOOP ( 'NONE', ( #23053, #46435, #39279, #28428 ) ) ;
#41215=DIRECTION ( 'NONE',  ( -1.000000000000000000, -0.000000000000000000, -0.000000000000000000 ) ) ;
#41218=VERTEX_POINT ( 'NONE', #46174 ) ;
#41219=LINE ( 'NONE', #33983, #25495 ) ;
#41221=VERTEX_POINT ( 'NONE', #49521 ) ;
#41222=FACE_BOUND ( 'NONE', #20455, .T. ) ;
#41223=DIRECTION ( 'NONE',  ( -3.469446951953613696E-16, 0.000000000000000000, -1.000000000000000000 ) ) ;
#41224=LINE ( 'NONE', #5335, #29253 ) ;
#41225=FACE_OUTER_BOUND ( 'NONE', #40822, .T. ) ;
#41226=EDGE_CURVE ( 'NONE', #40680, #33135, #33077, .T. ) ;
#41227=ORIENTED_EDGE ( 'NONE', *, *, #27872, .T. ) ;
#41229=LINE ( 'NONE', #13098, #26301 ) ;
#41231=CARTESIAN_POINT ( 'NONE',  ( -0.6214413264104945434, 0.000000000000000000, -0.4724409448818886470 ) ) ;
#41233=EDGE_CURVE ( 'NONE', #22611, #1994, #21698, .T. ) ;
#41235=EDGE_CURVE ( 'NONE', #38291, #23969, #37716, .T. ) ;
#41236=VECTOR ( 'NONE', #29030, 39.37007874015748143 ) ;
#41237=ORIENTED_EDGE ( 'NONE', *, *, #10527, .F. ) ;
#41238=LINE ( 'NONE', #21360, #28213 ) ;
#41239=EDGE_CURVE ( 'NONE', #41221, #39889, #10081, .T. ) ;
#41240=DIRECTION ( 'NONE',  ( 1.734723475976806848E-16, -0.000000000000000000, 1.000000000000000000 ) ) ;
#41241=EDGE_LOOP ( 'NONE', ( #25042, #18108, #32289, #22557 ) ) ;
#41243=CARTESIAN_POINT ( 'NONE',  ( 1.636583440222563635, 0.000000000000000000, -0.9448818897637765168 ) ) ;
#41244=ORIENTED_EDGE ( 'NONE', *, *, #40714, .T. ) ;
#41245=ORIENTED_EDGE ( 'NONE', *, *, #26732, .T. ) ;
#41246=VECTOR ( 'NONE', #10829, 39.37007874015748143 ) ;
#41248=VERTEX_POINT ( 'NONE', #30464 ) ;
#41251=ORIENTED_EDGE ( 'NONE', *, *, #12189, .F. ) ;
#41252=VECTOR ( 'NONE', #41098, 39.37007874015748143 ) ;
#41253=DIRECTION ( 'NONE',  ( 1.734723475976806848E-16, -0.000000000000000000, 1.000000000000000000 ) ) ;
#41254=DIRECTION ( 'NONE',  ( -3.469446951953613696E-16, 0.000000000000000000, -1.000000000000000000 ) ) ;
#41256=CARTESIAN_POINT ( 'NONE',  ( 0.2727639067037604392, 3.346456692913386100, 0.2755905511810994302 ) ) ;
#41259=CARTESIAN_POINT ( 'NONE',  ( -0.8182917201112814842, 0.000000000000000000, 1.220472440944875281 ) ) ;
#41260=LINE ( 'NONE', #49710, #11430 ) ;
#41261=EDGE_CURVE ( 'NONE', #34367, #41791, #50029, .T. ) ;
#41263=CARTESIAN_POINT ( 'NONE',  ( 0.5455278134075208785, 3.346456692913386100, -1.574803149606293529 ) ) ;
#41268=DIRECTION ( 'NONE',  ( -3.469446951953613696E-16, 0.000000000000000000, -1.000000000000000000 ) ) ;
#41269=EDGE_LOOP ( 'NONE', ( #25418, #25870, #26313, #3382 ) ) ;
#41272=EDGE_LOOP ( 'NONE', ( #13464, #26139, #42879, #15245 ) ) ;
#41273=CARTESIAN_POINT ( 'NONE',  ( 0.000000000000000000, 3.267716535433071279, -0.8267716535433052849 ) ) ;
#41274=ORIENTED_EDGE ( 'NONE', *, *, #452, .F. ) ;
#41277=VECTOR ( 'NONE', #16555, 39.37007874015748143 ) ;
#41278=DIRECTION ( 'NONE',  ( -0.000000000000000000, 1.000000000000000000, -0.000000000000000000 ) ) ;
#41279=VECTOR ( 'NONE', #20310, 39.37007874015748143 ) ;
#41280=DIRECTION ( 'NONE',  ( 1.000000000000000000, 0.000000000000000000, -3.469446951953613696E-16 ) ) ;
#41281=PLANE ( 'NONE',  #31026 ) ;
#41282=ORIENTED_EDGE ( 'NONE', *, *, #16179, .F. ) ;
#41283=DIRECTION ( 'NONE',  ( -3.469446951953613696E-16, 0.000000000000000000, -1.000000000000000000 ) ) ;
#41284=ORIENTED_EDGE ( 'NONE', *, *, #11452, .T. ) ;
#41286=ORIENTED_EDGE ( 'NONE', *, *, #13187, .T. ) ;
#41287=CARTESIAN_POINT ( 'NONE',  ( -1.166969139818015977, 3.267716535433071279, 2.047244094488179567 ) ) ;
#41290=VERTEX_POINT ( 'NONE', #21958 ) ;
#41292=ADVANCED_FACE ( 'NONE', ( #17823 ), #29952, .F. ) ;
#41293=LINE ( 'NONE', #31444, #45480 ) ;
#41294=EDGE_CURVE ( 'NONE', #10030, #16727, #18839, .T. ) ;
#41296=LINE ( 'NONE', #132, #4114 ) ;
#41297=ORIENTED_EDGE ( 'NONE', *, *, #17357, .F. ) ;
#41299=DIRECTION ( 'NONE',  ( 1.000000000000000000, 0.000000000000000000, 0.000000000000000000 ) ) ;
#41300=FACE_BOUND ( 'NONE', #5274, .T. ) ;
#41301=ORIENTED_EDGE ( 'NONE', *, *, #11585, .T. ) ;
#41302=DIRECTION ( 'NONE',  ( -1.000000000000000000, 0.000000000000000000, 0.000000000000000000 ) ) ;
#41303=CARTESIAN_POINT ( 'NONE',  ( 0.5455278134075208785, 3.267716535433071279, -1.771653543307081025 ) ) ;
#41305=ORIENTED_EDGE ( 'NONE', *, *, #18587, .F. ) ;
#41307=DIRECTION ( 'NONE',  ( -3.469446951953613696E-16, 0.000000000000000000, -1.000000000000000000 ) ) ;
#41308=ORIENTED_EDGE ( 'NONE', *, *, #44323, .F. ) ;
#41309=EDGE_LOOP ( 'NONE', ( #15490, #4387, #45687, #42607 ) ) ;
#41311=ORIENTED_EDGE ( 'NONE', *, *, #41091, .T. ) ;
#41312=CARTESIAN_POINT ( 'NONE',  ( 0.8182917201112817063, 3.267716535433071279, -2.244094488188969283 ) ) ;
#41314=CARTESIAN_POINT ( 'NONE',  ( 1.909347346926324684, 0.000000000000000000, 0.7874015748031456541 ) ) ;
#41315=EDGE_CURVE ( 'NONE', #1290, #34165, #33590, .T. ) ;
#41316=VECTOR ( 'NONE', #21362, 39.37007874015748143 ) ;
#41318=CARTESIAN_POINT ( 'NONE',  ( 0.000000000000000000, 3.267716535433071279, 0.000000000000000000 ) ) ;
#41319=ADVANCED_FACE ( 'NONE', ( #34589 ), #2837, .F. ) ;
#41321=EDGE_LOOP ( 'NONE', ( #38638, #8380, #49442, #47157 ) ) ;
#41323=DIRECTION ( 'NONE',  ( -3.469446951953613696E-16, 0.000000000000000000, -1.000000000000000000 ) ) ;
#41324=EDGE_CURVE ( 'NONE', #40996, #16084, #49277, .T. ) ;
#41325=DIRECTION ( 'NONE',  ( 1.000000000000000000, -0.000000000000000000, 0.000000000000000000 ) ) ;
#41326=VECTOR ( 'NONE', #42487, 39.37007874015748143 ) ;
#41327=DIRECTION ( 'NONE',  ( 1.734723475976806848E-16, -0.000000000000000000, 1.000000000000000000 ) ) ;
#41328=PLANE ( 'NONE',  #5046 ) ;
#41329=VECTOR ( 'NONE', #24439, 39.37007874015748143 ) ;
#41330=DIRECTION ( 'NONE',  ( -0.000000000000000000, 0.000000000000000000, 1.000000000000000000 ) ) ;
#41332=EDGE_LOOP ( 'NONE', ( #1013, #28275, #36161, #1456 ) ) ;
#41334=DIRECTION ( 'NONE',  ( -0.000000000000000000, 1.000000000000000000, -0.000000000000000000 ) ) ;
#41335=ORIENTED_EDGE ( 'NONE', *, *, #14796, .T. ) ;
#41336=EDGE_LOOP ( 'NONE', ( #8081, #23713, #37559, #12483 ) ) ;
#41337=DIRECTION ( 'NONE',  ( -1.000000000000000000, 0.000000000000000000, 1.734723475976806848E-16 ) ) ;
#41339=EDGE_LOOP ( 'NONE', ( #48389, #7145, #22628, #4570 ) ) ;
#41341=ORIENTED_EDGE ( 'NONE', *, *, #47657, .T. ) ;
#41342=VECTOR ( 'NONE', #20025, 39.37007874015748143 ) ;
#41344=CARTESIAN_POINT ( 'NONE',  ( -2.106299212598425008, 3.346456692913386100, -6.146657985744592735E-16 ) ) ;
#41346=ADVANCED_FACE ( 'NONE', ( #14713 ), #14460, .F. ) ;
#41347=ORIENTED_EDGE ( 'NONE', *, *, #50333, .T. ) ;
#41348=VECTOR ( 'NONE', #24901, 39.37007874015748143 ) ;
#41349=CARTESIAN_POINT ( 'NONE',  ( 2.378961647330872786, 0.000000000000000000, 0.6299212598425161236 ) ) ;
#41350=EDGE_CURVE ( 'NONE', #46637, #45913, #14965, .T. ) ;
#41352=VERTEX_POINT ( 'NONE', #7224 ) ;
#41355=AXIS2_PLACEMENT_3D ( 'NONE', #20259, #40659, #387 ) ;
#41357=EDGE_CURVE ( 'NONE', #45206, #14060, #22963, .T. ) ;
#41358=AXIS2_PLACEMENT_3D ( 'NONE', #40630, #9384, #37021 ) ;
#41362=DIRECTION ( 'NONE',  ( -3.469446951953613696E-16, 0.000000000000000000, -1.000000000000000000 ) ) ;
#41363=EDGE_LOOP ( 'NONE', ( #41948, #10912, #13916, #20919 ) ) ;
#41365=FACE_OUTER_BOUND ( 'NONE', #25623, .T. ) ;
#41366=LINE ( 'NONE', #17871, #24136 ) ;
#41368=EDGE_LOOP ( 'NONE', ( #6179, #6913, #6592, #41063 ) ) ;
#41370=CARTESIAN_POINT ( 'NONE',  ( 0.1968503937007877735, 0.000000000000000000, 1.377952755905504256 ) ) ;
#41371=EDGE_CURVE ( 'NONE', #27812, #45405, #15212, .T. ) ;
#41372=LINE ( 'NONE', #21241, #27774 ) ;
#41374=ORIENTED_EDGE ( 'NONE', *, *, #32399, .F. ) ;
#41378=ORIENTED_EDGE ( 'NONE', *, *, #24290, .T. ) ;
#41381=VECTOR ( 'NONE', #49845, 39.37007874015748143 ) ;
#41382=VECTOR ( 'NONE', #15511, 39.37007874015748143 ) ;
#41384=FACE_OUTER_BOUND ( 'NONE', #2362, .T. ) ;
#41386=LINE ( 'NONE', #6011, #1518 ) ;
#41387=ORIENTED_EDGE ( 'NONE', *, *, #41995, .F. ) ;
#41389=DIRECTION ( 'NONE',  ( 1.000000000000000000, 0.000000000000000000, 0.000000000000000000 ) ) ;
#41393=VECTOR ( 'NONE', #50980, 39.37007874015748143 ) ;
#41397=ORIENTED_EDGE ( 'NONE', *, *, #10841, .F. ) ;
#41399=CARTESIAN_POINT ( 'NONE',  ( 0.000000000000000000, 3.267716535433071279, 0.9448818897637749625 ) ) ;
#41401=DIRECTION ( 'NONE',  ( -0.000000000000000000, 1.000000000000000000, -0.000000000000000000 ) ) ;
#41405=PLANE ( 'NONE',  #47348 ) ;
#41406=DIRECTION ( 'NONE',  ( 1.000000000000000000, -0.000000000000000000, 0.000000000000000000 ) ) ;
#41408=CARTESIAN_POINT ( 'NONE',  ( 0.2727639067037605503, 3.267716535433071279, -4.731699523581609741E-17 ) ) ;
#41409=EDGE_CURVE ( 'NONE', #38085, #10739, #15715, .T. ) ;
#41410=VERTEX_POINT ( 'NONE', #26825 ) ;
#41411=ORIENTED_EDGE ( 'NONE', *, *, #51038, .T. ) ;
#41413=LINE ( 'NONE', #897, #19685 ) ;
#41414=ADVANCED_FACE ( 'NONE', ( #35093 ), #50519, .F. ) ;
#41417=CARTESIAN_POINT ( 'NONE',  ( -1.636583440222563635, 3.346456692913386100, 1.062992125984246083 ) ) ;
#41420=ORIENTED_EDGE ( 'NONE', *, *, #11110, .F. ) ;
#41421=AXIS2_PLACEMENT_3D ( 'NONE', #6698, #26809, #46161 ) ;
#41422=ORIENTED_EDGE ( 'NONE', *, *, #41542, .F. ) ;
#41424=LINE ( 'NONE', #41180, #4373 ) ;
#41425=DIRECTION ( 'NONE',  ( -0.000000000000000000, 1.000000000000000000, -0.000000000000000000 ) ) ;
#41427=ORIENTED_EDGE ( 'NONE', *, *, #18708, .T. ) ;
#41428=CARTESIAN_POINT ( 'NONE',  ( -1.909347346926324462, 3.267716535433071279, 3.312189666507127188E-16 ) ) ;
#41430=ORIENTED_EDGE ( 'NONE', *, *, #35573, .F. ) ;
#41431=DIRECTION ( 'NONE',  ( 0.000000000000000000, -1.000000000000000000, 0.000000000000000000 ) ) ;
#41432=EDGE_LOOP ( 'NONE', ( #49798, #5912, #13939, #5279 ) ) ;
#41433=VECTOR ( 'NONE', #26745, 39.37007874015748143 ) ;
#41435=DIRECTION ( 'NONE',  ( 0.000000000000000000, 0.000000000000000000, -1.000000000000000000 ) ) ;
#41436=PLANE ( 'NONE',  #15978 ) ;
#41437=VECTOR ( 'NONE', #48652, 39.37007874015748143 ) ;
#41439=ORIENTED_EDGE ( 'NONE', *, *, #11541, .F. ) ;
#41440=DIRECTION ( 'NONE',  ( 0.000000000000000000, 0.000000000000000000, 1.000000000000000000 ) ) ;
#41441=PLANE ( 'NONE',  #1581 ) ;
#41443=EDGE_CURVE ( 'NONE', #4205, #8227, #42822, .T. ) ;
#41444=DIRECTION ( 'NONE',  ( 1.000000000000000000, 0.000000000000000000, 0.000000000000000000 ) ) ;
#41445=FACE_OUTER_BOUND ( 'NONE', #28659, .T. ) ;
#41446=ADVANCED_FACE ( 'NONE', ( #39211 ), #20084, .F. ) ;
#41447=DIRECTION ( 'NONE',  ( -3.469446951953613696E-16, 0.000000000000000000, -1.000000000000000000 ) ) ;
#41448=DIRECTION ( 'NONE',  ( -0.000000000000000000, 0.000000000000000000, 1.000000000000000000 ) ) ;
#41450=EDGE_LOOP ( 'NONE', ( #27340, #50759, #17830, #27015 ) ) ;
#41451=DIRECTION ( 'NONE',  ( 0.000000000000000000, 0.000000000000000000, -1.000000000000000000 ) ) ;
#41453=EDGE_CURVE ( 'NONE', #31299, #27036, #11589, .T. ) ;
#41454=DIRECTION ( 'NONE',  ( -1.000000000000000000, -0.000000000000000000, -0.000000000000000000 ) ) ;
#41455=ORIENTED_EDGE ( 'NONE', *, *, #1693, .T. ) ;
#41456=VECTOR ( 'NONE', #31971, 39.37007874015748143 ) ;
#41457=DIRECTION ( 'NONE',  ( -3.469446951953613696E-16, 0.000000000000000000, -1.000000000000000000 ) ) ;
#41458=CARTESIAN_POINT ( 'NONE',  ( -1.909347346926324462, 3.346456692913386100, 1.102362204724404160 ) ) ;
#41460=LINE ( 'NONE', #18219, #37841 ) ;
#41461=DIRECTION ( 'NONE',  ( -0.000000000000000000, 1.000000000000000000, -0.000000000000000000 ) ) ;
#41463=VECTOR ( 'NONE', #9164, 39.37007874015748143 ) ;
#41466=LINE ( 'NONE', #10225, #40365 ) ;
#41467=VERTEX_POINT ( 'NONE', #43067 ) ;
#41468=FACE_BOUND ( 'NONE', #18031, .T. ) ;
#41470=VECTOR ( 'NONE', #29951, 39.37007874015748143 ) ;
#41471=FACE_OUTER_BOUND ( 'NONE', #1647, .T. ) ;
#41473=ORIENTED_EDGE ( 'NONE', *, *, #7848, .F. ) ;
#41475=CARTESIAN_POINT ( 'NONE',  ( -1.195183497228115035E-16, 3.346456692913386100, -1.259842519685035134 ) ) ;
#41476=EDGE_LOOP ( 'NONE', ( #10023, #52, #27547, #6725 ) ) ;
#41479=EDGE_CURVE ( 'NONE', #472, #187, #3850, .T. ) ;
#41480=CARTESIAN_POINT ( 'NONE',  ( 0.2727639067037604947, 0.000000000000000000, 0.4724409448818868706 ) ) ;
#41481=EDGE_CURVE ( 'NONE', #16704, #9041, #35348, .T. ) ;
#41482=EDGE_LOOP ( 'NONE', ( #490, #2975, #49886, #35516 ) ) ;
#41484=EDGE_CURVE ( 'NONE', #43099, #14557, #31470, .T. ) ;
#41486=ORIENTED_EDGE ( 'NONE', *, *, #17507, .F. ) ;
#41488=ORIENTED_EDGE ( 'NONE', *, *, #13972, .T. ) ;
#41489=ORIENTED_EDGE ( 'NONE', *, *, #30790, .F. ) ;
#41490=ORIENTED_EDGE ( 'NONE', *, *, #9534, .F. ) ;
#41491=ORIENTED_EDGE ( 'NONE', *, *, #19946, .T. ) ;
#41494=VERTEX_POINT ( 'NONE', #43327 ) ;
#41496=CARTESIAN_POINT ( 'NONE',  ( -1.166969139818016865, 3.267716535433071279, 4.048737525165548620E-16 ) ) ;
#41500=EDGE_CURVE ( 'NONE', #18533, #35538, #7971, .T. ) ;
#41501=CARTESIAN_POINT ( 'NONE',  ( 0.1968503937007873017, 3.267716535433071279, -0.6299212598425177889 ) ) ;
#41502=ORIENTED_EDGE ( 'NONE', *, *, #30868, .F. ) ;
#41503=PLANE ( 'NONE',  #40129 ) ;
#41504=CARTESIAN_POINT ( 'NONE',  ( 0.7423782071083087075, 3.346456692913386100, 0.9448818897637746295 ) ) ;
#41505=AXIS2_PLACEMENT_3D ( 'NONE', #26892, #2905, #18907 ) ;
#41507=CARTESIAN_POINT ( 'NONE',  ( 0.8182917201112817063, 3.267716535433071279, -1.732283464566923614 ) ) ;
#41508=CARTESIAN_POINT ( 'NONE',  ( -1.712496953225537633, 0.000000000000000000, -0.7874015748031470974 ) ) ;
#41511=CARTESIAN_POINT ( 'NONE',  ( 1.833433833923351353, 3.346456692913386100, -0.3149606299212596716 ) ) ;
#41513=FACE_OUTER_BOUND ( 'NONE', #41855, .T. ) ;
#41514=VERTEX_POINT ( 'NONE', #20866 ) ;
#41515=CARTESIAN_POINT ( 'NONE',  ( -0.5455278134075208785, 0.000000000000000000, 0.7480314960629874665 ) ) ;
#41517=CARTESIAN_POINT ( 'NONE',  ( 0.000000000000000000, 3.267716535433071279, 0.000000000000000000 ) ) ;
#41519=LINE ( 'NONE', #15102, #43215 ) ;
#41520=EDGE_CURVE ( 'NONE', #50367, #39693, #25251, .T. ) ;
#41521=VERTEX_POINT ( 'NONE', #24995 ) ;
#41522=CARTESIAN_POINT ( 'NONE',  ( 1.560669927219590525, 3.267716535433071279, -0.6692913385826764205 ) ) ;
#41523=EDGE_CURVE ( 'NONE', #19504, #22619, #4611, .T. ) ;
#41524=DIRECTION ( 'NONE',  ( 1.734723475976806848E-16, -0.000000000000000000, 1.000000000000000000 ) ) ;
#41525=CARTESIAN_POINT ( 'NONE',  ( -1.712496953225537633, 3.267716535433071279, 1.226315847645293999 ) ) ;
#41527=DIRECTION ( 'NONE',  ( -3.469446951953613696E-16, 0.000000000000000000, -1.000000000000000000 ) ) ;
#41528=EDGE_LOOP ( 'NONE', ( #38842, #18558, #45073, #45937 ) ) ;
#41529=LINE ( 'NONE', #10289, #6742 ) ;
#41530=ORIENTED_EDGE ( 'NONE', *, *, #34662, .T. ) ;
#41531=ORIENTED_EDGE ( 'NONE', *, *, #47984, .F. ) ;
#41532=DIRECTION ( 'NONE',  ( -3.469446951953613696E-16, 0.000000000000000000, -1.000000000000000000 ) ) ;
#41533=ORIENTED_EDGE ( 'NONE', *, *, #9125, .T. ) ;
#41534=DIRECTION ( 'NONE',  ( -0.000000000000000000, 1.000000000000000000, -0.000000000000000000 ) ) ;
#41535=DIRECTION ( 'NONE',  ( 1.000000000000000000, 0.000000000000000000, 0.000000000000000000 ) ) ;
#41536=VERTEX_POINT ( 'NONE', #36879 ) ;
#41537=AXIS2_PLACEMENT_3D ( 'NONE', #43999, #47842, #899 ) ;
#41538=EDGE_CURVE ( 'NONE', #16952, #23409, #24744, .T. ) ;
#41541=DIRECTION ( 'NONE',  ( 0.000000000000000000, -1.000000000000000000, 0.000000000000000000 ) ) ;
#41542=EDGE_CURVE ( 'NONE', #28842, #49676, #32501, .T. ) ;
#41544=CARTESIAN_POINT ( 'NONE',  ( -1.909347346926324906, 3.267716535433071279, -0.6692913385826758654 ) ) ;
#41545=EDGE_CURVE ( 'NONE', #38459, #42332, #32764, .T. ) ;
#41549=FACE_BOUND ( 'NONE', #44056, .T. ) ;
#41550=EDGE_LOOP ( 'NONE', ( #24094, #42476, #26499, #18003 ) ) ;
#41552=CARTESIAN_POINT ( 'NONE',  ( 0.000000000000000000, 3.267716535433071279, -1.259842519685035800 ) ) ;
#41556=DIRECTION ( 'NONE',  ( 1.000000000000000000, 0.000000000000000000, 0.000000000000000000 ) ) ;
#41557=VERTEX_POINT ( 'NONE', #8485 ) ;
#41560=CARTESIAN_POINT ( 'NONE',  ( -1.439733046521776139, 3.267716535433071279, 4.995077429881866871E-16 ) ) ;
#41562=CARTESIAN_POINT ( 'NONE',  ( 1.560669927219590747, 0.000000000000000000, 1.417322834645662777 ) ) ;
#41567=VECTOR ( 'NONE', #20539, 39.37007874015748143 ) ;
#41568=CARTESIAN_POINT ( 'NONE',  ( 1.287906020515830141, 0.000000000000000000, -0.6299212598425181220 ) ) ;
#41571=CARTESIAN_POINT ( 'NONE',  ( -0.8942052331142552601, 0.000000000000000000, -0.8267716535433052849 ) ) ;
#41575=AXIS2_PLACEMENT_3D ( 'NONE', #13524, #40891, #29526 ) ;
#41577=VECTOR ( 'NONE', #8549, 39.37007874015748143 ) ;
#41578=ADVANCED_FACE ( 'NONE', ( #20612 ), #40748, .F. ) ;
#41581=LINE ( 'NONE', #18338, #26713 ) ;
#41582=VECTOR ( 'NONE', #27468, 39.37007874015748143 ) ;
#41583=ORIENTED_EDGE ( 'NONE', *, *, #27388, .F. ) ;
#41584=DIRECTION ( 'NONE',  ( -0.000000000000000000, 1.000000000000000000, -0.000000000000000000 ) ) ;
#41586=ORIENTED_EDGE ( 'NONE', *, *, #2888, .F. ) ;
#41587=EDGE_LOOP ( 'NONE', ( #49356, #39051, #17081, #10389 ) ) ;
#41589=ORIENTED_EDGE ( 'NONE', *, *, #45563, .T. ) ;
#41590=EDGE_CURVE ( 'NONE', #2069, #12621, #9503, .T. ) ;
#41592=ORIENTED_EDGE ( 'NONE', *, *, #32460, .T. ) ;
#41593=CARTESIAN_POINT ( 'NONE',  ( 2.106197740627112402, 3.346456692913386100, -0.02067487291359444701 ) ) ;
#41595=ORIENTED_EDGE ( 'NONE', *, *, #40978, .F. ) ;
#41596=CARTESIAN_POINT ( 'NONE',  ( 0.000000000000000000, 2.344748451760389596, 0.000000000000000000 ) ) ;
#41597=DIRECTION ( 'NONE',  ( -0.000000000000000000, 1.000000000000000000, -0.000000000000000000 ) ) ;
#41598=EDGE_CURVE ( 'NONE', #32620, #7484, #47937, .T. ) ;
#41599=EDGE_LOOP ( 'NONE', ( #50858, #26847, #7050, #7734 ) ) ;
#41600=ORIENTED_EDGE ( 'NONE', *, *, #7765, .T. ) ;
#41605=VERTEX_POINT ( 'NONE', #12356 ) ;
#41607=DIRECTION ( 'NONE',  ( 0.000000000000000000, 1.000000000000000000, 0.000000000000000000 ) ) ;
#41608=CARTESIAN_POINT ( 'NONE',  ( -2.258024766633058622, 3.267716535433071279, -0.3543307086614173040 ) ) ;
#41610=AXIS2_PLACEMENT_3D ( 'NONE', #22168, #13397, #33798 ) ;
#41611=VECTOR ( 'NONE', #49722, 39.37007874015748143 ) ;
#41614=DIRECTION ( 'NONE',  ( 1.000000000000000000, 0.000000000000000000, -3.469446951953613696E-16 ) ) ;
#41615=DIRECTION ( 'NONE',  ( 0.000000000000000000, -1.000000000000000000, 0.000000000000000000 ) ) ;
#41617=VERTEX_POINT ( 'NONE', #43834 ) ;
#41618=CARTESIAN_POINT ( 'NONE',  ( 0.1968503937007878291, 3.346456692913386100, 2.097080421798980687 ) ) ;
#41619=CARTESIAN_POINT ( 'NONE',  ( 2.106197740627111514, 3.346456692913386100, -0.9842519685039348154 ) ) ;
#41620=VECTOR ( 'NONE', #23013, 39.37007874015748143 ) ;
#41621=DIRECTION ( 'NONE',  ( -3.469446951953613696E-16, 0.000000000000000000, -1.000000000000000000 ) ) ;
#41622=ORIENTED_EDGE ( 'NONE', *, *, #41294, .F. ) ;
#41631=ORIENTED_EDGE ( 'NONE', *, *, #28592, .T. ) ;
#41632=DIRECTION ( 'NONE',  ( -3.469446951953613696E-16, 0.000000000000000000, -1.000000000000000000 ) ) ;
#41633=DIRECTION ( 'NONE',  ( 1.734723475976806848E-16, -0.000000000000000000, 1.000000000000000000 ) ) ;
#41634=EDGE_CURVE ( 'NONE', #15854, #17057, #41260, .T. ) ;
#41635=DIRECTION ( 'NONE',  ( 1.000000000000000000, 0.000000000000000000, 0.000000000000000000 ) ) ;
#41636=EDGE_CURVE ( 'NONE', #10110, #40291, #14390, .T. ) ;
#41637=CARTESIAN_POINT ( 'NONE',  ( 0.2727639067037602172, 0.000000000000000000, -2.047244094488182231 ) ) ;
#41638=DIRECTION ( 'NONE',  ( -0.000000000000000000, 1.000000000000000000, -0.000000000000000000 ) ) ;
#41641=EDGE_CURVE ( 'NONE', #24717, #45399, #21885, .T. ) ;
#41642=CARTESIAN_POINT ( 'NONE',  ( -1.439733046521776583, 3.346456692913386100, -0.6299212598425177889 ) ) ;
#41643=DIRECTION ( 'NONE',  ( 1.734723475976806848E-16, 0.000000000000000000, 1.000000000000000000 ) ) ;
#41645=LINE ( 'NONE', #26149, #42186 ) ;
#41647=ORIENTED_EDGE ( 'NONE', *, *, #34571, .F. ) ;
#41648=LINE ( 'NONE', #3412, #13356 ) ;
#41652=CARTESIAN_POINT ( 'NONE',  ( -0.8182917201112819283, 3.267716535433071279, -0.6692913385826760875 ) ) ;
#41653=VECTOR ( 'NONE', #14614, 39.37007874015748143 ) ;
#41655=PLANE ( 'NONE',  #5717 ) ;
#41656=LINE ( 'NONE', #29266, #9292 ) ;
#41659=DIRECTION ( 'NONE',  ( -3.469446951953613696E-16, 0.000000000000000000, -1.000000000000000000 ) ) ;
#41660=CARTESIAN_POINT ( 'NONE',  ( 1.560669927219590303, 0.000000000000000000, -1.732283464566923170 ) ) ;
#41663=PLANE ( 'NONE',  #39172 ) ;
#41664=ORIENTED_EDGE ( 'NONE', *, *, #23854, .T. ) ;
#41666=CARTESIAN_POINT ( 'NONE',  ( -1.091055626815042645, 3.346456692913386100, -1.574803149606293529 ) ) ;
#41668=EDGE_CURVE ( 'NONE', #37443, #17837, #37391, .T. ) ;
#41669=ORIENTED_EDGE ( 'NONE', *, *, #1883, .F. ) ;
#41670=DIRECTION ( 'NONE',  ( 1.000000000000000000, 0.000000000000000000, 0.000000000000000000 ) ) ;
#41671=LINE ( 'NONE', #17163, #40952 ) ;
#41672=CARTESIAN_POINT ( 'NONE',  ( 0.8182917201112819283, 0.000000000000000000, -0.4724409448818889246 ) ) ;
#41673=ADVANCED_FACE ( 'NONE', ( #2770 ), #22143, .F. ) ;
#41674=ORIENTED_EDGE ( 'NONE', *, *, #16731, .F. ) ;
#41675=ORIENTED_EDGE ( 'NONE', *, *, #42368, .F. ) ;
#41676=LINE ( 'NONE', #6312, #36187 ) ;
#41677=PLANE ( 'NONE',  #34855 ) ;
#41679=ORIENTED_EDGE ( 'NONE', *, *, #43858, .F. ) ;
#41680=CARTESIAN_POINT ( 'NONE',  ( 1.091055626815042645, 3.267716535433071279, -0.1968503937007883287 ) ) ;
#41681=LINE ( 'NONE', #29806, #5456 ) ;
#41683=ORIENTED_EDGE ( 'NONE', *, *, #43640, .F. ) ;
#41685=DIRECTION ( 'NONE',  ( 1.000000000000000000, -0.000000000000000000, 0.000000000000000000 ) ) ;
#41686=ORIENTED_EDGE ( 'NONE', *, *, #4852, .T. ) ;
#41687=VERTEX_POINT ( 'NONE', #38152 ) ;
#41688=LINE ( 'NONE', #18705, #16356 ) ;
#41689=DIRECTION ( 'NONE',  ( 1.000000000000000000, 0.000000000000000000, 0.000000000000000000 ) ) ;
#41690=VECTOR ( 'NONE', #32592, 39.37007874015748143 ) ;
#41693=ORIENTED_EDGE ( 'NONE', *, *, #45268, .T. ) ;
#41695=FACE_OUTER_BOUND ( 'NONE', #45088, .T. ) ;
#41696=EDGE_LOOP ( 'NONE', ( #27687, #1134, #21419, #16289 ) ) ;
#41697=CIRCLE ( 'NONE', #37612, 2.165354330708661568 ) ;
#41698=ORIENTED_EDGE ( 'NONE', *, *, #20496, .F. ) ;
#41700=DIRECTION ( 'NONE',  ( -0.000000000000000000, 0.000000000000000000, 1.000000000000000000 ) ) ;
#41701=DIRECTION ( 'NONE',  ( -1.000000000000000000, 0.000000000000000000, -0.000000000000000000 ) ) ;
#41703=DIRECTION ( 'NONE',  ( -1.000000000000000000, 0.000000000000000000, -0.000000000000000000 ) ) ;
#41708=PLANE ( 'NONE',  #19070 ) ;
#41711=DIRECTION ( 'NONE',  ( 0.000000000000000000, 0.000000000000000000, -1.000000000000000000 ) ) ;
#41712=CARTESIAN_POINT ( 'NONE',  ( -0.3486774197067340486, 3.267716535433071279, -0.5118110236220467790 ) ) ;
#41713=VERTEX_POINT ( 'NONE', #25754 ) ;
#41714=LINE ( 'NONE', #6351, #8965 ) ;
#41715=EDGE_CURVE ( 'NONE', #8542, #3630, #45100, .T. ) ;
#41716=DIRECTION ( 'NONE',  ( 1.000000000000000000, 0.000000000000000000, 0.000000000000000000 ) ) ;
#41718=VECTOR ( 'NONE', #32059, 39.37007874015748143 ) ;
#41721=CARTESIAN_POINT ( 'NONE',  ( 0.000000000000000000, 3.267716535433071279, 1.102362204724403938 ) ) ;
#41722=ORIENTED_EDGE ( 'NONE', *, *, #9689, .T. ) ;
#41723=FACE_BOUND ( 'NONE', #37727, .T. ) ;
#41724=AXIS2_PLACEMENT_3D ( 'NONE', #3874, #23481, #243 ) ;
#41726=CARTESIAN_POINT ( 'NONE',  ( 1.636583440222563635, 3.346456692913386100, -1.325930245594399537 ) ) ;
#41728=CARTESIAN_POINT ( 'NONE',  ( 0.1968503937007873017, 3.346456692913386100, 0.3149606299212576177 ) ) ;
#41729=AXIS2_PLACEMENT_3D ( 'NONE', #27187, #7331, #18945 ) ;
#41730=VECTOR ( 'NONE', #2742, 39.37007874015748143 ) ;
#41731=VERTEX_POINT ( 'NONE', #41504 ) ;
#41733=DIRECTION ( 'NONE',  ( 0.000000000000000000, -1.000000000000000000, 0.000000000000000000 ) ) ;
#41734=EDGE_CURVE ( 'NONE', #35545, #122, #37647, .T. ) ;
#41736=ORIENTED_EDGE ( 'NONE', *, *, #17940, .F. ) ;
#41738=ORIENTED_EDGE ( 'NONE', *, *, #48780, .T. ) ;
#41739=DIRECTION ( 'NONE',  ( 1.000000000000000000, 0.000000000000000000, 0.000000000000000000 ) ) ;
#41740=DIRECTION ( 'NONE',  ( -0.000000000000000000, 1.000000000000000000, -0.000000000000000000 ) ) ;
#41742=DIRECTION ( 'NONE',  ( -3.469446951953613696E-16, 0.000000000000000000, -1.000000000000000000 ) ) ;
#41745=EDGE_CURVE ( 'NONE', #13697, #14697, #18012, .T. ) ;
#41746=ORIENTED_EDGE ( 'NONE', *, *, #5959, .F. ) ;
#41747=ORIENTED_EDGE ( 'NONE', *, *, #5871, .F. ) ;
#41751=VERTEX_POINT ( 'NONE', #21383 ) ;
#41752=CARTESIAN_POINT ( 'NONE',  ( 0.1968503937007873017, 3.346456692913386100, 0.6299212598425161236 ) ) ;
#41753=AXIS2_PLACEMENT_3D ( 'NONE', #36980, #9859, #36724 ) ;
#41754=FACE_OUTER_BOUND ( 'NONE', #46281, .T. ) ;
#41755=AXIS2_PLACEMENT_3D ( 'NONE', #21058, #40935, #41440 ) ;
#41756=CARTESIAN_POINT ( 'NONE',  ( -1.195183497228115035E-16, 0.000000000000000000, 0.3149606299212576177 ) ) ;
#41757=VECTOR ( 'NONE', #32733, 39.37007874015748143 ) ;
#41758=DIRECTION ( 'NONE',  ( 0.000000000000000000, 1.000000000000000000, 0.000000000000000000 ) ) ;
#41760=ORIENTED_EDGE ( 'NONE', *, *, #49095, .T. ) ;
#41761=EDGE_CURVE ( 'NONE', #22865, #7418, #37136, .T. ) ;
#41763=LINE ( 'NONE', #42016, #4418 ) ;
#41767=VERTEX_POINT ( 'NONE', #13633 ) ;
#41768=LINE ( 'NONE', #1758, #16593 ) ;
#41769=EDGE_CURVE ( 'NONE', #3690, #50140, #47360, .T. ) ;
#41770=CARTESIAN_POINT ( 'NONE',  ( -1.091055626815042645, 0.000000000000000000, -1.574803149606293529 ) ) ;
#41772=LINE ( 'NONE', #49721, #707 ) ;
#41773=EDGE_CURVE ( 'NONE', #4193, #25793, #3529, .T. ) ;
#41776=VERTEX_POINT ( 'NONE', #46861 ) ;
#41777=VERTEX_POINT ( 'NONE', #35031 ) ;
#41778=CARTESIAN_POINT ( 'NONE',  ( -1.363819533518803473, 3.346456692913386100, -0.4724409448818886470 ) ) ;
#41779=LINE ( 'NONE', #6417, #39910 ) ;
#41780=CARTESIAN_POINT ( 'NONE',  ( 1.091055626815042423, 3.346456692913386100, -1.574803149606294417 ) ) ;
#41782=EDGE_CURVE ( 'NONE', #28296, #23553, #49314, .T. ) ;
#41783=LINE ( 'NONE', #26289, #42596 ) ;
#41785=AXIS2_PLACEMENT_3D ( 'NONE', #36435, #32572, #21640 ) ;
#41786=CARTESIAN_POINT ( 'NONE',  ( 0.7423782071083087075, 0.000000000000000000, -0.6299212598425181220 ) ) ;
#41789=ORIENTED_EDGE ( 'NONE', *, *, #46008, .F. ) ;
#41791=VERTEX_POINT ( 'NONE', #39405 ) ;
#41792=EDGE_CURVE ( 'NONE', #32442, #22912, #50964, .T. ) ;
#41793=CARTESIAN_POINT ( 'NONE',  ( 1.363819533518803251, 3.346456692913386100, -0.03937007874015908959 ) ) ;
#41794=DIRECTION ( 'NONE',  ( -1.000000000000000000, 0.000000000000000000, 1.734723475976806848E-16 ) ) ;
#41795=ORIENTED_EDGE ( 'NONE', *, *, #8974, .T. ) ;
#41796=CARTESIAN_POINT ( 'NONE',  ( 1.833433833923351353, 3.346456692913386100, 1.377952755905504256 ) ) ;
#41797=VECTOR ( 'NONE', #12468, 39.37007874015748143 ) ;
#41801=CARTESIAN_POINT ( 'NONE',  ( 0.5455278134075212115, 0.000000000000000000, -0.3149606299212593941 ) ) ;
#41802=ORIENTED_EDGE ( 'NONE', *, *, #45928, .T. ) ;
#41803=ORIENTED_EDGE ( 'NONE', *, *, #27981, .T. ) ;
#41805=FACE_BOUND ( 'NONE', #28635, .T. ) ;
#41809=DIRECTION ( 'NONE',  ( 1.000000000000000000, 0.000000000000000000, -3.469446951953613696E-16 ) ) ;
#41811=ORIENTED_EDGE ( 'NONE', *, *, #24467, .F. ) ;
#41813=CARTESIAN_POINT ( 'NONE',  ( 1.287906020515829919, 0.000000000000000000, -2.086614173228339641 ) ) ;
#41816=EDGE_LOOP ( 'NONE', ( #29817, #18650, #27570, #34190 ) ) ;
#41817=ORIENTED_EDGE ( 'NONE', *, *, #7719, .F. ) ;
#41819=CARTESIAN_POINT ( 'NONE',  ( -0.5455278134075214336, 3.346456692913386100, -0.1968503937007883287 ) ) ;
#41820=DIRECTION ( 'NONE',  ( -0.000000000000000000, 1.000000000000000000, -0.000000000000000000 ) ) ;
#41821=VECTOR ( 'NONE', #17776, 39.37007874015748143 ) ;
#41822=VECTOR ( 'NONE', #38293, 39.37007874015748143 ) ;
#41823=CARTESIAN_POINT ( 'NONE',  ( 1.818390528211208945, 3.346456692913386100, 1.062992125984245639 ) ) ;
#41825=ORIENTED_EDGE ( 'NONE', *, *, #36369, .F. ) ;
#41826=ORIENTED_EDGE ( 'NONE', *, *, #22824, .T. ) ;
#41828=VECTOR ( 'NONE', #50902, 39.37007874015748143 ) ;
#41830=CARTESIAN_POINT ( 'NONE',  ( -0.8942052331142552601, 3.346456692913386100, -0.5118110236220467790 ) ) ;
#41834=LINE ( 'NONE', #22218, #15247 ) ;
#41836=CARTESIAN_POINT ( 'NONE',  ( -0.5455278134075214336, 3.267716535433071279, 2.034427629037600660 ) ) ;
#41837=ORIENTED_EDGE ( 'NONE', *, *, #28777, .T. ) ;
#41838=CARTESIAN_POINT ( 'NONE',  ( -0.3486774197067334380, 3.346456692913386100, 1.259842519685033357 ) ) ;
#41840=AXIS2_PLACEMENT_3D ( 'NONE', #7466, #3593, #31725 ) ;
#41843=DIRECTION ( 'NONE',  ( 1.734723475976806848E-16, -0.000000000000000000, 1.000000000000000000 ) ) ;
#41844=VERTEX_POINT ( 'NONE', #30902 ) ;
#41845=EDGE_LOOP ( 'NONE', ( #30611, #18447, #22946, #8566 ) ) ;
#41846=CARTESIAN_POINT ( 'NONE',  ( 1.909347346926324462, 3.346456692913386100, -1.299212598425194320 ) ) ;
#41847=ORIENTED_EDGE ( 'NONE', *, *, #22145, .F. ) ;
#41848=CARTESIAN_POINT ( 'NONE',  ( -1.536664496436148184E-16, 3.346456692913386100, 0.4330708661417287386 ) ) ;
#41849=CARTESIAN_POINT ( 'NONE',  ( -0.3486774197067339376, 0.000000000000000000, -8.878505979408855953E-16 ) ) ;
#41850=AXIS2_PLACEMENT_3D ( 'NONE', #12626, #47184, #39484 ) ;
#41852=VERTEX_POINT ( 'NONE', #43260 ) ;
#41855=EDGE_LOOP ( 'NONE', ( #1386, #34673, #15759, #31529 ) ) ;
#41857=CARTESIAN_POINT ( 'NONE',  ( 0.000000000000000000, 3.267716535433071279, -0.4724409448818889246 ) ) ;
#41858=CARTESIAN_POINT ( 'NONE',  ( -0.2727639067037611054, 0.000000000000000000, -2.244094488188968395 ) ) ;
#41859=DIRECTION ( 'NONE',  ( -0.000000000000000000, 1.000000000000000000, -0.000000000000000000 ) ) ;
#41863=ORIENTED_EDGE ( 'NONE', *, *, #8211, .T. ) ;
#41865=CARTESIAN_POINT ( 'NONE',  ( 0.000000000000000000, 3.267716535433071279, 0.3149606299212576177 ) ) ;
#41866=DIRECTION ( 'NONE',  ( 1.734723475976806848E-16, 0.000000000000000000, 1.000000000000000000 ) ) ;
#41868=ADVANCED_FACE ( 'NONE', ( #23144 ), #19265, .F. ) ;
#41870=VECTOR ( 'NONE', #27064, 39.37007874015748143 ) ;
#41873=CARTESIAN_POINT ( 'NONE',  ( -0.5455278134075208785, 0.000000000000000000, 0.9448818897637749625 ) ) ;
#41874=ORIENTED_EDGE ( 'NONE', *, *, #36428, .T. ) ;
#41877=VECTOR ( 'NONE', #19713, 39.37007874015748143 ) ;
#41878=PLANE ( 'NONE',  #35481 ) ;
#41880=ADVANCED_FACE ( 'NONE', ( #7653 ), #11022, .F. ) ;
#41882=ORIENTED_EDGE ( 'NONE', *, *, #28681, .F. ) ;
#41884=LINE ( 'NONE', #37769, #10278 ) ;
#41885=ORIENTED_EDGE ( 'NONE', *, *, #22416, .T. ) ;
#41886=CARTESIAN_POINT ( 'NONE',  ( -2.071704270381554913, 3.346456692913386100, 0.6299212598425164567 ) ) ;
#41887=CARTESIAN_POINT ( 'NONE',  ( 0.4696143004045476577, 3.346456692913386100, -2.053280005709960054 ) ) ;
#41888=EDGE_CURVE ( 'NONE', #41557, #37648, #23915, .T. ) ;
#41889=VECTOR ( 'NONE', #22795, 39.37007874015748143 ) ;
#41890=VECTOR ( 'NONE', #20756, 39.37007874015748143 ) ;
#41891=EDGE_CURVE ( 'NONE', #41040, #18225, #36819, .T. ) ;
#41893=LINE ( 'NONE', #18904, #10421 ) ;
#41896=DIRECTION ( 'NONE',  ( -1.000000000000000000, 0.000000000000000000, 1.734723475976806848E-16 ) ) ;
#41897=VECTOR ( 'NONE', #48176, 39.37007874015748143 ) ;
#41898=DIRECTION ( 'NONE',  ( -1.000000000000000000, 0.000000000000000000, 0.000000000000000000 ) ) ;
#41900=VECTOR ( 'NONE', #9848, 39.37007874015748143 ) ;
#41901=CARTESIAN_POINT ( 'NONE',  ( -0.5455278134075214336, 3.346456692913386100, -1.889763779527552146 ) ) ;
#41903=DIRECTION ( 'NONE',  ( -1.000000000000000000, -0.000000000000000000, -0.000000000000000000 ) ) ;
#41904=VERTEX_POINT ( 'NONE', #12299 ) ;
#41906=CARTESIAN_POINT ( 'NONE',  ( -1.909347346926324462, 0.000000000000000000, 0.2755905511810996522 ) ) ;
#41907=ORIENTED_EDGE ( 'NONE', *, *, #15002, .F. ) ;
#41909=EDGE_LOOP ( 'NONE', ( #27419, #10506, #10537, #33608 ) ) ;
#41910=VECTOR ( 'NONE', #18905, 39.37007874015748143 ) ;
#41911=CARTESIAN_POINT ( 'NONE',  ( 0.2727639067037604947, 3.346456692913386100, -0.7874015748031473194 ) ) ;
#41912=CARTESIAN_POINT ( 'NONE',  ( -0.5455278134075216556, 3.267716535433071279, -2.204724409448810540 ) ) ;
#41913=LINE ( 'NONE', #30295, #20600 ) ;
#41914=DIRECTION ( 'NONE',  ( -0.000000000000000000, 1.000000000000000000, -0.000000000000000000 ) ) ;
#41915=ORIENTED_EDGE ( 'NONE', *, *, #2340, .T. ) ;
#41916=ORIENTED_EDGE ( 'NONE', *, *, #14149, .F. ) ;
#41917=CARTESIAN_POINT ( 'NONE',  ( -1.636583440222563635, 3.267716535433071279, 1.259842519685033357 ) ) ;
#41918=DIRECTION ( 'NONE',  ( -0.000000000000000000, 1.000000000000000000, -0.000000000000000000 ) ) ;
#41919=ORIENTED_EDGE ( 'NONE', *, *, #43337, .F. ) ;
#41920=CARTESIAN_POINT ( 'NONE',  ( -1.091055626815042645, 0.000000000000000000, 1.692913385826762873 ) ) ;
#41922=DIRECTION ( 'NONE',  ( -1.000000000000000000, -0.000000000000000000, -0.000000000000000000 ) ) ;
#41925=EDGE_CURVE ( 'NONE', #1039, #12446, #44294, .T. ) ;
#41926=CARTESIAN_POINT ( 'NONE',  ( -2.182111253630085290, 3.226699998040846395, -1.141732283464563791 ) ) ;
#41928=VECTOR ( 'NONE', #4074, 39.37007874015748143 ) ;
#41930=EDGE_CURVE ( 'NONE', #47925, #39171, #44541, .T. ) ;
#41931=ORIENTED_EDGE ( 'NONE', *, *, #32567, .T. ) ;
#41933=EDGE_CURVE ( 'NONE', #12607, #32732, #36308, .T. ) ;
#41934=FACE_BOUND ( 'NONE', #8282, .T. ) ;
#41935=ORIENTED_EDGE ( 'NONE', *, *, #25198, .T. ) ;
#41936=DIRECTION ( 'NONE',  ( 1.000000000000000000, 0.000000000000000000, 0.000000000000000000 ) ) ;
#41937=VERTEX_POINT ( 'NONE', #48638 ) ;
#41938=VECTOR ( 'NONE', #30982, 39.37007874015748143 ) ;
#41939=ORIENTED_EDGE ( 'NONE', *, *, #36834, .T. ) ;
#41943=VECTOR ( 'NONE', #13663, 39.37007874015748143 ) ;
#41945=VERTEX_POINT ( 'NONE', #28034 ) ;
#41947=CARTESIAN_POINT ( 'NONE',  ( 0.000000000000000000, 3.267716535433071279, 1.062992125984246083 ) ) ;
#41948=ORIENTED_EDGE ( 'NONE', *, *, #27629, .T. ) ;
#41950=VECTOR ( 'NONE', #8942, 39.37007874015748143 ) ;
#41951=ORIENTED_EDGE ( 'NONE', *, *, #25790, .T. ) ;
#41952=DIRECTION ( 'NONE',  ( -0.000000000000000000, 1.000000000000000000, -0.000000000000000000 ) ) ;
#41953=PLANE ( 'NONE',  #11921 ) ;
#41954=EDGE_CURVE ( 'NONE', #29231, #11067, #16431, .T. ) ;
#41955=CARTESIAN_POINT ( 'NONE',  ( -0.2727639067037607723, 3.267716535433071279, -0.4724409448818883694 ) ) ;
#41957=CARTESIAN_POINT ( 'NONE',  ( 0.8182917201112819283, 3.346456692913386100, 0.2755905511810994302 ) ) ;
#41958=PLANE ( 'NONE',  #17958 ) ;
#41961=EDGE_CURVE ( 'NONE', #9086, #36296, #47874, .T. ) ;
#41963=FACE_OUTER_BOUND ( 'NONE', #48142, .T. ) ;
#41966=CARTESIAN_POINT ( 'NONE',  ( 0.000000000000000000, 3.267716535433071279, 0.6299212598425161236 ) ) ;
#41967=ORIENTED_EDGE ( 'NONE', *, *, #41006, .T. ) ;
#41970=DIRECTION ( 'NONE',  ( -0.000000000000000000, 1.000000000000000000, -0.000000000000000000 ) ) ;
#41971=CARTESIAN_POINT ( 'NONE',  ( 0.4696143004045476022, 3.267716535433071279, -2.244094488188969727 ) ) ;
#41972=ORIENTED_EDGE ( 'NONE', *, *, #21361, .F. ) ;
#41973=DIRECTION ( 'NONE',  ( 1.000000000000000000, 0.000000000000000000, -3.469446951953613696E-16 ) ) ;
#41974=ORIENTED_EDGE ( 'NONE', *, *, #48401, .T. ) ;
#41975=FACE_BOUND ( 'NONE', #4705, .T. ) ;
#41976=CARTESIAN_POINT ( 'NONE',  ( 0.1968503937007874127, 3.267716535433071279, -6.829619984160656814E-17 ) ) ;
#41979=LINE ( 'NONE', #19230, #28430 ) ;
#41980=LINE ( 'NONE', #10737, #38381 ) ;
#41981=VECTOR ( 'NONE', #22267, 39.37007874015748143 ) ;
#41983=EDGE_LOOP ( 'NONE', ( #23570, #44878, #9328, #30598 ) ) ;
#41988=CARTESIAN_POINT ( 'NONE',  ( -0.07591351300297366489, 3.267716535433071279, -2.244094488188968395 ) ) ;
#41989=FACE_OUTER_BOUND ( 'NONE', #19919, .T. ) ;
#41991=CARTESIAN_POINT ( 'NONE',  ( 0.2727639067037609943, 3.346456692913386100, 1.535433070866133898 ) ) ;
#41992=CARTESIAN_POINT ( 'NONE',  ( 1.909347346926324462, 3.346456692913386100, -1.299212598425194320 ) ) ;
#41993=EDGE_CURVE ( 'NONE', #12580, #7930, #48385, .T. ) ;
#41994=VERTEX_POINT ( 'NONE', #35791 ) ;
#41995=EDGE_CURVE ( 'NONE', #12211, #50070, #31930, .T. ) ;
#41996=CARTESIAN_POINT ( 'NONE',  ( -0.5455278134075208785, 3.346456692913386100, 0.6299212598425164567 ) ) ;
#41999=EDGE_CURVE ( 'NONE', #456, #22772, #4292, .T. ) ;
#42000=VECTOR ( 'NONE', #41918, 39.37007874015748143 ) ;
#42001=ORIENTED_EDGE ( 'NONE', *, *, #43277, .T. ) ;
#42002=ORIENTED_EDGE ( 'NONE', *, *, #3103, .T. ) ;
#42003=CARTESIAN_POINT ( 'NONE',  ( -1.536664496436148184E-16, 3.346456692913386100, -1.456692913385822630 ) ) ;
#42004=ORIENTED_EDGE ( 'NONE', *, *, #7329, .T. ) ;
#42005=LINE ( 'NONE', #29101, #20485 ) ;
#42006=LINE ( 'NONE', #49957, #504 ) ;
#42007=AXIS2_PLACEMENT_3D ( 'NONE', #49827, #45978, #38520 ) ;
#42008=EDGE_CURVE ( 'NONE', #31067, #16368, #32441, .T. ) ;
#42009=CARTESIAN_POINT ( 'NONE',  ( -1.985260859929298016, 3.267716535433071279, -0.6299212598425177889 ) ) ;
#42010=AXIS2_PLACEMENT_3D ( 'NONE', #2729, #6856, #10732 ) ;
#42012=CARTESIAN_POINT ( 'NONE',  ( 0.4696143004045476577, 3.346456692913386100, -2.047244094488182231 ) ) ;
#42013=ORIENTED_EDGE ( 'NONE', *, *, #15545, .T. ) ;
#42014=EDGE_CURVE ( 'NONE', #32787, #18949, #32704, .T. ) ;
#42016=CARTESIAN_POINT ( 'NONE',  ( -1.363819533518803029, 3.346456692913386100, 0.5905511811023582691 ) ) ;
#42017=EDGE_CURVE ( 'NONE', #24291, #23949, #36562, .T. ) ;
#42018=AXIS2_PLACEMENT_3D ( 'NONE', #48092, #14925, #377 ) ;
#42019=CARTESIAN_POINT ( 'NONE',  ( 1.909347346926324684, 0.000000000000000000, -0.6692913385826764205 ) ) ;
#42021=EDGE_LOOP ( 'NONE', ( #5256, #29584, #11176, #15676 ) ) ;
#42023=CARTESIAN_POINT ( 'NONE',  ( -0.3486774197067339376, 3.346456692913386100, -1.889763779527552146 ) ) ;
#42024=ORIENTED_EDGE ( 'NONE', *, *, #21888, .T. ) ;
#42028=DIRECTION ( 'NONE',  ( -1.000000000000000000, -0.000000000000000000, -0.000000000000000000 ) ) ;
#42032=LINE ( 'NONE', #14157, #24565 ) ;
#42033=FACE_OUTER_BOUND ( 'NONE', #43613, .T. ) ;
#42034=CARTESIAN_POINT ( 'NONE',  ( -0.2727639067037602172, 0.000000000000000000, 1.732283464566921172 ) ) ;
#42035=VECTOR ( 'NONE', #39239, 39.37007874015748143 ) ;
#42036=ORIENTED_EDGE ( 'NONE', *, *, #23383, .T. ) ;
#42039=ORIENTED_EDGE ( 'NONE', *, *, #5922, .T. ) ;
#42040=LINE ( 'NONE', #34307, #16350 ) ;
#42042=DIRECTION ( 'NONE',  ( 1.000000000000000000, -0.000000000000000000, 0.000000000000000000 ) ) ;
#42043=FACE_OUTER_BOUND ( 'NONE', #1502, .T. ) ;
#42044=ORIENTED_EDGE ( 'NONE', *, *, #45335, .T. ) ;
#42045=AXIS2_PLACEMENT_3D ( 'NONE', #21694, #37452, #2074 ) ;
#42046=DIRECTION ( 'NONE',  ( 1.000000000000000000, 0.000000000000000000, 0.000000000000000000 ) ) ;
#42047=FACE_OUTER_BOUND ( 'NONE', #37490, .T. ) ;
#42048=ADVANCED_FACE ( 'NONE', ( #47623 ), #40442, .F. ) ;
#42049=DIRECTION ( 'NONE',  ( -1.000000000000000000, 0.000000000000000000, 0.000000000000000000 ) ) ;
#42051=ADVANCED_FACE ( 'NONE', ( #30085 ), #41958, .F. ) ;
#42052=ORIENTED_EDGE ( 'NONE', *, *, #48782, .T. ) ;
#42054=FACE_BOUND ( 'NONE', #21662, .T. ) ;
#42055=ORIENTED_EDGE ( 'NONE', *, *, #7485, .T. ) ;
#42056=VECTOR ( 'NONE', #37736, 39.37007874015748143 ) ;
#42057=EDGE_CURVE ( 'NONE', #44367, #45040, #34220, .T. ) ;
#42058=DIRECTION ( 'NONE',  ( -0.000000000000000000, 0.000000000000000000, 1.000000000000000000 ) ) ;
#42059=LINE ( 'NONE', #15889, #48923 ) ;
#42060=EDGE_CURVE ( 'NONE', #16832, #37208, #634, .T. ) ;
#42062=ORIENTED_EDGE ( 'NONE', *, *, #5982, .F. ) ;
#42063=ORIENTED_EDGE ( 'NONE', *, *, #36162, .T. ) ;
#42065=CARTESIAN_POINT ( 'NONE',  ( 0.7423782071083084855, 3.267716535433071279, -1.971134437475891454 ) ) ;
#42066=ORIENTED_EDGE ( 'NONE', *, *, #41538, .F. ) ;
#42069=DIRECTION ( 'NONE',  ( 1.734723475976806848E-16, 0.000000000000000000, 1.000000000000000000 ) ) ;
#42070=CARTESIAN_POINT ( 'NONE',  ( -1.636583440222563635, 0.000000000000000000, 0.9448818897637749625 ) ) ;
#42072=LINE ( 'NONE', #50024, #37119 ) ;
#42073=VERTEX_POINT ( 'NONE', #22340 ) ;
#42074=ORIENTED_EDGE ( 'NONE', *, *, #38588, .F. ) ;
#42075=PLANE ( 'NONE',  #49640 ) ;
#42077=DIRECTION ( 'NONE',  ( -1.000000000000000000, 0.000000000000000000, 0.000000000000000000 ) ) ;
#42078=EDGE_CURVE ( 'NONE', #4136, #12830, #49152, .T. ) ;
#42079=DIRECTION ( 'NONE',  ( -0.000000000000000000, 0.000000000000000000, 1.000000000000000000 ) ) ;
#42081=VECTOR ( 'NONE', #41447, 39.37007874015748143 ) ;
#42083=CARTESIAN_POINT ( 'NONE',  ( 1.833433833923351353, 3.346456692913386100, 0.4330708661417290162 ) ) ;
#42085=CARTESIAN_POINT ( 'NONE',  ( -1.166969139818015533, 3.267716535433071279, 1.102362204724404160 ) ) ;
#42086=ORIENTED_EDGE ( 'NONE', *, *, #23207, .T. ) ;
#42087=CARTESIAN_POINT ( 'NONE',  ( -0.8182917201112819283, 3.346456692913386100, -1.732283464566922726 ) ) ;
#42089=VECTOR ( 'NONE', #1785, 39.37007874015748143 ) ;
#42090=VERTEX_POINT ( 'NONE', #2470 ) ;
#42092=ORIENTED_EDGE ( 'NONE', *, *, #39443, .T. ) ;
#42096=CARTESIAN_POINT ( 'NONE',  ( -1.636583440222563857, 3.267716535433071279, 2.839019714148966584E-16 ) ) ;
#42097=VERTEX_POINT ( 'NONE', #6341 ) ;
#42100=ORIENTED_EDGE ( 'NONE', *, *, #15975, .F. ) ;
#42101=DIRECTION ( 'NONE',  ( 0.000000000000000000, 0.000000000000000000, -1.000000000000000000 ) ) ;
#42102=ORIENTED_EDGE ( 'NONE', *, *, #30498, .F. ) ;
#42103=ORIENTED_EDGE ( 'NONE', *, *, #18349, .F. ) ;
#42106=CARTESIAN_POINT ( 'NONE',  ( 0.8182917201112824834, 0.000000000000000000, 1.535433070866133898 ) ) ;
#42107=DIRECTION ( 'NONE',  ( -0.000000000000000000, 0.000000000000000000, 1.000000000000000000 ) ) ;
#42110=EDGE_LOOP ( 'NONE', ( #32222, #46, #1795, #10027 ) ) ;
#42111=AXIS2_PLACEMENT_3D ( 'NONE', #31567, #31063, #26672 ) ;
#42113=CARTESIAN_POINT ( 'NONE',  ( -1.091055626815042645, 0.000000000000000000, -0.8267716535433052849 ) ) ;
#42115=LINE ( 'NONE', #22752, #29469 ) ;
#42116=EDGE_CURVE ( 'NONE', #35907, #22479, #45799, .T. ) ;
#42118=CARTESIAN_POINT ( 'NONE',  ( 0.000000000000000000, 3.346456692913386100, 0.000000000000000000 ) ) ;
#42119=VERTEX_POINT ( 'NONE', #6074 ) ;
#42121=VECTOR ( 'NONE', #12584, 39.37007874015748143 ) ;
#42124=DIRECTION ( 'NONE',  ( -1.000000000000000000, 0.000000000000000000, 0.000000000000000000 ) ) ;
#42126=ORIENTED_EDGE ( 'NONE', *, *, #8419, .T. ) ;
#42127=ORIENTED_EDGE ( 'NONE', *, *, #29921, .T. ) ;
#42128=DIRECTION ( 'NONE',  ( 1.734723475976806848E-16, -0.000000000000000000, 1.000000000000000000 ) ) ;
#42130=EDGE_LOOP ( 'NONE', ( #49112, #22726, #16011, #27929 ) ) ;
#42135=CARTESIAN_POINT ( 'NONE',  ( -3.927031490892378253E-16, 0.000000000000000000, -2.204724409448811429 ) ) ;
#42137=ORIENTED_EDGE ( 'NONE', *, *, #32959, .F. ) ;
#42138=DIRECTION ( 'NONE',  ( -1.000000000000000000, 0.000000000000000000, 1.734723475976806848E-16 ) ) ;
#42139=PLANE ( 'NONE',  #5444 ) ;
#42140=DIRECTION ( 'NONE',  ( -0.000000000000000000, 0.000000000000000000, 1.000000000000000000 ) ) ;
#42142=AXIS2_PLACEMENT_3D ( 'NONE', #29835, #9193, #24941 ) ;
#42144=PLANE ( 'NONE',  #20746 ) ;
#42145=VECTOR ( 'NONE', #6114, 39.37007874015748143 ) ;
#42146=CARTESIAN_POINT ( 'NONE',  ( 1.287906020515830585, 3.267716535433071279, 1.740706023381843659 ) ) ;
#42147=CARTESIAN_POINT ( 'NONE',  ( -0.3486774197067342151, 3.346456692913386100, -2.204724409448810540 ) ) ;
#42148=ORIENTED_EDGE ( 'NONE', *, *, #41933, .F. ) ;
#42150=DIRECTION ( 'NONE',  ( 1.734723475976806848E-16, 0.000000000000000000, 1.000000000000000000 ) ) ;
#42151=EDGE_CURVE ( 'NONE', #49700, #33556, #21832, .T. ) ;
#42152=ORIENTED_EDGE ( 'NONE', *, *, #30796, .F. ) ;
#42153=FACE_OUTER_BOUND ( 'NONE', #31308, .T. ) ;
#42154=VECTOR ( 'NONE', #35632, 39.37007874015748143 ) ;
#42156=CARTESIAN_POINT ( 'NONE',  ( -1.985260859929298016, 0.000000000000000000, -0.9448818897637762948 ) ) ;
#42158=VECTOR ( 'NONE', #31671, 39.37007874015748143 ) ;
#42160=CARTESIAN_POINT ( 'NONE',  ( -1.439733046521776361, 3.346456692913386100, 0.4330708661417290162 ) ) ;
#42161=DIRECTION ( 'NONE',  ( 1.000000000000000000, -0.000000000000000000, 0.000000000000000000 ) ) ;
#42164=CARTESIAN_POINT ( 'NONE',  ( -1.078729122356643755, 3.244501632956205306, 2.204724409448808764 ) ) ;
#42165=CARTESIAN_POINT ( 'NONE',  ( -0.07591351300297340121, 3.346456692913386100, -0.3543307086614175816 ) ) ;
#42166=VERTEX_POINT ( 'NONE', #3725 ) ;
#42167=CARTESIAN_POINT ( 'NONE',  ( -1.439733046521776361, 0.000000000000000000, -0.1968503937007879123 ) ) ;
#42169=CARTESIAN_POINT ( 'NONE',  ( -1.636583440222564301, 3.267716535433071279, -1.325930245594398871 ) ) ;
#42170=EDGE_CURVE ( 'NONE', #1056, #6843, #34470, .T. ) ;
#42171=EDGE_LOOP ( 'NONE', ( #35398, #22034, #43153, #19977 ) ) ;
#42172=EDGE_LOOP ( 'NONE', ( #15309, #32975, #39880, #49760 ) ) ;
#42173=DIRECTION ( 'NONE',  ( -1.000000000000000000, 0.000000000000000000, 0.000000000000000000 ) ) ;
#42174=DIRECTION ( 'NONE',  ( 1.734723475976806848E-16, -0.000000000000000000, 1.000000000000000000 ) ) ;
#42175=CARTESIAN_POINT ( 'NONE',  ( -0.5455278134075214336, 0.000000000000000000, 0.3149606299212577287 ) ) ;
#42176=ADVANCED_FACE ( 'NONE', ( #26705 ), #2970, .F. ) ;
#42177=ORIENTED_EDGE ( 'NONE', *, *, #457, .F. ) ;
#42180=VERTEX_POINT ( 'NONE', #15347 ) ;
#42182=ORIENTED_EDGE ( 'NONE', *, *, #1239, .F. ) ;
#42185=LINE ( 'NONE', #42688, #14369 ) ;
#42186=VECTOR ( 'NONE', #30534, 39.37007874015748143 ) ;
#42188=VECTOR ( 'NONE', #45775, 39.37007874015748143 ) ;
#42189=DIRECTION ( 'NONE',  ( -0.000000000000000000, 1.000000000000000000, -0.000000000000000000 ) ) ;
#42190=DIRECTION ( 'NONE',  ( -3.469446951953613696E-16, 0.000000000000000000, -1.000000000000000000 ) ) ;
#42192=VECTOR ( 'NONE', #38180, 39.37007874015748143 ) ;
#42193=ORIENTED_EDGE ( 'NONE', *, *, #49519, .F. ) ;
#42194=LINE ( 'NONE', #27203, #26920 ) ;
#42195=FACE_OUTER_BOUND ( 'NONE', #7240, .T. ) ;
#42196=VECTOR ( 'NONE', #49351, 39.37007874015748143 ) ;
#42199=FACE_OUTER_BOUND ( 'NONE', #44219, .T. ) ;
#42200=LINE ( 'NONE', #32122, #23727 ) ;
#42202=DIRECTION ( 'NONE',  ( 1.734723475976806848E-16, -0.000000000000000000, 1.000000000000000000 ) ) ;
#42203=CARTESIAN_POINT ( 'NONE',  ( 0.000000000000000000, 3.267716535433071279, 0.7874015748031456541 ) ) ;
#42205=DIRECTION ( 'NONE',  ( 1.000000000000000000, -0.000000000000000000, 0.000000000000000000 ) ) ;
#42209=CARTESIAN_POINT ( 'NONE',  ( 1.363819533518803695, 3.346456692913386100, 1.732283464566921172 ) ) ;
#42211=DIRECTION ( 'NONE',  ( 1.734723475976806848E-16, 0.000000000000000000, 1.000000000000000000 ) ) ;
#42212=ADVANCED_FACE ( 'NONE', ( #38347 ), #15599, .F. ) ;
#42214=VERTEX_POINT ( 'NONE', #6842 ) ;
#42216=EDGE_LOOP ( 'NONE', ( #29877, #48667, #11438, #34461 ) ) ;
#42217=FACE_BOUND ( 'NONE', #21295, .T. ) ;
#42219=CARTESIAN_POINT ( 'NONE',  ( -0.3486774197067339376, 0.000000000000000000, -1.889763779527552146 ) ) ;
#42220=CARTESIAN_POINT ( 'NONE',  ( -1.985260859929298016, 3.346456692913386100, -0.7037298423582233342 ) ) ;
#42221=AXIS2_PLACEMENT_3D ( 'NONE', #7810, #23550, #34057 ) ;
#42222=ORIENTED_EDGE ( 'NONE', *, *, #13217, .F. ) ;
#42223=VERTEX_POINT ( 'NONE', #27457 ) ;
#42226=VECTOR ( 'NONE', #18189, 39.37007874015748143 ) ;
#42227=PLANE ( 'NONE',  #11209 ) ;
#42229=PLANE ( 'NONE',  #26890 ) ;
#42231=VECTOR ( 'NONE', #22413, 39.37007874015748143 ) ;
#42232=ADVANCED_FACE ( 'NONE', ( #3215 ), #38841, .F. ) ;
#42233=ORIENTED_EDGE ( 'NONE', *, *, #34591, .T. ) ;
#42234=ORIENTED_EDGE ( 'NONE', *, *, #39146, .F. ) ;
#42237=FACE_OUTER_BOUND ( 'NONE', #21682, .T. ) ;
#42238=EDGE_LOOP ( 'NONE', ( #29037, #7520, #13619, #35246 ) ) ;
#42239=EDGE_CURVE ( 'NONE', #38076, #36543, #11475, .T. ) ;
#42240=DIRECTION ( 'NONE',  ( -3.469446951953613696E-16, 0.000000000000000000, -1.000000000000000000 ) ) ;
#42241=EDGE_LOOP ( 'NONE', ( #7565, #30552, #41274, #25980 ) ) ;
#42243=ORIENTED_EDGE ( 'NONE', *, *, #2747, .F. ) ;
#42244=ORIENTED_EDGE ( 'NONE', *, *, #49204, .T. ) ;
#42246=DIRECTION ( 'NONE',  ( 1.000000000000000000, 0.000000000000000000, -3.469446951953613696E-16 ) ) ;
#42247=DIRECTION ( 'NONE',  ( 1.000000000000000000, -0.000000000000000000, 0.000000000000000000 ) ) ;
#42253=CARTESIAN_POINT ( 'NONE',  ( 0.5455278134075213226, 3.267716535433071279, -9.463399047163221947E-17 ) ) ;
#42254=EDGE_LOOP ( 'NONE', ( #46975, #49604, #12805, #49750 ) ) ;
#42255=LINE ( 'NONE', #46612, #39845 ) ;
#42256=PLANE ( 'NONE',  #31621 ) ;
#42257=AXIS2_PLACEMENT_3D ( 'NONE', #28716, #5225, #35968 ) ;
#42258=LINE ( 'NONE', #50214, #20213 ) ;
#42260=CIRCLE ( 'NONE', #24957, 2.165354330708661568 ) ;
#42261=AXIS2_PLACEMENT_3D ( 'NONE', #43887, #8538, #40037 ) ;
#42263=LINE ( 'NONE', #31161, #3388 ) ;
#42264=EDGE_CURVE ( 'NONE', #43429, #35595, #26955, .T. ) ;
#42265=CARTESIAN_POINT ( 'NONE',  ( -1.985260859929298016, 3.267716535433071279, -0.9448818897637762948 ) ) ;
#42266=ORIENTED_EDGE ( 'NONE', *, *, #35647, .T. ) ;
#42267=DIRECTION ( 'NONE',  ( -0.000000000000000000, 1.000000000000000000, -0.000000000000000000 ) ) ;
#42268=LINE ( 'NONE', #14912, #27553 ) ;
#42269=EDGE_CURVE ( 'NONE', #41945, #11695, #23089, .T. ) ;
#42270=ORIENTED_EDGE ( 'NONE', *, *, #3778, .T. ) ;
#42271=EDGE_CURVE ( 'NONE', #30486, #7592, #19209, .T. ) ;
#42272=LINE ( 'NONE', #22663, #27364 ) ;
#42273=ORIENTED_EDGE ( 'NONE', *, *, #4908, .T. ) ;
#42275=EDGE_CURVE ( 'NONE', #39958, #373, #19457, .T. ) ;
#42276=FACE_OUTER_BOUND ( 'NONE', #11454, .T. ) ;
#42277=DIRECTION ( 'NONE',  ( 1.734723475976806848E-16, 0.000000000000000000, 1.000000000000000000 ) ) ;
#42278=LINE ( 'NONE', #46877, #11888 ) ;
#42279=PLANE ( 'NONE',  #14567 ) ;
#42281=CARTESIAN_POINT ( 'NONE',  ( 0.2727639067037604947, 3.346456692913386100, -0.4724409448818886470 ) ) ;
#42282=EDGE_LOOP ( 'NONE', ( #16582, #5876, #5797, #37221 ) ) ;
#42283=EDGE_LOOP ( 'NONE', ( #29558, #704, #6658, #19146 ) ) ;
#42284=LINE ( 'NONE', #50482, #13083 ) ;
#42286=CARTESIAN_POINT ( 'NONE',  ( 1.363819533518803251, 0.000000000000000000, -0.1574803149606304187 ) ) ;
#42290=FACE_OUTER_BOUND ( 'NONE', #35344, .T. ) ;
#42291=EDGE_CURVE ( 'NONE', #46532, #10670, #42200, .T. ) ;
#42292=DIRECTION ( 'NONE',  ( 0.000000000000000000, -1.000000000000000000, 0.000000000000000000 ) ) ;
#42293=VECTOR ( 'NONE', #31069, 39.37007874015748143 ) ;
#42294=DIRECTION ( 'NONE',  ( -0.000000000000000000, 0.000000000000000000, 1.000000000000000000 ) ) ;
#42299=FACE_BOUND ( 'NONE', #40284, .T. ) ;
#42301=VECTOR ( 'NONE', #34392, 39.37007874015748143 ) ;
#42302=VECTOR ( 'NONE', #24746, 39.37007874015748143 ) ;
#42303=DIRECTION ( 'NONE',  ( 1.000000000000000000, 0.000000000000000000, 0.000000000000000000 ) ) ;
#42304=VERTEX_POINT ( 'NONE', #13005 ) ;
#42305=EDGE_LOOP ( 'NONE', ( #33254, #29799, #17999, #29330 ) ) ;
#42307=PLANE ( 'NONE',  #41421 ) ;
#42308=AXIS2_PLACEMENT_3D ( 'NONE', #32964, #45546, #48640 ) ;
#42311=CARTESIAN_POINT ( 'NONE',  ( -2.182111253630085290, 3.346456692913386100, 0.9448818897637749625 ) ) ;
#42312=ORIENTED_EDGE ( 'NONE', *, *, #37240, .T. ) ;
#42313=DIRECTION ( 'NONE',  ( 1.734723475976806848E-16, -0.000000000000000000, 1.000000000000000000 ) ) ;
#42314=LINE ( 'NONE', #35339, #37424 ) ;
#42315=DIRECTION ( 'NONE',  ( -1.000000000000000000, 0.000000000000000000, 0.000000000000000000 ) ) ;
#42316=ORIENTED_EDGE ( 'NONE', *, *, #262, .T. ) ;
#42318=DIRECTION ( 'NONE',  ( 1.000000000000000000, 0.000000000000000000, 0.000000000000000000 ) ) ;
#42319=CARTESIAN_POINT ( 'NONE',  ( -1.166969139818015533, 0.000000000000000000, 0.1574803149606287811 ) ) ;
#42324=LINE ( 'NONE', #2086, #27513 ) ;
#42325=VECTOR ( 'NONE', #27367, 39.37007874015748143 ) ;
#42327=ORIENTED_EDGE ( 'NONE', *, *, #20123, .T. ) ;
#42329=DIRECTION ( 'NONE',  ( -0.000000000000000000, 1.000000000000000000, -0.000000000000000000 ) ) ;
#42330=EDGE_CURVE ( 'NONE', #41046, #795, #16624, .T. ) ;
#42331=AXIS2_PLACEMENT_3D ( 'NONE', #6087, #18221, #33733 ) ;
#42332=VERTEX_POINT ( 'NONE', #40378 ) ;
#42333=EDGE_CURVE ( 'NONE', #26538, #39358, #28737, .T. ) ;
#42334=CIRCLE ( 'NONE', #11819, 2.165354330708661568 ) ;
#42339=ORIENTED_EDGE ( 'NONE', *, *, #43569, .T. ) ;
#42341=VECTOR ( 'NONE', #33406, 39.37007874015748143 ) ;
#42342=ORIENTED_EDGE ( 'NONE', *, *, #39649, .T. ) ;
#42343=CARTESIAN_POINT ( 'NONE',  ( -0.8182917201112819283, 3.346456692913386100, -1.299212598425193210 ) ) ;
#42344=VERTEX_POINT ( 'NONE', #40625 ) ;
#42345=LINE ( 'NONE', #41848, #48233 ) ;
#42346=LINE ( 'NONE', #38741, #6612 ) ;
#42347=EDGE_CURVE ( 'NONE', #15273, #919, #39598, .T. ) ;
#42348=ORIENTED_EDGE ( 'NONE', *, *, #37768, .T. ) ;
#42349=LINE ( 'NONE', #38496, #5705 ) ;
#42350=EDGE_LOOP ( 'NONE', ( #49677, #28313, #7646, #10319 ) ) ;
#42352=EDGE_CURVE ( 'NONE', #5817, #4778, #35724, .T. ) ;
#42353=DIRECTION ( 'NONE',  ( -1.000000000000000000, 0.000000000000000000, 1.734723475976806848E-16 ) ) ;
#42355=DIRECTION ( 'NONE',  ( -0.000000000000000000, 1.000000000000000000, -0.000000000000000000 ) ) ;
#42356=FACE_OUTER_BOUND ( 'NONE', #29129, .T. ) ;
#42357=EDGE_LOOP ( 'NONE', ( #38505, #37660, #21316, #15644 ) ) ;
#42360=DIRECTION ( 'NONE',  ( -0.000000000000000000, 1.000000000000000000, -0.000000000000000000 ) ) ;
#42362=DIRECTION ( 'NONE',  ( 1.000000000000000000, 0.000000000000000000, 0.000000000000000000 ) ) ;
#42365=ORIENTED_EDGE ( 'NONE', *, *, #13967, .F. ) ;
#42366=VECTOR ( 'NONE', #41524, 39.37007874015748143 ) ;
#42367=VERTEX_POINT ( 'NONE', #31600 ) ;
#42368=EDGE_CURVE ( 'NONE', #34396, #32442, #27713, .T. ) ;
#42369=LINE ( 'NONE', #39517, #26789 ) ;
#42371=CARTESIAN_POINT ( 'NONE',  ( 0.000000000000000000, 3.267716535433071279, 0.9448818897637746295 ) ) ;
#42372=CARTESIAN_POINT ( 'NONE',  ( 0.4696143004045478797, 0.000000000000000000, -1.299212598425193210 ) ) ;
#42373=FACE_OUTER_BOUND ( 'NONE', #46871, .T. ) ;
#42374=ORIENTED_EDGE ( 'NONE', *, *, #21837, .F. ) ;
#42375=ORIENTED_EDGE ( 'NONE', *, *, #6912, .F. ) ;
#42376=VECTOR ( 'NONE', #50528, 39.37007874015748143 ) ;
#42377=CARTESIAN_POINT ( 'NONE',  ( -0.2727639067037602172, 3.346456692913386100, 1.417322834645662777 ) ) ;
#42378=CARTESIAN_POINT ( 'NONE',  ( 0.2727639067037605503, 3.267716535433071279, -4.731699523581609741E-17 ) ) ;
#42380=DIRECTION ( 'NONE',  ( 0.000000000000000000, 1.000000000000000000, 0.000000000000000000 ) ) ;
#42381=CARTESIAN_POINT ( 'NONE',  ( -0.8942052331142552601, 3.267716535433071279, -0.1968503937007881899 ) ) ;
#42383=CARTESIAN_POINT ( 'NONE',  ( 0.8182917201112824834, 3.346456692913386100, 1.732283464566921172 ) ) ;
#42384=LINE ( 'NONE', #14527, #40255 ) ;
#42385=VERTEX_POINT ( 'NONE', #12746 ) ;
#42387=DIRECTION ( 'NONE',  ( -0.000000000000000000, 1.000000000000000000, -0.000000000000000000 ) ) ;
#42390=ADVANCED_FACE ( 'NONE', ( #20998 ), #4744, .F. ) ;
#42391=ORIENTED_EDGE ( 'NONE', *, *, #20431, .F. ) ;
#42392=DIRECTION ( 'NONE',  ( -3.469446951953613696E-16, 0.000000000000000000, -1.000000000000000000 ) ) ;
#42395=EDGE_CURVE ( 'NONE', #45868, #24633, #28222, .T. ) ;
#42398=DIRECTION ( 'NONE',  ( -1.000000000000000000, 0.000000000000000000, -0.000000000000000000 ) ) ;
#42400=VECTOR ( 'NONE', #8864, 39.37007874015748143 ) ;
#42402=VECTOR ( 'NONE', #33487, 39.37007874015748143 ) ;
#42404=EDGE_LOOP ( 'NONE', ( #32227, #24417, #18540, #2516 ) ) ;
#42405=DIRECTION ( 'NONE',  ( 1.000000000000000000, 0.000000000000000000, -3.469446951953613696E-16 ) ) ;
#42406=VECTOR ( 'NONE', #6419, 39.37007874015748143 ) ;
#42407=EDGE_LOOP ( 'NONE', ( #47352, #14721, #27110, #27230 ) ) ;
#42410=LINE ( 'NONE', #22044, #24736 ) ;
#42411=CARTESIAN_POINT ( 'NONE',  ( -1.712496953225537188, 0.000000000000000000, -0.3543307086614171930 ) ) ;
#42412=EDGE_CURVE ( 'NONE', #8577, #33170, #43965, .T. ) ;
#42413=VERTEX_POINT ( 'NONE', #24364 ) ;
#42414=ORIENTED_EDGE ( 'NONE', *, *, #259, .F. ) ;
#42416=LINE ( 'NONE', #10680, #10898 ) ;
#42417=PLANE ( 'NONE',  #18889 ) ;
#42418=ORIENTED_EDGE ( 'NONE', *, *, #43800, .F. ) ;
#42419=EDGE_CURVE ( 'NONE', #721, #46932, #24106, .T. ) ;
#42422=CARTESIAN_POINT ( 'NONE',  ( 0.000000000000000000, 3.346456692913386100, 0.000000000000000000 ) ) ;
#42424=VERTEX_POINT ( 'NONE', #36754 ) ;
#42425=ORIENTED_EDGE ( 'NONE', *, *, #36990, .F. ) ;
#42427=DIRECTION ( 'NONE',  ( 1.734723475976806848E-16, 0.000000000000000000, 1.000000000000000000 ) ) ;
#42430=ORIENTED_EDGE ( 'NONE', *, *, #35514, .F. ) ;
#42431=DIRECTION ( 'NONE',  ( -0.000000000000000000, 1.000000000000000000, -0.000000000000000000 ) ) ;
#42434=VERTEX_POINT ( 'NONE', #2144 ) ;
#42435=CARTESIAN_POINT ( 'NONE',  ( 0.8182917201112817063, 0.000000000000000000, -1.614173228346451605 ) ) ;
#42436=ORIENTED_EDGE ( 'NONE', *, *, #14482, .T. ) ;
#42437=ORIENTED_EDGE ( 'NONE', *, *, #42683, .T. ) ;
#42438=CARTESIAN_POINT ( 'NONE',  ( 1.091055626815042423, 0.000000000000000000, -1.456692913385822630 ) ) ;
#42439=DIRECTION ( 'NONE',  ( -1.000000000000000000, 0.000000000000000000, 0.000000000000000000 ) ) ;
#42442=CARTESIAN_POINT ( 'NONE',  ( -2.454875160333845674, 3.241704813874235480, 0.09245170100039766525 ) ) ;
#42443=LINE ( 'NONE', #19703, #30445 ) ;
#42444=VERTEX_POINT ( 'NONE', #9379 ) ;
#42445=VECTOR ( 'NONE', #36687, 39.37007874015748143 ) ;
#42449=CARTESIAN_POINT ( 'NONE',  ( -0.8182917201112814842, 3.346456692913386100, 1.417322834645662777 ) ) ;
#42453=CARTESIAN_POINT ( 'NONE',  ( 2.106197740627111514, 3.346456692913386100, -1.102362204724406602 ) ) ;
#42454=DIRECTION ( 'NONE',  ( -1.000000000000000000, 0.000000000000000000, -0.000000000000000000 ) ) ;
#42456=ORIENTED_EDGE ( 'NONE', *, *, #13683, .F. ) ;
#42457=LINE ( 'NONE', #42707, #30823 ) ;
#42458=CARTESIAN_POINT ( 'NONE',  ( 0.000000000000000000, 3.267716535433071279, -0.3149606299212589500 ) ) ;
#42460=EDGE_LOOP ( 'NONE', ( #32839, #16839, #44551, #14183 ) ) ;
#42461=DIRECTION ( 'NONE',  ( -0.000000000000000000, 1.000000000000000000, -0.000000000000000000 ) ) ;
#42462=PLANE ( 'NONE',  #3890 ) ;
#42465=ADVANCED_FACE ( 'NONE', ( #33144 ), #3137, .T. ) ;
#42467=EDGE_CURVE ( 'NONE', #29752, #31368, #10142, .T. ) ;
#42468=CARTESIAN_POINT ( 'NONE',  ( 0.000000000000000000, 3.267716535433071279, 1.102362204724404160 ) ) ;
#42470=DIRECTION ( 'NONE',  ( -3.469446951953613696E-16, 0.000000000000000000, -1.000000000000000000 ) ) ;
#42472=FACE_OUTER_BOUND ( 'NONE', #50574, .T. ) ;
#42473=CARTESIAN_POINT ( 'NONE',  ( -0.8182917201112819283, 0.000000000000000000, -1.929133858267710000 ) ) ;
#42475=VERTEX_POINT ( 'NONE', #33901 ) ;
#42476=ORIENTED_EDGE ( 'NONE', *, *, #16038, .T. ) ;
#42477=CARTESIAN_POINT ( 'NONE',  ( 1.953585199828835828, 3.346456692913386100, 0.7874015748031456541 ) ) ;
#42478=VECTOR ( 'NONE', #15969, 39.37007874015748143 ) ;
#42481=VECTOR ( 'NONE', #23666, 39.37007874015748143 ) ;
#42483=LINE ( 'NONE', #11502, #15948 ) ;
#42485=CARTESIAN_POINT ( 'NONE',  ( -0.07591351300297333182, 3.346456692913386100, -0.7874015748031470974 ) ) ;
#42486=VECTOR ( 'NONE', #2606, 39.37007874015748143 ) ;
#42487=DIRECTION ( 'NONE',  ( -3.469446951953613696E-16, 0.000000000000000000, -1.000000000000000000 ) ) ;
#42488=ORIENTED_EDGE ( 'NONE', *, *, #27237, .F. ) ;
#42489=DIRECTION ( 'NONE',  ( 0.000000000000000000, -1.000000000000000000, 0.000000000000000000 ) ) ;
#42490=DIRECTION ( 'NONE',  ( -0.000000000000000000, 1.000000000000000000, -0.000000000000000000 ) ) ;
#42493=AXIS2_PLACEMENT_3D ( 'NONE', #5082, #13094, #20831 ) ;
#42496=VERTEX_POINT ( 'NONE', #21766 ) ;
#42497=VERTEX_POINT ( 'NONE', #37015 ) ;
#42499=EDGE_CURVE ( 'NONE', #2677, #14952, #9638, .T. ) ;
#42500=EDGE_CURVE ( 'NONE', #46482, #44152, #13258, .T. ) ;
#42501=ORIENTED_EDGE ( 'NONE', *, *, #31984, .T. ) ;
#42502=ORIENTED_EDGE ( 'NONE', *, *, #32735, .T. ) ;
#42507=CARTESIAN_POINT ( 'NONE',  ( 0.5455278134075217666, 0.000000000000000000, 1.574803149606291974 ) ) ;
#42508=DIRECTION ( 'NONE',  ( -0.000000000000000000, 1.000000000000000000, -0.000000000000000000 ) ) ;
#42509=EDGE_CURVE ( 'NONE', #4391, #33442, #13066, .T. ) ;
#42516=CARTESIAN_POINT ( 'NONE',  ( 2.182111253630085290, 3.346456692913386100, -0.3149606299212596716 ) ) ;
#42517=VECTOR ( 'NONE', #14621, 39.37007874015748143 ) ;
#42518=FACE_OUTER_BOUND ( 'NONE', #19124, .T. ) ;
#42519=EDGE_CURVE ( 'NONE', #26476, #15306, #29511, .T. ) ;
#42520=ORIENTED_EDGE ( 'NONE', *, *, #27918, .F. ) ;
#42521=CARTESIAN_POINT ( 'NONE',  ( -1.636583440222563635, 0.000000000000000000, 0.7480314960629874665 ) ) ;
#42522=DIRECTION ( 'NONE',  ( -1.000000000000000000, 0.000000000000000000, 0.000000000000000000 ) ) ;
#42523=ORIENTED_EDGE ( 'NONE', *, *, #25909, .T. ) ;
#42524=CARTESIAN_POINT ( 'NONE',  ( 0.2727639067037610499, 3.346456692913386100, 2.362204724409437961 ) ) ;
#42526=ADVANCED_FACE ( 'NONE', ( #44729 ), #2401, .F. ) ;
#42527=FACE_OUTER_BOUND ( 'NONE', #23629, .T. ) ;
#42528=EDGE_CURVE ( 'NONE', #43953, #37676, #1631, .T. ) ;
#42530=EDGE_CURVE ( 'NONE', #23553, #5850, #41386, .T. ) ;
#42531=CARTESIAN_POINT ( 'NONE',  ( 1.091055626815042645, 3.346456692913386100, -0.3149606299212596716 ) ) ;
#42532=VERTEX_POINT ( 'NONE', #50337 ) ;
#42534=CARTESIAN_POINT ( 'NONE',  ( 0.7423782071083085965, 0.000000000000000000, 0.4330708661417287386 ) ) ;
#42539=DIRECTION ( 'NONE',  ( -1.000000000000000000, 0.000000000000000000, 0.000000000000000000 ) ) ;
#42540=EDGE_LOOP ( 'NONE', ( #50734, #36453, #20602, #35012 ) ) ;
#42543=ORIENTED_EDGE ( 'NONE', *, *, #917, .F. ) ;
#42544=LINE ( 'NONE', #22428, #46042 ) ;
#42545=DIRECTION ( 'NONE',  ( 1.734723475976806848E-16, 0.000000000000000000, 1.000000000000000000 ) ) ;
#42547=DIRECTION ( 'NONE',  ( -0.000000000000000000, 0.000000000000000000, 1.000000000000000000 ) ) ;
#42548=CARTESIAN_POINT ( 'NONE',  ( 0.000000000000000000, 3.267716535433071279, 0.6299212598425161236 ) ) ;
#42551=VECTOR ( 'NONE', #12949, 39.37007874015748143 ) ;
#42553=ORIENTED_EDGE ( 'NONE', *, *, #17469, .F. ) ;
#42554=AXIS2_PLACEMENT_3D ( 'NONE', #43001, #15401, #6646 ) ;
#42555=DIRECTION ( 'NONE',  ( 1.734723475976806848E-16, -0.000000000000000000, 1.000000000000000000 ) ) ;
#42556=FACE_BOUND ( 'NONE', #1078, .T. ) ;
#42557=ORIENTED_EDGE ( 'NONE', *, *, #34204, .F. ) ;
#42559=DIRECTION ( 'NONE',  ( -0.000000000000000000, 0.000000000000000000, 1.000000000000000000 ) ) ;
#42561=VECTOR ( 'NONE', #17025, 39.37007874015748143 ) ;
#42565=ADVANCED_FACE ( 'NONE', ( #11406 ), #7286, .F. ) ;
#42566=VECTOR ( 'NONE', #12843, 39.37007874015748143 ) ;
#42567=CARTESIAN_POINT ( 'NONE',  ( 1.015142113812069091, 3.267716535433071279, -1.732283464566923614 ) ) ;
#42568=VERTEX_POINT ( 'NONE', #30274 ) ;
#42569=LINE ( 'NONE', #31459, #17144 ) ;
#42570=ORIENTED_EDGE ( 'NONE', *, *, #27196, .F. ) ;
#42571=LINE ( 'NONE', #7964, #5411 ) ;
#42573=CARTESIAN_POINT ( 'NONE',  ( -0.8942052331142547050, 3.267716535433071279, 0.3149606299212580063 ) ) ;
#42574=EDGE_LOOP ( 'NONE', ( #41795, #11075, #20158, #41972 ) ) ;
#42576=CARTESIAN_POINT ( 'NONE',  ( -1.985260859929297794, 3.267716535433071279, 0.4330708661417290162 ) ) ;
#42579=ADVANCED_FACE ( 'NONE', ( #22780 ), #11152, .F. ) ;
#42582=EDGE_CURVE ( 'NONE', #31004, #2919, #38778, .T. ) ;
#42583=DIRECTION ( 'NONE',  ( 1.734723475976806848E-16, 0.000000000000000000, 1.000000000000000000 ) ) ;
#42585=EDGE_CURVE ( 'NONE', #4245, #29967, #46239, .T. ) ;
#42586=EDGE_LOOP ( 'NONE', ( #27551, #5537, #10778, #31975 ) ) ;
#42589=DIRECTION ( 'NONE',  ( -0.000000000000000000, 1.000000000000000000, -0.000000000000000000 ) ) ;
#42590=VECTOR ( 'NONE', #43450, 39.37007874015748143 ) ;
#42591=EDGE_CURVE ( 'NONE', #17636, #33691, #19145, .T. ) ;
#42592=EDGE_LOOP ( 'NONE', ( #42686, #43088, #38628, #9301 ) ) ;
#42595=PLANE ( 'NONE',  #45948 ) ;
#42596=VECTOR ( 'NONE', #37669, 39.37007874015748143 ) ;
#42597=EDGE_LOOP ( 'NONE', ( #41837, #16355, #34210, #45959 ) ) ;
#42598=AXIS2_PLACEMENT_3D ( 'NONE', #40915, #5540, #17164 ) ;
#42599=EDGE_LOOP ( 'NONE', ( #45124, #34385, #25588, #3411 ) ) ;
#42600=CARTESIAN_POINT ( 'NONE',  ( 0.1968503937007872462, 0.000000000000000000, -0.5118110236220465570 ) ) ;
#42601=EDGE_LOOP ( 'NONE', ( #40338, #7537, #30756, #39323 ) ) ;
#42603=DIRECTION ( 'NONE',  ( 1.000000000000000000, 0.000000000000000000, 0.000000000000000000 ) ) ;
#42604=ORIENTED_EDGE ( 'NONE', *, *, #41961, .T. ) ;
#42605=LINE ( 'NONE', #15498, #12330 ) ;
#42606=VERTEX_POINT ( 'NONE', #15535 ) ;
#42607=ORIENTED_EDGE ( 'NONE', *, *, #48182, .F. ) ;
#42608=CARTESIAN_POINT ( 'NONE',  ( -1.363819533518803473, 0.000000000000000000, 1.732283464566920950 ) ) ;
#42610=CARTESIAN_POINT ( 'NONE',  ( 1.363819533518803029, 0.000000000000000000, -1.614173228346452715 ) ) ;
#42611=ORIENTED_EDGE ( 'NONE', *, *, #3612, .F. ) ;
#42612=FACE_OUTER_BOUND ( 'NONE', #37675, .T. ) ;
#42613=CARTESIAN_POINT ( 'NONE',  ( 0.5455278134075211005, 0.000000000000000000, 0.1181102362204701633 ) ) ;
#42615=ORIENTED_EDGE ( 'NONE', *, *, #45812, .T. ) ;
#42617=ADVANCED_FACE ( 'NONE', ( #30529 ), #10657, .F. ) ;
#42618=VECTOR ( 'NONE', #10207, 39.37007874015748143 ) ;
#42619=EDGE_CURVE ( 'NONE', #22241, #43639, #42384, .T. ) ;
#42620=VERTEX_POINT ( 'NONE', #38531 ) ;
#42623=ADVANCED_FACE ( 'NONE', ( #22521 ), #22276, .F. ) ;
#42625=CARTESIAN_POINT ( 'NONE',  ( -0.8182917201112819283, 0.000000000000000000, -2.244094488188968395 ) ) ;
#42629=ORIENTED_EDGE ( 'NONE', *, *, #14831, .F. ) ;
#42632=VECTOR ( 'NONE', #481, 39.37007874015748143 ) ;
#42634=DIRECTION ( 'NONE',  ( -1.000000000000000000, -0.000000000000000000, -0.000000000000000000 ) ) ;
#42636=EDGE_CURVE ( 'NONE', #14507, #36538, #7532, .T. ) ;
#42637=EDGE_CURVE ( 'NONE', #47200, #706, #26889, .T. ) ;
#42639=PLANE ( 'NONE',  #35143 ) ;
#42641=ORIENTED_EDGE ( 'NONE', *, *, #45585, .F. ) ;
#42642=CARTESIAN_POINT ( 'NONE',  ( 1.909347346926324684, 0.000000000000000000, -0.3543307086614178592 ) ) ;
#42645=CARTESIAN_POINT ( 'NONE',  ( -0.2727639067037608278, 3.346456692913386100, -1.299212598425193210 ) ) ;
#42646=VERTEX_POINT ( 'NONE', #15279 ) ;
#42649=VECTOR ( 'NONE', #29991, 39.37007874015748143 ) ;
#42651=VECTOR ( 'NONE', #2349, 39.37007874015748143 ) ;
#42652=CARTESIAN_POINT ( 'NONE',  ( 0.4696143004045481018, 3.267716535433071279, -1.629301903132388246E-16 ) ) ;
#42654=ORIENTED_EDGE ( 'NONE', *, *, #5815, .F. ) ;
#42655=CARTESIAN_POINT ( 'NONE',  ( 1.363819533518803251, 3.346456692913386100, -0.3543307086614178592 ) ) ;
#42656=ORIENTED_EDGE ( 'NONE', *, *, #43321, .F. ) ;
#42657=LINE ( 'NONE', #11927, #34456 ) ;
#42661=DIRECTION ( 'NONE',  ( -1.000000000000000000, 0.000000000000000000, 1.734723475976806848E-16 ) ) ;
#42664=ORIENTED_EDGE ( 'NONE', *, *, #28535, .F. ) ;
#42665=EDGE_LOOP ( 'NONE', ( #41951, #18147, #48189, #1479 ) ) ;
#42666=CARTESIAN_POINT ( 'NONE',  ( 0.000000000000000000, 3.267716535433071279, 0.000000000000000000 ) ) ;
#42667=CARTESIAN_POINT ( 'NONE',  ( 1.091055626815042645, 0.000000000000000000, 0.4330708661417287386 ) ) ;
#42668=ORIENTED_EDGE ( 'NONE', *, *, #5843, .F. ) ;
#42670=DIRECTION ( 'NONE',  ( 1.000000000000000000, 0.000000000000000000, 0.000000000000000000 ) ) ;
#42671=FACE_OUTER_BOUND ( 'NONE', #25294, .T. ) ;
#42672=PLANE ( 'NONE',  #2227 ) ;
#42673=VECTOR ( 'NONE', #16687, 39.37007874015748143 ) ;
#42674=ORIENTED_EDGE ( 'NONE', *, *, #33205, .F. ) ;
#42675=EDGE_LOOP ( 'NONE', ( #32986, #17236, #2861, #24381, #22301, #1356, #10010, #35670, #46668, #28135, #34917, #24961, #41802, #7178, #12768, #10529, #21186, #39576, #39713, #16982, #16432, #46398, #33292, #48305, #42437, #28789, #30980, #43342, #40416, #45276, #12840, #38182, #7450, #30802, #119, #36671, #43679, #3187, #18635, #6334, #21879, #21993, #23789, #8527, #40801, #1978, #24733, #14992, #19820, #25075, #41583, #48917, #33573, #18444, #910, #14301, #13611, #36911, #13767, #14396, #37250, #47388, #28065, #49617, #27821, #14213, #31939, #46489, #48536, #22992, #29612, #50812, #24343, #47771, #35187, #44138, #17670, #50170, #8692, #32790, #34357, #23526, #24304, #408, #15492, #29940, #38700 ) ) ;
#42676=DIRECTION ( 'NONE',  ( -1.000000000000000000, -0.000000000000000000, -0.000000000000000000 ) ) ;
#42677=CARTESIAN_POINT ( 'NONE',  ( 0.1968503937007873017, 3.346456692913386100, -1.259842519685035134 ) ) ;
#42678=CARTESIAN_POINT ( 'NONE',  ( 1.636583440222563857, 0.000000000000000000, 0.4330708661417290162 ) ) ;
#42679=ORIENTED_EDGE ( 'NONE', *, *, #8178, .T. ) ;
#42681=DIRECTION ( 'NONE',  ( -0.000000000000000000, 0.000000000000000000, 1.000000000000000000 ) ) ;
#42683=EDGE_CURVE ( 'NONE', #20401, #19154, #50906, .T. ) ;
#42684=LINE ( 'NONE', #42435, #19190 ) ;
#42685=ORIENTED_EDGE ( 'NONE', *, *, #30041, .F. ) ;
#42686=ORIENTED_EDGE ( 'NONE', *, *, #36049, .T. ) ;
#42687=FACE_OUTER_BOUND ( 'NONE', #24613, .T. ) ;
#42688=CARTESIAN_POINT ( 'NONE',  ( 1.091055626815042645, 0.000000000000000000, 0.3149606299212578953 ) ) ;
#42692=VECTOR ( 'NONE', #32656, 39.37007874015748143 ) ;
#42693=CIRCLE ( 'NONE', #22908, 2.106299212598425008 ) ;
#42696=DIRECTION ( 'NONE',  ( -3.469446951953613696E-16, 0.000000000000000000, -1.000000000000000000 ) ) ;
#42697=ORIENTED_EDGE ( 'NONE', *, *, #35685, .F. ) ;
#42698=VECTOR ( 'NONE', #40020, 39.37007874015748143 ) ;
#42700=LINE ( 'NONE', #7349, #3019 ) ;
#42701=CARTESIAN_POINT ( 'NONE',  ( -1.909347346926324462, 3.267716535433071279, 1.021348170950612255 ) ) ;
#42702=EDGE_CURVE ( 'NONE', #3958, #11368, #7784, .T. ) ;
#42704=DIRECTION ( 'NONE',  ( 1.734723475976806848E-16, 0.000000000000000000, 1.000000000000000000 ) ) ;
#42705=CARTESIAN_POINT ( 'NONE',  ( 1.091055626815042645, 3.346456692913386100, 1.259842519685033357 ) ) ;
#42706=ORIENTED_EDGE ( 'NONE', *, *, #34378, .F. ) ;
#42707=CARTESIAN_POINT ( 'NONE',  ( 0.4696143004045479907, 3.267716535433071279, -1.629301903132387999E-16 ) ) ;
#42709=VECTOR ( 'NONE', #8103, 39.37007874015748143 ) ;
#42710=DIRECTION ( 'NONE',  ( 1.000000000000000000, -0.000000000000000000, 0.000000000000000000 ) ) ;
#42711=ORIENTED_EDGE ( 'NONE', *, *, #27233, .F. ) ;
#42712=CARTESIAN_POINT ( 'NONE',  ( -0.5455278134075212115, 3.267716535433071279, 9.463399047163220715E-17 ) ) ;
#42715=EDGE_CURVE ( 'NONE', #10781, #11701, #12882, .T. ) ;
#42716=DIRECTION ( 'NONE',  ( -3.469446951953613696E-16, 0.000000000000000000, -1.000000000000000000 ) ) ;
#42717=DIRECTION ( 'NONE',  ( -3.469446951953613696E-16, 0.000000000000000000, -1.000000000000000000 ) ) ;
#42718=LINE ( 'NONE', #23346, #30983 ) ;
#42719=ORIENTED_EDGE ( 'NONE', *, *, #36660, .T. ) ;
#42720=LINE ( 'NONE', #7612, #10654 ) ;
#42723=EDGE_CURVE ( 'NONE', #23450, #41713, #17267, .T. ) ;
#42724=CARTESIAN_POINT ( 'NONE',  ( 1.636583440222563857, 0.000000000000000000, 0.6299212598425164567 ) ) ;
#42725=DIRECTION ( 'NONE',  ( 1.000000000000000000, 0.000000000000000000, 0.000000000000000000 ) ) ;
#42727=ORIENTED_EDGE ( 'NONE', *, *, #50514, .F. ) ;
#42728=VERTEX_POINT ( 'NONE', #1255 ) ;
#42729=PLANE ( 'NONE',  #5083 ) ;
#42730=PLANE ( 'NONE',  #32881 ) ;
#42732=DIRECTION ( 'NONE',  ( 1.000000000000000000, 0.000000000000000000, 0.000000000000000000 ) ) ;
#42733=VECTOR ( 'NONE', #31333, 39.37007874015748143 ) ;
#42734=DIRECTION ( 'NONE',  ( 1.000000000000000000, 0.000000000000000000, -3.469446951953613696E-16 ) ) ;
#42736=LINE ( 'NONE', #47334, #16553 ) ;
#42737=VECTOR ( 'NONE', #35763, 39.37007874015748143 ) ;
#42739=ORIENTED_EDGE ( 'NONE', *, *, #25331, .F. ) ;
#42740=VERTEX_POINT ( 'NONE', #24753 ) ;
#42742=VECTOR ( 'NONE', #6390, 39.37007874015748143 ) ;
#42743=CARTESIAN_POINT ( 'NONE',  ( 0.000000000000000000, 3.267716535433071279, 1.220472440944875281 ) ) ;
#42745=DIRECTION ( 'NONE',  ( 1.734723475976806848E-16, -0.000000000000000000, 1.000000000000000000 ) ) ;
#42746=ORIENTED_EDGE ( 'NONE', *, *, #13803, .T. ) ;
#42748=AXIS2_PLACEMENT_3D ( 'NONE', #39928, #12559, #32972 ) ;
#42749=ADVANCED_FACE ( 'NONE', ( #13646 ), #33024, .F. ) ;
#42750=AXIS2_PLACEMENT_3D ( 'NONE', #23453, #19829, #218 ) ;
#42752=ORIENTED_EDGE ( 'NONE', *, *, #36156, .T. ) ;
#42753=DIRECTION ( 'NONE',  ( -1.000000000000000000, -0.000000000000000000, -0.000000000000000000 ) ) ;
#42756=LINE ( 'NONE', #22641, #48302 ) ;
#42758=VECTOR ( 'NONE', #1979, 39.37007874015748143 ) ;
#42759=DIRECTION ( 'NONE',  ( 1.000000000000000000, -0.000000000000000000, 0.000000000000000000 ) ) ;
#42760=CARTESIAN_POINT ( 'NONE',  ( -1.636583440222564301, 0.000000000000000000, -1.456692913385822186 ) ) ;
#42762=EDGE_LOOP ( 'NONE', ( #32252, #878, #28896, #42668 ) ) ;
#42763=CARTESIAN_POINT ( 'NONE',  ( 0.4696143004045484903, 3.346456692913386100, 1.102362204724404160 ) ) ;
#42764=FACE_OUTER_BOUND ( 'NONE', #8093, .T. ) ;
#42765=CARTESIAN_POINT ( 'NONE',  ( -1.166969139818016199, 3.346456692913386100, -0.6692913385826760875 ) ) ;
#42766=PLANE ( 'NONE',  #47077 ) ;
#42767=VECTOR ( 'NONE', #40347, 39.37007874015748143 ) ;
#42768=AXIS2_PLACEMENT_3D ( 'NONE', #42286, #37681, #29668 ) ;
#42773=DIRECTION ( 'NONE',  ( -3.469446951953613696E-16, 0.000000000000000000, -1.000000000000000000 ) ) ;
#42774=EDGE_CURVE ( 'NONE', #37198, #47182, #9515, .T. ) ;
#42777=DIRECTION ( 'NONE',  ( 1.000000000000000000, 0.000000000000000000, 0.000000000000000000 ) ) ;
#42778=ORIENTED_EDGE ( 'NONE', *, *, #30176, .F. ) ;
#42781=CARTESIAN_POINT ( 'NONE',  ( -1.439733046521777027, 0.000000000000000000, -1.141732283464563791 ) ) ;
#42783=CARTESIAN_POINT ( 'NONE',  ( 0.1968503937007878568, 0.000000000000000000, 1.889763779527550369 ) ) ;
#42784=CARTESIAN_POINT ( 'NONE',  ( -1.166969139818015533, 0.000000000000000000, 0.7874015748031456541 ) ) ;
#42787=ORIENTED_EDGE ( 'NONE', *, *, #29666, .T. ) ;
#42788=EDGE_LOOP ( 'NONE', ( #46392, #27392, #38590, #6036 ) ) ;
#42789=CARTESIAN_POINT ( 'NONE',  ( 0.2727639067037610499, 3.346456692913386100, 2.047244094488179567 ) ) ;
#42790=ORIENTED_EDGE ( 'NONE', *, *, #24784, .F. ) ;
#42791=EDGE_CURVE ( 'NONE', #9101, #48909, #35663, .T. ) ;
#42792=CARTESIAN_POINT ( 'NONE',  ( -1.636583440222564301, 3.346456692913386100, -1.771653543307080581 ) ) ;
#42793=CARTESIAN_POINT ( 'NONE',  ( -0.6214413264104939882, 3.267716535433071279, 0.2755905511810998187 ) ) ;
#42794=VERTEX_POINT ( 'NONE', #21393 ) ;
#42795=EDGE_CURVE ( 'NONE', #11317, #5956, #48707, .T. ) ;
#42797=VECTOR ( 'NONE', #7314, 39.37007874015748143 ) ;
#42799=CARTESIAN_POINT ( 'NONE',  ( 0.8182917201112819283, 3.267716535433071279, -1.419509857074483292E-16 ) ) ;
#42800=EDGE_LOOP ( 'NONE', ( #47258, #12308, #11217, #5192 ) ) ;
#42801=VERTEX_POINT ( 'NONE', #13388 ) ;
#42802=CARTESIAN_POINT ( 'NONE',  ( -1.363819533518803473, 3.346456692913386100, -1.417322834645664109 ) ) ;
#42803=VERTEX_POINT ( 'NONE', #48451 ) ;
#42804=EDGE_CURVE ( 'NONE', #41352, #17988, #13138, .T. ) ;
#42806=CARTESIAN_POINT ( 'NONE',  ( 0.000000000000000000, 3.267716535433071279, -1.574803149606293529 ) ) ;
#42807=ORIENTED_EDGE ( 'NONE', *, *, #49236, .F. ) ;
#42808=ORIENTED_EDGE ( 'NONE', *, *, #40942, .T. ) ;
#42810=VECTOR ( 'NONE', #40893, 39.37007874015748143 ) ;
#42811=CARTESIAN_POINT ( 'NONE',  ( 1.015142113812069313, 0.000000000000000000, 0.1574803149606286423 ) ) ;
#42812=CARTESIAN_POINT ( 'NONE',  ( -2.443991082961025185, 3.256070107886888110, -0.1574803149606298636 ) ) ;
#42814=LINE ( 'NONE', #35586, #11381 ) ;
#42817=CARTESIAN_POINT ( 'NONE',  ( 0.000000000000000000, 3.346456692913386100, 0.000000000000000000 ) ) ;
#42818=CARTESIAN_POINT ( 'NONE',  ( 1.636583440222563635, 0.000000000000000000, -1.259842519685035800 ) ) ;
#42822=LINE ( 'NONE', #46920, #12988 ) ;
#42825=DIRECTION ( 'NONE',  ( -0.000000000000000000, 1.000000000000000000, -0.000000000000000000 ) ) ;
#42826=DIRECTION ( 'NONE',  ( -0.000000000000000000, 1.000000000000000000, -0.000000000000000000 ) ) ;
#42827=AXIS2_PLACEMENT_3D ( 'NONE', #4267, #12275, #12016 ) ;
#42828=CARTESIAN_POINT ( 'NONE',  ( 2.106197740627111958, 0.000000000000000000, 0.5905511811023582691 ) ) ;
#42829=ORIENTED_EDGE ( 'NONE', *, *, #37151, .T. ) ;
#42830=DIRECTION ( 'NONE',  ( -1.000000000000000000, 0.000000000000000000, 0.000000000000000000 ) ) ;
#42831=ORIENTED_EDGE ( 'NONE', *, *, #5987, .F. ) ;
#42834=VECTOR ( 'NONE', #45157, 39.37007874015748143 ) ;
#42836=EDGE_CURVE ( 'NONE', #22772, #21459, #33787, .T. ) ;
#42837=VERTEX_POINT ( 'NONE', #2275 ) ;
#42838=EDGE_CURVE ( 'NONE', #9111, #9804, #6908, .T. ) ;
#42839=EDGE_CURVE ( 'NONE', #27124, #15499, #30408, .T. ) ;
#42840=CARTESIAN_POINT ( 'NONE',  ( 0.4696143004045476577, 0.000000000000000000, -2.047244094488182231 ) ) ;
#42842=DIRECTION ( 'NONE',  ( 1.000000000000000000, 0.000000000000000000, 0.000000000000000000 ) ) ;
#42843=AXIS2_PLACEMENT_3D ( 'NONE', #25590, #12699, #29203 ) ;
#42844=VERTEX_POINT ( 'NONE', #29647 ) ;
#42846=CARTESIAN_POINT ( 'NONE',  ( 1.091055626815042645, 3.346456692913386100, 0.4330708661417287386 ) ) ;
#42848=DIRECTION ( 'NONE',  ( 1.000000000000000000, 0.000000000000000000, 0.000000000000000000 ) ) ;
#42849=EDGE_LOOP ( 'NONE', ( #9839, #23029, #24107, #7577 ) ) ;
#42850=EDGE_LOOP ( 'NONE', ( #3422, #37027, #31390, #43561 ) ) ;
#42851=CARTESIAN_POINT ( 'NONE',  ( -1.166969139818015533, 0.000000000000000000, 1.102362204724404160 ) ) ;
#42852=CARTESIAN_POINT ( 'NONE',  ( 0.5455278134075212115, 0.000000000000000000, 0.9448818897637746295 ) ) ;
#42855=ADVANCED_FACE ( 'NONE', ( #49467 ), #25511, .F. ) ;
#42856=ORIENTED_EDGE ( 'NONE', *, *, #26136, .F. ) ;
#42857=EDGE_CURVE ( 'NONE', #11491, #40469, #30150, .T. ) ;
#42858=CARTESIAN_POINT ( 'NONE',  ( 0.1968503937007878568, 0.000000000000000000, 2.204724409448808764 ) ) ;
#42859=DIRECTION ( 'NONE',  ( 1.734723475976806848E-16, -0.000000000000000000, 1.000000000000000000 ) ) ;
#42860=VERTEX_POINT ( 'NONE', #2531 ) ;
#42861=EDGE_CURVE ( 'NONE', #28846, #38729, #41772, .T. ) ;
#42862=CARTESIAN_POINT ( 'NONE',  ( -1.439733046521777027, 3.267716535433071279, -1.456692913385822186 ) ) ;
#42864=EDGE_LOOP ( 'NONE', ( #43657, #37742, #8717, #30903 ) ) ;
#42867=VERTEX_POINT ( 'NONE', #17769 ) ;
#42869=VECTOR ( 'NONE', #17499, 39.37007874015748143 ) ;
#42872=LINE ( 'NONE', #39773, #10475 ) ;
#42873=CARTESIAN_POINT ( 'NONE',  ( 0.8182917201112817063, 0.000000000000000000, -1.614173228346451605 ) ) ;
#42874=EDGE_LOOP ( 'NONE', ( #39815, #4216, #28980, #26357, #24352 ) ) ;
#42875=ORIENTED_EDGE ( 'NONE', *, *, #45524, .F. ) ;
#42876=CARTESIAN_POINT ( 'NONE',  ( 3.616083068348484413E-16, 3.346456692913386100, 2.952755905511811552 ) ) ;
#42877=CARTESIAN_POINT ( 'NONE',  ( -1.091055626815042645, 3.267716535433071279, -0.8267716535433052849 ) ) ;
#42878=VECTOR ( 'NONE', #36654, 39.37007874015748143 ) ;
#42879=ORIENTED_EDGE ( 'NONE', *, *, #27428, .T. ) ;
#42880=DIRECTION ( 'NONE',  ( 1.000000000000000000, 0.000000000000000000, -3.469446951953613696E-16 ) ) ;
#42882=CARTESIAN_POINT ( 'NONE',  ( -0.2727639067037607723, 3.346456692913386100, 0.1574803149606283648 ) ) ;
#42883=LINE ( 'NONE', #23270, #47443 ) ;
#42884=CARTESIAN_POINT ( 'NONE',  ( 3.927031490892378253E-16, 0.000000000000000000, 1.377952755905504256 ) ) ;
#42885=ORIENTED_EDGE ( 'NONE', *, *, #48210, .F. ) ;
#42886=PLANE ( 'NONE',  #41505 ) ;
#42889=ORIENTED_EDGE ( 'NONE', *, *, #20394, .T. ) ;
#42890=FACE_OUTER_BOUND ( 'NONE', #21815, .T. ) ;
#42891=CARTESIAN_POINT ( 'NONE',  ( -0.2727639067037607723, 3.346456692913386100, -1.732283464566922726 ) ) ;
#42894=EDGE_CURVE ( 'NONE', #24866, #30287, #34035, .T. ) ;
#42897=CARTESIAN_POINT ( 'NONE',  ( 0.2727639067037607168, 3.267716535433071279, -4.731699523581612206E-17 ) ) ;
#42898=VERTEX_POINT ( 'NONE', #22158 ) ;
#42899=CARTESIAN_POINT ( 'NONE',  ( 0.2727639067037609943, 3.346456692913386100, 1.850393700787392293 ) ) ;
#42900=EDGE_CURVE ( 'NONE', #49899, #42214, #49975, .T. ) ;
#42903=DIRECTION ( 'NONE',  ( 1.000000000000000000, 0.000000000000000000, 0.000000000000000000 ) ) ;
#42905=DIRECTION ( 'NONE',  ( -1.000000000000000000, 0.000000000000000000, -0.000000000000000000 ) ) ;
#42906=AXIS2_PLACEMENT_3D ( 'NONE', #9265, #25010, #5134 ) ;
#42908=ORIENTED_EDGE ( 'NONE', *, *, #23870, .F. ) ;
#42910=DIRECTION ( 'NONE',  ( -0.000000000000000000, 1.000000000000000000, -0.000000000000000000 ) ) ;
#42911=CARTESIAN_POINT ( 'NONE',  ( -1.344120862506149594, 3.256110399587370807, 2.047244094488179567 ) ) ;
#42917=CARTESIAN_POINT ( 'NONE',  ( -1.091055626815042645, 3.267716535433071279, -0.5118110236220467790 ) ) ;
#42918=ORIENTED_EDGE ( 'NONE', *, *, #34956, .F. ) ;
#42919=EDGE_LOOP ( 'NONE', ( #38875, #28700, #26873, #46369 ) ) ;
#42920=EDGE_CURVE ( 'NONE', #20320, #17100, #10024, .T. ) ;
#42921=DIRECTION ( 'NONE',  ( 0.000000000000000000, 1.000000000000000000, 0.000000000000000000 ) ) ;
#42922=CARTESIAN_POINT ( 'NONE',  ( -1.363819533518803029, 0.000000000000000000, 0.1574803149606287811 ) ) ;
#42923=DIRECTION ( 'NONE',  ( 1.734723475976806848E-16, -0.000000000000000000, 1.000000000000000000 ) ) ;
#42924=ORIENTED_EDGE ( 'NONE', *, *, #43317, .F. ) ;
#42926=PLANE ( 'NONE',  #45824 ) ;
#42928=EDGE_CURVE ( 'NONE', #19691, #1644, #18841, .T. ) ;
#42930=ORIENTED_EDGE ( 'NONE', *, *, #6634, .T. ) ;
#42931=ORIENTED_EDGE ( 'NONE', *, *, #36585, .F. ) ;
#42932=DIRECTION ( 'NONE',  ( -3.469446951953613696E-16, 0.000000000000000000, -1.000000000000000000 ) ) ;
#42935=CARTESIAN_POINT ( 'NONE',  ( -2.454875160333845674, 3.232777166330581320, 0.1574803149606286423 ) ) ;
#42936=PLANE ( 'NONE',  #16437 ) ;
#42937=ORIENTED_EDGE ( 'NONE', *, *, #13743, .F. ) ;
#42940=VERTEX_POINT ( 'NONE', #49219 ) ;
#42941=CARTESIAN_POINT ( 'NONE',  ( -1.363819533518803473, 3.346456692913386100, -1.102362204724405270 ) ) ;
#42943=VECTOR ( 'NONE', #39728, 39.37007874015748143 ) ;
#42944=VECTOR ( 'NONE', #49438, 39.37007874015748143 ) ;
#42945=CARTESIAN_POINT ( 'NONE',  ( 1.636583440222563635, 3.267716535433071279, -1.456692913385823296 ) ) ;
#42948=CARTESIAN_POINT ( 'NONE',  ( 0.000000000000000000, 3.267716535433071279, 0.000000000000000000 ) ) ;
#42951=EDGE_LOOP ( 'NONE', ( #11174, #41126, #29421 ) ) ;
#42952=VECTOR ( 'NONE', #6083, 39.37007874015748143 ) ;
#42953=LINE ( 'NONE', #44736, #24060 ) ;
#42955=LINE ( 'NONE', #23343, #39505 ) ;
#42956=CARTESIAN_POINT ( 'NONE',  ( 1.091055626815042423, 3.267716535433071279, -1.259842519685035134 ) ) ;
#42958=LINE ( 'NONE', #3227, #16133 ) ;
#42960=EDGE_CURVE ( 'NONE', #50349, #9679, #45109, .T. ) ;
#42961=ORIENTED_EDGE ( 'NONE', *, *, #20476, .T. ) ;
#42962=LINE ( 'NONE', #23351, #14777 ) ;
#42963=ORIENTED_EDGE ( 'NONE', *, *, #31882, .T. ) ;
#42964=LINE ( 'NONE', #4246, #36104 ) ;
#42967=DIRECTION ( 'NONE',  ( 1.000000000000000000, -0.000000000000000000, 0.000000000000000000 ) ) ;
#42970=EDGE_LOOP ( 'NONE', ( #42991, #25145, #45697, #4408 ) ) ;
#42972=CARTESIAN_POINT ( 'NONE',  ( -1.636583440222563857, 3.267716535433071279, 2.839019714148966584E-16 ) ) ;
#42974=DIRECTION ( 'NONE',  ( -0.000000000000000000, 1.000000000000000000, -0.000000000000000000 ) ) ;
#42975=LINE ( 'NONE', #49933, #35926 ) ;
#42977=VECTOR ( 'NONE', #30344, 39.37007874015748143 ) ;
#42978=DIRECTION ( 'NONE',  ( -1.000000000000000000, 0.000000000000000000, 0.000000000000000000 ) ) ;
#42979=VECTOR ( 'NONE', #46839, 39.37007874015748143 ) ;
#42980=VERTEX_POINT ( 'NONE', #43017 ) ;
#42981=EDGE_CURVE ( 'NONE', #33170, #4557, #7169, .T. ) ;
#42983=CARTESIAN_POINT ( 'NONE',  ( -1.712496953225537188, 3.346456692913386100, 0.4724409448818871482 ) ) ;
#42984=FACE_OUTER_BOUND ( 'NONE', #12208, .T. ) ;
#42985=VECTOR ( 'NONE', #14675, 39.37007874015748143 ) ;
#42987=ADVANCED_FACE ( 'NONE', ( #20033 ), #163, .F. ) ;
#42989=ORIENTED_EDGE ( 'NONE', *, *, #31487, .T. ) ;
#42990=VECTOR ( 'NONE', #39959, 39.37007874015748143 ) ;
#42991=ORIENTED_EDGE ( 'NONE', *, *, #3776, .F. ) ;
#42993=VECTOR ( 'NONE', #6281, 39.37007874015748143 ) ;
#42995=VERTEX_POINT ( 'NONE', #46373 ) ;
#42996=DIRECTION ( 'NONE',  ( -1.000000000000000000, -0.000000000000000000, -0.000000000000000000 ) ) ;
#42997=ORIENTED_EDGE ( 'NONE', *, *, #26254, .F. ) ;
#42998=CARTESIAN_POINT ( 'NONE',  ( 0.000000000000000000, 3.267716535433071279, -1.574803149606293529 ) ) ;
#43001=CARTESIAN_POINT ( 'NONE',  ( 1.091055626815042423, 0.000000000000000000, -1.574803149606294417 ) ) ;
#43002=LINE ( 'NONE', #7649, #21779 ) ;
#43007=ORIENTED_EDGE ( 'NONE', *, *, #40933, .T. ) ;
#43009=CARTESIAN_POINT ( 'NONE',  ( 0.000000000000000000, 3.267716535433071279, 0.1574803149606286423 ) ) ;
#43012=ORIENTED_EDGE ( 'NONE', *, *, #46557, .F. ) ;
#43013=VECTOR ( 'NONE', #25357, 39.37007874015748143 ) ;
#43016=EDGE_LOOP ( 'NONE', ( #34568, #7897, #50896, #10412 ) ) ;
#43017=CARTESIAN_POINT ( 'NONE',  ( -0.8942052331142552601, 3.346456692913386100, -1.889763779527552146 ) ) ;
#43018=DIRECTION ( 'NONE',  ( -0.000000000000000000, 0.000000000000000000, 1.000000000000000000 ) ) ;
#43019=VECTOR ( 'NONE', #11435, 39.37007874015748143 ) ;
#43021=LINE ( 'NONE', #7671, #5968 ) ;
#43024=EDGE_CURVE ( 'NONE', #5216, #16605, #38664, .T. ) ;
#43026=VECTOR ( 'NONE', #4307, 39.37007874015748143 ) ;
#43027=CARTESIAN_POINT ( 'NONE',  ( 0.5455278134075212115, 3.346456692913386100, -1.259842519685035134 ) ) ;
#43028=DIRECTION ( 'NONE',  ( -3.469446951953613696E-16, 0.000000000000000000, -1.000000000000000000 ) ) ;
#43029=EDGE_CURVE ( 'NONE', #32071, #45936, #35802, .T. ) ;
#43030=ORIENTED_EDGE ( 'NONE', *, *, #21537, .F. ) ;
#43031=EDGE_CURVE ( 'NONE', #6021, #11147, #47373, .T. ) ;
#43032=ORIENTED_EDGE ( 'NONE', *, *, #5161, .T. ) ;
#43034=CARTESIAN_POINT ( 'NONE',  ( -0.2727639067037607723, 3.346456692913386100, 0.4724409448818869817 ) ) ;
#43035=ORIENTED_EDGE ( 'NONE', *, *, #50514, .T. ) ;
#43036=DIRECTION ( 'NONE',  ( 1.734723475976806848E-16, -0.000000000000000000, 1.000000000000000000 ) ) ;
#43037=FACE_OUTER_BOUND ( 'NONE', #3100, .T. ) ;
#43038=EDGE_LOOP ( 'NONE', ( #19351, #14042, #15007, #10104 ) ) ;
#43039=DIRECTION ( 'NONE',  ( -3.469446951953613696E-16, 0.000000000000000000, -1.000000000000000000 ) ) ;
#43042=ORIENTED_EDGE ( 'NONE', *, *, #48742, .T. ) ;
#43043=ORIENTED_EDGE ( 'NONE', *, *, #44895, .T. ) ;
#43044=CARTESIAN_POINT ( 'NONE',  ( 0.8182917201112824834, 3.346456692913386100, 1.850393700787392293 ) ) ;
#43047=LINE ( 'NONE', #7449, #41062 ) ;
#43048=EDGE_CURVE ( 'NONE', #22523, #36726, #15666, .T. ) ;
#43049=ORIENTED_EDGE ( 'NONE', *, *, #49522, .T. ) ;
#43050=ORIENTED_EDGE ( 'NONE', *, *, #25132, .F. ) ;
#43051=DIRECTION ( 'NONE',  ( 0.000000000000000000, 1.000000000000000000, 0.000000000000000000 ) ) ;
#43052=VECTOR ( 'NONE', #7194, 39.37007874015748143 ) ;
#43054=ORIENTED_EDGE ( 'NONE', *, *, #36448, .T. ) ;
#43055=VECTOR ( 'NONE', #47283, 39.37007874015748143 ) ;
#43058=VERTEX_POINT ( 'NONE', #50469 ) ;
#43060=VECTOR ( 'NONE', #49834, 39.37007874015748143 ) ;
#43062=CARTESIAN_POINT ( 'NONE',  ( -1.363819533518803473, 3.267716535433071279, 1.535433070866133232 ) ) ;
#43063=CARTESIAN_POINT ( 'NONE',  ( -1.195183497228115035E-16, 3.346456692913386100, 0.3149606299212576177 ) ) ;
#43064=EDGE_LOOP ( 'NONE', ( #44057, #43249, #41919, #10991 ) ) ;
#43066=DIRECTION ( 'NONE',  ( -1.000000000000000000, 0.000000000000000000, -0.000000000000000000 ) ) ;
#43067=CARTESIAN_POINT ( 'NONE',  ( -0.3486774197067339376, 3.346456692913386100, -0.6299212598425175669 ) ) ;
#43078=ORIENTED_EDGE ( 'NONE', *, *, #38648, .T. ) ;
#43079=EDGE_LOOP ( 'NONE', ( #15742, #48276, #38142, #35186 ) ) ;
#43080=EDGE_CURVE ( 'NONE', #18489, #46097, #30913, .T. ) ;
#43081=DIRECTION ( 'NONE',  ( 0.000000000000000000, 0.000000000000000000, -1.000000000000000000 ) ) ;
#43082=CARTESIAN_POINT ( 'NONE',  ( -0.2727639067037607723, 0.000000000000000000, -1.417322834645664331 ) ) ;
#43083=ORIENTED_EDGE ( 'NONE', *, *, #37836, .T. ) ;
#43084=ADVANCED_FACE ( 'NONE', ( #19277 ), #23664, .F. ) ;
#43085=EDGE_CURVE ( 'NONE', #49411, #22546, #11540, .T. ) ;
#43086=VECTOR ( 'NONE', #48293, 39.37007874015748143 ) ;
#43087=DIRECTION ( 'NONE',  ( 1.000000000000000000, -0.000000000000000000, 0.000000000000000000 ) ) ;
#43088=ORIENTED_EDGE ( 'NONE', *, *, #42170, .T. ) ;
#43089=FACE_OUTER_BOUND ( 'NONE', #18250, .T. ) ;
#43092=VECTOR ( 'NONE', #49777, 39.37007874015748143 ) ;
#43094=CARTESIAN_POINT ( 'NONE',  ( 0.2727639067037604947, 0.000000000000000000, 0.1574803149606283648 ) ) ;
#43095=EDGE_CURVE ( 'NONE', #7950, #45913, #27276, .T. ) ;
#43097=VECTOR ( 'NONE', #49212, 39.37007874015748143 ) ;
#43098=LINE ( 'NONE', #7744, #4919 ) ;
#43099=VERTEX_POINT ( 'NONE', #27530 ) ;
#43102=DIRECTION ( 'NONE',  ( -0.000000000000000000, 0.000000000000000000, 1.000000000000000000 ) ) ;
#43104=ORIENTED_EDGE ( 'NONE', *, *, #42014, .T. ) ;
#43105=LINE ( 'NONE', #11378, #18788 ) ;
#43108=ORIENTED_EDGE ( 'NONE', *, *, #45976, .F. ) ;
#43109=DIRECTION ( 'NONE',  ( -3.469446951953613696E-16, 0.000000000000000000, -1.000000000000000000 ) ) ;
#43110=VERTEX_POINT ( 'NONE', #19529 ) ;
#43111=ORIENTED_EDGE ( 'NONE', *, *, #17693, .T. ) ;
#43113=EDGE_CURVE ( 'NONE', #23957, #4956, #43272, .T. ) ;
#43116=CARTESIAN_POINT ( 'NONE',  ( -2.032045338671488288, 3.346456692913386100, 0.7480314960629874665 ) ) ;
#43117=EDGE_CURVE ( 'NONE', #45764, #30593, #35546, .T. ) ;
#43118=EDGE_CURVE ( 'NONE', #46760, #38185, #25201, .T. ) ;
#43119=PLANE ( 'NONE',  #27545 ) ;
#43120=CARTESIAN_POINT ( 'NONE',  ( -0.3486774197067334380, 3.346456692913386100, 0.9448818897637749625 ) ) ;
#43122=EDGE_LOOP ( 'NONE', ( #1632, #25466, #23731, #7030 ) ) ;
#43123=VECTOR ( 'NONE', #25860, 39.37007874015748143 ) ;
#43127=CARTESIAN_POINT ( 'NONE',  ( -1.636583440222563635, 0.000000000000000000, 0.4330708661417290162 ) ) ;
#43128=DIRECTION ( 'NONE',  ( 0.000000000000000000, -1.000000000000000000, 0.000000000000000000 ) ) ;
#43130=LINE ( 'NONE', #27639, #50279 ) ;
#43131=VECTOR ( 'NONE', #45988, 39.37007874015748143 ) ;
#43132=CARTESIAN_POINT ( 'NONE',  ( -0.5455278134075208785, 0.000000000000000000, 1.259842519685033357 ) ) ;
#43134=DIRECTION ( 'NONE',  ( -1.000000000000000000, 0.000000000000000000, -0.000000000000000000 ) ) ;
#43135=CIRCLE ( 'NONE', #38238, 2.106299212598425008 ) ;
#43136=VERTEX_POINT ( 'NONE', #1198 ) ;
#43139=EDGE_CURVE ( 'NONE', #16462, #44897, #44552, .T. ) ;
#43141=ORIENTED_EDGE ( 'NONE', *, *, #15016, .F. ) ;
#43142=FACE_OUTER_BOUND ( 'NONE', #19403, .T. ) ;
#43143=DIRECTION ( 'NONE',  ( 1.000000000000000000, 0.000000000000000000, 0.000000000000000000 ) ) ;
#43144=FACE_OUTER_BOUND ( 'NONE', #9394, .T. ) ;
#43145=ORIENTED_EDGE ( 'NONE', *, *, #18170, .T. ) ;
#43147=ADVANCED_FACE ( 'NONE', ( #17205 ), #941, .F. ) ;
#43151=ORIENTED_EDGE ( 'NONE', *, *, #4039, .T. ) ;
#43153=ORIENTED_EDGE ( 'NONE', *, *, #14498, .T. ) ;
#43155=CARTESIAN_POINT ( 'NONE',  ( 0.5455278134075217666, 0.000000000000000000, 2.204724409448808764 ) ) ;
#43156=DIRECTION ( 'NONE',  ( 1.734723475976806848E-16, -0.000000000000000000, 1.000000000000000000 ) ) ;
#43157=VERTEX_POINT ( 'NONE', #24185 ) ;
#43158=VECTOR ( 'NONE', #32543, 39.37007874015748143 ) ;
#43159=VERTEX_POINT ( 'NONE', #8686 ) ;
#43161=CARTESIAN_POINT ( 'NONE',  ( 0.5455278134075211005, 0.000000000000000000, 0.7480314960629872445 ) ) ;
#43162=FACE_OUTER_BOUND ( 'NONE', #40892, .T. ) ;
#43163=VERTEX_POINT ( 'NONE', #40958 ) ;
#43165=CARTESIAN_POINT ( 'NONE',  ( 1.091055626815042645, 3.346456692913386100, 0.3149606299212578953 ) ) ;
#43166=DIRECTION ( 'NONE',  ( 1.734723475976806848E-16, -0.000000000000000000, 1.000000000000000000 ) ) ;
#43168=VECTOR ( 'NONE', #31364, 39.37007874015748143 ) ;
#43170=VERTEX_POINT ( 'NONE', #5582 ) ;
#43171=EDGE_LOOP ( 'NONE', ( #39653, #50755, #3306, #6300 ) ) ;
#43173=CARTESIAN_POINT ( 'NONE',  ( -2.071704270381554913, 3.267716535433071279, -0.6299212598425177889 ) ) ;
#43174=PLANE ( 'NONE',  #13819 ) ;
#43175=VERTEX_POINT ( 'NONE', #28555 ) ;
#43176=DIRECTION ( 'NONE',  ( -0.000000000000000000, 0.000000000000000000, 1.000000000000000000 ) ) ;
#43177=CARTESIAN_POINT ( 'NONE',  ( -2.182111253630085290, 3.267716535433071279, 0.4330708661417290162 ) ) ;
#43178=AXIS2_PLACEMENT_3D ( 'NONE', #41082, #1315, #29190 ) ;
#43179=ORIENTED_EDGE ( 'NONE', *, *, #47002, .F. ) ;
#43180=CARTESIAN_POINT ( 'NONE',  ( 0.8182917201112817063, 3.346456692913386100, -1.929133858267711110 ) ) ;
#43182=ORIENTED_EDGE ( 'NONE', *, *, #38815, .T. ) ;
#43183=CARTESIAN_POINT ( 'NONE',  ( -1.636583440222564301, 0.000000000000000000, 1.574803149606291530 ) ) ;
#43185=CARTESIAN_POINT ( 'NONE',  ( 1.536664496436161003E-16, 3.267716535433071279, -2.665687976667886873E-32 ) ) ;
#43187=DIRECTION ( 'NONE',  ( -0.000000000000000000, 1.000000000000000000, -0.000000000000000000 ) ) ;
#43188=LINE ( 'NONE', #43446, #14776 ) ;
#43191=EDGE_CURVE ( 'NONE', #20798, #3180, #21334, .T. ) ;
#43192=EDGE_LOOP ( 'NONE', ( #44084, #913, #44557, #43601 ) ) ;
#43193=DIRECTION ( 'NONE',  ( -1.000000000000000000, 0.000000000000000000, -0.000000000000000000 ) ) ;
#43196=CARTESIAN_POINT ( 'NONE',  ( -1.712496953225537188, 3.346456692913386100, -0.1574803149606297248 ) ) ;
#43199=DIRECTION ( 'NONE',  ( 0.000000000000000000, 1.000000000000000000, 0.000000000000000000 ) ) ;
#43201=AXIS2_PLACEMENT_3D ( 'NONE', #44311, #17216, #40708 ) ;
#43202=EDGE_CURVE ( 'NONE', #8694, #18289, #35351, .T. ) ;
#43203=DIRECTION ( 'NONE',  ( -3.469446951953613696E-16, 0.000000000000000000, -1.000000000000000000 ) ) ;
#43204=AXIS2_PLACEMENT_3D ( 'NONE', #41906, #30027, #10411 ) ;
#43205=VECTOR ( 'NONE', #21904, 39.37007874015748143 ) ;
#43206=ORIENTED_EDGE ( 'NONE', *, *, #26540, .T. ) ;
#43207=CARTESIAN_POINT ( 'NONE',  ( 1.499921196763806419, 3.267716535433071279, -1.929133858267710666 ) ) ;
#43211=ORIENTED_EDGE ( 'NONE', *, *, #21994, .T. ) ;
#43212=DIRECTION ( 'NONE',  ( 0.000000000000000000, 1.000000000000000000, 0.000000000000000000 ) ) ;
#43213=CARTESIAN_POINT ( 'NONE',  ( -0.3486774197067334935, 3.346456692913386100, 1.377952755905504256 ) ) ;
#43214=CARTESIAN_POINT ( 'NONE',  ( -2.182111253630085734, 3.346456692913386100, -1.141732283464563791 ) ) ;
#43215=VECTOR ( 'NONE', #46564, 39.37007874015748143 ) ;
#43217=ADVANCED_FACE ( 'NONE', ( #20564 ), #44304, .F. ) ;
#43219=LINE ( 'NONE', #40396, #37899 ) ;
#43221=PLANE ( 'NONE',  #22907 ) ;
#43222=FACE_OUTER_BOUND ( 'NONE', #41171, .T. ) ;
#43223=LINE ( 'NONE', #15113, #6237 ) ;
#43224=EDGE_LOOP ( 'NONE', ( #33223, #4655, #7348, #15822 ) ) ;
#43225=EDGE_LOOP ( 'NONE', ( #40859, #38427, #4639, #49595 ) ) ;
#43226=DIRECTION ( 'NONE',  ( 0.000000000000000000, 1.000000000000000000, 0.000000000000000000 ) ) ;
#43227=CARTESIAN_POINT ( 'NONE',  ( -1.091055626815042645, 3.267716535433071279, -0.9448818897637760728 ) ) ;
#43228=ORIENTED_EDGE ( 'NONE', *, *, #44940, .T. ) ;
#43229=CARTESIAN_POINT ( 'NONE',  ( 0.8182917201112824834, 0.000000000000000000, 1.417322834645662777 ) ) ;
#43230=DIRECTION ( 'NONE',  ( 1.734723475976806848E-16, 0.000000000000000000, 1.000000000000000000 ) ) ;
#43231=PLANE ( 'NONE',  #39238 ) ;
#43234=ORIENTED_EDGE ( 'NONE', *, *, #15068, .T. ) ;
#43235=DIRECTION ( 'NONE',  ( 1.000000000000000000, -0.000000000000000000, 0.000000000000000000 ) ) ;
#43236=PLANE ( 'NONE',  #128 ) ;
#43238=EDGE_LOOP ( 'NONE', ( #11784, #9602, #14491, #249 ) ) ;
#43240=VECTOR ( 'NONE', #33845, 39.37007874015748143 ) ;
#43241=ORIENTED_EDGE ( 'NONE', *, *, #17627, .T. ) ;
#43242=EDGE_LOOP ( 'NONE', ( #5026, #6445, #43806, #38316 ) ) ;
#43243=DIRECTION ( 'NONE',  ( -3.469446951953613696E-16, 0.000000000000000000, -1.000000000000000000 ) ) ;
#43244=VECTOR ( 'NONE', #21596, 39.37007874015748143 ) ;
#43245=VECTOR ( 'NONE', #15851, 39.37007874015748143 ) ;
#43246=ORIENTED_EDGE ( 'NONE', *, *, #31370, .F. ) ;
#43248=CARTESIAN_POINT ( 'NONE',  ( 2.106197740627112402, 3.267716535433071279, 0.02067487291359298637 ) ) ;
#43249=ORIENTED_EDGE ( 'NONE', *, *, #37184, .T. ) ;
#43250=EDGE_CURVE ( 'NONE', #3960, #28934, #16698, .T. ) ;
#43251=VECTOR ( 'NONE', #5336, 39.37007874015748143 ) ;
#43255=ADVANCED_FACE ( 'NONE', ( #16182 ), #48393, .F. ) ;
#43259=DIRECTION ( 'NONE',  ( 0.000000000000000000, 0.000000000000000000, -1.000000000000000000 ) ) ;
#43260=CARTESIAN_POINT ( 'NONE',  ( -0.2727639067037608278, 3.346456692913386100, 0.2755905511810995412 ) ) ;
#43262=DIRECTION ( 'NONE',  ( 0.000000000000000000, -1.000000000000000000, 0.000000000000000000 ) ) ;
#43263=LINE ( 'NONE', #23148, #34274 ) ;
#43264=CARTESIAN_POINT ( 'NONE',  ( 0.2727639067037606613, 3.267716535433071279, -4.731699523581610974E-17 ) ) ;
#43265=VERTEX_POINT ( 'NONE', #8435 ) ;
#43266=LINE ( 'NONE', #23661, #23178 ) ;
#43267=EDGE_CURVE ( 'NONE', #17956, #2104, #23800, .T. ) ;
#43271=ORIENTED_EDGE ( 'NONE', *, *, #50118, .T. ) ;
#43272=LINE ( 'NONE', #7919, #27078 ) ;
#43273=PLANE ( 'NONE',  #32554 ) ;
#43274=CARTESIAN_POINT ( 'NONE',  ( 1.909347346926324684, 3.267716535433071279, -3.312189666507128175E-16 ) ) ;
#43276=VECTOR ( 'NONE', #13415, 39.37007874015748143 ) ;
#43277=EDGE_CURVE ( 'NONE', #47459, #17713, #30350, .T. ) ;
#43278=VECTOR ( 'NONE', #5950, 39.37007874015748143 ) ;
#43279=DIRECTION ( 'NONE',  ( 1.734723475976806848E-16, -0.000000000000000000, 1.000000000000000000 ) ) ;
#43280=ORIENTED_EDGE ( 'NONE', *, *, #35788, .F. ) ;
#43281=LINE ( 'NONE', #3550, #26452 ) ;
#43282=AXIS2_PLACEMENT_3D ( 'NONE', #16124, #31889, #47578 ) ;
#43283=CARTESIAN_POINT ( 'NONE',  ( 0.4696143004045484903, 3.267716535433071279, 1.732283464566921172 ) ) ;
#43284=DIRECTION ( 'NONE',  ( 1.000000000000000000, 0.000000000000000000, 0.000000000000000000 ) ) ;
#43285=CARTESIAN_POINT ( 'NONE',  ( 0.000000000000000000, 3.267716535433071279, 0.000000000000000000 ) ) ;
#43288=ORIENTED_EDGE ( 'NONE', *, *, #22621, .T. ) ;
#43290=CARTESIAN_POINT ( 'NONE',  ( 0.8182917201112819283, 3.346456692913386100, 0.9055118110236164419 ) ) ;
#43291=ORIENTED_EDGE ( 'NONE', *, *, #2010, .F. ) ;
#43294=EDGE_CURVE ( 'NONE', #1152, #19232, #33731, .T. ) ;
#43295=ORIENTED_EDGE ( 'NONE', *, *, #37187, .F. ) ;
#43296=DIRECTION ( 'NONE',  ( 0.000000000000000000, 0.000000000000000000, -1.000000000000000000 ) ) ;
#43297=ORIENTED_EDGE ( 'NONE', *, *, #27520, .F. ) ;
#43298=CARTESIAN_POINT ( 'NONE',  ( -1.909347346926324906, 3.267716535433071279, 1.417322834645662333 ) ) ;
#43299=CARTESIAN_POINT ( 'NONE',  ( 1.499921196763806419, 3.267716535433071279, -1.929133858267710666 ) ) ;
#43301=VERTEX_POINT ( 'NONE', #29588 ) ;
#43304=DIRECTION ( 'NONE',  ( 1.734723475976806848E-16, -0.000000000000000000, 1.000000000000000000 ) ) ;
#43305=VERTEX_POINT ( 'NONE', #42209 ) ;
#43307=LINE ( 'NONE', #23701, #21557 ) ;
#43308=VECTOR ( 'NONE', #45231, 39.37007874015748143 ) ;
#43309=EDGE_CURVE ( 'NONE', #49899, #2298, #29840, .T. ) ;
#43310=CARTESIAN_POINT ( 'NONE',  ( 4.268512490100411402E-16, 0.000000000000000000, 0.9448818897637749625 ) ) ;
#43311=VECTOR ( 'NONE', #25456, 39.37007874015748143 ) ;
#43312=VERTEX_POINT ( 'NONE', #33478 ) ;
#43314=AXIS2_PLACEMENT_3D ( 'NONE', #5722, #41097, #21725 ) ;
#43317=EDGE_CURVE ( 'NONE', #28387, #47614, #45554, .T. ) ;
#43318=DIRECTION ( 'NONE',  ( 0.000000000000000000, -1.000000000000000000, 0.000000000000000000 ) ) ;
#43319=EDGE_CURVE ( 'NONE', #41767, #18572, #25965, .T. ) ;
#43321=EDGE_CURVE ( 'NONE', #9931, #33373, #33218, .T. ) ;
#43322=DIRECTION ( 'NONE',  ( -0.000000000000000000, 1.000000000000000000, -0.000000000000000000 ) ) ;
#43323=ORIENTED_EDGE ( 'NONE', *, *, #31920, .F. ) ;
#43324=EDGE_LOOP ( 'NONE', ( #18969, #7634, #8703, #30091 ) ) ;
#43325=VECTOR ( 'NONE', #9661, 39.37007874015748143 ) ;
#43326=CARTESIAN_POINT ( 'NONE',  ( 0.8182917201112819283, 3.267716535433071279, -1.419509857074483292E-16 ) ) ;
#43327=CARTESIAN_POINT ( 'NONE',  ( 1.363819533518803029, 3.346456692913386100, -1.102362204724405714 ) ) ;
#43328=CARTESIAN_POINT ( 'NONE',  ( 4.268512490100411402E-16, 3.346456692913386100, 1.574803149606291974 ) ) ;
#43330=LINE ( 'NONE', #23720, #26451 ) ;
#43332=ADVANCED_FACE ( 'NONE', ( #13840 ), #49662, .F. ) ;
#43333=ORIENTED_EDGE ( 'NONE', *, *, #33540, .F. ) ;
#43334=DIRECTION ( 'NONE',  ( -0.000000000000000000, 1.000000000000000000, -0.000000000000000000 ) ) ;
#43335=ORIENTED_EDGE ( 'NONE', *, *, #35650, .T. ) ;
#43336=LINE ( 'NONE', #50779, #16860 ) ;
#43337=EDGE_CURVE ( 'NONE', #31565, #24019, #41714, .T. ) ;
#43338=ORIENTED_EDGE ( 'NONE', *, *, #7278, .F. ) ;
#43339=PLANE ( 'NONE',  #31654 ) ;
#43341=DIRECTION ( 'NONE',  ( 1.734723475976806848E-16, -0.000000000000000000, 1.000000000000000000 ) ) ;
#43342=ORIENTED_EDGE ( 'NONE', *, *, #26096, .T. ) ;
#43344=CARTESIAN_POINT ( 'NONE',  ( 1.091055626815042423, 3.346456692913386100, -1.456692913385822630 ) ) ;
#43345=VECTOR ( 'NONE', #36046, 39.37007874015748143 ) ;
#43346=ORIENTED_EDGE ( 'NONE', *, *, #21707, .F. ) ;
#43347=CARTESIAN_POINT ( 'NONE',  ( 0.2727639067037604392, 0.000000000000000000, 0.5905511811023579360 ) ) ;
#43348=EDGE_CURVE ( 'NONE', #1059, #4594, #41460, .T. ) ;
#43349=AXIS2_PLACEMENT_3D ( 'NONE', #17534, #6871, #46829 ) ;
#43350=EDGE_LOOP ( 'NONE', ( #9653, #10679, #37914, #35269 ) ) ;
#43351=CARTESIAN_POINT ( 'NONE',  ( -0.07591351300297277671, 3.346456692913386100, 2.047244094488179567 ) ) ;
#43352=DIRECTION ( 'NONE',  ( 1.000000000000000000, -0.000000000000000000, 0.000000000000000000 ) ) ;
#43356=VECTOR ( 'NONE', #9219, 39.37007874015748143 ) ;
#43358=ORIENTED_EDGE ( 'NONE', *, *, #38723, .T. ) ;
#43359=ORIENTED_EDGE ( 'NONE', *, *, #38667, .F. ) ;
#43360=EDGE_CURVE ( 'NONE', #18949, #5207, #48902, .T. ) ;
#43362=LINE ( 'NONE', #8001, #26493 ) ;
#43363=DIRECTION ( 'NONE',  ( 1.734723475976806848E-16, -0.000000000000000000, 1.000000000000000000 ) ) ;
#43364=EDGE_CURVE ( 'NONE', #16143, #370, #13591, .T. ) ;
#43365=ORIENTED_EDGE ( 'NONE', *, *, #17184, .T. ) ;
#43366=DIRECTION ( 'NONE',  ( -0.000000000000000000, 1.000000000000000000, -0.000000000000000000 ) ) ;
#43368=VERTEX_POINT ( 'NONE', #45807 ) ;
#43369=CARTESIAN_POINT ( 'NONE',  ( 0.2727639067037608278, 3.267716535433071279, -4.731699523581614055E-17 ) ) ;
#43370=ORIENTED_EDGE ( 'NONE', *, *, #7443, .T. ) ;
#43371=EDGE_LOOP ( 'NONE', ( #45092, #7871, #31688, #16382 ) ) ;
#43372=ORIENTED_EDGE ( 'NONE', *, *, #6730, .F. ) ;
#43373=CARTESIAN_POINT ( 'NONE',  ( 4.268512490100411402E-16, 3.346456692913386100, 1.574803149606291974 ) ) ;
#43374=EDGE_CURVE ( 'NONE', #25574, #39964, #17714, .T. ) ;
#43375=DIRECTION ( 'NONE',  ( -1.000000000000000000, 0.000000000000000000, -0.000000000000000000 ) ) ;
#43376=AXIS2_PLACEMENT_3D ( 'NONE', #36753, #29246, #41140 ) ;
#43377=CARTESIAN_POINT ( 'NONE',  ( -1.636583440222564301, 0.000000000000000000, -0.9448818897637762948 ) ) ;
#43379=CARTESIAN_POINT ( 'NONE',  ( 0.000000000000000000, 3.267716535433071279, 1.692913385826762873 ) ) ;
#43382=AXIS2_PLACEMENT_3D ( 'NONE', #49533, #22225, #22722 ) ;
#43384=VECTOR ( 'NONE', #46794, 39.37007874015748143 ) ;
#43385=PLANE ( 'NONE',  #35853 ) ;
#43386=VERTEX_POINT ( 'NONE', #26219 ) ;
#43387=DIRECTION ( 'NONE',  ( 1.000000000000000000, 0.000000000000000000, 0.000000000000000000 ) ) ;
#43388=VECTOR ( 'NONE', #39817, 39.37007874015748143 ) ;
#43390=VECTOR ( 'NONE', #2795, 39.37007874015748143 ) ;
#43391=DIRECTION ( 'NONE',  ( 1.734723475976806848E-16, 0.000000000000000000, 1.000000000000000000 ) ) ;
#43393=DIRECTION ( 'NONE',  ( 1.734723475976806848E-16, -0.000000000000000000, 1.000000000000000000 ) ) ;
#43394=AXIS2_PLACEMENT_3D ( 'NONE', #24656, #9158, #13293 ) ;
#43395=ORIENTED_EDGE ( 'NONE', *, *, #14707, .F. ) ;
#43396=CARTESIAN_POINT ( 'NONE',  ( 1.909347346926324684, 0.000000000000000000, 0.4724409448818868706 ) ) ;
#43398=VERTEX_POINT ( 'NONE', #22350 ) ;
#43399=VERTEX_POINT ( 'NONE', #29325 ) ;
#43401=CARTESIAN_POINT ( 'NONE',  ( 0.000000000000000000, 3.267716535433071279, -0.3149606299212593941 ) ) ;
#43402=DIRECTION ( 'NONE',  ( 1.000000000000000000, 0.000000000000000000, 0.000000000000000000 ) ) ;
#43403=ORIENTED_EDGE ( 'NONE', *, *, #44934, .F. ) ;
#43404=EDGE_CURVE ( 'NONE', #32825, #24862, #38106, .T. ) ;
#43406=DIRECTION ( 'NONE',  ( -1.000000000000000000, -0.000000000000000000, -0.000000000000000000 ) ) ;
#43407=ORIENTED_EDGE ( 'NONE', *, *, #7596, .F. ) ;
#43410=ORIENTED_EDGE ( 'NONE', *, *, #45397, .F. ) ;
#43415=EDGE_CURVE ( 'NONE', #44588, #23253, #7607, .T. ) ;
#43417=VERTEX_POINT ( 'NONE', #26963 ) ;
#43420=DIRECTION ( 'NONE',  ( -0.000000000000000000, 1.000000000000000000, -0.000000000000000000 ) ) ;
#43423=ORIENTED_EDGE ( 'NONE', *, *, #45422, .F. ) ;
#43427=CARTESIAN_POINT ( 'NONE',  ( 1.287906020515830141, 3.267716535433071279, -0.3149606299212596716 ) ) ;
#43428=LINE ( 'NONE', #7817, #25286 ) ;
#43429=VERTEX_POINT ( 'NONE', #27721 ) ;
#43431=LINE ( 'NONE', #48039, #38974 ) ;
#43432=AXIS2_PLACEMENT_3D ( 'NONE', #40033, #24023, #39260 ) ;
#43434=ORIENTED_EDGE ( 'NONE', *, *, #2252, .T. ) ;
#43435=FACE_OUTER_BOUND ( 'NONE', #29623, .T. ) ;
#43437=ORIENTED_EDGE ( 'NONE', *, *, #32796, .T. ) ;
#43439=ORIENTED_EDGE ( 'NONE', *, *, #47070, .T. ) ;
#43440=EDGE_LOOP ( 'NONE', ( #20039, #26251, #23104, #32885 ) ) ;
#43442=EDGE_CURVE ( 'NONE', #7243, #39002, #50412, .T. ) ;
#43443=LINE ( 'NONE', #3456, #46149 ) ;
#43445=EDGE_CURVE ( 'NONE', #35577, #11067, #15101, .T. ) ;
#43446=CARTESIAN_POINT ( 'NONE',  ( -0.8182917201112814842, 3.346456692913386100, 1.102362204724404160 ) ) ;
#43447=EDGE_LOOP ( 'NONE', ( #3734, #16587, #12970, #15018 ) ) ;
#43449=ORIENTED_EDGE ( 'NONE', *, *, #28654, .F. ) ;
#43450=DIRECTION ( 'NONE',  ( -3.469446951953613696E-16, 0.000000000000000000, -1.000000000000000000 ) ) ;
#43452=CIRCLE ( 'NONE', #39338, 2.165354330708661568 ) ;
#43453=VECTOR ( 'NONE', #16633, 39.37007874015748143 ) ;
#43454=CARTESIAN_POINT ( 'NONE',  ( 0.5455278134075212115, 0.000000000000000000, 0.6299212598425161236 ) ) ;
#43455=CARTESIAN_POINT ( 'NONE',  ( 0.2727639067037609943, 3.346456692913386100, 2.165354330708650910 ) ) ;
#43457=ORIENTED_EDGE ( 'NONE', *, *, #42057, .T. ) ;
#43461=FACE_OUTER_BOUND ( 'NONE', #33766, .T. ) ;
#43462=FACE_OUTER_BOUND ( 'NONE', #6689, .T. ) ;
#43464=ORIENTED_EDGE ( 'NONE', *, *, #36826, .T. ) ;
#43466=DIRECTION ( 'NONE',  ( -0.000000000000000000, 1.000000000000000000, -0.000000000000000000 ) ) ;
#43467=LINE ( 'NONE', #7863, #4456 ) ;
#43468=ORIENTED_EDGE ( 'NONE', *, *, #31440, .F. ) ;
#43469=FACE_OUTER_BOUND ( 'NONE', #3824, .T. ) ;
#43471=EDGE_LOOP ( 'NONE', ( #22444, #8537, #5651, #26486, #10002, #2389 ) ) ;
#43472=VECTOR ( 'NONE', #4228, 39.37007874015748143 ) ;
#43474=DIRECTION ( 'NONE',  ( -1.000000000000000000, -0.000000000000000000, -0.000000000000000000 ) ) ;
#43476=LINE ( 'NONE', #47834, #19743 ) ;
#43478=ADVANCED_FACE ( 'NONE', ( #2979 ), #3222, .F. ) ;
#43481=ORIENTED_EDGE ( 'NONE', *, *, #34854, .F. ) ;
#43482=CARTESIAN_POINT ( 'NONE',  ( -0.07591351300297277671, 0.000000000000000000, 1.417322834645662777 ) ) ;
#43483=DIRECTION ( 'NONE',  ( 1.734723475976806848E-16, -0.000000000000000000, 1.000000000000000000 ) ) ;
#43484=ORIENTED_EDGE ( 'NONE', *, *, #48714, .F. ) ;
#43485=PLANE ( 'NONE',  #8544 ) ;
#43487=DIRECTION ( 'NONE',  ( -1.000000000000000000, 0.000000000000000000, 0.000000000000000000 ) ) ;
#43490=ORIENTED_EDGE ( 'NONE', *, *, #23509, .T. ) ;
#43491=ORIENTED_EDGE ( 'NONE', *, *, #45620, .T. ) ;
#43492=CARTESIAN_POINT ( 'NONE',  ( 1.687984952120845428, 3.346456692913386100, 1.259842519685033135 ) ) ;
#43493=AXIS2_PLACEMENT_3D ( 'NONE', #42156, #45755, #26166 ) ;
#43494=VECTOR ( 'NONE', #22230, 39.37007874015748143 ) ;
#43495=DIRECTION ( 'NONE',  ( 1.734723475976806848E-16, 0.000000000000000000, 1.000000000000000000 ) ) ;
#43496=DIRECTION ( 'NONE',  ( -3.469446951953613696E-16, 0.000000000000000000, -1.000000000000000000 ) ) ;
#43497=FACE_BOUND ( 'NONE', #46779, .T. ) ;
#43498=ORIENTED_EDGE ( 'NONE', *, *, #142, .T. ) ;
#43499=CARTESIAN_POINT ( 'NONE',  ( 4.268512490100411402E-16, 3.346456692913386100, 1.889763779527550369 ) ) ;
#43501=AXIS2_PLACEMENT_3D ( 'NONE', #30501, #34381, #50071 ) ;
#43502=ORIENTED_EDGE ( 'NONE', *, *, #36759, .F. ) ;
#43506=ORIENTED_EDGE ( 'NONE', *, *, #8430, .T. ) ;
#43508=DIRECTION ( 'NONE',  ( 1.000000000000000000, 0.000000000000000000, -3.469446951953613696E-16 ) ) ;
#43510=VECTOR ( 'NONE', #30193, 39.37007874015748143 ) ;
#43512=B_SPLINE_CURVE_WITH_KNOTS ( 'NONE', 3,
 ( #23813, #39561, #42911, #19921 ),
 .UNSPECIFIED., .F., .F.,
 ( 4, 4 ),
 ( 0.04164592054790196285, 0.04281073085324779703 ),
 .UNSPECIFIED. ) ;
#43513=EDGE_CURVE ( 'NONE', #21641, #37337, #42955, .T. ) ;
#43514=AXIS2_PLACEMENT_3D ( 'NONE', #18657, #11653, #50096 ) ;
#43515=DIRECTION ( 'NONE',  ( 1.734723475976806848E-16, -0.000000000000000000, 1.000000000000000000 ) ) ;
#43517=DIRECTION ( 'NONE',  ( -1.000000000000000000, 0.000000000000000000, 0.000000000000000000 ) ) ;
#43518=CARTESIAN_POINT ( 'NONE',  ( -0.3486774197067339376, 3.346456692913386100, 2.077238655036873549 ) ) ;
#43524=CARTESIAN_POINT ( 'NONE',  ( 0.2727639067037604392, 0.000000000000000000, -0.6692913385826760875 ) ) ;
#43525=VERTEX_POINT ( 'NONE', #35232 ) ;
#43526=CARTESIAN_POINT ( 'NONE',  ( 0.8182917201112824834, 3.267716535433071279, 1.850393700787392293 ) ) ;
#43527=CARTESIAN_POINT ( 'NONE',  ( 1.091055626815042645, 0.000000000000000000, 0.6299212598425161236 ) ) ;
#43528=VERTEX_POINT ( 'NONE', #19466 ) ;
#43529=CARTESIAN_POINT ( 'NONE',  ( -1.732283464566932052, 3.346456692913386100, -1.299212598425193210 ) ) ;
#43530=AXIS2_PLACEMENT_3D ( 'NONE', #28175, #48981, #41532 ) ;
#43535=ORIENTED_EDGE ( 'NONE', *, *, #6618, .T. ) ;
#43536=PLANE ( 'NONE',  #27251 ) ;
#43539=CIRCLE ( 'NONE', #21311, 2.165354330708661568 ) ;
#43540=DIRECTION ( 'NONE',  ( -0.000000000000000000, 1.000000000000000000, -0.000000000000000000 ) ) ;
#43541=DIRECTION ( 'NONE',  ( -0.000000000000000000, 1.000000000000000000, -0.000000000000000000 ) ) ;
#43542=EDGE_LOOP ( 'NONE', ( #27764, #23536, #20813, #34084 ) ) ;
#43543=AXIS2_PLACEMENT_3D ( 'NONE', #23962, #727, #47926 ) ;
#43544=EDGE_CURVE ( 'NONE', #39002, #1584, #23598, .T. ) ;
#43545=EDGE_LOOP ( 'NONE', ( #20696, #18312, #37167, #40409 ) ) ;
#43546=ORIENTED_EDGE ( 'NONE', *, *, #20358, .F. ) ;
#43549=VERTEX_POINT ( 'NONE', #27466 ) ;
#43550=CARTESIAN_POINT ( 'NONE',  ( 0.000000000000000000, 3.267716535433071279, -0.7874015748031473194 ) ) ;
#43554=EDGE_CURVE ( 'NONE', #13419, #34660, #16634, .T. ) ;
#43556=EDGE_LOOP ( 'NONE', ( #24205, #49864, #4511, #50534 ) ) ;
#43559=ORIENTED_EDGE ( 'NONE', *, *, #48401, .F. ) ;
#43560=CARTESIAN_POINT ( 'NONE',  ( -1.636583440222563635, 3.346456692913386100, 0.6299212598425164567 ) ) ;
#43561=ORIENTED_EDGE ( 'NONE', *, *, #42333, .T. ) ;
#43563=EDGE_CURVE ( 'NONE', #5670, #39828, #40387, .T. ) ;
#43565=EDGE_LOOP ( 'NONE', ( #6580, #4400, #36142, #37691 ) ) ;
#43569=EDGE_CURVE ( 'NONE', #48864, #31004, #24373, .T. ) ;
#43570=ORIENTED_EDGE ( 'NONE', *, *, #38387, .T. ) ;
#43571=AXIS2_PLACEMENT_3D ( 'NONE', #47445, #12374, #23733 ) ;
#43572=FACE_OUTER_BOUND ( 'NONE', #50845, .T. ) ;
#43573=VERTEX_POINT ( 'NONE', #31873 ) ;
#43574=FACE_OUTER_BOUND ( 'NONE', #40866, .T. ) ;
#43575=CARTESIAN_POINT ( 'NONE',  ( 0.000000000000000000, 3.267716535433071279, 0.000000000000000000 ) ) ;
#43576=AXIS2_PLACEMENT_3D ( 'NONE', #8329, #31834, #27942 ) ;
#43577=VECTOR ( 'NONE', #9408, 39.37007874015748143 ) ;
#43578=LINE ( 'NONE', #5113, #8245 ) ;
#43579=ORIENTED_EDGE ( 'NONE', *, *, #13771, .F. ) ;
#43580=ORIENTED_EDGE ( 'NONE', *, *, #13076, .T. ) ;
#43581=DIRECTION ( 'NONE',  ( 0.000000000000000000, 0.000000000000000000, 1.000000000000000000 ) ) ;
#43582=CARTESIAN_POINT ( 'NONE',  ( 1.636583440222563857, 3.346456692913386100, 1.377952755905504256 ) ) ;
#43583=LINE ( 'NONE', #38960, #48862 ) ;
#43584=AXIS2_PLACEMENT_3D ( 'NONE', #36320, #40699, #37086 ) ;
#43586=LINE ( 'NONE', #24240, #42943 ) ;
#43588=ORIENTED_EDGE ( 'NONE', *, *, #48765, .F. ) ;
#43589=DIRECTION ( 'NONE',  ( 1.734723475976806848E-16, -0.000000000000000000, 1.000000000000000000 ) ) ;
#43590=EDGE_LOOP ( 'NONE', ( #28040, #47770, #47391, #49249 ) ) ;
#43591=CARTESIAN_POINT ( 'NONE',  ( -0.3486774197067334380, 3.267716535433071279, 1.574803149606291974 ) ) ;
#43593=CARTESIAN_POINT ( 'NONE',  ( -2.009899395340762229, 3.267716535433071279, -0.6299212598425177889 ) ) ;
#43594=DIRECTION ( 'NONE',  ( -0.000000000000000000, 1.000000000000000000, -0.000000000000000000 ) ) ;
#43596=VECTOR ( 'NONE', #31564, 39.37007874015748143 ) ;
#43598=EDGE_CURVE ( 'NONE', #2778, #40451, #32385, .T. ) ;
#43601=ORIENTED_EDGE ( 'NONE', *, *, #14329, .F. ) ;
#43602=DIRECTION ( 'NONE',  ( 1.000000000000000000, 0.000000000000000000, 0.000000000000000000 ) ) ;
#43603=ORIENTED_EDGE ( 'NONE', *, *, #37705, .T. ) ;
#43604=EDGE_CURVE ( 'NONE', #7678, #28374, #43973, .T. ) ;
#43605=VECTOR ( 'NONE', #13538, 39.37007874015748143 ) ;
#43607=DIRECTION ( 'NONE',  ( -0.000000000000000000, 1.000000000000000000, -0.000000000000000000 ) ) ;
#43608=EDGE_CURVE ( 'NONE', #8198, #33931, #12758, .T. ) ;
#43610=AXIS2_PLACEMENT_3D ( 'NONE', #8120, #11734, #39615 ) ;
#43612=ORIENTED_EDGE ( 'NONE', *, *, #38123, .T. ) ;
#43613=EDGE_LOOP ( 'NONE', ( #43043, #21330, #22096, #24226 ) ) ;
#43615=DIRECTION ( 'NONE',  ( 1.734723475976806848E-16, -0.000000000000000000, 1.000000000000000000 ) ) ;
#43617=CIRCLE ( 'NONE', #8187, 2.874015748031496731 ) ;
#43619=CARTESIAN_POINT ( 'NONE',  ( 1.558105373646058167, 3.267716535433071279, -1.417322834645665219 ) ) ;
#43620=EDGE_CURVE ( 'NONE', #23414, #44911, #36763, .T. ) ;
#43621=CARTESIAN_POINT ( 'NONE',  ( -2.009899395340762673, 3.346456692913386100, 0.6299212598425164567 ) ) ;
#43625=EDGE_LOOP ( 'NONE', ( #16228, #5641, #7389, #28572 ) ) ;
#43626=ORIENTED_EDGE ( 'NONE', *, *, #32954, .F. ) ;
#43629=LINE ( 'NONE', #25048, #4543 ) ;
#43630=CARTESIAN_POINT ( 'NONE',  ( 0.000000000000000000, 3.267716535433071279, -1.889763779527552146 ) ) ;
#43632=EDGE_CURVE ( 'NONE', #24862, #4018, #12493, .T. ) ;
#43634=DIRECTION ( 'NONE',  ( 0.000000000000000000, 1.000000000000000000, 0.000000000000000000 ) ) ;
#43635=VERTEX_POINT ( 'NONE', #40632 ) ;
#43636=ORIENTED_EDGE ( 'NONE', *, *, #17782, .T. ) ;
#43639=VERTEX_POINT ( 'NONE', #17141 ) ;
#43640=EDGE_CURVE ( 'NONE', #39372, #50839, #35996, .T. ) ;
#43641=PLANE ( 'NONE',  #44899 ) ;
#43642=CARTESIAN_POINT ( 'NONE',  ( 1.091055626815042423, 0.000000000000000000, -1.259842519685035134 ) ) ;
#43643=VECTOR ( 'NONE', #18891, 39.37007874015748143 ) ;
#43646=CARTESIAN_POINT ( 'NONE',  ( -0.8942052331142552601, 3.346456692913386100, -1.972094414217999914 ) ) ;
#43647=DIRECTION ( 'NONE',  ( 0.000000000000000000, -1.000000000000000000, 0.000000000000000000 ) ) ;
#43648=ORIENTED_EDGE ( 'NONE', *, *, #1210, .T. ) ;
#43649=LINE ( 'NONE', #31538, #15991 ) ;
#43651=AXIS2_PLACEMENT_3D ( 'NONE', #10911, #23036, #3162 ) ;
#43652=VERTEX_POINT ( 'NONE', #36508 ) ;
#43653=VERTEX_POINT ( 'NONE', #12241 ) ;
#43654=LINE ( 'NONE', #32063, #34829 ) ;
#43655=FACE_OUTER_BOUND ( 'NONE', #34543, .T. ) ;
#43656=DIRECTION ( 'NONE',  ( 1.000000000000000000, 0.000000000000000000, -3.469446951953613696E-16 ) ) ;
#43657=ORIENTED_EDGE ( 'NONE', *, *, #23102, .T. ) ;
#43658=ORIENTED_EDGE ( 'NONE', *, *, #27408, .F. ) ;
#43660=VERTEX_POINT ( 'NONE', #43716 ) ;
#43662=ORIENTED_EDGE ( 'NONE', *, *, #43710, .F. ) ;
#43665=DIRECTION ( 'NONE',  ( 1.734723475976806848E-16, -0.000000000000000000, 1.000000000000000000 ) ) ;
#43666=DIRECTION ( 'NONE',  ( -1.000000000000000000, 0.000000000000000000, 0.000000000000000000 ) ) ;
#43667=VECTOR ( 'NONE', #17678, 39.37007874015748143 ) ;
#43668=EDGE_CURVE ( 'NONE', #2919, #23674, #4237, .T. ) ;
#43670=ORIENTED_EDGE ( 'NONE', *, *, #8449, .T. ) ;
#43673=DIRECTION ( 'NONE',  ( -3.469446951953613696E-16, 0.000000000000000000, -1.000000000000000000 ) ) ;
#43674=ORIENTED_EDGE ( 'NONE', *, *, #19758, .T. ) ;
#43675=EDGE_LOOP ( 'NONE', ( #9775, #4706, #35101, #1235 ) ) ;
#43676=LINE ( 'NONE', #44193, #43714 ) ;
#43677=DIRECTION ( 'NONE',  ( -0.000000000000000000, 1.000000000000000000, -0.000000000000000000 ) ) ;
#43678=DIRECTION ( 'NONE',  ( -3.469446951953613696E-16, 0.000000000000000000, -1.000000000000000000 ) ) ;
#43679=ORIENTED_EDGE ( 'NONE', *, *, #45682, .T. ) ;
#43680=LINE ( 'NONE', #49315, #9805 ) ;
#43682=CARTESIAN_POINT ( 'NONE',  ( -0.6214413264104945434, 0.000000000000000000, -0.7874015748031467643 ) ) ;
#43684=CARTESIAN_POINT ( 'NONE',  ( -1.636583440222564301, 0.000000000000000000, -0.6299212598425177889 ) ) ;
#43686=ORIENTED_EDGE ( 'NONE', *, *, #6585, .T. ) ;
#43687=ORIENTED_EDGE ( 'NONE', *, *, #50874, .F. ) ;
#43688=ORIENTED_EDGE ( 'NONE', *, *, #33141, .T. ) ;
#43689=VECTOR ( 'NONE', #33925, 39.37007874015748143 ) ;
#43690=CARTESIAN_POINT ( 'NONE',  ( -0.5455278134075214336, 3.346456692913386100, 0.1181102362204703021 ) ) ;
#43692=CARTESIAN_POINT ( 'NONE',  ( -1.198202975868765119, 3.346456692913386100, -1.732283464566922726 ) ) ;
#43693=EDGE_CURVE ( 'NONE', #15979, #30087, #24632, .T. ) ;
#43694=LINE ( 'NONE', #39588, #45090 ) ;
#43695=LINE ( 'NONE', #5235, #34569 ) ;
#43697=ORIENTED_EDGE ( 'NONE', *, *, #24280, .T. ) ;
#43698=ORIENTED_EDGE ( 'NONE', *, *, #48831, .T. ) ;
#43701=DIRECTION ( 'NONE',  ( -0.000000000000000000, 1.000000000000000000, -0.000000000000000000 ) ) ;
#43702=EDGE_CURVE ( 'NONE', #13031, #1905, #23859, .T. ) ;
#43703=CARTESIAN_POINT ( 'NONE',  ( 1.091055626815043311, 0.000000000000000000, 1.574803149606291974 ) ) ;
#43706=EDGE_LOOP ( 'NONE', ( #22235, #44043, #8141, #11659 ) ) ;
#43708=EDGE_CURVE ( 'NONE', #27397, #31869, #48837, .T. ) ;
#43709=DIRECTION ( 'NONE',  ( -0.000000000000000000, 1.000000000000000000, -0.000000000000000000 ) ) ;
#43710=EDGE_CURVE ( 'NONE', #22725, #24393, #30025, .T. ) ;
#43714=VECTOR ( 'NONE', #13228, 39.37007874015748143 ) ;
#43715=CARTESIAN_POINT ( 'NONE',  ( -0.8942052331142547050, 0.000000000000000000, 0.3149606299212580063 ) ) ;
#43716=CARTESIAN_POINT ( 'NONE',  ( 2.378961647330872786, 3.267716535433071279, -0.1968503937007886062 ) ) ;
#43720=DIRECTION ( 'NONE',  ( -1.000000000000000000, -0.000000000000000000, -0.000000000000000000 ) ) ;
#43721=VERTEX_POINT ( 'NONE', #6544 ) ;
#43722=FACE_BOUND ( 'NONE', #14996, .T. ) ;
#43724=DIRECTION ( 'NONE',  ( -3.469446951953613696E-16, 0.000000000000000000, -1.000000000000000000 ) ) ;
#43725=EDGE_LOOP ( 'NONE', ( #45940, #32415, #24800, #47585 ) ) ;
#43726=PLANE ( 'NONE',  #8045 ) ;
#43728=PLANE ( 'NONE',  #13609 ) ;
#43731=EDGE_CURVE ( 'NONE', #30180, #10179, #49093, .T. ) ;
#43733=ORIENTED_EDGE ( 'NONE', *, *, #11853, .T. ) ;
#43734=ORIENTED_EDGE ( 'NONE', *, *, #44416, .F. ) ;
#43735=LINE ( 'NONE', #43482, #33143 ) ;
#43736=EDGE_CURVE ( 'NONE', #17239, #29386, #41151, .T. ) ;
#43737=DIRECTION ( 'NONE',  ( -1.000000000000000000, 0.000000000000000000, -0.000000000000000000 ) ) ;
#43738=ORIENTED_EDGE ( 'NONE', *, *, #548, .T. ) ;
#43739=CARTESIAN_POINT ( 'NONE',  ( 0.1968503937007877735, 3.267716535433071279, 1.377952755905504256 ) ) ;
#43740=DIRECTION ( 'NONE',  ( -3.469446951953613696E-16, 0.000000000000000000, -1.000000000000000000 ) ) ;
#43743=ORIENTED_EDGE ( 'NONE', *, *, #39968, .T. ) ;
#43745=FACE_OUTER_BOUND ( 'NONE', #50456, .T. ) ;
#43746=DIRECTION ( 'NONE',  ( 0.000000000000000000, 0.000000000000000000, -1.000000000000000000 ) ) ;
#43747=CARTESIAN_POINT ( 'NONE',  ( 0.5455278134075212115, 0.000000000000000000, -0.9448818897637765168 ) ) ;
#43749=FACE_BOUND ( 'NONE', #21709, .T. ) ;
#43750=EDGE_LOOP ( 'NONE', ( #10983, #3566, #43984, #42339 ) ) ;
#43751=CARTESIAN_POINT ( 'NONE',  ( 1.909347346926324684, 3.346456692913386100, -0.1574803149606304187 ) ) ;
#43753=ORIENTED_EDGE ( 'NONE', *, *, #14673, .T. ) ;
#43755=AXIS2_PLACEMENT_3D ( 'NONE', #45105, #1507, #5883 ) ;
#43758=ADVANCED_FACE ( 'NONE', ( #45492 ), #26154, .F. ) ;
#43761=ORIENTED_EDGE ( 'NONE', *, *, #41479, .F. ) ;
#43762=AXIS2_PLACEMENT_3D ( 'NONE', #40720, #1725, #5347 ) ;
#43765=EDGE_CURVE ( 'NONE', #38732, #3406, #13776, .T. ) ;
#43767=ADVANCED_FACE ( 'NONE', ( #1638 ), #33663, .F. ) ;
#43768=EDGE_CURVE ( 'NONE', #42606, #27951, #43617, .T. ) ;
#43769=FACE_OUTER_BOUND ( 'NONE', #6834, .T. ) ;
#43771=LINE ( 'NONE', #4550, #10502 ) ;
#43773=ORIENTED_EDGE ( 'NONE', *, *, #45532, .F. ) ;
#43776=CARTESIAN_POINT ( 'NONE',  ( 0.4696143004045479352, 3.346456692913386100, -0.4724409448818886470 ) ) ;
#43777=ORIENTED_EDGE ( 'NONE', *, *, #761, .T. ) ;
#43779=CARTESIAN_POINT ( 'NONE',  ( -0.8182917201112819283, 3.267716535433071279, -1.929133858267710000 ) ) ;
#43783=CARTESIAN_POINT ( 'NONE',  ( 0.4696143004045484348, 0.000000000000000000, 1.220472440944875281 ) ) ;
#43786=ADVANCED_FACE ( 'NONE', ( #34164 ), #17900, .F. ) ;
#43793=VECTOR ( 'NONE', #30315, 39.37007874015748143 ) ;
#43795=CARTESIAN_POINT ( 'NONE',  ( -2.182111253630085734, 3.346456692913386100, -0.8267716535433052849 ) ) ;
#43796=ADVANCED_FACE ( 'NONE', ( #29774 ), #10151, .F. ) ;
#43797=VECTOR ( 'NONE', #29279, 39.37007874015748143 ) ;
#43800=EDGE_CURVE ( 'NONE', #50716, #17666, #37278, .T. ) ;
#43801=DIRECTION ( 'NONE',  ( 1.000000000000000000, 0.000000000000000000, 0.000000000000000000 ) ) ;
#43802=EDGE_CURVE ( 'NONE', #47200, #32548, #17645, .T. ) ;
#43804=VECTOR ( 'NONE', #8775, 39.37007874015748143 ) ;
#43806=ORIENTED_EDGE ( 'NONE', *, *, #44435, .F. ) ;
#43807=CARTESIAN_POINT ( 'NONE',  ( 1.015142113812069313, 0.000000000000000000, 1.102362204724403938 ) ) ;
#43808=AXIS2_PLACEMENT_3D ( 'NONE', #10217, #33215, #20815 ) ;
#43810=ORIENTED_EDGE ( 'NONE', *, *, #44695, .T. ) ;
#43811=CARTESIAN_POINT ( 'NONE',  ( -1.091055626815042645, 3.346456692913386100, -1.259842519685034690 ) ) ;
#43812=ORIENTED_EDGE ( 'NONE', *, *, #8355, .F. ) ;
#43813=FACE_OUTER_BOUND ( 'NONE', #773, .T. ) ;
#43815=CARTESIAN_POINT ( 'NONE',  ( 1.636583440222563857, 3.346456692913386100, -0.3149606299212596716 ) ) ;
#43818=LINE ( 'NONE', #8469, #30618 ) ;
#43820=EDGE_LOOP ( 'NONE', ( #50766, #17657, #47990, #27827 ) ) ;
#43821=DIRECTION ( 'NONE',  ( -1.000000000000000000, -0.000000000000000000, -0.000000000000000000 ) ) ;
#43822=ORIENTED_EDGE ( 'NONE', *, *, #33761, .T. ) ;
#43826=VECTOR ( 'NONE', #7264, 39.37007874015748143 ) ;
#43828=LINE ( 'NONE', #48188, #30512 ) ;
#43829=ORIENTED_EDGE ( 'NONE', *, *, #34783, .F. ) ;
#43832=AXIS2_PLACEMENT_3D ( 'NONE', #47518, #3942, #19415 ) ;
#43833=CARTESIAN_POINT ( 'NONE',  ( -2.258024766633058622, 3.346456692913386100, 0.1574803149606286423 ) ) ;
#43834=CARTESIAN_POINT ( 'NONE',  ( -1.909347346926324462, 3.267716535433071279, -0.1574803149606297248 ) ) ;
#43837=VECTOR ( 'NONE', #971, 39.37007874015748143 ) ;
#43839=LINE ( 'NONE', #8490, #46212 ) ;
#43840=AXIS2_PLACEMENT_3D ( 'NONE', #34476, #10971, #11228 ) ;
#43844=ORIENTED_EDGE ( 'NONE', *, *, #29760, .F. ) ;
#43845=CARTESIAN_POINT ( 'NONE',  ( -1.985260859929297572, 3.346456692913386100, 0.9448818897637749625 ) ) ;
#43847=EDGE_LOOP ( 'NONE', ( #11312, #48857, #47024, #49505 ) ) ;
#43848=PLANE ( 'NONE',  #1131 ) ;
#43849=CARTESIAN_POINT ( 'NONE',  ( -1.636583440222564301, 0.000000000000000000, -0.3149606299212592275 ) ) ;
#43850=EDGE_CURVE ( 'NONE', #30308, #20408, #34413, .T. ) ;
#43851=CARTESIAN_POINT ( 'NONE',  ( -1.712496953225537188, 3.267716535433071279, -0.03937007874015881204 ) ) ;
#43852=ORIENTED_EDGE ( 'NONE', *, *, #49452, .T. ) ;
#43854=FACE_OUTER_BOUND ( 'NONE', #30953, .T. ) ;
#43857=CARTESIAN_POINT ( 'NONE',  ( -1.091055626815042201, 0.000000000000000000, 0.9448818897637749625 ) ) ;
#43858=EDGE_CURVE ( 'NONE', #47575, #34814, #15290, .T. ) ;
#43861=LINE ( 'NONE', #15239, #32188 ) ;
#43862=AXIS2_PLACEMENT_3D ( 'NONE', #42118, #41116, #17867 ) ;
#43865=ORIENTED_EDGE ( 'NONE', *, *, #15737, .F. ) ;
#43866=ORIENTED_EDGE ( 'NONE', *, *, #21705, .T. ) ;
#43868=VECTOR ( 'NONE', #48625, 39.37007874015748143 ) ;
#43869=LINE ( 'NONE', #8519, #29780 ) ;
#43870=DIRECTION ( 'NONE',  ( 1.734723475976806848E-16, 0.000000000000000000, 1.000000000000000000 ) ) ;
#43872=LINE ( 'NONE', #39507, #3122 ) ;
#43875=DIRECTION ( 'NONE',  ( -0.000000000000000000, 1.000000000000000000, -0.000000000000000000 ) ) ;
#43877=ORIENTED_EDGE ( 'NONE', *, *, #7097, .F. ) ;
#43879=ORIENTED_EDGE ( 'NONE', *, *, #28489, .F. ) ;
#43881=CARTESIAN_POINT ( 'NONE',  ( 2.182111253630085290, 0.000000000000000000, -0.3149606299212596716 ) ) ;
#43882=DIRECTION ( 'NONE',  ( 1.734723475976806848E-16, 0.000000000000000000, 1.000000000000000000 ) ) ;
#43883=CARTESIAN_POINT ( 'NONE',  ( -1.439733046521776583, 3.267716535433071279, -0.9448818897637762948 ) ) ;
#43884=EDGE_LOOP ( 'NONE', ( #8189, #40505, #23900, #13014 ) ) ;
#43886=EDGE_CURVE ( 'NONE', #49800, #46986, #4097, .T. ) ;
#43887=CARTESIAN_POINT ( 'NONE',  ( 1.091055626815043311, 0.000000000000000000, 1.889763779527550369 ) ) ;
#43888=DIRECTION ( 'NONE',  ( -0.000000000000000000, 1.000000000000000000, -0.000000000000000000 ) ) ;
#43889=EDGE_CURVE ( 'NONE', #20960, #39237, #29640, .T. ) ;
#43890=LINE ( 'NONE', #40556, #12641 ) ;
#43891=ORIENTED_EDGE ( 'NONE', *, *, #12475, .F. ) ;
#43892=EDGE_CURVE ( 'NONE', #15727, #2869, #14791, .T. ) ;
#43893=DIRECTION ( 'NONE',  ( -1.000000000000000000, -0.000000000000000000, -0.000000000000000000 ) ) ;
#43894=EDGE_CURVE ( 'NONE', #49655, #34486, #47716, .T. ) ;
#43895=CARTESIAN_POINT ( 'NONE',  ( -1.363819533518803473, 0.000000000000000000, 2.047244094488179567 ) ) ;
#43896=VECTOR ( 'NONE', #43875, 39.37007874015748143 ) ;
#43897=LINE ( 'NONE', #8548, #33408 ) ;
#43898=ADVANCED_FACE ( 'NONE', ( #43144 ), #46003, .F. ) ;
#43899=CARTESIAN_POINT ( 'NONE',  ( -0.6214413264104945434, 0.000000000000000000, -1.417322834645664331 ) ) ;
#43901=VECTOR ( 'NONE', #19242, 39.37007874015748143 ) ;
#43902=ORIENTED_EDGE ( 'NONE', *, *, #29358, .F. ) ;
#43903=LINE ( 'NONE', #31289, #50539 ) ;
#43904=DIRECTION ( 'NONE',  ( -0.000000000000000000, 1.000000000000000000, -0.000000000000000000 ) ) ;
#43905=VECTOR ( 'NONE', #21405, 39.37007874015748143 ) ;
#43908=ORIENTED_EDGE ( 'NONE', *, *, #41641, .F. ) ;
#43909=FACE_OUTER_BOUND ( 'NONE', #21180, .T. ) ;
#43910=DIRECTION ( 'NONE',  ( -0.000000000000000000, 1.000000000000000000, -0.000000000000000000 ) ) ;
#43912=LINE ( 'NONE', #8560, #33780 ) ;
#43914=VECTOR ( 'NONE', #49155, 39.37007874015748143 ) ;
#43917=PLANE ( 'NONE',  #45999 ) ;
#43918=ORIENTED_EDGE ( 'NONE', *, *, #45306, .F. ) ;
#43920=PLANE ( 'NONE',  #43530 ) ;
#43924=LINE ( 'NONE', #48025, #5423 ) ;
#43925=VERTEX_POINT ( 'NONE', #15039 ) ;
#43928=CARTESIAN_POINT ( 'NONE',  ( -0.3486774197067339376, 3.346456692913386100, -1.259842519685035134 ) ) ;
#43929=VERTEX_POINT ( 'NONE', #26401 ) ;
#43930=VERTEX_POINT ( 'NONE', #7295 ) ;
#43931=PLANE ( 'NONE',  #25641 ) ;
#43932=CARTESIAN_POINT ( 'NONE',  ( 0.000000000000000000, 3.267716535433071279, 1.102362204724404160 ) ) ;
#43936=CARTESIAN_POINT ( 'NONE',  ( 0.5455278134075217666, 3.346456692913386100, 1.574803149606291974 ) ) ;
#43937=LINE ( 'NONE', #843, #6001 ) ;
#43938=DIRECTION ( 'NONE',  ( -0.000000000000000000, 1.000000000000000000, -0.000000000000000000 ) ) ;
#43941=VECTOR ( 'NONE', #26680, 39.37007874015748143 ) ;
#43942=CARTESIAN_POINT ( 'NONE',  ( -0.3486774197067339376, 3.346456692913386100, -0.6299212598425175669 ) ) ;
#43944=CARTESIAN_POINT ( 'NONE',  ( -1.363819533518803473, 3.346456692913386100, 1.681890501046756192 ) ) ;
#43945=ORIENTED_EDGE ( 'NONE', *, *, #29953, .T. ) ;
#43946=VERTEX_POINT ( 'NONE', #35423 ) ;
#43948=VECTOR ( 'NONE', #19375, 39.37007874015748143 ) ;
#43949=VECTOR ( 'NONE', #21959, 39.37007874015748143 ) ;
#43950=DIRECTION ( 'NONE',  ( -1.000000000000000000, 0.000000000000000000, 0.000000000000000000 ) ) ;
#43951=CARTESIAN_POINT ( 'NONE',  ( -0.6214413264104945434, 0.000000000000000000, -0.3543307086614175816 ) ) ;
#43953=VERTEX_POINT ( 'NONE', #6788 ) ;
#43954=VERTEX_POINT ( 'NONE', #38295 ) ;
#43955=VECTOR ( 'NONE', #27972, 39.37007874015748143 ) ;
#43959=CARTESIAN_POINT ( 'NONE',  ( 0.000000000000000000, 3.267716535433071279, 2.007874015748021268 ) ) ;
#43960=EDGE_CURVE ( 'NONE', #11828, #5323, #47503, .T. ) ;
#43961=ADVANCED_FACE ( 'NONE', ( #8814 ), #24050, .F. ) ;
#43962=ADVANCED_FACE ( 'NONE', ( #31806 ), #32320, .F. ) ;
#43963=DIRECTION ( 'NONE',  ( -1.000000000000000000, 0.000000000000000000, 0.000000000000000000 ) ) ;
#43964=LINE ( 'NONE', #20487, #27686 ) ;
#43965=LINE ( 'NONE', #43455, #42709 ) ;
#43966=ORIENTED_EDGE ( 'NONE', *, *, #12757, .F. ) ;
#43968=PLANE ( 'NONE',  #28161 ) ;
#43969=ORIENTED_EDGE ( 'NONE', *, *, #6845, .F. ) ;
#43970=DIRECTION ( 'NONE',  ( -0.000000000000000000, 0.000000000000000000, 1.000000000000000000 ) ) ;
#43973=LINE ( 'NONE', #16377, #1588 ) ;
#43975=DIRECTION ( 'NONE',  ( -1.000000000000000000, 0.000000000000000000, 0.000000000000000000 ) ) ;
#43977=CARTESIAN_POINT ( 'NONE',  ( -1.602125192864240821, 3.346456692913386100, -1.456692913385822186 ) ) ;
#43980=VERTEX_POINT ( 'NONE', #48013 ) ;
#43982=DIRECTION ( 'NONE',  ( -0.000000000000000000, 1.000000000000000000, -0.000000000000000000 ) ) ;
#43983=DIRECTION ( 'NONE',  ( -0.000000000000000000, 1.000000000000000000, -0.000000000000000000 ) ) ;
#43984=ORIENTED_EDGE ( 'NONE', *, *, #7425, .T. ) ;
#43987=AXIS2_PLACEMENT_3D ( 'NONE', #25886, #18144, #49836 ) ;
#43989=CARTESIAN_POINT ( 'NONE',  ( -0.5455278134075214336, 3.267716535433071279, -1.889763779527552146 ) ) ;
#43990=LINE ( 'NONE', #38678, #11504 ) ;
#43992=EDGE_CURVE ( 'NONE', #42860, #7477, #25503, .T. ) ;
#43994=ORIENTED_EDGE ( 'NONE', *, *, #22760, .F. ) ;
#43995=LINE ( 'NONE', #36527, #14963 ) ;
#43997=CARTESIAN_POINT ( 'NONE',  ( 0.000000000000000000, 3.313179664429866556, 0.000000000000000000 ) ) ;
#43998=EDGE_LOOP ( 'NONE', ( #12662, #8656, #4839, #42222 ) ) ;
#43999=CARTESIAN_POINT ( 'NONE',  ( -0.3486774197067339376, 0.000000000000000000, -1.889763779527552146 ) ) ;
#44000=DIRECTION ( 'NONE',  ( 1.000000000000000000, 0.000000000000000000, -3.469446951953613696E-16 ) ) ;
#44002=ADVANCED_FACE ( 'NONE', ( #4429 ), #48273, .F. ) ;
#44003=CARTESIAN_POINT ( 'NONE',  ( 1.287906020515829919, 3.346456692913386100, -1.259842519685035134 ) ) ;
#44004=ORIENTED_EDGE ( 'NONE', *, *, #12047, .T. ) ;
#44005=ORIENTED_EDGE ( 'NONE', *, *, #43608, .F. ) ;
#44006=PLANE ( 'NONE',  #12229 ) ;
#44007=LINE ( 'NONE', #8651, #41463 ) ;
#44009=DIRECTION ( 'NONE',  ( 1.734723475976806848E-16, -0.000000000000000000, 1.000000000000000000 ) ) ;
#44010=FACE_BOUND ( 'NONE', #41129, .T. ) ;
#44011=ORIENTED_EDGE ( 'NONE', *, *, #10466, .F. ) ;
#44012=EDGE_CURVE ( 'NONE', #30696, #46419, #8300, .T. ) ;
#44015=ORIENTED_EDGE ( 'NONE', *, *, #33378, .T. ) ;
#44018=ORIENTED_EDGE ( 'NONE', *, *, #36639, .F. ) ;
#44019=ORIENTED_EDGE ( 'NONE', *, *, #18684, .T. ) ;
#44020=CARTESIAN_POINT ( 'NONE',  ( 0.2727639067037604947, 3.346456692913386100, -0.1574803149606298636 ) ) ;
#44021=ORIENTED_EDGE ( 'NONE', *, *, #42060, .T. ) ;
#44023=AXIS2_PLACEMENT_3D ( 'NONE', #35648, #15518, #16281 ) ;
#44025=CARTESIAN_POINT ( 'NONE',  ( -1.636583440222563635, 3.267716535433071279, 0.1181102362204704270 ) ) ;
#44028=VECTOR ( 'NONE', #17145, 39.37007874015748143 ) ;
#44030=AXIS2_PLACEMENT_3D ( 'NONE', #26581, #26084, #37468 ) ;
#44031=DIRECTION ( 'NONE',  ( 0.000000000000000000, -1.000000000000000000, 0.000000000000000000 ) ) ;
#44032=EDGE_CURVE ( 'NONE', #34431, #7984, #43912, .T. ) ;
#44033=LINE ( 'NONE', #8676, #8013 ) ;
#44034=DIRECTION ( 'NONE',  ( -0.000000000000000000, 1.000000000000000000, -0.000000000000000000 ) ) ;
#44035=VECTOR ( 'NONE', #47569, 39.37007874015748143 ) ;
#44038=PLANE ( 'NONE',  #466 ) ;
#44039=PLANE ( 'NONE',  #10019 ) ;
#44041=DIRECTION ( 'NONE',  ( -3.469446951953613696E-16, 0.000000000000000000, -1.000000000000000000 ) ) ;
#44043=ORIENTED_EDGE ( 'NONE', *, *, #26926, .T. ) ;
#44045=CARTESIAN_POINT ( 'NONE',  ( 0.000000000000000000, 3.267716535433071279, -2.086614173228339641 ) ) ;
#44046=DIRECTION ( 'NONE',  ( -1.000000000000000000, -0.000000000000000000, -0.000000000000000000 ) ) ;
#44047=EDGE_LOOP ( 'NONE', ( #30679, #18413, #37697, #46479 ) ) ;
#44049=ORIENTED_EDGE ( 'NONE', *, *, #37952, .T. ) ;
#44051=CARTESIAN_POINT ( 'NONE',  ( 1.015142113812069313, 3.346456692913386100, -0.3543307086614175816 ) ) ;
#44052=LINE ( 'NONE', #28310, #7801 ) ;
#44056=EDGE_LOOP ( 'NONE', ( #32323, #31832, #20474 ) ) ;
#44057=ORIENTED_EDGE ( 'NONE', *, *, #20502, .T. ) ;
#44058=DIRECTION ( 'NONE',  ( 0.000000000000000000, -1.000000000000000000, 0.000000000000000000 ) ) ;
#44059=ORIENTED_EDGE ( 'NONE', *, *, #49769, .T. ) ;
#44061=LINE ( 'NONE', #1721, #14528 ) ;
#44063=EDGE_CURVE ( 'NONE', #31184, #49197, #16825, .T. ) ;
#44064=VECTOR ( 'NONE', #43540, 39.37007874015748143 ) ;
#44065=VECTOR ( 'NONE', #31479, 39.37007874015748143 ) ;
#44066=DIRECTION ( 'NONE',  ( -3.469446951953613696E-16, 0.000000000000000000, -1.000000000000000000 ) ) ;
#44069=ORIENTED_EDGE ( 'NONE', *, *, #11265, .T. ) ;
#44070=CARTESIAN_POINT ( 'NONE',  ( -0.3486774197067340486, 3.346456692913386100, -0.1968503937007883287 ) ) ;
#44071=ADVANCED_FACE ( 'NONE', ( #31623 ), #36268, .F. ) ;
#44072=PLANE ( 'NONE',  #3375 ) ;
#44073=VECTOR ( 'NONE', #42716, 39.37007874015748143 ) ;
#44075=DIRECTION ( 'NONE',  ( 0.000000000000000000, 1.000000000000000000, 0.000000000000000000 ) ) ;
#44076=ORIENTED_EDGE ( 'NONE', *, *, #27237, .T. ) ;
#44077=DIRECTION ( 'NONE',  ( -1.000000000000000000, -0.000000000000000000, -0.000000000000000000 ) ) ;
#44079=VERTEX_POINT ( 'NONE', #20245 ) ;
#44080=EDGE_CURVE ( 'NONE', #33373, #13332, #637, .T. ) ;
#44081=CARTESIAN_POINT ( 'NONE',  ( -4.268512490100411402E-16, 3.346456692913386100, -2.401574803149598480 ) ) ;
#44082=VERTEX_POINT ( 'NONE', #32142 ) ;
#44084=ORIENTED_EDGE ( 'NONE', *, *, #26912, .F. ) ;
#44086=ADVANCED_FACE ( 'NONE', ( #12505 ), #12771, .F. ) ;
#44087=CARTESIAN_POINT ( 'NONE',  ( 0.000000000000000000, 3.267716535433071279, 1.692913385826762873 ) ) ;
#44088=CARTESIAN_POINT ( 'NONE',  ( -0.3486774197067334380, 0.000000000000000000, 0.9448818897637749625 ) ) ;
#44090=ADVANCED_FACE ( 'NONE', ( #35746 ), #39621, .F. ) ;
#44092=VERTEX_POINT ( 'NONE', #8891 ) ;
#44093=LINE ( 'NONE', #16746, #16243 ) ;
#44094=CARTESIAN_POINT ( 'NONE',  ( -0.07591351300297340121, 0.000000000000000000, -1.299212598425193210 ) ) ;
#44095=VECTOR ( 'NONE', #3656, 39.37007874015748143 ) ;
#44096=PLANE ( 'NONE',  #50463 ) ;
#44097=DIRECTION ( 'NONE',  ( -1.000000000000000000, 0.000000000000000000, 0.000000000000000000 ) ) ;
#44098=VECTOR ( 'NONE', #2589, 39.37007874015748143 ) ;
#44099=LINE ( 'NONE', #9765, #21886 ) ;
#44100=VECTOR ( 'NONE', #33989, 39.37007874015748143 ) ;
#44102=DIRECTION ( 'NONE',  ( 1.000000000000000000, 0.000000000000000000, 0.000000000000000000 ) ) ;
#44103=ORIENTED_EDGE ( 'NONE', *, *, #17480, .F. ) ;
#44105=LINE ( 'NONE', #39988, #45706 ) ;
#44108=CARTESIAN_POINT ( 'NONE',  ( -1.712496953225537188, 3.346456692913386100, -0.03937007874015881204 ) ) ;
#44109=ORIENTED_EDGE ( 'NONE', *, *, #18170, .F. ) ;
#44110=LINE ( 'NONE', #9781, #4451 ) ;
#44111=LINE ( 'NONE', #7987, #21253 ) ;
#44112=DIRECTION ( 'NONE',  ( 1.734723475976806848E-16, -0.000000000000000000, 1.000000000000000000 ) ) ;
#44113=CARTESIAN_POINT ( 'NONE',  ( 1.560669927219590747, 0.000000000000000000, 1.102362204724403938 ) ) ;
#44116=FACE_BOUND ( 'NONE', #30573, .T. ) ;
#44117=ORIENTED_EDGE ( 'NONE', *, *, #44287, .F. ) ;
#44122=EDGE_CURVE ( 'NONE', #11359, #12085, #43476, .T. ) ;
#44124=EDGE_CURVE ( 'NONE', #49030, #2108, #15860, .T. ) ;
#44126=AXIS2_PLACEMENT_3D ( 'NONE', #17263, #13381, #17761 ) ;
#44129=AXIS2_PLACEMENT_3D ( 'NONE', #42608, #26361, #34375 ) ;
#44130=PLANE ( 'NONE',  #3752 ) ;
#44132=LINE ( 'NONE', #17046, #32633 ) ;
#44133=VECTOR ( 'NONE', #30797, 39.37007874015748143 ) ;
#44134=EDGE_CURVE ( 'NONE', #11433, #44433, #43990, .T. ) ;
#44136=FACE_OUTER_BOUND ( 'NONE', #13078, .T. ) ;
#44137=VECTOR ( 'NONE', #43363, 39.37007874015748143 ) ;
#44138=ORIENTED_EDGE ( 'NONE', *, *, #30752, .T. ) ;
#44139=CARTESIAN_POINT ( 'NONE',  ( -1.166969139818015755, 3.267716535433071279, -0.03937007874015868020 ) ) ;
#44140=VECTOR ( 'NONE', #21855, 39.37007874015748143 ) ;
#44142=ORIENTED_EDGE ( 'NONE', *, *, #6758, .T. ) ;
#44143=ADVANCED_FACE ( 'NONE', ( #44251 ), #8637, .F. ) ;
#44147=EDGE_CURVE ( 'NONE', #22729, #50486, #20512, .T. ) ;
#44148=LINE ( 'NONE', #45156, #30029 ) ;
#44150=EDGE_CURVE ( 'NONE', #6703, #26688, #889, .T. ) ;
#44152=VERTEX_POINT ( 'NONE', #40140 ) ;
#44154=DIRECTION ( 'NONE',  ( 1.000000000000000000, 0.000000000000000000, -3.469446951953613696E-16 ) ) ;
#44156=LINE ( 'NONE', #40813, #212 ) ;
#44158=CARTESIAN_POINT ( 'NONE',  ( 2.378961647330872786, 0.000000000000000000, 0.3149606299212573401 ) ) ;
#44159=FACE_OUTER_BOUND ( 'NONE', #50134, .T. ) ;
#44160=DIRECTION ( 'NONE',  ( -3.469446951953613696E-16, 0.000000000000000000, -1.000000000000000000 ) ) ;
#44161=FACE_OUTER_BOUND ( 'NONE', #16098, .T. ) ;
#44163=ORIENTED_EDGE ( 'NONE', *, *, #34725, .T. ) ;
#44166=DIRECTION ( 'NONE',  ( 1.734723475976806848E-16, -0.000000000000000000, 1.000000000000000000 ) ) ;
#44168=ORIENTED_EDGE ( 'NONE', *, *, #2840, .F. ) ;
#44169=VECTOR ( 'NONE', #48101, 39.37007874015748143 ) ;
#44170=EDGE_LOOP ( 'NONE', ( #23668, #21518, #32126, #24954 ) ) ;
#44171=CARTESIAN_POINT ( 'NONE',  ( 1.833433833923351353, 0.000000000000000000, 0.9448818897637746295 ) ) ;
#44173=DIRECTION ( 'NONE',  ( -3.469446951953613696E-16, 0.000000000000000000, -1.000000000000000000 ) ) ;
#44174=VECTOR ( 'NONE', #6250, 39.37007874015748143 ) ;
#44176=VECTOR ( 'NONE', #14932, 39.37007874015748143 ) ;
#44178=FACE_OUTER_BOUND ( 'NONE', #47921, .T. ) ;
#44179=ORIENTED_EDGE ( 'NONE', *, *, #45189, .T. ) ;
#44180=LINE ( 'NONE', #29665, #41089 ) ;
#44182=CARTESIAN_POINT ( 'NONE',  ( -1.363819533518803029, 3.267716535433071279, 0.9055118110236167750 ) ) ;
#44183=DIRECTION ( 'NONE',  ( 1.000000000000000000, 0.000000000000000000, -3.469446951953613696E-16 ) ) ;
#44184=LINE ( 'NONE', #24577, #2145 ) ;
#44186=EDGE_CURVE ( 'NONE', #3260, #11420, #46383, .T. ) ;
#44187=ORIENTED_EDGE ( 'NONE', *, *, #9777, .F. ) ;
#44188=ORIENTED_EDGE ( 'NONE', *, *, #564, .F. ) ;
#44190=EDGE_CURVE ( 'NONE', #10246, #19504, #9403, .T. ) ;
#44191=ORIENTED_EDGE ( 'NONE', *, *, #14666, .T. ) ;
#44192=ORIENTED_EDGE ( 'NONE', *, *, #33913, .F. ) ;
#44193=CARTESIAN_POINT ( 'NONE',  ( -0.2727639067037607723, 3.346456692913386100, -0.4724409448818883694 ) ) ;
#44194=CARTESIAN_POINT ( 'NONE',  ( -1.363819533518803029, 3.267716535433071279, 2.365849761790804994E-16 ) ) ;
#44197=ORIENTED_EDGE ( 'NONE', *, *, #9558, .T. ) ;
#44198=CARTESIAN_POINT ( 'NONE',  ( -2.001301579076982584, 3.346456692913386100, -0.8267716535433052849 ) ) ;
#44199=CARTESIAN_POINT ( 'NONE',  ( -1.712496953225537633, 3.267716535433071279, -1.102362204724405492 ) ) ;
#44200=CARTESIAN_POINT ( 'NONE',  ( 1.015142113812069313, 3.346456692913386100, -0.03937007874015881204 ) ) ;
#44203=LINE ( 'NONE', #47535, #44674 ) ;
#44204=CARTESIAN_POINT ( 'NONE',  ( 0.7423782071083085965, 3.346456692913386100, -1.141732283464564013 ) ) ;
#44205=VECTOR ( 'NONE', #6640, 39.37007874015748143 ) ;
#44206=ORIENTED_EDGE ( 'NONE', *, *, #5220, .T. ) ;
#44209=ORIENTED_EDGE ( 'NONE', *, *, #31812, .T. ) ;
#44210=ORIENTED_EDGE ( 'NONE', *, *, #24264, .F. ) ;
#44213=VECTOR ( 'NONE', #12200, 39.37007874015748143 ) ;
#44215=ADVANCED_FACE ( 'NONE', ( #33678 ), #1398, .F. ) ;
#44216=VECTOR ( 'NONE', #24677, 39.37007874015748143 ) ;
#44218=DIRECTION ( 'NONE',  ( -0.000000000000000000, 1.000000000000000000, -0.000000000000000000 ) ) ;
#44219=EDGE_LOOP ( 'NONE', ( #19306, #22511, #15590, #38728 ) ) ;
#44220=ORIENTED_EDGE ( 'NONE', *, *, #10749, .T. ) ;
#44221=VECTOR ( 'NONE', #33996, 39.37007874015748143 ) ;
#44222=EDGE_CURVE ( 'NONE', #42166, #337, #28759, .T. ) ;
#44224=DIRECTION ( 'NONE',  ( -0.000000000000000000, 1.000000000000000000, -0.000000000000000000 ) ) ;
#44225=ORIENTED_EDGE ( 'NONE', *, *, #9348, .F. ) ;
#44226=CARTESIAN_POINT ( 'NONE',  ( 0.000000000000000000, 3.346456692913386100, -2.106299212598425008 ) ) ;
#44228=CARTESIAN_POINT ( 'NONE',  ( 1.636583440222563857, 3.267716535433071279, -0.6299212598425181220 ) ) ;
#44229=DIRECTION ( 'NONE',  ( 1.734723475976806848E-16, 0.000000000000000000, 1.000000000000000000 ) ) ;
#44234=VERTEX_POINT ( 'NONE', #5018 ) ;
#44235=CARTESIAN_POINT ( 'NONE',  ( 1.833433833923351353, 3.267716535433071279, 1.259842519685033135 ) ) ;
#44236=DIRECTION ( 'NONE',  ( -0.000000000000000000, 0.000000000000000000, 1.000000000000000000 ) ) ;
#44238=ORIENTED_EDGE ( 'NONE', *, *, #35117, .T. ) ;
#44239=VECTOR ( 'NONE', #4935, 39.37007874015748143 ) ;
#44240=DIRECTION ( 'NONE',  ( -1.000000000000000000, 0.000000000000000000, 0.000000000000000000 ) ) ;
#44241=PLANE ( 'NONE',  #32444 ) ;
#44243=VECTOR ( 'NONE', #5371, 39.37007874015748143 ) ;
#44244=AXIS2_PLACEMENT_3D ( 'NONE', #44976, #1370, #2135 ) ;
#44245=ORIENTED_EDGE ( 'NONE', *, *, #42683, .F. ) ;
#44247=CARTESIAN_POINT ( 'NONE',  ( -1.166969139818015977, 3.346456692913386100, -0.1574803149606300023 ) ) ;
#44248=ORIENTED_EDGE ( 'NONE', *, *, #33978, .T. ) ;
#44249=LINE ( 'NONE', #4763, #11366 ) ;
#44250=CARTESIAN_POINT ( 'NONE',  ( -0.8182917201112819283, 3.346456692913386100, -0.1574803149606301411 ) ) ;
#44251=FACE_OUTER_BOUND ( 'NONE', #27085, .T. ) ;
#44252=CARTESIAN_POINT ( 'NONE',  ( -1.166969139818015977, 0.000000000000000000, -0.1574803149606300023 ) ) ;
#44254=ORIENTED_EDGE ( 'NONE', *, *, #15303, .T. ) ;
#44255=ORIENTED_EDGE ( 'NONE', *, *, #6068, .T. ) ;
#44256=LINE ( 'NONE', #19987, #37267 ) ;
#44258=ADVANCED_FACE ( 'NONE', ( #17662 ), #25656, .F. ) ;
#44262=CARTESIAN_POINT ( 'NONE',  ( -1.363819533518803473, 3.346456692913386100, 2.047244094488179567 ) ) ;
#44263=EDGE_CURVE ( 'NONE', #17636, #4073, #41162, .T. ) ;
#44264=CARTESIAN_POINT ( 'NONE',  ( 1.287906020515830141, 3.346456692913386100, -8.878505979408855953E-16 ) ) ;
#44265=ORIENTED_EDGE ( 'NONE', *, *, #42619, .T. ) ;
#44267=ADVANCED_FACE ( 'NONE', ( #40403 ), #37547, .F. ) ;
#44269=CARTESIAN_POINT ( 'NONE',  ( 0.5455278134075211005, 0.000000000000000000, -1.141732283464564013 ) ) ;
#44270=DIRECTION ( 'NONE',  ( -3.469446951953613696E-16, 0.000000000000000000, -1.000000000000000000 ) ) ;
#44271=EDGE_CURVE ( 'NONE', #17812, #30118, #5271, .T. ) ;
#44272=ORIENTED_EDGE ( 'NONE', *, *, #17282, .F. ) ;
#44274=FACE_BOUND ( 'NONE', #19485, .T. ) ;
#44276=CARTESIAN_POINT ( 'NONE',  ( -0.8182917201112819283, 3.346456692913386100, -1.417322834645664331 ) ) ;
#44277=VERTEX_POINT ( 'NONE', #36520 ) ;
#44278=ORIENTED_EDGE ( 'NONE', *, *, #17589, .T. ) ;
#44279=CARTESIAN_POINT ( 'NONE',  ( -0.5455278134075208785, 0.000000000000000000, 1.062992125984246083 ) ) ;
#44280=EDGE_CURVE ( 'NONE', #1365, #36460, #48346, .T. ) ;
#44281=VECTOR ( 'NONE', #7359, 39.37007874015748143 ) ;
#44282=VERTEX_POINT ( 'NONE', #9147 ) ;
#44283=ORIENTED_EDGE ( 'NONE', *, *, #48985, .T. ) ;
#44284=LINE ( 'NONE', #20012, #26931 ) ;
#44286=VECTOR ( 'NONE', #35030, 39.37007874015748143 ) ;
#44287=EDGE_CURVE ( 'NONE', #34275, #42801, #1140, .T. ) ;
#44288=CARTESIAN_POINT ( 'NONE',  ( 0.000000000000000000, 3.267716535433071279, -0.3149606299212591165 ) ) ;
#44292=PLANE ( 'NONE',  #22296 ) ;
#44293=CARTESIAN_POINT ( 'NONE',  ( 0.000000000000000000, 3.267716535433071279, -0.1574803149606300023 ) ) ;
#44294=LINE ( 'NONE', #13073, #9708 ) ;
#44295=VERTEX_POINT ( 'NONE', #13791 ) ;
#44298=ADVANCED_FACE ( 'NONE', ( #13282 ), #29013, .F. ) ;
#44300=ORIENTED_EDGE ( 'NONE', *, *, #16986, .T. ) ;
#44301=CARTESIAN_POINT ( 'NONE',  ( 0.5455278134075216556, 0.000000000000000000, 2.007874015748021268 ) ) ;
#44304=PLANE ( 'NONE',  #43584 ) ;
#44305=DIRECTION ( 'NONE',  ( 0.000000000000000000, 0.000000000000000000, -1.000000000000000000 ) ) ;
#44306=CARTESIAN_POINT ( 'NONE',  ( -0.8942052331142547050, 3.267716535433071279, 1.062992125984246083 ) ) ;
#44308=DIRECTION ( 'NONE',  ( -1.000000000000000000, -0.000000000000000000, -0.000000000000000000 ) ) ;
#44309=EDGE_LOOP ( 'NONE', ( #3124, #48479, #17625, #33871 ) ) ;
#44310=FACE_BOUND ( 'NONE', #8850, .T. ) ;
#44311=CARTESIAN_POINT ( 'NONE',  ( -0.2727639067037607723, 0.000000000000000000, -1.102362204724405714 ) ) ;
#44312=LINE ( 'NONE', #24959, #2842 ) ;
#44314=VECTOR ( 'NONE', #43938, 39.37007874015748143 ) ;
#44315=VECTOR ( 'NONE', #46935, 39.37007874015748143 ) ;
#44316=ORIENTED_EDGE ( 'NONE', *, *, #18299, .F. ) ;
#44317=ORIENTED_EDGE ( 'NONE', *, *, #37145, .F. ) ;
#44318=FACE_OUTER_BOUND ( 'NONE', #10606, .T. ) ;
#44320=VECTOR ( 'NONE', #38449, 39.37007874015748143 ) ;
#44323=EDGE_CURVE ( 'NONE', #14478, #33096, #17404, .T. ) ;
#44324=CARTESIAN_POINT ( 'NONE',  ( 0.000000000000000000, 3.267716535433071279, -0.03937007874015936021 ) ) ;
#44327=EDGE_CURVE ( 'NONE', #30813, #38209, #13536, .T. ) ;
#44329=ORIENTED_EDGE ( 'NONE', *, *, #18412, .T. ) ;
#44330=CARTESIAN_POINT ( 'NONE',  ( -0.8182917201112819283, 0.000000000000000000, -2.244094488188968395 ) ) ;
#44331=ORIENTED_EDGE ( 'NONE', *, *, #36343, .T. ) ;
#44333=DIRECTION ( 'NONE',  ( 1.000000000000000000, 0.000000000000000000, -3.469446951953613696E-16 ) ) ;
#44335=ORIENTED_EDGE ( 'NONE', *, *, #41538, .T. ) ;
#44338=DIRECTION ( 'NONE',  ( -1.000000000000000000, 0.000000000000000000, 0.000000000000000000 ) ) ;
#44341=DIRECTION ( 'NONE',  ( 1.734723475976806848E-16, 0.000000000000000000, 1.000000000000000000 ) ) ;
#44343=VECTOR ( 'NONE', #2793, 39.37007874015748143 ) ;
#44345=CARTESIAN_POINT ( 'NONE',  ( -0.8942052331142547050, 3.346456692913386100, 1.574803149606291974 ) ) ;
#44346=VERTEX_POINT ( 'NONE', #15050 ) ;
#44347=CARTESIAN_POINT ( 'NONE',  ( -0.3486774197067340486, 0.000000000000000000, -1.141732283464563791 ) ) ;
#44349=LINE ( 'NONE', #4869, #11752 ) ;
#44352=DIRECTION ( 'NONE',  ( -0.000000000000000000, 0.000000000000000000, 1.000000000000000000 ) ) ;
#44353=ADVANCED_FACE ( 'NONE', ( #26412 ), #45758, .F. ) ;
#44358=ORIENTED_EDGE ( 'NONE', *, *, #15924, .T. ) ;
#44360=EDGE_CURVE ( 'NONE', #30424, #11499, #38053, .T. ) ;
#44361=LINE ( 'NONE', #40251, #34176 ) ;
#44363=ORIENTED_EDGE ( 'NONE', *, *, #25620, .F. ) ;
#44364=DIRECTION ( 'NONE',  ( 1.000000000000000000, -0.000000000000000000, 0.000000000000000000 ) ) ;
#44366=VECTOR ( 'NONE', #49589, 39.37007874015748143 ) ;
#44367=VERTEX_POINT ( 'NONE', #42160 ) ;
#44368=CARTESIAN_POINT ( 'NONE',  ( 0.8182917201112817063, 0.000000000000000000, -2.047244094488181343 ) ) ;
#44370=CARTESIAN_POINT ( 'NONE',  ( 0.000000000000000000, 3.267716535433071279, -1.732283464566922726 ) ) ;
#44373=CARTESIAN_POINT ( 'NONE',  ( 0.000000000000000000, 3.267716535433071279, 1.889763779527550147 ) ) ;
#44377=ORIENTED_EDGE ( 'NONE', *, *, #32887, .F. ) ;
#44378=CARTESIAN_POINT ( 'NONE',  ( 1.287906020515830141, 0.000000000000000000, 0.3149606299212578953 ) ) ;
#44379=EDGE_LOOP ( 'NONE', ( #11824, #23558, #5240, #37042 ) ) ;
#44380=EDGE_CURVE ( 'NONE', #22546, #10739, #49610, .T. ) ;
#44381=DIRECTION ( 'NONE',  ( -1.000000000000000000, -0.000000000000000000, -0.000000000000000000 ) ) ;
#44384=ADVANCED_FACE ( 'NONE', ( #26910 ), #46756, .F. ) ;
#44387=ORIENTED_EDGE ( 'NONE', *, *, #16818, .F. ) ;
#44389=DIRECTION ( 'NONE',  ( 0.000000000000000000, 0.000000000000000000, -1.000000000000000000 ) ) ;
#44390=LINE ( 'NONE', #40016, #35087 ) ;
#44392=VECTOR ( 'NONE', #8199, 39.37007874015748143 ) ;
#44393=DIRECTION ( 'NONE',  ( -1.000000000000000000, 0.000000000000000000, -0.000000000000000000 ) ) ;
#44394=CARTESIAN_POINT ( 'NONE',  ( 1.833433833923351353, 3.346456692913386100, 0.9448818897637746295 ) ) ;
#44395=ORIENTED_EDGE ( 'NONE', *, *, #104, .F. ) ;
#44398=DIRECTION ( 'NONE',  ( 1.734723475976806848E-16, -0.000000000000000000, 1.000000000000000000 ) ) ;
#44399=ORIENTED_EDGE ( 'NONE', *, *, #5156, .T. ) ;
#44400=ORIENTED_EDGE ( 'NONE', *, *, #25935, .T. ) ;
#44401=VECTOR ( 'NONE', #14657, 39.37007874015748143 ) ;
#44402=ORIENTED_EDGE ( 'NONE', *, *, #31943, .T. ) ;
#44404=DIRECTION ( 'NONE',  ( 1.734723475976806848E-16, 0.000000000000000000, 1.000000000000000000 ) ) ;
#44405=AXIS2_PLACEMENT_3D ( 'NONE', #23394, #22896, #31153 ) ;
#44406=FACE_OUTER_BOUND ( 'NONE', #15487, .T. ) ;
#44407=CARTESIAN_POINT ( 'NONE',  ( -0.6214413264104939882, 0.000000000000000000, 1.732283464566921172 ) ) ;
#44408=VERTEX_POINT ( 'NONE', #14287 ) ;
#44409=ORIENTED_EDGE ( 'NONE', *, *, #35942, .F. ) ;
#44410=DIRECTION ( 'NONE',  ( 1.734723475976806848E-16, 0.000000000000000000, 1.000000000000000000 ) ) ;
#44411=LINE ( 'NONE', #9311, #45225 ) ;
#44415=CARTESIAN_POINT ( 'NONE',  ( -0.07591351300297362326, 3.346456692913386100, -2.104930761696520491 ) ) ;
#44416=EDGE_CURVE ( 'NONE', #28119, #50243, #30039, .T. ) ;
#44420=DIRECTION ( 'NONE',  ( 1.000000000000000000, 0.000000000000000000, -3.469446951953613696E-16 ) ) ;
#44421=EDGE_CURVE ( 'NONE', #15323, #1336, #50606, .T. ) ;
#44422=ORIENTED_EDGE ( 'NONE', *, *, #37893, .T. ) ;
#44424=LINE ( 'NONE', #33347, #40908 ) ;
#44425=EDGE_LOOP ( 'NONE', ( #14661, #42244, #20296, #8860 ) ) ;
#44426=ORIENTED_EDGE ( 'NONE', *, *, #3360, .F. ) ;
#44427=CIRCLE ( 'NONE', #4051, 2.165354330708661568 ) ;
#44430=FACE_OUTER_BOUND ( 'NONE', #46772, .T. ) ;
#44431=EDGE_LOOP ( 'NONE', ( #32844, #14820, #50882, #48982 ) ) ;
#44433=VERTEX_POINT ( 'NONE', #50360 ) ;
#44434=CARTESIAN_POINT ( 'NONE',  ( 1.636583440222563857, 3.346456692913386100, 1.417869535855831975 ) ) ;
#44435=EDGE_CURVE ( 'NONE', #39739, #44754, #41913, .T. ) ;
#44436=VERTEX_POINT ( 'NONE', #49859 ) ;
#44437=VECTOR ( 'NONE', #41903, 39.37007874015748143 ) ;
#44438=ORIENTED_EDGE ( 'NONE', *, *, #9136, .F. ) ;
#44440=ADVANCED_FACE ( 'NONE', ( #30798 ), #6797, .F. ) ;
#44441=CARTESIAN_POINT ( 'NONE',  ( -1.091055626815042645, 0.000000000000000000, -1.456692913385822186 ) ) ;
#44442=EDGE_CURVE ( 'NONE', #34963, #10110, #42410, .T. ) ;
#44443=EDGE_LOOP ( 'NONE', ( #15479, #35288, #624, #32988 ) ) ;
#44444=VERTEX_POINT ( 'NONE', #2926 ) ;
#44445=ORIENTED_EDGE ( 'NONE', *, *, #19706, .F. ) ;
#44446=LINE ( 'NONE', #21472, #50996 ) ;
#44447=EDGE_CURVE ( 'NONE', #44656, #3958, #37800, .T. ) ;
#44449=ORIENTED_EDGE ( 'NONE', *, *, #47394, .T. ) ;
#44450=FACE_OUTER_BOUND ( 'NONE', #26895, .T. ) ;
#44451=LINE ( 'NONE', #33115, #26090 ) ;
#44452=CARTESIAN_POINT ( 'NONE',  ( -0.5455278134075208785, 3.346456692913386100, 0.6299212598425164567 ) ) ;
#44454=ORIENTED_EDGE ( 'NONE', *, *, #14073, .T. ) ;
#44455=DIRECTION ( 'NONE',  ( -0.000000000000000000, 1.000000000000000000, -0.000000000000000000 ) ) ;
#44456=DIRECTION ( 'NONE',  ( -3.469446951953613696E-16, 0.000000000000000000, -1.000000000000000000 ) ) ;
#44457=AXIS2_PLACEMENT_3D ( 'NONE', #11939, #27674, #43673 ) ;
#44458=CARTESIAN_POINT ( 'NONE',  ( 0.000000000000000000, 3.267716535433071279, -1.456692913385822630 ) ) ;
#44459=EDGE_LOOP ( 'NONE', ( #147, #20322, #29042, #7809 ) ) ;
#44460=DIRECTION ( 'NONE',  ( 1.000000000000000000, -0.000000000000000000, 0.000000000000000000 ) ) ;
#44461=DIRECTION ( 'NONE',  ( -0.000000000000000000, 1.000000000000000000, -0.000000000000000000 ) ) ;
#44463=ORIENTED_EDGE ( 'NONE', *, *, #10693, .F. ) ;
#44464=EDGE_LOOP ( 'NONE', ( #28532, #7423, #12057, #29259 ) ) ;
#44465=LINE ( 'NONE', #47796, #15539 ) ;
#44468=LINE ( 'NONE', #33130, #38518 ) ;
#44469=DIRECTION ( 'NONE',  ( -1.000000000000000000, -0.000000000000000000, -0.000000000000000000 ) ) ;
#44470=VECTOR ( 'NONE', #12499, 39.37007874015748143 ) ;
#44471=ORIENTED_EDGE ( 'NONE', *, *, #44080, .T. ) ;
#44474=VECTOR ( 'NONE', #21024, 39.37007874015748143 ) ;
#44476=CARTESIAN_POINT ( 'NONE',  ( 1.363819533518803251, 3.267716535433071279, -2.365849761790805487E-16 ) ) ;
#44477=PLANE ( 'NONE',  #24277 ) ;
#44478=LINE ( 'NONE', #48576, #39875 ) ;
#44480=DIRECTION ( 'NONE',  ( -0.000000000000000000, 0.000000000000000000, 1.000000000000000000 ) ) ;
#44482=EDGE_LOOP ( 'NONE', ( #4849, #8536, #26485, #45583 ) ) ;
#44483=EDGE_CURVE ( 'NONE', #14063, #19810, #31305, .T. ) ;
#44484=DIRECTION ( 'NONE',  ( 1.734723475976806848E-16, -0.000000000000000000, 1.000000000000000000 ) ) ;
#44485=DIRECTION ( 'NONE',  ( -0.000000000000000000, 1.000000000000000000, -0.000000000000000000 ) ) ;
#44490=DIRECTION ( 'NONE',  ( -0.000000000000000000, 1.000000000000000000, -0.000000000000000000 ) ) ;
#44492=ORIENTED_EDGE ( 'NONE', *, *, #44124, .F. ) ;
#44494=LINE ( 'NONE', #9137, #20934 ) ;
#44495=ORIENTED_EDGE ( 'NONE', *, *, #32270, .F. ) ;
#44496=CARTESIAN_POINT ( 'NONE',  ( 0.000000000000000000, 3.267716535433071279, 0.4724409448818871482 ) ) ;
#44497=LINE ( 'NONE', #32654, #35294 ) ;
#44498=ORIENTED_EDGE ( 'NONE', *, *, #48742, .F. ) ;
#44499=CARTESIAN_POINT ( 'NONE',  ( 0.000000000000000000, 3.346456692913386100, 0.000000000000000000 ) ) ;
#44500=VECTOR ( 'NONE', #42508, 39.37007874015748143 ) ;
#44501=DIRECTION ( 'NONE',  ( 1.000000000000000000, 0.000000000000000000, 0.000000000000000000 ) ) ;
#44502=ADVANCED_FACE ( 'NONE', ( #39043 ), #46998, .F. ) ;
#44503=CARTESIAN_POINT ( 'NONE',  ( -0.2727639067037608278, 0.000000000000000000, -0.3543307086614175816 ) ) ;
#44504=CARTESIAN_POINT ( 'NONE',  ( 0.000000000000000000, 3.267716535433071279, 0.000000000000000000 ) ) ;
#44506=ORIENTED_EDGE ( 'NONE', *, *, #33623, .F. ) ;
#44507=ORIENTED_EDGE ( 'NONE', *, *, #18329, .F. ) ;
#44508=LINE ( 'NONE', #9152, #41348 ) ;
#44509=DIRECTION ( 'NONE',  ( -0.000000000000000000, 1.000000000000000000, -0.000000000000000000 ) ) ;
#44511=ORIENTED_EDGE ( 'NONE', *, *, #48589, .T. ) ;
#44512=LINE ( 'NONE', #28252, #32519 ) ;
#44513=DIRECTION ( 'NONE',  ( -1.000000000000000000, 0.000000000000000000, 1.734723475976806848E-16 ) ) ;
#44514=CIRCLE ( 'NONE', #7411, 2.106299212598425008 ) ;
#44517=VERTEX_POINT ( 'NONE', #27414 ) ;
#44518=ORIENTED_EDGE ( 'NONE', *, *, #39709, .T. ) ;
#44519=PLANE ( 'NONE',  #20483 ) ;
#44520=LINE ( 'NONE', #31906, #26631 ) ;
#44523=PLANE ( 'NONE',  #30656 ) ;
#44524=FACE_BOUND ( 'NONE', #9264, .T. ) ;
#44530=ORIENTED_EDGE ( 'NONE', *, *, #38808, .T. ) ;
#44537=VECTOR ( 'NONE', #33129, 39.37007874015748143 ) ;
#44538=DIRECTION ( 'NONE',  ( -0.000000000000000000, 0.000000000000000000, 1.000000000000000000 ) ) ;
#44541=LINE ( 'NONE', #4551, #16288 ) ;
#44543=EDGE_CURVE ( 'NONE', #29386, #40287, #16060, .T. ) ;
#44544=CARTESIAN_POINT ( 'NONE',  ( 1.091055626815042645, 0.000000000000000000, 1.259842519685033357 ) ) ;
#44546=LINE ( 'NONE', #45298, #1756 ) ;
#44547=ADVANCED_FACE ( 'NONE', ( #35432 ), #49, .F. ) ;
#44549=FACE_OUTER_BOUND ( 'NONE', #6983, .T. ) ;
#44551=ORIENTED_EDGE ( 'NONE', *, *, #5451, .F. ) ;
#44552=LINE ( 'NONE', #12823, #27885 ) ;
#44553=FACE_OUTER_BOUND ( 'NONE', #4344, .T. ) ;
#44555=EDGE_LOOP ( 'NONE', ( #32191, #24464, #37855, #16720 ) ) ;
#44557=ORIENTED_EDGE ( 'NONE', *, *, #46001, .F. ) ;
#44558=FACE_BOUND ( 'NONE', #8041, .T. ) ;
#44559=DIRECTION ( 'NONE',  ( -3.469446951953613696E-16, 0.000000000000000000, -1.000000000000000000 ) ) ;
#44562=DIRECTION ( 'NONE',  ( -1.000000000000000000, 0.000000000000000000, 0.000000000000000000 ) ) ;
#44563=ORIENTED_EDGE ( 'NONE', *, *, #42791, .F. ) ;
#44564=EDGE_LOOP ( 'NONE', ( #10724, #22233, #41070, #11645 ) ) ;
#44565=DIRECTION ( 'NONE',  ( -3.469446951953613696E-16, 0.000000000000000000, -1.000000000000000000 ) ) ;
#44566=EDGE_LOOP ( 'NONE', ( #32275, #18892, #5076, #42611 ) ) ;
#44568=LINE ( 'NONE', #5344, #43356 ) ;
#44569=VERTEX_POINT ( 'NONE', #15796 ) ;
#44571=CARTESIAN_POINT ( 'NONE',  ( -1.636583440222563635, 0.000000000000000000, 1.259842519685033357 ) ) ;
#44572=VECTOR ( 'NONE', #28051, 39.37007874015748143 ) ;
#44573=EDGE_LOOP ( 'NONE', ( #2559, #26509, #15692, #49129 ) ) ;
#44574=LINE ( 'NONE', #8713, #33222 ) ;
#44577=FACE_OUTER_BOUND ( 'NONE', #26171, .T. ) ;
#44578=ORIENTED_EDGE ( 'NONE', *, *, #34174, .F. ) ;
#44580=ORIENTED_EDGE ( 'NONE', *, *, #8718, .T. ) ;
#44581=EDGE_CURVE ( 'NONE', #30461, #11143, #31820, .T. ) ;
#44582=ORIENTED_EDGE ( 'NONE', *, *, #48477, .T. ) ;
#44583=EDGE_LOOP ( 'NONE', ( #5199, #20, #7277, #42937 ) ) ;
#44584=CARTESIAN_POINT ( 'NONE',  ( -0.2727639067037608278, 0.000000000000000000, 0.2755905511810995412 ) ) ;
#44585=CARTESIAN_POINT ( 'NONE',  ( 0.000000000000000000, 3.267716535433071279, -0.9448818897637762948 ) ) ;
#44586=ORIENTED_EDGE ( 'NONE', *, *, #761, .F. ) ;
#44588=VERTEX_POINT ( 'NONE', #12186 ) ;
#44589=LINE ( 'NONE', #23964, #35967 ) ;
#44592=CARTESIAN_POINT ( 'NONE',  ( 0.000000000000000000, 3.267716535433071279, -1.161035397307311917E-15 ) ) ;
#44593=CARTESIAN_POINT ( 'NONE',  ( -0.5455278134075208785, 0.000000000000000000, 1.889763779527550369 ) ) ;
#44595=LINE ( 'NONE', #29118, #23321 ) ;
#44596=DIRECTION ( 'NONE',  ( 1.000000000000000000, 0.000000000000000000, 0.000000000000000000 ) ) ;
#44597=LINE ( 'NONE', #31993, #15747 ) ;
#44598=EDGE_CURVE ( 'NONE', #31898, #13220, #12347, .T. ) ;
#44599=VECTOR ( 'NONE', #4873, 39.37007874015748143 ) ;
#44600=VECTOR ( 'NONE', #1341, 39.37007874015748143 ) ;
#44604=DIRECTION ( 'NONE',  ( 1.000000000000000000, 0.000000000000000000, 0.000000000000000000 ) ) ;
#44607=EDGE_LOOP ( 'NONE', ( #24601, #15730, #40004, #36158 ) ) ;
#44608=LINE ( 'NONE', #37148, #10255 ) ;
#44610=ORIENTED_EDGE ( 'NONE', *, *, #26274, .T. ) ;
#44611=DIRECTION ( 'NONE',  ( 1.000000000000000000, 0.000000000000000000, 0.000000000000000000 ) ) ;
#44612=CARTESIAN_POINT ( 'NONE',  ( 0.5455278134075212115, 0.000000000000000000, 0.6299212598425161236 ) ) ;
#44614=CARTESIAN_POINT ( 'NONE',  ( 0.5455278134075212115, 3.346456692913386100, 0.3149606299212576177 ) ) ;
#44615=CARTESIAN_POINT ( 'NONE',  ( -2.182111253630085734, 0.000000000000000000, -0.8267716535433052849 ) ) ;
#44616=EDGE_CURVE ( 'NONE', #11168, #25127, #27666, .T. ) ;
#44618=VERTEX_POINT ( 'NONE', #19915 ) ;
#44620=FACE_BOUND ( 'NONE', #6793, .T. ) ;
#44622=PLANE ( 'NONE',  #48487 ) ;
#44623=ORIENTED_EDGE ( 'NONE', *, *, #42116, .F. ) ;
#44624=CARTESIAN_POINT ( 'NONE',  ( 1.636583440222563857, 3.346456692913386100, -0.5118110236220471121 ) ) ;
#44625=CARTESIAN_POINT ( 'NONE',  ( -1.363819533518803029, 0.000000000000000000, 0.2755905511810996522 ) ) ;
#44628=DIRECTION ( 'NONE',  ( 0.000000000000000000, 0.000000000000000000, -1.000000000000000000 ) ) ;
#44632=LINE ( 'NONE', #5413, #35885 ) ;
#44634=FACE_BOUND ( 'NONE', #25961, .T. ) ;
#44635=EDGE_LOOP ( 'NONE', ( #48203, #37795, #38578, #40672 ) ) ;
#44636=ADVANCED_FACE ( 'NONE', ( #8311 ), #12960, .F. ) ;
#44637=VECTOR ( 'NONE', #18469, 39.37007874015748143 ) ;
#44638=VECTOR ( 'NONE', #1163, 39.37007874015748143 ) ;
#44639=CARTESIAN_POINT ( 'NONE',  ( -0.6214413264104945434, 3.267716535433071279, -1.732283464566922726 ) ) ;
#44640=CARTESIAN_POINT ( 'NONE',  ( -1.053808008129011320, 3.267716535433071279, 2.204724409448808764 ) ) ;
#44641=ORIENTED_EDGE ( 'NONE', *, *, #21549, .T. ) ;
#44642=DIRECTION ( 'NONE',  ( -1.000000000000000000, 0.000000000000000000, 0.000000000000000000 ) ) ;
#44643=VECTOR ( 'NONE', #46825, 39.37007874015748143 ) ;
#44644=CARTESIAN_POINT ( 'NONE',  ( -0.8182917201112819283, 0.000000000000000000, 2.047244094488179567 ) ) ;
#44645=EDGE_CURVE ( 'NONE', #25916, #25164, #28853, .T. ) ;
#44646=EDGE_LOOP ( 'NONE', ( #23790, #24767, #15636, #154 ) ) ;
#44647=ORIENTED_EDGE ( 'NONE', *, *, #7946, .T. ) ;
#44649=ORIENTED_EDGE ( 'NONE', *, *, #9634, .T. ) ;
#44650=EDGE_CURVE ( 'NONE', #4308, #41410, #36457, .T. ) ;
#44651=CARTESIAN_POINT ( 'NONE',  ( 1.636583440222563857, 3.267716535433071279, -2.839019714148966584E-16 ) ) ;
#44652=VECTOR ( 'NONE', #9899, 39.37007874015748143 ) ;
#44653=DIRECTION ( 'NONE',  ( -3.469446951953613696E-16, 0.000000000000000000, -1.000000000000000000 ) ) ;
#44656=VERTEX_POINT ( 'NONE', #41344 ) ;
#44657=ORIENTED_EDGE ( 'NONE', *, *, #41925, .T. ) ;
#44658=CARTESIAN_POINT ( 'NONE',  ( -1.636583440222563635, 3.346456692913386100, 0.3149606299212578953 ) ) ;
#44659=FACE_OUTER_BOUND ( 'NONE', #30879, .T. ) ;
#44660=DIRECTION ( 'NONE',  ( 1.734723475976806848E-16, 0.000000000000000000, 1.000000000000000000 ) ) ;
#44662=CARTESIAN_POINT ( 'NONE',  ( -1.712496953225537188, 3.267716535433071279, 0.5905511811023582691 ) ) ;
#44663=EDGE_CURVE ( 'NONE', #19974, #50372, #21727, .T. ) ;
#44664=DIRECTION ( 'NONE',  ( 1.734723475976806848E-16, -0.000000000000000000, 1.000000000000000000 ) ) ;
#44665=EDGE_CURVE ( 'NONE', #2713, #26706, #40836, .T. ) ;
#44666=EDGE_CURVE ( 'NONE', #18530, #924, #24830, .T. ) ;
#44668=VERTEX_POINT ( 'NONE', #44684 ) ;
#44670=LINE ( 'NONE', #9321, #25239 ) ;
#44671=ORIENTED_EDGE ( 'NONE', *, *, #36085, .F. ) ;
#44672=ORIENTED_EDGE ( 'NONE', *, *, #42591, .F. ) ;
#44673=DIRECTION ( 'NONE',  ( 0.000000000000000000, -1.000000000000000000, 0.000000000000000000 ) ) ;
#44674=VECTOR ( 'NONE', #44460, 39.37007874015748143 ) ;
#44675=CARTESIAN_POINT ( 'NONE',  ( 0.5455278134075217666, 3.346456692913386100, 2.034427629037600660 ) ) ;
#44677=AXIS2_PLACEMENT_3D ( 'NONE', #44883, #44628, #11682 ) ;
#44678=ORIENTED_EDGE ( 'NONE', *, *, #38034, .T. ) ;
#44679=CARTESIAN_POINT ( 'NONE',  ( -1.712496953225537188, 3.346456692913386100, 0.4724409448818871482 ) ) ;
#44682=VECTOR ( 'NONE', #43279, 39.37007874015748143 ) ;
#44683=LINE ( 'NONE', #29722, #31766 ) ;
#44684=CARTESIAN_POINT ( 'NONE',  ( 2.182111253630085290, 3.267716535433071279, -0.3149606299212596716 ) ) ;
#44685=EDGE_CURVE ( 'NONE', #24976, #18933, #28947, .T. ) ;
#44686=VERTEX_POINT ( 'NONE', #1073 ) ;
#44688=ORIENTED_EDGE ( 'NONE', *, *, #16757, .F. ) ;
#44689=FACE_OUTER_BOUND ( 'NONE', #49141, .T. ) ;
#44690=ORIENTED_EDGE ( 'NONE', *, *, #27335, .T. ) ;
#44691=ORIENTED_EDGE ( 'NONE', *, *, #13409, .F. ) ;
#44692=DIRECTION ( 'NONE',  ( 1.000000000000000000, -0.000000000000000000, 0.000000000000000000 ) ) ;
#44694=DIRECTION ( 'NONE',  ( 1.734723475976806848E-16, -0.000000000000000000, 1.000000000000000000 ) ) ;
#44695=EDGE_CURVE ( 'NONE', #14934, #17666, #25086, .T. ) ;
#44696=ORIENTED_EDGE ( 'NONE', *, *, #13225, .F. ) ;
#44697=EDGE_CURVE ( 'NONE', #47149, #46941, #45188, .T. ) ;
#44698=LINE ( 'NONE', #25103, #26309 ) ;
#44701=EDGE_CURVE ( 'NONE', #46419, #2713, #25336, .T. ) ;
#44704=DIRECTION ( 'NONE',  ( -0.000000000000000000, 1.000000000000000000, -0.000000000000000000 ) ) ;
#44707=VERTEX_POINT ( 'NONE', #1591 ) ;
#44708=DIRECTION ( 'NONE',  ( 0.000000000000000000, 0.000000000000000000, -1.000000000000000000 ) ) ;
#44709=CARTESIAN_POINT ( 'NONE',  ( -1.091055626815042201, 3.346456692913386100, 0.9448818897637749625 ) ) ;
#44713=EDGE_LOOP ( 'NONE', ( #29875, #4958, #30493, #47629 ) ) ;
#44715=VECTOR ( 'NONE', #31130, 39.37007874015748143 ) ;
#44716=CARTESIAN_POINT ( 'NONE',  ( 1.363819533518803251, 3.267716535433071279, -0.7874015748031473194 ) ) ;
#44717=VECTOR ( 'NONE', #40518, 39.37007874015748143 ) ;
#44719=PLANE ( 'NONE',  #44244 ) ;
#44722=ADVANCED_FACE ( 'NONE', ( #48024 ), #24576, .F. ) ;
#44724=VECTOR ( 'NONE', #1048, 39.37007874015748143 ) ;
#44725=ADVANCED_FACE ( 'NONE', ( #4951 ), #48788, .F. ) ;
#44726=ADVANCED_FACE ( 'NONE', ( #28433 ), #9594, .F. ) ;
#44729=FACE_OUTER_BOUND ( 'NONE', #882, .T. ) ;
#44732=EDGE_CURVE ( 'NONE', #6991, #38732, #16834, .T. ) ;
#44734=DIRECTION ( 'NONE',  ( 1.734723475976806848E-16, -0.000000000000000000, 1.000000000000000000 ) ) ;
#44735=ORIENTED_EDGE ( 'NONE', *, *, #46224, .T. ) ;
#44736=CARTESIAN_POINT ( 'NONE',  ( 2.106197740627112402, 3.346456692913386100, 0.7874015748031456541 ) ) ;
#44737=CARTESIAN_POINT ( 'NONE',  ( 0.5455278134075212115, 3.346456692913386100, -0.6299212598425181220 ) ) ;
#44738=CARTESIAN_POINT ( 'NONE',  ( -2.121605289024800722, 3.346456692913386100, 0.4330708661417290162 ) ) ;
#44739=EDGE_LOOP ( 'NONE', ( #12802, #21930, #38713, #26382 ) ) ;
#44743=ORIENTED_EDGE ( 'NONE', *, *, #22760, .T. ) ;
#44744=CARTESIAN_POINT ( 'NONE',  ( 0.000000000000000000, 3.267716535433071279, 0.000000000000000000 ) ) ;
#44745=CARTESIAN_POINT ( 'NONE',  ( -2.258024766633058622, 3.346456692913386100, -0.03937007874015881204 ) ) ;
#44746=ORIENTED_EDGE ( 'NONE', *, *, #49140, .T. ) ;
#44747=FACE_OUTER_BOUND ( 'NONE', #40949, .T. ) ;
#44749=DIRECTION ( 'NONE',  ( 0.000000000000000000, 0.000000000000000000, -1.000000000000000000 ) ) ;
#44750=PLANE ( 'NONE',  #1257 ) ;
#44751=CARTESIAN_POINT ( 'NONE',  ( 3.927031490892378253E-16, 0.000000000000000000, 2.007874015748021268 ) ) ;
#44752=VECTOR ( 'NONE', #7573, 39.37007874015748143 ) ;
#44753=ORIENTED_EDGE ( 'NONE', *, *, #8929, .F. ) ;
#44754=VERTEX_POINT ( 'NONE', #1846 ) ;
#44755=DIRECTION ( 'NONE',  ( -0.000000000000000000, 1.000000000000000000, -0.000000000000000000 ) ) ;
#44756=DIRECTION ( 'NONE',  ( 0.000000000000000000, 0.000000000000000000, -1.000000000000000000 ) ) ;
#44758=DIRECTION ( 'NONE',  ( -3.469446951953613696E-16, 0.000000000000000000, -1.000000000000000000 ) ) ;
#44759=DIRECTION ( 'NONE',  ( -3.469446951953613696E-16, 0.000000000000000000, -1.000000000000000000 ) ) ;
#44761=AXIS2_PLACEMENT_3D ( 'NONE', #42070, #17815, #37448 ) ;
#44763=VECTOR ( 'NONE', #29955, 39.37007874015748143 ) ;
#44765=EDGE_LOOP ( 'NONE', ( #41142, #14725, #19245, #23503 ) ) ;
#44766=EDGE_CURVE ( 'NONE', #448, #31173, #33357, .T. ) ;
#44769=DIRECTION ( 'NONE',  ( -3.469446951953613696E-16, 0.000000000000000000, -1.000000000000000000 ) ) ;
#44770=ORIENTED_EDGE ( 'NONE', *, *, #41350, .T. ) ;
#44771=LINE ( 'NONE', #36286, #15784 ) ;
#44773=FACE_BOUND ( 'NONE', #28453, .T. ) ;
#44774=VECTOR ( 'NONE', #29834, 39.37007874015748143 ) ;
#44776=DIRECTION ( 'NONE',  ( 1.000000000000000000, 0.000000000000000000, 0.000000000000000000 ) ) ;
#44777=EDGE_LOOP ( 'NONE', ( #23889, #35867, #18281, #14125 ) ) ;
#44779=DIRECTION ( 'NONE',  ( -1.000000000000000000, -0.000000000000000000, -0.000000000000000000 ) ) ;
#44780=ORIENTED_EDGE ( 'NONE', *, *, #32146, .T. ) ;
#44781=FACE_OUTER_BOUND ( 'NONE', #23018, .T. ) ;
#44782=CARTESIAN_POINT ( 'NONE',  ( -0.5455278134075214336, 0.000000000000000000, -0.8267716535433049518 ) ) ;
#44784=EDGE_CURVE ( 'NONE', #42119, #13544, #44514, .T. ) ;
#44786=CARTESIAN_POINT ( 'NONE',  ( 0.8182917201112819283, 0.000000000000000000, 0.9055118110236164419 ) ) ;
#44787=DIRECTION ( 'NONE',  ( -0.000000000000000000, 0.000000000000000000, 1.000000000000000000 ) ) ;
#44788=EDGE_CURVE ( 'NONE', #8152, #12919, #3365, .T. ) ;
#44789=DIRECTION ( 'NONE',  ( 1.734723475976806848E-16, -0.000000000000000000, 1.000000000000000000 ) ) ;
#44790=EDGE_CURVE ( 'NONE', #42413, #25659, #34112, .T. ) ;
#44792=CARTESIAN_POINT ( 'NONE',  ( 0.2727639067037610499, 0.000000000000000000, 2.047244094488179567 ) ) ;
#44795=PLANE ( 'NONE',  #25809 ) ;
#44796=EDGE_CURVE ( 'NONE', #6021, #38746, #37987, .T. ) ;
#44798=LINE ( 'NONE', #10213, #15781 ) ;
#44800=VECTOR ( 'NONE', #46115, 39.37007874015748143 ) ;
#44801=ORIENTED_EDGE ( 'NONE', *, *, #27102, .T. ) ;
#44805=EDGE_LOOP ( 'NONE', ( #49086, #28354, #14421, #40544 ) ) ;
#44807=CARTESIAN_POINT ( 'NONE',  ( -0.8942052331142552601, 3.267716535433071279, -1.259842519685034690 ) ) ;
#44808=LINE ( 'NONE', #45557, #11202 ) ;
#44809=VECTOR ( 'NONE', #26211, 39.37007874015748143 ) ;
#44810=VERTEX_POINT ( 'NONE', #49546 ) ;
#44811=DIRECTION ( 'NONE',  ( -0.000000000000000000, 1.000000000000000000, -0.000000000000000000 ) ) ;
#44813=FACE_BOUND ( 'NONE', #45255, .T. ) ;
#44814=CARTESIAN_POINT ( 'NONE',  ( 0.5455278134075212115, 3.267716535433071279, 0.6299212598425161236 ) ) ;
#44815=DIRECTION ( 'NONE',  ( 1.000000000000000000, 0.000000000000000000, -3.469446951953613696E-16 ) ) ;
#44816=LINE ( 'NONE', #20314, #32598 ) ;
#44819=FACE_OUTER_BOUND ( 'NONE', #20590, .T. ) ;
#44820=ORIENTED_EDGE ( 'NONE', *, *, #12182, .F. ) ;
#44821=LINE ( 'NONE', #25222, #35979 ) ;
#44823=FACE_OUTER_BOUND ( 'NONE', #15108, .T. ) ;
#44824=ORIENTED_EDGE ( 'NONE', *, *, #8200, .T. ) ;
#44826=AXIS2_PLACEMENT_3D ( 'NONE', #18450, #17431, #37573 ) ;
#44827=LINE ( 'NONE', #969, #24009 ) ;
#44828=EDGE_CURVE ( 'NONE', #8308, #38746, #42346, .T. ) ;
#44829=VERTEX_POINT ( 'NONE', #6232 ) ;
#44831=LINE ( 'NONE', #8716, #30662 ) ;
#44833=ORIENTED_EDGE ( 'NONE', *, *, #38648, .F. ) ;
#44834=ORIENTED_EDGE ( 'NONE', *, *, #33139, .T. ) ;
#44835=EDGE_CURVE ( 'NONE', #25675, #721, #13979, .T. ) ;
#44837=VECTOR ( 'NONE', #46735, 39.37007874015748143 ) ;
#44838=VERTEX_POINT ( 'NONE', #14990 ) ;
#44839=ORIENTED_EDGE ( 'NONE', *, *, #9407, .T. ) ;
#44840=CARTESIAN_POINT ( 'NONE',  ( -1.712496953225537188, 3.267716535433071279, 5.941417334598190051E-16 ) ) ;
#44841=VECTOR ( 'NONE', #1057, 39.37007874015748143 ) ;
#44842=ORIENTED_EDGE ( 'NONE', *, *, #22861, .T. ) ;
#44843=LINE ( 'NONE', #9752, #37837 ) ;
#44846=ADVANCED_FACE ( 'NONE', ( #14741 ), #18866, .F. ) ;
#44847=PLANE ( 'NONE',  #22261 ) ;
#44851=ORIENTED_EDGE ( 'NONE', *, *, #4644, .T. ) ;
#44852=LINE ( 'NONE', #27521, #15919 ) ;
#44853=DIRECTION ( 'NONE',  ( 1.734723475976806848E-16, -0.000000000000000000, 1.000000000000000000 ) ) ;
#44854=EDGE_CURVE ( 'NONE', #11368, #34116, #18105, .T. ) ;
#44856=CARTESIAN_POINT ( 'NONE',  ( -1.985260859929297572, 0.000000000000000000, -6.146657985744592735E-16 ) ) ;
#44861=B_SPLINE_CURVE_WITH_KNOTS ( 'NONE', 3,
 ( #37475, #25583, #2092, #17838 ),
 .UNSPECIFIED., .F., .F.,
 ( 4, 4 ),
 ( 0.03694420483709656700, 0.03855293945462513056 ),
 .UNSPECIFIED. ) ;
#44862=ORIENTED_EDGE ( 'NONE', *, *, #11042, .T. ) ;
#44863=LINE ( 'NONE', #3225, #37503 ) ;
#44864=VECTOR ( 'NONE', #17378, 39.37007874015748143 ) ;
#44867=ADVANCED_FACE ( 'NONE', ( #6737 ), #22486, .F. ) ;
#44868=AXIS2_PLACEMENT_3D ( 'NONE', #36903, #12890, #36644 ) ;
#44869=DIRECTION ( 'NONE',  ( 1.000000000000000000, -0.000000000000000000, 0.000000000000000000 ) ) ;
#44871=LINE ( 'NONE', #13396, #8909 ) ;
#44872=CARTESIAN_POINT ( 'NONE',  ( 0.000000000000000000, 3.267716535433071279, 1.062992125984246083 ) ) ;
#44873=LINE ( 'NONE', #44113, #40922 ) ;
#44874=VERTEX_POINT ( 'NONE', #29975 ) ;
#44875=DIRECTION ( 'NONE',  ( 1.000000000000000000, -0.000000000000000000, 0.000000000000000000 ) ) ;
#44876=VECTOR ( 'NONE', #25515, 39.37007874015748143 ) ;
#44877=FACE_BOUND ( 'NONE', #19996, .T. ) ;
#44878=ORIENTED_EDGE ( 'NONE', *, *, #15765, .T. ) ;
#44879=CARTESIAN_POINT ( 'NONE',  ( 2.378961647330872786, 3.243536745096756047, 0.6063129507101621130 ) ) ;
#44881=DIRECTION ( 'NONE',  ( 1.000000000000000000, 0.000000000000000000, -3.469446951953613696E-16 ) ) ;
#44882=PLANE ( 'NONE',  #24772 ) ;
#44883=CARTESIAN_POINT ( 'NONE',  ( -1.909347346926324462, 0.000000000000000000, 0.5905511811023582691 ) ) ;
#44884=DIRECTION ( 'NONE',  ( 1.734723475976806848E-16, -0.000000000000000000, 1.000000000000000000 ) ) ;
#44886=ADVANCED_FACE ( 'NONE', ( #46199 ), #6990, .F. ) ;
#44887=ORIENTED_EDGE ( 'NONE', *, *, #15124, .T. ) ;
#44888=LINE ( 'NONE', #33307, #38370 ) ;
#44889=CARTESIAN_POINT ( 'NONE',  ( 0.000000000000000000, 3.267716535433071279, -0.5118110236220467790 ) ) ;
#44890=FACE_BOUND ( 'NONE', #18906, .T. ) ;
#44891=ORIENTED_EDGE ( 'NONE', *, *, #7842, .F. ) ;
#44892=EDGE_CURVE ( 'NONE', #3654, #5972, #26103, .T. ) ;
#44893=DIRECTION ( 'NONE',  ( -0.000000000000000000, 0.000000000000000000, 1.000000000000000000 ) ) ;
#44895=EDGE_CURVE ( 'NONE', #46251, #6728, #30739, .T. ) ;
#44897=VERTEX_POINT ( 'NONE', #45438 ) ;
#44898=LINE ( 'NONE', #10315, #35659 ) ;
#44899=AXIS2_PLACEMENT_3D ( 'NONE', #24547, #47741, #43387 ) ;
#44900=LINE ( 'NONE', #41813, #40252 ) ;
#44903=ORIENTED_EDGE ( 'NONE', *, *, #49603, .T. ) ;
#44904=AXIS2_PLACEMENT_3D ( 'NONE', #13280, #25655, #44501 ) ;
#44907=DIRECTION ( 'NONE',  ( 1.000000000000000000, 0.000000000000000000, 0.000000000000000000 ) ) ;
#44908=EDGE_CURVE ( 'NONE', #29976, #33624, #10103, .T. ) ;
#44909=DIRECTION ( 'NONE',  ( -1.000000000000000000, -0.000000000000000000, -0.000000000000000000 ) ) ;
#44910=CARTESIAN_POINT ( 'NONE',  ( 1.091055626815043311, 3.346456692913386100, 1.889763779527550369 ) ) ;
#44911=VERTEX_POINT ( 'NONE', #42846 ) ;
#44914=FACE_OUTER_BOUND ( 'NONE', #35084, .T. ) ;
#44917=EDGE_CURVE ( 'NONE', #19997, #23450, #50797, .T. ) ;
#44920=CARTESIAN_POINT ( 'NONE',  ( 0.8182917201112824834, 0.000000000000000000, 1.417322834645662777 ) ) ;
#44922=CARTESIAN_POINT ( 'NONE',  ( -1.363819533518803029, 0.000000000000000000, 1.102362204724404160 ) ) ;
#44923=EDGE_LOOP ( 'NONE', ( #1364, #2790, #22133, #21243 ) ) ;
#44924=CARTESIAN_POINT ( 'NONE',  ( -0.2727639067037611054, 3.267716535433071279, -2.088563196121306476 ) ) ;
#44927=ADVANCED_FACE ( 'NONE', ( #39749 ), #7995, .F. ) ;
#44928=ORIENTED_EDGE ( 'NONE', *, *, #27968, .F. ) ;
#44929=CARTESIAN_POINT ( 'NONE',  ( 1.997134316236881091, 3.346456692913386100, -0.6692913385826764205 ) ) ;
#44930=CARTESIAN_POINT ( 'NONE',  ( -0.6214413264104939882, 0.000000000000000000, 0.4724409448818872592 ) ) ;
#44932=VECTOR ( 'NONE', #4295, 39.37007874015748143 ) ;
#44933=VECTOR ( 'NONE', #690, 39.37007874015748143 ) ;
#44934=EDGE_CURVE ( 'NONE', #17812, #32722, #31755, .T. ) ;
#44935=ORIENTED_EDGE ( 'NONE', *, *, #23698, .F. ) ;
#44936=VECTOR ( 'NONE', #44102, 39.37007874015748143 ) ;
#44937=PLANE ( 'NONE',  #15506 ) ;
#44938=VECTOR ( 'NONE', #46698, 39.37007874015748143 ) ;
#44939=ORIENTED_EDGE ( 'NONE', *, *, #49451, .F. ) ;
#44940=EDGE_CURVE ( 'NONE', #3623, #7160, #31249, .T. ) ;
#44942=DIRECTION ( 'NONE',  ( 0.000000000000000000, -1.000000000000000000, 0.000000000000000000 ) ) ;
#44943=ORIENTED_EDGE ( 'NONE', *, *, #6694, .T. ) ;
#44944=ORIENTED_EDGE ( 'NONE', *, *, #47434, .T. ) ;
#44945=VERTEX_POINT ( 'NONE', #35375 ) ;
#44946=VECTOR ( 'NONE', #46820, 39.37007874015748143 ) ;
#44948=ORIENTED_EDGE ( 'NONE', *, *, #6912, .T. ) ;
#44949=ORIENTED_EDGE ( 'NONE', *, *, #24929, .T. ) ;
#44950=LINE ( 'NONE', #10111, #27285 ) ;
#44952=CARTESIAN_POINT ( 'NONE',  ( 1.091055626815042423, 0.000000000000000000, -1.574803149606294417 ) ) ;
#44954=EDGE_LOOP ( 'NONE', ( #30317, #47292, #12331, #34495 ) ) ;
#44955=FACE_OUTER_BOUND ( 'NONE', #15040, .T. ) ;
#44957=LINE ( 'NONE', #9351, #30801 ) ;
#44960=ORIENTED_EDGE ( 'NONE', *, *, #9271, .T. ) ;
#44961=CARTESIAN_POINT ( 'NONE',  ( 0.7423782071083091516, 3.346456692913386100, 1.062992125984246083 ) ) ;
#44963=DIRECTION ( 'NONE',  ( -0.000000000000000000, 1.000000000000000000, -0.000000000000000000 ) ) ;
#44964=VERTEX_POINT ( 'NONE', #3620 ) ;
#44965=ORIENTED_EDGE ( 'NONE', *, *, #10962, .T. ) ;
#44970=ORIENTED_EDGE ( 'NONE', *, *, #9108, .T. ) ;
#44971=ORIENTED_EDGE ( 'NONE', *, *, #39375, .T. ) ;
#44972=VECTOR ( 'NONE', #44166, 39.37007874015748143 ) ;
#44974=CARTESIAN_POINT ( 'NONE',  ( -0.8942052331142552601, 3.346456692913386100, -7.512581982576723358E-16 ) ) ;
#44975=VERTEX_POINT ( 'NONE', #19350 ) ;
#44976=CARTESIAN_POINT ( 'NONE',  ( -2.182111253630085290, 0.000000000000000000, 0.3149606299212578953 ) ) ;
#44977=CARTESIAN_POINT ( 'NONE',  ( 0.8182917201112822614, 3.267716535433071279, -1.419509857074483785E-16 ) ) ;
#44978=VECTOR ( 'NONE', #16255, 39.37007874015748143 ) ;
#44980=EDGE_CURVE ( 'NONE', #43175, #39048, #46943, .T. ) ;
#44981=DIRECTION ( 'NONE',  ( -0.000000000000000000, 0.000000000000000000, 1.000000000000000000 ) ) ;
#44982=LINE ( 'NONE', #17634, #7941 ) ;
#44983=CARTESIAN_POINT ( 'NONE',  ( 0.4696143004045484903, 3.346456692913386100, 2.047244094488179567 ) ) ;
#44987=CARTESIAN_POINT ( 'NONE',  ( 0.8182917201112824834, 3.346456692913386100, 1.220472440944875281 ) ) ;
#44988=CARTESIAN_POINT ( 'NONE',  ( -1.716666360678977155, 3.346456692913386100, 1.220472440944875059 ) ) ;
#44990=ORIENTED_EDGE ( 'NONE', *, *, #24776, .T. ) ;
#44992=EDGE_CURVE ( 'NONE', #36525, #36526, #27352, .T. ) ;
#44994=DIRECTION ( 'NONE',  ( -0.000000000000000000, 1.000000000000000000, -0.000000000000000000 ) ) ;
#44996=EDGE_CURVE ( 'NONE', #17115, #3832, #7741, .T. ) ;
#44999=EDGE_CURVE ( 'NONE', #29935, #30018, #23482, .T. ) ;
#45000=VERTEX_POINT ( 'NONE', #51051 ) ;
#45004=DIRECTION ( 'NONE',  ( 1.734723475976806848E-16, 0.000000000000000000, 1.000000000000000000 ) ) ;
#45009=FACE_OUTER_BOUND ( 'NONE', #417, .T. ) ;
#45012=CARTESIAN_POINT ( 'NONE',  ( -0.5455278134075214336, 3.346456692913386100, -1.456692913385822630 ) ) ;
#45013=CIRCLE ( 'NONE', #36780, 2.106299212598425008 ) ;
#45014=FACE_OUTER_BOUND ( 'NONE', #39475, .T. ) ;
#45016=ORIENTED_EDGE ( 'NONE', *, *, #48835, .T. ) ;
#45017=DIRECTION ( 'NONE',  ( 1.000000000000000000, 0.000000000000000000, -3.469446951953613696E-16 ) ) ;
#45019=DIRECTION ( 'NONE',  ( -0.000000000000000000, 1.000000000000000000, -0.000000000000000000 ) ) ;
#45020=CIRCLE ( 'NONE', #3828, 2.443628662382284489 ) ;
#45023=ORIENTED_EDGE ( 'NONE', *, *, #11633, .F. ) ;
#45024=CARTESIAN_POINT ( 'NONE',  ( -0.07591351300297277671, 3.346456692913386100, 1.417322834645662777 ) ) ;
#45025=VECTOR ( 'NONE', #44461, 39.37007874015748143 ) ;
#45029=DIRECTION ( 'NONE',  ( -1.000000000000000000, -0.000000000000000000, -0.000000000000000000 ) ) ;
#45030=FACE_BOUND ( 'NONE', #39198, .T. ) ;
#45031=VECTOR ( 'NONE', #31901, 39.37007874015748143 ) ;
#45033=CARTESIAN_POINT ( 'NONE',  ( -1.712496953225537188, 0.000000000000000000, 0.2755905511810996522 ) ) ;
#45036=CARTESIAN_POINT ( 'NONE',  ( 2.378961647330872786, 0.000000000000000000, -0.3149606299212596716 ) ) ;
#45037=ORIENTED_EDGE ( 'NONE', *, *, #10814, .F. ) ;
#45038=DIRECTION ( 'NONE',  ( -0.000000000000000000, 0.000000000000000000, 1.000000000000000000 ) ) ;
#45039=LINE ( 'NONE', #6832, #38697 ) ;
#45040=VERTEX_POINT ( 'NONE', #28116 ) ;
#45041=LINE ( 'NONE', #25951, #5486 ) ;
#45042=LINE ( 'NONE', #9950, #23454 ) ;
#45043=VECTOR ( 'NONE', #22904, 39.37007874015748143 ) ;
#45044=DIRECTION ( 'NONE',  ( 1.000000000000000000, 0.000000000000000000, 0.000000000000000000 ) ) ;
#45045=DIRECTION ( 'NONE',  ( -0.000000000000000000, 1.000000000000000000, -0.000000000000000000 ) ) ;
#45047=CIRCLE ( 'NONE', #7111, 2.106299212598425008 ) ;
#45048=ORIENTED_EDGE ( 'NONE', *, *, #25228, .F. ) ;
#45049=CARTESIAN_POINT ( 'NONE',  ( 1.636583440222563857, 0.000000000000000000, 1.574803149606291974 ) ) ;
#45050=VECTOR ( 'NONE', #39594, 39.37007874015748143 ) ;
#45051=CARTESIAN_POINT ( 'NONE',  ( -1.909347346926324462, 3.267716535433071279, 0.2755905511810996522 ) ) ;
#45052=ORIENTED_EDGE ( 'NONE', *, *, #4538, .T. ) ;
#45053=CARTESIAN_POINT ( 'NONE',  ( -0.6214413264104945434, 0.000000000000000000, -0.7874015748031467643 ) ) ;
#45054=EDGE_CURVE ( 'NONE', #27411, #45218, #43861, .T. ) ;
#45056=ORIENTED_EDGE ( 'NONE', *, *, #16531, .T. ) ;
#45058=VECTOR ( 'NONE', #45534, 39.37007874015748143 ) ;
#45059=EDGE_CURVE ( 'NONE', #34396, #19510, #30989, .T. ) ;
#45061=EDGE_CURVE ( 'NONE', #12747, #37485, #36395, .T. ) ;
#45062=CARTESIAN_POINT ( 'NONE',  ( 1.287906020515829919, 3.267716535433071279, -4.468321617281354090E-16 ) ) ;
#45064=LINE ( 'NONE', #5330, #30706 ) ;
#45065=ORIENTED_EDGE ( 'NONE', *, *, #18268, .F. ) ;
#45066=FACE_BOUND ( 'NONE', #47410, .T. ) ;
#45068=DIRECTION ( 'NONE',  ( -0.000000000000000000, 0.000000000000000000, 1.000000000000000000 ) ) ;
#45072=CARTESIAN_POINT ( 'NONE',  ( 0.5455278134075208785, 3.267716535433071279, -1.574803149606293529 ) ) ;
#45073=ORIENTED_EDGE ( 'NONE', *, *, #47536, .F. ) ;
#45075=FACE_OUTER_BOUND ( 'NONE', #2896, .T. ) ;
#45077=CARTESIAN_POINT ( 'NONE',  ( 0.000000000000000000, 3.346456692913386100, 0.000000000000000000 ) ) ;
#45078=ADVANCED_FACE ( 'NONE', ( #1277 ), #44882, .F. ) ;
#45079=ORIENTED_EDGE ( 'NONE', *, *, #49907, .F. ) ;
#45080=DIRECTION ( 'NONE',  ( -0.000000000000000000, 1.000000000000000000, -0.000000000000000000 ) ) ;
#45081=AXIS2_PLACEMENT_3D ( 'NONE', #6349, #26217, #2478 ) ;
#45082=ADVANCED_FACE ( 'NONE', ( #5403 ), #770, .F. ) ;
#45084=VECTOR ( 'NONE', #38467, 39.37007874015748143 ) ;
#45086=EDGE_CURVE ( 'NONE', #9369, #20825, #12903, .T. ) ;
#45088=EDGE_LOOP ( 'NONE', ( #7829, #29491, #49741, #21729 ) ) ;
#45090=VECTOR ( 'NONE', #11708, 39.37007874015748143 ) ;
#45091=EDGE_LOOP ( 'NONE', ( #44688, #41489, #35326, #18790 ) ) ;
#45092=ORIENTED_EDGE ( 'NONE', *, *, #15041, .T. ) ;
#45093=DIRECTION ( 'NONE',  ( 0.000000000000000000, 1.000000000000000000, 0.000000000000000000 ) ) ;
#45095=CARTESIAN_POINT ( 'NONE',  ( 0.4696143004045476577, 3.267716535433071279, -1.732283464566922726 ) ) ;
#45096=FACE_OUTER_BOUND ( 'NONE', #9008, .T. ) ;
#45097=LINE ( 'NONE', #5368, #32181 ) ;
#45098=EDGE_LOOP ( 'NONE', ( #13902, #40366, #31959, #18317 ) ) ;
#45100=LINE ( 'NONE', #34273, #29574 ) ;
#45102=CARTESIAN_POINT ( 'NONE',  ( 4.439252989704372263E-17, 3.267716535433071279, -7.700876377040399808E-33 ) ) ;
#45103=CARTESIAN_POINT ( 'NONE',  ( -1.198202975868765119, 3.346456692913386100, -1.732283464566922726 ) ) ;
#45104=DIRECTION ( 'NONE',  ( -1.000000000000000000, 0.000000000000000000, 0.000000000000000000 ) ) ;
#45105=CARTESIAN_POINT ( 'NONE',  ( 0.000000000000000000, 3.346456692913386100, 0.000000000000000000 ) ) ;
#45106=CARTESIAN_POINT ( 'NONE',  ( -0.8182917201112819283, 3.267716535433071279, -1.614173228346451605 ) ) ;
#45107=CARTESIAN_POINT ( 'NONE',  ( -1.363819533518803473, 3.346456692913386100, 2.047244094488179567 ) ) ;
#45108=ORIENTED_EDGE ( 'NONE', *, *, #41668, .F. ) ;
#45109=LINE ( 'NONE', #45869, #46051 ) ;
#45110=VECTOR ( 'NONE', #21485, 39.37007874015748143 ) ;
#45112=CARTESIAN_POINT ( 'NONE',  ( 0.000000000000000000, 3.267716535433071279, 0.5905511811023582691 ) ) ;
#45114=ORIENTED_EDGE ( 'NONE', *, *, #30782, .T. ) ;
#45115=VECTOR ( 'NONE', #45045, 39.37007874015748143 ) ;
#45116=CARTESIAN_POINT ( 'NONE',  ( 1.636583440222563857, 3.346456692913386100, 0.3149606299212576177 ) ) ;
#45118=ORIENTED_EDGE ( 'NONE', *, *, #30682, .T. ) ;
#45119=CARTESIAN_POINT ( 'NONE',  ( 0.8182917201112817063, 0.000000000000000000, -2.047244094488181343 ) ) ;
#45120=EDGE_CURVE ( 'NONE', #22175, #40166, #34687, .T. ) ;
#45124=ORIENTED_EDGE ( 'NONE', *, *, #12692, .T. ) ;
#45125=DIRECTION ( 'NONE',  ( -1.000000000000000000, 0.000000000000000000, -0.000000000000000000 ) ) ;
#45127=CARTESIAN_POINT ( 'NONE',  ( 0.000000000000000000, 3.346456692913386100, 0.000000000000000000 ) ) ;
#45130=VECTOR ( 'NONE', #39661, 39.37007874015748143 ) ;
#45131=LINE ( 'NONE', #25531, #30993 ) ;
#45132=ORIENTED_EDGE ( 'NONE', *, *, #7752, .T. ) ;
#45133=DIRECTION ( 'NONE',  ( 0.000000000000000000, 0.000000000000000000, -1.000000000000000000 ) ) ;
#45134=EDGE_CURVE ( 'NONE', #21655, #1296, #25534, .T. ) ;
#45136=CARTESIAN_POINT ( 'NONE',  ( 1.909347346926324684, 0.000000000000000000, -0.1574803149606304187 ) ) ;
#45137=ORIENTED_EDGE ( 'NONE', *, *, #430, .F. ) ;
#45139=ADVANCED_FACE ( 'NONE', ( #48728 ), #9536, .F. ) ;
#45141=FACE_BOUND ( 'NONE', #43471, .T. ) ;
#45142=PLANE ( 'NONE',  #36112 ) ;
#45143=CARTESIAN_POINT ( 'NONE',  ( -0.07591351300297340121, 3.267716535433071279, -1.299212598425193210 ) ) ;
#45144=AXIS2_PLACEMENT_3D ( 'NONE', #49857, #42405, #26408 ) ;
#45148=CARTESIAN_POINT ( 'NONE',  ( -0.8942052331142552601, 3.267716535433071279, -2.086614173228339641 ) ) ;
#45149=CARTESIAN_POINT ( 'NONE',  ( 0.000000000000000000, 3.267716535433071279, 0.000000000000000000 ) ) ;
#45150=ORIENTED_EDGE ( 'NONE', *, *, #2973, .T. ) ;
#45151=ORIENTED_EDGE ( 'NONE', *, *, #23506, .T. ) ;
#45152=VECTOR ( 'NONE', #43366, 39.37007874015748143 ) ;
#45153=VERTEX_POINT ( 'NONE', #28378 ) ;
#45154=LINE ( 'NONE', #9818, #47414 ) ;
#45155=DIRECTION ( 'NONE',  ( 0.000000000000000000, 0.000000000000000000, 1.000000000000000000 ) ) ;
#45156=CARTESIAN_POINT ( 'NONE',  ( 1.909347346926324684, 3.267716535433071279, -3.312189666507128175E-16 ) ) ;
#45157=DIRECTION ( 'NONE',  ( 1.000000000000000000, 0.000000000000000000, 0.000000000000000000 ) ) ;
#45158=VECTOR ( 'NONE', #5932, 39.37007874015748143 ) ;
#45161=LINE ( 'NONE', #37714, #6828 ) ;
#45162=DIRECTION ( 'NONE',  ( -0.000000000000000000, 1.000000000000000000, -0.000000000000000000 ) ) ;
#45163=CARTESIAN_POINT ( 'NONE',  ( 1.636583440222563857, 3.267716535433071279, 1.259842519685033135 ) ) ;
#45165=DIRECTION ( 'NONE',  ( -0.000000000000000000, 0.000000000000000000, 1.000000000000000000 ) ) ;
#45167=DIRECTION ( 'NONE',  ( 1.734723475976806848E-16, -0.000000000000000000, 1.000000000000000000 ) ) ;
#45168=LINE ( 'NONE', #12945, #1138 ) ;
#45169=EDGE_CURVE ( 'NONE', #7335, #39537, #32792, .T. ) ;
#45171=DIRECTION ( 'NONE',  ( -0.000000000000000000, 1.000000000000000000, -0.000000000000000000 ) ) ;
#45172=PLANE ( 'NONE',  #11236 ) ;
#45174=ORIENTED_EDGE ( 'NONE', *, *, #28070, .T. ) ;
#45175=EDGE_CURVE ( 'NONE', #16977, #35527, #25283, .T. ) ;
#45177=LINE ( 'NONE', #13209, #21638 ) ;
#45179=VECTOR ( 'NONE', #959, 39.37007874015748143 ) ;
#45180=ORIENTED_EDGE ( 'NONE', *, *, #30230, .T. ) ;
#45181=ADVANCED_FACE ( 'NONE', ( #41042 ), #21413, .F. ) ;
#45183=CARTESIAN_POINT ( 'NONE',  ( -3.414809992080329023E-17, 3.346456692913386100, -0.1968503937007874405 ) ) ;
#45184=AXIS2_PLACEMENT_3D ( 'NONE', #38332, #41435, #17941 ) ;
#45185=ORIENTED_EDGE ( 'NONE', *, *, #38514, .T. ) ;
#45186=VECTOR ( 'NONE', #34858, 39.37007874015748143 ) ;
#45187=DIRECTION ( 'NONE',  ( -1.000000000000000000, 0.000000000000000000, 1.734723475976806848E-16 ) ) ;
#45188=LINE ( 'NONE', #9852, #40412 ) ;
#45189=EDGE_CURVE ( 'NONE', #28145, #21463, #8767, .T. ) ;
#45190=VECTOR ( 'NONE', #36556, 39.37007874015748143 ) ;
#45191=ORIENTED_EDGE ( 'NONE', *, *, #19937, .T. ) ;
#45193=DIRECTION ( 'NONE',  ( -1.000000000000000000, -0.000000000000000000, -0.000000000000000000 ) ) ;
#45194=ORIENTED_EDGE ( 'NONE', *, *, #29236, .F. ) ;
#45195=ORIENTED_EDGE ( 'NONE', *, *, #16465, .T. ) ;
#45196=EDGE_CURVE ( 'NONE', #43525, #24410, #20640, .T. ) ;
#45197=DIRECTION ( 'NONE',  ( -1.000000000000000000, 0.000000000000000000, 0.000000000000000000 ) ) ;
#45198=FACE_OUTER_BOUND ( 'NONE', #14407, .T. ) ;
#45199=DIRECTION ( 'NONE',  ( -0.000000000000000000, 0.000000000000000000, 1.000000000000000000 ) ) ;
#45200=AXIS2_PLACEMENT_3D ( 'NONE', #18534, #6659, #45362 ) ;
#45201=ORIENTED_EDGE ( 'NONE', *, *, #13967, .T. ) ;
#45202=CARTESIAN_POINT ( 'NONE',  ( 1.091055626815042645, 3.267716535433071279, -0.3149606299212596716 ) ) ;
#45203=CARTESIAN_POINT ( 'NONE',  ( -0.3486774197067334380, 0.000000000000000000, 1.889763779527550369 ) ) ;
#45204=EDGE_CURVE ( 'NONE', #15077, #28112, #14429, .T. ) ;
#45205=DIRECTION ( 'NONE',  ( -3.469446951953613696E-16, 0.000000000000000000, -1.000000000000000000 ) ) ;
#45206=VERTEX_POINT ( 'NONE', #41796 ) ;
#45207=LINE ( 'NONE', #27119, #19945 ) ;
#45208=DIRECTION ( 'NONE',  ( 1.734723475976806848E-16, 0.000000000000000000, 1.000000000000000000 ) ) ;
#45209=PLANE ( 'NONE',  #19990 ) ;
#45211=VERTEX_POINT ( 'NONE', #26044 ) ;
#45213=DIRECTION ( 'NONE',  ( -3.469446951953613696E-16, 0.000000000000000000, -1.000000000000000000 ) ) ;
#45214=CIRCLE ( 'NONE', #34523, 2.106299212598425008 ) ;
#45217=ORIENTED_EDGE ( 'NONE', *, *, #33399, .T. ) ;
#45218=VERTEX_POINT ( 'NONE', #21925 ) ;
#45219=CARTESIAN_POINT ( 'NONE',  ( -0.3486774197067340486, 3.346456692913386100, -1.141732283464563791 ) ) ;
#45220=VERTEX_POINT ( 'NONE', #25788 ) ;
#45221=DIRECTION ( 'NONE',  ( -3.469446951953613696E-16, 0.000000000000000000, -1.000000000000000000 ) ) ;
#45222=DIRECTION ( 'NONE',  ( 1.000000000000000000, -0.000000000000000000, 0.000000000000000000 ) ) ;
#45223=VECTOR ( 'NONE', #28709, 39.37007874015748143 ) ;
#45224=VECTOR ( 'NONE', #36523, 39.37007874015748143 ) ;
#45225=VECTOR ( 'NONE', #40302, 39.37007874015748143 ) ;
#45226=CARTESIAN_POINT ( 'NONE',  ( -0.3486774197067334380, 3.346456692913386100, 0.9448818897637749625 ) ) ;
#45227=CARTESIAN_POINT ( 'NONE',  ( 1.287906020515830141, 3.346456692913386100, 0.1181102362204704270 ) ) ;
#45228=CARTESIAN_POINT ( 'NONE',  ( 4.439252989704605840E-17, 3.267716535433071279, -7.700876377040806239E-33 ) ) ;
#45229=EDGE_LOOP ( 'NONE', ( #5275, #2818, #26312, #26064 ) ) ;
#45230=CARTESIAN_POINT ( 'NONE',  ( 1.015142113812069979, 3.346456692913386100, 1.417322834645662777 ) ) ;
#45231=DIRECTION ( 'NONE',  ( 1.734723475976806848E-16, -0.000000000000000000, 1.000000000000000000 ) ) ;
#45233=LINE ( 'NONE', #25637, #35589 ) ;
#45234=EDGE_CURVE ( 'NONE', #39032, #42424, #30680, .T. ) ;
#45236=LINE ( 'NONE', #20747, #25694 ) ;
#45238=CARTESIAN_POINT ( 'NONE',  ( 1.015142113812069313, 0.000000000000000000, -0.3543307086614175816 ) ) ;
#45239=EDGE_CURVE ( 'NONE', #41605, #24016, #37685, .T. ) ;
#45240=ORIENTED_EDGE ( 'NONE', *, *, #29703, .F. ) ;
#45241=FACE_OUTER_BOUND ( 'NONE', #6028, .T. ) ;
#45243=LINE ( 'NONE', #17904, #11852 ) ;
#45244=EDGE_LOOP ( 'NONE', ( #22954, #41427, #31886, #41882 ) ) ;
#45245=CARTESIAN_POINT ( 'NONE',  ( -1.712496953225537855, 3.346456692913386100, -1.226315847645294221 ) ) ;
#45246=PLANE ( 'NONE',  #16711 ) ;
#45247=ORIENTED_EDGE ( 'NONE', *, *, #24113, .T. ) ;
#45249=DIRECTION ( 'NONE',  ( -1.000000000000000000, 0.000000000000000000, -0.000000000000000000 ) ) ;
#45250=DIRECTION ( 'NONE',  ( 1.734723475976806848E-16, -0.000000000000000000, 1.000000000000000000 ) ) ;
#45251=FACE_OUTER_BOUND ( 'NONE', #24026, .T. ) ;
#45253=VECTOR ( 'NONE', #25920, 39.37007874015748143 ) ;
#45254=CARTESIAN_POINT ( 'NONE',  ( 1.287906020515830141, 0.000000000000000000, -0.1968503937007883287 ) ) ;
#45255=EDGE_LOOP ( 'NONE', ( #36974, #738, #48330, #45463 ) ) ;
#45257=CARTESIAN_POINT ( 'NONE',  ( 0.5455278134075217666, 0.000000000000000000, 1.259842519685033357 ) ) ;
#45258=DIRECTION ( 'NONE',  ( -1.000000000000000000, -0.000000000000000000, -0.000000000000000000 ) ) ;
#45259=VERTEX_POINT ( 'NONE', #45892 ) ;
#45260=DIRECTION ( 'NONE',  ( -1.000000000000000000, 0.000000000000000000, -0.000000000000000000 ) ) ;
#45262=DIRECTION ( 'NONE',  ( -1.000000000000000000, -0.000000000000000000, -0.000000000000000000 ) ) ;
#45263=VECTOR ( 'NONE', #13823, 39.37007874015748143 ) ;
#45265=ORIENTED_EDGE ( 'NONE', *, *, #42395, .F. ) ;
#45266=LINE ( 'NONE', #13806, #38658 ) ;
#45267=DIRECTION ( 'NONE',  ( 0.000000000000000000, 0.000000000000000000, -1.000000000000000000 ) ) ;
#45268=EDGE_CURVE ( 'NONE', #421, #5106, #30432, .T. ) ;
#45271=VECTOR ( 'NONE', #3739, 39.37007874015748143 ) ;
#45273=DIRECTION ( 'NONE',  ( -3.469446951953613696E-16, 0.000000000000000000, -1.000000000000000000 ) ) ;
#45274=ORIENTED_EDGE ( 'NONE', *, *, #30882, .T. ) ;
#45275=CARTESIAN_POINT ( 'NONE',  ( 0.000000000000000000, 3.267716535433071279, 2.047244094488179567 ) ) ;
#45276=ORIENTED_EDGE ( 'NONE', *, *, #50581, .T. ) ;
#45277=ORIENTED_EDGE ( 'NONE', *, *, #11585, .F. ) ;
#45278=AXIS2_PLACEMENT_3D ( 'NONE', #2915, #18912, #46745 ) ;
#45282=ADVANCED_FACE ( 'NONE', ( #6684 ), #34560, .F. ) ;
#45283=VERTEX_POINT ( 'NONE', #46394 ) ;
#45285=DIRECTION ( 'NONE',  ( 1.734723475976806848E-16, 0.000000000000000000, 1.000000000000000000 ) ) ;
#45286=ORIENTED_EDGE ( 'NONE', *, *, #47553, .F. ) ;
#45288=DIRECTION ( 'NONE',  ( 1.000000000000000000, 0.000000000000000000, -3.469446951953613696E-16 ) ) ;
#45291=VECTOR ( 'NONE', #30436, 39.37007874015748143 ) ;
#45292=LINE ( 'NONE', #1439, #26410 ) ;
#45296=DIRECTION ( 'NONE',  ( -1.000000000000000000, 0.000000000000000000, -0.000000000000000000 ) ) ;
#45297=B_SPLINE_CURVE_WITH_KNOTS ( 'NONE', 3,
 ( #13704, #1821, #9572, #17574 ),
 .UNSPECIFIED., .F., .F.,
 ( 4, 4 ),
 ( 0.02707144773250385814, 0.02825827685263899644 ),
 .UNSPECIFIED. ) ;
#45298=CARTESIAN_POINT ( 'NONE',  ( 0.2727639067037607168, 3.267716535433071279, -4.731699523581612823E-17 ) ) ;
#45299=EDGE_CURVE ( 'NONE', #65, #40996, #49743, .T. ) ;
#45302=DIRECTION ( 'NONE',  ( -1.000000000000000000, 0.000000000000000000, 0.000000000000000000 ) ) ;
#45303=CARTESIAN_POINT ( 'NONE',  ( -1.166969139818015533, 3.346456692913386100, 1.417322834645662777 ) ) ;
#45304=ORIENTED_EDGE ( 'NONE', *, *, #21998, .T. ) ;
#45305=CARTESIAN_POINT ( 'NONE',  ( -0.6214413264104945434, 0.000000000000000000, -1.102362204724405492 ) ) ;
#45306=EDGE_CURVE ( 'NONE', #31017, #2822, #10299, .T. ) ;
#45308=ADVANCED_FACE ( 'NONE', ( #42290 ), #6937, .F. ) ;
#45311=VERTEX_POINT ( 'NONE', #18559 ) ;
#45312=DIRECTION ( 'NONE',  ( -0.000000000000000000, 1.000000000000000000, -0.000000000000000000 ) ) ;
#45314=EDGE_LOOP ( 'NONE', ( #9064, #40170, #33395, #2414 ) ) ;
#45315=FACE_BOUND ( 'NONE', #27820, .T. ) ;
#45318=DIRECTION ( 'NONE',  ( -0.000000000000000000, 0.000000000000000000, 1.000000000000000000 ) ) ;
#45321=CARTESIAN_POINT ( 'NONE',  ( 0.000000000000000000, 3.267716535433071279, 0.000000000000000000 ) ) ;
#45324=ORIENTED_EDGE ( 'NONE', *, *, #38123, .F. ) ;
#45325=CARTESIAN_POINT ( 'NONE',  ( -1.636583440222564301, 3.346456692913386100, -0.8267716535433052849 ) ) ;
#45326=AXIS2_PLACEMENT_3D ( 'NONE', #10692, #49627, #37817 ) ;
#45328=LINE ( 'NONE', #22121, #34019 ) ;
#45329=EDGE_CURVE ( 'NONE', #46654, #12774, #3061, .T. ) ;
#45333=EDGE_LOOP ( 'NONE', ( #4683, #34550, #25083, #36777, #50159 ) ) ;
#45334=ORIENTED_EDGE ( 'NONE', *, *, #43563, .F. ) ;
#45335=EDGE_CURVE ( 'NONE', #9748, #22703, #46645, .T. ) ;
#45336=VECTOR ( 'NONE', #43322, 39.37007874015748143 ) ;
#45339=ADVANCED_FACE ( 'NONE', ( #31189 ), #7687, .F. ) ;
#45340=ORIENTED_EDGE ( 'NONE', *, *, #50057, .T. ) ;
#45342=LINE ( 'NONE', #36868, #8759 ) ;
#45343=EDGE_CURVE ( 'NONE', #5165, #31344, #23427, .T. ) ;
#45348=DIRECTION ( 'NONE',  ( 1.734723475976806848E-16, -0.000000000000000000, 1.000000000000000000 ) ) ;
#45353=ORIENTED_EDGE ( 'NONE', *, *, #49540, .F. ) ;
#45354=LINE ( 'NONE', #37394, #23320 ) ;
#45355=DIRECTION ( 'NONE',  ( 1.000000000000000000, 0.000000000000000000, -3.469446951953613696E-16 ) ) ;
#45356=EDGE_CURVE ( 'NONE', #41290, #37129, #4324, .T. ) ;
#45357=CARTESIAN_POINT ( 'NONE',  ( 0.2727639067037602172, 3.346456692913386100, -2.047244094488182231 ) ) ;
#45358=CARTESIAN_POINT ( 'NONE',  ( -1.636583440222564301, 0.000000000000000000, -1.259842519685034468 ) ) ;
#45360=FACE_OUTER_BOUND ( 'NONE', #20309, .T. ) ;
#45362=DIRECTION ( 'NONE',  ( -3.469446951953613696E-16, 0.000000000000000000, -1.000000000000000000 ) ) ;
#45363=DIRECTION ( 'NONE',  ( 1.000000000000000000, 0.000000000000000000, -3.469446951953613696E-16 ) ) ;
#45364=EDGE_CURVE ( 'NONE', #508, #39624, #39439, .T. ) ;
#45366=DIRECTION ( 'NONE',  ( -0.000000000000000000, 0.000000000000000000, 1.000000000000000000 ) ) ;
#45367=ADVANCED_FACE ( 'NONE', ( #20055 ), #31441, .F. ) ;
#45368=EDGE_CURVE ( 'NONE', #26820, #13480, #15937, .T. ) ;
#45369=ORIENTED_EDGE ( 'NONE', *, *, #49254, .T. ) ;
#45371=DIRECTION ( 'NONE',  ( -0.000000000000000000, 0.000000000000000000, 1.000000000000000000 ) ) ;
#45372=AXIS2_PLACEMENT_3D ( 'NONE', #1947, #44538, #21066 ) ;
#45373=LINE ( 'NONE', #25012, #45987 ) ;
#45374=CIRCLE ( 'NONE', #42906, 2.165354330708661568 ) ;
#45376=LINE ( 'NONE', #33545, #50753 ) ;
#45379=EDGE_LOOP ( 'NONE', ( #33961, #30448, #23349, #37304 ) ) ;
#45381=CARTESIAN_POINT ( 'NONE',  ( 1.560669927219590747, 3.346456692913386100, 0.4724409448818871482 ) ) ;
#45382=ORIENTED_EDGE ( 'NONE', *, *, #36631, .T. ) ;
#45385=CARTESIAN_POINT ( 'NONE',  ( -0.2727639067037607723, 0.000000000000000000, -1.102362204724405714 ) ) ;
#45386=EDGE_LOOP ( 'NONE', ( #41488, #1408, #19865, #49304 ) ) ;
#45387=DIRECTION ( 'NONE',  ( 0.000000000000000000, -1.000000000000000000, 0.000000000000000000 ) ) ;
#45388=CARTESIAN_POINT ( 'NONE',  ( -0.8182917201112819283, 3.346456692913386100, -1.732283464566922726 ) ) ;
#45390=ORIENTED_EDGE ( 'NONE', *, *, #36473, .F. ) ;
#45391=ORIENTED_EDGE ( 'NONE', *, *, #4351, .F. ) ;
#45392=CARTESIAN_POINT ( 'NONE',  ( 0.000000000000000000, 3.267716535433071279, 0.9055118110236167750 ) ) ;
#45393=FACE_BOUND ( 'NONE', #30701, .T. ) ;
#45394=EDGE_LOOP ( 'NONE', ( #38809, #19091, #15198, #32517 ) ) ;
#45396=CARTESIAN_POINT ( 'NONE',  ( -1.985260859929298238, 3.346456692913386100, -1.141732283464563791 ) ) ;
#45397=EDGE_CURVE ( 'NONE', #5904, #17447, #451, .T. ) ;
#45399=VERTEX_POINT ( 'NONE', #46889 ) ;
#45400=DIRECTION ( 'NONE',  ( -1.000000000000000000, -0.000000000000000000, -0.000000000000000000 ) ) ;
#45402=EDGE_CURVE ( 'NONE', #5663, #8594, #38931, .T. ) ;
#45403=CARTESIAN_POINT ( 'NONE',  ( 1.833433833923351353, 3.267716535433071279, -0.5118110236220471121 ) ) ;
#45404=ORIENTED_EDGE ( 'NONE', *, *, #34091, .T. ) ;
#45405=VERTEX_POINT ( 'NONE', #3563 ) ;
#45406=ORIENTED_EDGE ( 'NONE', *, *, #36826, .F. ) ;
#45407=CARTESIAN_POINT ( 'NONE',  ( -1.909347346926324462, 0.000000000000000000, 1.102362204724404160 ) ) ;
#45408=VECTOR ( 'NONE', #32833, 39.37007874015748143 ) ;
#45409=CARTESIAN_POINT ( 'NONE',  ( 2.579472588755252050E-16, 3.346456692913386100, 2.106299212598425008 ) ) ;
#45411=DIRECTION ( 'NONE',  ( 1.000000000000000000, 0.000000000000000000, 0.000000000000000000 ) ) ;
#45413=VERTEX_POINT ( 'NONE', #19297 ) ;
#45416=LINE ( 'NONE', #17571, #31588 ) ;
#45418=ADVANCED_FACE ( 'NONE', ( #19550 ), #35319, .F. ) ;
#45419=LINE ( 'NONE', #41076, #37523 ) ;
#45420=DIRECTION ( 'NONE',  ( -1.000000000000000000, 0.000000000000000000, 0.000000000000000000 ) ) ;
#45422=EDGE_CURVE ( 'NONE', #23012, #12697, #50059, .T. ) ;
#45424=LINE ( 'NONE', #25827, #46473 ) ;
#45430=ORIENTED_EDGE ( 'NONE', *, *, #14029, .F. ) ;
#45434=CARTESIAN_POINT ( 'NONE',  ( 1.287906020515830585, 3.267716535433071279, 1.377952755905504256 ) ) ;
#45435=ORIENTED_EDGE ( 'NONE', *, *, #40309, .T. ) ;
#45436=VECTOR ( 'NONE', #27782, 39.37007874015748143 ) ;
#45437=DIRECTION ( 'NONE',  ( -1.000000000000000000, 0.000000000000000000, 0.000000000000000000 ) ) ;
#45438=CARTESIAN_POINT ( 'NONE',  ( -0.6214413264104939882, 3.346456692913386100, 1.535433070866133898 ) ) ;
#45439=VECTOR ( 'NONE', #3255, 39.37007874015748143 ) ;
#45440=ORIENTED_EDGE ( 'NONE', *, *, #24793, .F. ) ;
#45441=ORIENTED_EDGE ( 'NONE', *, *, #46252, .T. ) ;
#45442=VECTOR ( 'NONE', #23115, 39.37007874015748143 ) ;
#45443=CARTESIAN_POINT ( 'NONE',  ( 0.1968503937007872462, 3.267716535433071279, -0.8267716535433052849 ) ) ;
#45445=ORIENTED_EDGE ( 'NONE', *, *, #19726, .T. ) ;
#45447=DIRECTION ( 'NONE',  ( 0.000000000000000000, 0.000000000000000000, 1.000000000000000000 ) ) ;
#45448=VECTOR ( 'NONE', #10247, 39.37007874015748143 ) ;
#45449=FACE_OUTER_BOUND ( 'NONE', #14098, .T. ) ;
#45452=ORIENTED_EDGE ( 'NONE', *, *, #49323, .F. ) ;
#45453=CARTESIAN_POINT ( 'NONE',  ( 0.8182917201112819283, 3.267716535433071279, 0.1574803149606286423 ) ) ;
#45454=CARTESIAN_POINT ( 'NONE',  ( 0.000000000000000000, 3.267716535433071279, 0.000000000000000000 ) ) ;
#45455=LINE ( 'NONE', #10376, #6409 ) ;
#45457=CARTESIAN_POINT ( 'NONE',  ( 0.7423782071083085965, 0.000000000000000000, 0.7480314960629872445 ) ) ;
#45458=LINE ( 'NONE', #14505, #30991 ) ;
#45460=EDGE_CURVE ( 'NONE', #35067, #1831, #20585, .T. ) ;
#45462=VERTEX_POINT ( 'NONE', #28577 ) ;
#45463=ORIENTED_EDGE ( 'NONE', *, *, #15683, .T. ) ;
#45464=EDGE_CURVE ( 'NONE', #48582, #7654, #25224, .T. ) ;
#45466=CARTESIAN_POINT ( 'NONE',  ( 2.182111253630085290, 3.346456692913386100, -0.5118110236220471121 ) ) ;
#45467=CARTESIAN_POINT ( 'NONE',  ( 0.1968503937007877735, 3.267716535433071279, 1.062992125984246083 ) ) ;
#45468=EDGE_CURVE ( 'NONE', #22488, #39500, #32215, .T. ) ;
#45469=CARTESIAN_POINT ( 'NONE',  ( 0.8182917201112824834, 3.346456692913386100, 1.732283464566921172 ) ) ;
#45470=VERTEX_POINT ( 'NONE', #16460 ) ;
#45471=ORIENTED_EDGE ( 'NONE', *, *, #23704, .T. ) ;
#45472=DIRECTION ( 'NONE',  ( -3.469446951953613696E-16, 0.000000000000000000, -1.000000000000000000 ) ) ;
#45474=LINE ( 'NONE', #37517, #39794 ) ;
#45475=CARTESIAN_POINT ( 'NONE',  ( 1.636583440222563857, 3.346456692913386100, 0.3149606299212576177 ) ) ;
#45476=VECTOR ( 'NONE', #16882, 39.37007874015748143 ) ;
#45477=VECTOR ( 'NONE', #3195, 39.37007874015748143 ) ;
#45478=EDGE_CURVE ( 'NONE', #5602, #13181, #13104, .T. ) ;
#45479=CARTESIAN_POINT ( 'NONE',  ( 0.5455278134075216556, 0.000000000000000000, 1.377952755905504256 ) ) ;
#45480=VECTOR ( 'NONE', #26548, 39.37007874015748143 ) ;
#45481=DIRECTION ( 'NONE',  ( 0.000000000000000000, -1.000000000000000000, 0.000000000000000000 ) ) ;
#45484=CARTESIAN_POINT ( 'NONE',  ( 0.000000000000000000, 3.267716535433071279, 0.000000000000000000 ) ) ;
#45485=EDGE_CURVE ( 'NONE', #36932, #35018, #9481, .T. ) ;
#45486=VECTOR ( 'NONE', #33945, 39.37007874015748143 ) ;
#45487=LINE ( 'NONE', #10147, #8393 ) ;
#45488=ORIENTED_EDGE ( 'NONE', *, *, #32686, .F. ) ;
#45489=VECTOR ( 'NONE', #24560, 39.37007874015748143 ) ;
#45491=LINE ( 'NONE', #18155, #28614 ) ;
#45492=FACE_OUTER_BOUND ( 'NONE', #29238, .T. ) ;
#45493=VERTEX_POINT ( 'NONE', #965 ) ;
#45494=CARTESIAN_POINT ( 'NONE',  ( 1.909347346926324462, 3.346456692913386100, -1.102362204724406602 ) ) ;
#45495=ORIENTED_EDGE ( 'NONE', *, *, #47119, .T. ) ;
#45496=PLANE ( 'NONE',  #17255 ) ;
#45498=VERTEX_POINT ( 'NONE', #36083 ) ;
#45500=EDGE_CURVE ( 'NONE', #5175, #7776, #9221, .T. ) ;
#45501=CARTESIAN_POINT ( 'NONE',  ( -0.2727639067037608278, 3.346456692913386100, -1.614173228346451605 ) ) ;
#45503=DIRECTION ( 'NONE',  ( 1.000000000000000000, 0.000000000000000000, 0.000000000000000000 ) ) ;
#45504=DIRECTION ( 'NONE',  ( 0.000000000000000000, 0.000000000000000000, -1.000000000000000000 ) ) ;
#45505=ORIENTED_EDGE ( 'NONE', *, *, #27616, .T. ) ;
#45507=DIRECTION ( 'NONE',  ( -1.000000000000000000, -0.000000000000000000, -0.000000000000000000 ) ) ;
#45509=VERTEX_POINT ( 'NONE', #24463 ) ;
#45511=CARTESIAN_POINT ( 'NONE',  ( 0.5455278134075212115, 3.346456692913386100, 0.6299212598425161236 ) ) ;
#45512=DIRECTION ( 'NONE',  ( 1.734723475976806848E-16, -0.000000000000000000, 1.000000000000000000 ) ) ;
#45513=ORIENTED_EDGE ( 'NONE', *, *, #48026, .F. ) ;
#45514=CIRCLE ( 'NONE', #31532, 2.106299212598425008 ) ;
#45515=ORIENTED_EDGE ( 'NONE', *, *, #43348, .T. ) ;
#45516=DIRECTION ( 'NONE',  ( 1.734723475976806848E-16, 0.000000000000000000, 1.000000000000000000 ) ) ;
#45517=PLANE ( 'NONE',  #3527 ) ;
#45518=CARTESIAN_POINT ( 'NONE',  ( 0.000000000000000000, 3.267716535433071279, 1.850393700787391849 ) ) ;
#45519=ORIENTED_EDGE ( 'NONE', *, *, #40884, .T. ) ;
#45520=LINE ( 'NONE', #37311, #42188 ) ;
#45521=VECTOR ( 'NONE', #45080, 39.37007874015748143 ) ;
#45522=FACE_BOUND ( 'NONE', #4032, .T. ) ;
#45523=VERTEX_POINT ( 'NONE', #8968 ) ;
#45524=EDGE_CURVE ( 'NONE', #3116, #12576, #5091, .T. ) ;
#45525=CARTESIAN_POINT ( 'NONE',  ( 0.000000000000000000, 3.267716535433071279, 1.417322834645662777 ) ) ;
#45531=DIRECTION ( 'NONE',  ( 1.000000000000000000, 0.000000000000000000, -3.469446951953613696E-16 ) ) ;
#45532=EDGE_CURVE ( 'NONE', #924, #37147, #1472, .T. ) ;
#45533=EDGE_LOOP ( 'NONE', ( #32117, #14090, #37105, #20599 ) ) ;
#45534=DIRECTION ( 'NONE',  ( -3.469446951953613696E-16, 0.000000000000000000, -1.000000000000000000 ) ) ;
#45537=VERTEX_POINT ( 'NONE', #29085 ) ;
#45539=CARTESIAN_POINT ( 'NONE',  ( 0.8182917201112819283, 3.267716535433071279, -0.6692913385826764205 ) ) ;
#45540=CARTESIAN_POINT ( 'NONE',  ( 1.526828301548457834, 3.346456692913386100, 1.535433070866133898 ) ) ;
#45543=DIRECTION ( 'NONE',  ( -1.000000000000000000, 0.000000000000000000, 1.734723475976806848E-16 ) ) ;
#45545=ORIENTED_EDGE ( 'NONE', *, *, #13584, .T. ) ;
#45546=DIRECTION ( 'NONE',  ( -1.000000000000000000, 0.000000000000000000, 1.734723475976806848E-16 ) ) ;
#45547=ADVANCED_FACE ( 'NONE', ( #28836 ), #24967, .F. ) ;
#45551=PLANE ( 'NONE',  #20708 ) ;
#45552=CARTESIAN_POINT ( 'NONE',  ( 0.000000000000000000, 3.267716535433071279, 0.3149606299212578953 ) ) ;
#45554=LINE ( 'NONE', #10220, #46845 ) ;
#45556=CARTESIAN_POINT ( 'NONE',  ( 1.636583440222563857, 3.346456692913386100, 0.1181102362204701633 ) ) ;
#45557=CARTESIAN_POINT ( 'NONE',  ( 0.000000000000000000, 3.267716535433071279, 1.850393700787392293 ) ) ;
#45559=ORIENTED_EDGE ( 'NONE', *, *, #48548, .T. ) ;
#45560=DIRECTION ( 'NONE',  ( 0.000000000000000000, 0.000000000000000000, 1.000000000000000000 ) ) ;
#45561=ORIENTED_EDGE ( 'NONE', *, *, #45905, .T. ) ;
#45562=FACE_BOUND ( 'NONE', #21017, .T. ) ;
#45563=EDGE_CURVE ( 'NONE', #1604, #8994, #37107, .T. ) ;
#45564=CARTESIAN_POINT ( 'NONE',  ( 0.2727639067037605503, 3.267716535433071279, -4.731699523581609741E-17 ) ) ;
#45565=VECTOR ( 'NONE', #25500, 39.37007874015748143 ) ;
#45566=VECTOR ( 'NONE', #12412, 39.37007874015748143 ) ;
#45567=CARTESIAN_POINT ( 'NONE',  ( 0.8182917201112823724, 3.267716535433071279, 1.940849049717691122 ) ) ;
#45569=ORIENTED_EDGE ( 'NONE', *, *, #10238, .T. ) ;
#45570=ORIENTED_EDGE ( 'NONE', *, *, #46121, .T. ) ;
#45573=ADVANCED_FACE ( 'NONE', ( #44823 ), #40984, .F. ) ;
#45575=ORIENTED_EDGE ( 'NONE', *, *, #50156, .T. ) ;
#45576=ADVANCED_FACE ( 'NONE', ( #41989 ), #6108, .F. ) ;
#45579=DIRECTION ( 'NONE',  ( -1.000000000000000000, 0.000000000000000000, -0.000000000000000000 ) ) ;
#45583=ORIENTED_EDGE ( 'NONE', *, *, #2206, .F. ) ;
#45585=EDGE_CURVE ( 'NONE', #35595, #3716, #13863, .T. ) ;
#45586=EDGE_LOOP ( 'NONE', ( #22374, #33783, #28872, #38253 ) ) ;
#45589=EDGE_CURVE ( 'NONE', #32045, #19099, #29350, .T. ) ;
#45592=ORIENTED_EDGE ( 'NONE', *, *, #33232, .F. ) ;
#45593=AXIS2_PLACEMENT_3D ( 'NONE', #3226, #47057, #18975 ) ;
#45595=CARTESIAN_POINT ( 'NONE',  ( -0.8942052331142552601, 0.000000000000000000, -1.889763779527552146 ) ) ;
#45596=CIRCLE ( 'NONE', #19228, 2.106299212598425008 ) ;
#45597=VECTOR ( 'NONE', #37139, 39.37007874015748143 ) ;
#45598=FACE_OUTER_BOUND ( 'NONE', #21223, .T. ) ;
#45599=LINE ( 'NONE', #5628, #21190 ) ;
#45602=ORIENTED_EDGE ( 'NONE', *, *, #21250, .T. ) ;
#45605=DIRECTION ( 'NONE',  ( 0.000000000000000000, 0.000000000000000000, -1.000000000000000000 ) ) ;
#45607=ORIENTED_EDGE ( 'NONE', *, *, #51039, .T. ) ;
#45608=CARTESIAN_POINT ( 'NONE',  ( -1.363819533518803473, 0.000000000000000000, -0.3543307086614174151 ) ) ;
#45609=CARTESIAN_POINT ( 'NONE',  ( 0.000000000000000000, 3.267716535433071279, 0.000000000000000000 ) ) ;
#45610=EDGE_LOOP ( 'NONE', ( #14901, #10248, #37680, #20117 ) ) ;
#45611=CARTESIAN_POINT ( 'NONE',  ( -0.8942052331142552601, 0.000000000000000000, -0.9448818897637760728 ) ) ;
#45613=PLANE ( 'NONE',  #6160 ) ;
#45614=VERTEX_POINT ( 'NONE', #9985 ) ;
#45615=ORIENTED_EDGE ( 'NONE', *, *, #28452, .F. ) ;
#45618=LINE ( 'NONE', #29654, #6932 ) ;
#45620=EDGE_CURVE ( 'NONE', #33927, #2475, #38014, .T. ) ;
#45622=DIRECTION ( 'NONE',  ( -1.000000000000000000, 0.000000000000000000, -0.000000000000000000 ) ) ;
#45623=VERTEX_POINT ( 'NONE', #48920 ) ;
#45624=EDGE_CURVE ( 'NONE', #7189, #13035, #9960, .T. ) ;
#45626=AXIS2_PLACEMENT_3D ( 'NONE', #45785, #25424, #29562 ) ;
#45628=ORIENTED_EDGE ( 'NONE', *, *, #22757, .T. ) ;
#45631=LINE ( 'NONE', #38430, #37831 ) ;
#45633=ORIENTED_EDGE ( 'NONE', *, *, #44992, .T. ) ;
#45634=AXIS2_PLACEMENT_3D ( 'NONE', #32669, #29021, #28769 ) ;
#45635=AXIS2_PLACEMENT_3D ( 'NONE', #28673, #25068, #8804 ) ;
#45636=CARTESIAN_POINT ( 'NONE',  ( -1.636583440222564301, 0.000000000000000000, -1.259842519685034468 ) ) ;
#45637=LINE ( 'NONE', #29413, #7590 ) ;
#45638=EDGE_CURVE ( 'NONE', #50546, #40954, #14366, .T. ) ;
#45640=PLANE ( 'NONE',  #47731 ) ;
#45641=EDGE_LOOP ( 'NONE', ( #27765, #12862, #1294, #38864 ) ) ;
#45642=ORIENTED_EDGE ( 'NONE', *, *, #2990, .F. ) ;
#45643=DIRECTION ( 'NONE',  ( -1.000000000000000000, 0.000000000000000000, 1.734723475976806848E-16 ) ) ;
#45644=FACE_OUTER_BOUND ( 'NONE', #20350, .T. ) ;
#45646=EDGE_CURVE ( 'NONE', #32620, #28023, #10239, .T. ) ;
#45648=DIRECTION ( 'NONE',  ( 1.734723475976806848E-16, -0.000000000000000000, 1.000000000000000000 ) ) ;
#45650=ORIENTED_EDGE ( 'NONE', *, *, #8440, .F. ) ;
#45651=EDGE_CURVE ( 'NONE', #22497, #20299, #21866, .T. ) ;
#45652=CARTESIAN_POINT ( 'NONE',  ( -1.636583440222563635, 3.346456692913386100, 1.259842519685033357 ) ) ;
#45655=ORIENTED_EDGE ( 'NONE', *, *, #26996, .F. ) ;
#45656=ORIENTED_EDGE ( 'NONE', *, *, #43708, .T. ) ;
#45657=DIRECTION ( 'NONE',  ( -1.000000000000000000, 0.000000000000000000, 1.734723475976806848E-16 ) ) ;
#45658=CARTESIAN_POINT ( 'NONE',  ( -1.985260859929298016, 3.346456692913386100, -0.9448818897637762948 ) ) ;
#45662=ORIENTED_EDGE ( 'NONE', *, *, #43563, .T. ) ;
#45665=CARTESIAN_POINT ( 'NONE',  ( -0.07591351300297277671, 3.346456692913386100, 1.417322834645662777 ) ) ;
#45666=CARTESIAN_POINT ( 'NONE',  ( -1.712496953225537188, 0.000000000000000000, -0.03937007874015881204 ) ) ;
#45667=CARTESIAN_POINT ( 'NONE',  ( 1.909347346926324462, 0.000000000000000000, -1.102362204724406602 ) ) ;
#45668=VECTOR ( 'NONE', #37865, 39.37007874015748143 ) ;
#45669=CARTESIAN_POINT ( 'NONE',  ( -0.07591351300297359550, 3.346456692913386100, -2.047244094488181343 ) ) ;
#45670=VECTOR ( 'NONE', #19156, 39.37007874015748143 ) ;
#45671=LINE ( 'NONE', #33081, #22336 ) ;
#45673=LINE ( 'NONE', #26082, #20169 ) ;
#45676=EDGE_LOOP ( 'NONE', ( #21985, #28674 ) ) ;
#45677=LINE ( 'NONE', #26583, #3613 ) ;
#45678=CARTESIAN_POINT ( 'NONE',  ( -0.6214413264104939882, 0.000000000000000000, 0.7874015748031456541 ) ) ;
#45679=ORIENTED_EDGE ( 'NONE', *, *, #30428, .F. ) ;
#45682=EDGE_CURVE ( 'NONE', #28536, #24717, #884, .T. ) ;
#45683=EDGE_LOOP ( 'NONE', ( #34494, #29721, #28612 ) ) ;
#45687=ORIENTED_EDGE ( 'NONE', *, *, #483, .F. ) ;
#45688=CARTESIAN_POINT ( 'NONE',  ( 0.5455278134075208785, 0.000000000000000000, -1.574803149606293529 ) ) ;
#45690=EDGE_CURVE ( 'NONE', #32424, #27097, #10744, .T. ) ;
#45694=EDGE_LOOP ( 'NONE', ( #44445, #130, #38795, #13311 ) ) ;
#45697=ORIENTED_EDGE ( 'NONE', *, *, #43892, .F. ) ;
#45698=EDGE_LOOP ( 'NONE', ( #23054, #1231, #22440, #3992 ) ) ;
#45699=AXIS2_PLACEMENT_3D ( 'NONE', #31278, #27636, #35655 ) ;
#45700=DIRECTION ( 'NONE',  ( 1.000000000000000000, 0.000000000000000000, -3.469446951953613696E-16 ) ) ;
#45703=DIRECTION ( 'NONE',  ( 1.000000000000000000, 0.000000000000000000, 0.000000000000000000 ) ) ;
#45706=VECTOR ( 'NONE', #17014, 39.37007874015748143 ) ;
#45707=ORIENTED_EDGE ( 'NONE', *, *, #41500, .F. ) ;
#45709=LINE ( 'NONE', #21995, #13122 ) ;
#45710=DIRECTION ( 'NONE',  ( -0.000000000000000000, 1.000000000000000000, -0.000000000000000000 ) ) ;
#45714=DIRECTION ( 'NONE',  ( -1.000000000000000000, 0.000000000000000000, 1.734723475976806848E-16 ) ) ;
#45715=CARTESIAN_POINT ( 'NONE',  ( 0.4696143004045484348, 0.000000000000000000, 0.9055118110236167750 ) ) ;
#45716=VECTOR ( 'NONE', #32982, 39.37007874015748143 ) ;
#45718=DIRECTION ( 'NONE',  ( -1.000000000000000000, 0.000000000000000000, 0.000000000000000000 ) ) ;
#45721=EDGE_CURVE ( 'NONE', #19187, #49634, #17734, .T. ) ;
#45724=CARTESIAN_POINT ( 'NONE',  ( -1.057143431661240696, 3.346456692913386100, 1.889763779527550147 ) ) ;
#45725=ORIENTED_EDGE ( 'NONE', *, *, #10772, .F. ) ;
#45727=LINE ( 'NONE', #22268, #8658 ) ;
#45729=DIRECTION ( 'NONE',  ( 1.000000000000000000, 0.000000000000000000, -3.469446951953613696E-16 ) ) ;
#45731=CARTESIAN_POINT ( 'NONE',  ( 1.560669927219590747, 3.346456692913386100, 0.7874015748031454320 ) ) ;
#45735=AXIS2_PLACEMENT_3D ( 'NONE', #26881, #26141, #23266 ) ;
#45736=FACE_OUTER_BOUND ( 'NONE', #40931, .T. ) ;
#45737=LINE ( 'NONE', #44987, #16168 ) ;
#45739=CIRCLE ( 'NONE', #49844, 2.106299212598425008 ) ;
#45743=CARTESIAN_POINT ( 'NONE',  ( -0.07591351300297340121, 3.346456692913386100, 2.165354330708650465 ) ) ;
#45745=DIRECTION ( 'NONE',  ( -0.000000000000000000, 1.000000000000000000, -0.000000000000000000 ) ) ;
#45746=EDGE_LOOP ( 'NONE', ( #24649, #34995, #27337, #37284 ) ) ;
#45747=FACE_OUTER_BOUND ( 'NONE', #3316, .T. ) ;
#45748=ADVANCED_FACE ( 'NONE', ( #26737 ), #7382, .F. ) ;
#45751=ORIENTED_EDGE ( 'NONE', *, *, #44147, .F. ) ;
#45753=DIRECTION ( 'NONE',  ( -0.000000000000000000, 1.000000000000000000, -0.000000000000000000 ) ) ;
#45755=DIRECTION ( 'NONE',  ( 1.000000000000000000, 0.000000000000000000, -3.469446951953613696E-16 ) ) ;
#45758=PLANE ( 'NONE',  #28821 ) ;
#45759=CARTESIAN_POINT ( 'NONE',  ( 0.2727639067037602172, 3.346456692913386100, -2.244094488188969727 ) ) ;
#45761=ORIENTED_EDGE ( 'NONE', *, *, #17395, .F. ) ;
#45763=CARTESIAN_POINT ( 'NONE',  ( 0.8182917201112823724, 3.346456692913386100, 1.940849049717691122 ) ) ;
#45764=VERTEX_POINT ( 'NONE', #22873 ) ;
#45765=DIRECTION ( 'NONE',  ( 0.000000000000000000, 0.000000000000000000, -1.000000000000000000 ) ) ;
#45766=CARTESIAN_POINT ( 'NONE',  ( 0.7423782071083087075, 3.346456692913386100, -0.9448818897637765168 ) ) ;
#45768=ORIENTED_EDGE ( 'NONE', *, *, #27564, .T. ) ;
#45771=CARTESIAN_POINT ( 'NONE',  ( -2.167711126757420725, 3.254047560071126721, -1.141732283464563791 ) ) ;
#45772=CARTESIAN_POINT ( 'NONE',  ( 0.9671406142315196464, 3.267716535433070391, -2.244094488188969283 ) ) ;
#45774=ORIENTED_EDGE ( 'NONE', *, *, #16932, .T. ) ;
#45775=DIRECTION ( 'NONE',  ( 1.000000000000000000, 0.000000000000000000, 0.000000000000000000 ) ) ;
#45776=CARTESIAN_POINT ( 'NONE',  ( 1.287906020515830141, 3.346456692913386100, 0.6299212598425161236 ) ) ;
#45777=AXIS2_PLACEMENT_3D ( 'NONE', #33654, #25635, #41389 ) ;
#45780=ADVANCED_FACE ( 'NONE', ( #23627 ), #39378, .F. ) ;
#45781=CARTESIAN_POINT ( 'NONE',  ( -0.5455278134075208785, 3.267716535433071279, 0.9448818897637749625 ) ) ;
#45783=ORIENTED_EDGE ( 'NONE', *, *, #16762, .F. ) ;
#45784=PLANE ( 'NONE',  #47637 ) ;
#45785=CARTESIAN_POINT ( 'NONE',  ( 1.091055626815042423, 0.000000000000000000, -1.771653543307081691 ) ) ;
#45789=ORIENTED_EDGE ( 'NONE', *, *, #17489, .T. ) ;
#45791=LINE ( 'NONE', #6066, #37867 ) ;
#45793=AXIS2_PLACEMENT_3D ( 'NONE', #11678, #26911, #38310 ) ;
#45798=CARTESIAN_POINT ( 'NONE',  ( -1.636583440222563635, 3.267716535433071279, 0.6299212598425164567 ) ) ;
#45799=LINE ( 'NONE', #1697, #5575 ) ;
#45800=EDGE_LOOP ( 'NONE', ( #31678, #8772, #14230, #12532 ) ) ;
#45801=CARTESIAN_POINT ( 'NONE',  ( 0.5455278134075211005, 0.000000000000000000, 0.7480314960629872445 ) ) ;
#45802=CARTESIAN_POINT ( 'NONE',  ( 0.7423782071083091516, 3.267716535433071279, -2.575641807848711673E-16 ) ) ;
#45803=VERTEX_POINT ( 'NONE', #35002 ) ;
#45804=CARTESIAN_POINT ( 'NONE',  ( -1.195183497228115035E-16, 3.346456692913386100, -0.9448818897637765168 ) ) ;
#45806=ORIENTED_EDGE ( 'NONE', *, *, #9276, .T. ) ;
#45807=CARTESIAN_POINT ( 'NONE',  ( 2.100403847690402337, 3.267716535433071279, -0.1574803149606304187 ) ) ;
#45812=EDGE_CURVE ( 'NONE', #4242, #27610, #42736, .T. ) ;
#45814=ORIENTED_EDGE ( 'NONE', *, *, #28824, .F. ) ;
#45817=FACE_BOUND ( 'NONE', #42305, .T. ) ;
#45818=VECTOR ( 'NONE', #8391, 39.37007874015748143 ) ;
#45820=LINE ( 'NONE', #37353, #15181 ) ;
#45821=CARTESIAN_POINT ( 'NONE',  ( 1.287906020515830585, 0.000000000000000000, 1.574803149606291974 ) ) ;
#45822=LINE ( 'NONE', #34241, #41653 ) ;
#45823=EDGE_CURVE ( 'NONE', #40070, #26463, #14875, .T. ) ;
#45824=AXIS2_PLACEMENT_3D ( 'NONE', #27950, #50879, #46531 ) ;
#45827=ORIENTED_EDGE ( 'NONE', *, *, #35245, .F. ) ;
#45829=PLANE ( 'NONE',  #4854 ) ;
#45831=DIRECTION ( 'NONE',  ( 1.000000000000000000, 0.000000000000000000, 0.000000000000000000 ) ) ;
#45832=ORIENTED_EDGE ( 'NONE', *, *, #10913, .F. ) ;
#45834=EDGE_CURVE ( 'NONE', #9679, #23187, #31634, .T. ) ;
#45835=VERTEX_POINT ( 'NONE', #19493 ) ;
#45836=DIRECTION ( 'NONE',  ( -3.469446951953613696E-16, 0.000000000000000000, -1.000000000000000000 ) ) ;
#45837=CARTESIAN_POINT ( 'NONE',  ( -1.909347346926324462, 0.000000000000000000, 0.1574803149606286423 ) ) ;
#45838=EDGE_LOOP ( 'NONE', ( #20508, #31192, #35105, #18185 ) ) ;
#45839=EDGE_CURVE ( 'NONE', #16948, #7950, #35255, .T. ) ;
#45840=LINE ( 'NONE', #14117, #29823 ) ;
#45841=VERTEX_POINT ( 'NONE', #15631 ) ;
#45842=ORIENTED_EDGE ( 'NONE', *, *, #48309, .F. ) ;
#45843=EDGE_CURVE ( 'NONE', #43652, #39871, #30620, .T. ) ;
#45848=VECTOR ( 'NONE', #18601, 39.37007874015748143 ) ;
#45849=AXIS2_PLACEMENT_3D ( 'NONE', #27828, #39714, #35843 ) ;
#45851=CARTESIAN_POINT ( 'NONE',  ( -1.439733046521776583, 3.346456692913386100, -1.617383112398506295 ) ) ;
#45852=EDGE_CURVE ( 'NONE', #26317, #49734, #47078, .T. ) ;
#45854=DIRECTION ( 'NONE',  ( -0.000000000000000000, 1.000000000000000000, -0.000000000000000000 ) ) ;
#45855=VECTOR ( 'NONE', #38422, 39.37007874015748143 ) ;
#45856=LINE ( 'NONE', #26261, #9952 ) ;
#45857=VECTOR ( 'NONE', #20774, 39.37007874015748143 ) ;
#45859=CARTESIAN_POINT ( 'NONE',  ( -1.195183497228115035E-16, 3.346456692913386100, 0.3149606299212576177 ) ) ;
#45860=ORIENTED_EDGE ( 'NONE', *, *, #28206, .T. ) ;
#45861=DIRECTION ( 'NONE',  ( -3.469446951953613696E-16, 0.000000000000000000, -1.000000000000000000 ) ) ;
#45862=CARTESIAN_POINT ( 'NONE',  ( -0.6214413264104945434, 0.000000000000000000, -0.1574803149606301411 ) ) ;
#45865=ORIENTED_EDGE ( 'NONE', *, *, #32530, .T. ) ;
#45867=CARTESIAN_POINT ( 'NONE',  ( 0.000000000000000000, 3.346456692913386100, 0.000000000000000000 ) ) ;
#45868=VERTEX_POINT ( 'NONE', #25163 ) ;
#45869=CARTESIAN_POINT ( 'NONE',  ( -2.182111253630085734, 3.346456692913386100, -1.141732283464563791 ) ) ;
#45870=FACE_OUTER_BOUND ( 'NONE', #4922, .T. ) ;
#45874=EDGE_CURVE ( 'NONE', #12583, #33355, #24399, .T. ) ;
#45875=CARTESIAN_POINT ( 'NONE',  ( -0.8182917201112819283, 3.267716535433071279, -1.102362204724405492 ) ) ;
#45877=FACE_OUTER_BOUND ( 'NONE', #19858, .T. ) ;
#45879=CARTESIAN_POINT ( 'NONE',  ( -0.5455278134075214336, 3.267716535433071279, -0.3149606299212593941 ) ) ;
#45881=VECTOR ( 'NONE', #17203, 39.37007874015748143 ) ;
#45884=AXIS2_PLACEMENT_3D ( 'NONE', #8736, #47426, #20083 ) ;
#45886=ORIENTED_EDGE ( 'NONE', *, *, #30434, .T. ) ;
#45887=LINE ( 'NONE', #11555, #8943 ) ;
#45888=EDGE_LOOP ( 'NONE', ( #16674, #15048, #37589, #26328 ) ) ;
#45891=ORIENTED_EDGE ( 'NONE', *, *, #42352, .F. ) ;
#45892=CARTESIAN_POINT ( 'NONE',  ( -1.985260859929297572, 3.267716535433071279, 0.6299212598425164567 ) ) ;
#45893=VECTOR ( 'NONE', #35209, 39.37007874015748143 ) ;
#45894=CARTESIAN_POINT ( 'NONE',  ( -1.636583440222564301, 3.346456692913386100, -1.325930245594398871 ) ) ;
#45895=VECTOR ( 'NONE', #30245, 39.37007874015748143 ) ;
#45896=PLANE ( 'NONE',  #5736 ) ;
#45899=CARTESIAN_POINT ( 'NONE',  ( -2.182111253630085290, 3.267716535433071279, 3.785359618865288779E-16 ) ) ;
#45900=FACE_BOUND ( 'NONE', #13548, .T. ) ;
#45903=CARTESIAN_POINT ( 'NONE',  ( 0.5455278134075217666, 3.346456692913386100, 1.259842519685033357 ) ) ;
#45904=PLANE ( 'NONE',  #50561 ) ;
#45905=EDGE_CURVE ( 'NONE', #33786, #12621, #49524, .T. ) ;
#45906=VERTEX_POINT ( 'NONE', #8394 ) ;
#45908=CARTESIAN_POINT ( 'NONE',  ( 0.000000000000000000, 3.267716535433071279, 0.000000000000000000 ) ) ;
#45909=DIRECTION ( 'NONE',  ( -0.000000000000000000, 1.000000000000000000, -0.000000000000000000 ) ) ;
#45910=EDGE_LOOP ( 'NONE', ( #3006, #30974, #39846, #49308 ) ) ;
#45911=ORIENTED_EDGE ( 'NONE', *, *, #26504, .F. ) ;
#45912=EDGE_CURVE ( 'NONE', #33009, #12066, #16912, .T. ) ;
#45913=VERTEX_POINT ( 'NONE', #44003 ) ;
#45914=PLANE ( 'NONE',  #50708 ) ;
#45915=DIRECTION ( 'NONE',  ( 0.000000000000000000, -1.000000000000000000, 0.000000000000000000 ) ) ;
#45918=VECTOR ( 'NONE', #12492, 39.37007874015748143 ) ;
#45920=ORIENTED_EDGE ( 'NONE', *, *, #20661, .T. ) ;
#45921=ORIENTED_EDGE ( 'NONE', *, *, #26162, .T. ) ;
#45922=CARTESIAN_POINT ( 'NONE',  ( 2.088192093915797631, 3.267716535433071279, 0.2755905511810994302 ) ) ;
#45924=CARTESIAN_POINT ( 'NONE',  ( -1.439733046521776139, 0.000000000000000000, 0.6299212598425164567 ) ) ;
#45928=EDGE_CURVE ( 'NONE', #28890, #44964, #47047, .T. ) ;
#45930=DIRECTION ( 'NONE',  ( 1.000000000000000000, 0.000000000000000000, 0.000000000000000000 ) ) ;
#45931=DIRECTION ( 'NONE',  ( -0.000000000000000000, 0.000000000000000000, 1.000000000000000000 ) ) ;
#45932=EDGE_LOOP ( 'NONE', ( #18507, #9191, #4733, #42553 ) ) ;
#45933=DIRECTION ( 'NONE',  ( -1.000000000000000000, 0.000000000000000000, 0.000000000000000000 ) ) ;
#45934=DIRECTION ( 'NONE',  ( -0.000000000000000000, 1.000000000000000000, -0.000000000000000000 ) ) ;
#45935=AXIS2_PLACEMENT_3D ( 'NONE', #18592, #13954, #34086 ) ;
#45936=VERTEX_POINT ( 'NONE', #28256 ) ;
#45937=ORIENTED_EDGE ( 'NONE', *, *, #18580, .F. ) ;
#45940=ORIENTED_EDGE ( 'NONE', *, *, #9235, .T. ) ;
#45941=EDGE_CURVE ( 'NONE', #43368, #12647, #1413, .T. ) ;
#45942=ORIENTED_EDGE ( 'NONE', *, *, #14795, .T. ) ;
#45944=ORIENTED_EDGE ( 'NONE', *, *, #17880, .T. ) ;
#45946=DIRECTION ( 'NONE',  ( 0.000000000000000000, -1.000000000000000000, 0.000000000000000000 ) ) ;
#45947=VECTOR ( 'NONE', #38548, 39.37007874015748143 ) ;
#45948=AXIS2_PLACEMENT_3D ( 'NONE', #6727, #34359, #49791 ) ;
#45949=ORIENTED_EDGE ( 'NONE', *, *, #16892, .T. ) ;
#45952=ORIENTED_EDGE ( 'NONE', *, *, #15737, .T. ) ;
#45953=ORIENTED_EDGE ( 'NONE', *, *, #10212, .F. ) ;
#45954=CARTESIAN_POINT ( 'NONE',  ( -1.909347346926324906, 0.000000000000000000, -0.9842519685039344823 ) ) ;
#45959=ORIENTED_EDGE ( 'NONE', *, *, #33568, .F. ) ;
#45960=DIRECTION ( 'NONE',  ( 1.000000000000000000, -0.000000000000000000, 0.000000000000000000 ) ) ;
#45961=LINE ( 'NONE', #22250, #25017 ) ;
#45962=CARTESIAN_POINT ( 'NONE',  ( -2.009899395340762229, 3.346456692913386100, -0.6299212598425177889 ) ) ;
#45963=ADVANCED_FACE ( 'NONE', ( #12267 ), #36279, .F. ) ;
#45964=ORIENTED_EDGE ( 'NONE', *, *, #21532, .F. ) ;
#45965=AXIS2_PLACEMENT_3D ( 'NONE', #11580, #30703, #27313 ) ;
#45967=DIRECTION ( 'NONE',  ( 1.000000000000000000, 0.000000000000000000, 0.000000000000000000 ) ) ;
#45969=VERTEX_POINT ( 'NONE', #902 ) ;
#45971=VECTOR ( 'NONE', #23334, 39.37007874015748143 ) ;
#45974=EDGE_CURVE ( 'NONE', #24477, #20150, #8902, .T. ) ;
#45976=EDGE_CURVE ( 'NONE', #1768, #42497, #647, .T. ) ;
#45977=LINE ( 'NONE', #10641, #31927 ) ;
#45978=DIRECTION ( 'NONE',  ( -1.000000000000000000, 0.000000000000000000, 1.734723475976806848E-16 ) ) ;
#45981=EDGE_CURVE ( 'NONE', #28082, #24863, #27294, .T. ) ;
#45983=ORIENTED_EDGE ( 'NONE', *, *, #48328, .T. ) ;
#45984=FACE_OUTER_BOUND ( 'NONE', #41339, .T. ) ;
#45985=CARTESIAN_POINT ( 'NONE',  ( 0.000000000000000000, 3.267716535433071279, -1.732283464566922726 ) ) ;
#45986=AXIS2_PLACEMENT_3D ( 'NONE', #38925, #30931, #22174 ) ;
#45987=VECTOR ( 'NONE', #5393, 39.37007874015748143 ) ;
#45988=DIRECTION ( 'NONE',  ( -3.469446951953613696E-16, 0.000000000000000000, -1.000000000000000000 ) ) ;
#45989=DIRECTION ( 'NONE',  ( -0.000000000000000000, 1.000000000000000000, -0.000000000000000000 ) ) ;
#45990=CARTESIAN_POINT ( 'NONE',  ( 1.287906020515830141, 0.000000000000000000, -8.878505979408855953E-16 ) ) ;
#45991=ORIENTED_EDGE ( 'NONE', *, *, #28226, .T. ) ;
#45997=LINE ( 'NONE', #22280, #41381 ) ;
#45998=VERTEX_POINT ( 'NONE', #32412 ) ;
#45999=AXIS2_PLACEMENT_3D ( 'NONE', #32324, #31814, #3928 ) ;
#46000=LINE ( 'NONE', #41901, #42993 ) ;
#46001=EDGE_CURVE ( 'NONE', #36538, #29354, #28514, .T. ) ;
#46003=PLANE ( 'NONE',  #40370 ) ;
#46005=EDGE_CURVE ( 'NONE', #1681, #5831, #20776, .T. ) ;
#46006=VECTOR ( 'NONE', #15648, 39.37007874015748143 ) ;
#46007=PLANE ( 'NONE',  #23425 ) ;
#46008=EDGE_CURVE ( 'NONE', #38012, #7287, #5541, .T. ) ;
#46011=LINE ( 'NONE', #2920, #10582 ) ;
#46013=VECTOR ( 'NONE', #48958, 39.37007874015748143 ) ;
#46014=CARTESIAN_POINT ( 'NONE',  ( 1.091055626815042867, 3.267716535433071279, -1.892679809432644882E-16 ) ) ;
#46017=DIRECTION ( 'NONE',  ( 0.000000000000000000, 0.000000000000000000, -1.000000000000000000 ) ) ;
#46019=ORIENTED_EDGE ( 'NONE', *, *, #10668, .F. ) ;
#46021=CARTESIAN_POINT ( 'NONE',  ( -0.4832241344345758471, 3.255108573300695252, -2.401574803149598036 ) ) ;
#46025=LINE ( 'NONE', #10685, #8806 ) ;
#46027=ORIENTED_EDGE ( 'NONE', *, *, #8718, .F. ) ;
#46028=CARTESIAN_POINT ( 'NONE',  ( 1.091055626815042645, 0.000000000000000000, -0.3149606299212596716 ) ) ;
#46031=CARTESIAN_POINT ( 'NONE',  ( 4.268512490100411402E-16, 3.346456692913386100, 1.259842519685033357 ) ) ;
#46033=DIRECTION ( 'NONE',  ( -0.000000000000000000, 1.000000000000000000, -0.000000000000000000 ) ) ;
#46036=LINE ( 'NONE', #10699, #47973 ) ;
#46037=ORIENTED_EDGE ( 'NONE', *, *, #40079, .T. ) ;
#46038=VECTOR ( 'NONE', #20110, 39.37007874015748143 ) ;
#46039=EDGE_LOOP ( 'NONE', ( #17630, #36943, #19559, #11690 ) ) ;
#46042=VECTOR ( 'NONE', #2044, 39.37007874015748143 ) ;
#46043=CARTESIAN_POINT ( 'NONE',  ( 1.015142113812069313, 3.346456692913386100, 0.1574803149606286423 ) ) ;
#46044=CARTESIAN_POINT ( 'NONE',  ( -2.454875160333845674, 3.242921367653845977, -0.03937007874015881204 ) ) ;
#46046=DIRECTION ( 'NONE',  ( -0.000000000000000000, 1.000000000000000000, -0.000000000000000000 ) ) ;
#46050=EDGE_CURVE ( 'NONE', #40640, #27577, #27112, .T. ) ;
#46051=VECTOR ( 'NONE', #50222, 39.37007874015748143 ) ;
#46053=LINE ( 'NONE', #2965, #40951 ) ;
#46054=EDGE_CURVE ( 'NONE', #26348, #21582, #37997, .T. ) ;
#46055=DIRECTION ( 'NONE',  ( -0.000000000000000000, 1.000000000000000000, -0.000000000000000000 ) ) ;
#46058=CARTESIAN_POINT ( 'NONE',  ( 0.7423782071083091516, 3.267716535433071279, -2.575641807848711673E-16 ) ) ;
#46060=CARTESIAN_POINT ( 'NONE',  ( 0.4696143004045478797, 3.267716535433071279, 0.5905511811023579360 ) ) ;
#46061=EDGE_CURVE ( 'NONE', #5100, #28890, #38502, .T. ) ;
#46063=EDGE_LOOP ( 'NONE', ( #38542, #25371, #9608, #10252 ) ) ;
#46064=CARTESIAN_POINT ( 'NONE',  ( -0.5455278134075214336, 3.267716535433071279, -1.259842519685035134 ) ) ;
#46065=ADVANCED_FACE ( 'NONE', ( #26611 ), #15000, .F. ) ;
#46068=CARTESIAN_POINT ( 'NONE',  ( -1.363819533518803473, 0.000000000000000000, 2.047244094488179567 ) ) ;
#46069=VECTOR ( 'NONE', #21731, 39.37007874015748143 ) ;
#46070=CARTESIAN_POINT ( 'NONE',  ( -0.6214413264104952095, 3.267716535433071279, 2.156057715732903491E-16 ) ) ;
#46071=DIRECTION ( 'NONE',  ( 1.734723475976806848E-16, -0.000000000000000000, 1.000000000000000000 ) ) ;
#46072=EDGE_CURVE ( 'NONE', #25893, #31173, #11373, .T. ) ;
#46073=ORIENTED_EDGE ( 'NONE', *, *, #24754, .F. ) ;
#46076=FACE_BOUND ( 'NONE', #5300, .T. ) ;
#46077=VECTOR ( 'NONE', #33879, 39.37007874015748143 ) ;
#46078=VECTOR ( 'NONE', #21820, 39.37007874015748143 ) ;
#46079=LINE ( 'NONE', #11243, #37529 ) ;
#46080=CARTESIAN_POINT ( 'NONE',  ( -0.8942052331142547050, 0.000000000000000000, 0.9448818897637749625 ) ) ;
#46083=ORIENTED_EDGE ( 'NONE', *, *, #30089, .T. ) ;
#46084=PLANE ( 'NONE',  #26523 ) ;
#46085=LINE ( 'NONE', #29856, #20514 ) ;
#46086=PLANE ( 'NONE',  #49923 ) ;
#46091=EDGE_LOOP ( 'NONE', ( #40895, #13858, #18836, #12984 ) ) ;
#46092=LINE ( 'NONE', #10747, #1021 ) ;
#46094=EDGE_LOOP ( 'NONE', ( #38874, #38111, #42570, #2662 ) ) ;
#46096=EDGE_LOOP ( 'NONE', ( #32997, #24448, #36646, #7429, #37530 ) ) ;
#46097=VERTEX_POINT ( 'NONE', #15249 ) ;
#46101=CARTESIAN_POINT ( 'NONE',  ( -0.8182917201112815953, 3.267716535433071279, 1.419509857074482553E-16 ) ) ;
#46102=EDGE_CURVE ( 'NONE', #17882, #46852, #17415, .T. ) ;
#46104=DIRECTION ( 'NONE',  ( 0.000000000000000000, 0.000000000000000000, -1.000000000000000000 ) ) ;
#46105=CARTESIAN_POINT ( 'NONE',  ( 0.4696143004045478797, 3.346456692913386100, 0.5905511811023579360 ) ) ;
#46108=LINE ( 'NONE', #34524, #27250 ) ;
#46109=B_SPLINE_CURVE_WITH_KNOTS ( 'NONE', 3,
 ( #9725, #13343, #17973, #29077 ),
 .UNSPECIFIED., .F., .F.,
 ( 4, 4 ),
 ( 0.05133901200620183403, 0.05249386097095985054 ),
 .UNSPECIFIED. ) ;
#46110=DIRECTION ( 'NONE',  ( -0.000000000000000000, 1.000000000000000000, -0.000000000000000000 ) ) ;
#46112=VERTEX_POINT ( 'NONE', #38251 ) ;
#46114=DIRECTION ( 'NONE',  ( 0.000000000000000000, -1.000000000000000000, 0.000000000000000000 ) ) ;
#46115=DIRECTION ( 'NONE',  ( 1.000000000000000000, 0.000000000000000000, 0.000000000000000000 ) ) ;
#46118=CARTESIAN_POINT ( 'NONE',  ( -1.363819533518803473, 0.000000000000000000, -1.732283464566922726 ) ) ;
#46120=LINE ( 'NONE', #50466, #13319 ) ;
#46121=EDGE_CURVE ( 'NONE', #12444, #44668, #18626, .T. ) ;
#46122=CARTESIAN_POINT ( 'NONE',  ( -1.363819533518803473, 3.346456692913386100, 2.047244094488179567 ) ) ;
#46128=EDGE_CURVE ( 'NONE', #38637, #41521, #46209, .T. ) ;
#46129=CARTESIAN_POINT ( 'NONE',  ( -1.091055626815042645, 3.346456692913386100, -1.259842519685034690 ) ) ;
#46133=LINE ( 'NONE', #22916, #44343 ) ;
#46135=CARTESIAN_POINT ( 'NONE',  ( -0.5455278134075208785, 0.000000000000000000, 1.259842519685033357 ) ) ;
#46137=ORIENTED_EDGE ( 'NONE', *, *, #10327, .T. ) ;
#46138=DIRECTION ( 'NONE',  ( -0.000000000000000000, 1.000000000000000000, -0.000000000000000000 ) ) ;
#46139=VERTEX_POINT ( 'NONE', #18876 ) ;
#46140=ORIENTED_EDGE ( 'NONE', *, *, #33889, .F. ) ;
#46141=LINE ( 'NONE', #38681, #50924 ) ;
#46142=ORIENTED_EDGE ( 'NONE', *, *, #14498, .F. ) ;
#46143=DIRECTION ( 'NONE',  ( 0.000000000000000000, 0.000000000000000000, 1.000000000000000000 ) ) ;
#46147=AXIS2_PLACEMENT_3D ( 'NONE', #16744, #19825, #35592 ) ;
#46149=VECTOR ( 'NONE', #3206, 39.37007874015748143 ) ;
#46151=FACE_OUTER_BOUND ( 'NONE', #35161, .T. ) ;
#46153=ORIENTED_EDGE ( 'NONE', *, *, #15047, .T. ) ;
#46155=FACE_BOUND ( 'NONE', #17811, .T. ) ;
#46157=VECTOR ( 'NONE', #1334, 39.37007874015748143 ) ;
#46158=CARTESIAN_POINT ( 'NONE',  ( 0.000000000000000000, 3.346456692913386100, 0.000000000000000000 ) ) ;
#46161=DIRECTION ( 'NONE',  ( 1.734723475976806848E-16, 0.000000000000000000, 1.000000000000000000 ) ) ;
#46162=CARTESIAN_POINT ( 'NONE',  ( 0.7423782071083085965, 0.000000000000000000, 0.1181102362204701633 ) ) ;
#46164=VERTEX_POINT ( 'NONE', #3371 ) ;
#46166=ADVANCED_FACE ( 'NONE', ( #50551 ), #11873, .F. ) ;
#46167=CARTESIAN_POINT ( 'NONE',  ( -1.909347346926324462, 0.000000000000000000, 0.7874015748031456541 ) ) ;
#46168=EDGE_CURVE ( 'NONE', #24319, #45969, #19359, .T. ) ;
#46169=EDGE_CURVE ( 'NONE', #44079, #45841, #24004, .T. ) ;
#46170=CARTESIAN_POINT ( 'NONE',  ( 1.363819533518803251, 0.000000000000000000, -0.6692913385826764205 ) ) ;
#46173=DIRECTION ( 'NONE',  ( -0.000000000000000000, 0.000000000000000000, 1.000000000000000000 ) ) ;
#46174=CARTESIAN_POINT ( 'NONE',  ( -0.8942052331142547050, 3.346456692913386100, 0.7480314960629874665 ) ) ;
#46175=DIRECTION ( 'NONE',  ( 1.000000000000000000, 0.000000000000000000, -3.469446951953613696E-16 ) ) ;
#46177=DIRECTION ( 'NONE',  ( -1.000000000000000000, 0.000000000000000000, -0.000000000000000000 ) ) ;
#46178=VECTOR ( 'NONE', #44789, 39.37007874015748143 ) ;
#46179=VECTOR ( 'NONE', #48288, 39.37007874015748143 ) ;
#46181=EDGE_CURVE ( 'NONE', #28099, #13566, #16006, .T. ) ;
#46183=ORIENTED_EDGE ( 'NONE', *, *, #43374, .F. ) ;
#46185=CARTESIAN_POINT ( 'NONE',  ( -1.439733046521776583, 0.000000000000000000, -0.9448818897637762948 ) ) ;
#46187=VECTOR ( 'NONE', #510, 39.37007874015748143 ) ;
#46188=ORIENTED_EDGE ( 'NONE', *, *, #18107, .T. ) ;
#46189=ORIENTED_EDGE ( 'NONE', *, *, #27004, .T. ) ;
#46190=FACE_OUTER_BOUND ( 'NONE', #12249, .T. ) ;
#46191=CARTESIAN_POINT ( 'NONE',  ( -1.909347346926324462, 3.346456692913386100, 0.2755905511810996522 ) ) ;
#46194=VERTEX_POINT ( 'NONE', #31503 ) ;
#46195=DIRECTION ( 'NONE',  ( -1.000000000000000000, 0.000000000000000000, 0.000000000000000000 ) ) ;
#46199=FACE_OUTER_BOUND ( 'NONE', #10455, .T. ) ;
#46201=VERTEX_POINT ( 'NONE', #8263 ) ;
#46204=EDGE_LOOP ( 'NONE', ( #50509, #11135, #35560, #14974 ) ) ;
#46205=ORIENTED_EDGE ( 'NONE', *, *, #1727, .T. ) ;
#46206=EDGE_CURVE ( 'NONE', #17928, #10946, #43362, .T. ) ;
#46208=CARTESIAN_POINT ( 'NONE',  ( 1.091055626815043311, 3.346456692913386100, 1.801691980386208591 ) ) ;
#46209=LINE ( 'NONE', #6999, #18247 ) ;
#46210=CARTESIAN_POINT ( 'NONE',  ( 0.2727639067037604947, 3.346456692913386100, -1.417322834645664331 ) ) ;
#46211=EDGE_CURVE ( 'NONE', #15045, #12815, #31256, .T. ) ;
#46212=VECTOR ( 'NONE', #4112, 39.37007874015748143 ) ;
#46213=ORIENTED_EDGE ( 'NONE', *, *, #5639, .F. ) ;
#46216=CARTESIAN_POINT ( 'NONE',  ( -0.8182917201112819283, 0.000000000000000000, -0.7874015748031467643 ) ) ;
#46217=LINE ( 'NONE', #37499, #6373 ) ;
#46218=ORIENTED_EDGE ( 'NONE', *, *, #50051, .F. ) ;
#46219=CARTESIAN_POINT ( 'NONE',  ( 0.000000000000000000, 3.346456692913386100, 0.000000000000000000 ) ) ;
#46220=ORIENTED_EDGE ( 'NONE', *, *, #48688, .F. ) ;
#46221=ORIENTED_EDGE ( 'NONE', *, *, #2556, .F. ) ;
#46223=CARTESIAN_POINT ( 'NONE',  ( -3.927031490892378253E-16, 3.346456692913386100, -1.889763779527552146 ) ) ;
#46224=EDGE_CURVE ( 'NONE', #49325, #35993, #32023, .T. ) ;
#46225=CARTESIAN_POINT ( 'NONE',  ( -0.8182917201112819283, 3.346456692913386100, -1.417322834645664331 ) ) ;
#46228=EDGE_CURVE ( 'NONE', #45803, #50682, #47461, .T. ) ;
#46230=ORIENTED_EDGE ( 'NONE', *, *, #684, .F. ) ;
#46231=ORIENTED_EDGE ( 'NONE', *, *, #8959, .T. ) ;
#46233=CARTESIAN_POINT ( 'NONE',  ( -0.5455278134075209895, 3.267716535433071279, 9.463399047163218249E-17 ) ) ;
#46236=DIRECTION ( 'NONE',  ( 1.000000000000000000, 0.000000000000000000, 0.000000000000000000 ) ) ;
#46239=LINE ( 'NONE', #50833, #7269 ) ;
#46240=VERTEX_POINT ( 'NONE', #12649 ) ;
#46242=CARTESIAN_POINT ( 'NONE',  ( -1.334208625815133553, 3.267716535433071279, 2.047244094488179567 ) ) ;
#46244=FACE_OUTER_BOUND ( 'NONE', #18153, .T. ) ;
#46247=PLANE ( 'NONE',  #19913 ) ;
#46248=AXIS2_PLACEMENT_3D ( 'NONE', #25348, #41607, #37745 ) ;
#46249=CARTESIAN_POINT ( 'NONE',  ( -1.712496953225537188, 3.346456692913386100, 1.102362204724404160 ) ) ;
#46251=VERTEX_POINT ( 'NONE', #251 ) ;
#46252=EDGE_CURVE ( 'NONE', #37178, #38637, #12136, .T. ) ;
#46254=VECTOR ( 'NONE', #2381, 39.37007874015748143 ) ;
#46256=DIRECTION ( 'NONE',  ( 0.000000000000000000, 0.000000000000000000, -1.000000000000000000 ) ) ;
#46258=ORIENTED_EDGE ( 'NONE', *, *, #2825, .T. ) ;
#46259=CARTESIAN_POINT ( 'NONE',  ( 1.833433833923351353, 3.346456692913386100, 0.3149606299212576177 ) ) ;
#46260=EDGE_CURVE ( 'NONE', #2462, #34201, #20120, .T. ) ;
#46261=VECTOR ( 'NONE', #1195, 39.37007874015748143 ) ;
#46264=DIRECTION ( 'NONE',  ( 0.000000000000000000, 0.000000000000000000, -1.000000000000000000 ) ) ;
#46265=EDGE_CURVE ( 'NONE', #37644, #3939, #12389, .T. ) ;
#46266=EDGE_CURVE ( 'NONE', #32732, #20175, #43869, .T. ) ;
#46267=ORIENTED_EDGE ( 'NONE', *, *, #255, .T. ) ;
#46268=VERTEX_POINT ( 'NONE', #38991 ) ;
#46269=ORIENTED_EDGE ( 'NONE', *, *, #15896, .F. ) ;
#46270=LINE ( 'NONE', #23055, #20785 ) ;
#46271=CARTESIAN_POINT ( 'NONE',  ( -6.488138984952638702E-17, 3.267716535433071279, 1.125512701259767226E-32 ) ) ;
#46272=ORIENTED_EDGE ( 'NONE', *, *, #8449, .F. ) ;
#46273=DIRECTION ( 'NONE',  ( 1.734723475976806848E-16, 0.000000000000000000, 1.000000000000000000 ) ) ;
#46274=CARTESIAN_POINT ( 'NONE',  ( 0.4696143004045476577, 3.346456692913386100, -1.732283464566922726 ) ) ;
#46276=ORIENTED_EDGE ( 'NONE', *, *, #30990, .T. ) ;
#46277=ORIENTED_EDGE ( 'NONE', *, *, #26058, .T. ) ;
#46278=CARTESIAN_POINT ( 'NONE',  ( 1.833433833923351353, 0.000000000000000000, -1.161035397307311917E-15 ) ) ;
#46279=DIRECTION ( 'NONE',  ( 1.734723475976806848E-16, 0.000000000000000000, 1.000000000000000000 ) ) ;
#46280=CARTESIAN_POINT ( 'NONE',  ( -0.2727639067037602727, 3.346456692913386100, 1.850393700787392293 ) ) ;
#46281=EDGE_LOOP ( 'NONE', ( #4618, #26448, #7311, #19873 ) ) ;
#46282=CARTESIAN_POINT ( 'NONE',  ( 0.7423782071083092626, 0.000000000000000000, 1.889763779527550369 ) ) ;
#46283=FACE_BOUND ( 'NONE', #35181, .T. ) ;
#46284=ORIENTED_EDGE ( 'NONE', *, *, #40679, .T. ) ;
#46285=CARTESIAN_POINT ( 'NONE',  ( 0.000000000000000000, 3.267716535433071279, 0.5905511811023582691 ) ) ;
#46287=ORIENTED_EDGE ( 'NONE', *, *, #28992, .T. ) ;
#46288=CARTESIAN_POINT ( 'NONE',  ( -0.8182917201112819283, 3.267716535433071279, -0.03937007874015895081 ) ) ;
#46290=VECTOR ( 'NONE', #10468, 39.37007874015748143 ) ;
#46292=DIRECTION ( 'NONE',  ( 1.000000000000000000, 0.000000000000000000, 0.000000000000000000 ) ) ;
#46293=VECTOR ( 'NONE', #21810, 39.37007874015748143 ) ;
#46294=DIRECTION ( 'NONE',  ( -1.000000000000000000, 0.000000000000000000, 0.000000000000000000 ) ) ;
#46295=EDGE_CURVE ( 'NONE', #129, #19452, #11620, .T. ) ;
#46297=CARTESIAN_POINT ( 'NONE',  ( 1.560669927219590525, 0.000000000000000000, 1.220472440944875281 ) ) ;
#46298=ORIENTED_EDGE ( 'NONE', *, *, #9890, .T. ) ;
#46302=ORIENTED_EDGE ( 'NONE', *, *, #11042, .F. ) ;
#46304=LINE ( 'NONE', #26700, #6153 ) ;
#46306=CARTESIAN_POINT ( 'NONE',  ( 1.363819533518803251, 0.000000000000000000, 0.9055118110236164419 ) ) ;
#46307=FACE_OUTER_BOUND ( 'NONE', #4355, .T. ) ;
#46308=CARTESIAN_POINT ( 'NONE',  ( 2.182111253630085290, 0.000000000000000000, -0.1968503937007886062 ) ) ;
#46313=LINE ( 'NONE', #30599, #48716 ) ;
#46314=CARTESIAN_POINT ( 'NONE',  ( -1.363819533518803029, 3.346456692913386100, -0.03937007874015868020 ) ) ;
#46315=DIRECTION ( 'NONE',  ( -0.000000000000000000, 0.000000000000000000, 1.000000000000000000 ) ) ;
#46316=DIRECTION ( 'NONE',  ( 1.000000000000000000, -0.000000000000000000, 0.000000000000000000 ) ) ;
#46318=DIRECTION ( 'NONE',  ( 1.734723475976806848E-16, -0.000000000000000000, 1.000000000000000000 ) ) ;
#46319=ORIENTED_EDGE ( 'NONE', *, *, #24426, .F. ) ;
#46320=DIRECTION ( 'NONE',  ( -1.000000000000000000, 0.000000000000000000, 0.000000000000000000 ) ) ;
#46322=FACE_BOUND ( 'NONE', #40395, .T. ) ;
#46325=DIRECTION ( 'NONE',  ( -1.000000000000000000, -0.000000000000000000, -0.000000000000000000 ) ) ;
#46327=EDGE_CURVE ( 'NONE', #24863, #3256, #17045, .T. ) ;
#46328=VECTOR ( 'NONE', #42910, 39.37007874015748143 ) ;
#46331=DIRECTION ( 'NONE',  ( 1.000000000000000000, 0.000000000000000000, 0.000000000000000000 ) ) ;
#46334=CARTESIAN_POINT ( 'NONE',  ( -1.636583440222563635, 3.346456692913386100, 0.1181102362204704270 ) ) ;
#46335=CARTESIAN_POINT ( 'NONE',  ( 0.7423782071083087075, 3.346456692913386100, -0.9448818897637765168 ) ) ;
#46336=CARTESIAN_POINT ( 'NONE',  ( -1.862188077367287642, 3.346456692913386100, -0.9842519685039344823 ) ) ;
#46338=AXIS2_PLACEMENT_3D ( 'NONE', #24047, #37213, #41086 ) ;
#46340=ORIENTED_EDGE ( 'NONE', *, *, #44447, .F. ) ;
#46341=DIRECTION ( 'NONE',  ( -0.000000000000000000, 1.000000000000000000, -0.000000000000000000 ) ) ;
#46342=LINE ( 'NONE', #30378, #31425 ) ;
#46343=EDGE_LOOP ( 'NONE', ( #40860, #37690, #38826, #19808 ) ) ;
#46346=ORIENTED_EDGE ( 'NONE', *, *, #5355, .F. ) ;
#46348=ADVANCED_FACE ( 'NONE', ( #33056 ), #16787, .F. ) ;
#46349=EDGE_LOOP ( 'NONE', ( #3328, #22424, #5944, #14984 ) ) ;
#46351=CARTESIAN_POINT ( 'NONE',  ( 0.000000000000000000, 3.267716535433071279, 0.4724409448818868706 ) ) ;
#46352=EDGE_CURVE ( 'NONE', #42837, #7418, #17798, .T. ) ;
#46354=LINE ( 'NONE', #47100, #22160 ) ;
#46356=VECTOR ( 'NONE', #16792, 39.37007874015748143 ) ;
#46357=DIRECTION ( 'NONE',  ( 1.000000000000000000, 0.000000000000000000, 0.000000000000000000 ) ) ;
#46358=VECTOR ( 'NONE', #45836, 39.37007874015748143 ) ;
#46359=LINE ( 'NONE', #30901, #44286 ) ;
#46361=EDGE_LOOP ( 'NONE', ( #19381, #29477, #18159, #41397 ) ) ;
#46367=VECTOR ( 'NONE', #48193, 39.37007874015748143 ) ;
#46368=VECTOR ( 'NONE', #50027, 39.37007874015748143 ) ;
#46369=ORIENTED_EDGE ( 'NONE', *, *, #42170, .F. ) ;
#46370=LINE ( 'NONE', #19023, #8368 ) ;
#46371=LINE ( 'NONE', #14909, #7144 ) ;
#46373=CARTESIAN_POINT ( 'NONE',  ( 0.1968503937007872462, 3.267716535433071279, -1.141732283464564013 ) ) ;
#46376=VERTEX_POINT ( 'NONE', #28898 ) ;
#46380=CARTESIAN_POINT ( 'NONE',  ( 1.636583440222563857, 3.267716535433071279, -1.161035397307311917E-15 ) ) ;
#46381=DIRECTION ( 'NONE',  ( 1.000000000000000000, 0.000000000000000000, 0.000000000000000000 ) ) ;
#46383=LINE ( 'NONE', #26788, #20572 ) ;
#46384=EDGE_CURVE ( 'NONE', #48435, #3807, #12914, .T. ) ;
#46386=VERTEX_POINT ( 'NONE', #9033 ) ;
#46387=EDGE_CURVE ( 'NONE', #11755, #9111, #33308, .T. ) ;
#46388=DIRECTION ( 'NONE',  ( 1.000000000000000000, 0.000000000000000000, -3.469446951953613696E-16 ) ) ;
#46389=ORIENTED_EDGE ( 'NONE', *, *, #41954, .T. ) ;
#46390=DIRECTION ( 'NONE',  ( -0.000000000000000000, 1.000000000000000000, -0.000000000000000000 ) ) ;
#46391=DIRECTION ( 'NONE',  ( 0.000000000000000000, 0.000000000000000000, 1.000000000000000000 ) ) ;
#46392=ORIENTED_EDGE ( 'NONE', *, *, #2415, .T. ) ;
#46393=ADVANCED_FACE ( 'NONE', ( #48993 ), #9288, .F. ) ;
#46394=CARTESIAN_POINT ( 'NONE',  ( 0.4696143004045479352, 3.346456692913386100, 0.7874015748031454320 ) ) ;
#46395=LINE ( 'NONE', #42548, #43052 ) ;
#46396=AXIS2_PLACEMENT_3D ( 'NONE', #42922, #15573, #46279 ) ;
#46398=ORIENTED_EDGE ( 'NONE', *, *, #13481, .T. ) ;
#46400=DIRECTION ( 'NONE',  ( 1.734723475976806848E-16, 0.000000000000000000, 1.000000000000000000 ) ) ;
#46401=FACE_BOUND ( 'NONE', #41528, .T. ) ;
#46403=VECTOR ( 'NONE', #41820, 39.37007874015748143 ) ;
#46405=LINE ( 'NONE', #22690, #12179 ) ;
#46406=EDGE_CURVE ( 'NONE', #44433, #31184, #5154, .T. ) ;
#46407=ORIENTED_EDGE ( 'NONE', *, *, #37705, .F. ) ;
#46410=CARTESIAN_POINT ( 'NONE',  ( 0.000000000000000000, 3.267716535433071279, 1.102362204724404160 ) ) ;
#46412=VERTEX_POINT ( 'NONE', #2053 ) ;
#46413=CARTESIAN_POINT ( 'NONE',  ( 1.287906020515830141, 3.346456692913386100, -0.9448818897637765168 ) ) ;
#46414=ORIENTED_EDGE ( 'NONE', *, *, #45485, .T. ) ;
#46415=CARTESIAN_POINT ( 'NONE',  ( -1.439733046521776139, 0.000000000000000000, 0.6299212598425164567 ) ) ;
#46416=CARTESIAN_POINT ( 'NONE',  ( -1.636583440222563635, 0.000000000000000000, 0.4330708661417290162 ) ) ;
#46417=LINE ( 'NONE', #46170, #23908 ) ;
#46419=VERTEX_POINT ( 'NONE', #5414 ) ;
#46421=CARTESIAN_POINT ( 'NONE',  ( -1.985260859929297572, 3.346456692913386100, 0.9448818897637749625 ) ) ;
#46423=EDGE_CURVE ( 'NONE', #11518, #27975, #4902, .T. ) ;
#46424=CARTESIAN_POINT ( 'NONE',  ( -1.195183497228115035E-16, 3.267716535433071279, -0.6299212598425177889 ) ) ;
#46427=DIRECTION ( 'NONE',  ( -1.000000000000000000, 0.000000000000000000, 0.000000000000000000 ) ) ;
#46428=VECTOR ( 'NONE', #9864, 39.37007874015748143 ) ;
#46429=ORIENTED_EDGE ( 'NONE', *, *, #39764, .F. ) ;
#46430=DIRECTION ( 'NONE',  ( -0.000000000000000000, 1.000000000000000000, -0.000000000000000000 ) ) ;
#46432=VECTOR ( 'NONE', #30603, 39.37007874015748143 ) ;
#46433=ORIENTED_EDGE ( 'NONE', *, *, #12441, .F. ) ;
#46434=VECTOR ( 'NONE', #23882, 39.37007874015748143 ) ;
#46435=ORIENTED_EDGE ( 'NONE', *, *, #3340, .T. ) ;
#46438=VECTOR ( 'NONE', #17633, 39.37007874015748143 ) ;
#46441=VERTEX_POINT ( 'NONE', #29156 ) ;
#46445=DIRECTION ( 'NONE',  ( -1.000000000000000000, -0.000000000000000000, -0.000000000000000000 ) ) ;
#46446=ORIENTED_EDGE ( 'NONE', *, *, #33052, .F. ) ;
#46448=FACE_OUTER_BOUND ( 'NONE', #40570, .T. ) ;
#46449=CARTESIAN_POINT ( 'NONE',  ( -0.8182917201112818173, 3.267716535433071279, 1.419509857074483292E-16 ) ) ;
#46451=EDGE_CURVE ( 'NONE', #2129, #38287, #21933, .T. ) ;
#46452=ORIENTED_EDGE ( 'NONE', *, *, #46252, .F. ) ;
#46455=ORIENTED_EDGE ( 'NONE', *, *, #41479, .T. ) ;
#46456=CARTESIAN_POINT ( 'NONE',  ( -1.363819533518803473, 3.346456692913386100, 1.605145679676863057 ) ) ;
#46458=DIRECTION ( 'NONE',  ( 1.000000000000000000, -0.000000000000000000, 0.000000000000000000 ) ) ;
#46459=ORIENTED_EDGE ( 'NONE', *, *, #46260, .F. ) ;
#46460=DIRECTION ( 'NONE',  ( -1.000000000000000000, 0.000000000000000000, -0.000000000000000000 ) ) ;
#46462=FACE_OUTER_BOUND ( 'NONE', #20634, .T. ) ;
#46463=VERTEX_POINT ( 'NONE', #22687 ) ;
#46464=LINE ( 'NONE', #46957, #43826 ) ;
#46465=AXIS2_PLACEMENT_3D ( 'NONE', #10311, #6184, #2566 ) ;
#46467=EDGE_CURVE ( 'NONE', #48458, #2485, #2816, .T. ) ;
#46469=VECTOR ( 'NONE', #21651, 39.37007874015748143 ) ;
#46470=EDGE_LOOP ( 'NONE', ( #39005, #28521, #46844, #29925 ) ) ;
#46471=VECTOR ( 'NONE', #43720, 39.37007874015748143 ) ;
#46473=VECTOR ( 'NONE', #34349, 39.37007874015748143 ) ;
#46474=PLANE ( 'NONE',  #20026 ) ;
#46475=EDGE_CURVE ( 'NONE', #29709, #43175, #38196, .T. ) ;
#46476=CARTESIAN_POINT ( 'NONE',  ( 1.015142113812069757, 3.267716535433071279, -3.521981712565033375E-16 ) ) ;
#46478=ORIENTED_EDGE ( 'NONE', *, *, #1847, .F. ) ;
#46479=ORIENTED_EDGE ( 'NONE', *, *, #39354, .T. ) ;
#46480=CARTESIAN_POINT ( 'NONE',  ( -1.166969139818015533, 3.267716535433071279, 0.1574803149606287811 ) ) ;
#46481=CARTESIAN_POINT ( 'NONE',  ( 1.363819533518803251, 0.000000000000000000, 0.4724409448818871482 ) ) ;
#46482=VERTEX_POINT ( 'NONE', #30687 ) ;
#46484=ADVANCED_FACE ( 'NONE', ( #6437 ), #18306, .F. ) ;
#46487=CARTESIAN_POINT ( 'NONE',  ( 1.091055626815042645, 0.000000000000000000, 0.9448818897637746295 ) ) ;
#46489=ORIENTED_EDGE ( 'NONE', *, *, #37710, .T. ) ;
#46492=EDGE_CURVE ( 'NONE', #49974, #23541, #34812, .T. ) ;
#46493=CARTESIAN_POINT ( 'NONE',  ( -0.8942052331142552601, 3.346456692913386100, -1.141732283464563569 ) ) ;
#46495=CARTESIAN_POINT ( 'NONE',  ( -1.166969139818015533, 0.000000000000000000, 0.1574803149606287811 ) ) ;
#46496=CARTESIAN_POINT ( 'NONE',  ( -1.439733046521776139, 3.346456692913386100, 0.3149606299212578953 ) ) ;
#46498=ORIENTED_EDGE ( 'NONE', *, *, #27240, .F. ) ;
#46502=ORIENTED_EDGE ( 'NONE', *, *, #38718, .F. ) ;
#46503=AXIS2_PLACEMENT_3D ( 'NONE', #28825, #32724, #44559 ) ;
#46505=ORIENTED_EDGE ( 'NONE', *, *, #29716, .F. ) ;
#46506=CARTESIAN_POINT ( 'NONE',  ( 0.5455278134075217666, 3.267716535433071279, 1.259842519685033357 ) ) ;
#46507=VECTOR ( 'NONE', #36384, 39.37007874015748143 ) ;
#46508=ORIENTED_EDGE ( 'NONE', *, *, #42151, .F. ) ;
#46513=DIRECTION ( 'NONE',  ( 0.000000000000000000, 0.000000000000000000, -1.000000000000000000 ) ) ;
#46514=ADVANCED_FACE ( 'NONE', ( #34062 ), #34321, .F. ) ;
#46516=ORIENTED_EDGE ( 'NONE', *, *, #46571, .T. ) ;
#46517=ORIENTED_EDGE ( 'NONE', *, *, #7563, .F. ) ;
#46519=DIRECTION ( 'NONE',  ( 0.000000000000000000, -0.9063077870366510469, -0.4226182617406972208 ) ) ;
#46520=ORIENTED_EDGE ( 'NONE', *, *, #50818, .F. ) ;
#46521=CARTESIAN_POINT ( 'NONE',  ( 0.2727639067037610499, 3.346456692913386100, 2.047244094488179567 ) ) ;
#46522=CARTESIAN_POINT ( 'NONE',  ( -0.8182917201112819283, 3.346456692913386100, -2.244094488188968395 ) ) ;
#46523=PLANE ( 'NONE',  #49962 ) ;
#46525=EDGE_LOOP ( 'NONE', ( #2728, #39174, #7579, #40379 ) ) ;
#46526=LINE ( 'NONE', #11947, #2394 ) ;
#46528=FACE_OUTER_BOUND ( 'NONE', #16984, .T. ) ;
#46530=( NAMED_UNIT ( * ) SI_UNIT ( $, .STERADIAN. ) SOLID_ANGLE_UNIT ( ) );
#46531=DIRECTION ( 'NONE',  ( -3.469446951953613696E-16, 0.000000000000000000, -1.000000000000000000 ) ) ;
#46532=VERTEX_POINT ( 'NONE', #30440 ) ;
#46534=ORIENTED_EDGE ( 'NONE', *, *, #35532, .F. ) ;
#46535=ORIENTED_EDGE ( 'NONE', *, *, #6058, .T. ) ;
#46536=DIRECTION ( 'NONE',  ( -0.000000000000000000, 1.000000000000000000, -0.000000000000000000 ) ) ;
#46537=DIRECTION ( 'NONE',  ( -0.000000000000000000, 1.000000000000000000, -0.000000000000000000 ) ) ;
#46538=DIRECTION ( 'NONE',  ( -3.469446951953613696E-16, 0.000000000000000000, -1.000000000000000000 ) ) ;
#46542=ORIENTED_EDGE ( 'NONE', *, *, #6158, .T. ) ;
#46546=LINE ( 'NONE', #26948, #43384 ) ;
#46549=AXIS2_PLACEMENT_3D ( 'NONE', #32141, #8890, #23610 ) ;
#46550=EDGE_CURVE ( 'NONE', #33305, #11733, #19056, .T. ) ;
#46551=EDGE_CURVE ( 'NONE', #6600, #46139, #13932, .T. ) ;
#46552=DIRECTION ( 'NONE',  ( -3.469446951953613696E-16, 0.000000000000000000, -1.000000000000000000 ) ) ;
#46554=VECTOR ( 'NONE', #15429, 39.37007874015748143 ) ;
#46555=ORIENTED_EDGE ( 'NONE', *, *, #9698, .F. ) ;
#46556=CARTESIAN_POINT ( 'NONE',  ( -0.6214413264104945434, 3.346456692913386100, 1.850393700787391849 ) ) ;
#46557=EDGE_CURVE ( 'NONE', #42496, #4027, #22438, .T. ) ;
#46560=ORIENTED_EDGE ( 'NONE', *, *, #31613, .T. ) ;
#46561=FACE_OUTER_BOUND ( 'NONE', #38988, .T. ) ;
#46562=DIRECTION ( 'NONE',  ( -1.000000000000000000, 0.000000000000000000, 1.734723475976806848E-16 ) ) ;
#46564=DIRECTION ( 'NONE',  ( -0.000000000000000000, 1.000000000000000000, -0.000000000000000000 ) ) ;
#46567=VERTEX_POINT ( 'NONE', #43044 ) ;
#46568=LINE ( 'NONE', #30099, #32942 ) ;
#46571=EDGE_CURVE ( 'NONE', #45040, #31775, #23183, .T. ) ;
#46572=DIRECTION ( 'NONE',  ( -3.469446951953613696E-16, 0.000000000000000000, -1.000000000000000000 ) ) ;
#46573=FACE_OUTER_BOUND ( 'NONE', #35977, .T. ) ;
#46574=EDGE_CURVE ( 'NONE', #17100, #8967, #31449, .T. ) ;
#46575=ORIENTED_EDGE ( 'NONE', *, *, #10574, .T. ) ;
#46576=ORIENTED_EDGE ( 'NONE', *, *, #8696, .F. ) ;
#46578=CIRCLE ( 'NONE', #27646, 2.165354330708661568 ) ;
#46584=CARTESIAN_POINT ( 'NONE',  ( 0.1968503937007878568, 3.267716535433071279, 1.574803149606291974 ) ) ;
#46589=CARTESIAN_POINT ( 'NONE',  ( 1.363819533518803251, 3.267716535433071279, 0.1574803149606283648 ) ) ;
#46594=EDGE_LOOP ( 'NONE', ( #11297, #2355, #118, #10609 ) ) ;
#46595=EDGE_LOOP ( 'NONE', ( #36486, #2642, #1045, #11121 ) ) ;
#46596=EDGE_LOOP ( 'NONE', ( #18927, #10067, #15304, #45655 ) ) ;
#46597=ORIENTED_EDGE ( 'NONE', *, *, #50257, .T. ) ;
#46600=CARTESIAN_POINT ( 'NONE',  ( 0.8182917201112819283, 0.000000000000000000, -0.1574803149606301411 ) ) ;
#46603=EDGE_CURVE ( 'NONE', #37684, #4024, #38937, .T. ) ;
#46605=ADVANCED_FACE ( 'NONE', ( #7446 ), #27305, .F. ) ;
#46607=EDGE_CURVE ( 'NONE', #18135, #448, #35069, .T. ) ;
#46608=DIRECTION ( 'NONE',  ( -1.000000000000000000, 0.000000000000000000, -0.000000000000000000 ) ) ;
#46611=ORIENTED_EDGE ( 'NONE', *, *, #4614, .F. ) ;
#46612=CARTESIAN_POINT ( 'NONE',  ( 1.363819533518803251, 3.346456692913386100, 1.417322834645662777 ) ) ;
#46613=CARTESIAN_POINT ( 'NONE',  ( 0.000000000000000000, 3.267716535433071279, -1.141732283464564013 ) ) ;
#46615=LINE ( 'NONE', #27013, #3750 ) ;
#46616=VECTOR ( 'NONE', #10493, 39.37007874015748143 ) ;
#46618=ORIENTED_EDGE ( 'NONE', *, *, #4041, .F. ) ;
#46619=FACE_OUTER_BOUND ( 'NONE', #2146, .T. ) ;
#46620=CARTESIAN_POINT ( 'NONE',  ( 0.2727639067037603837, 3.267716535433071279, -4.731699523581606660E-17 ) ) ;
#46621=EDGE_LOOP ( 'NONE', ( #31570, #40573, #30385, #15974 ) ) ;
#46622=CARTESIAN_POINT ( 'NONE',  ( 1.287906020515829919, 0.000000000000000000, -1.259842519685035134 ) ) ;
#46625=PRODUCT_DEFINITION_SHAPE ( 'NONE', 'NONE',  #47367 ) ;
#46626=LINE ( 'NONE', #34541, #4311 ) ;
#46627=ADVANCED_FACE ( 'NONE', ( #11318 ), #47660, .F. ) ;
#46629=CARTESIAN_POINT ( 'NONE',  ( -0.2727639067037611054, 3.346456692913386100, -2.244094488188968395 ) ) ;
#46630=LINE ( 'NONE', #42781, #33366 ) ;
#46632=EDGE_CURVE ( 'NONE', #6627, #19810, #15448, .T. ) ;
#46635=ORIENTED_EDGE ( 'NONE', *, *, #49959, .F. ) ;
#46636=ADVANCED_FACE ( 'NONE', ( #43813 ), #3568, .F. ) ;
#46637=VERTEX_POINT ( 'NONE', #39700 ) ;
#46639=LINE ( 'NONE', #3557, #3965 ) ;
#46641=EDGE_LOOP ( 'NONE', ( #47725, #31584, #21508, #9427 ) ) ;
#46643=CARTESIAN_POINT ( 'NONE',  ( 1.636583440222563857, 0.000000000000000000, 0.3149606299212576177 ) ) ;
#46645=LINE ( 'NONE', #15685, #39616 ) ;
#46647=AXIS2_PLACEMENT_3D ( 'NONE', #11718, #4227, #3980 ) ;
#46649=ORIENTED_EDGE ( 'NONE', *, *, #37125, .T. ) ;
#46650=ORIENTED_EDGE ( 'NONE', *, *, #13060, .T. ) ;
#46653=FACE_BOUND ( 'NONE', #2929, .T. ) ;
#46654=VERTEX_POINT ( 'NONE', #27562 ) ;
#46655=VECTOR ( 'NONE', #14559, 39.37007874015748143 ) ;
#46656=DIRECTION ( 'NONE',  ( 1.000000000000000000, 0.000000000000000000, 0.000000000000000000 ) ) ;
#46657=VERTEX_POINT ( 'NONE', #12080 ) ;
#46659=CARTESIAN_POINT ( 'NONE',  ( 0.000000000000000000, 3.267716535433071279, 0.4724409448818868706 ) ) ;
#46663=CARTESIAN_POINT ( 'NONE',  ( 1.441853549388196321, 3.346456692913386100, 1.535433070866133898 ) ) ;
#46665=DIRECTION ( 'NONE',  ( 0.000000000000000000, -1.000000000000000000, 0.000000000000000000 ) ) ;
#46668=ORIENTED_EDGE ( 'NONE', *, *, #22868, .T. ) ;
#46669=VERTEX_POINT ( 'NONE', #23433 ) ;
#46671=DIRECTION ( 'NONE',  ( 1.734723475976806848E-16, -0.000000000000000000, 1.000000000000000000 ) ) ;
#46673=EDGE_CURVE ( 'NONE', #48909, #47245, #51002, .T. ) ;
#46675=CARTESIAN_POINT ( 'NONE',  ( -0.5455278134075214336, 0.000000000000000000, -1.259842519685035134 ) ) ;
#46676=EDGE_CURVE ( 'NONE', #37350, #2462, #20332, .T. ) ;
#46677=DIRECTION ( 'NONE',  ( -3.469446951953613696E-16, 0.000000000000000000, -1.000000000000000000 ) ) ;
#46679=VECTOR ( 'NONE', #36572, 39.37007874015748143 ) ;
#46680=DIRECTION ( 'NONE',  ( -0.000000000000000000, 0.000000000000000000, 1.000000000000000000 ) ) ;
#46681=ORIENTED_EDGE ( 'NONE', *, *, #46327, .T. ) ;
#46682=VECTOR ( 'NONE', #33262, 39.37007874015748143 ) ;
#46683=FACE_OUTER_BOUND ( 'NONE', #44954, .T. ) ;
#46684=VECTOR ( 'NONE', #864, 39.37007874015748143 ) ;
#46687=CARTESIAN_POINT ( 'NONE',  ( -1.794796351285541602, 3.267716535433071279, -1.102362204724405492 ) ) ;
#46688=LINE ( 'NONE', #11358, #33614 ) ;
#46690=VECTOR ( 'NONE', #18197, 39.37007874015748143 ) ;
#46692=CIRCLE ( 'NONE', #34364, 2.106299212598425008 ) ;
#46693=CARTESIAN_POINT ( 'NONE',  ( 0.7423782071083084855, 3.346456692913386100, -2.034117492951036166 ) ) ;
#46694=EDGE_CURVE ( 'NONE', #19694, #35070, #195, .T. ) ;
#46698=DIRECTION ( 'NONE',  ( 1.734723475976806848E-16, -0.000000000000000000, 1.000000000000000000 ) ) ;
#46701=CARTESIAN_POINT ( 'NONE',  ( -0.2727639067037607723, 0.000000000000000000, -1.417322834645664331 ) ) ;
#46704=LINE ( 'NONE', #38748, #30109 ) ;
#46707=ORIENTED_EDGE ( 'NONE', *, *, #46168, .F. ) ;
#46708=CARTESIAN_POINT ( 'NONE',  ( -1.536664496436148184E-16, 3.346456692913386100, -0.8267716535433052849 ) ) ;
#46711=ORIENTED_EDGE ( 'NONE', *, *, #16053, .F. ) ;
#46712=LINE ( 'NONE', #32033, #49623 ) ;
#46713=AXIS2_PLACEMENT_3D ( 'NONE', #40180, #28287, #12813 ) ;
#46714=ORIENTED_EDGE ( 'NONE', *, *, #46008, .T. ) ;
#46715=ORIENTED_EDGE ( 'NONE', *, *, #35483, .F. ) ;
#46719=LINE ( 'NONE', #3898, #50612 ) ;
#46725=EDGE_CURVE ( 'NONE', #12822, #26233, #23694, .T. ) ;
#46726=DIRECTION ( 'NONE',  ( 1.000000000000000000, 0.000000000000000000, -3.469446951953613696E-16 ) ) ;
#46727=EDGE_CURVE ( 'NONE', #23227, #39081, #27327, .T. ) ;
#46729=VECTOR ( 'NONE', #30713, 39.37007874015748143 ) ;
#46731=DIRECTION ( 'NONE',  ( -3.469446951953613696E-16, 0.000000000000000000, -1.000000000000000000 ) ) ;
#46734=ADVANCED_FACE ( 'NONE', ( #44577 ), #9487, .F. ) ;
#46735=DIRECTION ( 'NONE',  ( 1.000000000000000000, 0.000000000000000000, 0.000000000000000000 ) ) ;
#46737=DIRECTION ( 'NONE',  ( 1.734723475976806848E-16, -0.000000000000000000, 1.000000000000000000 ) ) ;
#46739=DIRECTION ( 'NONE',  ( 1.000000000000000000, 0.000000000000000000, 0.000000000000000000 ) ) ;
#46743=PLANE ( 'NONE',  #27832 ) ;
#46745=DIRECTION ( 'NONE',  ( 0.000000000000000000, 0.000000000000000000, -1.000000000000000000 ) ) ;
#46746=AXIS2_PLACEMENT_3D ( 'NONE', #14568, #11196, #7328 ) ;
#46747=VERTEX_POINT ( 'NONE', #25479 ) ;
#46749=ADVANCED_FACE ( 'NONE', ( #4850 ), #5862, .F. ) ;
#46751=CARTESIAN_POINT ( 'NONE',  ( -1.636583440222563635, 0.000000000000000000, -0.1968503937007879123 ) ) ;
#46752=ORIENTED_EDGE ( 'NONE', *, *, #627, .T. ) ;
#46753=DIRECTION ( 'NONE',  ( 1.734723475976806848E-16, -0.000000000000000000, 1.000000000000000000 ) ) ;
#46754=VERTEX_POINT ( 'NONE', #24472 ) ;
#46756=PLANE ( 'NONE',  #4939 ) ;
#46757=CARTESIAN_POINT ( 'NONE',  ( -1.363819533518803473, 0.000000000000000000, -1.929133858267710000 ) ) ;
#46758=EDGE_CURVE ( 'NONE', #44234, #40389, #10866, .T. ) ;
#46759=ORIENTED_EDGE ( 'NONE', *, *, #8261, .F. ) ;
#46760=VERTEX_POINT ( 'NONE', #717 ) ;
#46761=ORIENTED_EDGE ( 'NONE', *, *, #39947, .F. ) ;
#46763=CARTESIAN_POINT ( 'NONE',  ( -0.2727639067037611054, 3.267716535433071279, -2.148105963102950877 ) ) ;
#46767=PLANE ( 'NONE',  #28549 ) ;
#46768=DIRECTION ( 'NONE',  ( 1.000000000000000000, 0.000000000000000000, 0.000000000000000000 ) ) ;
#46769=AXIS2_PLACEMENT_3D ( 'NONE', #19519, #11777, #36051 ) ;
#46771=ORIENTED_EDGE ( 'NONE', *, *, #47765, .F. ) ;
#46772=EDGE_LOOP ( 'NONE', ( #29126, #43674, #48672, #25580 ) ) ;
#46773=DIRECTION ( 'NONE',  ( -1.000000000000000000, -0.000000000000000000, -0.000000000000000000 ) ) ;
#46775=CARTESIAN_POINT ( 'NONE',  ( -0.5455278134075214336, 3.267716535433071279, -0.5118110236220467790 ) ) ;
#46776=VERTEX_POINT ( 'NONE', #47916 ) ;
#46779=EDGE_LOOP ( 'NONE', ( #38021, #27051, #40729, #23368 ) ) ;
#46780=DIRECTION ( 'NONE',  ( -0.000000000000000000, 1.000000000000000000, -0.000000000000000000 ) ) ;
#46782=ORIENTED_EDGE ( 'NONE', *, *, #25453, .T. ) ;
#46783=LINE ( 'NONE', #11456, #42733 ) ;
#46784=CARTESIAN_POINT ( 'NONE',  ( -1.985260859929297794, 3.267716535433071279, 6.887757239314512246E-16 ) ) ;
#46786=AXIS2_PLACEMENT_3D ( 'NONE', #47577, #12250, #34988 ) ;
#46787=CIRCLE ( 'NONE', #22111, 2.165354330708661568 ) ;
#46789=LINE ( 'NONE', #23325, #32107 ) ;
#46790=VERTEX_POINT ( 'NONE', #29090 ) ;
#46791=VERTEX_POINT ( 'NONE', #12589 ) ;
#46793=ORIENTED_EDGE ( 'NONE', *, *, #42582, .T. ) ;
#46794=DIRECTION ( 'NONE',  ( -0.000000000000000000, 1.000000000000000000, -0.000000000000000000 ) ) ;
#46795=CARTESIAN_POINT ( 'NONE',  ( -1.439733046521777027, 0.000000000000000000, -0.5118110236220466680 ) ) ;
#46798=EDGE_CURVE ( 'NONE', #13419, #41040, #44831, .T. ) ;
#46799=EDGE_CURVE ( 'NONE', #36331, #31704, #21108, .T. ) ;
#46802=CARTESIAN_POINT ( 'NONE',  ( -1.521361932310741016, 3.346456692913386100, -1.456692913385822186 ) ) ;
#46803=CARTESIAN_POINT ( 'NONE',  ( 1.909347346926324684, 0.000000000000000000, 0.2755905511810994302 ) ) ;
#46804=ORIENTED_EDGE ( 'NONE', *, *, #9901, .T. ) ;
#46805=DIRECTION ( 'NONE',  ( -0.000000000000000000, 1.000000000000000000, -0.000000000000000000 ) ) ;
#46807=CARTESIAN_POINT ( 'NONE',  ( 1.560669927219590525, 3.346456692913386100, 0.2755905511810996522 ) ) ;
#46808=ORIENTED_EDGE ( 'NONE', *, *, #49180, .F. ) ;
#46809=DIRECTION ( 'NONE',  ( 1.734723475976806848E-16, -0.000000000000000000, 1.000000000000000000 ) ) ;
#46810=LINE ( 'NONE', #11482, #14629 ) ;
#46813=FACE_OUTER_BOUND ( 'NONE', #32293, .T. ) ;
#46814=CARTESIAN_POINT ( 'NONE',  ( 0.7423782071083092626, 0.000000000000000000, 1.259842519685033357 ) ) ;
#46815=ORIENTED_EDGE ( 'NONE', *, *, #7421, .F. ) ;
#46817=ORIENTED_EDGE ( 'NONE', *, *, #19083, .F. ) ;
#46819=CARTESIAN_POINT ( 'NONE',  ( -1.909347346926324906, 3.346456692913386100, -1.299212598425193210 ) ) ;
#46820=DIRECTION ( 'NONE',  ( -3.469446951953613696E-16, 0.000000000000000000, -1.000000000000000000 ) ) ;
#46822=EDGE_CURVE ( 'NONE', #5168, #28186, #9227, .T. ) ;
#46825=DIRECTION ( 'NONE',  ( -1.000000000000000000, -0.000000000000000000, -0.000000000000000000 ) ) ;
#46826=DIRECTION ( 'NONE',  ( 0.000000000000000000, -1.000000000000000000, 0.000000000000000000 ) ) ;
#46827=CARTESIAN_POINT ( 'NONE',  ( 1.560669927219590303, 3.346456692913386100, -1.417322834645665219 ) ) ;
#46829=DIRECTION ( 'NONE',  ( 1.000000000000000000, 0.000000000000000000, 0.000000000000000000 ) ) ;
#46830=LINE ( 'NONE', #35757, #45031 ) ;
#46831=EDGE_CURVE ( 'NONE', #49170, #12597, #25232, .T. ) ;
#46832=DIRECTION ( 'NONE',  ( 1.734723475976806848E-16, 0.000000000000000000, 1.000000000000000000 ) ) ;
#46833=VECTOR ( 'NONE', #43036, 39.37007874015748143 ) ;
#46834=VERTEX_POINT ( 'NONE', #17486 ) ;
#46838=VECTOR ( 'NONE', #980, 39.37007874015748143 ) ;
#46839=DIRECTION ( 'NONE',  ( 1.734723475976806848E-16, -0.000000000000000000, 1.000000000000000000 ) ) ;
#46841=EDGE_CURVE ( 'NONE', #19826, #33327, #40477, .T. ) ;
#46842=CARTESIAN_POINT ( 'NONE',  ( 1.636583440222563635, 3.267716535433071279, -1.325930245594399537 ) ) ;
#46843=ORIENTED_EDGE ( 'NONE', *, *, #18618, .F. ) ;
#46844=ORIENTED_EDGE ( 'NONE', *, *, #29697, .T. ) ;
#46845=VECTOR ( 'NONE', #25450, 39.37007874015748143 ) ;
#46846=DIRECTION ( 'NONE',  ( -0.000000000000000000, 0.000000000000000000, 1.000000000000000000 ) ) ;
#46847=ADVANCED_FACE ( 'NONE', ( #37115 ), #5099, .F. ) ;
#46848=VECTOR ( 'NONE', #27580, 39.37007874015748143 ) ;
#46851=CARTESIAN_POINT ( 'NONE',  ( -1.363819533518803473, 3.267716535433071279, -0.4724409448818886470 ) ) ;
#46852=VERTEX_POINT ( 'NONE', #6378 ) ;
#46853=DIRECTION ( 'NONE',  ( -3.469446951953613696E-16, 0.000000000000000000, -1.000000000000000000 ) ) ;
#46854=LINE ( 'NONE', #35276, #1317 ) ;
#46855=PLANE ( 'NONE',  #6927 ) ;
#46857=LINE ( 'NONE', #14645, #4149 ) ;
#46858=EDGE_CURVE ( 'NONE', #43954, #37379, #30630, .T. ) ;
#46859=EDGE_CURVE ( 'NONE', #26933, #36182, #1991, .T. ) ;
#46861=CARTESIAN_POINT ( 'NONE',  ( 1.560669927219591413, 3.267716535433071279, 1.732283464566921172 ) ) ;
#46863=CARTESIAN_POINT ( 'NONE',  ( -2.162130742952123263, 3.346456692913386100, 0.1181102362204704270 ) ) ;
#46865=DIRECTION ( 'NONE',  ( -0.000000000000000000, 1.000000000000000000, -0.000000000000000000 ) ) ;
#46866=DIRECTION ( 'NONE',  ( -0.000000000000000000, 0.000000000000000000, 1.000000000000000000 ) ) ;
#46867=VECTOR ( 'NONE', #6522, 39.37007874015748143 ) ;
#46870=CARTESIAN_POINT ( 'NONE',  ( 1.560669927219590747, 3.346456692913386100, 1.102362204724403938 ) ) ;
#46871=EDGE_LOOP ( 'NONE', ( #39113, #6930, #14876, #31604 ) ) ;
#46875=DIRECTION ( 'NONE',  ( -1.000000000000000000, 0.000000000000000000, 0.000000000000000000 ) ) ;
#46877=CARTESIAN_POINT ( 'NONE',  ( 0.5455278134075208785, 3.346456692913386100, -2.034427629037600660 ) ) ;
#46878=CARTESIAN_POINT ( 'NONE',  ( 2.182111253630085290, 3.267716535433071279, -3.785359618865289765E-16 ) ) ;
#46879=ORIENTED_EDGE ( 'NONE', *, *, #39250, .T. ) ;
#46882=ORIENTED_EDGE ( 'NONE', *, *, #462, .F. ) ;
#46883=FACE_OUTER_BOUND ( 'NONE', #12271, .T. ) ;
#46885=LINE ( 'NONE', #3814, #46833 ) ;
#46888=EDGE_CURVE ( 'NONE', #25127, #2869, #11008, .T. ) ;
#46889=CARTESIAN_POINT ( 'NONE',  ( 2.100403847690402337, 3.346456692913386100, 0.1574803149606280872 ) ) ;
#46890=EDGE_CURVE ( 'NONE', #30424, #42646, #45840, .T. ) ;
#46891=VECTOR ( 'NONE', #20448, 39.37007874015748143 ) ;
#46893=DIRECTION ( 'NONE',  ( 1.000000000000000000, 0.000000000000000000, 0.000000000000000000 ) ) ;
#46896=ORIENTED_EDGE ( 'NONE', *, *, #11352, .F. ) ;
#46897=DIRECTION ( 'NONE',  ( -0.000000000000000000, 1.000000000000000000, -0.000000000000000000 ) ) ;
#46899=VECTOR ( 'NONE', #17917, 39.37007874015748143 ) ;
#46901=EDGE_LOOP ( 'NONE', ( #49590, #1861, #36410, #27440 ) ) ;
#46902=VERTEX_POINT ( 'NONE', #10752 ) ;
#46903=ADVANCED_FACE ( 'NONE', ( #6631 ), #9994, .F. ) ;
#46904=AXIS2_PLACEMENT_3D ( 'NONE', #13337, #33225, #17718 ) ;
#46907=ORIENTED_EDGE ( 'NONE', *, *, #39204, .T. ) ;
#46908=EDGE_CURVE ( 'NONE', #10269, #7688, #26246, .T. ) ;
#46909=VECTOR ( 'NONE', #47579, 39.37007874015748143 ) ;
#46910=CARTESIAN_POINT ( 'NONE',  ( 2.106197740627111958, 3.267716535433071279, -0.6692913385826764205 ) ) ;
#46912=DIRECTION ( 'NONE',  ( 1.000000000000000000, -0.000000000000000000, 0.000000000000000000 ) ) ;
#46913=DIRECTION ( 'NONE',  ( -0.000000000000000000, 1.000000000000000000, -0.000000000000000000 ) ) ;
#46914=LINE ( 'NONE', #11584, #26376 ) ;
#46915=EDGE_CURVE ( 'NONE', #11581, #36186, #37884, .T. ) ;
#46917=VERTEX_POINT ( 'NONE', #18505 ) ;
#46918=ORIENTED_EDGE ( 'NONE', *, *, #5325, .F. ) ;
#46919=CARTESIAN_POINT ( 'NONE',  ( 0.2727639067037610499, 3.346456692913386100, 2.362204724409437961 ) ) ;
#46920=CARTESIAN_POINT ( 'NONE',  ( 0.000000000000000000, 3.267716535433071279, 1.259842519685033357 ) ) ;
#46923=CARTESIAN_POINT ( 'NONE',  ( -0.2727639067037608278, 3.346456692913386100, -1.614173228346451605 ) ) ;
#46924=DIRECTION ( 'NONE',  ( 1.000000000000000000, 0.000000000000000000, -3.469446951953613696E-16 ) ) ;
#46927=VERTEX_POINT ( 'NONE', #41996 ) ;
#46928=CARTESIAN_POINT ( 'NONE',  ( 0.7423782071083087075, 3.267716535433071279, -0.3149606299212593941 ) ) ;
#46930=DIRECTION ( 'NONE',  ( 1.734723475976806848E-16, -0.000000000000000000, 1.000000000000000000 ) ) ;
#46931=ORIENTED_EDGE ( 'NONE', *, *, #35558, .F. ) ;
#46932=VERTEX_POINT ( 'NONE', #2751 ) ;
#46933=CARTESIAN_POINT ( 'NONE',  ( -1.536664496436148184E-16, 3.346456692913386100, 0.1181102362204701633 ) ) ;
#46935=DIRECTION ( 'NONE',  ( -0.000000000000000000, 1.000000000000000000, -0.000000000000000000 ) ) ;
#46936=ORIENTED_EDGE ( 'NONE', *, *, #33978, .F. ) ;
#46939=CARTESIAN_POINT ( 'NONE',  ( -1.363819533518803029, 0.000000000000000000, 0.9055118110236167750 ) ) ;
#46941=VERTEX_POINT ( 'NONE', #49692 ) ;
#46943=LINE ( 'NONE', #39494, #11571 ) ;
#46945=ORIENTED_EDGE ( 'NONE', *, *, #35014, .F. ) ;
#46946=EDGE_CURVE ( 'NONE', #35716, #42223, #6879, .T. ) ;
#46948=ORIENTED_EDGE ( 'NONE', *, *, #22719, .F. ) ;
#46949=EDGE_LOOP ( 'NONE', ( #36039, #26027, #12086, #14259 ) ) ;
#46953=VERTEX_POINT ( 'NONE', #22626 ) ;
#46954=DIRECTION ( 'NONE',  ( -3.469446951953613696E-16, 0.000000000000000000, -1.000000000000000000 ) ) ;
#46957=CARTESIAN_POINT ( 'NONE',  ( -0.6214413264104942103, 3.267716535433071279, 2.156057715732900040E-16 ) ) ;
#46958=ORIENTED_EDGE ( 'NONE', *, *, #2955, .T. ) ;
#46959=ORIENTED_EDGE ( 'NONE', *, *, #5854, .T. ) ;
#46962=VERTEX_POINT ( 'NONE', #33505 ) ;
#46964=DIRECTION ( 'NONE',  ( 1.734723475976806848E-16, -0.000000000000000000, 1.000000000000000000 ) ) ;
#46966=VECTOR ( 'NONE', #19944, 39.37007874015748143 ) ;
#46967=LINE ( 'NONE', #791, #50562 ) ;
#46968=CARTESIAN_POINT ( 'NONE',  ( -1.712496953225537633, 3.346456692913386100, -1.102362204724405492 ) ) ;
#46969=ORIENTED_EDGE ( 'NONE', *, *, #24999, .T. ) ;
#46970=VERTEX_POINT ( 'NONE', #46842 ) ;
#46971=DIRECTION ( 'NONE',  ( -3.469446951953613696E-16, 0.000000000000000000, -1.000000000000000000 ) ) ;
#46974=VECTOR ( 'NONE', #27604, 39.37007874015748143 ) ;
#46975=ORIENTED_EDGE ( 'NONE', *, *, #45169, .T. ) ;
#46978=DIRECTION ( 'NONE',  ( -0.000000000000000000, 1.000000000000000000, -0.000000000000000000 ) ) ;
#46979=PLANE ( 'NONE',  #15987 ) ;
#46980=CARTESIAN_POINT ( 'NONE',  ( 1.091055626815042423, 3.267716535433071279, -1.574803149606294417 ) ) ;
#46981=DIRECTION ( 'NONE',  ( -0.000000000000000000, 1.000000000000000000, -0.000000000000000000 ) ) ;
#46985=VERTEX_POINT ( 'NONE', #8154 ) ;
#46986=VERTEX_POINT ( 'NONE', #23895 ) ;
#46988=LINE ( 'NONE', #7041, #41822 ) ;
#46989=DIRECTION ( 'NONE',  ( -0.000000000000000000, 1.000000000000000000, -0.000000000000000000 ) ) ;
#46990=EDGE_LOOP ( 'NONE', ( #16994, #18072, #21369, #48629 ) ) ;
#46991=EDGE_LOOP ( 'NONE', ( #4178, #4624, #43372, #18893 ) ) ;
#46993=VERTEX_POINT ( 'NONE', #7639 ) ;
#46994=CARTESIAN_POINT ( 'NONE',  ( 1.558105373646060388, 3.346456692913386100, 1.417322834645662777 ) ) ;
#46995=ORIENTED_EDGE ( 'NONE', *, *, #443, .T. ) ;
#46996=VECTOR ( 'NONE', #26, 39.37007874015748143 ) ;
#46997=PLANE ( 'NONE',  #49038 ) ;
#46998=PLANE ( 'NONE',  #13206 ) ;
#46999=PLANE ( 'NONE',  #29341 ) ;
#47000=VECTOR ( 'NONE', #7673, 39.37007874015748143 ) ;
#47002=EDGE_CURVE ( 'NONE', #23113, #15497, #39131, .T. ) ;
#47003=ORIENTED_EDGE ( 'NONE', *, *, #33865, .F. ) ;
#47005=LINE ( 'NONE', #43161, #21598 ) ;
#47006=PLANE ( 'NONE',  #44457 ) ;
#47008=VERTEX_POINT ( 'NONE', #43499 ) ;
#47009=EDGE_LOOP ( 'NONE', ( #35489, #42342, #4660, #18074 ) ) ;
#47010=FACE_OUTER_BOUND ( 'NONE', #34577, .T. ) ;
#47011=LINE ( 'NONE', #46522, #25243 ) ;
#47012=AXIS2_PLACEMENT_3D ( 'NONE', #11563, #19802, #4080 ) ;
#47021=ORIENTED_EDGE ( 'NONE', *, *, #1922, .F. ) ;
#47023=FACE_OUTER_BOUND ( 'NONE', #34801, .T. ) ;
#47024=ORIENTED_EDGE ( 'NONE', *, *, #40607, .F. ) ;
#47026=CARTESIAN_POINT ( 'NONE',  ( 1.636583440222563857, 3.267716535433071279, 0.4330708661417290162 ) ) ;
#47027=ORIENTED_EDGE ( 'NONE', *, *, #26886, .F. ) ;
#47030=LINE ( 'NONE', #14580, #4440 ) ;
#47033=LINE ( 'NONE', #7836, #41797 ) ;
#47034=DIRECTION ( 'NONE',  ( -0.000000000000000000, 1.000000000000000000, -0.000000000000000000 ) ) ;
#47035=ORIENTED_EDGE ( 'NONE', *, *, #1440, .T. ) ;
#47037=EDGE_CURVE ( 'NONE', #22325, #42444, #31644, .T. ) ;
#47038=ORIENTED_EDGE ( 'NONE', *, *, #37437, .T. ) ;
#47039=DIRECTION ( 'NONE',  ( 1.000000000000000000, 0.000000000000000000, 0.000000000000000000 ) ) ;
#47040=FACE_OUTER_BOUND ( 'NONE', #34373, .T. ) ;
#47042=VECTOR ( 'NONE', #29088, 39.37007874015748143 ) ;
#47043=CARTESIAN_POINT ( 'NONE',  ( 0.000000000000000000, 3.267716535433071279, -6.146657985744592735E-16 ) ) ;
#47045=ORIENTED_EDGE ( 'NONE', *, *, #41357, .F. ) ;
#47046=LINE ( 'NONE', #6601, #6056 ) ;
#47047=CIRCLE ( 'NONE', #41355, 2.106299212598425008 ) ;
#47048=EDGE_CURVE ( 'NONE', #5596, #13971, #12280, .T. ) ;
#47049=CARTESIAN_POINT ( 'NONE',  ( -0.5455278134075214336, 3.346456692913386100, -0.8267716535433049518 ) ) ;
#47050=ORIENTED_EDGE ( 'NONE', *, *, #13430, .F. ) ;
#47051=VECTOR ( 'NONE', #36570, 39.37007874015748143 ) ;
#47052=CARTESIAN_POINT ( 'NONE',  ( 0.7423782071083092626, 3.346456692913386100, 1.259842519685033357 ) ) ;
#47054=DIRECTION ( 'NONE',  ( 1.734723475976806848E-16, -0.000000000000000000, 1.000000000000000000 ) ) ;
#47055=ORIENTED_EDGE ( 'NONE', *, *, #33689, .T. ) ;
#47056=CARTESIAN_POINT ( 'NONE',  ( -0.07591351300297333182, 3.267716535433071279, -1.417322834645664331 ) ) ;
#47057=DIRECTION ( 'NONE',  ( -1.000000000000000000, 0.000000000000000000, 1.734723475976806848E-16 ) ) ;
#47058=LINE ( 'NONE', #35736, #48931 ) ;
#47059=ORIENTED_EDGE ( 'NONE', *, *, #15377, .F. ) ;
#47060=DIRECTION ( 'NONE',  ( -1.000000000000000000, 0.000000000000000000, -0.000000000000000000 ) ) ;
#47062=PLANE ( 'NONE',  #46786 ) ;
#47066=ORIENTED_EDGE ( 'NONE', *, *, #7215, .T. ) ;
#47068=CARTESIAN_POINT ( 'NONE',  ( -1.363819533518803251, 3.267716535433071279, 2.365849761790805487E-16 ) ) ;
#47070=EDGE_CURVE ( 'NONE', #15612, #38883, #35515, .T. ) ;
#47072=CARTESIAN_POINT ( 'NONE',  ( 1.015142113812069313, 0.000000000000000000, -0.4724409448818889246 ) ) ;
#47073=CARTESIAN_POINT ( 'NONE',  ( 1.091055626815042645, 0.000000000000000000, 0.6299212598425161236 ) ) ;
#47074=DIRECTION ( 'NONE',  ( -1.000000000000000000, 0.000000000000000000, -0.000000000000000000 ) ) ;
#47076=ADVANCED_FACE ( 'NONE', ( #7139 ), #22882, .F. ) ;
#47077=AXIS2_PLACEMENT_3D ( 'NONE', #3032, #7164, #15662 ) ;
#47078=LINE ( 'NONE', #9418, #49490 ) ;
#47079=VECTOR ( 'NONE', #12277, 39.37007874015748143 ) ;
#47080=ORIENTED_EDGE ( 'NONE', *, *, #46673, .F. ) ;
#47082=ORIENTED_EDGE ( 'NONE', *, *, #17127, .F. ) ;
#47085=DIRECTION ( 'NONE',  ( -0.000000000000000000, 1.000000000000000000, -0.000000000000000000 ) ) ;
#47086=VECTOR ( 'NONE', #39881, 39.37007874015748143 ) ;
#47088=DIRECTION ( 'NONE',  ( -3.469446951953613696E-16, 0.000000000000000000, -1.000000000000000000 ) ) ;
#47090=VECTOR ( 'NONE', #13675, 39.37007874015748143 ) ;
#47091=VERTEX_POINT ( 'NONE', #15388 ) ;
#47094=EDGE_CURVE ( 'NONE', #43110, #41248, #19000, .T. ) ;
#47095=VERTEX_POINT ( 'NONE', #31136 ) ;
#47096=ORIENTED_EDGE ( 'NONE', *, *, #37095, .F. ) ;
#47098=ORIENTED_EDGE ( 'NONE', *, *, #42269, .T. ) ;
#47100=CARTESIAN_POINT ( 'NONE',  ( 0.000000000000000000, 3.267716535433071279, -8.878505979408855953E-16 ) ) ;
#47101=CARTESIAN_POINT ( 'NONE',  ( 0.000000000000000000, 3.267716535433071279, -1.889763779527552368 ) ) ;
#47105=DIRECTION ( 'NONE',  ( 1.000000000000000000, -0.000000000000000000, 0.000000000000000000 ) ) ;
#47106=CARTESIAN_POINT ( 'NONE',  ( -1.636583440222564301, 3.346456692913386100, -1.574803149606293307 ) ) ;
#47108=CARTESIAN_POINT ( 'NONE',  ( 0.000000000000000000, 3.267716535433071279, -2.106299212598425008 ) ) ;
#47109=DIRECTION ( 'NONE',  ( 1.000000000000000000, 0.000000000000000000, 0.000000000000000000 ) ) ;
#47112=VERTEX_POINT ( 'NONE', #28788 ) ;
#47114=LINE ( 'NONE', #23153, #45043 ) ;
#47115=ORIENTED_EDGE ( 'NONE', *, *, #25513, .T. ) ;
#47116=CARTESIAN_POINT ( 'NONE',  ( 0.000000000000000000, 3.267716535433071279, -1.102362204724405492 ) ) ;
#47118=LINE ( 'NONE', #24445, #39162 ) ;
#47119=EDGE_CURVE ( 'NONE', #23450, #660, #4788, .T. ) ;
#47120=AXIS2_PLACEMENT_3D ( 'NONE', #13814, #41431, #6578 ) ;
#47121=DIRECTION ( 'NONE',  ( -0.000000000000000000, 1.000000000000000000, -0.000000000000000000 ) ) ;
#47123=CARTESIAN_POINT ( 'NONE',  ( -0.2727639067037607723, 3.346456692913386100, -1.417322834645664331 ) ) ;
#47124=EDGE_CURVE ( 'NONE', #1491, #21615, #16673, .T. ) ;
#47126=VECTOR ( 'NONE', #27150, 39.37007874015748143 ) ;
#47128=LINE ( 'NONE', #46878, #24327 ) ;
#47129=ORIENTED_EDGE ( 'NONE', *, *, #32175, .F. ) ;
#47130=VERTEX_POINT ( 'NONE', #24411 ) ;
#47134=CARTESIAN_POINT ( 'NONE',  ( -0.2727639067037608278, 0.000000000000000000, -0.03937007874015908959 ) ) ;
#47135=PLANE ( 'NONE',  #28560 ) ;
#47136=ORIENTED_EDGE ( 'NONE', *, *, #45823, .F. ) ;
#47137=EDGE_CURVE ( 'NONE', #46760, #29688, #17508, .T. ) ;
#47138=CARTESIAN_POINT ( 'NONE',  ( -0.3486774197067341041, 3.267716535433071279, 1.209717811016579571E-16 ) ) ;
#47139=ORIENTED_EDGE ( 'NONE', *, *, #4953, .T. ) ;
#47140=PLANE ( 'NONE',  #29033 ) ;
#47141=EDGE_CURVE ( 'NONE', #40640, #12444, #33191, .T. ) ;
#47142=CARTESIAN_POINT ( 'NONE',  ( -0.8942052331142547050, 0.000000000000000000, 0.1181102362204705658 ) ) ;
#47143=ORIENTED_EDGE ( 'NONE', *, *, #25323, .T. ) ;
#47144=ORIENTED_EDGE ( 'NONE', *, *, #2147, .F. ) ;
#47145=CARTESIAN_POINT ( 'NONE',  ( -2.182111253630085290, 3.267716535433071279, 3.785359618865288779E-16 ) ) ;
#47146=ORIENTED_EDGE ( 'NONE', *, *, #34091, .F. ) ;
#47148=DIRECTION ( 'NONE',  ( -0.000000000000000000, 0.000000000000000000, 1.000000000000000000 ) ) ;
#47149=VERTEX_POINT ( 'NONE', #1424 ) ;
#47150=ORIENTED_EDGE ( 'NONE', *, *, #13139, .T. ) ;
#47152=VECTOR ( 'NONE', #3007, 39.37007874015748143 ) ;
#47153=DIRECTION ( 'NONE',  ( -1.000000000000000000, 0.000000000000000000, -0.000000000000000000 ) ) ;
#47155=VECTOR ( 'NONE', #34048, 39.37007874015748143 ) ;
#47157=ORIENTED_EDGE ( 'NONE', *, *, #34639, .T. ) ;
#47159=VECTOR ( 'NONE', #48822, 39.37007874015748143 ) ;
#47160=VECTOR ( 'NONE', #21525, 39.37007874015748143 ) ;
#47161=DIRECTION ( 'NONE',  ( -0.000000000000000000, 1.000000000000000000, -0.000000000000000000 ) ) ;
#47162=EDGE_CURVE ( 'NONE', #33914, #25208, #20535, .T. ) ;
#47165=EDGE_LOOP ( 'NONE', ( #43491, #39438, #11565, #15106, #38886 ) ) ;
#47166=CARTESIAN_POINT ( 'NONE',  ( 0.000000000000000000, 3.346456692913386100, 0.000000000000000000 ) ) ;
#47167=DIRECTION ( 'NONE',  ( -1.000000000000000000, -0.000000000000000000, -0.000000000000000000 ) ) ;
#47168=CARTESIAN_POINT ( 'NONE',  ( -0.8182917201112814842, 3.267716535433071279, 1.535433070866133898 ) ) ;
#47171=DIRECTION ( 'NONE',  ( 1.000000000000000000, 0.000000000000000000, 0.000000000000000000 ) ) ;
#47173=CARTESIAN_POINT ( 'NONE',  ( 0.000000000000000000, 3.346456692913386100, 0.000000000000000000 ) ) ;
#47177=LINE ( 'NONE', #27845, #20102 ) ;
#47179=ORIENTED_EDGE ( 'NONE', *, *, #734, .T. ) ;
#47180=FACE_OUTER_BOUND ( 'NONE', #41450, .T. ) ;
#47181=EDGE_CURVE ( 'NONE', #40865, #7678, #16925, .T. ) ;
#47182=VERTEX_POINT ( 'NONE', #43751 ) ;
#47184=DIRECTION ( 'NONE',  ( -1.000000000000000000, 0.000000000000000000, 1.734723475976806848E-16 ) ) ;
#47185=ORIENTED_EDGE ( 'NONE', *, *, #30868, .T. ) ;
#47186=VECTOR ( 'NONE', #16916, 39.37007874015748143 ) ;
#47187=DIRECTION ( 'NONE',  ( 1.000000000000000000, -0.000000000000000000, 0.000000000000000000 ) ) ;
#47188=VERTEX_POINT ( 'NONE', #4532 ) ;
#47189=CARTESIAN_POINT ( 'NONE',  ( -1.363819533518803029, 3.267716535433071279, 0.5905511811023582691 ) ) ;
#47192=EDGE_CURVE ( 'NONE', #13480, #43159, #28526, .T. ) ;
#47196=EDGE_CURVE ( 'NONE', #37961, #14632, #15033, .T. ) ;
#47200=VERTEX_POINT ( 'NONE', #13054 ) ;
#47201=ORIENTED_EDGE ( 'NONE', *, *, #24228, .F. ) ;
#47202=CARTESIAN_POINT ( 'NONE',  ( 0.2727639067037604392, 3.267716535433071279, -0.03937007874015908959 ) ) ;
#47204=CARTESIAN_POINT ( 'NONE',  ( 0.8182917201112817063, 3.346456692913386100, -1.732283464566923614 ) ) ;
#47205=ORIENTED_EDGE ( 'NONE', *, *, #29168, .T. ) ;
#47207=PLANE ( 'NONE',  #12632 ) ;
#47209=DIRECTION ( 'NONE',  ( 0.000000000000000000, 0.000000000000000000, -1.000000000000000000 ) ) ;
#47210=ORIENTED_EDGE ( 'NONE', *, *, #25731, .F. ) ;
#47213=ORIENTED_EDGE ( 'NONE', *, *, #26216, .F. ) ;
#47214=CARTESIAN_POINT ( 'NONE',  ( 0.2727639067037604947, 3.267716535433071279, -0.7874015748031473194 ) ) ;
#47215=FACE_OUTER_BOUND ( 'NONE', #1106, .T. ) ;
#47216=FACE_OUTER_BOUND ( 'NONE', #24514, .T. ) ;
#47225=DIRECTION ( 'NONE',  ( 0.000000000000000000, -1.000000000000000000, 0.000000000000000000 ) ) ;
#47226=AXIS2_PLACEMENT_3D ( 'NONE', #47930, #24229, #44341 ) ;
#47229=EDGE_CURVE ( 'NONE', #10448, #3033, #36801, .T. ) ;
#47231=LINE ( 'NONE', #27387, #44837 ) ;
#47234=CARTESIAN_POINT ( 'NONE',  ( 1.909347346926324684, 3.346456692913386100, -0.1574803149606304187 ) ) ;
#47236=ORIENTED_EDGE ( 'NONE', *, *, #13447, .T. ) ;
#47238=CARTESIAN_POINT ( 'NONE',  ( -1.712496953225537188, 3.346456692913386100, 0.1574803149606286423 ) ) ;
#47239=ORIENTED_EDGE ( 'NONE', *, *, #11383, .T. ) ;
#47240=VERTEX_POINT ( 'NONE', #25176 ) ;
#47241=CARTESIAN_POINT ( 'NONE',  ( 0.000000000000000000, 3.346456692913386100, 0.000000000000000000 ) ) ;
#47244=ORIENTED_EDGE ( 'NONE', *, *, #13694, .T. ) ;
#47245=VERTEX_POINT ( 'NONE', #29296 ) ;
#47248=EDGE_CURVE ( 'NONE', #17684, #45462, #25937, .T. ) ;
#47249=ORIENTED_EDGE ( 'NONE', *, *, #25790, .F. ) ;
#47250=CARTESIAN_POINT ( 'NONE',  ( 0.1968503937007873017, 3.346456692913386100, 0.3149606299212576177 ) ) ;
#47251=ORIENTED_EDGE ( 'NONE', *, *, #11384, .T. ) ;
#47252=FACE_OUTER_BOUND ( 'NONE', #22000, .T. ) ;
#47253=EDGE_CURVE ( 'NONE', #29709, #12695, #12565, .T. ) ;
#47255=DIRECTION ( 'NONE',  ( 1.000000000000000000, 0.000000000000000000, 0.000000000000000000 ) ) ;
#47256=EDGE_CURVE ( 'NONE', #32019, #4450, #34199, .T. ) ;
#47257=ORIENTED_EDGE ( 'NONE', *, *, #16485, .T. ) ;
#47258=ORIENTED_EDGE ( 'NONE', *, *, #33623, .T. ) ;
#47259=VERTEX_POINT ( 'NONE', #6821 ) ;
#47260=CARTESIAN_POINT ( 'NONE',  ( -0.5455278134075208785, 3.346456692913386100, 1.889763779527550369 ) ) ;
#47261=DIRECTION ( 'NONE',  ( -3.469446951953613696E-16, 0.000000000000000000, -1.000000000000000000 ) ) ;
#47262=VECTOR ( 'NONE', #25437, 39.37007874015748143 ) ;
#47264=EDGE_LOOP ( 'NONE', ( #43697, #6067, #30412, #33250 ) ) ;
#47265=ORIENTED_EDGE ( 'NONE', *, *, #28916, .F. ) ;
#47266=AXIS2_PLACEMENT_3D ( 'NONE', #44612, #36901, #48715 ) ;
#47268=DIRECTION ( 'NONE',  ( 1.734723475976806848E-16, -0.000000000000000000, 1.000000000000000000 ) ) ;
#47270=EDGE_CURVE ( 'NONE', #36033, #26276, #50137, .T. ) ;
#47271=VECTOR ( 'NONE', #48588, 39.37007874015748143 ) ;
#47272=VECTOR ( 'NONE', #1053, 39.37007874015748143 ) ;
#47273=ORIENTED_EDGE ( 'NONE', *, *, #33370, .F. ) ;
#47274=ORIENTED_EDGE ( 'NONE', *, *, #25455, .T. ) ;
#47277=DIRECTION ( 'NONE',  ( 1.734723475976806848E-16, -0.000000000000000000, 1.000000000000000000 ) ) ;
#47278=ORIENTED_EDGE ( 'NONE', *, *, #36510, .T. ) ;
#47280=PLANE ( 'NONE',  #2994 ) ;
#47281=VECTOR ( 'NONE', #47498, 39.37007874015748143 ) ;
#47282=VERTEX_POINT ( 'NONE', #38074 ) ;
#47283=DIRECTION ( 'NONE',  ( -0.000000000000000000, 1.000000000000000000, -0.000000000000000000 ) ) ;
#47284=VERTEX_POINT ( 'NONE', #5806 ) ;
#47285=ORIENTED_EDGE ( 'NONE', *, *, #30719, .F. ) ;
#47286=CARTESIAN_POINT ( 'NONE',  ( -0.8942052331142545940, 3.267716535433071279, 3.102397620449221495E-16 ) ) ;
#47287=PLANE ( 'NONE',  #48158 ) ;
#47288=CARTESIAN_POINT ( 'NONE',  ( 0.7423782071083092626, 0.000000000000000000, 1.574803149606291974 ) ) ;
#47292=ORIENTED_EDGE ( 'NONE', *, *, #605, .T. ) ;
#47297=PLANE ( 'NONE',  #30212 ) ;
#47298=CARTESIAN_POINT ( 'NONE',  ( 1.909347346926324684, 0.000000000000000000, -0.6692913385826764205 ) ) ;
#47299=ORIENTED_EDGE ( 'NONE', *, *, #18231, .T. ) ;
#47300=VECTOR ( 'NONE', #8422, 39.37007874015748143 ) ;
#47301=EDGE_CURVE ( 'NONE', #7706, #33786, #18702, .T. ) ;
#47302=CARTESIAN_POINT ( 'NONE',  ( -0.07591351300297340121, 3.267716535433071279, 2.165354330708650465 ) ) ;
#47305=EDGE_CURVE ( 'NONE', #29676, #20090, #9940, .T. ) ;
#47306=AXIS2_PLACEMENT_3D ( 'NONE', #33037, #18796, #50477 ) ;
#47308=VERTEX_POINT ( 'NONE', #14313 ) ;
#47311=DIRECTION ( 'NONE',  ( 1.000000000000000000, 0.000000000000000000, 0.000000000000000000 ) ) ;
#47312=VERTEX_POINT ( 'NONE', #2693 ) ;
#47313=DIRECTION ( 'NONE',  ( -0.000000000000000000, 0.000000000000000000, 1.000000000000000000 ) ) ;
#47314=DIRECTION ( 'NONE',  ( 1.734723475976806848E-16, -0.000000000000000000, 1.000000000000000000 ) ) ;
#47315=CARTESIAN_POINT ( 'NONE',  ( -2.454875160333845674, 3.232777166330581320, -0.1574803149606298636 ) ) ;
#47317=EDGE_LOOP ( 'NONE', ( #32493, #11778, #30843, #22827 ) ) ;
#47318=CARTESIAN_POINT ( 'NONE',  ( 0.000000000000000000, 3.267716535433071279, 1.417322834645662777 ) ) ;
#47319=ORIENTED_EDGE ( 'NONE', *, *, #10183, .F. ) ;
#47320=CARTESIAN_POINT ( 'NONE',  ( -0.8182917201112814842, 3.346456692913386100, 0.2755905511810998187 ) ) ;
#47322=EDGE_CURVE ( 'NONE', #3406, #7692, #26187, .T. ) ;
#47323=DIRECTION ( 'NONE',  ( -0.000000000000000000, 0.000000000000000000, 1.000000000000000000 ) ) ;
#47324=DIRECTION ( 'NONE',  ( 1.734723475976806848E-16, -0.000000000000000000, 1.000000000000000000 ) ) ;
#47325=ORIENTED_EDGE ( 'NONE', *, *, #22543, .T. ) ;
#47327=CARTESIAN_POINT ( 'NONE',  ( 0.5455278134075208785, 3.346456692913386100, -1.889763779527552812 ) ) ;
#47328=CARTESIAN_POINT ( 'NONE',  ( 2.182111253630085290, 0.000000000000000000, -1.161035397307311917E-15 ) ) ;
#47329=EDGE_CURVE ( 'NONE', #22772, #24416, #6059, .T. ) ;
#47330=ORIENTED_EDGE ( 'NONE', *, *, #31042, .F. ) ;
#47331=CARTESIAN_POINT ( 'NONE',  ( -0.8942052331142552601, 0.000000000000000000, -1.259842519685034690 ) ) ;
#47333=LINE ( 'NONE', #26981, #25249 ) ;
#47334=CARTESIAN_POINT ( 'NONE',  ( 0.000000000000000000, 3.267716535433071279, -0.1968503937007880511 ) ) ;
#47335=VERTEX_POINT ( 'NONE', #14576 ) ;
#47336=ORIENTED_EDGE ( 'NONE', *, *, #29661, .F. ) ;
#47337=ORIENTED_EDGE ( 'NONE', *, *, #35788, .T. ) ;
#47338=LINE ( 'NONE', #24404, #16736 ) ;
#47340=CARTESIAN_POINT ( 'NONE',  ( -1.363819533518803029, 3.346456692913386100, 0.7874015748031456541 ) ) ;
#47342=VERTEX_POINT ( 'NONE', #21813 ) ;
#47344=AXIS2_PLACEMENT_3D ( 'NONE', #32569, #24301, #24036 ) ;
#47345=VERTEX_POINT ( 'NONE', #22567 ) ;
#47346=ORIENTED_EDGE ( 'NONE', *, *, #48201, .F. ) ;
#47347=CARTESIAN_POINT ( 'NONE',  ( -1.439733046521776139, 3.346456692913386100, 0.6299212598425164567 ) ) ;
#47348=AXIS2_PLACEMENT_3D ( 'NONE', #37799, #6031, #29012 ) ;
#47349=VERTEX_POINT ( 'NONE', #45781 ) ;
#47350=ORIENTED_EDGE ( 'NONE', *, *, #3808, .F. ) ;
#47351=FACE_OUTER_BOUND ( 'NONE', #45800, .T. ) ;
#47352=ORIENTED_EDGE ( 'NONE', *, *, #48546, .F. ) ;
#47353=AXIS2_PLACEMENT_3D ( 'NONE', #268, #30511, #26624 ) ;
#47354=DIRECTION ( 'NONE',  ( 1.000000000000000000, 0.000000000000000000, 0.000000000000000000 ) ) ;
#47356=CARTESIAN_POINT ( 'NONE',  ( 0.5455278134075208785, 3.346456692913386100, -1.889763779527552812 ) ) ;
#47357=DIRECTION ( 'NONE',  ( -0.000000000000000000, 0.000000000000000000, 1.000000000000000000 ) ) ;
#47358=EDGE_CURVE ( 'NONE', #33927, #20401, #46036, .T. ) ;
#47359=FACE_OUTER_BOUND ( 'NONE', #14302, .T. ) ;
#47360=LINE ( 'NONE', #153, #2373 ) ;
#47362=EDGE_CURVE ( 'NONE', #15712, #42475, #10446, .T. ) ;
#47364=LINE ( 'NONE', #35540, #13634 ) ;
#47366=EDGE_CURVE ( 'NONE', #9706, #25737, #6322, .T. ) ;
#47367=PRODUCT_DEFINITION ( 'UNKNOWN', '', #39941, #36089 ) ;
#47372=ORIENTED_EDGE ( 'NONE', *, *, #21361, .T. ) ;
#47373=LINE ( 'NONE', #50717, #6502 ) ;
#47374=EDGE_CURVE ( 'NONE', #15116, #40070, #37317, .T. ) ;
#47377=AXIS2_PLACEMENT_3D ( 'NONE', #25062, #10084, #29182 ) ;
#47378=AXIS2_PLACEMENT_3D ( 'NONE', #7922, #31676, #12312 ) ;
#47380=CARTESIAN_POINT ( 'NONE',  ( -1.091055626815042645, 3.267716535433071279, 1.892679809432644389E-16 ) ) ;
#47381=ORIENTED_EDGE ( 'NONE', *, *, #21250, .F. ) ;
#47382=CARTESIAN_POINT ( 'NONE',  ( -1.909347346926324462, 0.000000000000000000, -0.03937007874015881204 ) ) ;
#47383=VECTOR ( 'NONE', #19162, 39.37007874015748143 ) ;
#47385=CARTESIAN_POINT ( 'NONE',  ( -1.363819533518803473, 3.267716535433071279, -0.9842519685039344823 ) ) ;
#47387=LINE ( 'NONE', #7177, #25957 ) ;
#47388=ORIENTED_EDGE ( 'NONE', *, *, #16731, .T. ) ;
#47389=VECTOR ( 'NONE', #16648, 39.37007874015748143 ) ;
#47390=ORIENTED_EDGE ( 'NONE', *, *, #46181, .F. ) ;
#47391=ORIENTED_EDGE ( 'NONE', *, *, #11007, .F. ) ;
#47392=LINE ( 'NONE', #12065, #33694 ) ;
#47393=VERTEX_POINT ( 'NONE', #1935 ) ;
#47394=EDGE_CURVE ( 'NONE', #46268, #47393, #49134, .T. ) ;
#47395=CARTESIAN_POINT ( 'NONE',  ( 0.2727639067037602172, 3.346456692913386100, -2.244094488188969727 ) ) ;
#47396=FACE_OUTER_BOUND ( 'NONE', #39449, .T. ) ;
#47397=ORIENTED_EDGE ( 'NONE', *, *, #21647, .T. ) ;
#47398=DIRECTION ( 'NONE',  ( -3.469446951953613696E-16, 0.000000000000000000, -1.000000000000000000 ) ) ;
#47399=ORIENTED_EDGE ( 'NONE', *, *, #12931, .T. ) ;
#47402=CARTESIAN_POINT ( 'NONE',  ( 1.540582001147990487, 3.213852389688475863, -1.929133858267710666 ) ) ;
#47403=EDGE_LOOP ( 'NONE', ( #19423, #18826, #15812, #41698 ) ) ;
#47405=CARTESIAN_POINT ( 'NONE',  ( -0.2727639067037607723, 3.346456692913386100, 0.4724409448818869817 ) ) ;
#47406=ORIENTED_EDGE ( 'NONE', *, *, #37240, .F. ) ;
#47408=FACE_OUTER_BOUND ( 'NONE', #32642, .T. ) ;
#47409=ORIENTED_EDGE ( 'NONE', *, *, #9130, .T. ) ;
#47410=EDGE_LOOP ( 'NONE', ( #31382, #45942, #43145, #20005 ) ) ;
#47411=DIRECTION ( 'NONE',  ( -0.000000000000000000, 1.000000000000000000, -0.000000000000000000 ) ) ;
#47413=DIRECTION ( 'NONE',  ( -3.469446951953613696E-16, 0.000000000000000000, -1.000000000000000000 ) ) ;
#47414=VECTOR ( 'NONE', #25556, 39.37007874015748143 ) ;
#47417=AXIS2_PLACEMENT_3D ( 'NONE', #36785, #37300, #13800 ) ;
#47419=LINE ( 'NONE', #23708, #35149 ) ;
#47421=VECTOR ( 'NONE', #11374, 39.37007874015748143 ) ;
#47422=DIRECTION ( 'NONE',  ( -3.469446951953613696E-16, 0.000000000000000000, -1.000000000000000000 ) ) ;
#47424=ORIENTED_EDGE ( 'NONE', *, *, #527, .F. ) ;
#47426=DIRECTION ( 'NONE',  ( 1.000000000000000000, 0.000000000000000000, -3.469446951953613696E-16 ) ) ;
#47428=DIRECTION ( 'NONE',  ( -0.000000000000000000, 0.000000000000000000, 1.000000000000000000 ) ) ;
#47431=EDGE_CURVE ( 'NONE', #14934, #15242, #49635, .T. ) ;
#47433=VERTEX_POINT ( 'NONE', #23568 ) ;
#47434=EDGE_CURVE ( 'NONE', #20959, #31365, #11954, .T. ) ;
#47435=DIRECTION ( 'NONE',  ( 1.000000000000000000, 0.000000000000000000, -3.469446951953613696E-16 ) ) ;
#47436=VERTEX_POINT ( 'NONE', #8083 ) ;
#47437=CARTESIAN_POINT ( 'NONE',  ( -1.636583440222564301, 3.346456692913386100, -0.6299212598425177889 ) ) ;
#47438=ORIENTED_EDGE ( 'NONE', *, *, #37952, .F. ) ;
#47440=LINE ( 'NONE', #27853, #17171 ) ;
#47441=LINE ( 'NONE', #39742, #19331 ) ;
#47443=VECTOR ( 'NONE', #39025, 39.37007874015748143 ) ;
#47444=VECTOR ( 'NONE', #48264, 39.37007874015748143 ) ;
#47445=CARTESIAN_POINT ( 'NONE',  ( -0.8182917201112819283, 0.000000000000000000, -0.1574803149606301411 ) ) ;
#47447=EDGE_LOOP ( 'NONE', ( #20674, #35625, #4170, #30214 ) ) ;
#47448=PLANE ( 'NONE',  #29600 ) ;
#47449=VECTOR ( 'NONE', #20522, 39.37007874015748143 ) ;
#47450=ORIENTED_EDGE ( 'NONE', *, *, #49803, .T. ) ;
#47451=CARTESIAN_POINT ( 'NONE',  ( -1.636583440222564301, 0.000000000000000000, -1.574803149606293307 ) ) ;
#47452=CARTESIAN_POINT ( 'NONE',  ( -1.166969139818015977, 3.267716535433071279, 4.048737525165546155E-16 ) ) ;
#47453=VECTOR ( 'NONE', #16601, 39.37007874015748143 ) ;
#47454=EDGE_CURVE ( 'NONE', #5052, #351, #35706, .T. ) ;
#47455=ORIENTED_EDGE ( 'NONE', *, *, #13217, .T. ) ;
#47457=CARTESIAN_POINT ( 'NONE',  ( -0.8182917201112814842, 3.267716535433071279, 1.417322834645662777 ) ) ;
#47458=ORIENTED_EDGE ( 'NONE', *, *, #19122, .F. ) ;
#47459=VERTEX_POINT ( 'NONE', #3959 ) ;
#47460=CARTESIAN_POINT ( 'NONE',  ( 0.000000000000000000, 3.267716535433071279, 2.165354330708650910 ) ) ;
#47461=LINE ( 'NONE', #47974, #16590 ) ;
#47462=DIRECTION ( 'NONE',  ( 0.000000000000000000, 0.000000000000000000, -1.000000000000000000 ) ) ;
#47464=ORIENTED_EDGE ( 'NONE', *, *, #36655, .T. ) ;
#47465=CARTESIAN_POINT ( 'NONE',  ( 0.000000000000000000, 3.267716535433071279, 1.377952755905504256 ) ) ;
#47466=LINE ( 'NONE', #23758, #13488 ) ;
#47467=EDGE_CURVE ( 'NONE', #13332, #42385, #15325, .T. ) ;
#47469=DIRECTION ( 'NONE',  ( 1.000000000000000000, 0.000000000000000000, 0.000000000000000000 ) ) ;
#47470=EDGE_CURVE ( 'NONE', #34071, #35542, #31078, .T. ) ;
#47472=ORIENTED_EDGE ( 'NONE', *, *, #45059, .T. ) ;
#47476=DIRECTION ( 'NONE',  ( 1.734723475976806848E-16, -0.000000000000000000, 1.000000000000000000 ) ) ;
#47478=VECTOR ( 'NONE', #29323, 39.37007874015748143 ) ;
#47479=LINE ( 'NONE', #8279, #36634 ) ;
#47485=VECTOR ( 'NONE', #26698, 39.37007874015748143 ) ;
#47486=DIRECTION ( 'NONE',  ( -1.000000000000000000, -0.000000000000000000, -0.000000000000000000 ) ) ;
#47487=VERTEX_POINT ( 'NONE', #43180 ) ;
#47488=DIRECTION ( 'NONE',  ( 1.000000000000000000, 0.000000000000000000, 0.000000000000000000 ) ) ;
#47490=EDGE_CURVE ( 'NONE', #14000, #12695, #11453, .T. ) ;
#47492=ADVANCED_FACE ( 'NONE', ( #11203 ), #50881, .F. ) ;
#47493=LINE ( 'NONE', #12163, #5269 ) ;
#47494=LINE ( 'NONE', #12164, #12928 ) ;
#47496=VERTEX_POINT ( 'NONE', #3450 ) ;
#47497=EDGE_CURVE ( 'NONE', #8443, #47240, #42684, .T. ) ;
#47498=DIRECTION ( 'NONE',  ( -3.469446951953613696E-16, 0.000000000000000000, -1.000000000000000000 ) ) ;
#47499=EDGE_LOOP ( 'NONE', ( #23958, #3497, #34684, #18102 ) ) ;
#47500=VERTEX_POINT ( 'NONE', #7079 ) ;
#47501=CARTESIAN_POINT ( 'NONE',  ( 1.287906020515829919, 3.346456692913386100, -1.666671669919371102 ) ) ;
#47502=CARTESIAN_POINT ( 'NONE',  ( -1.091055626815042645, 3.346456692913386100, 2.204724409448808764 ) ) ;
#47503=LINE ( 'NONE', #294, #37092 ) ;
#47504=VERTEX_POINT ( 'NONE', #47026 ) ;
#47507=ORIENTED_EDGE ( 'NONE', *, *, #7752, .F. ) ;
#47508=CARTESIAN_POINT ( 'NONE',  ( -1.636583440222564301, 3.346456692913386100, -1.259842519685034468 ) ) ;
#47509=ORIENTED_EDGE ( 'NONE', *, *, #7384, .F. ) ;
#47512=FACE_OUTER_BOUND ( 'NONE', #46594, .T. ) ;
#47515=VERTEX_POINT ( 'NONE', #27694 ) ;
#47517=VERTEX_POINT ( 'NONE', #7830 ) ;
#47518=CARTESIAN_POINT ( 'NONE',  ( 1.363819533518803251, 0.000000000000000000, 0.4724409448818871482 ) ) ;
#47519=AXIS2_PLACEMENT_3D ( 'NONE', #6136, #41758, #2520 ) ;
#47520=FACE_OUTER_BOUND ( 'NONE', #24714, .T. ) ;
#47521=ORIENTED_EDGE ( 'NONE', *, *, #27007, .T. ) ;
#47522=ORIENTED_EDGE ( 'NONE', *, *, #15522, .T. ) ;
#47524=CARTESIAN_POINT ( 'NONE',  ( 1.363819533518803251, 3.346456692913386100, 0.9055118110236164419 ) ) ;
#47526=ORIENTED_EDGE ( 'NONE', *, *, #42723, .F. ) ;
#47527=ORIENTED_EDGE ( 'NONE', *, *, #21093, .F. ) ;
#47528=EDGE_CURVE ( 'NONE', #25746, #29370, #75, .T. ) ;
#47529=FACE_OUTER_BOUND ( 'NONE', #35523, .T. ) ;
#47530=DIRECTION ( 'NONE',  ( -0.000000000000000000, 1.000000000000000000, -0.000000000000000000 ) ) ;
#47531=VECTOR ( 'NONE', #8857, 39.37007874015748143 ) ;
#47532=CARTESIAN_POINT ( 'NONE',  ( -1.363819533518803473, 0.000000000000000000, -0.9842519685039344823 ) ) ;
#47533=ADVANCED_FACE ( 'NONE', ( #31582 ), #4724, .F. ) ;
#47534=EDGE_LOOP ( 'NONE', ( #45023, #25073, #38203, #28768 ) ) ;
#47535=CARTESIAN_POINT ( 'NONE',  ( 0.000000000000000000, 3.267716535433071279, -2.047244094488181343 ) ) ;
#47536=EDGE_CURVE ( 'NONE', #26618, #19754, #20463, .T. ) ;
#47537=CARTESIAN_POINT ( 'NONE',  ( -1.091055626815042645, 3.244425644700272393, 2.198663907112657689 ) ) ;
#47539=DIRECTION ( 'NONE',  ( -0.000000000000000000, -1.000000000000000000, -0.000000000000000000 ) ) ;
#47541=ORIENTED_EDGE ( 'NONE', *, *, #20344, .F. ) ;
#47542=DIRECTION ( 'NONE',  ( 1.000000000000000000, 0.000000000000000000, 0.000000000000000000 ) ) ;
#47543=DIRECTION ( 'NONE',  ( -0.000000000000000000, 0.000000000000000000, 1.000000000000000000 ) ) ;
#47544=DIRECTION ( 'NONE',  ( 1.000000000000000000, -0.000000000000000000, 0.000000000000000000 ) ) ;
#47549=EDGE_CURVE ( 'NONE', #5669, #6147, #24600, .T. ) ;
#47551=DIRECTION ( 'NONE',  ( -3.469446951953613696E-16, 0.000000000000000000, -1.000000000000000000 ) ) ;
#47553=EDGE_CURVE ( 'NONE', #11040, #42606, #17113, .T. ) ;
#47554=VECTOR ( 'NONE', #30504, 39.37007874015748143 ) ;
#47555=VECTOR ( 'NONE', #3922, 39.37007874015748143 ) ;
#47557=DIRECTION ( 'NONE',  ( -0.000000000000000000, 0.000000000000000000, 1.000000000000000000 ) ) ;
#47559=VECTOR ( 'NONE', #14590, 39.37007874015748143 ) ;
#47560=ORIENTED_EDGE ( 'NONE', *, *, #39318, .F. ) ;
#47563=FACE_OUTER_BOUND ( 'NONE', #28072, .T. ) ;
#47566=LINE ( 'NONE', #32644, #5559 ) ;
#47569=DIRECTION ( 'NONE',  ( -3.469446951953613696E-16, 0.000000000000000000, -1.000000000000000000 ) ) ;
#47574=CARTESIAN_POINT ( 'NONE',  ( 1.363819533518803029, 3.346456692913386100, -1.732283464566923170 ) ) ;
#47575=VERTEX_POINT ( 'NONE', #24344 ) ;
#47576=AXIS2_PLACEMENT_3D ( 'NONE', #50703, #11529, #27265 ) ;
#47577=CARTESIAN_POINT ( 'NONE',  ( 0.2727639067037602172, 0.000000000000000000, -2.047244094488182231 ) ) ;
#47578=DIRECTION ( 'NONE',  ( -3.469446951953613696E-16, 0.000000000000000000, -1.000000000000000000 ) ) ;
#47579=DIRECTION ( 'NONE',  ( 1.734723475976806848E-16, -0.000000000000000000, 1.000000000000000000 ) ) ;
#47580=DIRECTION ( 'NONE',  ( -1.000000000000000000, 0.000000000000000000, 1.734723475976806848E-16 ) ) ;
#47585=ORIENTED_EDGE ( 'NONE', *, *, #44012, .F. ) ;
#47588=FACE_OUTER_BOUND ( 'NONE', #31741, .T. ) ;
#47589=DIRECTION ( 'NONE',  ( -0.000000000000000000, 1.000000000000000000, -0.000000000000000000 ) ) ;
#47591=ORIENTED_EDGE ( 'NONE', *, *, #44616, .T. ) ;
#47593=DIRECTION ( 'NONE',  ( -3.469446951953613696E-16, 0.000000000000000000, -1.000000000000000000 ) ) ;
#47594=LINE ( 'NONE', #36284, #17577 ) ;
#47595=AXIS2_PLACEMENT_3D ( 'NONE', #50852, #19160, #27158 ) ;
#47596=VECTOR ( 'NONE', #32137, 39.37007874015748143 ) ;
#47597=DIRECTION ( 'NONE',  ( 1.734723475976806848E-16, -0.000000000000000000, 1.000000000000000000 ) ) ;
#47598=CARTESIAN_POINT ( 'NONE',  ( 0.8182917201112819283, 0.000000000000000000, 0.7874015748031454320 ) ) ;
#47599=ADVANCED_FACE ( 'NONE', ( #8849 ), #25111, .F. ) ;
#47600=FACE_BOUND ( 'NONE', #13943, .T. ) ;
#47601=VERTEX_POINT ( 'NONE', #36477 ) ;
#47604=ORIENTED_EDGE ( 'NONE', *, *, #33603, .T. ) ;
#47605=AXIS2_PLACEMENT_3D ( 'NONE', #23003, #35386, #46460 ) ;
#47606=ORIENTED_EDGE ( 'NONE', *, *, #1623, .T. ) ;
#47608=EDGE_CURVE ( 'NONE', #12011, #49793, #24014, .T. ) ;
#47611=ORIENTED_EDGE ( 'NONE', *, *, #13864, .F. ) ;
#47612=DIRECTION ( 'NONE',  ( -0.000000000000000000, 0.000000000000000000, 1.000000000000000000 ) ) ;
#47614=VERTEX_POINT ( 'NONE', #20202 ) ;
#47615=ADVANCED_FACE ( 'NONE', ( #20980 ), #1094, .F. ) ;
#47616=VECTOR ( 'NONE', #43393, 39.37007874015748143 ) ;
#47617=PLANE ( 'NONE',  #13095 ) ;
#47619=DIRECTION ( 'NONE',  ( -3.469446951953613696E-16, 0.000000000000000000, -1.000000000000000000 ) ) ;
#47620=ADVANCED_FACE ( 'NONE', ( #32875 ), #1355, .T. ) ;
#47622=PLANE ( 'NONE',  #9695 ) ;
#47623=FACE_OUTER_BOUND ( 'NONE', #32890, .T. ) ;
#47624=VERTEX_POINT ( 'NONE', #13240 ) ;
#47628=CARTESIAN_POINT ( 'NONE',  ( 1.636583440222563857, 3.267716535433071279, -2.839019714148966584E-16 ) ) ;
#47629=ORIENTED_EDGE ( 'NONE', *, *, #9180, .F. ) ;
#47630=DIRECTION ( 'NONE',  ( -1.000000000000000000, 0.000000000000000000, -0.000000000000000000 ) ) ;
#47634=VECTOR ( 'NONE', #16055, 39.37007874015748143 ) ;
#47636=LINE ( 'NONE', #43783, #49033 ) ;
#47637=AXIS2_PLACEMENT_3D ( 'NONE', #2455, #29812, #30575 ) ;
#47640=LINE ( 'NONE', #23931, #875 ) ;
#47641=DIRECTION ( 'NONE',  ( -3.469446951953613696E-16, 0.000000000000000000, -1.000000000000000000 ) ) ;
#47642=VECTOR ( 'NONE', #24567, 39.37007874015748143 ) ;
#47643=DIRECTION ( 'NONE',  ( -0.000000000000000000, 1.000000000000000000, -0.000000000000000000 ) ) ;
#47645=VECTOR ( 'NONE', #35529, 39.37007874015748143 ) ;
#47647=EDGE_LOOP ( 'NONE', ( #15738, #16071, #39992, #14404 ) ) ;
#47648=DIRECTION ( 'NONE',  ( -0.000000000000000000, 1.000000000000000000, -0.000000000000000000 ) ) ;
#47649=ORIENTED_EDGE ( 'NONE', *, *, #4290, .T. ) ;
#47653=DIRECTION ( 'NONE',  ( 1.000000000000000000, 0.000000000000000000, 0.000000000000000000 ) ) ;
#47654=VERTEX_POINT ( 'NONE', #16085 ) ;
#47655=LINE ( 'NONE', #32478, #17538 ) ;
#47656=PLANE ( 'NONE',  #6707 ) ;
#47657=EDGE_CURVE ( 'NONE', #16142, #46986, #12461, .T. ) ;
#47658=VERTEX_POINT ( 'NONE', #27952 ) ;
#47660=PLANE ( 'NONE',  #33148 ) ;
#47662=EDGE_CURVE ( 'NONE', #36186, #47487, #14245, .T. ) ;
#47663=LINE ( 'NONE', #20334, #30369 ) ;
#47664=AXIS2_PLACEMENT_3D ( 'NONE', #5340, #13349, #17225 ) ;
#47665=ADVANCED_FACE ( 'NONE', ( #33885 ), #6251, .F. ) ;
#47666=ORIENTED_EDGE ( 'NONE', *, *, #25653, .T. ) ;
#47667=EDGE_LOOP ( 'NONE', ( #26730, #28951, #26469, #13156 ) ) ;
#47668=DIRECTION ( 'NONE',  ( 0.000000000000000000, 0.000000000000000000, 1.000000000000000000 ) ) ;
#47669=FACE_OUTER_BOUND ( 'NONE', #33759, .T. ) ;
#47670=ORIENTED_EDGE ( 'NONE', *, *, #29168, .F. ) ;
#47671=CARTESIAN_POINT ( 'NONE',  ( -1.901721518280075296, 3.346456692913386100, 0.9055118110236167750 ) ) ;
#47675=VECTOR ( 'NONE', #21409, 39.37007874015748143 ) ;
#47676=EDGE_CURVE ( 'NONE', #16462, #28931, #41366, .T. ) ;
#47679=VERTEX_POINT ( 'NONE', #36992 ) ;
#47684=EDGE_CURVE ( 'NONE', #50578, #42803, #26123, .T. ) ;
#47685=VECTOR ( 'NONE', #5771, 39.37007874015748143 ) ;
#47687=CARTESIAN_POINT ( 'NONE',  ( 0.000000000000000000, 3.267716535433071279, 0.9448818897637746295 ) ) ;
#47689=ORIENTED_EDGE ( 'NONE', *, *, #16987, .T. ) ;
#47690=CARTESIAN_POINT ( 'NONE',  ( -1.636583440222564301, 0.000000000000000000, 1.377952755905504256 ) ) ;
#47692=LINE ( 'NONE', #20095, #18515 ) ;
#47693=ORIENTED_EDGE ( 'NONE', *, *, #35506, .F. ) ;
#47694=EDGE_CURVE ( 'NONE', #26125, #50486, #1864, .T. ) ;
#47697=CARTESIAN_POINT ( 'NONE',  ( 1.287906020515830141, 0.000000000000000000, 1.062992125984246083 ) ) ;
#47698=CIRCLE ( 'NONE', #18088, 2.165354330708661568 ) ;
#47700=LINE ( 'NONE', #24512, #14221 ) ;
#47702=ORIENTED_EDGE ( 'NONE', *, *, #28917, .T. ) ;
#47703=CARTESIAN_POINT ( 'NONE',  ( 0.8182917201112819283, 0.000000000000000000, 1.102362204724403938 ) ) ;
#47704=ORIENTED_EDGE ( 'NONE', *, *, #27524, .F. ) ;
#47705=VECTOR ( 'NONE', #14007, 39.37007874015748143 ) ;
#47711=ADVANCED_FACE ( 'NONE', ( #33126 ), #25359, .F. ) ;
#47713=DIRECTION ( 'NONE',  ( 1.000000000000000000, 0.000000000000000000, -3.469446951953613696E-16 ) ) ;
#47714=DIRECTION ( 'NONE',  ( -0.000000000000000000, 1.000000000000000000, -0.000000000000000000 ) ) ;
#47715=FACE_BOUND ( 'NONE', #42951, .T. ) ;
#47716=CIRCLE ( 'NONE', #7379, 2.443628662382284489 ) ;
#47718=DIRECTION ( 'NONE',  ( 0.000000000000000000, 0.000000000000000000, -1.000000000000000000 ) ) ;
#47719=LINE ( 'NONE', #12141, #5223 ) ;
#47720=EDGE_CURVE ( 'NONE', #50839, #25457, #29489, .T. ) ;
#47721=ADVANCED_FACE ( 'NONE', ( #37249 ), #17613, .F. ) ;
#47722=ORIENTED_EDGE ( 'NONE', *, *, #6860, .F. ) ;
#47724=EDGE_LOOP ( 'NONE', ( #3275, #35793, #13378, #7391 ) ) ;
#47725=ORIENTED_EDGE ( 'NONE', *, *, #21414, .T. ) ;
#47729=DIRECTION ( 'NONE',  ( 1.000000000000000000, 0.000000000000000000, 0.000000000000000000 ) ) ;
#47730=ADVANCED_FACE ( 'NONE', ( #38010 ), #45209, .F. ) ;
#47731=AXIS2_PLACEMENT_3D ( 'NONE', #2813, #42294, #10304 ) ;
#47732=PLANE ( 'NONE',  #30844 ) ;
#47733=DIRECTION ( 'NONE',  ( 0.000000000000000000, 0.000000000000000000, 1.000000000000000000 ) ) ;
#47734=ORIENTED_EDGE ( 'NONE', *, *, #10542, .F. ) ;
#47735=ORIENTED_EDGE ( 'NONE', *, *, #19328, .F. ) ;
#47736=PLANE ( 'NONE',  #27401 ) ;
#47739=EDGE_CURVE ( 'NONE', #13466, #24511, #33383, .T. ) ;
#47740=ORIENTED_EDGE ( 'NONE', *, *, #35215, .F. ) ;
#47741=DIRECTION ( 'NONE',  ( -0.000000000000000000, 0.000000000000000000, 1.000000000000000000 ) ) ;
#47743=VECTOR ( 'NONE', #22509, 39.37007874015748143 ) ;
#47746=DIRECTION ( 'NONE',  ( -3.469446951953613696E-16, 0.000000000000000000, -1.000000000000000000 ) ) ;
#47749=DIRECTION ( 'NONE',  ( -0.000000000000000000, 1.000000000000000000, -0.000000000000000000 ) ) ;
#47751=AXIS2_PLACEMENT_3D ( 'NONE', #14484, #30232, #42603 ) ;
#47752=VERTEX_POINT ( 'NONE', #37504 ) ;
#47754=VERTEX_POINT ( 'NONE', #33632 ) ;
#47755=CARTESIAN_POINT ( 'NONE',  ( -0.6214413264104945434, 3.346456692913386100, -1.929133858267710000 ) ) ;
#47756=CARTESIAN_POINT ( 'NONE',  ( 3.927031490892378253E-16, 3.346456692913386100, 1.377952755905504256 ) ) ;
#47758=ORIENTED_EDGE ( 'NONE', *, *, #43085, .T. ) ;
#47759=EDGE_CURVE ( 'NONE', #23582, #16989, #28371, .T. ) ;
#47762=EDGE_LOOP ( 'NONE', ( #33700, #50050, #27621, #46635 ) ) ;
#47765=EDGE_CURVE ( 'NONE', #21917, #34623, #17028, .T. ) ;
#47768=FACE_OUTER_BOUND ( 'NONE', #41102, .T. ) ;
#47770=ORIENTED_EDGE ( 'NONE', *, *, #13621, .T. ) ;
#47771=ORIENTED_EDGE ( 'NONE', *, *, #6894, .T. ) ;
#47772=EDGE_LOOP ( 'NONE', ( #21956, #13623, #48880, #46948 ) ) ;
#47773=CARTESIAN_POINT ( 'NONE',  ( -0.5455278134075214336, 3.346456692913386100, -1.889763779527552146 ) ) ;
#47774=VERTEX_POINT ( 'NONE', #32527 ) ;
#47778=DIRECTION ( 'NONE',  ( -1.000000000000000000, -0.000000000000000000, -0.000000000000000000 ) ) ;
#47781=ORIENTED_EDGE ( 'NONE', *, *, #22337, .T. ) ;
#47784=CARTESIAN_POINT ( 'NONE',  ( -0.07591351300297284610, 0.000000000000000000, 0.5905511811023582691 ) ) ;
#47786=DIRECTION ( 'NONE',  ( -1.000000000000000000, 0.000000000000000000, 1.734723475976806848E-16 ) ) ;
#47787=EDGE_CURVE ( 'NONE', #16143, #45509, #28885, .T. ) ;
#47788=ORIENTED_EDGE ( 'NONE', *, *, #14983, .T. ) ;
#47790=DIRECTION ( 'NONE',  ( 1.734723475976806848E-16, -0.000000000000000000, 1.000000000000000000 ) ) ;
#47792=CARTESIAN_POINT ( 'NONE',  ( 0.000000000000000000, 3.346456692913386100, 0.000000000000000000 ) ) ;
#47795=VECTOR ( 'NONE', #47398, 39.37007874015748143 ) ;
#47796=CARTESIAN_POINT ( 'NONE',  ( -1.439733046521776139, 0.000000000000000000, 0.9448818897637749625 ) ) ;
#47798=CARTESIAN_POINT ( 'NONE',  ( 1.833433833923351575, 3.267716535433071279, -6.361001426714000452E-16 ) ) ;
#47800=DIRECTION ( 'NONE',  ( 1.734723475976806848E-16, -0.000000000000000000, 1.000000000000000000 ) ) ;
#47801=ORIENTED_EDGE ( 'NONE', *, *, #44598, .F. ) ;
#47802=ORIENTED_EDGE ( 'NONE', *, *, #13961, .T. ) ;
#47804=DIRECTION ( 'NONE',  ( 0.000000000000000000, -1.000000000000000000, 0.000000000000000000 ) ) ;
#47805=CARTESIAN_POINT ( 'NONE',  ( 1.363819533518803251, 0.000000000000000000, -0.4724409448818889246 ) ) ;
#47811=VERTEX_POINT ( 'NONE', #47958 ) ;
#47812=CARTESIAN_POINT ( 'NONE',  ( 1.091055626815042645, 0.000000000000000000, -8.878505979408855953E-16 ) ) ;
#47813=DIRECTION ( 'NONE',  ( -1.000000000000000000, 0.000000000000000000, 1.734723475976806848E-16 ) ) ;
#47815=VECTOR ( 'NONE', #28152, 39.37007874015748143 ) ;
#47816=ORIENTED_EDGE ( 'NONE', *, *, #17015, .F. ) ;
#47818=VECTOR ( 'NONE', #38916, 39.37007874015748143 ) ;
#47819=ADVANCED_FACE ( 'NONE', ( #37161 ), #1526, .F. ) ;
#47822=ORIENTED_EDGE ( 'NONE', *, *, #24811, .F. ) ;
#47823=EDGE_CURVE ( 'NONE', #36525, #47095, #36647, .T. ) ;
#47824=FACE_OUTER_BOUND ( 'NONE', #29845, .T. ) ;
#47825=FACE_OUTER_BOUND ( 'NONE', #17775, .T. ) ;
#47827=ORIENTED_EDGE ( 'NONE', *, *, #17489, .F. ) ;
#47828=DIRECTION ( 'NONE',  ( -0.000000000000000000, 0.000000000000000000, 1.000000000000000000 ) ) ;
#47829=AXIS2_PLACEMENT_3D ( 'NONE', #11809, #43296, #11313 ) ;
#47830=CARTESIAN_POINT ( 'NONE',  ( 0.2727639067037604947, 3.346456692913386100, 0.4724409448818868706 ) ) ;
#47832=CARTESIAN_POINT ( 'NONE',  ( 1.091055626815042867, 3.267716535433071279, -1.892679809432645129E-16 ) ) ;
#47833=DIRECTION ( 'NONE',  ( -1.000000000000000000, -0.000000000000000000, -0.000000000000000000 ) ) ;
#47834=CARTESIAN_POINT ( 'NONE',  ( 0.000000000000000000, 3.267716535433071279, 2.007874015748021268 ) ) ;
#47835=DIRECTION ( 'NONE',  ( -0.000000000000000000, 1.000000000000000000, -0.000000000000000000 ) ) ;
#47837=ORIENTED_EDGE ( 'NONE', *, *, #47094, .F. ) ;
#47838=ORIENTED_EDGE ( 'NONE', *, *, #32950, .F. ) ;
#47839=LINE ( 'NONE', #47068, #12481 ) ;
#47841=EDGE_LOOP ( 'NONE', ( #39640, #2037, #22126, #8570 ) ) ;
#47842=DIRECTION ( 'NONE',  ( 1.000000000000000000, 0.000000000000000000, -3.469446951953613696E-16 ) ) ;
#47844=CARTESIAN_POINT ( 'NONE',  ( -1.712496953225537188, 3.346456692913386100, 0.5905511811023582691 ) ) ;
#47845=EDGE_CURVE ( 'NONE', #15979, #20171, #9527, .T. ) ;
#47847=EDGE_LOOP ( 'NONE', ( #25422, #45435, #28742, #42543 ) ) ;
#47848=EDGE_LOOP ( 'NONE', ( #21821, #14520, #22994, #1281 ) ) ;
#47849=FACE_OUTER_BOUND ( 'NONE', #1614, .T. ) ;
#47852=EDGE_CURVE ( 'NONE', #23167, #8443, #24256, .T. ) ;
#47854=EDGE_CURVE ( 'NONE', #22927, #13274, #47700, .T. ) ;
#47855=DIRECTION ( 'NONE',  ( -1.000000000000000000, 0.000000000000000000, 1.734723475976806848E-16 ) ) ;
#47856=FACE_BOUND ( 'NONE', #45910, .T. ) ;
#47857=EDGE_LOOP ( 'NONE', ( #37874, #27272, #31320, #45324 ) ) ;
#47859=ORIENTED_EDGE ( 'NONE', *, *, #1032, .F. ) ;
#47861=CARTESIAN_POINT ( 'NONE',  ( 0.8182917201112819283, 0.000000000000000000, -0.9842519685039348154 ) ) ;
#47862=VECTOR ( 'NONE', #33270, 39.37007874015748143 ) ;
#47863=VERTEX_POINT ( 'NONE', #24768 ) ;
#47869=LINE ( 'NONE', #47101, #3825 ) ;
#47871=VECTOR ( 'NONE', #2779, 39.37007874015748143 ) ;
#47872=DIRECTION ( 'NONE',  ( -1.000000000000000000, 0.000000000000000000, 1.734723475976806848E-16 ) ) ;
#47874=LINE ( 'NONE', #8677, #48425 ) ;
#47875=EDGE_LOOP ( 'NONE', ( #23359, #4366, #43280, #8251 ) ) ;
#47876=CARTESIAN_POINT ( 'NONE',  ( -0.07591351300297362326, 3.346456692913386100, -2.104930761696520491 ) ) ;
#47879=ORIENTED_EDGE ( 'NONE', *, *, #22853, .F. ) ;
#47881=EDGE_CURVE ( 'NONE', #36096, #32442, #12372, .T. ) ;
#47882=CARTESIAN_POINT ( 'NONE',  ( 1.909347346926324684, 3.346456692913386100, -0.4724409448818889246 ) ) ;
#47883=ORIENTED_EDGE ( 'NONE', *, *, #24329, .F. ) ;
#47885=DIRECTION ( 'NONE',  ( 1.000000000000000000, 0.000000000000000000, 0.000000000000000000 ) ) ;
#47889=CARTESIAN_POINT ( 'NONE',  ( 2.021817418930639931, 3.346456692913386100, 0.5905511811023582691 ) ) ;
#47890=VERTEX_POINT ( 'NONE', #4888 ) ;
#47895=AXIS2_PLACEMENT_3D ( 'NONE', #36797, #47855, #40667 ) ;
#47897=LINE ( 'NONE', #42220, #44140 ) ;
#47898=VECTOR ( 'NONE', #14292, 39.37007874015748143 ) ;
#47899=ORIENTED_EDGE ( 'NONE', *, *, #16782, .F. ) ;
#47900=ORIENTED_EDGE ( 'NONE', *, *, #44280, .T. ) ;
#47902=ORIENTED_EDGE ( 'NONE', *, *, #35809, .T. ) ;
#47903=AXIS2_PLACEMENT_3D ( 'NONE', #32931, #48612, #48103 ) ;
#47904=EDGE_CURVE ( 'NONE', #47658, #13697, #20632, .T. ) ;
#47907=DIRECTION ( 'NONE',  ( -0.000000000000000000, 1.000000000000000000, -0.000000000000000000 ) ) ;
#47908=VECTOR ( 'NONE', #30347, 39.37007874015748143 ) ;
#47909=EDGE_CURVE ( 'NONE', #8496, #23557, #21916, .T. ) ;
#47910=ORIENTED_EDGE ( 'NONE', *, *, #36603, .T. ) ;
#47912=ADVANCED_FACE ( 'NONE', ( #26291 ), #37673, .F. ) ;
#47914=ORIENTED_EDGE ( 'NONE', *, *, #41888, .F. ) ;
#47916=CARTESIAN_POINT ( 'NONE',  ( -1.166969139818015977, 3.267716535433071279, -1.753476375576570323 ) ) ;
#47917=EDGE_LOOP ( 'NONE', ( #41674, #23470, #38057, #27018 ) ) ;
#47919=CARTESIAN_POINT ( 'NONE',  ( 1.287906020515830141, 3.267716535433071279, -1.141732283464564013 ) ) ;
#47920=ORIENTED_EDGE ( 'NONE', *, *, #32632, .F. ) ;
#47921=EDGE_LOOP ( 'NONE', ( #9645, #957, #522, #7039 ) ) ;
#47923=LINE ( 'NONE', #40228, #5996 ) ;
#47924=CARTESIAN_POINT ( 'NONE',  ( 0.4696143004045484903, 0.000000000000000000, 1.732283464566921172 ) ) ;
#47925=VERTEX_POINT ( 'NONE', #42281 ) ;
#47926=DIRECTION ( 'NONE',  ( 1.000000000000000000, 0.000000000000000000, 0.000000000000000000 ) ) ;
#47927=ORIENTED_EDGE ( 'NONE', *, *, #11287, .T. ) ;
#47928=LINE ( 'NONE', #729, #39266 ) ;
#47929=AXIS2_PLACEMENT_3D ( 'NONE', #11160, #25892, #10662 ) ;
#47930=CARTESIAN_POINT ( 'NONE',  ( -1.909347346926324462, 0.000000000000000000, 0.1574803149606286423 ) ) ;
#47932=FACE_OUTER_BOUND ( 'NONE', #48891, .T. ) ;
#47937=LINE ( 'NONE', #16490, #32789 ) ;
#47938=DIRECTION ( 'NONE',  ( -0.000000000000000000, 1.000000000000000000, -0.000000000000000000 ) ) ;
#47939=CARTESIAN_POINT ( 'NONE',  ( 1.909347346926324684, 3.267716535433071279, 0.7874015748031456541 ) ) ;
#47940=AXIS2_PLACEMENT_3D ( 'NONE', #28643, #44389, #24782 ) ;
#47941=CARTESIAN_POINT ( 'NONE',  ( -0.6214413264104945434, 0.000000000000000000, 0.1574803149606285035 ) ) ;
#47942=CARTESIAN_POINT ( 'NONE',  ( -1.636583440222564301, 3.346456692913386100, -0.5118110236220466680 ) ) ;
#47943=VECTOR ( 'NONE', #8298, 39.37007874015748143 ) ;
#47949=LINE ( 'NONE', #28100, #29229 ) ;
#47951=ORIENTED_EDGE ( 'NONE', *, *, #1922, .T. ) ;
#47952=EDGE_CURVE ( 'NONE', #49218, #25289, #2038, .T. ) ;
#47953=DIRECTION ( 'NONE',  ( -0.000000000000000000, 0.000000000000000000, 1.000000000000000000 ) ) ;
#47954=CARTESIAN_POINT ( 'NONE',  ( 0.000000000000000000, 3.346456692913386100, 0.000000000000000000 ) ) ;
#47958=CARTESIAN_POINT ( 'NONE',  ( 0.5455278134075216556, 3.346456692913386100, 2.007874015748021268 ) ) ;
#47959=FACE_BOUND ( 'NONE', #6253, .T. ) ;
#47960=EDGE_LOOP ( 'NONE', ( #3920, #34631, #16604, #5796 ) ) ;
#47962=ORIENTED_EDGE ( 'NONE', *, *, #21126, .F. ) ;
#47963=LINE ( 'NONE', #43351, #12864 ) ;
#47965=AXIS2_PLACEMENT_3D ( 'NONE', #29936, #41058, #17305 ) ;
#47968=CARTESIAN_POINT ( 'NONE',  ( -1.195183497228115035E-16, 3.267716535433071279, 0.3149606299212576177 ) ) ;
#47970=VERTEX_POINT ( 'NONE', #37923 ) ;
#47971=ADVANCED_FACE ( 'NONE', ( #6672 ), #5906, .F. ) ;
#47972=FACE_OUTER_BOUND ( 'NONE', #13794, .T. ) ;
#47973=VECTOR ( 'NONE', #41187, 39.37007874015748143 ) ;
#47974=CARTESIAN_POINT ( 'NONE',  ( 1.636583440222563635, 3.267716535433071279, -2.839019714148966584E-16 ) ) ;
#47975=DIRECTION ( 'NONE',  ( 0.000000000000000000, -1.000000000000000000, 0.000000000000000000 ) ) ;
#47977=LINE ( 'NONE', #16009, #35266 ) ;
#47979=VERTEX_POINT ( 'NONE', #22423 ) ;
#47980=CARTESIAN_POINT ( 'NONE',  ( -1.636583440222564301, 3.346456692913386100, -0.9448818897637762948 ) ) ;
#47981=ORIENTED_EDGE ( 'NONE', *, *, #22604, .T. ) ;
#47982=ORIENTED_EDGE ( 'NONE', *, *, #36510, .F. ) ;
#47984=EDGE_CURVE ( 'NONE', #30956, #22242, #29662, .T. ) ;
#47985=ORIENTED_EDGE ( 'NONE', *, *, #6556, .T. ) ;
#47988=DIRECTION ( 'NONE',  ( -0.000000000000000000, 0.000000000000000000, 1.000000000000000000 ) ) ;
#47989=PLANE ( 'NONE',  #23062 ) ;
#47990=ORIENTED_EDGE ( 'NONE', *, *, #26546, .F. ) ;
#47995=CARTESIAN_POINT ( 'NONE',  ( -0.07591351300297277671, 3.346456692913386100, 1.102362204724404160 ) ) ;
#47997=CARTESIAN_POINT ( 'NONE',  ( -0.5455278134075214336, 3.267716535433071279, -0.8267716535433049518 ) ) ;
#47999=CARTESIAN_POINT ( 'NONE',  ( -0.2727639067037610499, 0.000000000000000000, -2.047244094488181343 ) ) ;
#48004=EDGE_CURVE ( 'NONE', #33562, #21655, #41529, .T. ) ;
#48005=VECTOR ( 'NONE', #12894, 39.37007874015748143 ) ;
#48006=ORIENTED_EDGE ( 'NONE', *, *, #26409, .F. ) ;
#48009=ORIENTED_EDGE ( 'NONE', *, *, #8430, .F. ) ;
#48010=VECTOR ( 'NONE', #10587, 39.37007874015748143 ) ;
#48011=CARTESIAN_POINT ( 'NONE',  ( 0.5455278134075212115, 3.346456692913386100, -6.146657985744592735E-16 ) ) ;
#48012=DIRECTION ( 'NONE',  ( 1.734723475976806848E-16, 0.000000000000000000, 1.000000000000000000 ) ) ;
#48013=CARTESIAN_POINT ( 'NONE',  ( -1.985260859929298238, 3.267716535433071279, -1.141732283464563791 ) ) ;
#48016=EDGE_CURVE ( 'NONE', #31313, #27397, #49989, .T. ) ;
#48017=VECTOR ( 'NONE', #36564, 39.37007874015748143 ) ;
#48018=ORIENTED_EDGE ( 'NONE', *, *, #42582, .F. ) ;
#48019=PLANE ( 'NONE',  #38627 ) ;
#48020=EDGE_LOOP ( 'NONE', ( #47900, #45768, #40603, #13625 ) ) ;
#48021=LINE ( 'NONE', #25528, #18007 ) ;
#48024=FACE_OUTER_BOUND ( 'NONE', #38804, .T. ) ;
#48025=CARTESIAN_POINT ( 'NONE',  ( 2.378961647330872342, 3.267716535433071279, -8.253681236146642869E-16 ) ) ;
#48026=EDGE_CURVE ( 'NONE', #14385, #5048, #18039, .T. ) ;
#48027=ORIENTED_EDGE ( 'NONE', *, *, #19177, .F. ) ;
#48028=ORIENTED_EDGE ( 'NONE', *, *, #37437, .F. ) ;
#48029=ORIENTED_EDGE ( 'NONE', *, *, #8071, .F. ) ;
#48030=LINE ( 'NONE', #41349, #4081 ) ;
#48031=EDGE_LOOP ( 'NONE', ( #10907, #50851, #44316, #2235 ) ) ;
#48033=ADVANCED_FACE ( 'NONE', ( #33288 ), #18291, .F. ) ;
#48034=CARTESIAN_POINT ( 'NONE',  ( -1.363819533518803473, 0.000000000000000000, -0.6692913385826760875 ) ) ;
#48035=CARTESIAN_POINT ( 'NONE',  ( -0.07591351300297333182, 0.000000000000000000, -0.7874015748031470974 ) ) ;
#48038=CARTESIAN_POINT ( 'NONE',  ( -2.454875160333845674, 0.000000000000000000, 0.1574803149606286423 ) ) ;
#48039=CARTESIAN_POINT ( 'NONE',  ( 0.4696143004045478797, 0.000000000000000000, 0.5905511811023579360 ) ) ;
#48040=EDGE_CURVE ( 'NONE', #23689, #19826, #25526, .T. ) ;
#48042=ORIENTED_EDGE ( 'NONE', *, *, #17572, .F. ) ;
#48044=AXIS2_PLACEMENT_3D ( 'NONE', #8006, #39508, #19868 ) ;
#48045=CARTESIAN_POINT ( 'NONE',  ( -0.6214413264104945434, 0.000000000000000000, -1.417322834645664331 ) ) ;
#48046=ORIENTED_EDGE ( 'NONE', *, *, #20900, .F. ) ;
#48047=DIRECTION ( 'NONE',  ( -1.000000000000000000, 0.000000000000000000, -0.000000000000000000 ) ) ;
#48048=ORIENTED_EDGE ( 'NONE', *, *, #4852, .F. ) ;
#48049=VECTOR ( 'NONE', #16700, 39.37007874015748143 ) ;
#48050=VERTEX_POINT ( 'NONE', #19486 ) ;
#48051=DIRECTION ( 'NONE',  ( -3.469446951953613696E-16, 0.000000000000000000, -1.000000000000000000 ) ) ;
#48053=ADVANCED_FACE ( 'NONE', ( #10490 ), #46084, .F. ) ;
#48056=FACE_OUTER_BOUND ( 'NONE', #18995, .T. ) ;
#48058=CARTESIAN_POINT ( 'NONE',  ( -0.6214413264104939882, 3.267716535433071279, 1.732283464566921172 ) ) ;
#48059=ORIENTED_EDGE ( 'NONE', *, *, #20163, .T. ) ;
#48060=ORIENTED_EDGE ( 'NONE', *, *, #32370, .T. ) ;
#48062=EDGE_CURVE ( 'NONE', #39173, #36517, #27231, .T. ) ;
#48064=ORIENTED_EDGE ( 'NONE', *, *, #8722, .T. ) ;
#48065=CARTESIAN_POINT ( 'NONE',  ( -1.521361932310741016, 3.346456692913386100, -1.456692913385822186 ) ) ;
#48068=DIRECTION ( 'NONE',  ( 1.734723475976806848E-16, -0.000000000000000000, 1.000000000000000000 ) ) ;
#48069=DIRECTION ( 'NONE',  ( -0.000000000000000000, 1.000000000000000000, -0.000000000000000000 ) ) ;
#48070=ORIENTED_EDGE ( 'NONE', *, *, #2507, .T. ) ;
#48071=DIRECTION ( 'NONE',  ( 1.000000000000000000, 0.000000000000000000, 0.000000000000000000 ) ) ;
#48073=EDGE_CURVE ( 'NONE', #8409, #13544, #19234, .T. ) ;
#48074=VERTEX_POINT ( 'NONE', #38122 ) ;
#48075=CARTESIAN_POINT ( 'NONE',  ( -2.071704270381554913, 3.346456692913386100, 0.6299212598425164567 ) ) ;
#48077=CARTESIAN_POINT ( 'NONE',  ( 1.091055626815042645, 3.346456692913386100, 0.4330708661417287386 ) ) ;
#48078=ORIENTED_EDGE ( 'NONE', *, *, #7973, .F. ) ;
#48079=CARTESIAN_POINT ( 'NONE',  ( 0.000000000000000000, 3.267716535433071279, -1.456692913385822630 ) ) ;
#48080=PLANE ( 'NONE',  #19224 ) ;
#48083=AXIS2_PLACEMENT_3D ( 'NONE', #9037, #46846, #18065 ) ;
#48084=ORIENTED_EDGE ( 'NONE', *, *, #24329, .T. ) ;
#48085=DIRECTION ( 'NONE',  ( 1.000000000000000000, 0.000000000000000000, 0.000000000000000000 ) ) ;
#48087=VERTEX_POINT ( 'NONE', #26477 ) ;
#48090=CIRCLE ( 'NONE', #25024, 2.493791675044291445 ) ;
#48091=CARTESIAN_POINT ( 'NONE',  ( -2.182111253630085290, 3.346456692913386100, -6.146657985744592735E-16 ) ) ;
#48092=CARTESIAN_POINT ( 'NONE',  ( -1.091055626815042645, 0.000000000000000000, -0.5118110236220467790 ) ) ;
#48094=VERTEX_POINT ( 'NONE', #50181 ) ;
#48098=DIRECTION ( 'NONE',  ( -3.469446951953613696E-16, 0.000000000000000000, -1.000000000000000000 ) ) ;
#48100=CARTESIAN_POINT ( 'NONE',  ( 1.015142113812069313, 3.346456692913386100, 0.1574803149606286423 ) ) ;
#48101=DIRECTION ( 'NONE',  ( -0.000000000000000000, 1.000000000000000000, -0.000000000000000000 ) ) ;
#48103=DIRECTION ( 'NONE',  ( 1.734723475976806848E-16, 0.000000000000000000, 1.000000000000000000 ) ) ;
#48104=VERTEX_POINT ( 'NONE', #30366 ) ;
#48105=ORIENTED_EDGE ( 'NONE', *, *, #34919, .F. ) ;
#48106=CARTESIAN_POINT ( 'NONE',  ( -1.985260859929297572, 0.000000000000000000, 0.3149606299212578953 ) ) ;
#48107=CARTESIAN_POINT ( 'NONE',  ( 0.000000000000000000, 3.267716535433071279, 1.377952755905504256 ) ) ;
#48111=FACE_BOUND ( 'NONE', #14769, .T. ) ;
#48112=EDGE_LOOP ( 'NONE', ( #9457, #44163, #23188, #20200 ) ) ;
#48115=ORIENTED_EDGE ( 'NONE', *, *, #44908, .F. ) ;
#48117=EDGE_CURVE ( 'NONE', #19314, #18704, #11500, .T. ) ;
#48118=EDGE_CURVE ( 'NONE', #19367, #11567, #34496, .T. ) ;
#48120=EDGE_LOOP ( 'NONE', ( #17992, #30374, #38214, #8109 ) ) ;
#48122=LINE ( 'NONE', #20799, #36832 ) ;
#48123=ORIENTED_EDGE ( 'NONE', *, *, #18385, .T. ) ;
#48124=VECTOR ( 'NONE', #25816, 39.37007874015748143 ) ;
#48125=EDGE_CURVE ( 'NONE', #9419, #10330, #6867, .T. ) ;
#48131=ADVANCED_FACE ( 'NONE', ( #18490 ), #38367, .F. ) ;
#48133=CARTESIAN_POINT ( 'NONE',  ( 1.363819533518803251, 0.000000000000000000, -0.7874015748031473194 ) ) ;
#48134=DIRECTION ( 'NONE',  ( -0.000000000000000000, 1.000000000000000000, -0.000000000000000000 ) ) ;
#48136=VECTOR ( 'NONE', #46316, 39.37007874015748143 ) ;
#48137=ORIENTED_EDGE ( 'NONE', *, *, #36250, .F. ) ;
#48139=CARTESIAN_POINT ( 'NONE',  ( 0.8182917201112817063, 3.346456692913386100, -1.929133858267711110 ) ) ;
#48140=CARTESIAN_POINT ( 'NONE',  ( -1.166969139818016199, 3.346456692913386100, 1.535433070866133232 ) ) ;
#48141=EDGE_CURVE ( 'NONE', #33328, #11080, #15623, .T. ) ;
#48142=EDGE_LOOP ( 'NONE', ( #39689, #48724, #8587, #24915 ) ) ;
#48144=DIRECTION ( 'NONE',  ( 1.000000000000000000, 0.000000000000000000, 0.000000000000000000 ) ) ;
#48148=EDGE_CURVE ( 'NONE', #26524, #15323, #31375, .T. ) ;
#48150=ADVANCED_FACE ( 'NONE', ( #14619 ), #10740, .F. ) ;
#48151=ORIENTED_EDGE ( 'NONE', *, *, #27689, .T. ) ;
#48152=LINE ( 'NONE', #12056, #22454 ) ;
#48154=FACE_BOUND ( 'NONE', #35191, .T. ) ;
#48155=CARTESIAN_POINT ( 'NONE',  ( -1.636583440222563635, 3.346456692913386100, 0.6299212598425164567 ) ) ;
#48157=LINE ( 'NONE', #32726, #21870 ) ;
#48158=AXIS2_PLACEMENT_3D ( 'NONE', #9105, #47543, #16865 ) ;
#48159=ORIENTED_EDGE ( 'NONE', *, *, #38629, .F. ) ;
#48161=CARTESIAN_POINT ( 'NONE',  ( -0.2727639067037602172, 3.267716535433071279, 2.047244094488179567 ) ) ;
#48163=VECTOR ( 'NONE', #542, 39.37007874015748143 ) ;
#48164=DIRECTION ( 'NONE',  ( -0.000000000000000000, 1.000000000000000000, -0.000000000000000000 ) ) ;
#48165=EDGE_LOOP ( 'NONE', ( #12238, #25395, #43030, #6907 ) ) ;
#48166=VECTOR ( 'NONE', #44112, 39.37007874015748143 ) ;
#48167=AXIS2_PLACEMENT_3D ( 'NONE', #15163, #11036, #34539 ) ;
#48168=CARTESIAN_POINT ( 'NONE',  ( 0.000000000000000000, 3.267716535433071279, -0.9448818897637762948 ) ) ;
#48172=VECTOR ( 'NONE', #28911, 39.37007874015748143 ) ;
#48173=ORIENTED_EDGE ( 'NONE', *, *, #5815, .T. ) ;
#48175=VERTEX_POINT ( 'NONE', #42477 ) ;
#48176=DIRECTION ( 'NONE',  ( -0.000000000000000000, 1.000000000000000000, -0.000000000000000000 ) ) ;
#48178=ADVANCED_FACE ( 'NONE', ( #26977 ), #42729, .F. ) ;
#48181=CARTESIAN_POINT ( 'NONE',  ( -1.712496953225537633, 3.346456692913386100, -0.9842519685039344823 ) ) ;
#48182=EDGE_CURVE ( 'NONE', #21434, #34071, #381, .T. ) ;
#48183=EDGE_LOOP ( 'NONE', ( #25330, #50006, #21659, #12234 ) ) ;
#48184=LINE ( 'NONE', #28338, #50941 ) ;
#48185=ORIENTED_EDGE ( 'NONE', *, *, #1303, .F. ) ;
#48188=CARTESIAN_POINT ( 'NONE',  ( -0.5455278134075214336, 3.346456692913386100, -1.141732283464563791 ) ) ;
#48189=ORIENTED_EDGE ( 'NONE', *, *, #14076, .F. ) ;
#48190=CARTESIAN_POINT ( 'NONE',  ( 0.000000000000000000, 3.267716535433071279, 0.000000000000000000 ) ) ;
#48192=AXIS2_PLACEMENT_3D ( 'NONE', #4927, #36429, #1308 ) ;
#48193=DIRECTION ( 'NONE',  ( -1.000000000000000000, 0.000000000000000000, 0.000000000000000000 ) ) ;
#48194=FACE_OUTER_BOUND ( 'NONE', #42601, .T. ) ;
#48196=AXIS2_PLACEMENT_3D ( 'NONE', #13894, #37909, #40754 ) ;
#48198=DIRECTION ( 'NONE',  ( -0.000000000000000000, 0.000000000000000000, 1.000000000000000000 ) ) ;
#48199=VECTOR ( 'NONE', #3742, 39.37007874015748143 ) ;
#48201=EDGE_CURVE ( 'NONE', #34165, #50693, #896, .T. ) ;
#48203=ORIENTED_EDGE ( 'NONE', *, *, #40607, .T. ) ;
#48206=EDGE_CURVE ( 'NONE', #45835, #49700, #44256, .T. ) ;
#48208=ORIENTED_EDGE ( 'NONE', *, *, #49708, .F. ) ;
#48209=DIRECTION ( 'NONE',  ( 1.734723475976806848E-16, -0.000000000000000000, 1.000000000000000000 ) ) ;
#48210=EDGE_CURVE ( 'NONE', #42475, #28392, #43735, .T. ) ;
#48211=VERTEX_POINT ( 'NONE', #15865 ) ;
#48212=FACE_OUTER_BOUND ( 'NONE', #23443, .T. ) ;
#48214=CARTESIAN_POINT ( 'NONE',  ( -1.712496953225537633, 0.000000000000000000, 1.417322834645662333 ) ) ;
#48215=DIRECTION ( 'NONE',  ( 0.000000000000000000, 1.000000000000000000, 0.000000000000000000 ) ) ;
#48216=DIRECTION ( 'NONE',  ( 1.734723475976806848E-16, -0.000000000000000000, 1.000000000000000000 ) ) ;
#48217=VERTEX_POINT ( 'NONE', #24388 ) ;
#48218=CARTESIAN_POINT ( 'NONE',  ( -1.985260859929297572, 0.000000000000000000, -0.3149606299212589500 ) ) ;
#48219=DIRECTION ( 'NONE',  ( -3.469446951953613696E-16, 0.000000000000000000, -1.000000000000000000 ) ) ;
#48221=PLANE ( 'NONE',  #27099 ) ;
#48224=DIRECTION ( 'NONE',  ( 1.000000000000000000, 0.000000000000000000, 0.000000000000000000 ) ) ;
#48225=LINE ( 'NONE', #8515, #36256 ) ;
#48226=VECTOR ( 'NONE', #15718, 39.37007874015748143 ) ;
#48227=ORIENTED_EDGE ( 'NONE', *, *, #4538, .F. ) ;
#48229=AXIS2_PLACEMENT_3D ( 'NONE', #2023, #11872, #36661 ) ;
#48232=FACE_BOUND ( 'NONE', #37863, .T. ) ;
#48233=VECTOR ( 'NONE', #33863, 39.37007874015748143 ) ;
#48234=CARTESIAN_POINT ( 'NONE',  ( -1.363819533518803029, 0.000000000000000000, -0.03937007874015868020 ) ) ;
#48235=FACE_OUTER_BOUND ( 'NONE', #38245, .T. ) ;
#48236=VECTOR ( 'NONE', #11621, 39.37007874015748143 ) ;
#48237=ORIENTED_EDGE ( 'NONE', *, *, #27350, .F. ) ;
#48238=DIRECTION ( 'NONE',  ( -0.000000000000000000, 1.000000000000000000, -0.000000000000000000 ) ) ;
#48241=EDGE_CURVE ( 'NONE', #9429, #5467, #47839, .T. ) ;
#48242=ORIENTED_EDGE ( 'NONE', *, *, #26162, .F. ) ;
#48247=CARTESIAN_POINT ( 'NONE',  ( 1.833433833923351575, 3.267716535433071279, -6.361001426714000452E-16 ) ) ;
#48249=PLANE ( 'NONE',  #5747 ) ;
#48250=ORIENTED_EDGE ( 'NONE', *, *, #33146, .T. ) ;
#48251=EDGE_LOOP ( 'NONE', ( #9438, #33113, #43333, #42102 ) ) ;
#48252=FACE_OUTER_BOUND ( 'NONE', #5744, .T. ) ;
#48253=DIRECTION ( 'NONE',  ( -3.469446951953613696E-16, 0.000000000000000000, -1.000000000000000000 ) ) ;
#48254=DIRECTION ( 'NONE',  ( 0.000000000000000000, -1.000000000000000000, 0.000000000000000000 ) ) ;
#48256=LINE ( 'NONE', #28671, #5001 ) ;
#48257=ADVANCED_FACE ( 'NONE', ( #120 ), #16130, .F. ) ;
#48258=CARTESIAN_POINT ( 'NONE',  ( -1.363819533518803029, 3.346456692913386100, 1.417322834645662777 ) ) ;
#48259=CARTESIAN_POINT ( 'NONE',  ( -1.636583440222564301, 0.000000000000000000, -1.771653543307080581 ) ) ;
#48261=VERTEX_POINT ( 'NONE', #8130 ) ;
#48262=VECTOR ( 'NONE', #32838, 39.37007874015748143 ) ;
#48264=DIRECTION ( 'NONE',  ( -1.000000000000000000, -0.000000000000000000, -0.000000000000000000 ) ) ;
#48265=VECTOR ( 'NONE', #34079, 39.37007874015748143 ) ;
#48266=EDGE_CURVE ( 'NONE', #28712, #19154, #43995, .T. ) ;
#48268=ORIENTED_EDGE ( 'NONE', *, *, #33789, .T. ) ;
#48269=AXIS2_PLACEMENT_3D ( 'NONE', #22870, #23118, #19237 ) ;
#48270=EDGE_LOOP ( 'NONE', ( #44197, #14142, #43481, #17861 ) ) ;
#48271=DIRECTION ( 'NONE',  ( 0.000000000000000000, 0.000000000000000000, -1.000000000000000000 ) ) ;
#48272=LINE ( 'NONE', #35673, #11336 ) ;
#48273=PLANE ( 'NONE',  #23884 ) ;
#48276=ORIENTED_EDGE ( 'NONE', *, *, #5442, .F. ) ;
#48277=CARTESIAN_POINT ( 'NONE',  ( 0.2727639067037610499, 3.346456692913386100, 1.732283464566921172 ) ) ;
#48280=CARTESIAN_POINT ( 'NONE',  ( -0.8942052331142552601, 3.267716535433071279, -0.9448818897637760728 ) ) ;
#48281=CARTESIAN_POINT ( 'NONE',  ( -1.636583440222564301, 3.346456692913386100, 1.417869535855831753 ) ) ;
#48282=VERTEX_POINT ( 'NONE', #47327 ) ;
#48284=ORIENTED_EDGE ( 'NONE', *, *, #21065, .F. ) ;
#48286=VERTEX_POINT ( 'NONE', #31896 ) ;
#48287=VERTEX_POINT ( 'NONE', #8896 ) ;
#48288=DIRECTION ( 'NONE',  ( -0.000000000000000000, 1.000000000000000000, -0.000000000000000000 ) ) ;
#48289=DIRECTION ( 'NONE',  ( -1.000000000000000000, -0.000000000000000000, -0.000000000000000000 ) ) ;
#48292=DIRECTION ( 'NONE',  ( 1.734723475976806848E-16, 0.000000000000000000, 1.000000000000000000 ) ) ;
#48293=DIRECTION ( 'NONE',  ( -0.000000000000000000, 1.000000000000000000, -0.000000000000000000 ) ) ;
#48294=DIRECTION ( 'NONE',  ( -1.000000000000000000, 0.000000000000000000, 0.000000000000000000 ) ) ;
#48295=VECTOR ( 'NONE', #1630, 39.37007874015748143 ) ;
#48296=EDGE_LOOP ( 'NONE', ( #10958, #28184, #31753, #28435 ) ) ;
#48298=CARTESIAN_POINT ( 'NONE',  ( -0.8182917201112819283, 3.267716535433071279, 1.419509857074483292E-16 ) ) ;
#48299=ADVANCED_FACE ( 'NONE', ( #20518 ), #27484, .F. ) ;
#48301=EDGE_CURVE ( 'NONE', #15287, #17089, #134, .T. ) ;
#48302=VECTOR ( 'NONE', #23140, 39.37007874015748143 ) ;
#48303=DIRECTION ( 'NONE',  ( -0.000000000000000000, 1.000000000000000000, -0.000000000000000000 ) ) ;
#48304=ORIENTED_EDGE ( 'NONE', *, *, #23745, .T. ) ;
#48305=ORIENTED_EDGE ( 'NONE', *, *, #47358, .T. ) ;
#48306=DIRECTION ( 'NONE',  ( 1.734723475976806848E-16, -0.000000000000000000, 1.000000000000000000 ) ) ;
#48308=VECTOR ( 'NONE', #16073, 39.37007874015748143 ) ;
#48309=EDGE_CURVE ( 'NONE', #10670, #15077, #4770, .T. ) ;
#48310=DIRECTION ( 'NONE',  ( 1.734723475976806848E-16, 0.000000000000000000, 1.000000000000000000 ) ) ;
#48311=AXIS2_PLACEMENT_3D ( 'NONE', #29566, #48630, #41195 ) ;
#48317=VECTOR ( 'NONE', #7065, 39.37007874015748143 ) ;
#48319=ORIENTED_EDGE ( 'NONE', *, *, #43569, .F. ) ;
#48321=CARTESIAN_POINT ( 'NONE',  ( 0.000000000000000000, 3.267716535433071279, -0.9842519685039348154 ) ) ;
#48323=FACE_OUTER_BOUND ( 'NONE', #21980, .T. ) ;
#48326=ORIENTED_EDGE ( 'NONE', *, *, #34707, .F. ) ;
#48328=EDGE_CURVE ( 'NONE', #12462, #18551, #5024, .T. ) ;
#48329=DIRECTION ( 'NONE',  ( 0.000000000000000000, 0.000000000000000000, -1.000000000000000000 ) ) ;
#48330=ORIENTED_EDGE ( 'NONE', *, *, #28181, .T. ) ;
#48331=CARTESIAN_POINT ( 'NONE',  ( 0.000000000000000000, 3.267716535433071279, 1.377952755905504256 ) ) ;
#48332=DIRECTION ( 'NONE',  ( -0.000000000000000000, 1.000000000000000000, -0.000000000000000000 ) ) ;
#48334=ORIENTED_EDGE ( 'NONE', *, *, #22658, .F. ) ;
#48335=VECTOR ( 'NONE', #11290, 39.37007874015748143 ) ;
#48336=DIRECTION ( 'NONE',  ( -0.000000000000000000, 1.000000000000000000, -0.000000000000000000 ) ) ;
#48338=VECTOR ( 'NONE', #25753, 39.37007874015748143 ) ;
#48340=DIRECTION ( 'NONE',  ( 1.000000000000000000, 0.000000000000000000, 0.000000000000000000 ) ) ;
#48343=CARTESIAN_POINT ( 'NONE',  ( 1.833433833923351353, 3.346456692913386100, -0.5118110236220471121 ) ) ;
#48345=DIRECTION ( 'NONE',  ( 1.734723475976806848E-16, -0.000000000000000000, 1.000000000000000000 ) ) ;
#48346=LINE ( 'NONE', #44503, #44474 ) ;
#48347=FACE_OUTER_BOUND ( 'NONE', #19746, .T. ) ;
#48351=LINE ( 'NONE', #45257, #5892 ) ;
#48352=CARTESIAN_POINT ( 'NONE',  ( -0.07591351300297277671, 0.000000000000000000, 0.7874015748031456541 ) ) ;
#48353=ORIENTED_EDGE ( 'NONE', *, *, #16958, .F. ) ;
#48354=DIRECTION ( 'NONE',  ( -1.000000000000000000, 0.000000000000000000, 1.734723475976806848E-16 ) ) ;
#48355=DIRECTION ( 'NONE',  ( 0.000000000000000000, 0.000000000000000000, -1.000000000000000000 ) ) ;
#48359=ORIENTED_EDGE ( 'NONE', *, *, #41175, .F. ) ;
#48360=LINE ( 'NONE', #40158, #38626 ) ;
#48362=CARTESIAN_POINT ( 'NONE',  ( -1.363819533518803029, 3.267716535433071279, 1.417322834645662777 ) ) ;
#48363=ORIENTED_EDGE ( 'NONE', *, *, #17282, .T. ) ;
#48365=FACE_BOUND ( 'NONE', #40844, .T. ) ;
#48366=VERTEX_POINT ( 'NONE', #45012 ) ;
#48370=CARTESIAN_POINT ( 'NONE',  ( 1.363819533518803029, 3.346456692913386100, -1.605145679676863724 ) ) ;
#48372=EDGE_CURVE ( 'NONE', #39490, #180, #6038, .T. ) ;
#48374=VECTOR ( 'NONE', #15318, 39.37007874015748143 ) ;
#48375=VERTEX_POINT ( 'NONE', #5790 ) ;
#48378=ORIENTED_EDGE ( 'NONE', *, *, #28042, .F. ) ;
#48379=VECTOR ( 'NONE', #7098, 39.37007874015748143 ) ;
#48380=CARTESIAN_POINT ( 'NONE',  ( -0.5455278134075214336, 0.000000000000000000, -1.574803149606293529 ) ) ;
#48384=CARTESIAN_POINT ( 'NONE',  ( 0.7423782071083082634, 3.346456692913386100, -1.771653543307081025 ) ) ;
#48385=LINE ( 'NONE', #40689, #42673 ) ;
#48386=ORIENTED_EDGE ( 'NONE', *, *, #32502, .F. ) ;
#48388=FACE_OUTER_BOUND ( 'NONE', #32250, .T. ) ;
#48389=ORIENTED_EDGE ( 'NONE', *, *, #28557, .T. ) ;
#48392=EDGE_LOOP ( 'NONE', ( #24097, #45575, #45471, #2514 ) ) ;
#48393=PLANE ( 'NONE',  #39471 ) ;
#48394=EDGE_CURVE ( 'NONE', #13777, #4133, #9922, .T. ) ;
#48395=PLANE ( 'NONE',  #13575 ) ;
#48399=ORIENTED_EDGE ( 'NONE', *, *, #36420, .T. ) ;
#48400=FACE_BOUND ( 'NONE', #39970, .T. ) ;
#48401=EDGE_CURVE ( 'NONE', #18633, #46194, #29018, .T. ) ;
#48402=FACE_OUTER_BOUND ( 'NONE', #32926, .T. ) ;
#48405=AXIS2_PLACEMENT_3D ( 'NONE', #25149, #36518, #9657 ) ;
#48406=VECTOR ( 'NONE', #11418, 39.37007874015748143 ) ;
#48408=ORIENTED_EDGE ( 'NONE', *, *, #26709, .T. ) ;
#48409=DIRECTION ( 'NONE',  ( 1.734723475976806848E-16, 0.000000000000000000, 1.000000000000000000 ) ) ;
#48410=ORIENTED_EDGE ( 'NONE', *, *, #27177, .T. ) ;
#48413=CARTESIAN_POINT ( 'NONE',  ( 1.363819533518803251, 3.346456692913386100, 0.4724409448818871482 ) ) ;
#48414=ORIENTED_EDGE ( 'NONE', *, *, #38133, .T. ) ;
#48415=EDGE_CURVE ( 'NONE', #30087, #6948, #9411, .T. ) ;
#48416=DIRECTION ( 'NONE',  ( -1.000000000000000000, 0.000000000000000000, 0.000000000000000000 ) ) ;
#48418=CARTESIAN_POINT ( 'NONE',  ( 0.8182917201112819283, 3.346456692913386100, 0.7874015748031454320 ) ) ;
#48420=CARTESIAN_POINT ( 'NONE',  ( -4.268512490100411402E-16, 0.000000000000000000, -2.086614173228339641 ) ) ;
#48421=EDGE_LOOP ( 'NONE', ( #39430, #13120, #37550, #5542 ) ) ;
#48422=DIRECTION ( 'NONE',  ( 0.000000000000000000, -1.000000000000000000, 0.000000000000000000 ) ) ;
#48423=VERTEX_POINT ( 'NONE', #37552 ) ;
#48424=ORIENTED_EDGE ( 'NONE', *, *, #1303, .T. ) ;
#48425=VECTOR ( 'NONE', #40181, 39.37007874015748143 ) ;
#48426=EDGE_CURVE ( 'NONE', #528, #20175, #2170, .T. ) ;
#48427=ORIENTED_EDGE ( 'NONE', *, *, #10486, .T. ) ;
#48429=ADVANCED_FACE ( 'NONE', ( #21535 ), #2430, .F. ) ;
#48431=LINE ( 'NONE', #44585, #21451 ) ;
#48432=EDGE_CURVE ( 'NONE', #2087, #28641, #25918, .T. ) ;
#48434=DIRECTION ( 'NONE',  ( -0.000000000000000000, 1.000000000000000000, -0.000000000000000000 ) ) ;
#48435=VERTEX_POINT ( 'NONE', #13796 ) ;
#48437=VECTOR ( 'NONE', #7681, 39.37007874015748143 ) ;
#48438=VECTOR ( 'NONE', #1522, 39.37007874015748143 ) ;
#48439=CARTESIAN_POINT ( 'NONE',  ( -0.07591351300297333182, 0.000000000000000000, -0.4724409448818883694 ) ) ;
#48440=ORIENTED_EDGE ( 'NONE', *, *, #6771, .T. ) ;
#48443=PLANE ( 'NONE',  #14223 ) ;
#48444=DIRECTION ( 'NONE',  ( 1.734723475976806848E-16, 0.000000000000000000, 1.000000000000000000 ) ) ;
#48446=DIRECTION ( 'NONE',  ( -0.000000000000000000, -1.000000000000000000, -0.000000000000000000 ) ) ;
#48447=PLANE ( 'NONE',  #22369 ) ;
#48448=VECTOR ( 'NONE', #6483, 39.37007874015748143 ) ;
#48449=DIRECTION ( 'NONE',  ( -1.000000000000000000, 0.000000000000000000, -0.000000000000000000 ) ) ;
#48451=CARTESIAN_POINT ( 'NONE',  ( 0.4696143004045478797, 3.346456692913386100, -0.9842519685039348154 ) ) ;
#48452=EDGE_CURVE ( 'NONE', #1599, #1205, #13541, .T. ) ;
#48453=LINE ( 'NONE', #48708, #5309 ) ;
#48457=AXIS2_PLACEMENT_3D ( 'NONE', #16367, #28479, #31864 ) ;
#48458=VERTEX_POINT ( 'NONE', #36779 ) ;
#48460=EDGE_CURVE ( 'NONE', #43653, #46669, #17159, .T. ) ;
#48461=LINE ( 'NONE', #44370, #19256 ) ;
#48462=DIRECTION ( 'NONE',  ( 0.000000000000000000, -1.000000000000000000, 0.000000000000000000 ) ) ;
#48463=EDGE_CURVE ( 'NONE', #2530, #1296, #48351, .T. ) ;
#48464=DIRECTION ( 'NONE',  ( -3.469446951953613696E-16, 0.000000000000000000, -1.000000000000000000 ) ) ;
#48466=VERTEX_POINT ( 'NONE', #28766 ) ;
#48467=EDGE_CURVE ( 'NONE', #45283, #14052, #44508, .T. ) ;
#48469=FACE_BOUND ( 'NONE', #17108, .T. ) ;
#48471=CARTESIAN_POINT ( 'NONE',  ( 2.378961647330872342, 3.230577599468342775, 0.6299212598425161236 ) ) ;
#48472=ORIENTED_EDGE ( 'NONE', *, *, #7617, .F. ) ;
#48473=PLANE ( 'NONE',  #37607 ) ;
#48475=VECTOR ( 'NONE', #8452, 39.37007874015748143 ) ;
#48476=LINE ( 'NONE', #8063, #1837 ) ;
#48477=EDGE_CURVE ( 'NONE', #33855, #28296, #34930, .T. ) ;
#48478=DIRECTION ( 'NONE',  ( -0.000000000000000000, 1.000000000000000000, -0.000000000000000000 ) ) ;
#48479=ORIENTED_EDGE ( 'NONE', *, *, #36215, .T. ) ;
#48481=CARTESIAN_POINT ( 'NONE',  ( -0.6214413264104939882, 0.000000000000000000, 0.2755905511810998187 ) ) ;
#48482=DIRECTION ( 'NONE',  ( 1.734723475976806848E-16, 0.000000000000000000, 1.000000000000000000 ) ) ;
#48483=FACE_BOUND ( 'NONE', #12690, .T. ) ;
#48484=EDGE_CURVE ( 'NONE', #31704, #21978, #25690, .T. ) ;
#48486=EDGE_CURVE ( 'NONE', #14018, #13884, #14808, .T. ) ;
#48487=AXIS2_PLACEMENT_3D ( 'NONE', #41037, #9275, #25530 ) ;
#48488=CARTESIAN_POINT ( 'NONE',  ( 0.4696143004045479352, 0.000000000000000000, -0.7874015748031473194 ) ) ;
#48494=CARTESIAN_POINT ( 'NONE',  ( 0.000000000000000000, 3.267716535433071279, 1.220472440944875059 ) ) ;
#48498=ORIENTED_EDGE ( 'NONE', *, *, #18494, .F. ) ;
#48499=VECTOR ( 'NONE', #5324, 39.37007874015748143 ) ;
#48500=ORIENTED_EDGE ( 'NONE', *, *, #28410, .T. ) ;
#48501=LINE ( 'NONE', #13183, #19336 ) ;
#48502=DIRECTION ( 'NONE',  ( -1.000000000000000000, 0.000000000000000000, 1.734723475976806848E-16 ) ) ;
#48503=DIRECTION ( 'NONE',  ( 1.734723475976806848E-16, -0.000000000000000000, 1.000000000000000000 ) ) ;
#48504=DIRECTION ( 'NONE',  ( 0.000000000000000000, 0.000000000000000000, -1.000000000000000000 ) ) ;
#48505=ORIENTED_EDGE ( 'NONE', *, *, #50686, .T. ) ;
#48506=VERTEX_POINT ( 'NONE', #10424 ) ;
#48511=CARTESIAN_POINT ( 'NONE',  ( -0.8942052331142547050, 3.346456692913386100, 1.062992125984246083 ) ) ;
#48512=LINE ( 'NONE', #12943, #39132 ) ;
#48513=VECTOR ( 'NONE', #29345, 39.37007874015748143 ) ;
#48515=ORIENTED_EDGE ( 'NONE', *, *, #32804, .T. ) ;
#48517=LINE ( 'NONE', #5954, #13710 ) ;
#48518=ORIENTED_EDGE ( 'NONE', *, *, #43668, .T. ) ;
#48522=LINE ( 'NONE', #40824, #45489 ) ;
#48523=CARTESIAN_POINT ( 'NONE',  ( -1.363819533518803473, 3.256074231195845936, 2.034181048058245178 ) ) ;
#48525=ORIENTED_EDGE ( 'NONE', *, *, #30409, .F. ) ;
#48526=AXIS2_PLACEMENT_3D ( 'NONE', #23043, #18160, #37793 ) ;
#48529=DIRECTION ( 'NONE',  ( -3.469446951953613696E-16, 0.000000000000000000, -1.000000000000000000 ) ) ;
#48531=VECTOR ( 'NONE', #44994, 39.37007874015748143 ) ;
#48532=ORIENTED_EDGE ( 'NONE', *, *, #36179, .F. ) ;
#48533=CARTESIAN_POINT ( 'NONE',  ( -1.091055626815042645, 3.346456692913386100, -0.9448818897637760728 ) ) ;
#48536=ORIENTED_EDGE ( 'NONE', *, *, #23875, .T. ) ;
#48538=ORIENTED_EDGE ( 'NONE', *, *, #44766, .F. ) ;
#48540=DIRECTION ( 'NONE',  ( -0.000000000000000000, 1.000000000000000000, -0.000000000000000000 ) ) ;
#48541=ORIENTED_EDGE ( 'NONE', *, *, #1367, .T. ) ;
#48543=FACE_OUTER_BOUND ( 'NONE', #13354, .T. ) ;
#48545=CARTESIAN_POINT ( 'NONE',  ( 0.2727639067037602172, 3.346456692913386100, -1.732283464566922726 ) ) ;
#48546=EDGE_CURVE ( 'NONE', #5661, #1626, #46270, .T. ) ;
#48547=ORIENTED_EDGE ( 'NONE', *, *, #47881, .F. ) ;
#48548=EDGE_CURVE ( 'NONE', #7183, #536, #30044, .T. ) ;
#48549=LINE ( 'NONE', #44198, #8174 ) ;
#48550=CARTESIAN_POINT ( 'NONE',  ( -0.2727639067037607723, 0.000000000000000000, -0.1574803149606301411 ) ) ;
#48552=LINE ( 'NONE', #24595, #31950 ) ;
#48553=ORIENTED_EDGE ( 'NONE', *, *, #42057, .F. ) ;
#48554=EDGE_CURVE ( 'NONE', #3036, #36908, #50122, .T. ) ;
#48556=CARTESIAN_POINT ( 'NONE',  ( -0.9302092402134559679, 3.346456692913386100, 1.889763779527550147 ) ) ;
#48557=ADVANCED_FACE ( 'NONE', ( #2931 ), #34433, .F. ) ;
#48558=DIRECTION ( 'NONE',  ( 0.000000000000000000, 0.000000000000000000, -1.000000000000000000 ) ) ;
#48559=ORIENTED_EDGE ( 'NONE', *, *, #16470, .F. ) ;
#48560=ORIENTED_EDGE ( 'NONE', *, *, #10519, .T. ) ;
#48561=B_SPLINE_CURVE_WITH_KNOTS ( 'NONE', 3,
 ( #9165, #41181, #21043, #24914 ),
 .UNSPECIFIED., .F., .F.,
 ( 4, 4 ),
 ( 0.05135061866764987354, 0.05233018460755119172 ),
 .UNSPECIFIED. ) ;
#48562=CARTESIAN_POINT ( 'NONE',  ( -2.182111253630085290, 3.346456692913386100, 0.9448818897637749625 ) ) ;
#48566=CARTESIAN_POINT ( 'NONE',  ( -1.985260859929297794, 3.346456692913386100, -0.5118110236220464460 ) ) ;
#48572=VECTOR ( 'NONE', #24645, 39.37007874015748143 ) ;
#48575=LINE ( 'NONE', #33645, #25948 ) ;
#48576=CARTESIAN_POINT ( 'NONE',  ( 0.1968503937007869686, 0.000000000000000000, -2.086614173228339641 ) ) ;
#48580=CARTESIAN_POINT ( 'NONE',  ( -0.8182917201112817063, 3.267716535433071279, 1.419509857074483046E-16 ) ) ;
#48581=LINE ( 'NONE', #44988, #23230 ) ;
#48582=VERTEX_POINT ( 'NONE', #41917 ) ;
#48584=DIRECTION ( 'NONE',  ( 0.000000000000000000, 0.000000000000000000, -1.000000000000000000 ) ) ;
#48585=VECTOR ( 'NONE', #9799, 39.37007874015748143 ) ;
#48586=EDGE_LOOP ( 'NONE', ( #405, #35901, #6527, #47458, #37199 ) ) ;
#48587=PLANE ( 'NONE',  #9360 ) ;
#48588=DIRECTION ( 'NONE',  ( -1.000000000000000000, 0.000000000000000000, 0.000000000000000000 ) ) ;
#48589=EDGE_CURVE ( 'NONE', #45311, #10447, #42416, .T. ) ;
#48590=ADVANCED_FACE ( 'NONE', ( #26419 ), #19168, .F. ) ;
#48595=CARTESIAN_POINT ( 'NONE',  ( 1.287906020515830585, 3.346456692913386100, 1.889763779527550369 ) ) ;
#48596=EDGE_CURVE ( 'NONE', #12397, #50364, #5369, .T. ) ;
#48597=AXIS2_PLACEMENT_3D ( 'NONE', #42818, #14960, #7460 ) ;
#48600=LINE ( 'NONE', #38054, #30962 ) ;
#48602=LINE ( 'NONE', #13284, #43577 ) ;
#48604=ORIENTED_EDGE ( 'NONE', *, *, #40903, .F. ) ;
#48605=CARTESIAN_POINT ( 'NONE',  ( -0.2727639067037608278, 0.000000000000000000, -1.929133858267710000 ) ) ;
#48606=CARTESIAN_POINT ( 'NONE',  ( -2.182111253630085734, 0.000000000000000000, -1.141732283464563791 ) ) ;
#48609=DIRECTION ( 'NONE',  ( -0.000000000000000000, 1.000000000000000000, -0.000000000000000000 ) ) ;
#48611=LINE ( 'NONE', #16911, #26097 ) ;
#48612=DIRECTION ( 'NONE',  ( -1.000000000000000000, 0.000000000000000000, 1.734723475976806848E-16 ) ) ;
#48616=CARTESIAN_POINT ( 'NONE',  ( 0.000000000000000000, 3.267716535433071279, 0.9055118110236164419 ) ) ;
#48617=DIRECTION ( 'NONE',  ( -1.000000000000000000, 0.000000000000000000, -0.000000000000000000 ) ) ;
#48619=ORIENTED_EDGE ( 'NONE', *, *, #48016, .F. ) ;
#48620=CARTESIAN_POINT ( 'NONE',  ( 0.000000000000000000, 3.267716535433071279, -0.9842519685039344823 ) ) ;
#48621=FACE_BOUND ( 'NONE', #42110, .T. ) ;
#48623=ORIENTED_EDGE ( 'NONE', *, *, #16884, .T. ) ;
#48624=EDGE_CURVE ( 'NONE', #35542, #29386, #13163, .T. ) ;
#48625=DIRECTION ( 'NONE',  ( -0.000000000000000000, 1.000000000000000000, -0.000000000000000000 ) ) ;
#48627=ORIENTED_EDGE ( 'NONE', *, *, #18548, .F. ) ;
#48629=ORIENTED_EDGE ( 'NONE', *, *, #16932, .F. ) ;
#48630=DIRECTION ( 'NONE',  ( -1.000000000000000000, 0.000000000000000000, 1.734723475976806848E-16 ) ) ;
#48635=AXIS2_PLACEMENT_3D ( 'NONE', #39403, #28285, #37331 ) ;
#48636=DIRECTION ( 'NONE',  ( -1.000000000000000000, 0.000000000000000000, 0.000000000000000000 ) ) ;
#48637=LINE ( 'NONE', #44792, #41021 ) ;
#48638=CARTESIAN_POINT ( 'NONE',  ( -1.091055626815042645, 3.346456692913386100, -1.141732283464563569 ) ) ;
#48639=ORIENTED_EDGE ( 'NONE', *, *, #2206, .T. ) ;
#48640=DIRECTION ( 'NONE',  ( 1.734723475976806848E-16, 0.000000000000000000, 1.000000000000000000 ) ) ;
#48641=VECTOR ( 'NONE', #34313, 39.37007874015748143 ) ;
#48642=DIRECTION ( 'NONE',  ( -3.469446951953613696E-16, 0.000000000000000000, -1.000000000000000000 ) ) ;
#48645=CARTESIAN_POINT ( 'NONE',  ( -1.363819533518803473, 3.267716535433071279, 2.027638360164056852 ) ) ;
#48646=ORIENTED_EDGE ( 'NONE', *, *, #4703, .T. ) ;
#48647=DIRECTION ( 'NONE',  ( 0.000000000000000000, 1.000000000000000000, 0.000000000000000000 ) ) ;
#48648=CARTESIAN_POINT ( 'NONE',  ( -0.2727639067037602727, 0.000000000000000000, 1.850393700787392293 ) ) ;
#48650=EDGE_CURVE ( 'NONE', #6833, #30930, #48476, .T. ) ;
#48651=ORIENTED_EDGE ( 'NONE', *, *, #10915, .F. ) ;
#48652=DIRECTION ( 'NONE',  ( -0.000000000000000000, 1.000000000000000000, -0.000000000000000000 ) ) ;
#48654=FACE_BOUND ( 'NONE', #20179, .T. ) ;
#48656=LINE ( 'NONE', #697, #2027 ) ;
#48657=DIRECTION ( 'NONE',  ( 0.000000000000000000, -1.000000000000000000, 0.000000000000000000 ) ) ;
#48658=DIRECTION ( 'NONE',  ( -0.000000000000000000, 1.000000000000000000, -0.000000000000000000 ) ) ;
#48659=EDGE_CURVE ( 'NONE', #26933, #49804, #31563, .T. ) ;
#48660=ADVANCED_FACE ( 'NONE', ( #17039 ), #35688, .F. ) ;
#48663=DIRECTION ( 'NONE',  ( 1.734723475976806848E-16, -0.000000000000000000, 1.000000000000000000 ) ) ;
#48665=ORIENTED_EDGE ( 'NONE', *, *, #18268, .T. ) ;
#48666=DIRECTION ( 'NONE',  ( 1.000000000000000000, 0.000000000000000000, -3.469446951953613696E-16 ) ) ;
#48667=ORIENTED_EDGE ( 'NONE', *, *, #4623, .T. ) ;
#48670=AXIS2_PLACEMENT_3D ( 'NONE', #44368, #9011, #21143 ) ;
#48671=ADVANCED_FACE ( 'NONE', ( #35182 ), #31825, .F. ) ;
#48672=ORIENTED_EDGE ( 'NONE', *, *, #9241, .T. ) ;
#48673=DIRECTION ( 'NONE',  ( 1.734723475976806848E-16, -0.000000000000000000, 1.000000000000000000 ) ) ;
#48679=AXIS2_PLACEMENT_3D ( 'NONE', #37619, #17986, #2743 ) ;
#48680=ORIENTED_EDGE ( 'NONE', *, *, #38720, .F. ) ;
#48681=EDGE_CURVE ( 'NONE', #6600, #15817, #19673, .T. ) ;
#48682=ORIENTED_EDGE ( 'NONE', *, *, #44854, .F. ) ;
#48686=ORIENTED_EDGE ( 'NONE', *, *, #15522, .F. ) ;
#48688=EDGE_CURVE ( 'NONE', #45405, #14632, #40783, .T. ) ;
#48689=VERTEX_POINT ( 'NONE', #9537 ) ;
#48690=DIRECTION ( 'NONE',  ( -0.000000000000000000, 1.000000000000000000, -0.000000000000000000 ) ) ;
#48691=DIRECTION ( 'NONE',  ( 0.000000000000000000, -1.000000000000000000, 0.000000000000000000 ) ) ;
#48692=ORIENTED_EDGE ( 'NONE', *, *, #49935, .T. ) ;
#48697=LINE ( 'NONE', #28348, #3537 ) ;
#48699=AXIS2_PLACEMENT_3D ( 'NONE', #45908, #35075, #31202 ) ;
#48700=DIRECTION ( 'NONE',  ( -0.000000000000000000, 1.000000000000000000, -0.000000000000000000 ) ) ;
#48702=LINE ( 'NONE', #45358, #47862 ) ;
#48704=VECTOR ( 'NONE', #13987, 39.37007874015748143 ) ;
#48705=DIRECTION ( 'NONE',  ( 0.000000000000000000, -1.000000000000000000, 0.000000000000000000 ) ) ;
#48707=LINE ( 'NONE', #16755, #46013 ) ;
#48708=CARTESIAN_POINT ( 'NONE',  ( -1.636583440222563635, 3.346456692913386100, 1.259842519685033357 ) ) ;
#48710=CARTESIAN_POINT ( 'NONE',  ( 2.081842287654605883, 3.245535198059565030, -1.299212598425194320 ) ) ;
#48712=ORIENTED_EDGE ( 'NONE', *, *, #39480, .T. ) ;
#48713=CARTESIAN_POINT ( 'NONE',  ( 0.2727639067037610499, 3.346456692913386100, 1.417322834645662777 ) ) ;
#48714=EDGE_CURVE ( 'NONE', #13413, #17741, #15562, .T. ) ;
#48715=DIRECTION ( 'NONE',  ( 1.000000000000000000, 0.000000000000000000, 0.000000000000000000 ) ) ;
#48716=VECTOR ( 'NONE', #26961, 39.37007874015748143 ) ;
#48718=DIRECTION ( 'NONE',  ( 1.734723475976806848E-16, -0.000000000000000000, 1.000000000000000000 ) ) ;
#48719=DIRECTION ( 'NONE',  ( 0.000000000000000000, 1.000000000000000000, 0.000000000000000000 ) ) ;
#48721=EDGE_CURVE ( 'NONE', #37350, #11567, #47005, .T. ) ;
#48723=FACE_BOUND ( 'NONE', #48112, .T. ) ;
#48724=ORIENTED_EDGE ( 'NONE', *, *, #40814, .T. ) ;
#48726=ORIENTED_EDGE ( 'NONE', *, *, #5059, .T. ) ;
#48728=FACE_OUTER_BOUND ( 'NONE', #38942, .T. ) ;
#48731=ORIENTED_EDGE ( 'NONE', *, *, #3123, .F. ) ;
#48735=FACE_BOUND ( 'NONE', #3194, .T. ) ;
#48738=VECTOR ( 'NONE', #28994, 39.37007874015748143 ) ;
#48739=VECTOR ( 'NONE', #45029, 39.37007874015748143 ) ;
#48742=EDGE_CURVE ( 'NONE', #3322, #15064, #15028, .T. ) ;
#48744=DIRECTION ( 'NONE',  ( 1.734723475976806848E-16, -0.000000000000000000, 1.000000000000000000 ) ) ;
#48746=DIRECTION ( 'NONE',  ( -0.000000000000000000, 0.000000000000000000, 1.000000000000000000 ) ) ;
#48747=ORIENTED_EDGE ( 'NONE', *, *, #50003, .T. ) ;
#48748=ORIENTED_EDGE ( 'NONE', *, *, #4272, .F. ) ;
#48750=EDGE_CURVE ( 'NONE', #2388, #25196, #1786, .T. ) ;
#48752=DIRECTION ( 'NONE',  ( -0.000000000000000000, 1.000000000000000000, -0.000000000000000000 ) ) ;
#48754=LINE ( 'NONE', #29435, #11782 ) ;
#48755=EDGE_CURVE ( 'NONE', #18572, #47436, #26302, .T. ) ;
#48757=DIRECTION ( 'NONE',  ( 1.734723475976806848E-16, -0.000000000000000000, 1.000000000000000000 ) ) ;
#48760=ORIENTED_EDGE ( 'NONE', *, *, #29732, .T. ) ;
#48761=PLANE ( 'NONE',  #42261 ) ;
#48764=DIRECTION ( 'NONE',  ( -0.000000000000000000, 1.000000000000000000, -0.000000000000000000 ) ) ;
#48765=EDGE_CURVE ( 'NONE', #50693, #16476, #37427, .T. ) ;
#48766=DIRECTION ( 'NONE',  ( 1.734723475976806848E-16, 0.000000000000000000, 1.000000000000000000 ) ) ;
#48769=PLANE ( 'NONE',  #48932 ) ;
#48770=ORIENTED_EDGE ( 'NONE', *, *, #41233, .T. ) ;
#48771=CARTESIAN_POINT ( 'NONE',  ( -1.636583440222563635, 3.346456692913386100, 0.7480314960629874665 ) ) ;
#48772=LINE ( 'NONE', #36694, #12860 ) ;
#48773=ORIENTED_EDGE ( 'NONE', *, *, #48241, .T. ) ;
#48775=EDGE_CURVE ( 'NONE', #23942, #35864, #26045, .T. ) ;
#48776=DIRECTION ( 'NONE',  ( 0.000000000000000000, 0.000000000000000000, -1.000000000000000000 ) ) ;
#48778=DIRECTION ( 'NONE',  ( 0.000000000000000000, -1.000000000000000000, 0.000000000000000000 ) ) ;
#48780=EDGE_CURVE ( 'NONE', #5399, #16323, #48988, .T. ) ;
#48781=VECTOR ( 'NONE', #3435, 39.37007874015748143 ) ;
#48782=EDGE_CURVE ( 'NONE', #6227, #31182, #2049, .T. ) ;
#48783=ORIENTED_EDGE ( 'NONE', *, *, #43202, .F. ) ;
#48784=CARTESIAN_POINT ( 'NONE',  ( -0.5455278134075214336, 0.000000000000000000, 2.204724409448808764 ) ) ;
#48786=VECTOR ( 'NONE', #42028, 39.37007874015748143 ) ;
#48787=CARTESIAN_POINT ( 'NONE',  ( -1.363819533518803029, 3.346456692913386100, 0.7874015748031456541 ) ) ;
#48788=PLANE ( 'NONE',  #42843 ) ;
#48790=ORIENTED_EDGE ( 'NONE', *, *, #5685, .F. ) ;
#48791=ORIENTED_EDGE ( 'NONE', *, *, #17590, .T. ) ;
#48792=CARTESIAN_POINT ( 'NONE',  ( 0.2727639067037604947, 0.000000000000000000, 0.1574803149606283648 ) ) ;
#48793=ORIENTED_EDGE ( 'NONE', *, *, #25382, .T. ) ;
#48795=LINE ( 'NONE', #34118, #4224 ) ;
#48796=CARTESIAN_POINT ( 'NONE',  ( 0.000000000000000000, 3.346456692913386100, 0.000000000000000000 ) ) ;
#48798=ORIENTED_EDGE ( 'NONE', *, *, #25483, .F. ) ;
#48799=DIRECTION ( 'NONE',  ( -0.000000000000000000, 1.000000000000000000, -0.000000000000000000 ) ) ;
#48802=ORIENTED_EDGE ( 'NONE', *, *, #43442, .F. ) ;
#48803=LINE ( 'NONE', #10120, #16662 ) ;
#48804=CARTESIAN_POINT ( 'NONE',  ( 1.560669927219590747, 3.267716535433071279, 1.414498409778230492 ) ) ;
#48805=CARTESIAN_POINT ( 'NONE',  ( -1.636583440222563635, 3.267716535433071279, 2.839019714148966584E-16 ) ) ;
#48806=ORIENTED_EDGE ( 'NONE', *, *, #9074, .F. ) ;
#48807=EDGE_LOOP ( 'NONE', ( #16895, #15805, #2510, #30971 ) ) ;
#48809=CARTESIAN_POINT ( 'NONE',  ( 0.000000000000000000, 3.267716535433071279, 2.165354330708650465 ) ) ;
#48811=ADVANCED_FACE ( 'NONE', ( #42047 ), #6176, .F. ) ;
#48812=EDGE_CURVE ( 'NONE', #22659, #14850, #45637, .T. ) ;
#48814=LINE ( 'NONE', #45469, #9025 ) ;
#48815=VERTEX_POINT ( 'NONE', #38191 ) ;
#48816=ORIENTED_EDGE ( 'NONE', *, *, #32831, .F. ) ;
#48818=VECTOR ( 'NONE', #46341, 39.37007874015748143 ) ;
#48819=LINE ( 'NONE', #16872, #21781 ) ;
#48821=ORIENTED_EDGE ( 'NONE', *, *, #31680, .F. ) ;
#48822=DIRECTION ( 'NONE',  ( -1.000000000000000000, 0.000000000000000000, 0.000000000000000000 ) ) ;
#48823=DIRECTION ( 'NONE',  ( 1.000000000000000000, 0.000000000000000000, 0.000000000000000000 ) ) ;
#48825=VECTOR ( 'NONE', #49017, 39.37007874015748143 ) ;
#48831=EDGE_CURVE ( 'NONE', #48458, #19314, #33813, .T. ) ;
#48833=VERTEX_POINT ( 'NONE', #21927 ) ;
#48834=DIRECTION ( 'NONE',  ( 0.000000000000000000, -1.000000000000000000, 0.000000000000000000 ) ) ;
#48835=EDGE_CURVE ( 'NONE', #40451, #20168, #10558, .T. ) ;
#48836=LINE ( 'NONE', #13269, #2243 ) ;
#48837=LINE ( 'NONE', #45238, #48531 ) ;
#48838=VERTEX_POINT ( 'NONE', #5667 ) ;
#48840=EDGE_CURVE ( 'NONE', #47624, #784, #13927, .T. ) ;
#48841=DIRECTION ( 'NONE',  ( -0.000000000000000000, 1.000000000000000000, -0.000000000000000000 ) ) ;
#48846=EDGE_LOOP ( 'NONE', ( #49006, #25917, #5358, #9410 ) ) ;
#48847=CARTESIAN_POINT ( 'NONE',  ( 0.5455278134075217666, 0.000000000000000000, 1.889763779527550369 ) ) ;
#48849=DIRECTION ( 'NONE',  ( -0.000000000000000000, 1.000000000000000000, -0.000000000000000000 ) ) ;
#48851=CARTESIAN_POINT ( 'NONE',  ( 0.4696143004045484903, 3.267716535433071279, 1.102362204724404160 ) ) ;
#48852=AXIS2_PLACEMENT_3D ( 'NONE', #23821, #32347, #39821 ) ;
#48854=ORIENTED_EDGE ( 'NONE', *, *, #34854, .T. ) ;
#48855=CARTESIAN_POINT ( 'NONE',  ( -0.5455278134075208785, 3.346456692913386100, 1.259842519685033357 ) ) ;
#48856=CARTESIAN_POINT ( 'NONE',  ( -1.363819533518803029, 0.000000000000000000, 1.102362204724404160 ) ) ;
#48857=ORIENTED_EDGE ( 'NONE', *, *, #46475, .T. ) ;
#48858=CARTESIAN_POINT ( 'NONE',  ( -0.5455278134075212115, 3.267716535433071279, 9.463399047163220715E-17 ) ) ;
#48860=FACE_OUTER_BOUND ( 'NONE', #17709, .T. ) ;
#48861=VECTOR ( 'NONE', #28142, 39.37007874015748143 ) ;
#48862=VECTOR ( 'NONE', #19079, 39.37007874015748143 ) ;
#48864=VERTEX_POINT ( 'NONE', #14170 ) ;
#48868=EDGE_LOOP ( 'NONE', ( #37808, #13116, #28061, #18253 ) ) ;
#48870=FACE_BOUND ( 'NONE', #8784, .T. ) ;
#48875=ORIENTED_EDGE ( 'NONE', *, *, #452, .T. ) ;
#48877=ORIENTED_EDGE ( 'NONE', *, *, #16866, .F. ) ;
#48878=LINE ( 'NONE', #6329, #29412 ) ;
#48880=ORIENTED_EDGE ( 'NONE', *, *, #10650, .F. ) ;
#48881=EDGE_CURVE ( 'NONE', #19346, #49275, #10802, .T. ) ;
#48883=DIRECTION ( 'NONE',  ( -1.000000000000000000, 0.000000000000000000, 1.734723475976806848E-16 ) ) ;
#48884=CARTESIAN_POINT ( 'NONE',  ( 1.363819533518803695, 3.267716535433071279, 1.732283464566921172 ) ) ;
#48886=DIRECTION ( 'NONE',  ( 1.000000000000000000, 0.000000000000000000, 0.000000000000000000 ) ) ;
#48887=FACE_OUTER_BOUND ( 'NONE', #2195, .T. ) ;
#48888=VECTOR ( 'NONE', #29160, 39.37007874015748143 ) ;
#48891=EDGE_LOOP ( 'NONE', ( #17349, #27886, #46761, #28977 ) ) ;
#48893=VECTOR ( 'NONE', #35735, 39.37007874015748143 ) ;
#48896=VECTOR ( 'NONE', #27268, 39.37007874015748143 ) ;
#48898=CARTESIAN_POINT ( 'NONE',  ( 2.106197740627112402, 3.267716535433071279, -7.307341331430322647E-16 ) ) ;
#48899=EDGE_CURVE ( 'NONE', #39780, #28095, #41293, .T. ) ;
#48901=VERTEX_POINT ( 'NONE', #19553 ) ;
#48902=LINE ( 'NONE', #2223, #37061 ) ;
#48903=LINE ( 'NONE', #17715, #12637 ) ;
#48905=VECTOR ( 'NONE', #7288, 39.37007874015748143 ) ;
#48906=ADVANCED_FACE ( 'NONE', ( #39442 ), #7442, .F. ) ;
#48908=DIRECTION ( 'NONE',  ( -3.469446951953613696E-16, 0.000000000000000000, -1.000000000000000000 ) ) ;
#48909=VERTEX_POINT ( 'NONE', #43298 ) ;
#48910=FACE_BOUND ( 'NONE', #31443, .T. ) ;
#48911=CARTESIAN_POINT ( 'NONE',  ( -1.195183497228115035E-16, 0.000000000000000000, 0.6299212598425161236 ) ) ;
#48913=LINE ( 'NONE', #37356, #34258 ) ;
#48914=VERTEX_POINT ( 'NONE', #35321 ) ;
#48915=ORIENTED_EDGE ( 'NONE', *, *, #36057, .F. ) ;
#48916=LINE ( 'NONE', #40466, #22979 ) ;
#48917=ORIENTED_EDGE ( 'NONE', *, *, #34238, .T. ) ;
#48918=CARTESIAN_POINT ( 'NONE',  ( -0.2727639067037602172, 0.000000000000000000, 1.417322834645662777 ) ) ;
#48919=VERTEX_POINT ( 'NONE', #27301 ) ;
#48920=CARTESIAN_POINT ( 'NONE',  ( 1.966928503432568975, 3.267716535433071279, 0.9055118110236164419 ) ) ;
#48921=ORIENTED_EDGE ( 'NONE', *, *, #5901, .T. ) ;
#48923=VECTOR ( 'NONE', #139, 39.37007874015748143 ) ;
#48924=CARTESIAN_POINT ( 'NONE',  ( -0.3486774197067339376, 3.346456692913386100, 2.137096964226333107 ) ) ;
#48925=AXIS2_PLACEMENT_3D ( 'NONE', #33071, #13437, #33325 ) ;
#48929=ORIENTED_EDGE ( 'NONE', *, *, #48782, .F. ) ;
#48931=VECTOR ( 'NONE', #3995, 39.37007874015748143 ) ;
#48932=AXIS2_PLACEMENT_3D ( 'NONE', #44922, #5706, #37207 ) ;
#48933=VERTEX_POINT ( 'NONE', #15939 ) ;
#48934=ORIENTED_EDGE ( 'NONE', *, *, #34488, .F. ) ;
#48935=CARTESIAN_POINT ( 'NONE',  ( 0.000000000000000000, 3.346456692913386100, 0.000000000000000000 ) ) ;
#48937=AXIS2_PLACEMENT_3D ( 'NONE', #29962, #11351, #6217 ) ;
#48938=EDGE_CURVE ( 'NONE', #12593, #13726, #7690, .T. ) ;
#48940=CARTESIAN_POINT ( 'NONE',  ( -0.07591351300297284610, 3.267716535433071279, 1.220472440944875281 ) ) ;
#48941=ORIENTED_EDGE ( 'NONE', *, *, #13029, .F. ) ;
#48944=ADVANCED_FACE ( 'NONE', ( #34562 ), #38934, .F. ) ;
#48947=ORIENTED_EDGE ( 'NONE', *, *, #28101, .T. ) ;
#48948=CARTESIAN_POINT ( 'NONE',  ( -1.091055626815042645, 3.267716535433071279, 1.889763779527550147 ) ) ;
#48951=CARTESIAN_POINT ( 'NONE',  ( -2.182111253630085290, 3.346456692913386100, -6.146657985744592735E-16 ) ) ;
#48952=CARTESIAN_POINT ( 'NONE',  ( 0.1968503937007872462, 3.346456692913386100, -1.456692913385822630 ) ) ;
#48953=CARTESIAN_POINT ( 'NONE',  ( -1.909347346926324906, 0.000000000000000000, 1.220472440944875059 ) ) ;
#48955=DIRECTION ( 'NONE',  ( 1.000000000000000000, -0.000000000000000000, 0.000000000000000000 ) ) ;
#48957=ORIENTED_EDGE ( 'NONE', *, *, #32499, .T. ) ;
#48958=DIRECTION ( 'NONE',  ( -0.000000000000000000, 1.000000000000000000, -0.000000000000000000 ) ) ;
#48959=CARTESIAN_POINT ( 'NONE',  ( 0.000000000000000000, 3.267716535433071279, 0.9448818897637749625 ) ) ;
#48963=DIRECTION ( 'NONE',  ( -0.000000000000000000, 1.000000000000000000, -0.000000000000000000 ) ) ;
#48965=ADVANCED_FACE ( 'NONE', ( #3820 ), #19299, .F. ) ;
#48967=ORIENTED_EDGE ( 'NONE', *, *, #31514, .T. ) ;
#48969=VECTOR ( 'NONE', #43284, 39.37007874015748143 ) ;
#48970=FACE_OUTER_BOUND ( 'NONE', #28910, .T. ) ;
#48972=CARTESIAN_POINT ( 'NONE',  ( 2.378961647330872786, 3.267716535433071279, 0.1181102362204698858 ) ) ;
#48974=FACE_OUTER_BOUND ( 'NONE', #35270, .T. ) ;
#48975=PLANE ( 'NONE',  #49127 ) ;
#48977=ADVANCED_FACE ( 'NONE', ( #15445 ), #47140, .F. ) ;
#48978=CARTESIAN_POINT ( 'NONE',  ( 0.2727639067037609943, 0.000000000000000000, 1.535433070866133898 ) ) ;
#48979=VECTOR ( 'NONE', #43975, 39.37007874015748143 ) ;
#48980=PLANE ( 'NONE',  #19648 ) ;
#48981=DIRECTION ( 'NONE',  ( 1.000000000000000000, 0.000000000000000000, -3.469446951953613696E-16 ) ) ;
#48982=ORIENTED_EDGE ( 'NONE', *, *, #9203, .F. ) ;
#48984=CARTESIAN_POINT ( 'NONE',  ( -1.909347346926324906, 3.267716535433071279, -1.102362204724405492 ) ) ;
#48985=EDGE_CURVE ( 'NONE', #18498, #44838, #46395, .T. ) ;
#48986=ORIENTED_EDGE ( 'NONE', *, *, #30089, .F. ) ;
#48987=DIRECTION ( 'NONE',  ( 1.734723475976806848E-16, 0.000000000000000000, 1.000000000000000000 ) ) ;
#48988=LINE ( 'NONE', #14430, #168 ) ;
#48990=ORIENTED_EDGE ( 'NONE', *, *, #24034, .F. ) ;
#48991=ORIENTED_EDGE ( 'NONE', *, *, #47467, .T. ) ;
#48992=CARTESIAN_POINT ( 'NONE',  ( 1.287906020515830585, 3.346456692913386100, 1.740706023381843659 ) ) ;
#48993=FACE_OUTER_BOUND ( 'NONE', #33736, .T. ) ;
#48994=FACE_BOUND ( 'NONE', #32921, .T. ) ;
#48995=LINE ( 'NONE', #21938, #36933 ) ;
#48996=CARTESIAN_POINT ( 'NONE',  ( -0.6214413264104945434, 3.346456692913386100, -2.047244094488181343 ) ) ;
#48997=ORIENTED_EDGE ( 'NONE', *, *, #1438, .F. ) ;
#48998=ORIENTED_EDGE ( 'NONE', *, *, #40487, .F. ) ;
#49000=AXIS2_PLACEMENT_3D ( 'NONE', #9829, #45165, #5180 ) ;
#49002=ORIENTED_EDGE ( 'NONE', *, *, #41792, .F. ) ;
#49003=ORIENTED_EDGE ( 'NONE', *, *, #17510, .T. ) ;
#49006=ORIENTED_EDGE ( 'NONE', *, *, #23698, .T. ) ;
#49007=CARTESIAN_POINT ( 'NONE',  ( -1.166969139818015977, 3.346456692913386100, -1.732283464566922726 ) ) ;
#49010=EDGE_CURVE ( 'NONE', #3513, #46251, #23429, .T. ) ;
#49012=EDGE_CURVE ( 'NONE', #12583, #10448, #19805, .T. ) ;
#49015=EDGE_LOOP ( 'NONE', ( #39904, #33710, #32341, #12765 ) ) ;
#49017=DIRECTION ( 'NONE',  ( -0.000000000000000000, 1.000000000000000000, -0.000000000000000000 ) ) ;
#49018=CARTESIAN_POINT ( 'NONE',  ( -1.363819533518803473, 3.346456692913386100, -0.6692913385826760875 ) ) ;
#49021=LINE ( 'NONE', #13705, #21051 ) ;
#49023=ORIENTED_EDGE ( 'NONE', *, *, #37072, .F. ) ;
#49029=DIRECTION ( 'NONE',  ( -3.469446951953613696E-16, 0.000000000000000000, -1.000000000000000000 ) ) ;
#49030=VERTEX_POINT ( 'NONE', #15689 ) ;
#49031=EDGE_CURVE ( 'NONE', #9971, #44436, #11811, .T. ) ;
#49032=VECTOR ( 'NONE', #50771, 39.37007874015748143 ) ;
#49033=VECTOR ( 'NONE', #36065, 39.37007874015748143 ) ;
#49034=VERTEX_POINT ( 'NONE', #36341 ) ;
#49035=AXIS2_PLACEMENT_3D ( 'NONE', #34347, #18846, #22717 ) ;
#49036=CARTESIAN_POINT ( 'NONE',  ( 0.4696143004045484903, 0.000000000000000000, 1.417322834645662777 ) ) ;
#49038=AXIS2_PLACEMENT_3D ( 'NONE', #8825, #305, #31819 ) ;
#49039=ORIENTED_EDGE ( 'NONE', *, *, #22861, .F. ) ;
#49040=CARTESIAN_POINT ( 'NONE',  ( 1.015142113812069313, 3.267716535433071279, -0.6692913385826764205 ) ) ;
#49041=DIRECTION ( 'NONE',  ( -3.469446951953613696E-16, 0.000000000000000000, -1.000000000000000000 ) ) ;
#49042=EDGE_CURVE ( 'NONE', #17416, #12576, #20821, .T. ) ;
#49044=ORIENTED_EDGE ( 'NONE', *, *, #45823, .T. ) ;
#49045=VECTOR ( 'NONE', #30104, 39.37007874015748143 ) ;
#49048=VERTEX_POINT ( 'NONE', #48418 ) ;
#49049=ADVANCED_FACE ( 'NONE', ( #20844 ), #24465, .F. ) ;
#49052=FACE_OUTER_BOUND ( 'NONE', #44583, .T. ) ;
#49053=ADVANCED_FACE ( 'NONE', ( #13106 ), #8972, .F. ) ;
#49054=ORIENTED_EDGE ( 'NONE', *, *, #29128, .T. ) ;
#49056=DIRECTION ( 'NONE',  ( -0.000000000000000000, 1.000000000000000000, -0.000000000000000000 ) ) ;
#49058=ORIENTED_EDGE ( 'NONE', *, *, #39791, .F. ) ;
#49060=PLANE ( 'NONE',  #13720 ) ;
#49061=DIRECTION ( 'NONE',  ( -1.000000000000000000, 0.000000000000000000, 0.000000000000000000 ) ) ;
#49062=EDGE_LOOP ( 'NONE', ( #12177, #14515, #44210, #43773 ) ) ;
#49063=VERTEX_POINT ( 'NONE', #20057 ) ;
#49065=CARTESIAN_POINT ( 'NONE',  ( 0.1968503937007872462, 3.346456692913386100, 0.1181102362204701633 ) ) ;
#49067=EDGE_CURVE ( 'NONE', #536, #48466, #44574, .T. ) ;
#49068=EDGE_CURVE ( 'NONE', #13102, #38331, #17234, .T. ) ;
#49069=PLANE ( 'NONE',  #19732 ) ;
#49070=ORIENTED_EDGE ( 'NONE', *, *, #37125, .F. ) ;
#49071=ORIENTED_EDGE ( 'NONE', *, *, #24355, .F. ) ;
#49074=AXIS2_PLACEMENT_3D ( 'NONE', #14859, #27221, #6609 ) ;
#49076=VERTEX_POINT ( 'NONE', #44070 ) ;
#49077=DIRECTION ( 'NONE',  ( -0.000000000000000000, 1.000000000000000000, -0.000000000000000000 ) ) ;
#49078=CARTESIAN_POINT ( 'NONE',  ( 1.833433833923351353, 3.267716535433071279, 0.3149606299212576177 ) ) ;
#49081=EDGE_CURVE ( 'NONE', #46932, #10831, #454, .T. ) ;
#49082=CARTESIAN_POINT ( 'NONE',  ( 0.8182917201112819283, 0.000000000000000000, 0.1574803149606286423 ) ) ;
#49085=CIRCLE ( 'NONE', #30153, 2.165354330708661568 ) ;
#49086=ORIENTED_EDGE ( 'NONE', *, *, #48004, .T. ) ;
#49088=CARTESIAN_POINT ( 'NONE',  ( 2.106197740627112402, 3.346456692913386100, 1.102362204724403938 ) ) ;
#49089=CARTESIAN_POINT ( 'NONE',  ( 0.7423782071083087075, 3.346456692913386100, -1.259842519685035134 ) ) ;
#49092=DIRECTION ( 'NONE',  ( -1.000000000000000000, -0.000000000000000000, -0.000000000000000000 ) ) ;
#49093=LINE ( 'NONE', #33414, #35384 ) ;
#49094=VERTEX_POINT ( 'NONE', #43811 ) ;
#49095=EDGE_CURVE ( 'NONE', #4027, #5831, #8458, .T. ) ;
#49096=CARTESIAN_POINT ( 'NONE',  ( -0.2727639067037603837, 3.267716535433071279, 4.731699523581606660E-17 ) ) ;
#49097=CARTESIAN_POINT ( 'NONE',  ( -0.8182917201112814842, 3.267716535433071279, 1.220472440944875281 ) ) ;
#49098=ORIENTED_EDGE ( 'NONE', *, *, #35119, .F. ) ;
#49099=LINE ( 'NONE', #13785, #22232 ) ;
#49100=FACE_OUTER_BOUND ( 'NONE', #28131, .T. ) ;
#49104=DIRECTION ( 'NONE',  ( 0.000000000000000000, 1.000000000000000000, 0.000000000000000000 ) ) ;
#49105=CARTESIAN_POINT ( 'NONE',  ( 0.000000000000000000, 3.267716535433071279, -1.417322834645664331 ) ) ;
#49107=ADVANCED_FACE ( 'NONE', ( #28320 ), #5350, .F. ) ;
#49108=EDGE_CURVE ( 'NONE', #47112, #21738, #15862, .T. ) ;
#49110=EDGE_CURVE ( 'NONE', #30179, #35447, #47655, .T. ) ;
#49112=ORIENTED_EDGE ( 'NONE', *, *, #12627, .T. ) ;
#49115=VECTOR ( 'NONE', #19008, 39.37007874015748143 ) ;
#49116=LINE ( 'NONE', #29542, #35365 ) ;
#49118=EDGE_LOOP ( 'NONE', ( #46452, #8811, #28276, #19418 ) ) ;
#49120=LINE ( 'NONE', #13292, #10434 ) ;
#49121=PLANE ( 'NONE',  #20340 ) ;
#49122=VECTOR ( 'NONE', #18430, 39.37007874015748143 ) ;
#49125=CARTESIAN_POINT ( 'NONE',  ( 4.268512490100411402E-16, 0.000000000000000000, 1.889763779527550369 ) ) ;
#49127=AXIS2_PLACEMENT_3D ( 'NONE', #41030, #24766, #9269 ) ;
#49128=CARTESIAN_POINT ( 'NONE',  ( 1.833433833923351797, 3.267716535433071279, -6.361001426714001438E-16 ) ) ;
#49129=ORIENTED_EDGE ( 'NONE', *, *, #34360, .F. ) ;
#49131=FACE_OUTER_BOUND ( 'NONE', #47841, .T. ) ;
#49132=AXIS2_PLACEMENT_3D ( 'NONE', #49934, #2497, #14107 ) ;
#49133=ORIENTED_EDGE ( 'NONE', *, *, #5065, .F. ) ;
#49134=LINE ( 'NONE', #49633, #32367 ) ;
#49136=ORIENTED_EDGE ( 'NONE', *, *, #38218, .T. ) ;
#49137=EDGE_CURVE ( 'NONE', #4890, #20741, #20588, .T. ) ;
#49138=CARTESIAN_POINT ( 'NONE',  ( 0.1968503937007878568, 3.267716535433071279, 1.259842519685033357 ) ) ;
#49139=PLANE ( 'NONE',  #45626 ) ;
#49140=EDGE_CURVE ( 'NONE', #2123, #39618, #17736, .T. ) ;
#49141=EDGE_LOOP ( 'NONE', ( #37132, #49847, #567, #39047 ) ) ;
#49143=EDGE_CURVE ( 'NONE', #37431, #4542, #21610, .T. ) ;
#49144=CARTESIAN_POINT ( 'NONE',  ( 1.526828301548457834, 3.346456692913386100, 1.535433070866133898 ) ) ;
#49145=VERTEX_POINT ( 'NONE', #49687 ) ;
#49146=EDGE_CURVE ( 'NONE', #34665, #13554, #37370, .T. ) ;
#49147=CARTESIAN_POINT ( 'NONE',  ( 0.1968503937007870241, 3.267716535433071279, -2.204724409448811429 ) ) ;
#49148=DIRECTION ( 'NONE',  ( 0.000000000000000000, -1.000000000000000000, 0.000000000000000000 ) ) ;
#49150=PLANE ( 'NONE',  #8276 ) ;
#49151=CARTESIAN_POINT ( 'NONE',  ( -0.5455278134075208785, 0.000000000000000000, 1.574803149606291974 ) ) ;
#49152=LINE ( 'NONE', #18464, #40223 ) ;
#49153=VECTOR ( 'NONE', #49709, 39.37007874015748143 ) ;
#49154=ORIENTED_EDGE ( 'NONE', *, *, #5334, .F. ) ;
#49155=DIRECTION ( 'NONE',  ( 1.734723475976806848E-16, -0.000000000000000000, 1.000000000000000000 ) ) ;
#49156=AXIS2_PLACEMENT_3D ( 'NONE', #2204, #45288, #21319 ) ;
#49159=ORIENTED_EDGE ( 'NONE', *, *, #19461, .T. ) ;
#49163=CARTESIAN_POINT ( 'NONE',  ( 2.378961647330872786, 0.000000000000000000, -1.161035397307311917E-15 ) ) ;
#49164=AXIS2_PLACEMENT_3D ( 'NONE', #21313, #13564, #5814 ) ;
#49165=DIRECTION ( 'NONE',  ( 1.000000000000000000, 0.000000000000000000, 0.000000000000000000 ) ) ;
#49166=CARTESIAN_POINT ( 'NONE',  ( -0.8182917201112815953, 3.267716535433071279, 1.419509857074482553E-16 ) ) ;
#49167=VECTOR ( 'NONE', #14298, 39.37007874015748143 ) ;
#49168=ORIENTED_EDGE ( 'NONE', *, *, #34159, .T. ) ;
#49169=CARTESIAN_POINT ( 'NONE',  ( 1.636583440222563857, 0.000000000000000000, -0.6299212598425181220 ) ) ;
#49170=VERTEX_POINT ( 'NONE', #29087 ) ;
#49171=FACE_BOUND ( 'NONE', #44425, .T. ) ;
#49172=DIRECTION ( 'NONE',  ( -3.469446951953613696E-16, 0.000000000000000000, -1.000000000000000000 ) ) ;
#49173=LINE ( 'NONE', #37355, #22666 ) ;
#49174=CARTESIAN_POINT ( 'NONE',  ( 0.1968503937007870241, 0.000000000000000000, -2.204724409448811429 ) ) ;
#49175=EDGE_CURVE ( 'NONE', #45835, #46993, #41238, .T. ) ;
#49179=ORIENTED_EDGE ( 'NONE', *, *, #35866, .T. ) ;
#49180=EDGE_CURVE ( 'NONE', #5543, #18782, #45328, .T. ) ;
#49182=ORIENTED_EDGE ( 'NONE', *, *, #43117, .F. ) ;
#49183=CARTESIAN_POINT ( 'NONE',  ( -0.5455278134075214336, 0.000000000000000000, -8.878505979408855953E-16 ) ) ;
#49186=ORIENTED_EDGE ( 'NONE', *, *, #25973, .F. ) ;
#49187=DIRECTION ( 'NONE',  ( -0.000000000000000000, 1.000000000000000000, -0.000000000000000000 ) ) ;
#49188=AXIS2_PLACEMENT_3D ( 'NONE', #36762, #5770, #14025 ) ;
#49191=VERTEX_POINT ( 'NONE', #38132 ) ;
#49192=CARTESIAN_POINT ( 'NONE',  ( 0.000000000000000000, 3.267716535433071279, 1.535433070866133898 ) ) ;
#49194=ORIENTED_EDGE ( 'NONE', *, *, #28557, .F. ) ;
#49195=ADVANCED_FACE ( 'NONE', ( #33500 ), #18499, .F. ) ;
#49196=EDGE_CURVE ( 'NONE', #38185, #44444, #25475, .T. ) ;
#49197=VERTEX_POINT ( 'NONE', #33243 ) ;
#49199=LINE ( 'NONE', #22388, #5485 ) ;
#49200=EDGE_CURVE ( 'NONE', #2091, #15789, #10498, .T. ) ;
#49201=ORIENTED_EDGE ( 'NONE', *, *, #21282, .F. ) ;
#49203=CARTESIAN_POINT ( 'NONE',  ( 0.1968503937007869686, 3.267716535433071279, -2.401574803149598480 ) ) ;
#49204=EDGE_CURVE ( 'NONE', #48261, #19363, #26242, .T. ) ;
#49205=LINE ( 'NONE', #36874, #16172 ) ;
#49209=CARTESIAN_POINT ( 'NONE',  ( 0.1968503937007873017, 0.000000000000000000, -1.259842519685035134 ) ) ;
#49210=CARTESIAN_POINT ( 'NONE',  ( 2.100403847690402337, 3.346456692913386100, 0.1574803149606280872 ) ) ;
#49211=ORIENTED_EDGE ( 'NONE', *, *, #36503, .T. ) ;
#49212=DIRECTION ( 'NONE',  ( -1.000000000000000000, -0.000000000000000000, -0.000000000000000000 ) ) ;
#49213=DIRECTION ( 'NONE',  ( -1.000000000000000000, -0.000000000000000000, -0.000000000000000000 ) ) ;
#49218=VERTEX_POINT ( 'NONE', #2502 ) ;
#49219=CARTESIAN_POINT ( 'NONE',  ( 0.2727639067037604392, 3.346456692913386100, 0.2755905511810994302 ) ) ;
#49220=VECTOR ( 'NONE', #48294, 39.37007874015748143 ) ;
#49221=VECTOR ( 'NONE', #30729, 39.37007874015748143 ) ;
#49222=DIRECTION ( 'NONE',  ( 1.000000000000000000, -0.000000000000000000, 0.000000000000000000 ) ) ;
#49224=DIRECTION ( 'NONE',  ( 1.734723475976806848E-16, -0.000000000000000000, 1.000000000000000000 ) ) ;
#49225=ORIENTED_EDGE ( 'NONE', *, *, #38920, .F. ) ;
#49226=FACE_OUTER_BOUND ( 'NONE', #31293, .T. ) ;
#49227=CARTESIAN_POINT ( 'NONE',  ( 0.2727639067037604392, 0.000000000000000000, -0.03937007874015908959 ) ) ;
#49228=LINE ( 'NONE', #13910, #653 ) ;
#49234=EDGE_CURVE ( 'NONE', #28604, #16977, #13358, .T. ) ;
#49236=EDGE_CURVE ( 'NONE', #19595, #23409, #9989, .T. ) ;
#49239=PLANE ( 'NONE',  #42768 ) ;
#49240=CARTESIAN_POINT ( 'NONE',  ( -1.091055626815042201, 3.346456692913386100, 1.574803149606291974 ) ) ;
#49242=ORIENTED_EDGE ( 'NONE', *, *, #30690, .F. ) ;
#49243=ADVANCED_FACE ( 'NONE', ( #29865 ), #25227, .F. ) ;
#49244=CARTESIAN_POINT ( 'NONE',  ( -1.636583440222563635, 0.000000000000000000, 0.9448818897637749625 ) ) ;
#49245=DIRECTION ( 'NONE',  ( 1.734723475976806848E-16, -0.000000000000000000, 1.000000000000000000 ) ) ;
#49246=EDGE_CURVE ( 'NONE', #6476, #15435, #34001, .T. ) ;
#49247=DIRECTION ( 'NONE',  ( -0.000000000000000000, 0.000000000000000000, 1.000000000000000000 ) ) ;
#49248=ORIENTED_EDGE ( 'NONE', *, *, #6224, .T. ) ;
#49249=ORIENTED_EDGE ( 'NONE', *, *, #2407, .F. ) ;
#49251=FACE_BOUND ( 'NONE', #8407, .T. ) ;
#49253=CARTESIAN_POINT ( 'NONE',  ( 1.636583440222563857, 3.346456692913386100, 1.259842519685033135 ) ) ;
#49254=EDGE_CURVE ( 'NONE', #5100, #2988, #11742, .T. ) ;
#49255=DIRECTION ( 'NONE',  ( -3.469446951953613696E-16, 0.000000000000000000, -1.000000000000000000 ) ) ;
#49259=EDGE_LOOP ( 'NONE', ( #46287, #39522, #15365, #17142 ) ) ;
#49260=ORIENTED_EDGE ( 'NONE', *, *, #33906, .F. ) ;
#49261=CARTESIAN_POINT ( 'NONE',  ( -1.636583440222563635, 3.346456692913386100, 0.1181102362204704270 ) ) ;
#49262=LINE ( 'NONE', #1552, #45158 ) ;
#49263=EDGE_CURVE ( 'NONE', #44079, #22183, #14368, .T. ) ;
#49264=ORIENTED_EDGE ( 'NONE', *, *, #9348, .T. ) ;
#49265=ORIENTED_EDGE ( 'NONE', *, *, #33020, .F. ) ;
#49266=AXIS2_PLACEMENT_3D ( 'NONE', #40281, #24010, #16529 ) ;
#49267=ORIENTED_EDGE ( 'NONE', *, *, #12256, .F. ) ;
#49268=DIRECTION ( 'NONE',  ( -1.000000000000000000, 0.000000000000000000, -0.000000000000000000 ) ) ;
#49269=DIRECTION ( 'NONE',  ( -0.000000000000000000, 1.000000000000000000, -0.000000000000000000 ) ) ;
#49271=DIRECTION ( 'NONE',  ( -1.000000000000000000, 0.000000000000000000, -0.000000000000000000 ) ) ;
#49272=CARTESIAN_POINT ( 'NONE',  ( -0.2727639067037607723, 3.346456692913386100, -1.102362204724405714 ) ) ;
#49274=ORIENTED_EDGE ( 'NONE', *, *, #13485, .T. ) ;
#49275=VERTEX_POINT ( 'NONE', #23370 ) ;
#49276=LINE ( 'NONE', #34342, #48825 ) ;
#49277=LINE ( 'NONE', #42319, #3907 ) ;
#49278=DIRECTION ( 'NONE',  ( -3.469446951953613696E-16, 0.000000000000000000, -1.000000000000000000 ) ) ;
#49280=FACE_OUTER_BOUND ( 'NONE', #29965, .T. ) ;
#49281=LINE ( 'NONE', #29704, #50308 ) ;
#49282=CARTESIAN_POINT ( 'NONE',  ( -0.5455278134075214336, 3.346456692913386100, -1.771653543307081025 ) ) ;
#49283=DIRECTION ( 'NONE',  ( 1.734723475976806848E-16, -0.000000000000000000, 1.000000000000000000 ) ) ;
#49285=PLANE ( 'NONE',  #43178 ) ;
#49288=VERTEX_POINT ( 'NONE', #11257 ) ;
#49289=CARTESIAN_POINT ( 'NONE',  ( 0.000000000000000000, 3.346456692913386100, 0.000000000000000000 ) ) ;
#49290=ORIENTED_EDGE ( 'NONE', *, *, #40263, .T. ) ;
#49292=ORIENTED_EDGE ( 'NONE', *, *, #19003, .T. ) ;
#49293=DIRECTION ( 'NONE',  ( 1.734723475976806848E-16, -0.000000000000000000, 1.000000000000000000 ) ) ;
#49296=EDGE_CURVE ( 'NONE', #34006, #22659, #11509, .T. ) ;
#49297=AXIS2_PLACEMENT_3D ( 'NONE', #49125, #13551, #29801 ) ;
#49299=DIRECTION ( 'NONE',  ( -3.469446951953613696E-16, 0.000000000000000000, -1.000000000000000000 ) ) ;
#49301=EDGE_CURVE ( 'NONE', #10548, #6479, #7386, .T. ) ;
#49302=EDGE_CURVE ( 'NONE', #43953, #23181, #35258, .T. ) ;
#49303=VECTOR ( 'NONE', #19512, 39.37007874015748143 ) ;
#49304=ORIENTED_EDGE ( 'NONE', *, *, #13344, .F. ) ;
#49308=ORIENTED_EDGE ( 'NONE', *, *, #16257, .F. ) ;
#49311=CARTESIAN_POINT ( 'NONE',  ( 0.2727639067037609943, 0.000000000000000000, 0.9055118110236167750 ) ) ;
#49313=ORIENTED_EDGE ( 'NONE', *, *, #16062, .T. ) ;
#49314=CIRCLE ( 'NONE', #44405, 2.165354330708661568 ) ;
#49315=CARTESIAN_POINT ( 'NONE',  ( 0.4696143004045479352, 3.346456692913386100, 0.4724409448818868706 ) ) ;
#49318=CARTESIAN_POINT ( 'NONE',  ( 2.076281802138679300, 3.346456692913386100, -0.3543307086614178592 ) ) ;
#49319=EDGE_LOOP ( 'NONE', ( #34762, #22804, #2849, #23380 ) ) ;
#49321=LINE ( 'NONE', #2380, #35974 ) ;
#49323=EDGE_CURVE ( 'NONE', #27124, #13102, #27242, .T. ) ;
#49325=VERTEX_POINT ( 'NONE', #3508 ) ;
#49326=DIRECTION ( 'NONE',  ( -3.469446951953613696E-16, 0.000000000000000000, -1.000000000000000000 ) ) ;
#49328=CARTESIAN_POINT ( 'NONE',  ( -0.07591351300297284610, 0.000000000000000000, 1.535433070866133898 ) ) ;
#49331=ORIENTED_EDGE ( 'NONE', *, *, #13803, .F. ) ;
#49335=EDGE_CURVE ( 'NONE', #49191, #46791, #15634, .T. ) ;
#49336=CARTESIAN_POINT ( 'NONE',  ( 1.363819533518803251, 3.267716535433071279, -2.365849761790805487E-16 ) ) ;
#49337=AXIS2_PLACEMENT_3D ( 'NONE', #3952, #42921, #35449 ) ;
#49338=VECTOR ( 'NONE', #42842, 39.37007874015748143 ) ;
#49341=CARTESIAN_POINT ( 'NONE',  ( 1.015142113812069313, 3.346456692913386100, 0.7874015748031454320 ) ) ;
#49343=VERTEX_POINT ( 'NONE', #50435 ) ;
#49344=CARTESIAN_POINT ( 'NONE',  ( 0.7423782071083092626, 3.346456692913386100, 1.574803149606291974 ) ) ;
#49345=CARTESIAN_POINT ( 'NONE',  ( -1.363819533518803473, 3.267716535433071279, 2.365849761790805980E-16 ) ) ;
#49346=EDGE_CURVE ( 'NONE', #35447, #45462, #15385, .T. ) ;
#49348=DIRECTION ( 'NONE',  ( 1.734723475976806848E-16, 0.000000000000000000, 1.000000000000000000 ) ) ;
#49349=ADVANCED_FACE ( 'NONE', ( #3254 ), #7884, .F. ) ;
#49351=DIRECTION ( 'NONE',  ( 1.734723475976806848E-16, -0.000000000000000000, 1.000000000000000000 ) ) ;
#49352=CARTESIAN_POINT ( 'NONE',  ( 1.636583440222563857, 0.000000000000000000, -0.8267716535433055070 ) ) ;
#49354=ORIENTED_EDGE ( 'NONE', *, *, #34668, .F. ) ;
#49356=ORIENTED_EDGE ( 'NONE', *, *, #18392, .T. ) ;
#49357=DIRECTION ( 'NONE',  ( 0.000000000000000000, -0.000000000000000000, 1.000000000000000000 ) ) ;
#49359=ORIENTED_EDGE ( 'NONE', *, *, #43892, .T. ) ;
#49360=LINE ( 'NONE', #46014, #45947 ) ;
#49361=EDGE_CURVE ( 'NONE', #4073, #7296, #39124, .T. ) ;
#49362=PLANE ( 'NONE',  #2875 ) ;
#49363=CARTESIAN_POINT ( 'NONE',  ( 1.636583440222563635, 0.000000000000000000, -1.456692913385823296 ) ) ;
#49364=DIRECTION ( 'NONE',  ( 1.000000000000000000, -0.000000000000000000, 0.000000000000000000 ) ) ;
#49365=VECTOR ( 'NONE', #26669, 39.37007874015748143 ) ;
#49367=PLANE ( 'NONE',  #33771 ) ;
#49368=EDGE_LOOP ( 'NONE', ( #18112, #28247, #49201, #1314 ) ) ;
#49369=VERTEX_POINT ( 'NONE', #46589 ) ;
#49371=CARTESIAN_POINT ( 'NONE',  ( 0.2727639067037609943, 3.346456692913386100, 1.850393700787392293 ) ) ;
#49372=ORIENTED_EDGE ( 'NONE', *, *, #50263, .F. ) ;
#49373=CARTESIAN_POINT ( 'NONE',  ( 1.909347346926324684, 0.000000000000000000, 1.102362204724403938 ) ) ;
#49374=DIRECTION ( 'NONE',  ( 0.000000000000000000, -1.000000000000000000, 0.000000000000000000 ) ) ;
#49375=CARTESIAN_POINT ( 'NONE',  ( -0.2727639067037608278, 3.346456692913386100, -1.299212598425193210 ) ) ;
#49376=ORIENTED_EDGE ( 'NONE', *, *, #20193, .T. ) ;
#49380=CARTESIAN_POINT ( 'NONE',  ( 0.000000000000000000, 3.267716535433071279, 0.5905511811023579360 ) ) ;
#49381=ORIENTED_EDGE ( 'NONE', *, *, #28762, .T. ) ;
#49383=LINE ( 'NONE', #25673, #34749 ) ;
#49384=FACE_BOUND ( 'NONE', #41482, .T. ) ;
#49385=ORIENTED_EDGE ( 'NONE', *, *, #50056, .T. ) ;
#49388=VERTEX_POINT ( 'NONE', #4020 ) ;
#49390=DIRECTION ( 'NONE',  ( 1.000000000000000000, 0.000000000000000000, 0.000000000000000000 ) ) ;
#49393=EDGE_CURVE ( 'NONE', #4531, #2803, #23124, .T. ) ;
#49395=LINE ( 'NONE', #26694, #26094 ) ;
#49397=VERTEX_POINT ( 'NONE', #22620 ) ;
#49398=DIRECTION ( 'NONE',  ( -1.000000000000000000, -0.000000000000000000, -0.000000000000000000 ) ) ;
#49401=EDGE_CURVE ( 'NONE', #32285, #12432, #46092, .T. ) ;
#49403=EDGE_CURVE ( 'NONE', #19154, #26003, #8144, .T. ) ;
#49405=LINE ( 'NONE', #21831, #45115 ) ;
#49408=LINE ( 'NONE', #6343, #12612 ) ;
#49409=DIRECTION ( 'NONE',  ( -1.000000000000000000, 0.000000000000000000, 1.734723475976806848E-16 ) ) ;
#49411=VERTEX_POINT ( 'NONE', #20265 ) ;
#49415=DIRECTION ( 'NONE',  ( 0.000000000000000000, 0.000000000000000000, 1.000000000000000000 ) ) ;
#49417=CARTESIAN_POINT ( 'NONE',  ( 0.2727639067037610499, 0.000000000000000000, 1.417322834645662777 ) ) ;
#49418=FACE_OUTER_BOUND ( 'NONE', #2060, .T. ) ;
#49419=ORIENTED_EDGE ( 'NONE', *, *, #49428, .T. ) ;
#49420=CARTESIAN_POINT ( 'NONE',  ( 0.8182917201112817063, 0.000000000000000000, -2.244094488188969283 ) ) ;
#49423=DIRECTION ( 'NONE',  ( -0.000000000000000000, 1.000000000000000000, -0.000000000000000000 ) ) ;
#49424=LINE ( 'NONE', #45564, #45668 ) ;
#49425=EDGE_CURVE ( 'NONE', #11701, #42898, #7619, .T. ) ;
#49426=DIRECTION ( 'NONE',  ( -0.000000000000000000, 0.000000000000000000, 1.000000000000000000 ) ) ;
#49428=EDGE_CURVE ( 'NONE', #784, #11828, #27751, .T. ) ;
#49430=ORIENTED_EDGE ( 'NONE', *, *, #37252, .T. ) ;
#49431=VERTEX_POINT ( 'NONE', #4266 ) ;
#49438=DIRECTION ( 'NONE',  ( -0.000000000000000000, 1.000000000000000000, -0.000000000000000000 ) ) ;
#49439=ORIENTED_EDGE ( 'NONE', *, *, #1463, .T. ) ;
#49441=ORIENTED_EDGE ( 'NONE', *, *, #21895, .F. ) ;
#49442=ORIENTED_EDGE ( 'NONE', *, *, #24231, .T. ) ;
#49444=VECTOR ( 'NONE', #1360, 39.37007874015748143 ) ;
#49445=VERTEX_POINT ( 'NONE', #28518 ) ;
#49447=CARTESIAN_POINT ( 'NONE',  ( -0.7053729475263631477, 3.267716535433071279, 2.047244094488179567 ) ) ;
#49448=ORIENTED_EDGE ( 'NONE', *, *, #41520, .T. ) ;
#49450=CARTESIAN_POINT ( 'NONE',  ( 0.1968503937007872462, 3.267716535433071279, 0.4330708661417287386 ) ) ;
#49451=EDGE_CURVE ( 'NONE', #49431, #22488, #44520, .T. ) ;
#49452=EDGE_CURVE ( 'NONE', #1336, #2180, #44007, .T. ) ;
#49454=EDGE_CURVE ( 'NONE', #13787, #22204, #16665, .T. ) ;
#49456=DIRECTION ( 'NONE',  ( 1.734723475976806848E-16, -0.000000000000000000, 1.000000000000000000 ) ) ;
#49461=DIRECTION ( 'NONE',  ( 0.000000000000000000, 0.000000000000000000, -1.000000000000000000 ) ) ;
#49462=EDGE_CURVE ( 'NONE', #35644, #18957, #1160, .T. ) ;
#49463=ORIENTED_EDGE ( 'NONE', *, *, #42078, .F. ) ;
#49465=DIRECTION ( 'NONE',  ( 1.000000000000000000, 0.000000000000000000, 0.000000000000000000 ) ) ;
#49466=ORIENTED_EDGE ( 'NONE', *, *, #7557, .F. ) ;
#49467=FACE_OUTER_BOUND ( 'NONE', #28404, .T. ) ;
#49468=FACE_OUTER_BOUND ( 'NONE', #14291, .T. ) ;
#49469=EDGE_LOOP ( 'NONE', ( #13115, #44495, #31396, #20447 ) ) ;
#49470=CARTESIAN_POINT ( 'NONE',  ( 1.091055626815043311, 3.346456692913386100, 1.870389530743258755 ) ) ;
#49471=EDGE_CURVE ( 'NONE', #31195, #26854, #24913, .T. ) ;
#49476=DIRECTION ( 'NONE',  ( -1.000000000000000000, -0.000000000000000000, -0.000000000000000000 ) ) ;
#49477=EDGE_CURVE ( 'NONE', #47284, #41751, #32678, .T. ) ;
#49478=VECTOR ( 'NONE', #30416, 39.37007874015748143 ) ;
#49479=CARTESIAN_POINT ( 'NONE',  ( -0.3486774197067339376, 0.000000000000000000, -8.878505979408855953E-16 ) ) ;
#49480=DIRECTION ( 'NONE',  ( -0.000000000000000000, 1.000000000000000000, -0.000000000000000000 ) ) ;
#49483=CARTESIAN_POINT ( 'NONE',  ( 0.8182917201112819283, 0.000000000000000000, -0.6692913385826764205 ) ) ;
#49484=ORIENTED_EDGE ( 'NONE', *, *, #2496, .T. ) ;
#49485=ORIENTED_EDGE ( 'NONE', *, *, #11801, .T. ) ;
#49489=DIRECTION ( 'NONE',  ( -0.000000000000000000, 0.000000000000000000, 1.000000000000000000 ) ) ;
#49490=VECTOR ( 'NONE', #40917, 39.37007874015748143 ) ;
#49491=LINE ( 'NONE', #14167, #50721 ) ;
#49492=EDGE_CURVE ( 'NONE', #25584, #23451, #47594, .T. ) ;
#49493=ORIENTED_EDGE ( 'NONE', *, *, #7780, .F. ) ;
#49495=CARTESIAN_POINT ( 'NONE',  ( -0.07591351300297340121, 0.000000000000000000, -0.03937007874015908959 ) ) ;
#49496=DIRECTION ( 'NONE',  ( 1.734723475976806848E-16, -0.000000000000000000, 1.000000000000000000 ) ) ;
#49500=FACE_BOUND ( 'NONE', #19494, .T. ) ;
#49501=ORIENTED_EDGE ( 'NONE', *, *, #13789, .T. ) ;
#49502=CARTESIAN_POINT ( 'NONE',  ( -0.8182917201112819283, 3.267716535433071279, -0.3543307086614175816 ) ) ;
#49503=DIRECTION ( 'NONE',  ( -1.000000000000000000, 0.000000000000000000, -0.000000000000000000 ) ) ;
#49505=ORIENTED_EDGE ( 'NONE', *, *, #1555, .F. ) ;
#49507=CARTESIAN_POINT ( 'NONE',  ( 0.7423782071083087075, 3.267716535433071279, -1.259842519685035134 ) ) ;
#49508=ORIENTED_EDGE ( 'NONE', *, *, #34789, .T. ) ;
#49509=ORIENTED_EDGE ( 'NONE', *, *, #10366, .T. ) ;
#49511=CARTESIAN_POINT ( 'NONE',  ( 1.015142113812069979, 3.346456692913386100, 2.047244094488179567 ) ) ;
#49513=CARTESIAN_POINT ( 'NONE',  ( 0.000000000000000000, 3.267716535433071279, -0.3149606299212596716 ) ) ;
#49514=VECTOR ( 'NONE', #25992, 39.37007874015748143 ) ;
#49518=ORIENTED_EDGE ( 'NONE', *, *, #20544, .F. ) ;
#49519=EDGE_CURVE ( 'NONE', #1584, #33429, #35510, .T. ) ;
#49520=DIRECTION ( 'NONE',  ( 0.000000000000000000, 0.000000000000000000, -1.000000000000000000 ) ) ;
#49521=CARTESIAN_POINT ( 'NONE',  ( -1.439733046521776139, 3.267716535433071279, 0.6299212598425164567 ) ) ;
#49522=EDGE_CURVE ( 'NONE', #38248, #34706, #47338, .T. ) ;
#49523=DIRECTION ( 'NONE',  ( -0.000000000000000000, 1.000000000000000000, -0.000000000000000000 ) ) ;
#49524=CIRCLE ( 'NONE', #20705, 2.165354330708661568 ) ;
#49528=VECTOR ( 'NONE', #42205, 39.37007874015748143 ) ;
#49529=CARTESIAN_POINT ( 'NONE',  ( -2.258024766633058622, 3.346456692913386100, -0.3543307086614173040 ) ) ;
#49530=CARTESIAN_POINT ( 'NONE',  ( 0.000000000000000000, 3.267716535433071279, 0.1181102362204705658 ) ) ;
#49533=CARTESIAN_POINT ( 'NONE',  ( 0.7423782071083084855, 0.000000000000000000, -1.889763779527552812 ) ) ;
#49534=VERTEX_POINT ( 'NONE', #906 ) ;
#49535=ORIENTED_EDGE ( 'NONE', *, *, #16474, .T. ) ;
#49536=LINE ( 'NONE', #14981, #32808 ) ;
#49537=EDGE_CURVE ( 'NONE', #15306, #32210, #40418, .T. ) ;
#49538=ORIENTED_EDGE ( 'NONE', *, *, #24100, .T. ) ;
#49540=EDGE_CURVE ( 'NONE', #28392, #30339, #1672, .T. ) ;
#49543=ORIENTED_EDGE ( 'NONE', *, *, #3046, .T. ) ;
#49545=LINE ( 'NONE', #11114, #42486 ) ;
#49546=CARTESIAN_POINT ( 'NONE',  ( 0.1968503937007870241, 3.267716535433071279, -1.889763779527552146 ) ) ;
#49547=VECTOR ( 'NONE', #16669, 39.37007874015748143 ) ;
#49548=ORIENTED_EDGE ( 'NONE', *, *, #4519, .T. ) ;
#49549=ORIENTED_EDGE ( 'NONE', *, *, #28992, .F. ) ;
#49550=VECTOR ( 'NONE', #33548, 39.37007874015748143 ) ;
#49551=CARTESIAN_POINT ( 'NONE',  ( 2.378961647330872786, 3.346456692913386100, 0.3149606299212573401 ) ) ;
#49553=ORIENTED_EDGE ( 'NONE', *, *, #44940, .F. ) ;
#49554=FACE_OUTER_BOUND ( 'NONE', #41213, .T. ) ;
#49555=FACE_OUTER_BOUND ( 'NONE', #42574, .T. ) ;
#49556=VECTOR ( 'NONE', #7949, 39.37007874015748143 ) ;
#49557=DIRECTION ( 'NONE',  ( 0.000000000000000000, -1.000000000000000000, 0.000000000000000000 ) ) ;
#49561=LINE ( 'NONE', #41865, #21344 ) ;
#49562=LINE ( 'NONE', #14238, #34927 ) ;
#49563=CARTESIAN_POINT ( 'NONE',  ( -1.636583440222564301, 3.267716535433071279, -1.417869535855831975 ) ) ;
#49568=EDGE_LOOP ( 'NONE', ( #23295, #28183, #22794, #30912 ) ) ;
#49569=VERTEX_POINT ( 'NONE', #36792 ) ;
#49571=CARTESIAN_POINT ( 'NONE',  ( 0.4696143004045484348, 3.346456692913386100, 2.165354330708650910 ) ) ;
#49573=DIRECTION ( 'NONE',  ( 1.734723475976806848E-16, -0.000000000000000000, 1.000000000000000000 ) ) ;
#49574=ORIENTED_EDGE ( 'NONE', *, *, #18548, .T. ) ;
#49575=ORIENTED_EDGE ( 'NONE', *, *, #39730, .T. ) ;
#49576=EDGE_CURVE ( 'NONE', #19974, #35899, #14054, .T. ) ;
#49578=ORIENTED_EDGE ( 'NONE', *, *, #1412, .F. ) ;
#49579=CARTESIAN_POINT ( 'NONE',  ( -2.142325647309101022, 3.346456692913386100, 0.3149606299212578953 ) ) ;
#49580=DIRECTION ( 'NONE',  ( 0.000000000000000000, 0.000000000000000000, 1.000000000000000000 ) ) ;
#49582=AXIS2_PLACEMENT_3D ( 'NONE', #32902, #48329, #32641 ) ;
#49584=ADVANCED_FACE ( 'NONE', ( #9677 ), #45517, .F. ) ;
#49585=EDGE_CURVE ( 'NONE', #31796, #10769, #41424, .T. ) ;
#49586=FACE_OUTER_BOUND ( 'NONE', #16886, .T. ) ;
#49587=FACE_OUTER_BOUND ( 'NONE', #1661, .T. ) ;
#49589=DIRECTION ( 'NONE',  ( -3.469446951953613696E-16, 0.000000000000000000, -1.000000000000000000 ) ) ;
#49590=ORIENTED_EDGE ( 'NONE', *, *, #31042, .T. ) ;
#49592=CARTESIAN_POINT ( 'NONE',  ( 1.636583440222563857, 0.000000000000000000, 0.7480314960629872445 ) ) ;
#49593=VECTOR ( 'NONE', #39389, 39.37007874015748143 ) ;
#49594=CARTESIAN_POINT ( 'NONE',  ( -0.3486774197067339376, 3.346456692913386100, -8.878505979408855953E-16 ) ) ;
#49595=ORIENTED_EDGE ( 'NONE', *, *, #14770, .F. ) ;
#49596=AXIS2_PLACEMENT_3D ( 'NONE', #38, #39540, #31037 ) ;
#49597=DIRECTION ( 'NONE',  ( -1.000000000000000000, 0.000000000000000000, -0.000000000000000000 ) ) ;
#49598=LINE ( 'NONE', #1383, #1430 ) ;
#49599=EDGE_CURVE ( 'NONE', #17328, #31017, #13299, .T. ) ;
#49600=DIRECTION ( 'NONE',  ( 1.000000000000000000, 0.000000000000000000, 0.000000000000000000 ) ) ;
#49601=EDGE_LOOP ( 'NONE', ( #41387, #36393, #37244, #35921 ) ) ;
#49603=EDGE_CURVE ( 'NONE', #11339, #23728, #25929, .T. ) ;
#49604=ORIENTED_EDGE ( 'NONE', *, *, #12323, .T. ) ;
#49605=CARTESIAN_POINT ( 'NONE',  ( -2.182111253630085290, 3.346456692913386100, 0.9448818897637749625 ) ) ;
#49606=CARTESIAN_POINT ( 'NONE',  ( 1.363819533518803251, 0.000000000000000000, 1.220472440944875281 ) ) ;
#49607=VERTEX_POINT ( 'NONE', #5799 ) ;
#49608=LINE ( 'NONE', #2668, #21252 ) ;
#49609=LINE ( 'NONE', #49858, #40832 ) ;
#49610=LINE ( 'NONE', #7306, #43689 ) ;
#49611=DIRECTION ( 'NONE',  ( 1.000000000000000000, -0.000000000000000000, 0.000000000000000000 ) ) ;
#49612=ADVANCED_FACE ( 'NONE', ( #21547 ), #41677, .F. ) ;
#49616=LINE ( 'NONE', #15803, #43596 ) ;
#49617=ORIENTED_EDGE ( 'NONE', *, *, #10693, .T. ) ;
#49618=PLANE ( 'NONE',  #34137 ) ;
#49619=CARTESIAN_POINT ( 'NONE',  ( -1.439733046521776139, 3.267716535433071279, 4.995077429881866871E-16 ) ) ;
#49620=LINE ( 'NONE', #22553, #4682 ) ;
#49623=VECTOR ( 'NONE', #20913, 39.37007874015748143 ) ;
#49624=VERTEX_POINT ( 'NONE', #18183 ) ;
#49625=PLANE ( 'NONE',  #50970 ) ;
#49626=DIRECTION ( 'NONE',  ( 0.000000000000000000, 0.000000000000000000, -1.000000000000000000 ) ) ;
#49627=DIRECTION ( 'NONE',  ( 1.000000000000000000, 0.000000000000000000, -3.469446951953613696E-16 ) ) ;
#49628=VERTEX_POINT ( 'NONE', #37815 ) ;
#49629=LINE ( 'NONE', #23825, #29816 ) ;
#49630=AXIS2_PLACEMENT_3D ( 'NONE', #28066, #5094, #40474 ) ;
#49631=DIRECTION ( 'NONE',  ( 1.734723475976806848E-16, 0.000000000000000000, 1.000000000000000000 ) ) ;
#49632=VERTEX_POINT ( 'NONE', #10438 ) ;
#49633=CARTESIAN_POINT ( 'NONE',  ( -0.2727639067037607723, 3.346456692913386100, -1.732283464566922726 ) ) ;
#49634=VERTEX_POINT ( 'NONE', #13807 ) ;
#49635=CIRCLE ( 'NONE', #36490, 2.165354330708661568 ) ;
#49637=DIRECTION ( 'NONE',  ( -0.000000000000000000, 0.000000000000000000, 1.000000000000000000 ) ) ;
#49640=AXIS2_PLACEMENT_3D ( 'NONE', #33838, #49520, #38217 ) ;
#49641=DIRECTION ( 'NONE',  ( 0.000000000000000000, 0.000000000000000000, -1.000000000000000000 ) ) ;
#49642=ORIENTED_EDGE ( 'NONE', *, *, #30990, .F. ) ;
#49643=LINE ( 'NONE', #50390, #46690 ) ;
#49645=VERTEX_POINT ( 'NONE', #29550 ) ;
#49647=ORIENTED_EDGE ( 'NONE', *, *, #5096, .F. ) ;
#49649=CARTESIAN_POINT ( 'NONE',  ( 0.000000000000000000, 3.267716535433071279, 0.000000000000000000 ) ) ;
#49652=ADVANCED_FACE ( 'NONE', ( #40921 ), #2441, .F. ) ;
#49655=VERTEX_POINT ( 'NONE', #45772 ) ;
#49656=PLANE ( 'NONE',  #246 ) ;
#49657=CARTESIAN_POINT ( 'NONE',  ( -2.454875160333845674, 0.000000000000000000, -0.1574803149606298636 ) ) ;
#49658=VERTEX_POINT ( 'NONE', #17930 ) ;
#49659=DIRECTION ( 'NONE',  ( 1.734723475976806848E-16, -0.000000000000000000, 1.000000000000000000 ) ) ;
#49660=DIRECTION ( 'NONE',  ( -0.000000000000000000, 1.000000000000000000, -0.000000000000000000 ) ) ;
#49661=ORIENTED_EDGE ( 'NONE', *, *, #29233, .T. ) ;
#49662=PLANE ( 'NONE',  #31222 ) ;
#49665=VECTOR ( 'NONE', #5035, 39.37007874015748143 ) ;
#49666=ORIENTED_EDGE ( 'NONE', *, *, #34, .T. ) ;
#49667=CARTESIAN_POINT ( 'NONE',  ( 0.5455278134075212115, 3.267716535433071279, 0.3149606299212576177 ) ) ;
#49668=ORIENTED_EDGE ( 'NONE', *, *, #35594, .F. ) ;
#49671=VECTOR ( 'NONE', #44653, 39.37007874015748143 ) ;
#49672=AXIS2_PLACEMENT_3D ( 'NONE', #5120, #17261, #12615 ) ;
#49673=CARTESIAN_POINT ( 'NONE',  ( 0.8182917201112824834, 3.346456692913386100, 1.417322834645662777 ) ) ;
#49674=DIRECTION ( 'NONE',  ( 1.000000000000000000, -0.000000000000000000, 0.000000000000000000 ) ) ;
#49676=VERTEX_POINT ( 'NONE', #9933 ) ;
#49677=ORIENTED_EDGE ( 'NONE', *, *, #5295, .T. ) ;
#49681=DIRECTION ( 'NONE',  ( 1.000000000000000000, 0.000000000000000000, 0.000000000000000000 ) ) ;
#49682=ORIENTED_EDGE ( 'NONE', *, *, #30457, .T. ) ;
#49686=ORIENTED_EDGE ( 'NONE', *, *, #45721, .T. ) ;
#49687=CARTESIAN_POINT ( 'NONE',  ( 0.4696143004045479352, 3.267716535433071279, -0.7874015748031473194 ) ) ;
#49690=ORIENTED_EDGE ( 'NONE', *, *, #40385, .T. ) ;
#49691=EDGE_CURVE ( 'NONE', #17741, #48287, #27182, .T. ) ;
#49692=CARTESIAN_POINT ( 'NONE',  ( -0.2727639067037602727, 3.346456692913386100, 1.535433070866133898 ) ) ;
#49694=ORIENTED_EDGE ( 'NONE', *, *, #1373, .F. ) ;
#49697=EDGE_LOOP ( 'NONE', ( #39793, #32487, #19524, #14639 ) ) ;
#49698=CARTESIAN_POINT ( 'NONE',  ( 0.5455278134075217666, 3.267716535433071279, 1.889763779527550369 ) ) ;
#49700=VERTEX_POINT ( 'NONE', #22816 ) ;
#49703=CARTESIAN_POINT ( 'NONE',  ( -0.8942052331142552601, 3.346456692913386100, -1.907064071829739582 ) ) ;
#49704=VECTOR ( 'NONE', #19236, 39.37007874015748143 ) ;
#49705=EDGE_CURVE ( 'NONE', #39500, #5813, #22314, .T. ) ;
#49706=AXIS2_PLACEMENT_3D ( 'NONE', #16365, #20220, #11027 ) ;
#49708=EDGE_CURVE ( 'NONE', #12597, #4458, #10939, .T. ) ;
#49709=DIRECTION ( 'NONE',  ( -0.000000000000000000, 1.000000000000000000, -0.000000000000000000 ) ) ;
#49710=CARTESIAN_POINT ( 'NONE',  ( 1.091055626815042423, 3.346456692913386100, -2.086614173228339641 ) ) ;
#49711=EDGE_CURVE ( 'NONE', #48287, #32550, #14818, .T. ) ;
#49712=ORIENTED_EDGE ( 'NONE', *, *, #26693, .F. ) ;
#49713=CARTESIAN_POINT ( 'NONE',  ( 1.287906020515830141, 3.346456692913386100, -0.6299212598425181220 ) ) ;
#49714=LINE ( 'NONE', #37904, #24216 ) ;
#49715=LINE ( 'NONE', #49968, #38368 ) ;
#49716=CARTESIAN_POINT ( 'NONE',  ( -0.07591351300297333182, 0.000000000000000000, 2.362204724409437961 ) ) ;
#49717=EDGE_LOOP ( 'NONE', ( #25480, #18714, #2730, #6321 ) ) ;
#49718=CARTESIAN_POINT ( 'NONE',  ( 0.2727639067037609943, 3.346456692913386100, 2.165354330708650910 ) ) ;
#49719=DIRECTION ( 'NONE',  ( 1.734723475976806848E-16, -0.000000000000000000, 1.000000000000000000 ) ) ;
#49720=ORIENTED_EDGE ( 'NONE', *, *, #164, .T. ) ;
#49721=CARTESIAN_POINT ( 'NONE',  ( 1.363819533518803695, 3.346456692913386100, 1.535433070866133898 ) ) ;
#49722=DIRECTION ( 'NONE',  ( -1.000000000000000000, 0.000000000000000000, 0.000000000000000000 ) ) ;
#49728=LINE ( 'NONE', #37918, #23744 ) ;
#49729=FACE_OUTER_BOUND ( 'NONE', #5999, .T. ) ;
#49730=DIRECTION ( 'NONE',  ( 0.000000000000000000, 0.000000000000000000, -1.000000000000000000 ) ) ;
#49732=DIRECTION ( 'NONE',  ( -1.000000000000000000, 0.000000000000000000, -0.000000000000000000 ) ) ;
#49733=VECTOR ( 'NONE', #21939, 39.37007874015748143 ) ;
#49734=VERTEX_POINT ( 'NONE', #42677 ) ;
#49735=ORIENTED_EDGE ( 'NONE', *, *, #25935, .F. ) ;
#49737=ORIENTED_EDGE ( 'NONE', *, *, #6982, .T. ) ;
#49738=DIRECTION ( 'NONE',  ( 1.000000000000000000, -0.000000000000000000, 0.000000000000000000 ) ) ;
#49740=LINE ( 'NONE', #14681, #17808 ) ;
#49741=ORIENTED_EDGE ( 'NONE', *, *, #40791, .F. ) ;
#49742=CIRCLE ( 'NONE', #19296, 2.106299212598425008 ) ;
#49743=LINE ( 'NONE', #38434, #28889 ) ;
#49745=DIRECTION ( 'NONE',  ( 1.000000000000000000, -0.000000000000000000, 0.000000000000000000 ) ) ;
#49748=PLANE ( 'NONE',  #34596 ) ;
#49750=ORIENTED_EDGE ( 'NONE', *, *, #17457, .T. ) ;
#49751=CARTESIAN_POINT ( 'NONE',  ( -1.363819533518803473, 3.346456692913386100, 1.732283464566920950 ) ) ;
#49752=FACE_BOUND ( 'NONE', #50295, .T. ) ;
#49754=LINE ( 'NONE', #30947, #26201 ) ;
#49756=ORIENTED_EDGE ( 'NONE', *, *, #6673, .T. ) ;
#49760=ORIENTED_EDGE ( 'NONE', *, *, #4398, .T. ) ;
#49761=ORIENTED_EDGE ( 'NONE', *, *, #23479, .F. ) ;
#49762=ADVANCED_FACE ( 'NONE', ( #11194 ), #38323, .F. ) ;
#49766=ADVANCED_FACE ( 'NONE', ( #18438 ), #2940, .F. ) ;
#49767=DIRECTION ( 'NONE',  ( -3.469446951953613696E-16, 0.000000000000000000, -1.000000000000000000 ) ) ;
#49768=LINE ( 'NONE', #49272, #41209 ) ;
#49769=EDGE_CURVE ( 'NONE', #44152, #10179, #31322, .T. ) ;
#49772=LINE ( 'NONE', #9825, #15082 ) ;
#49773=DIRECTION ( 'NONE',  ( -0.000000000000000000, 1.000000000000000000, -0.000000000000000000 ) ) ;
#49774=VECTOR ( 'NONE', #22208, 39.37007874015748143 ) ;
#49775=EDGE_CURVE ( 'NONE', #35273, #5175, #3191, .T. ) ;
#49776=ADVANCED_FACE ( 'NONE', ( #30312 ), #15066, .F. ) ;
#49777=DIRECTION ( 'NONE',  ( -1.000000000000000000, -0.000000000000000000, -0.000000000000000000 ) ) ;
#49780=VECTOR ( 'NONE', #21401, 39.37007874015748143 ) ;
#49782=VECTOR ( 'NONE', #10534, 39.37007874015748143 ) ;
#49783=DIRECTION ( 'NONE',  ( -0.000000000000000000, 1.000000000000000000, -0.000000000000000000 ) ) ;
#49784=CARTESIAN_POINT ( 'NONE',  ( -1.636583440222564301, 3.346456692913386100, -0.3149606299212592275 ) ) ;
#49785=VECTOR ( 'NONE', #2025, 39.37007874015748143 ) ;
#49787=LINE ( 'NONE', #37974, #37428 ) ;
#49788=LINE ( 'NONE', #30217, #38477 ) ;
#49791=DIRECTION ( 'NONE',  ( 1.000000000000000000, 0.000000000000000000, 0.000000000000000000 ) ) ;
#49793=VERTEX_POINT ( 'NONE', #23068 ) ;
#49798=ORIENTED_EDGE ( 'NONE', *, *, #38910, .T. ) ;
#49800=VERTEX_POINT ( 'NONE', #35959 ) ;
#49801=PLANE ( 'NONE',  #37036 ) ;
#49802=AXIS2_PLACEMENT_3D ( 'NONE', #14522, #7282, #49580 ) ;
#49803=EDGE_CURVE ( 'NONE', #14060, #35430, #20019, .T. ) ;
#49804=VERTEX_POINT ( 'NONE', #19930 ) ;
#49805=ORIENTED_EDGE ( 'NONE', *, *, #46841, .F. ) ;
#49807=CARTESIAN_POINT ( 'NONE',  ( -1.636583440222564301, 3.267716535433071279, -0.5118110236220466680 ) ) ;
#49808=FACE_OUTER_BOUND ( 'NONE', #4449, .T. ) ;
#49809=DIRECTION ( 'NONE',  ( 1.734723475976806848E-16, -0.000000000000000000, 1.000000000000000000 ) ) ;
#49810=LINE ( 'NONE', #49311, #1403 ) ;
#49814=ORIENTED_EDGE ( 'NONE', *, *, #11731, .T. ) ;
#49815=CARTESIAN_POINT ( 'NONE',  ( 1.091055626815043311, 0.000000000000000000, 1.889763779527550369 ) ) ;
#49817=DIRECTION ( 'NONE',  ( -1.000000000000000000, 0.000000000000000000, 0.000000000000000000 ) ) ;
#49818=ORIENTED_EDGE ( 'NONE', *, *, #50553, .F. ) ;
#49819=LINE ( 'NONE', #45457, #32318 ) ;
#49822=ORIENTED_EDGE ( 'NONE', *, *, #48117, .T. ) ;
#49823=ORIENTED_EDGE ( 'NONE', *, *, #34174, .T. ) ;
#49824=LINE ( 'NONE', #17876, #5786 ) ;
#49825=EDGE_CURVE ( 'NONE', #46902, #26706, #39315, .T. ) ;
#49827=CARTESIAN_POINT ( 'NONE',  ( 1.909347346926324684, 0.000000000000000000, 1.102362204724403938 ) ) ;
#49828=ORIENTED_EDGE ( 'NONE', *, *, #26258, .T. ) ;
#49829=ORIENTED_EDGE ( 'NONE', *, *, #26645, .F. ) ;
#49830=DIRECTION ( 'NONE',  ( -1.000000000000000000, 0.000000000000000000, 1.734723475976806848E-16 ) ) ;
#49831=EDGE_CURVE ( 'NONE', #2103, #32862, #12455, .T. ) ;
#49832=CARTESIAN_POINT ( 'NONE',  ( 0.4696143004045479352, 3.267716535433071279, -1.417322834645664331 ) ) ;
#49834=DIRECTION ( 'NONE',  ( -0.000000000000000000, 1.000000000000000000, -0.000000000000000000 ) ) ;
#49835=CARTESIAN_POINT ( 'NONE',  ( -0.3486774197067340486, 3.267716535433071279, -2.077238655036873549 ) ) ;
#49836=DIRECTION ( 'NONE',  ( 1.734723475976806848E-16, 0.000000000000000000, 1.000000000000000000 ) ) ;
#49839=EDGE_LOOP ( 'NONE', ( #41156, #48427, #35738, #47239 ) ) ;
#49840=VECTOR ( 'NONE', #4162, 39.37007874015748143 ) ;
#49841=DIRECTION ( 'NONE',  ( -3.469446951953613696E-16, 0.000000000000000000, -1.000000000000000000 ) ) ;
#49843=VECTOR ( 'NONE', #40454, 39.37007874015748143 ) ;
#49844=AXIS2_PLACEMENT_3D ( 'NONE', #23980, #997, #36116 ) ;
#49845=DIRECTION ( 'NONE',  ( 1.734723475976806848E-16, -0.000000000000000000, 1.000000000000000000 ) ) ;
#49846=AXIS2_PLACEMENT_3D ( 'NONE', #25398, #9914, #45249 ) ;
#49847=ORIENTED_EDGE ( 'NONE', *, *, #30498, .T. ) ;
#49848=FACE_OUTER_BOUND ( 'NONE', #42849, .T. ) ;
#49850=DIRECTION ( 'NONE',  ( 0.000000000000000000, 0.000000000000000000, -1.000000000000000000 ) ) ;
#49851=ORIENTED_EDGE ( 'NONE', *, *, #27233, .T. ) ;
#49852=CARTESIAN_POINT ( 'NONE',  ( 1.091055626815042645, 0.000000000000000000, -0.5118110236220471121 ) ) ;
#49853=AXIS2_PLACEMENT_3D ( 'NONE', #27736, #19735, #19231 ) ;
#49854=ORIENTED_EDGE ( 'NONE', *, *, #48721, .F. ) ;
#49855=DIRECTION ( 'NONE',  ( 1.000000000000000000, 0.000000000000000000, 0.000000000000000000 ) ) ;
#49856=ORIENTED_EDGE ( 'NONE', *, *, #23323, .F. ) ;
#49857=CARTESIAN_POINT ( 'NONE',  ( -0.07591351300297277671, 0.000000000000000000, 1.102362204724404160 ) ) ;
#49858=CARTESIAN_POINT ( 'NONE',  ( 0.8182917201112817063, 3.346456692913386100, -1.417322834645664331 ) ) ;
#49859=CARTESIAN_POINT ( 'NONE',  ( -0.8182917201112819283, 3.346456692913386100, -0.6692913385826760875 ) ) ;
#49860=CARTESIAN_POINT ( 'NONE',  ( 0.000000000000000000, 3.267716535433071279, 0.6299212598425161236 ) ) ;
#49864=ORIENTED_EDGE ( 'NONE', *, *, #325, .T. ) ;
#49866=LINE ( 'NONE', #45763, #36218 ) ;
#49867=EDGE_CURVE ( 'NONE', #47312, #11113, #8585, .T. ) ;
#49868=ORIENTED_EDGE ( 'NONE', *, *, #18050, .F. ) ;
#49869=PLANE ( 'NONE',  #9400 ) ;
#49872=EDGE_CURVE ( 'NONE', #48423, #24715, #327, .T. ) ;
#49877=CARTESIAN_POINT ( 'NONE',  ( 1.363819533518803251, 3.346456692913386100, 0.4724409448818871482 ) ) ;
#49879=ORIENTED_EDGE ( 'NONE', *, *, #6521, .T. ) ;
#49882=AXIS2_PLACEMENT_3D ( 'NONE', #1753, #44352, #4872 ) ;
#49883=ORIENTED_EDGE ( 'NONE', *, *, #29311, .F. ) ;
#49886=ORIENTED_EDGE ( 'NONE', *, *, #16485, .F. ) ;
#49887=VERTEX_POINT ( 'NONE', #40348 ) ;
#49889=DIRECTION ( 'NONE',  ( 0.000000000000000000, -1.000000000000000000, 0.000000000000000000 ) ) ;
#49891=LINE ( 'NONE', #14582, #8247 ) ;
#49892=ADVANCED_FACE ( 'NONE', ( #8331 ), #32095, .F. ) ;
#49894=DIRECTION ( 'NONE',  ( 1.734723475976806848E-16, 0.000000000000000000, 1.000000000000000000 ) ) ;
#49896=ORIENTED_EDGE ( 'NONE', *, *, #29869, .F. ) ;
#49897=VECTOR ( 'NONE', #42161, 39.37007874015748143 ) ;
#49898=EDGE_CURVE ( 'NONE', #9086, #14000, #43937, .T. ) ;
#49899=VERTEX_POINT ( 'NONE', #16596 ) ;
#49902=DIRECTION ( 'NONE',  ( -0.000000000000000000, 1.000000000000000000, -0.000000000000000000 ) ) ;
#49905=EDGE_LOOP ( 'NONE', ( #8092, #29982, #7746, #22414 ) ) ;
#49907=EDGE_CURVE ( 'NONE', #15732, #14052, #43431, .T. ) ;
#49908=FACE_OUTER_BOUND ( 'NONE', #9801, .T. ) ;
#49909=VERTEX_POINT ( 'NONE', #44199 ) ;
#49910=CARTESIAN_POINT ( 'NONE',  ( 1.909347346926324684, 0.000000000000000000, -0.03937007874015936021 ) ) ;
#49912=EDGE_LOOP ( 'NONE', ( #36463, #29540, #44696, #36632 ) ) ;
#49913=CARTESIAN_POINT ( 'NONE',  ( 2.182111253630085290, 0.000000000000000000, 0.3149606299212573401 ) ) ;
#49914=AXIS2_PLACEMENT_3D ( 'NONE', #27712, #612, #12480 ) ;
#49915=LINE ( 'NONE', #9967, #1222 ) ;
#49916=DIRECTION ( 'NONE',  ( 1.000000000000000000, -0.000000000000000000, 0.000000000000000000 ) ) ;
#49919=VERTEX_POINT ( 'NONE', #587 ) ;
#49921=ORIENTED_EDGE ( 'NONE', *, *, #38239, .F. ) ;
#49922=FACE_BOUND ( 'NONE', #29324, .T. ) ;
#49923=AXIS2_PLACEMENT_3D ( 'NONE', #47073, #14873, #43230 ) ;
#49924=LINE ( 'NONE', #37608, #9442 ) ;
#49925=CARTESIAN_POINT ( 'NONE',  ( -0.2727639067037602172, 3.267716535433071279, 0.7874015748031456541 ) ) ;
#49926=CARTESIAN_POINT ( 'NONE',  ( 0.4696143004045484903, 3.267716535433071279, 2.362204724409437961 ) ) ;
#49927=CIRCLE ( 'NONE', #12051, 2.106299212598425008 ) ;
#49930=ORIENTED_EDGE ( 'NONE', *, *, #16695, .T. ) ;
#49931=CARTESIAN_POINT ( 'NONE',  ( 0.5455278134075211005, 3.346456692913386100, 0.7480314960629872445 ) ) ;
#49932=CARTESIAN_POINT ( 'NONE',  ( -2.102985103392958077, 3.346456692913386100, 0.1181102362204704270 ) ) ;
#49933=CARTESIAN_POINT ( 'NONE',  ( -0.5455278134075214336, 3.346456692913386100, 2.204724409448808764 ) ) ;
#49934=CARTESIAN_POINT ( 'NONE',  ( 1.636583440222563857, 0.000000000000000000, 0.6299212598425164567 ) ) ;
#49935=EDGE_CURVE ( 'NONE', #46463, #25200, #67, .T. ) ;
#49937=ORIENTED_EDGE ( 'NONE', *, *, #35945, .T. ) ;
#49939=ORIENTED_EDGE ( 'NONE', *, *, #43404, .T. ) ;
#49941=EDGE_CURVE ( 'NONE', #3939, #24556, #20711, .T. ) ;
#49944=DIRECTION ( 'NONE',  ( -0.000000000000000000, 1.000000000000000000, -0.000000000000000000 ) ) ;
#49945=VERTEX_POINT ( 'NONE', #43173 ) ;
#49946=ORIENTED_EDGE ( 'NONE', *, *, #9436, .F. ) ;
#49951=LINE ( 'NONE', #46101, #44205 ) ;
#49952=AXIS2_PLACEMENT_3D ( 'NONE', #2255, #13624, #5870 ) ;
#49955=PLANE ( 'NONE',  #23760 ) ;
#49956=AXIS2_PLACEMENT_3D ( 'NONE', #27937, #12973, #7816 ) ;
#49957=CARTESIAN_POINT ( 'NONE',  ( -1.195183497228115035E-16, 3.346456692913386100, -1.574803149606293529 ) ) ;
#49958=AXIS2_PLACEMENT_3D ( 'NONE', #12289, #43508, #32174 ) ;
#49959=EDGE_CURVE ( 'NONE', #27610, #383, #8075, .T. ) ;
#49962=AXIS2_PLACEMENT_3D ( 'NONE', #4198, #39311, #11441 ) ;
#49966=LINE ( 'NONE', #18774, #29937 ) ;
#49968=CARTESIAN_POINT ( 'NONE',  ( 9.902948977033107009E-17, 3.267716535433071279, -1.717887807185983406E-32 ) ) ;
#49971=ORIENTED_EDGE ( 'NONE', *, *, #34770, .T. ) ;
#49972=LINE ( 'NONE', #15417, #5058 ) ;
#49974=VERTEX_POINT ( 'NONE', #13740 ) ;
#49975=LINE ( 'NONE', #10779, #4028 ) ;
#49976=CARTESIAN_POINT ( 'NONE',  ( -0.8942052331142552601, 3.267716535433071279, -1.972094414217999914 ) ) ;
#49977=ORIENTED_EDGE ( 'NONE', *, *, #2960, .F. ) ;
#49980=EDGE_LOOP ( 'NONE', ( #9206, #36236, #3434, #35129 ) ) ;
#49981=DIRECTION ( 'NONE',  ( -0.000000000000000000, 1.000000000000000000, -0.000000000000000000 ) ) ;
#49982=EDGE_CURVE ( 'NONE', #19986, #49275, #40649, .T. ) ;
#49983=PLANE ( 'NONE',  #33334 ) ;
#49984=LINE ( 'NONE', #30160, #6444 ) ;
#49985=CARTESIAN_POINT ( 'NONE',  ( -1.985260859929297572, 3.267716535433071279, 0.9448818897637749625 ) ) ;
#49986=FACE_OUTER_BOUND ( 'NONE', #9982, .T. ) ;
#49988=VECTOR ( 'NONE', #36060, 39.37007874015748143 ) ;
#49989=LINE ( 'NONE', #2289, #42985 ) ;
#49990=VECTOR ( 'NONE', #17003, 39.37007874015748143 ) ;
#49991=ORIENTED_EDGE ( 'NONE', *, *, #27297, .T. ) ;
#49992=ORIENTED_EDGE ( 'NONE', *, *, #4765, .T. ) ;
#49993=PLANE ( 'NONE',  #9755 ) ;
#49994=VERTEX_POINT ( 'NONE', #17607 ) ;
#49995=CARTESIAN_POINT ( 'NONE',  ( 0.7423782071083085965, 0.000000000000000000, -0.8267716535433055070 ) ) ;
#49996=CARTESIAN_POINT ( 'NONE',  ( -0.8182917201112819283, 0.000000000000000000, -1.102362204724405492 ) ) ;
#49997=B_SPLINE_CURVE_WITH_KNOTS ( 'NONE', 3,
 ( #29127, #21396, #48710, #13392 ),
 .UNSPECIFIED., .F., .F.,
 ( 4, 4 ),
 ( 0.05160696124554316894, 0.05353638449097523899 ),
 .UNSPECIFIED. ) ;
#49998=ORIENTED_EDGE ( 'NONE', *, *, #3074, .F. ) ;
#49999=EDGE_CURVE ( 'NONE', #12958, #16898, #25828, .T. ) ;
#50003=EDGE_CURVE ( 'NONE', #36675, #12460, #32870, .T. ) ;
#50004=LINE ( 'NONE', #22434, #45291 ) ;
#50006=ORIENTED_EDGE ( 'NONE', *, *, #42804, .F. ) ;
#50007=EDGE_LOOP ( 'NONE', ( #28833, #30889, #35251, #42430 ) ) ;
#50008=CARTESIAN_POINT ( 'NONE',  ( 0.2727639067037602172, 0.000000000000000000, -2.047244094488182231 ) ) ;
#50009=FACE_BOUND ( 'NONE', #4948, .T. ) ;
#50010=ORIENTED_EDGE ( 'NONE', *, *, #25687, .F. ) ;
#50015=ORIENTED_EDGE ( 'NONE', *, *, #35304, .T. ) ;
#50016=CARTESIAN_POINT ( 'NONE',  ( -1.091055626815042645, 0.000000000000000000, -0.3149606299212593941 ) ) ;
#50017=PLANE ( 'NONE',  #19585 ) ;
#50020=DIRECTION ( 'NONE',  ( -1.000000000000000000, 0.000000000000000000, -0.000000000000000000 ) ) ;
#50022=VECTOR ( 'NONE', #39317, 39.37007874015748143 ) ;
#50024=CARTESIAN_POINT ( 'NONE',  ( 0.1968503937007874405, 3.267716535433071279, -6.829619984160658046E-17 ) ) ;
#50025=EDGE_LOOP ( 'NONE', ( #32452, #30571, #13665, #7621 ) ) ;
#50026=VERTEX_POINT ( 'NONE', #5218 ) ;
#50027=DIRECTION ( 'NONE',  ( -0.000000000000000000, 1.000000000000000000, -0.000000000000000000 ) ) ;
#50028=VECTOR ( 'NONE', #33721, 39.37007874015748143 ) ;
#50029=LINE ( 'NONE', #9826, #30411 ) ;
#50030=CARTESIAN_POINT ( 'NONE',  ( -1.985260859929297572, 3.267716535433071279, 6.887757239314511260E-16 ) ) ;
#50032=EDGE_CURVE ( 'NONE', #39171, #29717, #44957, .T. ) ;
#50033=LINE ( 'NONE', #14718, #24828 ) ;
#50034=EDGE_CURVE ( 'NONE', #22389, #29512, #9095, .T. ) ;
#50037=CARTESIAN_POINT ( 'NONE',  ( 0.5455278134075212115, 0.000000000000000000, -1.259842519685035134 ) ) ;
#50039=ORIENTED_EDGE ( 'NONE', *, *, #11293, .T. ) ;
#50043=VERTEX_POINT ( 'NONE', #37242 ) ;
#50044=ORIENTED_EDGE ( 'NONE', *, *, #47536, .T. ) ;
#50045=CARTESIAN_POINT ( 'NONE',  ( 0.8182917201112824834, 3.346456692913386100, 1.535433070866133898 ) ) ;
#50047=EDGE_LOOP ( 'NONE', ( #45382, #17422, #50433, #29439 ) ) ;
#50048=ORIENTED_EDGE ( 'NONE', *, *, #37509, .F. ) ;
#50050=ORIENTED_EDGE ( 'NONE', *, *, #3167, .T. ) ;
#50051=EDGE_CURVE ( 'NONE', #21463, #20848, #37498, .T. ) ;
#50052=LINE ( 'NONE', #2358, #6229 ) ;
#50055=CIRCLE ( 'NONE', #29470, 2.106299212598425008 ) ;
#50056=EDGE_CURVE ( 'NONE', #370, #11074, #40597, .T. ) ;
#50057=EDGE_CURVE ( 'NONE', #5904, #17741, #1859, .T. ) ;
#50058=ORIENTED_EDGE ( 'NONE', *, *, #44222, .F. ) ;
#50059=B_SPLINE_CURVE_WITH_KNOTS ( 'NONE', 3,
 ( #50995, #23947, #27554, #26798 ),
 .UNSPECIFIED., .F., .F.,
 ( 4, 4 ),
 ( 0.04063207013448753152, 0.04124740858473308069 ),
 .UNSPECIFIED. ) ;
#50060=CARTESIAN_POINT ( 'NONE',  ( 0.8182917201112819283, 0.000000000000000000, 0.1574803149606286423 ) ) ;
#50061=EDGE_CURVE ( 'NONE', #14069, #49887, #9611, .T. ) ;
#50062=EDGE_CURVE ( 'NONE', #17057, #10877, #40852, .T. ) ;
#50063=ORIENTED_EDGE ( 'NONE', *, *, #30976, .F. ) ;
#50064=VERTEX_POINT ( 'NONE', #36985 ) ;
#50066=DIRECTION ( 'NONE',  ( -1.000000000000000000, 0.000000000000000000, 1.734723475976806848E-16 ) ) ;
#50067=DIRECTION ( 'NONE',  ( 1.734723475976806848E-16, -0.000000000000000000, 1.000000000000000000 ) ) ;
#50069=VECTOR ( 'NONE', #33312, 39.37007874015748143 ) ;
#50070=VERTEX_POINT ( 'NONE', #41113 ) ;
#50071=DIRECTION ( 'NONE',  ( 1.000000000000000000, 0.000000000000000000, 0.000000000000000000 ) ) ;
#50072=PLANE ( 'NONE',  #17611 ) ;
#50074=EDGE_LOOP ( 'NONE', ( #6000, #6560, #28441, #46815 ) ) ;
#50075=AXIS2_PLACEMENT_3D ( 'NONE', #45149, #37441, #17809 ) ;
#50076=CARTESIAN_POINT ( 'NONE',  ( 2.182111253630085290, 3.346456692913386100, 0.4330708661417287386 ) ) ;
#50077=ORIENTED_EDGE ( 'NONE', *, *, #179, .F. ) ;
#50078=ORIENTED_EDGE ( 'NONE', *, *, #7025, .T. ) ;
#50081=CARTESIAN_POINT ( 'NONE',  ( -1.712496953225537411, 3.267716535433071279, 5.941417334598190051E-16 ) ) ;
#50082=LINE ( 'NONE', #42372, #7193 ) ;
#50083=CARTESIAN_POINT ( 'NONE',  ( -0.3486774197067340486, 0.000000000000000000, -0.8267716535433049518 ) ) ;
#50084=EDGE_LOOP ( 'NONE', ( #1202, #6883, #28319, #27739 ) ) ;
#50090=FACE_OUTER_BOUND ( 'NONE', #27467, .T. ) ;
#50094=ADVANCED_FACE ( 'NONE', ( #38753 ), #7261, .F. ) ;
#50096=DIRECTION ( 'NONE',  ( 1.000000000000000000, 0.000000000000000000, 0.000000000000000000 ) ) ;
#50097=ORIENTED_EDGE ( 'NONE', *, *, #16294, .T. ) ;
#50098=LINE ( 'NONE', #3154, #29970 ) ;
#50101=VECTOR ( 'NONE', #27920, 39.37007874015748143 ) ;
#50103=FACE_OUTER_BOUND ( 'NONE', #10465, .T. ) ;
#50106=AXIS2_PLACEMENT_3D ( 'NONE', #8984, #16481, #24985 ) ;
#50107=DIRECTION ( 'NONE',  ( -1.000000000000000000, 0.000000000000000000, 1.734723475976806848E-16 ) ) ;
#50109=LINE ( 'NONE', #26655, #37784 ) ;
#50110=EDGE_CURVE ( 'NONE', #32403, #49887, #10629, .T. ) ;
#50111=ORIENTED_EDGE ( 'NONE', *, *, #43442, .T. ) ;
#50112=AXIS2_PLACEMENT_3D ( 'NONE', #15420, #26772, #31415 ) ;
#50113=LINE ( 'NONE', #31046, #13001 ) ;
#50116=DIRECTION ( 'NONE',  ( -0.000000000000000000, 1.000000000000000000, -0.000000000000000000 ) ) ;
#50118=EDGE_CURVE ( 'NONE', #45493, #7930, #2878, .T. ) ;
#50119=ORIENTED_EDGE ( 'NONE', *, *, #37001, .T. ) ;
#50120=VERTEX_POINT ( 'NONE', #18371 ) ;
#50121=ORIENTED_EDGE ( 'NONE', *, *, #37012, .T. ) ;
#50122=LINE ( 'NONE', #31056, #46328 ) ;
#50123=CARTESIAN_POINT ( 'NONE',  ( 2.182111253630085290, 3.346456692913386100, 0.6299212598425161236 ) ) ;
#50127=DIRECTION ( 'NONE',  ( -1.000000000000000000, -0.000000000000000000, -0.000000000000000000 ) ) ;
#50129=VERTEX_POINT ( 'NONE', #26367 ) ;
#50131=LINE ( 'NONE', #14817, #16400 ) ;
#50132=CARTESIAN_POINT ( 'NONE',  ( 0.5455278134075216556, 3.346456692913386100, 1.692913385826762873 ) ) ;
#50133=DIRECTION ( 'NONE',  ( 1.734723475976806848E-16, -0.000000000000000000, 1.000000000000000000 ) ) ;
#50134=EDGE_LOOP ( 'NONE', ( #43580, #45519, #4433, #33023 ) ) ;
#50135=FACE_BOUND ( 'NONE', #35013, .T. ) ;
#50136=VERTEX_POINT ( 'NONE', #7004 ) ;
#50137=LINE ( 'NONE', #9683, #45486 ) ;
#50139=AXIS2_PLACEMENT_3D ( 'NONE', #42840, #7487, #19849 ) ;
#50140=VERTEX_POINT ( 'NONE', #26861 ) ;
#50141=CARTESIAN_POINT ( 'NONE',  ( 0.8182917201112821504, 3.267716535433071279, -1.419509857074483539E-16 ) ) ;
#50143=VECTOR ( 'NONE', #27431, 39.37007874015748143 ) ;
#50145=DIRECTION ( 'NONE',  ( -3.469446951953613696E-16, 0.000000000000000000, -1.000000000000000000 ) ) ;
#50146=LINE ( 'NONE', #11462, #7153 ) ;
#50147=VECTOR ( 'NONE', #7774, 39.37007874015748143 ) ;
#50149=ORIENTED_EDGE ( 'NONE', *, *, #10716, .T. ) ;
#50152=CARTESIAN_POINT ( 'NONE',  ( 0.8182917201112824834, 3.267716535433071279, 2.047244094488179567 ) ) ;
#50153=CARTESIAN_POINT ( 'NONE',  ( -1.091055626815042645, 0.000000000000000000, -0.9448818897637760728 ) ) ;
#50156=EDGE_CURVE ( 'NONE', #19452, #19800, #22751, .T. ) ;
#50158=DIRECTION ( 'NONE',  ( 1.000000000000000000, 0.000000000000000000, 0.000000000000000000 ) ) ;
#50159=ORIENTED_EDGE ( 'NONE', *, *, #44996, .F. ) ;
#50160=EDGE_CURVE ( 'NONE', #21917, #17338, #15255, .T. ) ;
#50161=CARTESIAN_POINT ( 'NONE',  ( -0.07591351300297333182, 0.000000000000000000, -1.417322834645664331 ) ) ;
#50162=CARTESIAN_POINT ( 'NONE',  ( -0.07591351300297333182, 3.267716535433071279, -0.4724409448818883694 ) ) ;
#50163=EDGE_CURVE ( 'NONE', #14001, #29095, #34625, .T. ) ;
#50168=CARTESIAN_POINT ( 'NONE',  ( 0.4696143004045482128, 3.267716535433071279, -1.629301903132388492E-16 ) ) ;
#50169=DIRECTION ( 'NONE',  ( -3.469446951953613696E-16, 0.000000000000000000, -1.000000000000000000 ) ) ;
#50170=ORIENTED_EDGE ( 'NONE', *, *, #5982, .T. ) ;
#50171=FACE_OUTER_BOUND ( 'NONE', #33618, .T. ) ;
#50173=FACE_BOUND ( 'NONE', #9151, .T. ) ;
#50176=EDGE_CURVE ( 'NONE', #28842, #16345, #45961, .T. ) ;
#50177=DIRECTION ( 'NONE',  ( 1.000000000000000000, -0.000000000000000000, 0.000000000000000000 ) ) ;
#50178=VECTOR ( 'NONE', #28495, 39.37007874015748143 ) ;
#50179=ORIENTED_EDGE ( 'NONE', *, *, #2198, .F. ) ;
#50180=ORIENTED_EDGE ( 'NONE', *, *, #5102, .F. ) ;
#50181=CARTESIAN_POINT ( 'NONE',  ( -0.3486774197067340486, 3.346456692913386100, -1.771653543307081025 ) ) ;
#50182=CARTESIAN_POINT ( 'NONE',  ( -0.2727639067037607723, 0.000000000000000000, -0.7874015748031470974 ) ) ;
#50183=EDGE_CURVE ( 'NONE', #19363, #1340, #49562, .T. ) ;
#50184=LINE ( 'NONE', #15626, #19260 ) ;
#50185=CARTESIAN_POINT ( 'NONE',  ( 2.378961647330872786, 3.267716535433070391, 0.5584465239797037350 ) ) ;
#50186=VECTOR ( 'NONE', #1124, 39.37007874015748143 ) ;
#50190=ORIENTED_EDGE ( 'NONE', *, *, #5171, .T. ) ;
#50193=ORIENTED_EDGE ( 'NONE', *, *, #25140, .T. ) ;
#50194=DIRECTION ( 'NONE',  ( 0.000000000000000000, 0.000000000000000000, -1.000000000000000000 ) ) ;
#50195=ORIENTED_EDGE ( 'NONE', *, *, #44697, .F. ) ;
#50197=ADVANCED_FACE ( 'NONE', ( #46462 ), #10375, .F. ) ;
#50199=VECTOR ( 'NONE', #17292, 39.37007874015748143 ) ;
#50202=LINE ( 'NONE', #11013, #25276 ) ;
#50203=PLANE ( 'NONE',  #40285 ) ;
#50206=VECTOR ( 'NONE', #39774, 39.37007874015748143 ) ;
#50209=DIRECTION ( 'NONE',  ( 1.000000000000000000, 0.000000000000000000, 0.000000000000000000 ) ) ;
#50211=EDGE_CURVE ( 'NONE', #5100, #46567, #38004, .T. ) ;
#50212=CARTESIAN_POINT ( 'NONE',  ( -1.091055626815042645, 3.346456692913386100, -7.512581982576723358E-16 ) ) ;
#50213=LINE ( 'NONE', #11532, #20067 ) ;
#50214=CARTESIAN_POINT ( 'NONE',  ( 1.287906020515829919, 0.000000000000000000, -1.771653543307081691 ) ) ;
#50216=ADVANCED_FACE ( 'NONE', ( #2625 ), #50072, .F. ) ;
#50218=CARTESIAN_POINT ( 'NONE',  ( 0.8182917201112818173, 3.267716535433071279, -1.419509857074483292E-16 ) ) ;
#50220=CARTESIAN_POINT ( 'NONE',  ( 1.363819533518803251, 3.267716535433071279, 1.417322834645662777 ) ) ;
#50221=EDGE_LOOP ( 'NONE', ( #24214, #31241, #46298, #29503 ) ) ;
#50222=DIRECTION ( 'NONE',  ( -1.000000000000000000, -0.000000000000000000, -0.000000000000000000 ) ) ;
#50224=CARTESIAN_POINT ( 'NONE',  ( -0.8182917201112814842, 0.000000000000000000, 1.732283464566921172 ) ) ;
#50229=DIRECTION ( 'NONE',  ( 1.000000000000000000, 0.000000000000000000, 0.000000000000000000 ) ) ;
#50232=DIRECTION ( 'NONE',  ( -3.469446951953613696E-16, 0.000000000000000000, -1.000000000000000000 ) ) ;
#50233=VECTOR ( 'NONE', #8910, 39.37007874015748143 ) ;
#50234=ORIENTED_EDGE ( 'NONE', *, *, #38710, .F. ) ;
#50235=CARTESIAN_POINT ( 'NONE',  ( -1.712496953225537188, 0.000000000000000000, 1.102362204724404160 ) ) ;
#50239=ORIENTED_EDGE ( 'NONE', *, *, #20108, .T. ) ;
#50242=CARTESIAN_POINT ( 'NONE',  ( -0.8942052331142552601, 0.000000000000000000, 2.204724409448808764 ) ) ;
#50243=VERTEX_POINT ( 'NONE', #28386 ) ;
#50246=DIRECTION ( 'NONE',  ( 1.000000000000000000, -0.000000000000000000, 0.000000000000000000 ) ) ;
#50247=AXIS2_PLACEMENT_3D ( 'NONE', #20723, #36482, #9623 ) ;
#50248=ADVANCED_FACE ( 'NONE', ( #44136 ), #47207, .F. ) ;
#50250=LINE ( 'NONE', #22683, #790 ) ;
#50254=FACE_BOUND ( 'NONE', #11680, .T. ) ;
#50257=EDGE_CURVE ( 'NONE', #42367, #27577, #3888, .T. ) ;
#50258=CARTESIAN_POINT ( 'NONE',  ( 0.5455278134075215446, 3.267716535433071279, -9.463399047163226878E-17 ) ) ;
#50259=ORIENTED_EDGE ( 'NONE', *, *, #38082, .F. ) ;
#50260=VERTEX_POINT ( 'NONE', #36151 ) ;
#50261=PLANE ( 'NONE',  #37338 ) ;
#50262=CARTESIAN_POINT ( 'NONE',  ( -2.258024766633058622, 3.346456692913386100, -0.1574803149606298636 ) ) ;
#50263=EDGE_CURVE ( 'NONE', #5669, #50863, #47719, .T. ) ;
#50264=ORIENTED_EDGE ( 'NONE', *, *, #40326, .F. ) ;
#50265=CARTESIAN_POINT ( 'NONE',  ( -2.454875160333845674, 3.208895926198073845, -0.2895261247332783228 ) ) ;
#50266=EDGE_LOOP ( 'NONE', ( #12513, #44059, #34126, #44438 ) ) ;
#50269=FACE_OUTER_BOUND ( 'NONE', #13616, .T. ) ;
#50270=DIRECTION ( 'NONE',  ( -3.469446951953613696E-16, 0.000000000000000000, -1.000000000000000000 ) ) ;
#50271=ORIENTED_EDGE ( 'NONE', *, *, #45690, .F. ) ;
#50273=DIRECTION ( 'NONE',  ( -3.469446951953613696E-16, 0.000000000000000000, -1.000000000000000000 ) ) ;
#50274=CARTESIAN_POINT ( 'NONE',  ( -0.8942052331142549271, 3.267716535433071279, 3.102397620449222481E-16 ) ) ;
#50275=PLANE ( 'NONE',  #3572 ) ;
#50278=ADVANCED_FACE ( 'NONE', ( #781 ), #27619, .F. ) ;
#50279=VECTOR ( 'NONE', #30589, 39.37007874015748143 ) ;
#50281=DIRECTION ( 'NONE',  ( -1.000000000000000000, -0.000000000000000000, -0.000000000000000000 ) ) ;
#50284=ORIENTED_EDGE ( 'NONE', *, *, #49146, .T. ) ;
#50289=ORIENTED_EDGE ( 'NONE', *, *, #1144, .F. ) ;
#50290=DIRECTION ( 'NONE',  ( 1.000000000000000000, 0.000000000000000000, -3.469446951953613696E-16 ) ) ;
#50294=LINE ( 'NONE', #18101, #33709 ) ;
#50295=EDGE_LOOP ( 'NONE', ( #4168, #38073, #7205 ) ) ;
#50296=CARTESIAN_POINT ( 'NONE',  ( -0.3486774197067339376, 3.267716535433071279, 2.077238655036873549 ) ) ;
#50299=EDGE_LOOP ( 'NONE', ( #7373, #4593, #10816, #39313 ) ) ;
#50302=VERTEX_POINT ( 'NONE', #35637 ) ;
#50303=VERTEX_POINT ( 'NONE', #4393 ) ;
#50305=CARTESIAN_POINT ( 'NONE',  ( 1.006250229852934774, 3.346456692913386100, 1.850393700787392293 ) ) ;
#50307=EDGE_CURVE ( 'NONE', #37535, #11433, #47466, .T. ) ;
#50308=VECTOR ( 'NONE', #45420, 39.37007874015748143 ) ;
#50309=ORIENTED_EDGE ( 'NONE', *, *, #36287, .F. ) ;
#50310=VECTOR ( 'NONE', #27558, 39.37007874015748143 ) ;
#50313=DIRECTION ( 'NONE',  ( -3.469446951953613696E-16, 0.000000000000000000, -1.000000000000000000 ) ) ;
#50314=EDGE_CURVE ( 'NONE', #39361, #3322, #27876, .T. ) ;
#50315=ORIENTED_EDGE ( 'NONE', *, *, #16107, .T. ) ;
#50316=CARTESIAN_POINT ( 'NONE',  ( 0.5455278134075211005, 3.346456692913386100, 0.4330708661417287386 ) ) ;
#50317=EDGE_CURVE ( 'NONE', #3630, #2069, #34095, .T. ) ;
#50319=VERTEX_POINT ( 'NONE', #4142 ) ;
#50320=VECTOR ( 'NONE', #8138, 39.37007874015748143 ) ;
#50321=CARTESIAN_POINT ( 'NONE',  ( 1.091055626815042645, 3.346456692913386100, 0.3149606299212578953 ) ) ;
#50322=VECTOR ( 'NONE', #26019, 39.37007874015748143 ) ;
#50323=DIRECTION ( 'NONE',  ( -0.000000000000000000, 1.000000000000000000, -0.000000000000000000 ) ) ;
#50324=FACE_OUTER_BOUND ( 'NONE', #42599, .T. ) ;
#50325=PLANE ( 'NONE',  #16472 ) ;
#50326=VERTEX_POINT ( 'NONE', #24011 ) ;
#50329=DIRECTION ( 'NONE',  ( -1.000000000000000000, -0.000000000000000000, -0.000000000000000000 ) ) ;
#50330=VERTEX_POINT ( 'NONE', #20128 ) ;
#50331=CARTESIAN_POINT ( 'NONE',  ( -2.454875160333845674, 3.242921367653845977, -0.03937007874015881204 ) ) ;
#50333=EDGE_CURVE ( 'NONE', #3555, #36460, #35894, .T. ) ;
#50334=EDGE_CURVE ( 'NONE', #3322, #45259, #25039, .T. ) ;
#50335=DIRECTION ( 'NONE',  ( -0.000000000000000000, 1.000000000000000000, -0.000000000000000000 ) ) ;
#50337=CARTESIAN_POINT ( 'NONE',  ( -0.07591351300297277671, 3.267716535433071279, 2.047244094488179567 ) ) ;
#50339=ADVANCED_FACE ( 'NONE', ( #29424 ), #1799, .F. ) ;
#50340=CARTESIAN_POINT ( 'NONE',  ( -0.6214413264104944323, 3.267716535433071279, 2.156057715732900533E-16 ) ) ;
#50341=VECTOR ( 'NONE', #22573, 39.37007874015748143 ) ;
#50342=CARTESIAN_POINT ( 'NONE',  ( -1.363819533518803029, 0.000000000000000000, 0.7874015748031456541 ) ) ;
#50343=VECTOR ( 'NONE', #14595, 39.37007874015748143 ) ;
#50344=ORIENTED_EDGE ( 'NONE', *, *, #23738, .F. ) ;
#50349=VERTEX_POINT ( 'NONE', #45396 ) ;
#50350=CARTESIAN_POINT ( 'NONE',  ( 0.000000000000000000, 3.267716535433071279, -0.8267716535433055070 ) ) ;
#50351=VECTOR ( 'NONE', #25404, 39.37007874015748143 ) ;
#50352=EDGE_LOOP ( 'NONE', ( #15647, #14096, #23001, #42004 ) ) ;
#50354=VECTOR ( 'NONE', #36662, 39.37007874015748143 ) ;
#50356=DIRECTION ( 'NONE',  ( -3.469446951953613696E-16, 0.000000000000000000, -1.000000000000000000 ) ) ;
#50357=EDGE_LOOP ( 'NONE', ( #28069, #18757, #3049, #48941 ) ) ;
#50358=VECTOR ( 'NONE', #28041, 39.37007874015748143 ) ;
#50359=DIRECTION ( 'NONE',  ( 1.000000000000000000, 0.000000000000000000, 0.000000000000000000 ) ) ;
#50360=CARTESIAN_POINT ( 'NONE',  ( -0.2727639067037602727, 3.267716535433071279, 0.9055118110236167750 ) ) ;
#50363=ORIENTED_EDGE ( 'NONE', *, *, #27459, .T. ) ;
#50364=VERTEX_POINT ( 'NONE', #44640 ) ;
#50366=LINE ( 'NONE', #3182, #14729 ) ;
#50367=VERTEX_POINT ( 'NONE', #45143 ) ;
#50368=CARTESIAN_POINT ( 'NONE',  ( -3.927031490892378253E-16, 0.000000000000000000, -1.889763779527552146 ) ) ;
#50370=CARTESIAN_POINT ( 'NONE',  ( 0.5455278134075217666, 3.267716535433071279, 1.574803149606291974 ) ) ;
#50371=ORIENTED_EDGE ( 'NONE', *, *, #6634, .F. ) ;
#50372=VERTEX_POINT ( 'NONE', #9294 ) ;
#50373=EDGE_CURVE ( 'NONE', #12621, #17781, #28902, .T. ) ;
#50374=LINE ( 'NONE', #22815, #50143 ) ;
#50375=CARTESIAN_POINT ( 'NONE',  ( 0.000000000000000000, 3.267716535433071279, 2.047244094488179567 ) ) ;
#50376=DIRECTION ( 'NONE',  ( -1.000000000000000000, 0.000000000000000000, -0.000000000000000000 ) ) ;
#50380=EDGE_CURVE ( 'NONE', #8962, #34698, #10060, .T. ) ;
#50381=FACE_OUTER_BOUND ( 'NONE', #21410, .T. ) ;
#50382=ORIENTED_EDGE ( 'NONE', *, *, #1372, .T. ) ;
#50386=CARTESIAN_POINT ( 'NONE',  ( 4.268512490100411402E-16, 3.346456692913386100, 1.259842519685033357 ) ) ;
#50389=LINE ( 'NONE', #16090, #39606 ) ;
#50390=CARTESIAN_POINT ( 'NONE',  ( 1.015142113812069313, 0.000000000000000000, -0.6692913385826764205 ) ) ;
#50391=CARTESIAN_POINT ( 'NONE',  ( 1.015142113812069313, 3.267716535433071279, 0.2755905511810994302 ) ) ;
#50393=VECTOR ( 'NONE', #25789, 39.37007874015748143 ) ;
#50394=AXIS2_PLACEMENT_3D ( 'NONE', #1733, #33246, #14634 ) ;
#50395=EDGE_CURVE ( 'NONE', #42867, #32098, #17301, .T. ) ;
#50397=PLANE ( 'NONE',  #36823 ) ;
#50399=VECTOR ( 'NONE', #23340, 39.37007874015748143 ) ;
#50405=VERTEX_POINT ( 'NONE', #41303 ) ;
#50406=DIRECTION ( 'NONE',  ( 1.000000000000000000, 0.000000000000000000, -3.469446951953613696E-16 ) ) ;
#50407=EDGE_CURVE ( 'NONE', #6760, #26747, #1288, .T. ) ;
#50409=ORIENTED_EDGE ( 'NONE', *, *, #24415, .F. ) ;
#50410=PLANE ( 'NONE',  #28141 ) ;
#50411=LINE ( 'NONE', #18972, #32773 ) ;
#50412=LINE ( 'NONE', #3483, #41145 ) ;
#50413=DIRECTION ( 'NONE',  ( 1.734723475976806848E-16, 0.000000000000000000, 1.000000000000000000 ) ) ;
#50415=LINE ( 'NONE', #2983, #6263 ) ;
#50416=ORIENTED_EDGE ( 'NONE', *, *, #33273, .T. ) ;
#50417=DIRECTION ( 'NONE',  ( 1.000000000000000000, -0.000000000000000000, 0.000000000000000000 ) ) ;
#50418=ORIENTED_EDGE ( 'NONE', *, *, #29697, .F. ) ;
#50419=FACE_BOUND ( 'NONE', #10511, .T. ) ;
#50420=CARTESIAN_POINT ( 'NONE',  ( -0.8182917201112814842, 0.000000000000000000, 0.9055118110236167750 ) ) ;
#50421=CARTESIAN_POINT ( 'NONE',  ( 0.000000000000000000, 3.267716535433071279, 0.9448818897637749625 ) ) ;
#50422=VECTOR ( 'NONE', #39182, 39.37007874015748143 ) ;
#50423=ORIENTED_EDGE ( 'NONE', *, *, #20895, .T. ) ;
#50428=DIRECTION ( 'NONE',  ( -0.000000000000000000, 1.000000000000000000, -0.000000000000000000 ) ) ;
#50429=LINE ( 'NONE', #23365, #42517 ) ;
#50430=DIRECTION ( 'NONE',  ( -0.000000000000000000, 0.000000000000000000, 1.000000000000000000 ) ) ;
#50432=AXIS2_PLACEMENT_3D ( 'NONE', #28420, #48271, #1062 ) ;
#50433=ORIENTED_EDGE ( 'NONE', *, *, #43850, .F. ) ;
#50435=CARTESIAN_POINT ( 'NONE',  ( -0.07591351300297277671, 3.346456692913386100, 2.047244094488179567 ) ) ;
#50437=EDGE_CURVE ( 'NONE', #13112, #9880, #17049, .T. ) ;
#50439=EDGE_CURVE ( 'NONE', #13554, #38641, #36923, .T. ) ;
#50441=EDGE_LOOP ( 'NONE', ( #6509, #16086, #2288, #3768 ) ) ;
#50442=ORIENTED_EDGE ( 'NONE', *, *, #24521, .F. ) ;
#50443=EDGE_CURVE ( 'NONE', #16466, #25584, #1548, .T. ) ;
#50448=LINE ( 'NONE', #46600, #18027 ) ;
#50449=DIRECTION ( 'NONE',  ( -3.469446951953613696E-16, 0.000000000000000000, -1.000000000000000000 ) ) ;
#50451=EDGE_CURVE ( 'NONE', #31614, #11498, #20911, .T. ) ;
#50453=AXIS2_PLACEMENT_3D ( 'NONE', #16205, #31962, #40217 ) ;
#50454=FACE_OUTER_BOUND ( 'NONE', #43224, .T. ) ;
#50456=EDGE_LOOP ( 'NONE', ( #31712, #19507, #4297, #8143, #33715 ) ) ;
#50459=ADVANCED_FACE ( 'NONE', ( #36407 ), #5160, .F. ) ;
#50460=VECTOR ( 'NONE', #44963, 39.37007874015748143 ) ;
#50462=LINE ( 'NONE', #19523, #29814 ) ;
#50463=AXIS2_PLACEMENT_3D ( 'NONE', #7525, #39018, #11400 ) ;
#50464=AXIS2_PLACEMENT_3D ( 'NONE', #16121, #39870, #36263 ) ;
#50465=ORIENTED_EDGE ( 'NONE', *, *, #8752, .F. ) ;
#50466=CARTESIAN_POINT ( 'NONE',  ( -0.8942052331142552601, 0.000000000000000000, -1.456692913385822186 ) ) ;
#50467=PLANE ( 'NONE',  #30250 ) ;
#50469=CARTESIAN_POINT ( 'NONE',  ( -1.909347346926325129, 3.267716535433071279, -0.8893194486674343979 ) ) ;
#50471=VECTOR ( 'NONE', #11283, 39.37007874015748143 ) ;
#50474=DIRECTION ( 'NONE',  ( 1.000000000000000000, 0.000000000000000000, -3.469446951953613696E-16 ) ) ;
#50476=DIRECTION ( 'NONE',  ( -0.000000000000000000, 1.000000000000000000, -0.000000000000000000 ) ) ;
#50477=DIRECTION ( 'NONE',  ( 1.734723475976806848E-16, 0.000000000000000000, 1.000000000000000000 ) ) ;
#50479=EDGE_LOOP ( 'NONE', ( #37030, #7434, #25279, #4816 ) ) ;
#50482=CARTESIAN_POINT ( 'NONE',  ( -1.909347346926324906, 0.000000000000000000, -1.102362204724405492 ) ) ;
#50483=ORIENTED_EDGE ( 'NONE', *, *, #5162, .F. ) ;
#50484=CARTESIAN_POINT ( 'NONE',  ( 2.579472588755252050E-16, 0.000000000000000000, 2.106299212598425008 ) ) ;
#50485=PLANE ( 'NONE',  #20304 ) ;
#50486=VERTEX_POINT ( 'NONE', #29683 ) ;
#50487=CARTESIAN_POINT ( 'NONE',  ( -0.2727639067037607723, 3.346456692913386100, -1.417322834645664331 ) ) ;
#50489=CARTESIAN_POINT ( 'NONE',  ( 0.000000000000000000, 3.267716535433071279, -8.878505979408855953E-16 ) ) ;
#50491=VECTOR ( 'NONE', #35764, 39.37007874015748143 ) ;
#50492=EDGE_CURVE ( 'NONE', #42344, #11143, #1033, .T. ) ;
#50493=ORIENTED_EDGE ( 'NONE', *, *, #20631, .F. ) ;
#50494=ADVANCED_FACE ( 'NONE', ( #48235 ), #12918, .F. ) ;
#50495=ORIENTED_EDGE ( 'NONE', *, *, #48463, .T. ) ;
#50496=DIRECTION ( 'NONE',  ( 1.734723475976806848E-16, -0.000000000000000000, 1.000000000000000000 ) ) ;
#50497=FACE_BOUND ( 'NONE', #12342, .T. ) ;
#50498=ORIENTED_EDGE ( 'NONE', *, *, #48452, .T. ) ;
#50500=VECTOR ( 'NONE', #4918, 39.37007874015748143 ) ;
#50501=AXIS2_PLACEMENT_3D ( 'NONE', #41508, #45355, #5632 ) ;
#50502=DIRECTION ( 'NONE',  ( -1.000000000000000000, 0.000000000000000000, 0.000000000000000000 ) ) ;
#50503=EDGE_CURVE ( 'NONE', #50302, #24946, #26311, .T. ) ;
#50504=ORIENTED_EDGE ( 'NONE', *, *, #47909, .T. ) ;
#50505=VERTEX_POINT ( 'NONE', #2820 ) ;
#50506=CARTESIAN_POINT ( 'NONE',  ( 1.363819533518803251, 3.346456692913386100, 0.9055118110236164419 ) ) ;
#50509=ORIENTED_EDGE ( 'NONE', *, *, #32634, .T. ) ;
#50512=CARTESIAN_POINT ( 'NONE',  ( -1.636583440222563635, 3.346456692913386100, 0.6299212598425164567 ) ) ;
#50514=EDGE_CURVE ( 'NONE', #5952, #14945, #13294, .T. ) ;
#50515=DIRECTION ( 'NONE',  ( -3.469446951953613696E-16, 0.000000000000000000, -1.000000000000000000 ) ) ;
#50516=ORIENTED_EDGE ( 'NONE', *, *, #5343, .T. ) ;
#50517=EDGE_LOOP ( 'NONE', ( #41245, #23954, #33066, #29902 ) ) ;
#50518=FACE_OUTER_BOUND ( 'NONE', #17334, .T. ) ;
#50519=PLANE ( 'NONE',  #42750 ) ;
#50520=CARTESIAN_POINT ( 'NONE',  ( 1.363819533518803251, 0.000000000000000000, 0.2755905511810996522 ) ) ;
#50521=ADVANCED_FACE ( 'NONE', ( #35268 ), #45904, .F. ) ;
#50522=CARTESIAN_POINT ( 'NONE',  ( -2.182111253630085734, 3.346456692913386100, -0.9448818897637762948 ) ) ;
#50527=ORIENTED_EDGE ( 'NONE', *, *, #11516, .F. ) ;
#50528=DIRECTION ( 'NONE',  ( 1.000000000000000000, 0.000000000000000000, 0.000000000000000000 ) ) ;
#50531=ORIENTED_EDGE ( 'NONE', *, *, #43632, .T. ) ;
#50533=VECTOR ( 'NONE', #12779, 39.37007874015748143 ) ;
#50534=ORIENTED_EDGE ( 'NONE', *, *, #28531, .F. ) ;
#50535=DIRECTION ( 'NONE',  ( -1.000000000000000000, 0.000000000000000000, -0.000000000000000000 ) ) ;
#50536=AXIS2_PLACEMENT_3D ( 'NONE', #26013, #21387, #37650 ) ;
#50539=VECTOR ( 'NONE', #47749, 39.37007874015748143 ) ;
#50541=ORIENTED_EDGE ( 'NONE', *, *, #2326, .F. ) ;
#50542=DIRECTION ( 'NONE',  ( 1.734723475976806848E-16, -0.000000000000000000, 1.000000000000000000 ) ) ;
#50543=ORIENTED_EDGE ( 'NONE', *, *, #19177, .T. ) ;
#50544=CARTESIAN_POINT ( 'NONE',  ( -0.6214413264104939882, 3.346456692913386100, 1.102362204724404160 ) ) ;
#50545=DIRECTION ( 'NONE',  ( 1.734723475976806848E-16, -0.000000000000000000, 1.000000000000000000 ) ) ;
#50546=VERTEX_POINT ( 'NONE', #30187 ) ;
#50547=CARTESIAN_POINT ( 'NONE',  ( 1.560669927219590303, 3.267716535433071279, -1.299212598425193210 ) ) ;
#50548=ORIENTED_EDGE ( 'NONE', *, *, #46831, .F. ) ;
#50549=VERTEX_POINT ( 'NONE', #31391 ) ;
#50551=FACE_OUTER_BOUND ( 'NONE', #11291, .T. ) ;
#50552=CARTESIAN_POINT ( 'NONE',  ( -1.909347346926324462, 3.267716535433071279, 3.312189666507127188E-16 ) ) ;
#50553=EDGE_CURVE ( 'NONE', #25411, #1622, #42059, .T. ) ;
#50555=CARTESIAN_POINT ( 'NONE',  ( 1.966928503432568975, 3.346456692913386100, 0.9055118110236164419 ) ) ;
#50557=ADVANCED_FACE ( 'NONE', ( #37947 ), #38202, .F. ) ;
#50558=ADVANCED_FACE ( 'NONE', ( #14693 ), #3771, .F. ) ;
#50559=ORIENTED_EDGE ( 'NONE', *, *, #45120, .T. ) ;
#50561=AXIS2_PLACEMENT_3D ( 'NONE', #50948, #19756, #49503 ) ;
#50562=VECTOR ( 'NONE', #23771, 39.37007874015748143 ) ;
#50563=EDGE_LOOP ( 'NONE', ( #6733, #49720, #20534, #23759 ) ) ;
#50564=VECTOR ( 'NONE', #32366, 39.37007874015748143 ) ;
#50566=VECTOR ( 'NONE', #12245, 39.37007874015748143 ) ;
#50568=DIRECTION ( 'NONE',  ( 0.000000000000000000, 0.000000000000000000, 1.000000000000000000 ) ) ;
#50569=VECTOR ( 'NONE', #49283, 39.37007874015748143 ) ;
#50570=CARTESIAN_POINT ( 'NONE',  ( -1.091055626815042645, 0.000000000000000000, -1.574803149606293529 ) ) ;
#50571=CARTESIAN_POINT ( 'NONE',  ( -0.8182917201112819283, 0.000000000000000000, -1.299212598425193210 ) ) ;
#50572=LINE ( 'NONE', #15268, #33810 ) ;
#50573=ORIENTED_EDGE ( 'NONE', *, *, #50317, .T. ) ;
#50574=EDGE_LOOP ( 'NONE', ( #23033, #25383, #47325, #19773, #18377, #50929, #44329, #27190, #50493, #40924, #23538, #11702, #12354, #50193, #1564, #18722, #25703, #25107, #4945, #42679, #14456, #34308, #14624, #48070, #25258, #1217, #14314, #25273, #38848, #32103, #16412, #47604, #44498, #34614, #18857, #41227, #45048, #26245, #32157, #16080, #43291, #35508, #987, #14799, #16819, #20801, #30190, #2479, #15396, #51013, #24064, #43295, #39219, #32198, #21338, #5104, #30605, #26043, #16441, #17382, #49822, #38451, #25829, #22134, #38816, #48773, #35978, #26065, #7415, #3183, #32812, #47781, #9924, #17345, #85, #29084, #32148, #40589, #28650, #10436, #4423, #4377, #45949, #21096, #19623, #40670, #11879, #44454, #47059, #29285, #45886, #42092, #38932, #9815, #24197, #29027, #49044, #2706, #12965, #48646, #11201, #5443, #848, #11560, #10815, #50465, #30365, #47910, #4119, #19610, #33054, #13061, #48064, #14995, #5728, #7860, #38131, #32711, #12732, #29751, #40428, #40759, #24218, #25089, #45137, #144, #48500, #12473, #31996, #44076, #44278, #7021, #35440, #41693, #579, #43636, #48783, #18874, #33459, #50593, #44245, #10423, #26135, #10547, #4692, #42856, #7893, #14031, #39012, #34962, #27672, #26802, #10249, #30184, #32778, #15695, #42273 ) ) ;
#50577=LINE ( 'NONE', #15272, #11924 ) ;
#50578=VERTEX_POINT ( 'NONE', #4029 ) ;
#50579=DIRECTION ( 'NONE',  ( -0.000000000000000000, 1.000000000000000000, -0.000000000000000000 ) ) ;
#50581=EDGE_CURVE ( 'NONE', #18289, #48175, #23376, .T. ) ;
#50582=CARTESIAN_POINT ( 'NONE',  ( -0.2727639067037607723, 3.267716535433071279, -1.732283464566922726 ) ) ;
#50584=DIRECTION ( 'NONE',  ( -0.000000000000000000, 1.000000000000000000, -0.000000000000000000 ) ) ;
#50586=CARTESIAN_POINT ( 'NONE',  ( -1.363819533518803473, 3.346456692913386100, 1.732283464566920950 ) ) ;
#50588=EDGE_CURVE ( 'NONE', #3179, #5174, #22193, .T. ) ;
#50590=DIRECTION ( 'NONE',  ( 1.000000000000000000, 0.000000000000000000, 0.000000000000000000 ) ) ;
#50593=ORIENTED_EDGE ( 'NONE', *, *, #48266, .T. ) ;
#50594=EDGE_CURVE ( 'NONE', #39889, #44367, #18571, .T. ) ;
#50595=VECTOR ( 'NONE', #2205, 39.37007874015748143 ) ;
#50597=VERTEX_POINT ( 'NONE', #19505 ) ;
#50599=DIRECTION ( 'NONE',  ( 0.000000000000000000, -1.000000000000000000, 0.000000000000000000 ) ) ;
#50603=ORIENTED_EDGE ( 'NONE', *, *, #532, .F. ) ;
#50604=EDGE_CURVE ( 'NONE', #15792, #12349, #27502, .T. ) ;
#50605=CARTESIAN_POINT ( 'NONE',  ( 0.7423782071083087075, 0.000000000000000000, -0.6299212598425181220 ) ) ;
#50606=LINE ( 'NONE', #34676, #31332 ) ;
#50607=LINE ( 'NONE', #31050, #49897 ) ;
#50609=ORIENTED_EDGE ( 'NONE', *, *, #36503, .F. ) ;
#50610=ORIENTED_EDGE ( 'NONE', *, *, #50110, .F. ) ;
#50612=VECTOR ( 'NONE', #7011, 39.37007874015748143 ) ;
#50614=ORIENTED_EDGE ( 'NONE', *, *, #33906, .T. ) ;
#50615=ORIENTED_EDGE ( 'NONE', *, *, #38294, .F. ) ;
#50616=LINE ( 'NONE', #46521, #13268 ) ;
#50617=DIRECTION ( 'NONE',  ( 1.734723475976806848E-16, 0.000000000000000000, 1.000000000000000000 ) ) ;
#50621=ORIENTED_EDGE ( 'NONE', *, *, #14472, .F. ) ;
#50622=DIRECTION ( 'NONE',  ( -3.469446951953613696E-16, 0.000000000000000000, -1.000000000000000000 ) ) ;
#50625=ADVANCED_FACE ( 'NONE', ( #32169 ), #403, .F. ) ;
#50628=CARTESIAN_POINT ( 'NONE',  ( -1.091055626815042645, 3.267716535433071279, 2.186531193194249045 ) ) ;
#50629=ORIENTED_EDGE ( 'NONE', *, *, #33020, .T. ) ;
#50632=ORIENTED_EDGE ( 'NONE', *, *, #20606, .F. ) ;
#50633=VERTEX_POINT ( 'NONE', #48370 ) ;
#50634=LINE ( 'NONE', #19695, #39420 ) ;
#50638=CARTESIAN_POINT ( 'NONE',  ( -0.5455278134075214336, 3.267716535433071279, 9.463399047163225645E-17 ) ) ;
#50639=ORIENTED_EDGE ( 'NONE', *, *, #2015, .T. ) ;
#50640=VECTOR ( 'NONE', #47225, 39.37007874015748143 ) ;
#50642=ORIENTED_EDGE ( 'NONE', *, *, #27134, .F. ) ;
#50643=CARTESIAN_POINT ( 'NONE',  ( 0.1968503937007877735, 3.346456692913386100, 1.377952755905504256 ) ) ;
#50645=VECTOR ( 'NONE', #23110, 39.37007874015748143 ) ;
#50647=LINE ( 'NONE', #15345, #43240 ) ;
#50648=LINE ( 'NONE', #46802, #48379 ) ;
#50649=CARTESIAN_POINT ( 'NONE',  ( -1.636583440222564301, 0.000000000000000000, -1.771653543307080581 ) ) ;
#50650=VECTOR ( 'NONE', #43541, 39.37007874015748143 ) ;
#50652=DIRECTION ( 'NONE',  ( 0.000000000000000000, 1.000000000000000000, 0.000000000000000000 ) ) ;
#50653=DIRECTION ( 'NONE',  ( -3.469446951953613696E-16, 0.000000000000000000, -1.000000000000000000 ) ) ;
#50654=ADVANCED_FACE ( 'NONE', ( #24157 ), #31914, .F. ) ;
#50655=ORIENTED_EDGE ( 'NONE', *, *, #18107, .F. ) ;
#50658=LINE ( 'NONE', #7859, #44281 ) ;
#50661=LINE ( 'NONE', #27219, #41582 ) ;
#50663=DIRECTION ( 'NONE',  ( 1.000000000000000000, -0.000000000000000000, 0.000000000000000000 ) ) ;
#50667=CARTESIAN_POINT ( 'NONE',  ( 0.4696143004045478797, 3.267716535433071279, -0.3543307086614173040 ) ) ;
#50669=LINE ( 'NONE', #23874, #31773 ) ;
#50671=ORIENTED_EDGE ( 'NONE', *, *, #79, .T. ) ;
#50672=DIRECTION ( 'NONE',  ( 1.000000000000000000, 0.000000000000000000, 0.000000000000000000 ) ) ;
#50673=VECTOR ( 'NONE', #39153, 39.37007874015748143 ) ;
#50674=LINE ( 'NONE', #15378, #50960 ) ;
#50676=CARTESIAN_POINT ( 'NONE',  ( -1.166969139818015977, 3.267716535433071279, -1.417322834645664109 ) ) ;
#50682=VERTEX_POINT ( 'NONE', #8158 ) ;
#50683=ORIENTED_EDGE ( 'NONE', *, *, #46676, .F. ) ;
#50686=EDGE_CURVE ( 'NONE', #50319, #2087, #28529, .T. ) ;
#50687=CARTESIAN_POINT ( 'NONE',  ( -0.6214413264104945434, 0.000000000000000000, -0.4724409448818886470 ) ) ;
#50688=AXIS2_PLACEMENT_3D ( 'NONE', #37610, #38363, #9975 ) ;
#50689=ORIENTED_EDGE ( 'NONE', *, *, #49361, .T. ) ;
#50693=VERTEX_POINT ( 'NONE', #24674 ) ;
#50694=ORIENTED_EDGE ( 'NONE', *, *, #7625, .F. ) ;
#50695=ORIENTED_EDGE ( 'NONE', *, *, #30682, .F. ) ;
#50696=CARTESIAN_POINT ( 'NONE',  ( 1.287906020515830141, 0.000000000000000000, -0.8267716535433055070 ) ) ;
#50697=ORIENTED_EDGE ( 'NONE', *, *, #45690, .T. ) ;
#50698=LINE ( 'NONE', #18767, #24617 ) ;
#50699=PLANE ( 'NONE',  #42554 ) ;
#50701=CARTESIAN_POINT ( 'NONE',  ( 0.7423782071083087075, 0.000000000000000000, -6.146657985744592735E-16 ) ) ;
#50702=DIRECTION ( 'NONE',  ( -1.000000000000000000, 0.000000000000000000, -0.000000000000000000 ) ) ;
#50703=CARTESIAN_POINT ( 'NONE',  ( -0.07591351300297333182, 0.000000000000000000, -1.732283464566922726 ) ) ;
#50705=VERTEX_POINT ( 'NONE', #13308 ) ;
#50706=LINE ( 'NONE', #7409, #50471 ) ;
#50707=LINE ( 'NONE', #23147, #48896 ) ;
#50708=AXIS2_PLACEMENT_3D ( 'NONE', #33067, #10580, #42069 ) ;
#50709=CARTESIAN_POINT ( 'NONE',  ( -0.6214413264104945434, 3.346456692913386100, -0.6692913385826760875 ) ) ;
#50710=VECTOR ( 'NONE', #1154, 39.37007874015748143 ) ;
#50712=ORIENTED_EDGE ( 'NONE', *, *, #36314, .F. ) ;
#50713=DIRECTION ( 'NONE',  ( -1.000000000000000000, -0.000000000000000000, -0.000000000000000000 ) ) ;
#50715=LINE ( 'NONE', #50974, #19506 ) ;
#50716=VERTEX_POINT ( 'NONE', #8661 ) ;
#50717=CARTESIAN_POINT ( 'NONE',  ( -1.636583440222564301, 3.267716535433071279, 2.839019714148967077E-16 ) ) ;
#50718=VECTOR ( 'NONE', #48216, 39.37007874015748143 ) ;
#50720=EDGE_CURVE ( 'NONE', #739, #180, #4792, .T. ) ;
#50721=VECTOR ( 'NONE', #22177, 39.37007874015748143 ) ;
#50725=EDGE_LOOP ( 'NONE', ( #23748, #30689, #28490, #37191 ) ) ;
#50726=LINE ( 'NONE', #696, #38001 ) ;
#50727=CARTESIAN_POINT ( 'NONE',  ( 1.833433833923351353, 0.000000000000000000, 1.574803149606291974 ) ) ;
#50730=VERTEX_POINT ( 'NONE', #20794 ) ;
#50731=VERTEX_POINT ( 'NONE', #36551 ) ;
#50732=ORIENTED_EDGE ( 'NONE', *, *, #48775, .F. ) ;
#50733=CARTESIAN_POINT ( 'NONE',  ( 1.015142113812069313, 0.000000000000000000, 0.7874015748031454320 ) ) ;
#50734=ORIENTED_EDGE ( 'NONE', *, *, #42795, .T. ) ;
#50738=ORIENTED_EDGE ( 'NONE', *, *, #1309, .F. ) ;
#50741=EDGE_LOOP ( 'NONE', ( #1233, #26026, #17552, #22401 ) ) ;
#50742=DIRECTION ( 'NONE',  ( 0.000000000000000000, 0.000000000000000000, -1.000000000000000000 ) ) ;
#50743=VECTOR ( 'NONE', #6010, 39.37007874015748143 ) ;
#50744=VERTEX_POINT ( 'NONE', #6584 ) ;
#50746=VECTOR ( 'NONE', #32179, 39.37007874015748143 ) ;
#50748=DIRECTION ( 'NONE',  ( 0.000000000000000000, 0.000000000000000000, -1.000000000000000000 ) ) ;
#50749=ORIENTED_EDGE ( 'NONE', *, *, #21500, .F. ) ;
#50750=EDGE_CURVE ( 'NONE', #34200, #36526, #38078, .T. ) ;
#50751=AXIS2_PLACEMENT_3D ( 'NONE', #25096, #21226, #20967 ) ;
#50752=DIRECTION ( 'NONE',  ( -0.000000000000000000, 1.000000000000000000, -0.000000000000000000 ) ) ;
#50753=VECTOR ( 'NONE', #41527, 39.37007874015748143 ) ;
#50755=ORIENTED_EDGE ( 'NONE', *, *, #20041, .T. ) ;
#50756=DIRECTION ( 'NONE',  ( 0.000000000000000000, 0.000000000000000000, 1.000000000000000000 ) ) ;
#50757=CIRCLE ( 'NONE', #40927, 2.165354330708661568 ) ;
#50759=ORIENTED_EDGE ( 'NONE', *, *, #21251, .T. ) ;
#50762=CARTESIAN_POINT ( 'NONE',  ( 0.000000000000000000, 3.267716535433071279, -1.102362204724405714 ) ) ;
#50763=DIRECTION ( 'NONE',  ( 1.000000000000000000, -0.000000000000000000, 0.000000000000000000 ) ) ;
#50765=ORIENTED_EDGE ( 'NONE', *, *, #22087, .F. ) ;
#50766=ORIENTED_EDGE ( 'NONE', *, *, #41135, .F. ) ;
#50768=CARTESIAN_POINT ( 'NONE',  ( 0.7423782071083085965, 3.267716535433071279, 0.4330708661417287386 ) ) ;
#50770=CARTESIAN_POINT ( 'NONE',  ( -1.195183497228115035E-16, 0.000000000000000000, -1.574803149606293529 ) ) ;
#50771=DIRECTION ( 'NONE',  ( 1.734723475976806848E-16, -0.000000000000000000, 1.000000000000000000 ) ) ;
#50772=LINE ( 'NONE', #30467, #33068 ) ;
#50774=CIRCLE ( 'NONE', #31875, 2.106299212598425008 ) ;
#50776=EDGE_CURVE ( 'NONE', #27786, #15713, #13562, .T. ) ;
#50779=CARTESIAN_POINT ( 'NONE',  ( 1.909347346926324684, 3.346456692913386100, 1.102362204724403938 ) ) ;
#50781=VECTOR ( 'NONE', #34964, 39.37007874015748143 ) ;
#50782=ORIENTED_EDGE ( 'NONE', *, *, #50062, .T. ) ;
#50783=ADVANCED_FACE ( 'NONE', ( #22327 ), #25941, .F. ) ;
#50788=VECTOR ( 'NONE', #3646, 39.37007874015748143 ) ;
#50789=VERTEX_POINT ( 'NONE', #37322 ) ;
#50790=ADVANCED_FACE ( 'NONE', ( #25681 ), #41436, .F. ) ;
#50791=VECTOR ( 'NONE', #41922, 39.37007874015748143 ) ;
#50793=ORIENTED_EDGE ( 'NONE', *, *, #44421, .F. ) ;
#50797=LINE ( 'NONE', #35116, #40445 ) ;
#50798=EDGE_CURVE ( 'NONE', #39562, #16142, #29994, .T. ) ;
#50799=ORIENTED_EDGE ( 'NONE', *, *, #41995, .T. ) ;
#50800=CARTESIAN_POINT ( 'NONE',  ( 0.000000000000000000, 3.267716535433071279, -1.889763779527552146 ) ) ;
#50802=ORIENTED_EDGE ( 'NONE', *, *, #295, .T. ) ;
#50808=LINE ( 'NONE', #23497, #6414 ) ;
#50812=ORIENTED_EDGE ( 'NONE', *, *, #48546, .T. ) ;
#50814=AXIS2_PLACEMENT_3D ( 'NONE', #31663, #36050, #32440 ) ;
#50816=VERTEX_POINT ( 'NONE', #34203 ) ;
#50818=EDGE_CURVE ( 'NONE', #12211, #29226, #12702, .T. ) ;
#50822=LINE ( 'NONE', #19882, #40994 ) ;
#50823=CARTESIAN_POINT ( 'NONE',  ( 1.560669927219590525, 3.267716535433071279, -0.9842519685039348154 ) ) ;
#50824=VERTEX_POINT ( 'NONE', #17687 ) ;
#50826=CARTESIAN_POINT ( 'NONE',  ( -1.091055626815042645, 3.346456692913386100, 1.692913385826762873 ) ) ;
#50827=VECTOR ( 'NONE', #16747, 39.37007874015748143 ) ;
#50829=FACE_OUTER_BOUND ( 'NONE', #35267, .T. ) ;
#50830=LINE ( 'NONE', #28151, #21047 ) ;
#50832=CARTESIAN_POINT ( 'NONE',  ( -1.195183497228115035E-16, 0.000000000000000000, 0.6299212598425161236 ) ) ;
#50833=CARTESIAN_POINT ( 'NONE',  ( -0.8182917201112814842, 3.346456692913386100, 0.7874015748031456541 ) ) ;
#50836=ADVANCED_FACE ( 'NONE', ( #33195 ), #49139, .F. ) ;
#50837=ORIENTED_EDGE ( 'NONE', *, *, #26092, .T. ) ;
#50839=VERTEX_POINT ( 'NONE', #9944 ) ;
#50840=CARTESIAN_POINT ( 'NONE',  ( 0.8182917201112817063, 3.346456692913386100, -2.244094488188969283 ) ) ;
#50841=CARTESIAN_POINT ( 'NONE',  ( -1.439733046521776361, 0.000000000000000000, 0.4330708661417290162 ) ) ;
#50842=DIRECTION ( 'NONE',  ( -3.469446951953613696E-16, 0.000000000000000000, -1.000000000000000000 ) ) ;
#50843=ADVANCED_FACE ( 'NONE', ( #21817 ), #2197, .F. ) ;
#50845=EDGE_LOOP ( 'NONE', ( #24558, #16063, #37473, #10062 ) ) ;
#50848=EDGE_LOOP ( 'NONE', ( #20992, #44743, #7883, #3624 ) ) ;
#50849=CARTESIAN_POINT ( 'NONE',  ( -0.2727639067037608278, 3.346456692913386100, -0.03937007874015908959 ) ) ;
#50851=ORIENTED_EDGE ( 'NONE', *, *, #8243, .T. ) ;
#50852=CARTESIAN_POINT ( 'NONE',  ( -0.3486774197067339376, 0.000000000000000000, -1.259842519685035134 ) ) ;
#50853=ORIENTED_EDGE ( 'NONE', *, *, #35534, .T. ) ;
#50855=CARTESIAN_POINT ( 'NONE',  ( -0.07591351300297333182, 0.000000000000000000, 0.4724409448818869817 ) ) ;
#50856=CARTESIAN_POINT ( 'NONE',  ( 0.000000000000000000, 3.267716535433071279, 0.000000000000000000 ) ) ;
#50857=EDGE_CURVE ( 'NONE', #10410, #22692, #3454, .T. ) ;
#50858=ORIENTED_EDGE ( 'NONE', *, *, #25989, .T. ) ;
#50860=ORIENTED_EDGE ( 'NONE', *, *, #34925, .T. ) ;
#50862=CARTESIAN_POINT ( 'NONE',  ( -0.5455278134075213226, 3.267716535433071279, 9.463399047163221947E-17 ) ) ;
#50863=VERTEX_POINT ( 'NONE', #7337 ) ;
#50864=ORIENTED_EDGE ( 'NONE', *, *, #45196, .T. ) ;
#50865=EDGE_CURVE ( 'NONE', #6703, #5399, #10952, .T. ) ;
#50869=AXIS2_PLACEMENT_3D ( 'NONE', #46308, #14591, #42454 ) ;
#50870=ORIENTED_EDGE ( 'NONE', *, *, #12547, .T. ) ;
#50871=ORIENTED_EDGE ( 'NONE', *, *, #29359, .F. ) ;
#50874=EDGE_CURVE ( 'NONE', #43110, #6435, #31082, .T. ) ;
#50875=CARTESIAN_POINT ( 'NONE',  ( 1.636583440222563857, 3.346456692913386100, 1.417869535855831975 ) ) ;
#50878=DIRECTION ( 'NONE',  ( 1.734723475976806848E-16, -0.000000000000000000, 1.000000000000000000 ) ) ;
#50879=DIRECTION ( 'NONE',  ( 1.000000000000000000, 0.000000000000000000, -3.469446951953613696E-16 ) ) ;
#50881=PLANE ( 'NONE',  #35667 ) ;
#50882=ORIENTED_EDGE ( 'NONE', *, *, #11633, .T. ) ;
#50883=EDGE_LOOP ( 'NONE', ( #22248, #22387, #50712, #47438 ) ) ;
#50885=DIRECTION ( 'NONE',  ( -0.000000000000000000, 1.000000000000000000, -0.000000000000000000 ) ) ;
#50886=EDGE_CURVE ( 'NONE', #30308, #13787, #7582, .T. ) ;
#50887=CARTESIAN_POINT ( 'NONE',  ( 0.000000000000000000, 3.267716535433071279, -1.574803149606293529 ) ) ;
#50889=AXIS2_PLACEMENT_3D ( 'NONE', #18795, #6667, #22668 ) ;
#50890=CARTESIAN_POINT ( 'NONE',  ( 1.909347346926324684, 3.267716535433071279, 0.2755905511810994302 ) ) ;
#50891=DIRECTION ( 'NONE',  ( -0.000000000000000000, 1.000000000000000000, -0.000000000000000000 ) ) ;
#50896=ORIENTED_EDGE ( 'NONE', *, *, #27981, .F. ) ;
#50897=CARTESIAN_POINT ( 'NONE',  ( 0.4696143004045484903, 0.000000000000000000, 2.047244094488179567 ) ) ;
#50898=CARTESIAN_POINT ( 'NONE',  ( 0.5455278134075211005, 3.346456692913386100, -0.1968503937007880511 ) ) ;
#50902=DIRECTION ( 'NONE',  ( -3.469446951953613696E-16, 0.000000000000000000, -1.000000000000000000 ) ) ;
#50903=CARTESIAN_POINT ( 'NONE',  ( 0.000000000000000000, 3.267716535433071279, 2.362204724409437961 ) ) ;
#50904=ORIENTED_EDGE ( 'NONE', *, *, #8723, .T. ) ;
#50905=CARTESIAN_POINT ( 'NONE',  ( -1.363819533518803029, 3.346456692913386100, 0.2755905511810996522 ) ) ;
#50906=CIRCLE ( 'NONE', #36982, 2.106299212598425008 ) ;
#50907=CARTESIAN_POINT ( 'NONE',  ( -1.636583440222564301, 0.000000000000000000, -0.6299212598425177889 ) ) ;
#50908=EDGE_CURVE ( 'NONE', #35067, #552, #11457, .T. ) ;
#50909=VERTEX_POINT ( 'NONE', #26439 ) ;
#50911=CARTESIAN_POINT ( 'NONE',  ( 0.5455278134075212115, 0.000000000000000000, -0.6299212598425181220 ) ) ;
#50912=CARTESIAN_POINT ( 'NONE',  ( 4.268512490100411402E-16, 0.000000000000000000, 1.259842519685033357 ) ) ;
#50913=ORIENTED_EDGE ( 'NONE', *, *, #5648, .F. ) ;
#50914=PLANE ( 'NONE',  #40774 ) ;
#50915=DIRECTION ( 'NONE',  ( -3.469446951953613696E-16, 0.000000000000000000, -1.000000000000000000 ) ) ;
#50917=CARTESIAN_POINT ( 'NONE',  ( 2.106197740627111514, 0.000000000000000000, -0.7874015748031473194 ) ) ;
#50918=EDGE_LOOP ( 'NONE', ( #46907, #13590, #40383, #33451 ) ) ;
#50919=DIRECTION ( 'NONE',  ( 1.000000000000000000, 0.000000000000000000, -3.469446951953613696E-16 ) ) ;
#50920=EDGE_LOOP ( 'NONE', ( #4320, #69, #48359, #6514 ) ) ;
#50922=LINE ( 'NONE', #30866, #35048 ) ;
#50923=PLANE ( 'NONE',  #37581 ) ;
#50924=VECTOR ( 'NONE', #27038, 39.37007874015748143 ) ;
#50926=ORIENTED_EDGE ( 'NONE', *, *, #45646, .F. ) ;
#50927=DIRECTION ( 'NONE',  ( 1.000000000000000000, 0.000000000000000000, 0.000000000000000000 ) ) ;
#50929=ORIENTED_EDGE ( 'NONE', *, *, #26066, .T. ) ;
#50930=FACE_OUTER_BOUND ( 'NONE', #2292, .T. ) ;
#50931=VECTOR ( 'NONE', #35617, 39.37007874015748143 ) ;
#50932=CARTESIAN_POINT ( 'NONE',  ( -1.363819533518803251, 3.267716535433071279, 2.365849761790805487E-16 ) ) ;
#50933=CARTESIAN_POINT ( 'NONE',  ( 0.4696143004045476577, 3.267716535433071279, -1.629301903132386767E-16 ) ) ;
#50934=CARTESIAN_POINT ( 'NONE',  ( 0.000000000000000000, 3.267716535433071279, -1.259842519685035134 ) ) ;
#50936=AXIS2_PLACEMENT_3D ( 'NONE', #43857, #11362, #27096 ) ;
#50938=ORIENTED_EDGE ( 'NONE', *, *, #49711, .T. ) ;
#50939=CARTESIAN_POINT ( 'NONE',  ( 3.927031490892378253E-16, 0.000000000000000000, 2.007874015748021268 ) ) ;
#50941=VECTOR ( 'NONE', #9238, 39.37007874015748143 ) ;
#50942=CARTESIAN_POINT ( 'NONE',  ( -1.195183497228115035E-16, 0.000000000000000000, 0.3149606299212576177 ) ) ;
#50943=ORIENTED_EDGE ( 'NONE', *, *, #24129, .T. ) ;
#50944=DIRECTION ( 'NONE',  ( -0.000000000000000000, 1.000000000000000000, -0.000000000000000000 ) ) ;
#50947=VECTOR ( 'NONE', #4057, 39.37007874015748143 ) ;
#50948=CARTESIAN_POINT ( 'NONE',  ( 0.5455278134075211005, 0.000000000000000000, -0.5118110236220467790 ) ) ;
#50952=EDGE_CURVE ( 'NONE', #35538, #20069, #47030, .T. ) ;
#50953=ORIENTED_EDGE ( 'NONE', *, *, #25389, .T. ) ;
#50954=VERTEX_POINT ( 'NONE', #30322 ) ;
#50959=FACE_OUTER_BOUND ( 'NONE', #21178, .T. ) ;
#50960=VECTOR ( 'NONE', #46826, 39.37007874015748143 ) ;
#50961=DIRECTION ( 'NONE',  ( 1.734723475976806848E-16, 0.000000000000000000, 1.000000000000000000 ) ) ;
#50962=EDGE_CURVE ( 'NONE', #1213, #17158, #42185, .T. ) ;
#50963=CARTESIAN_POINT ( 'NONE',  ( -0.5455278134075214336, 3.346456692913386100, 2.204724409448808764 ) ) ;
#50964=LINE ( 'NONE', #47106, #11320 ) ;
#50967=LINE ( 'NONE', #12043, #28467 ) ;
#50968=PLANE ( 'NONE',  #38871 ) ;
#50970=AXIS2_PLACEMENT_3D ( 'NONE', #46028, #33937, #45516 ) ;
#50971=AXIS2_PLACEMENT_3D ( 'NONE', #858, #24861, #8346 ) ;
#50972=ORIENTED_EDGE ( 'NONE', *, *, #34992, .T. ) ;
#50973=CARTESIAN_POINT ( 'NONE',  ( -0.8182917201112819283, 3.346456692913386100, -2.244094488188968395 ) ) ;
#50974=CARTESIAN_POINT ( 'NONE',  ( -0.07591351300297366489, 0.000000000000000000, -2.244094488188968395 ) ) ;
#50977=PLANE ( 'NONE',  #48167 ) ;
#50980=DIRECTION ( 'NONE',  ( -3.469446951953613696E-16, 0.000000000000000000, -1.000000000000000000 ) ) ;
#50983=PLANE ( 'NONE',  #25904 ) ;
#50985=CARTESIAN_POINT ( 'NONE',  ( 0.2727639067037602172, 3.346456692913386100, -2.148105963102950877 ) ) ;
#50986=ORIENTED_EDGE ( 'NONE', *, *, #38910, .F. ) ;
#50987=ORIENTED_EDGE ( 'NONE', *, *, #14541, .T. ) ;
#50989=CARTESIAN_POINT ( 'NONE',  ( -0.3486774197067343262, 3.346456692913386100, -2.401574803149598036 ) ) ;
#50991=CARTESIAN_POINT ( 'NONE',  ( -1.166969139818015755, 3.267716535433071279, 0.2755905511810996522 ) ) ;
#50995=CARTESIAN_POINT ( 'NONE',  ( 1.287906020515829919, 3.249608194809333384, -2.086614173228340086 ) ) ;
#50996=VECTOR ( 'NONE', #9085, 39.37007874015748143 ) ;
#50997=EDGE_LOOP ( 'NONE', ( #49998, #32164, #24441, #36789 ) ) ;
#50999=LINE ( 'NONE', #47142, #5857 ) ;
#51000=VERTEX_POINT ( 'NONE', #34454 ) ;
#51001=ORIENTED_EDGE ( 'NONE', *, *, #20623, .F. ) ;
#51002=LINE ( 'NONE', #20061, #42990 ) ;
#51005=DIRECTION ( 'NONE',  ( -3.469446951953613696E-16, 0.000000000000000000, -1.000000000000000000 ) ) ;
#51008=VERTEX_POINT ( 'NONE', #16348 ) ;
#51010=DIRECTION ( 'NONE',  ( 1.000000000000000000, 0.000000000000000000, -3.469446951953613696E-16 ) ) ;
#51011=EDGE_CURVE ( 'NONE', #8694, #8821, #24604, .T. ) ;
#51013=ORIENTED_EDGE ( 'NONE', *, *, #37802, .T. ) ;
#51015=CARTESIAN_POINT ( 'NONE',  ( -1.091055626815042645, 0.000000000000000000, -1.771653543307081025 ) ) ;
#51017=LINE ( 'NONE', #50762, #39229 ) ;
#51019=LINE ( 'NONE', #7965, #11018 ) ;
#51020=PLANE ( 'NONE',  #48597 ) ;
#51021=EDGE_LOOP ( 'NONE', ( #31507, #22941, #13329, #26946 ) ) ;
#51023=CARTESIAN_POINT ( 'NONE',  ( 1.560669927219590525, 3.267716535433071279, -5.414661521997676285E-16 ) ) ;
#51025=CARTESIAN_POINT ( 'NONE',  ( 0.000000000000000000, 3.267716535433071279, 1.102362204724403938 ) ) ;
#51027=LINE ( 'NONE', #7468, #32622 ) ;
#51029=ADVANCED_FACE ( 'NONE', ( #28459 ), #47287, .F. ) ;
#51030=FACE_OUTER_BOUND ( 'NONE', #40105, .T. ) ;
#51032=ORIENTED_EDGE ( 'NONE', *, *, #36353, .T. ) ;
#51034=LINE ( 'NONE', #3345, #38307 ) ;
#51036=ORIENTED_EDGE ( 'NONE', *, *, #39495, .F. ) ;
#51037=FACE_OUTER_BOUND ( 'NONE', #29112, .T. ) ;
#51038=EDGE_CURVE ( 'NONE', #29676, #18300, #11958, .T. ) ;
#51039=EDGE_CURVE ( 'NONE', #47349, #22389, #27956, .T. ) ;
#51040=ORIENTED_EDGE ( 'NONE', *, *, #3458, .F. ) ;
#51044=EDGE_LOOP ( 'NONE', ( #11163, #4568, #45944, #24877 ) ) ;
#51045=CARTESIAN_POINT ( 'NONE',  ( 1.015142113812069091, 3.346456692913386100, -1.732283464566923614 ) ) ;
#51047=FACE_OUTER_BOUND ( 'NONE', #7309, .T. ) ;
#51048=VECTOR ( 'NONE', #18614, 39.37007874015748143 ) ;
#51049=ORIENTED_EDGE ( 'NONE', *, *, #49361, .F. ) ;
#51051=CARTESIAN_POINT ( 'NONE',  ( -0.9302092402134559679, 3.346456692913386100, 1.889763779527550147 ) ) ;
#51053=CARTESIAN_POINT ( 'NONE',  ( -1.636583440222564301, 3.267716535433071279, 1.417869535855831753 ) ) ;
#51067=COLOUR_RGB('Light Blue',0.38,0.62,0.78);
#51068=FILL_AREA_STYLE_COLOUR('',#51067);
#51069=FILL_AREA_STYLE('',(#51068));
#51070=SURFACE_STYLE_FILL_AREA(#51069);
#51071=SURFACE_SIDE_STYLE('',(#51070));
#51072=SURFACE_STYLE_USAGE(.BOTH.,#51071);
#51073=PRESENTATION_STYLE_ASSIGNMENT((#51072));
ENDSEC;
END-ISO-10303-21;
